ISO-10303-21;
HEADER;
FILE_DESCRIPTION (('STEP AP214'),
    '1' );
FILE_NAME ('Barrel Adjuster Screw.step',
    '2026-10-30T09:41:00',
    ( '' ),
    ( '' ),
    'SwSTEP 2.0',
    'SolidWorks 2020',
    '' );
FILE_SCHEMA (( 'AUTOMOTIVE_DESIGN' ));
ENDSEC;

DATA;
#4=CARTESIAN_POINT ( 'NONE',  ( 113.1933481442453058, -4.089484607189486809, -7.948022111789456723 ) ) ;
#5=CARTESIAN_POINT ( 'NONE',  ( 112.6260814775786514, -9.261995988541697145, -16.69588392320189030 ) ) ;
#6=CARTESIAN_POINT ( 'NONE',  ( 122.0994348109119443, 0.9020085738987339008, -11.91225656197089222 ) ) ;
#7=CARTESIAN_POINT ( 'NONE',  ( 116.4267681442453153, -6.222761293078241884, -8.102969835052219238 ) ) ;
#9=CARTESIAN_POINT ( 'NONE',  ( 120.6245414775786458, -9.988377603198976828, -10.36322818467138340 ) ) ;
#11=CARTESIAN_POINT ( 'NONE',  ( 121.3619881442452879, -5.574606645277164318, -18.38911715685844683 ) ) ;
#12=ORIENTED_EDGE ( 'NONE', *, *, #37026, .T. ) ;
#15=CARTESIAN_POINT ( 'NONE',  ( 117.5613014775786525, 0.9020085738987339008, -11.91225656197089222 ) ) ;
#19=CARTESIAN_POINT ( 'NONE',  ( 137.1799701741921922, -1.245005990108144500, -9.487437202584745322 ) ) ;
#20=CARTESIAN_POINT ( 'NONE',  ( 121.4754414775786131, -8.166667518702819706, -8.995218007635861213 ) ) ;
#22=CARTESIAN_POINT ( 'NONE',  ( 119.6034614775786196, -3.505236298600246325, -18.68346056562440793 ) ) ;
#25=CARTESIAN_POINT ( 'NONE',  ( 115.3489614775786407, -9.261995988541697145, -16.69588392320189030 ) ) ;
#31=CARTESIAN_POINT ( 'NONE',  ( 121.5321681442453183, -9.988377603198976828, -10.36322818467138340 ) ) ;
#34=CARTESIAN_POINT ( 'NONE',  ( 122.3830681442452857, -8.166667518702819706, -8.995218007635861213 ) ) ;
#35=CARTESIAN_POINT ( 'NONE',  ( 120.3409081442453044, -0.4660016031367893996, -10.09054647747474043 ) ) ;
#36=CARTESIAN_POINT ( 'NONE',  ( 118.7525614775786380, -1.833838273342659253, -17.42832698103878286 ) ) ;
#37=CARTESIAN_POINT ( 'NONE',  ( 121.2485348109119769, -8.899110576539710493, -16.42337572283490132 ) ) ;
#39=CARTESIAN_POINT ( 'NONE',  ( 114.9518748109119883, -1.834011780172310813, -8.268836392978581529 ) ) ;
#45=CARTESIAN_POINT ( 'NONE',  ( 125.3895814775786448, -7.893985811506177619, -18.51759400769804742 ) ) ;
#46=CARTESIAN_POINT ( 'NONE',  ( 125.5597614775786326, -7.894159318335828068, -9.358103419637847864 ) ) ;
#48=CARTESIAN_POINT ( 'NONE',  ( 125.2761281442453054, -10.63000616557722466, -14.87417383870573495 ) ) ;
#52=CARTESIAN_POINT ( 'NONE',  ( 122.7234281442452755, -5.638512984488999180, -18.83840828888717311 ) ) ;
#53=CARTESIAN_POINT ( 'NONE',  ( 125.8433948109119456, -1.834011780172310813, -8.268836392978581529 ) ) ;
#54=CARTESIAN_POINT ( 'NONE',  ( 111.7184548109119788, -9.261995988541697145, -16.69588392320189030 ) ) ;
#60=CARTESIAN_POINT ( 'NONE',  ( 116.8238548109119819, -5.574606645277164318, -18.38911715685844683 ) ) ;
#61=CARTESIAN_POINT ( 'NONE',  ( 112.6260814775786514, -9.261995988541697145, -16.69588392320189030 ) ) ;
#65=CARTESIAN_POINT ( 'NONE',  ( 120.9081748109119872, -4.153390946401325223, -8.397313243818185668 ) ) ;
#66=CARTESIAN_POINT ( 'NONE',  ( 115.1787814775786387, -0.1624402480850797581, -16.17319339645315424 ) ) ;
#67=CARTESIAN_POINT ( 'NONE',  ( 112.1155414775786454, -10.15424416112533912, -14.75197769757731336 ) ) ;
#71=CARTESIAN_POINT ( 'NONE',  ( 112.3991748109119868, -1.833838273342658809, -17.42832698103878286 ) ) ;
#73=CARTESIAN_POINT ( 'NONE',  ( 126.4750299824193007, -9.298013242772034559, -15.96981777986906970 ) ) ;
#77=CARTESIAN_POINT ( 'NONE',  ( 116.8238548109119819, -5.574606645277164318, -18.38911715685844683 ) ) ;
#78=CARTESIAN_POINT ( 'NONE',  ( 113.1933481442453058, -5.574606645277164318, -18.38911715685844683 ) ) ;
#79=CARTESIAN_POINT ( 'NONE',  ( 112.8721930757767495, -0.9924539043446216624, -17.29976612834909133 ) ) ;
#86=B_SPLINE_CURVE_WITH_KNOTS ( 'NONE', 3,
 ( #37430, #6200, #27183, #20122 ),
 .UNSPECIFIED., .F., .F.,
 ( 4, 4 ),
 ( 7.175310251266321521E-15, 2.533189092146110195E-06 ),
 .UNSPECIFIED. ) ;
#89=CARTESIAN_POINT ( 'NONE',  ( 124.5954081442453116, -6.222761293078241884, -8.102969835052219238 ) ) ;
#90=CARTESIAN_POINT ( 'NONE',  ( 116.8805814775786445, -3.505236298600246325, -18.68346056562440793 ) ) ;
#94=CARTESIAN_POINT ( 'NONE',  ( 117.0507614775786465, 0.1319031606808879209, -14.10382304977623669 ) ) ;
#97=CARTESIAN_POINT ( 'NONE',  ( 125.5030348109119558, -3.383040157471821630, -19.15922257007629170 ) ) ;
#99=CARTESIAN_POINT ( 'NONE',  ( 113.5337081442453240, -9.261995988541697145, -16.69588392320189030 ) ) ;
#101=CARTESIAN_POINT ( 'NONE',  ( 112.7962614775786676, -3.383040157471821630, -19.15922257007629170 ) ) ;
#102=CARTESIAN_POINT ( 'NONE',  ( 114.4980614775786592, -7.893985811506184724, -18.51759400769803676 ) ) ;
#104=CARTESIAN_POINT ( 'NONE',  ( 112.3424481442453384, -6.344957434206662583, -7.627207830600332805 ) ) ;
#105=CARTESIAN_POINT ( 'NONE',  ( 114.4980614775786592, -7.893985811506177619, -18.51759400769804742 ) ) ;
#106=CARTESIAN_POINT ( 'NONE',  ( 124.3685014775786328, 0.4262465694468514643, -12.03445270309931736 ) ) ;
#112=CARTESIAN_POINT ( 'NONE',  ( 117.9583881442453048, 0.1319031606808879209, -14.10382304977623669 ) ) ;
#116=CARTESIAN_POINT ( 'NONE',  ( 128.2184548109119930, -5.622599431619523358, -7.441364641445410655 ) ) ;
#117=CARTESIAN_POINT ( 'NONE',  ( 124.1983214775786166, -8.166667518702819706, -8.995218007635861213 ) ) ;
#119=CARTESIAN_POINT ( 'NONE',  ( 121.5888948109119809, -10.30919188438810075, -12.61870101168855918 ) ) ;
#120=CARTESIAN_POINT ( 'NONE',  ( 117.9583881442453048, -10.30919188438810075, -12.61870101168855918 ) ) ;
#122=CARTESIAN_POINT ( 'NONE',  ( 115.6325948109119821, -9.565557343593413364, -10.61323700422348004 ) ) ;
#124=CARTESIAN_POINT ( 'NONE',  ( 122.0427081442452817, 0.5811942927096110934, -14.16772938898807510 ) ) ;
#125=CARTESIAN_POINT ( 'NONE',  ( 118.4689281442453392, 0.9020085738987339008, -11.91225656197089222 ) ) ;
#127=CARTESIAN_POINT ( 'NONE',  ( 115.7460481442453357, -10.15424416112533912, -14.75197769757731336 ) ) ;
#129=CARTESIAN_POINT ( 'NONE',  ( 120.0572748109119772, -6.222761293078241884, -8.102969835052219238 ) ) ;
#130=CARTESIAN_POINT ( 'NONE',  ( 115.0086014775786509, -4.089484607189486809, -7.948022111789456723 ) ) ;
#131=CARTESIAN_POINT ( 'NONE',  ( 137.2359773051214802, 0.4104479539111648978, -13.25635893580179925 ) ) ;
#137=CARTESIAN_POINT ( 'NONE',  ( 114.9518748109119883, -1.834011780172310813, -8.268836392978581529 ) ) ;
#143=CARTESIAN_POINT ( 'NONE',  ( 116.9373081442452929, -8.166667518702817929, -8.995218007635861213 ) ) ;
#145=CARTESIAN_POINT ( 'NONE',  ( 111.8528364273310274, -2.236191541394347837, -18.14152338500401385 ) ) ;
#146=CARTESIAN_POINT ( 'NONE',  ( 118.4689281442453250, 0.9020085738987385637, -11.91225656197091887 ) ) ;
#147=CARTESIAN_POINT ( 'NONE',  ( 125.0492214775786266, -3.505236298600246325, -18.68346056562440793 ) ) ;
#149=CARTESIAN_POINT ( 'NONE',  ( 136.0320772899156339, -9.514942969284794216, -9.745064694461806454 ) ) ;
#150=CARTESIAN_POINT ( 'NONE',  ( 124.4252281442452812, -9.261995988541697145, -16.69588392320189030 ) ) ;
#151=CARTESIAN_POINT ( 'NONE',  ( 125.9568481442452850, -6.344957434206665248, -7.627207830600338134 ) ) ;
#152=CARTESIAN_POINT ( 'NONE',  ( 115.2355081442453155, 0.1319031606808879209, -14.10382304977623669 ) ) ;
#153=CARTESIAN_POINT ( 'NONE',  ( 112.3424481442453384, -3.505236298600246325, -18.68346056562440793 ) ) ;
#156=CARTESIAN_POINT ( 'NONE',  ( 119.1496481442453046, -6.222761293078241884, -8.102969835052219238 ) ) ;
#157=CARTESIAN_POINT ( 'NONE',  ( 120.1707281442453166, -9.565557343593413364, -10.61323700422348004 ) ) ;
#162=CARTESIAN_POINT ( 'NONE',  ( 114.1577014775786552, -6.344957434206662583, -7.627207830600332805 ) ) ;
#163=CARTESIAN_POINT ( 'NONE',  ( 113.3068014775786594, -8.166667518702817929, -8.995218007635859436 ) ) ;
#168=CARTESIAN_POINT ( 'NONE',  ( 123.3474214775786209, -9.988377603198976828, -10.36322818467138340 ) ) ;
#170=CARTESIAN_POINT ( 'NONE',  ( 112.3991748109119868, -8.166667518702817929, -8.995218007635859436 ) ) ;
#171=CARTESIAN_POINT ( 'NONE',  ( 119.2063748109119814, -7.894159318335828068, -9.358103419637847864 ) ) ;
#172=CARTESIAN_POINT ( 'NONE',  ( 124.9357681442453014, -1.834011780172310813, -8.268836392978581529 ) ) ;
#173=CARTESIAN_POINT ( 'NONE',  ( 116.7104014775786425, -0.4660016031367893996, -10.09054647747474043 ) ) ;
#176=CARTESIAN_POINT ( 'NONE',  ( 111.6050014775786536, 0.1319031606808879209, -14.10382304977623669 ) ) ;
#178=CARTESIAN_POINT ( 'NONE',  ( 121.7023481442452777, -9.261995988541697145, -16.69588392320189030 ) ) ;
#181=CARTESIAN_POINT ( 'NONE',  ( 114.2711548109119803, -9.988377603198976828, -10.36322818467138340 ) ) ;
#184=CARTESIAN_POINT ( 'NONE',  ( 124.0848681442452772, -4.089484607189486809, -7.948022111789456723 ) ) ;
#186=CARTESIAN_POINT ( 'NONE',  ( 112.5693548109119888, 0.4262465694468514643, -12.03445270309931736 ) ) ;
#189=CARTESIAN_POINT ( 'NONE',  ( 119.4332814775786318, -8.899110576539710493, -16.42337572283490132 ) ) ;
#190=CARTESIAN_POINT ( 'NONE',  ( 121.0408330757767459, -0.9924539043446216624, -17.29976612834909133 ) ) ;
#192=CARTESIAN_POINT ( 'NONE',  ( 120.7947214775786193, -0.8288870151387760510, -10.36305467784173118 ) ) ;
#195=CARTESIAN_POINT ( 'NONE',  ( 119.4332814775786318, -8.899110576539710493, -16.42337572283490132 ) ) ;
#197=CARTESIAN_POINT ( 'NONE',  ( 115.0653281442453277, -6.344957434206662583, -7.627207830600332805 ) ) ;
#198=CARTESIAN_POINT ( 'NONE',  ( 123.3474214775786351, -9.988377603198957289, -10.36322818467135498 ) ) ;
#199=CARTESIAN_POINT ( 'NONE',  ( 117.8449348109119938, -1.833838273342659253, -17.42832698103878286 ) ) ;
#201=CARTESIAN_POINT ( 'NONE',  ( 116.8805814775786445, -6.344957434206662583, -7.627207830600332805 ) ) ;
#205=AXIS2_PLACEMENT_3D ( 'NONE', #1914, #29739, #9001 ) ;
#207=CARTESIAN_POINT ( 'NONE',  ( 127.7184548109119788, -4.683672500039348208, -14.88233656108870662 ) ) ;
#208=CARTESIAN_POINT ( 'NONE',  ( 121.2485348109119769, -0.4660016031367893996, -10.09054647747474043 ) ) ;
#211=CARTESIAN_POINT ( 'NONE',  ( 118.0151148109119816, 0.4262465694468514643, -12.03445270309931736 ) ) ;
#220=CARTESIAN_POINT ( 'NONE',  ( 113.4769814775786330, -10.63000616557722466, -14.87417383870573495 ) ) ;
#221=CARTESIAN_POINT ( 'NONE',  ( 124.5386814775786206, -4.153390946401325223, -8.397313243818185668 ) ) ;
#222=CARTESIAN_POINT ( 'NONE',  ( 124.3685014775786328, -10.63000616557722466, -14.87417383870573495 ) ) ;
#223=CARTESIAN_POINT ( 'NONE',  ( 115.6893214775786447, -9.859900752359374465, -12.68260735090039404 ) ) ;
#225=CARTESIAN_POINT ( 'NONE',  ( 118.6391081442452986, -4.089484607189486809, -7.948022111789456723 ) ) ;
#228=CARTESIAN_POINT ( 'NONE',  ( 122.8936081442453059, -9.565557343593413364, -10.61323700422348004 ) ) ;
#233=CARTESIAN_POINT ( 'NONE',  ( 116.8805814775786445, -6.344957434206662583, -7.627207830600332805 ) ) ;
#234=CARTESIAN_POINT ( 'NONE',  ( 136.3514896075913327, -8.489760904479810577, -17.93711134556155784 ) ) ;
#240=CARTESIAN_POINT ( 'NONE',  ( 123.4608748109119745, -10.63000616557722466, -14.87417383870573495 ) ) ;
#243=CARTESIAN_POINT ( 'NONE',  ( 121.4187148109119789, -3.505236298600246325, -18.68346056562440793 ) ) ;
#247=CARTESIAN_POINT ( 'NONE',  ( 113.6471614775786492, -5.638512984488999180, -18.83840828888717311 ) ) ;
#248=CARTESIAN_POINT ( 'NONE',  ( 123.6310548109119765, -4.153390946401325223, -8.397313243818185668 ) ) ;
#249=CARTESIAN_POINT ( 'NONE',  ( 112.7938987682628067, -1.040089454026971172, -17.23633227186634187 ) ) ;
#250=CARTESIAN_POINT ( 'NONE',  ( 121.7023481442452777, -9.261995988541697145, -16.69588392320189030 ) ) ;
#253=CARTESIAN_POINT ( 'NONE',  ( 122.2696148109119889, -4.089484607189486809, -7.948022111789456723 ) ) ;
#254=CARTESIAN_POINT ( 'NONE',  ( 120.7947214775786193, -9.261995988541697145, -16.69588392320189030 ) ) ;
#255=CARTESIAN_POINT ( 'NONE',  ( 123.2339681442453241, -3.505236298600246325, -18.68346056562440793 ) ) ;
#256=CARTESIAN_POINT ( 'NONE',  ( 118.8092881442453290, -0.1624402480850797581, -16.17319339645315424 ) ) ;
#258=CARTESIAN_POINT ( 'NONE',  ( 116.5402214775786405, 0.2603800115204892296, -16.42320221600525088 ) ) ;
#266=CARTESIAN_POINT ( 'NONE',  ( 125.3223148109119904, 0.3778260857404745487, -12.04688916545782185 ) ) ;
#267=CARTESIAN_POINT ( 'NONE',  ( 125.1059481442452750, -1.833838273342660141, -17.42832698103878286 ) ) ;
#269=CARTESIAN_POINT ( 'NONE',  ( 112.2857214775786474, -5.574606645277164318, -18.38911715685844683 ) ) ;
#272=CARTESIAN_POINT ( 'NONE',  ( 123.8012348109119642, 0.2603800115204892296, -16.42320221600525088 ) ) ;
#273=CARTESIAN_POINT ( 'NONE',  ( 124.0281414775786146, -1.834011780172310813, -8.268836392978581529 ) ) ;
#275=CARTESIAN_POINT ( 'NONE',  ( 112.9097148109120070, 0.2603800115204892296, -16.42320221600525088 ) ) ;
#281=CARTESIAN_POINT ( 'NONE',  ( 126.2202699136542350, -7.820588090633775025, -9.359791697047713299 ) ) ;
#282=CARTESIAN_POINT ( 'NONE',  ( 114.4413348109119823, -0.8288870151387760510, -10.36305467784173118 ) ) ;
#283=CARTESIAN_POINT ( 'NONE',  ( 126.1270281442452870, 0.1319031606808879209, -14.10382304977623669 ) ) ;
#286=CARTESIAN_POINT ( 'NONE',  ( 120.2841814775786276, -10.15424416112533912, -14.75197769757731336 ) ) ;
#287=CARTESIAN_POINT ( 'NONE',  ( 119.0929214775786278, -4.153390946401325223, -8.397313243818185668 ) ) ;
#288=CARTESIAN_POINT ( 'NONE',  ( 125.9001214775786224, -4.089484607189486809, -7.948022111789456723 ) ) ;
#290=CARTESIAN_POINT ( 'NONE',  ( 124.6521348109119884, -7.894159318335828068, -9.358103419637847864 ) ) ;
#292=CARTESIAN_POINT ( 'NONE',  ( 114.2144281442453178, -1.833838273342658809, -17.42832698103878286 ) ) ;
#294=CARTESIAN_POINT ( 'NONE',  ( 124.8328548109119822, -8.862178061931773598, -16.39564131203328401 ) ) ;
#299=CARTESIAN_POINT ( 'NONE',  ( 118.5823814775786360, -7.643976991954077427, -18.09477374809248928 ) ) ;
#300=CARTESIAN_POINT ( 'NONE',  ( 113.8740681442453138, -9.859900752359374465, -12.68260735090039404 ) ) ;
#304=ORIENTED_EDGE ( 'NONE', *, *, #43174, .F. ) ;
#308=CARTESIAN_POINT ( 'NONE',  ( 114.1009748109119784, -4.089484607189486809, -7.948022111789456723 ) ) ;
#309=CARTESIAN_POINT ( 'NONE',  ( 122.2696148109119889, -5.574606645277164318, -18.38911715685844683 ) ) ;
#310=CARTESIAN_POINT ( 'NONE',  ( 116.3700414775786527, -4.153390946401321671, -8.397313243818183892 ) ) ;
#311=FACE_OUTER_BOUND ( 'NONE', #28489, .T. ) ;
#313=CARTESIAN_POINT ( 'NONE',  ( 115.1787814775786387, -0.1624402480850797581, -16.17319339645315424 ) ) ;
#318=CARTESIAN_POINT ( 'NONE',  ( 116.5402214775786405, 0.2603800115204892296, -16.42320221600525088 ) ) ;
#320=CARTESIAN_POINT ( 'NONE',  ( 118.4689281442453392, 0.9020085738987339008, -11.91225656197089222 ) ) ;
#323=CARTESIAN_POINT ( 'NONE',  ( 113.3068014775786594, -8.166667518702817929, -8.995218007635859436 ) ) ;
#324=CARTESIAN_POINT ( 'NONE',  ( 112.2289948109119848, -1.834011780172310813, -8.268836392978581529 ) ) ;
#325=CARTESIAN_POINT ( 'NONE',  ( 123.5743281442453139, -2.084020599724406786, -8.691656652584148546 ) ) ;
#330=CARTESIAN_POINT ( 'NONE',  ( 120.5887993777725029, -1.267766418764730840, -16.93314635290706605 ) ) ;
#332=CARTESIAN_POINT ( 'NONE',  ( 115.2355081442453155, 0.1319031606808879209, -14.10382304977623669 ) ) ;
#337=CARTESIAN_POINT ( 'NONE',  ( 124.0281414775786146, -1.834011780172310813, -8.268836392978581529 ) ) ;
#339=CARTESIAN_POINT ( 'NONE',  ( 123.2339681442453241, -6.344957434206665248, -7.627207830600338134 ) ) ;
#340=CARTESIAN_POINT ( 'NONE',  ( 116.0296814775786345, -8.166667518702817929, -8.995218007635861213 ) ) ;
#342=ORIENTED_EDGE ( 'NONE', *, *, #31421, .T. ) ;
#343=CARTESIAN_POINT ( 'NONE',  ( 116.4267681442453153, -6.222761293078241884, -8.102969835052219238 ) ) ;
#344=CARTESIAN_POINT ( 'NONE',  ( 113.1933481442453058, -4.089484607189486809, -7.948022111789456723 ) ) ;
#345=CARTESIAN_POINT ( 'NONE',  ( 117.5045748109119756, 0.5811942927096110934, -14.16772938898807510 ) ) ;
#346=CARTESIAN_POINT ( 'NONE',  ( 117.4478481442453131, -9.565557343593413364, -10.61323700422348004 ) ) ;
#348=CARTESIAN_POINT ( 'NONE',  ( 119.7736414775786358, 0.1319031606808879209, -14.10382304977623669 ) ) ;
#350=CARTESIAN_POINT ( 'NONE',  ( 116.9940348109119839, -9.988377603198976828, -10.36322818467138340 ) ) ;
#355=VECTOR ( 'NONE', #33888, 1000.000000000000000 ) ;
#359=CARTESIAN_POINT ( 'NONE',  ( 113.0798948109119948, -0.4660016031367893996, -10.09054647747474043 ) ) ;
#361=CARTESIAN_POINT ( 'NONE',  ( 113.9307948109119764, -10.15424416112533912, -14.75197769757731336 ) ) ;
#365=CARTESIAN_POINT ( 'NONE',  ( 113.8740681442453138, -9.859900752359374465, -12.68260735090039404 ) ) ;
#370=CARTESIAN_POINT ( 'NONE',  ( 114.3278814775786429, -10.30919188438810075, -12.61870101168855918 ) ) ;
#371=CARTESIAN_POINT ( 'NONE',  ( 124.6521348109119884, -7.894159318335828068, -9.358103419637847864 ) ) ;
#372=CARTESIAN_POINT ( 'NONE',  ( 118.0151148109119816, 0.4262465694468514643, -12.03445270309931736 ) ) ;
#374=CARTESIAN_POINT ( 'NONE',  ( 125.5030348109119558, -3.383040157471821630, -19.15922257007629170 ) ) ;
#375=CARTESIAN_POINT ( 'NONE',  ( 121.4187148109119789, -6.344957434206665248, -7.627207830600338134 ) ) ;
#377=CARTESIAN_POINT ( 'NONE',  ( 115.6893214775786447, -9.859900752359374465, -12.68260735090039404 ) ) ;
#378=CARTESIAN_POINT ( 'NONE',  ( 111.7751814775786556, -2.084020599724406786, -8.691656652584148546 ) ) ;
#382=CARTESIAN_POINT ( 'NONE',  ( 121.1350814775786233, -9.859900752359378018, -12.68260735090039759 ) ) ;
#383=CARTESIAN_POINT ( 'NONE',  ( 119.9438214775786378, -2.084020599724406786, -8.691656652584148546 ) ) ;
#388=CARTESIAN_POINT ( 'NONE',  ( 117.3343948109119737, -3.383040157471821630, -19.15922257007629170 ) ) ;
#389=CARTESIAN_POINT ( 'NONE',  ( 115.0653281442453277, -6.344957434206662583, -7.627207830600332805 ) ) ;
#391=CARTESIAN_POINT ( 'NONE',  ( 112.2289948109119848, -1.834011780172310813, -8.268836392978581529 ) ) ;
#394=CARTESIAN_POINT ( 'NONE',  ( 120.7947214775786193, -9.261995988541697145, -16.69588392320189030 ) ) ;
#395=CARTESIAN_POINT ( 'NONE',  ( 114.8951481442453115, -0.4660016031367893996, -10.09054647747474043 ) ) ;
#396=CARTESIAN_POINT ( 'NONE',  ( 120.6245414775786458, -0.1624402480850797581, -16.17319339645315424 ) ) ;
#397=SURFACE_STYLE_FILL_AREA ( #24138 ) ;
#398=CARTESIAN_POINT ( 'NONE',  ( 111.7751814775786556, -2.084020599724406786, -8.691656652584148546 ) ) ;
#399=CARTESIAN_POINT ( 'NONE',  ( 121.0783548109119749, 0.2603800115204892296, -16.42320221600525088 ) ) ;
#402=CARTESIAN_POINT ( 'NONE',  ( 115.6893214775786447, -9.859900752359374465, -12.68260735090039404 ) ) ;
#403=CARTESIAN_POINT ( 'NONE',  ( 125.0375914802849024, -3.929494816607940422, -18.62311481910837685 ) ) ;
#404=EDGE_LOOP ( 'NONE', ( #33107, #21221, #35400, #21094, #24132, #19976, #30122, #32334, #19696, #15366, #342, #5443, #42035, #39327, #5928, #9393, #16209, #25408, #27389, #31461 ) ) ;
#405=CARTESIAN_POINT ( 'NONE',  ( 120.1707281442453166, 0.2603800115204892296, -16.42320221600525088 ) ) ;
#407=CARTESIAN_POINT ( 'NONE',  ( 118.1852948109119836, -5.638512984488999180, -18.83840828888717311 ) ) ;
#410=DIRECTION ( 'NONE',  ( -1.000000000000000000, 0.000000000000000000, 0.000000000000000000 ) ) ;
#411=CARTESIAN_POINT ( 'NONE',  ( 122.2696148109119889, -4.089484607189438847, -7.948022111789470934 ) ) ;
#412=CARTESIAN_POINT ( 'NONE',  ( 114.4980614775786734, -2.084020599724406786, -8.691656652584148546 ) ) ;
#413=CARTESIAN_POINT ( 'NONE',  ( 126.2184548109119788, -1.295815253274133161, -16.89579513612386563 ) ) ;
#414=CARTESIAN_POINT ( 'NONE',  ( 118.2420214775786320, -6.222761293078241884, -8.102969835052219238 ) ) ;
#415=CARTESIAN_POINT ( 'NONE',  ( 120.2122292294923938, -2.263366209404226392, -18.10533625161308180 ) ) ;
#417=CARTESIAN_POINT ( 'NONE',  ( 122.0427081442452817, -9.859900752359378018, -12.68260735090039759 ) ) ;
#419=CARTESIAN_POINT ( 'NONE',  ( 119.8870948109119752, -0.8288870151387760510, -10.36305467784173118 ) ) ;
#421=CARTESIAN_POINT ( 'NONE',  ( 114.4980614775786592, -7.893985811506177619, -18.51759400769804742 ) ) ;
#423=CARTESIAN_POINT ( 'NONE',  ( 120.8514481442452961, -2.084020599724406786, -8.691656652584148546 ) ) ;
#425=CARTESIAN_POINT ( 'NONE',  ( 117.5613014775786525, 0.9020085738987339008, -11.91225656197089222 ) ) ;
#431=CARTESIAN_POINT ( 'NONE',  ( 123.4608748109119745, -10.63000616557722466, -14.87417383870573495 ) ) ;
#433=CARTESIAN_POINT ( 'NONE',  ( 127.0298367773230979, -8.891943447879246065, -9.788057200751348219 ) ) ;
#434=CARTESIAN_POINT ( 'NONE',  ( 120.9081748109119872, -4.153390946401325223, -8.397313243818185668 ) ) ;
#442=CARTESIAN_POINT ( 'NONE',  ( 116.1431348109119881, -10.30919188438810075, -12.61870101168855918 ) ) ;
#443=CARTESIAN_POINT ( 'NONE',  ( 124.9924948109119924, -5.574606645277164318, -18.38911715685844683 ) ) ;
#444=CARTESIAN_POINT ( 'NONE',  ( 122.7801548109119665, -3.383040157471821630, -19.15922257007629170 ) ) ;
#445=CARTESIAN_POINT ( 'NONE',  ( 117.6180281442453150, -8.899110576539710493, -16.42337572283490132 ) ) ;
#447=CARTESIAN_POINT ( 'NONE',  ( 121.7023481442452777, -9.261995988541697145, -16.69588392320189030 ) ) ;
#448=CARTESIAN_POINT ( 'NONE',  ( 123.8579614775786126, -9.859900752359374465, -12.68260735090038693 ) ) ;
#451=CARTESIAN_POINT ( 'NONE',  ( 123.0070614775786169, -10.15424416112533912, -14.75197769757731336 ) ) ;
#452=VERTEX_POINT ( 'NONE', #31478 ) ;
#453=AXIS2_PLACEMENT_3D ( 'NONE', #36071, #15337, #1637 ) ;
#455=CARTESIAN_POINT ( 'NONE',  ( 120.1707281442453166, 0.2603800115204892296, -16.42320221600525088 ) ) ;
#456=CARTESIAN_POINT ( 'NONE',  ( 125.2761281442453054, 0.4262465694468514643, -12.03445270309931736 ) ) ;
#458=( BOUNDED_SURFACE ( )  B_SPLINE_SURFACE ( 1, 2, ( 
 ( #7146, #28584, #982, #21057, #38826, #7830, #25389, #7368, #746, #32433, #29027, #42716, #18090, #8052, #14669, #535, #42494, #38591, #10586, #34935, #3943, #35846, #14444, #35396, #28137, #31539, #24485, #28352, #14222, #11253, #4172, #39058, #21736, #35625, #35167, #17641, #21956, #4399, #11483, #18315, #18541, #42265, #308, #1207, #15121, #42045, #10806, #24701, #21281, #16248, #33317, #5066, #26508, #19213, #12381, #12151, #36075, #25611, #16017, #9176, #29467, #39958, #43383, #43605, #8501, #23083, #39732, #11700, #15792, #39513, #4846, #26054, #5297, #8720, #29694, #22405, #8277, #36964, #36524, #2091, #22626, #36744, #36298, #22179, #5512, #33093, #2320, #18765, #32654, #42938, #1421, #29925, #18982, #40416, #1862, #26279, #40187, #15341, #29250, #43839, #5735, #8953, #22853, #19431, #12606, #32871, #19654, #1640, #43159, #33541, #11926, #25825, #15564, #37885, #37431, #30151, #16473, #38105, #44298, #23548, #13507, #3229, #16929, #26732, #27415, #26952, #13729, #5965, #27638, #6661, #2546, #40874, #2779, #23773, #30824, #44067, #40641, #24214, #3456, #44972, #10312, #9627, #41335, #17155, #13053, #41552, #10094, #44748, #6201, #12833, #6880, #37665, #34670, #9396, #20123, #16704, #30376, #34233, #34008, #23997, #6440, #20349, #20790, #33776, #30598, #27186, #44515, #3007, #23307, #37191, #20571, #34448, #19889, #13280, #31042, #41106, #9864, #7537, #39226, #35793, #39000, #24875, #14841, #21454, #7311, #35337, #253, #17373, #34, #10753, #42656, #24651, #42211, #34881, #38320, #31261, #38536, #21007, #18030, #31704, #14612, #32154, #14162, #4109, #7991, #13946, #7770, #38767, #28751, #31927, #21230, #692, #28080, #27859, #41769, #35109, #11427, #3890, #10972, #3669, #7097, #10529, #17810, #17590, #28529, #474, #42435, #28299, #11199, #41988, #24428, #25333, #25104, #21677, #35565, #4337, #14387, #31483, #18258, #922, #21899, #11642, #25552, #4565, #23024, #40131, #11872, #33266, #26002, #19155, #18929, #42882, #32379, #22794, #15964, #36245, #1587 ),
 ( #39458, #12322, #26221, #25776, #18489, #36021, #12548, #18710, #43102, #33036, #36688, #36472, #1146, #1811, #1371, #2040, #8222, #29867, #8896, #22128, #15282, #22351, #43329, #5239, #15063, #28977, #43783, #4789, #19378, #26455, #29190, #15738, #5458, #32600, #40357, #29640, #43554, #39683, #8448, #9121, #12098, #5012, #32817, #15508, #29415, #39906, #8667, #22569, #37608, #30540, #44461, #13676, #40587, #19835, #33953, #9575, #9809, #20517, #33486, #23718, #27358, #2264, #5913, #17101, #13227, #16192, #27584, #16646, #30096, #41278, #44012, #30768, #37825, #27128, #33722, #44919, #26899, #41499, #12774, #41052, #9346, #30317, #2492, #37139, #16421, #44694, #34174, #23255, #10037, #13454, #34397, #44243, #23945, #20067, #26676, #13001, #37377, #40819, #19602, #6382, #10255, #36912, #5683, #20290, #23491, #2949, #6147, #2720, #16877, #6603, #3178, #30993, #24601, #35279, #31211, #10919, #14111, #642, #24819, #35511, #45134, #20958, #35050, #14557, #21175, #28475, #17754, #32099, #20737, #24162, #3834, #13893, #867, #21399, #4053, #31877, #7479, #14335, #18202, #11144, #42380, #10698, #28700, #25047, #195, #38942, #17977, #7710, #21623, #31651, #4283, #14786, #419, #28027, #42604, #38054, #10479, #17531, #28249, #42158, #38711, #34830, #6832, #34617, #3404, #17321, #41715, #27800, #24380, #38266, #41935, #7047, #3615, #31428, #38484, #7259, #22739, #4960, #8840, #5183, #22299, #36641, #19100, #35967, #32987, #1761, #42830, #15687, #29138, #32765, #29589, #11817, #15916, #18439, #32328, #11370, #29814, #43507, #18658, #40076, #1538, #25949, #25725, #4516, #39172, #12275, #5414, #43050, #8395, #15460, #39632, #29366, #19330, #8169, #25276, #43277, #7936, #1094, #26171, #33216, #32548, #21847, #11591, #1990, #25501, #4737, #39856, #35742, #12046, #15009, #8621, #22079, #28923, #39405, #1318, #15229, #36196, #18874, #22518, #36416, #44410, #12498, #9070, #38380, #17649, #14008, #24495, #40536, #27078, #31320, #12719, #10593, #9753, #13176, #26622, #43730, #7153 ) ),
 .UNSPECIFIED., .F., .F., .F. ) 
 B_SPLINE_SURFACE_WITH_KNOTS ( ( 2, 2 ),
 ( 3, 2, 2, 2, 2, 2, 2, 2, 2, 2, 2, 2, 2, 2, 2, 2, 2, 2, 2, 2, 2, 2, 2, 2, 2, 2, 2, 2, 2, 2, 2, 2, 2, 2, 2, 2, 2, 2, 2, 2, 2, 2, 2, 2, 2, 2, 2, 2, 2, 2, 2, 2, 2, 2, 2, 2, 2, 2, 2, 2, 2, 2, 2, 2, 2, 2, 2, 2, 2, 2, 2, 2, 2, 2, 2, 2, 2, 2, 2, 2, 2, 2, 2, 2, 2, 2, 2, 2, 2, 2, 2, 2, 2, 2, 2, 2, 2, 2, 2, 2, 2, 2, 2, 2, 2, 2, 2, 2, 2, 2, 2, 2, 2, 2, 2, 2, 2, 2, 2, 2, 2, 2, 2, 2, 2, 2, 2, 2, 3 ),
 ( 0.000000000000000000, 1.000000000000000000 ),
 ( 0.000000000000000000, 0.007812500000000000000, 0.01562500000000000000, 0.02343750000000000000, 0.03125000000000000000, 0.03906250000000000000, 0.04687500000000000000, 0.05468750000000000000, 0.06250000000000000000, 0.07031250000000000000, 0.07812500000000000000, 0.08593750000000000000, 0.09375000000000000000, 0.1015625000000000000, 0.1093750000000000000, 0.1171875000000000000, 0.1250000000000000000, 0.1328125000000000000, 0.1406250000000000000, 0.1484375000000000000, 0.1562500000000000000, 0.1640625000000000000, 0.1718750000000000000, 0.1796875000000000000, 0.1875000000000000000, 0.1953125000000000000, 0.2031250000000000000, 0.2109375000000000000, 0.2187500000000000000, 0.2265625000000000000, 0.2343750000000000000, 0.2421875000000000000, 0.2500000000000000000, 0.2578125000000000000, 0.2656250000000000000, 0.2734375000000000000, 0.2812500000000000000, 0.2890625000000000000, 0.2968750000000000000, 0.3046875000000000000, 0.3125000000000000000, 0.3203125000000000000, 0.3281250000000000000, 0.3359375000000000000, 0.3437500000000000000, 0.3515625000000000000, 0.3593750000000000000, 0.3671875000000000000, 0.3750000000000000000, 0.3828125000000000000, 0.3906250000000000000, 0.3984375000000000000, 0.4062500000000000000, 0.4140625000000000000, 0.4218750000000000000, 0.4296875000000000000, 0.4375000000000000000, 0.4453125000000000000, 0.4531250000000000000, 0.4609375000000000000, 0.4687500000000000000, 0.4765625000000000000, 0.4843750000000000000, 0.4921875000000000000, 0.5000000000000000000, 0.5078125000000000000, 0.5156250000000000000, 0.5234375000000000000, 0.5312500000000000000, 0.5390625000000000000, 0.5468750000000000000, 0.5546875000000000000, 0.5625000000000000000, 0.5703125000000000000, 0.5781250000000000000, 0.5859375000000000000, 0.5937500000000000000, 0.6015625000000000000, 0.6093750000000000000, 0.6171875000000000000, 0.6250000000000000000, 0.6328125000000000000, 0.6406250000000000000, 0.6484375000000000000, 0.6562500000000000000, 0.6640625000000000000, 0.6718750000000000000, 0.6796875000000000000, 0.6875000000000000000, 0.6953125000000000000, 0.7031250000000000000, 0.7109375000000000000, 0.7187500000000000000, 0.7265625000000000000, 0.7343750000000000000, 0.7421875000000000000, 0.7500000000000000000, 0.7578125000000000000, 0.7656250000000000000, 0.7734375000000000000, 0.7812500000000000000, 0.7890625000000000000, 0.7968750000000000000, 0.8046875000000000000, 0.8125000000000000000, 0.8203125000000000000, 0.8281250000000000000, 0.8359375000000000000, 0.8437500000000000000, 0.8515625000000000000, 0.8593750000000000000, 0.8671875000000000000, 0.8750000000000000000, 0.8828125000000000000, 0.8906250000000000000, 0.8984375000000000000, 0.9062500000000000000, 0.9140625000000000000, 0.9218750000000000000, 0.9296875000000000000, 0.9375000000000000000, 0.9453125000000000000, 0.9531250000000000000, 0.9609375000000000000, 0.9687500000000000000, 0.9765625000000000000, 0.9843750000000000000, 0.9921875000000000000, 1.000000000000000000 ),
 .UNSPECIFIED. ) 
 GEOMETRIC_REPRESENTATION_ITEM ( )  RATIONAL_B_SPLINE_SURFACE ( (
 ( 1.000000000000000000, 0.9238795325112869605, 1.000000000000000000, 0.9238795325112869605, 1.000000000000000000, 0.9238795325112869605, 1.000000000000000000, 0.9238795325112869605, 1.000000000000000000, 0.9238795325112869605, 1.000000000000000000, 0.9238795325112869605, 1.000000000000000000, 0.9238795325112869605, 1.000000000000000000, 0.9238795325112869605, 1.000000000000000000, 0.9238795325112869605, 1.000000000000000000, 0.9238795325112869605, 1.000000000000000000, 0.9238795325112869605, 1.000000000000000000, 0.9238795325112869605, 1.000000000000000000, 0.9238795325112869605, 1.000000000000000000, 0.9238795325112869605, 1.000000000000000000, 0.9238795325112869605, 1.000000000000000000, 0.9238795325112869605, 1.000000000000000000, 0.9238795325112869605, 1.000000000000000000, 0.9238795325112869605, 1.000000000000000000, 0.9238795325112869605, 1.000000000000000000, 0.9238795325112869605, 1.000000000000000000, 0.9238795325112869605, 1.000000000000000000, 0.9238795325112869605, 1.000000000000000000, 0.9238795325112869605, 1.000000000000000000, 0.9238795325112869605, 1.000000000000000000, 0.9238795325112869605, 1.000000000000000000, 0.9238795325112869605, 1.000000000000000000, 0.9238795325112869605, 1.000000000000000000, 0.9238795325112869605, 1.000000000000000000, 0.9238795325112869605, 1.000000000000000000, 0.9238795325112869605, 1.000000000000000000, 0.9238795325112869605, 1.000000000000000000, 0.9238795325112869605, 1.000000000000000000, 0.9238795325112869605, 1.000000000000000000, 0.9238795325112869605, 1.000000000000000000, 0.9238795325112869605, 1.000000000000000000, 0.9238795325112869605, 1.000000000000000000, 0.9238795325112869605, 1.000000000000000000, 0.9238795325112869605, 1.000000000000000000, 0.9238795325112869605, 1.000000000000000000, 0.9238795325112869605, 1.000000000000000000, 0.9238795325112869605, 1.000000000000000000, 0.9238795325112869605, 1.000000000000000000, 0.9238795325112869605, 1.000000000000000000, 0.9238795325112869605, 1.000000000000000000, 0.9238795325112869605, 1.000000000000000000, 0.9238795325112869605, 1.000000000000000000, 0.9238795325112869605, 1.000000000000000000, 0.9238795325112869605, 1.000000000000000000, 0.9238795325112869605, 1.000000000000000000, 0.9238795325112869605, 1.000000000000000000, 0.9238795325112869605, 1.000000000000000000, 0.9238795325112869605, 1.000000000000000000, 0.9238795325112869605, 1.000000000000000000, 0.9238795325112869605, 1.000000000000000000, 0.9238795325112869605, 1.000000000000000000, 0.9238795325112869605, 1.000000000000000000, 0.9238795325112869605, 1.000000000000000000, 0.9238795325112869605, 1.000000000000000000, 0.9238795325112869605, 1.000000000000000000, 0.9238795325112869605, 1.000000000000000000, 0.9238795325112869605, 1.000000000000000000, 0.9238795325112869605, 1.000000000000000000, 0.9238795325112869605, 1.000000000000000000, 0.9238795325112869605, 1.000000000000000000, 0.9238795325112869605, 1.000000000000000000, 0.9238795325112869605, 1.000000000000000000, 0.9238795325112869605, 1.000000000000000000, 0.9238795325112869605, 1.000000000000000000, 0.9238795325112869605, 1.000000000000000000, 0.9238795325112869605, 1.000000000000000000, 0.9238795325112869605, 1.000000000000000000, 0.9238795325112869605, 1.000000000000000000, 0.9238795325112869605, 1.000000000000000000, 0.9238795325112869605, 1.000000000000000000, 0.9238795325112869605, 1.000000000000000000, 0.9238795325112869605, 1.000000000000000000, 0.9238795325112869605, 1.000000000000000000, 0.9238795325112869605, 1.000000000000000000, 0.9238795325112869605, 1.000000000000000000, 0.9238795325112869605, 1.000000000000000000, 0.9238795325112869605, 1.000000000000000000, 0.9238795325112869605, 1.000000000000000000, 0.9238795325112869605, 1.000000000000000000, 0.9238795325112869605, 1.000000000000000000, 0.9238795325112869605, 1.000000000000000000, 0.9238795325112869605, 1.000000000000000000, 0.9238795325112869605, 1.000000000000000000, 0.9238795325112869605, 1.000000000000000000, 0.9238795325112869605, 1.000000000000000000, 0.9238795325112869605, 1.000000000000000000, 0.9238795325112869605, 1.000000000000000000, 0.9238795325112869605, 1.000000000000000000, 0.9238795325112869605, 1.000000000000000000, 0.9238795325112869605, 1.000000000000000000, 0.9238795325112869605, 1.000000000000000000, 0.9238795325112869605, 1.000000000000000000, 0.9238795325112869605, 1.000000000000000000, 0.9238795325112869605, 1.000000000000000000, 0.9238795325112869605, 1.000000000000000000, 0.9238795325112869605, 1.000000000000000000, 0.9238795325112869605, 1.000000000000000000, 0.9238795325112869605, 1.000000000000000000, 0.9238795325112869605, 1.000000000000000000, 0.9238795325112869605, 1.000000000000000000, 0.9238795325112869605, 1.000000000000000000, 0.9238795325112869605, 1.000000000000000000, 0.9238795325112869605, 1.000000000000000000, 0.9238795325112869605, 1.000000000000000000, 0.9238795325112869605, 1.000000000000000000, 0.9238795325112869605, 1.000000000000000000, 0.9238795325112869605, 1.000000000000000000, 0.9238795325112869605, 1.000000000000000000, 0.9238795325112869605, 1.000000000000000000, 0.9238795325112869605, 1.000000000000000000, 0.9238795325112869605, 1.000000000000000000, 0.9238795325112869605, 1.000000000000000000, 0.9238795325112869605, 1.000000000000000000, 0.9238795325112869605, 1.000000000000000000, 0.9238795325112869605, 1.000000000000000000, 0.9238795325112869605, 1.000000000000000000, 0.9238795325112869605, 1.000000000000000000, 0.9238795325112869605, 1.000000000000000000, 0.9238795325112869605, 1.000000000000000000, 0.9238795325112869605, 1.000000000000000000, 0.9238795325112869605, 1.000000000000000000, 0.9238795325112869605, 1.000000000000000000, 0.9238795325112869605, 1.000000000000000000, 0.9238795325112869605, 1.000000000000000000),
 ( 1.000000000000000000, 0.9238795325112869605, 1.000000000000000000, 0.9238795325112869605, 1.000000000000000000, 0.9238795325112869605, 1.000000000000000000, 0.9238795325112869605, 1.000000000000000000, 0.9238795325112869605, 1.000000000000000000, 0.9238795325112869605, 1.000000000000000000, 0.9238795325112869605, 1.000000000000000000, 0.9238795325112869605, 1.000000000000000000, 0.9238795325112869605, 1.000000000000000000, 0.9238795325112869605, 1.000000000000000000, 0.9238795325112869605, 1.000000000000000000, 0.9238795325112869605, 1.000000000000000000, 0.9238795325112869605, 1.000000000000000000, 0.9238795325112869605, 1.000000000000000000, 0.9238795325112869605, 1.000000000000000000, 0.9238795325112869605, 1.000000000000000000, 0.9238795325112869605, 1.000000000000000000, 0.9238795325112869605, 1.000000000000000000, 0.9238795325112869605, 1.000000000000000000, 0.9238795325112869605, 1.000000000000000000, 0.9238795325112869605, 1.000000000000000000, 0.9238795325112869605, 1.000000000000000000, 0.9238795325112869605, 1.000000000000000000, 0.9238795325112869605, 1.000000000000000000, 0.9238795325112869605, 1.000000000000000000, 0.9238795325112869605, 1.000000000000000000, 0.9238795325112869605, 1.000000000000000000, 0.9238795325112869605, 1.000000000000000000, 0.9238795325112869605, 1.000000000000000000, 0.9238795325112869605, 1.000000000000000000, 0.9238795325112869605, 1.000000000000000000, 0.9238795325112869605, 1.000000000000000000, 0.9238795325112869605, 1.000000000000000000, 0.9238795325112869605, 1.000000000000000000, 0.9238795325112869605, 1.000000000000000000, 0.9238795325112869605, 1.000000000000000000, 0.9238795325112869605, 1.000000000000000000, 0.9238795325112869605, 1.000000000000000000, 0.9238795325112869605, 1.000000000000000000, 0.9238795325112869605, 1.000000000000000000, 0.9238795325112869605, 1.000000000000000000, 0.9238795325112869605, 1.000000000000000000, 0.9238795325112869605, 1.000000000000000000, 0.9238795325112869605, 1.000000000000000000, 0.9238795325112869605, 1.000000000000000000, 0.9238795325112869605, 1.000000000000000000, 0.9238795325112869605, 1.000000000000000000, 0.9238795325112869605, 1.000000000000000000, 0.9238795325112869605, 1.000000000000000000, 0.9238795325112869605, 1.000000000000000000, 0.9238795325112869605, 1.000000000000000000, 0.9238795325112869605, 1.000000000000000000, 0.9238795325112869605, 1.000000000000000000, 0.9238795325112869605, 1.000000000000000000, 0.9238795325112869605, 1.000000000000000000, 0.9238795325112869605, 1.000000000000000000, 0.9238795325112869605, 1.000000000000000000, 0.9238795325112869605, 1.000000000000000000, 0.9238795325112869605, 1.000000000000000000, 0.9238795325112869605, 1.000000000000000000, 0.9238795325112869605, 1.000000000000000000, 0.9238795325112869605, 1.000000000000000000, 0.9238795325112869605, 1.000000000000000000, 0.9238795325112869605, 1.000000000000000000, 0.9238795325112869605, 1.000000000000000000, 0.9238795325112869605, 1.000000000000000000, 0.9238795325112869605, 1.000000000000000000, 0.9238795325112869605, 1.000000000000000000, 0.9238795325112869605, 1.000000000000000000, 0.9238795325112869605, 1.000000000000000000, 0.9238795325112869605, 1.000000000000000000, 0.9238795325112869605, 1.000000000000000000, 0.9238795325112869605, 1.000000000000000000, 0.9238795325112869605, 1.000000000000000000, 0.9238795325112869605, 1.000000000000000000, 0.9238795325112869605, 1.000000000000000000, 0.9238795325112869605, 1.000000000000000000, 0.9238795325112869605, 1.000000000000000000, 0.9238795325112869605, 1.000000000000000000, 0.9238795325112869605, 1.000000000000000000, 0.9238795325112869605, 1.000000000000000000, 0.9238795325112869605, 1.000000000000000000, 0.9238795325112869605, 1.000000000000000000, 0.9238795325112869605, 1.000000000000000000, 0.9238795325112869605, 1.000000000000000000, 0.9238795325112869605, 1.000000000000000000, 0.9238795325112869605, 1.000000000000000000, 0.9238795325112869605, 1.000000000000000000, 0.9238795325112869605, 1.000000000000000000, 0.9238795325112869605, 1.000000000000000000, 0.9238795325112869605, 1.000000000000000000, 0.9238795325112869605, 1.000000000000000000, 0.9238795325112869605, 1.000000000000000000, 0.9238795325112869605, 1.000000000000000000, 0.9238795325112869605, 1.000000000000000000, 0.9238795325112869605, 1.000000000000000000, 0.9238795325112869605, 1.000000000000000000, 0.9238795325112869605, 1.000000000000000000, 0.9238795325112869605, 1.000000000000000000, 0.9238795325112869605, 1.000000000000000000, 0.9238795325112869605, 1.000000000000000000, 0.9238795325112869605, 1.000000000000000000, 0.9238795325112869605, 1.000000000000000000, 0.9238795325112869605, 1.000000000000000000, 0.9238795325112869605, 1.000000000000000000, 0.9238795325112869605, 1.000000000000000000, 0.9238795325112869605, 1.000000000000000000, 0.9238795325112869605, 1.000000000000000000, 0.9238795325112869605, 1.000000000000000000, 0.9238795325112869605, 1.000000000000000000, 0.9238795325112869605, 1.000000000000000000, 0.9238795325112869605, 1.000000000000000000, 0.9238795325112869605, 1.000000000000000000, 0.9238795325112869605, 1.000000000000000000, 0.9238795325112869605, 1.000000000000000000, 0.9238795325112869605, 1.000000000000000000, 0.9238795325112869605, 1.000000000000000000, 0.9238795325112869605, 1.000000000000000000, 0.9238795325112869605, 1.000000000000000000, 0.9238795325112869605, 1.000000000000000000, 0.9238795325112869605, 1.000000000000000000, 0.9238795325112869605, 1.000000000000000000, 0.9238795325112869605, 1.000000000000000000, 0.9238795325112869605, 1.000000000000000000, 0.9238795325112869605, 1.000000000000000000, 0.9238795325112869605, 1.000000000000000000, 0.9238795325112869605, 1.000000000000000000, 0.9238795325112869605, 1.000000000000000000) ) ) 
 REPRESENTATION_ITEM ( '' )  SURFACE ( )  );
#459=CARTESIAN_POINT ( 'NONE',  ( 136.3568202015646875, 0.5053874888704125157, -11.17693241582777119 ) ) ;
#460=CARTESIAN_POINT ( 'NONE',  ( 121.9859814775786333, 0.2603800115204892296, -16.42320221600525088 ) ) ;
#462=CARTESIAN_POINT ( 'NONE',  ( 120.2841814775786276, -10.15424416112533912, -14.75197769757731336 ) ) ;
#464=CARTESIAN_POINT ( 'NONE',  ( 114.7816948109119863, 0.5811942927096154232, -14.16772938898807155 ) ) ;
#467=CARTESIAN_POINT ( 'NONE',  ( 120.1814158072985350, 0.3208234527006321724, -15.99825685930877839 ) ) ;
#470=CARTESIAN_POINT ( 'NONE',  ( 125.2194014775786286, -10.30919188438810075, -12.61870101168855918 ) ) ;
#471=CONICAL_SURFACE ( 'NONE', #35383, 5.999999999999997335, 0.4636476090008060935 ) ;
#473=CARTESIAN_POINT ( 'NONE',  ( 112.1243801106810167, -8.918668529216430940, -16.32041580884654053 ) ) ;
#474=CARTESIAN_POINT ( 'NONE',  ( 124.4819548109119722, -7.893985811506177619, -18.51759400769804742 ) ) ;
#475=CARTESIAN_POINT ( 'NONE',  ( 122.8368814775786291, -1.561330072975668948, -17.79121239304076951 ) ) ;
#476=CARTESIAN_POINT ( 'NONE',  ( 123.3474214775786209, -0.1624402480850797581, -16.17319339645315424 ) ) ;
#477=CARTESIAN_POINT ( 'NONE',  ( 118.2987481442453088, -7.894159318335828068, -9.358103419637847864 ) ) ;
#479=CARTESIAN_POINT ( 'NONE',  ( 116.5969481442453031, 0.5811942927096154232, -14.16772938898807155 ) ) ;
#483=CARTESIAN_POINT ( 'NONE',  ( 125.4357681442453156, -2.109465145233854422, -8.734689011828928429 ) ) ;
#488=CARTESIAN_POINT ( 'NONE',  ( 112.5693548109119888, -10.63000616557722466, -14.87417383870573495 ) ) ;
#491=CARTESIAN_POINT ( 'NONE',  ( 114.8951481442453115, -8.899110576539710493, -16.42337572283490132 ) ) ;
#493=CARTESIAN_POINT ( 'NONE',  ( 118.7735460444391862, -1.267766418764730840, -16.93314635290706605 ) ) ;
#494=CARTESIAN_POINT ( 'NONE',  ( 122.0427081442452817, 0.5811942927096110934, -14.16772938898807510 ) ) ;
#496=CARTESIAN_POINT ( 'NONE',  ( 126.0135748109119902, -8.166667518702819706, -8.995218007635861213 ) ) ;
#498=CARTESIAN_POINT ( 'NONE',  ( 116.6536748109119941, 0.9020085738987339008, -11.91225656197089222 ) ) ;
#502=CARTESIAN_POINT ( 'NONE',  ( 127.0150841466612093, -7.206988222280049428, -8.529861501223846787 ) ) ;
#503=CARTESIAN_POINT ( 'NONE',  ( 116.4834948109119779, -7.894159318335828068, -9.358103419637847864 ) ) ;
#504=CARTESIAN_POINT ( 'NONE',  ( 113.0798948109119948, -0.4660016031367893996, -10.09054647747474043 ) ) ;
#509=CARTESIAN_POINT ( 'NONE',  ( 118.2420214775786320, -6.222761293078241884, -8.102969835052219238 ) ) ;
#510=CARTESIAN_POINT ( 'NONE',  ( 112.9097148109120070, -9.565557343593413364, -10.61323700422348004 ) ) ;
#513=CARTESIAN_POINT ( 'NONE',  ( 125.7866681442452688, -8.899110576539710493, -16.42337572283490132 ) ) ;
#514=CARTESIAN_POINT ( 'NONE',  ( 125.3895814775786448, -2.084020599724406786, -8.691656652584148546 ) ) ;
#515=CARTESIAN_POINT ( 'NONE',  ( 112.4559014775786778, -0.1624402480850797581, -16.17319339645315424 ) ) ;
#516=ORIENTED_EDGE ( 'NONE', *, *, #914, .T. ) ;
#517=DIRECTION ( 'NONE',  ( -0.7071067811865480168, 0.5654279342906962658, 0.4246071727182139655 ) ) ;
#518=CARTESIAN_POINT ( 'NONE',  ( 112.6828081442453282, -7.893985811506177619, -18.51759400769804742 ) ) ;
#521=CARTESIAN_POINT ( 'NONE',  ( 124.8790414775786246, -8.899110576539710493, -16.42337572283490132 ) ) ;
#524=CARTESIAN_POINT ( 'NONE',  ( 117.9583881442453048, 0.1319031606808879209, -14.10382304977623669 ) ) ;
#525=CARTESIAN_POINT ( 'NONE',  ( 112.2857214775786474, -5.574606645277164318, -18.38911715685844683 ) ) ;
#530=CARTESIAN_POINT ( 'NONE',  ( 121.4178819144190129, -1.220279397241718966, -16.99638242193886484 ) ) ;
#535=CARTESIAN_POINT ( 'NONE',  ( 112.5693548109119888, -10.63000616557722466, -14.87417383870573495 ) ) ;
#536=CARTESIAN_POINT ( 'NONE',  ( 126.2972081442452890, -2.084020599724406786, -8.691656652584148546 ) ) ;
#537=CARTESIAN_POINT ( 'NONE',  ( 118.8092881442453290, -0.1624402480850797581, -16.17319339645315424 ) ) ;
#538=DIRECTION ( 'NONE',  ( 1.000000000000000000, 0.000000000000000000, -0.000000000000000000 ) ) ;
#540=CARTESIAN_POINT ( 'NONE',  ( 115.5758681442453053, -7.894159318335828068, -9.358103419637847864 ) ) ;
#544=CARTESIAN_POINT ( 'NONE',  ( 115.1787814775786387, -9.988377603198976828, -10.36322818467138340 ) ) ;
#546=CARTESIAN_POINT ( 'NONE',  ( 118.7525614775786380, -8.166667518702819706, -8.995218007635861213 ) ) ;
#547=CARTESIAN_POINT ( 'NONE',  ( 113.8740681442453138, 0.5811942927096102052, -14.16772938898808221 ) ) ;
#549=CARTESIAN_POINT ( 'NONE',  ( 111.7184548109119788, -9.261995988541697145, -16.69588392320189030 ) ) ;
#550=EDGE_CURVE ( 'NONE', #15771, #19842, #17806, .T. ) ;
#551=CARTESIAN_POINT ( 'NONE',  ( 114.5547881442453217, -5.638512984488999180, -18.83840828888717311 ) ) ;
#559=CARTESIAN_POINT ( 'NONE',  ( 116.8805814775786445, -3.505236298600246325, -18.68346056562440793 ) ) ;
#561=CARTESIAN_POINT ( 'NONE',  ( 122.7386537256648751, -1.063912429576147511, -17.20460841810472985 ) ) ;
#563=CARTESIAN_POINT ( 'NONE',  ( 126.5010429760476995, -4.770821923364382044, -8.252762481559532404 ) ) ;
#564=CARTESIAN_POINT ( 'NONE',  ( 111.3213681442453264, -7.643976991954077427, -18.09477374809248928 ) ) ;
#565=CARTESIAN_POINT ( 'NONE',  ( 135.7140458755418138, 1.062807768444411494, -12.64888035845507375 ) ) ;
#566=CARTESIAN_POINT ( 'NONE',  ( 122.8368814775786291, -1.561330072975668948, -17.79121239304076951 ) ) ;
#567=CARTESIAN_POINT ( 'NONE',  ( 117.4478481442453131, 0.2603800115204892296, -16.42320221600525088 ) ) ;
#569=CARTESIAN_POINT ( 'NONE',  ( 113.4769814775786330, 0.4262465694468514643, -12.03445270309931736 ) ) ;
#570=CARTESIAN_POINT ( 'NONE',  ( 125.7299414775786346, 0.9020085738987339008, -11.91225656197089222 ) ) ;
#571=CARTESIAN_POINT ( 'NONE',  ( 119.0361948109119652, -7.893985811506177619, -18.51759400769804742 ) ) ;
#573=CARTESIAN_POINT ( 'NONE',  ( 115.6325948109119821, -9.565557343593413364, -10.61323700422348004 ) ) ;
#575=CARTESIAN_POINT ( 'NONE',  ( 120.4543614775786295, -5.574606645277164318, -18.38911715685844683 ) ) ;
#576=CARTESIAN_POINT ( 'NONE',  ( 118.4122014775786340, 0.5811942927096110934, -14.16772938898807510 ) ) ;
#577=CARTESIAN_POINT ( 'NONE',  ( 137.2322813334390048, 0.1647898037908461233, -15.00067708421986978 ) ) ;
#578=B_SPLINE_CURVE_WITH_KNOTS ( 'NONE', 3,
 ( #44025, #9134, #33735, #2506, #13013, #26912, #37389, #6161, #17545, #41510, #31003, #21410, #14569, #34840, #207 ),
 .UNSPECIFIED., .F., .F.,
 ( 4, 2, 2, 1, 1, 1, 2, 2, 4 ),
 ( 0.000000000000000000, 0.2500000000000473510, 0.3750000000000788258, 0.4375000000001000311, 0.4687500000001022515, 0.4843750000001034173, 0.4921875000000962008, 0.5000000000000890399, 1.000000000000000000 ),
 .UNSPECIFIED. ) ;
#580=CARTESIAN_POINT ( 'NONE',  ( 114.2354127111058659, -1.267766418764742165, -16.93314635290707315 ) ) ;
#581=CARTESIAN_POINT ( 'NONE',  ( 126.5034829605236268, 0.2779052449522967372, -13.48229229357312597 ) ) ;
#583=CARTESIAN_POINT ( 'NONE',  ( 113.7038881442453402, -3.383040157471821630, -19.15922257007629170 ) ) ;
#585=CARTESIAN_POINT ( 'NONE',  ( 114.1009748109119784, -5.574606645277164318, -18.38911715685844683 ) ) ;
#590=CARTESIAN_POINT ( 'NONE',  ( 112.9664414775786412, -9.859900752359374465, -12.68260735090039404 ) ) ;
#593=CARTESIAN_POINT ( 'NONE',  ( 118.6391081442452986, -4.089484607189483256, -7.948022111789462052 ) ) ;
#594=CARTESIAN_POINT ( 'NONE',  ( 117.6747548109119919, -1.834011780172310813, -8.268836392978581529 ) ) ;
#595=CARTESIAN_POINT ( 'NONE',  ( 123.7445081442452874, -7.894159318335828068, -9.358103419637847864 ) ) ;
#596=CARTESIAN_POINT ( 'NONE',  ( 118.2420214775786320, -6.222761293078241884, -8.102969835052219238 ) ) ;
#597=CARTESIAN_POINT ( 'NONE',  ( 112.9664414775786412, -9.859900752359374465, -12.68260735090039404 ) ) ;
#599=CARTESIAN_POINT ( 'NONE',  ( 135.8497638153338585, -7.066639826094078813, -7.851922482749025711 ) ) ;
#600=CARTESIAN_POINT ( 'NONE',  ( 121.6456214775786293, -10.63000616557722466, -14.87417383870573495 ) ) ;
#602=CARTESIAN_POINT ( 'NONE',  ( 118.0718414775786442, -0.8288870151387760510, -10.36305467784173118 ) ) ;
#603=CARTESIAN_POINT ( 'NONE',  ( 114.1577014775786552, -3.505236298600246325, -18.68346056562440793 ) ) ;
#606=CARTESIAN_POINT ( 'NONE',  ( 121.0783548109119749, -9.565557343593413364, -10.61323700422348004 ) ) ;
#607=CARTESIAN_POINT ( 'NONE',  ( 123.1205148109119563, -7.643976991954077427, -18.09477374809248928 ) ) ;
#608=CARTESIAN_POINT ( 'NONE',  ( 114.6115148109119843, -6.222761293078232114, -8.102969835052212133 ) ) ;
#613=CARTESIAN_POINT ( 'NONE',  ( 118.0718414775786300, -9.261995988541697145, -16.69588392320189030 ) ) ;
#614=CARTESIAN_POINT ( 'NONE',  ( 116.5402214775786405, 0.2603800115204892296, -16.42320221600525088 ) ) ;
#616=EDGE_CURVE ( 'NONE', #38570, #22820, #35985, .T. ) ;
#617=CARTESIAN_POINT ( 'NONE',  ( 114.7816948109119863, 0.5811942927096154232, -14.16772938898807155 ) ) ;
#620=CARTESIAN_POINT ( 'NONE',  ( 124.0848681442452772, -4.089484607189486809, -7.948022111789456723 ) ) ;
#621=CARTESIAN_POINT ( 'NONE',  ( 117.0507614775786465, -10.30919188438810075, -12.61870101168855918 ) ) ;
#622=CARTESIAN_POINT ( 'NONE',  ( 122.8936081442453059, -9.565557343593413364, -10.61323700422348004 ) ) ;
#623=CARTESIAN_POINT ( 'NONE',  ( 112.0020881442453344, -9.565557343593413364, -10.61323700422348004 ) ) ;
#624=CARTESIAN_POINT ( 'NONE',  ( 121.5888948109119809, -10.30919188438810075, -12.61870101168855918 ) ) ;
#626=CARTESIAN_POINT ( 'NONE',  ( 116.3700414775786527, -4.153390946401321671, -8.397313243818183892 ) ) ;
#629=CARTESIAN_POINT ( 'NONE',  ( 120.5678148109119832, -8.166667518702819706, -8.995218007635861213 ) ) ;
#631=CARTESIAN_POINT ( 'NONE',  ( 121.0216281442452981, -1.561330072975668948, -17.79121239304076951 ) ) ;
#632=ORIENTED_EDGE ( 'NONE', *, *, #36066, .T. ) ;
#634=CARTESIAN_POINT ( 'NONE',  ( 125.7299414775786346, 0.9020085738987339008, -11.91225656197089222 ) ) ;
#635=CARTESIAN_POINT ( 'NONE',  ( 122.2128881442452979, -1.834011780172266848, -8.268836392978604621 ) ) ;
#636=CARTESIAN_POINT ( 'NONE',  ( 114.6115148109119986, -6.222761293078241884, -8.102969835052219238 ) ) ;
#638=CARTESIAN_POINT ( 'NONE',  ( 120.1707281442453166, -9.565557343593413364, -10.61323700422348004 ) ) ;
#640=CARTESIAN_POINT ( 'NONE',  ( 119.7736414775786358, 0.1319031606808879209, -14.10382304977623669 ) ) ;
#642=CARTESIAN_POINT ( 'NONE',  ( 117.9016614775786280, -0.1624402480850797581, -16.17319339645315424 ) ) ;
#643=CARTESIAN_POINT ( 'NONE',  ( 112.6260814775786514, -9.261995988541697145, -16.69588392320189030 ) ) ;
#644=CARTESIAN_POINT ( 'NONE',  ( 118.4689281442453392, 0.9020085738987339008, -11.91225656197089222 ) ) ;
#645=CARTESIAN_POINT ( 'NONE',  ( 111.8319081442453182, -5.638512984488999180, -18.83840828888717311 ) ) ;
#647=CARTESIAN_POINT ( 'NONE',  ( 120.4543614775786295, -5.574606645277164318, -18.38911715685844683 ) ) ;
#649=CARTESIAN_POINT ( 'NONE',  ( 117.6180281442453150, -0.4660016031367893996, -10.09054647747474043 ) ) ;
#651=CARTESIAN_POINT ( 'NONE',  ( 115.8595014775786609, -7.643976991954099631, -18.09477374809247152 ) ) ;
#655=CARTESIAN_POINT ( 'NONE',  ( 121.0783548109119749, 0.2603800115204892296, -16.42320221600525088 ) ) ;
#657=CARTESIAN_POINT ( 'NONE',  ( 118.7315769107182177, -2.467220198592778413, -17.83387418641524391 ) ) ;
#659=CARTESIAN_POINT ( 'NONE',  ( 122.8368814775786291, -7.894159318335828068, -9.358103419637847864 ) ) ;
#664=CARTESIAN_POINT ( 'NONE',  ( 114.6682414775786469, -1.561330072975668060, -17.79121239304076596 ) ) ;
#665=CARTESIAN_POINT ( 'NONE',  ( 125.1626748109119802, -0.1624402480850797581, -16.17319339645315424 ) ) ;
#667=CARTESIAN_POINT ( 'NONE',  ( 119.5467348109119712, -5.574606645277164318, -18.38911715685844683 ) ) ;
#668=CARTESIAN_POINT ( 'NONE',  ( 112.2857214775786474, -5.574606645277164318, -18.38911715685844683 ) ) ;
#669=CARTESIAN_POINT ( 'NONE',  ( 121.1918081442452859, 0.9020085738987339008, -11.91225656197089222 ) ) ;
#670=CARTESIAN_POINT ( 'NONE',  ( 112.0693548109120030, -10.10582367741923093, -14.73954123521778925 ) ) ;
#673=CARTESIAN_POINT ( 'NONE',  ( 125.5597614775786326, -7.894159318335828068, -9.358103419637847864 ) ) ;
#676=CARTESIAN_POINT ( 'NONE',  ( 121.9292548109119849, -1.561330072975668948, -17.79121239304076951 ) ) ;
#679=CARTESIAN_POINT ( 'NONE',  ( 136.9394333025986157, 0.1406925880472598978, -11.10009844214757813 ) ) ;
#680=CARTESIAN_POINT ( 'NONE',  ( 121.3619881442452879, -4.089484607189486809, -7.948022111789456723 ) ) ;
#681=DIRECTION ( 'NONE',  ( 1.000000000000000000, 0.000000000000000000, 0.000000000000000000 ) ) ;
#682=CARTESIAN_POINT ( 'NONE',  ( 123.1772414775786189, -5.574606645277164318, -18.38911715685844683 ) ) ;
#684=CARTESIAN_POINT ( 'NONE',  ( 114.2144281442453178, -8.166667518702817929, -8.995218007635859436 ) ) ;
#687=CARTESIAN_POINT ( 'NONE',  ( 120.2841814775786276, 0.9020085738987414503, -11.91225656197092242 ) ) ;
#689=CARTESIAN_POINT ( 'NONE',  ( 126.0135748109119902, -8.166667518702819706, -8.995218007635861213 ) ) ;
#692=CARTESIAN_POINT ( 'NONE',  ( 123.6877814775786533, -3.383040157471821630, -19.15922257007629170 ) ) ;
#693=CARTESIAN_POINT ( 'NONE',  ( 123.1205148109119563, -1.834011780172310813, -8.268836392978581529 ) ) ;
#694=CARTESIAN_POINT ( 'NONE',  ( 122.0427081442452817, -9.859900752359378018, -12.68260735090039759 ) ) ;
#695=CARTESIAN_POINT ( 'NONE',  ( 119.4900081442453086, -7.643976991954077427, -18.09477374809248928 ) ) ;
#697=CARTESIAN_POINT ( 'NONE',  ( 120.3409081442453044, -0.4660016031367893996, -10.09054647747474043 ) ) ;
#705=CARTESIAN_POINT ( 'NONE',  ( 124.9357681442453014, -1.834011780172310813, -8.268836392978581529 ) ) ;
#706=CARTESIAN_POINT ( 'NONE',  ( 125.7866681442452688, -8.899110576539710493, -16.42337572283490132 ) ) ;
#708=CARTESIAN_POINT ( 'NONE',  ( 111.7184548109119788, -0.8288870151387760510, -10.36305467784173118 ) ) ;
#711=CARTESIAN_POINT ( 'NONE',  ( 125.3895814775786448, -7.893985811506177619, -18.51759400769804742 ) ) ;
#713=CARTESIAN_POINT ( 'NONE',  ( 116.8238548109119819, -4.089484607189486809, -7.948022111789456723 ) ) ;
#718=CARTESIAN_POINT ( 'NONE',  ( 115.6325948109119821, -9.565557343593413364, -10.61323700422348004 ) ) ;
#719=CARTESIAN_POINT ( 'NONE',  ( 112.7962614775786676, -3.383040157471821630, -19.15922257007629170 ) ) ;
#722=CARTESIAN_POINT ( 'NONE',  ( 118.0718414775786442, -0.8288870151387542906, -10.36305467784175782 ) ) ;
#723=CARTESIAN_POINT ( 'NONE',  ( 121.2485348109119769, -8.899110576539710493, -16.42337572283490132 ) ) ;
#724=CARTESIAN_POINT ( 'NONE',  ( 115.9162281442453093, -5.574606645277164318, -18.38911715685844683 ) ) ;
#725=ORIENTED_EDGE ( 'NONE', *, *, #4716, .T. ) ;
#728=CARTESIAN_POINT ( 'NONE',  ( 121.6115542554890823, -2.372251574601201174, -17.96033910819751611 ) ) ;
#729=CARTESIAN_POINT ( 'NONE',  ( 112.2857214775786474, -5.574606645277164318, -18.38911715685844683 ) ) ;
#734=CARTESIAN_POINT ( 'NONE',  ( 113.0231681442453180, -10.15424416112533912, -14.75197769757731336 ) ) ;
#736=EDGE_LOOP ( 'NONE', ( #25087, #5555, #41613, #11878, #12693, #17378, #19659, #35868, #19138, #20829, #22693, #7077, #26268, #39578, #22712, #14892, #27175, #41481, #36545, #23506, #11620, #21726, #7317, #13984, #8190, #40680, #34034, #25489, #21906, #8484, #12745, #23708, #757, #38515, #7628, #13878, #11265, #4610, #632, #28496, #3732, #17194, #21188, #31683, #31251 ) ) ;
#737=CARTESIAN_POINT ( 'NONE',  ( 118.4689281442453392, -10.15424416112533912, -14.75197769757731336 ) ) ;
#738=CARTESIAN_POINT ( 'NONE',  ( 118.4689281442453250, -10.15424416112533912, -14.75197769757731336 ) ) ;
#743=CYLINDRICAL_SURFACE ( 'NONE', #3356, 5.999999999999997335 ) ;
#746=CARTESIAN_POINT ( 'NONE',  ( 112.1722681442453222, -0.4660016031367893996, -10.09054647747474043 ) ) ;
#747=CARTESIAN_POINT ( 'NONE',  ( 113.1933481442453058, -4.089484607189486809, -7.948022111789456723 ) ) ;
#748=CARTESIAN_POINT ( 'NONE',  ( 117.4478481442453131, -9.565557343593413364, -10.61323700422348004 ) ) ;
#749=CARTESIAN_POINT ( 'NONE',  ( 138.2184548109119930, -4.863998795840020151, -13.39321520033889890 ) ) ;
#751=CARTESIAN_POINT ( 'NONE',  ( 117.9016614775786280, -0.1624402480850797581, -16.17319339645315424 ) ) ;
#754=CARTESIAN_POINT ( 'NONE',  ( 125.1533364939176636, -1.283731733903592076, -16.91188614879543906 ) ) ;
#756=CARTESIAN_POINT ( 'NONE',  ( 115.5758681442453053, -1.561330072975668060, -17.79121239304076951 ) ) ;
#757=ORIENTED_EDGE ( 'NONE', *, *, #19062, .F. ) ;
#759=CARTESIAN_POINT ( 'NONE',  ( 118.8660148109119774, -10.30919188438810075, -12.61870101168855918 ) ) ;
#762=CARTESIAN_POINT ( 'NONE',  ( 116.0864081442453113, -9.988377603198976828, -10.36322818467138340 ) ) ;
#763=CARTESIAN_POINT ( 'NONE',  ( 113.4202548109119846, -10.30919188438810075, -12.61870101168855918 ) ) ;
#767=EDGE_CURVE ( 'NONE', #10224, #32004, #15058, .T. ) ;
#771=CARTESIAN_POINT ( 'NONE',  ( 115.1787814775786387, -0.1624402480850797581, -16.17319339645315424 ) ) ;
#773=CARTESIAN_POINT ( 'NONE',  ( 118.1852948109119836, -5.638512984489023161, -18.83840828888716601 ) ) ;
#775=CARTESIAN_POINT ( 'NONE',  ( 126.5254139958991431, -4.795709975826312643, -8.240175154163296156 ) ) ;
#776=CARTESIAN_POINT ( 'NONE',  ( 114.4413348109119823, -0.8288870151387760510, -10.36305467784173118 ) ) ;
#777=CARTESIAN_POINT ( 'NONE',  ( 135.8582226017265384, 1.040662781756023447, -12.66189764563367604 ) ) ;
#778=EDGE_CURVE ( 'NONE', #21905, #21031, #9632, .T. ) ;
#779=CARTESIAN_POINT ( 'NONE',  ( 122.3830681442452857, -8.166667518702819706, -8.995218007635861213 ) ) ;
#780=CARTESIAN_POINT ( 'NONE',  ( 119.3765548109119834, 0.9020085738987339008, -11.91225656197089222 ) ) ;
#783=CARTESIAN_POINT ( 'NONE',  ( 116.6536748109119941, -10.15424416112533912, -14.75197769757731336 ) ) ;
#784=CARTESIAN_POINT ( 'NONE',  ( 112.6828081442453282, -7.893985811506177619, -18.51759400769804742 ) ) ;
#786=CARTESIAN_POINT ( 'NONE',  ( 117.0507614775786465, -10.30919188438810075, -12.61870101168855918 ) ) ;
#787=CARTESIAN_POINT ( 'NONE',  ( 119.4900081442453086, -7.643976991954077427, -18.09477374809248928 ) ) ;
#789=CARTESIAN_POINT ( 'NONE',  ( 121.3052614775786111, -7.643976991954077427, -18.09477374809248928 ) ) ;
#792=CARTESIAN_POINT ( 'NONE',  ( 119.8303681442453126, -10.63000616557722466, -14.87417383870573495 ) ) ;
#797=EDGE_CURVE ( 'NONE', #37424, #32220, #29734, .T. ) ;
#798=EDGE_CURVE ( 'NONE', #38024, #6756, #5259, .T. ) ;
#802=CARTESIAN_POINT ( 'NONE',  ( 113.9875214775786532, -0.4660016031367893996, -10.09054647747474043 ) ) ;
#804=CARTESIAN_POINT ( 'NONE',  ( 116.8238548109119819, -5.574606645277164318, -18.38911715685844683 ) ) ;
#808=CARTESIAN_POINT ( 'NONE',  ( 112.2289948109119848, -7.643976991954077427, -18.09477374809248928 ) ) ;
#813=CARTESIAN_POINT ( 'NONE',  ( 117.6180281442453150, -0.4660016031367893996, -10.09054647747474043 ) ) ;
#814=CARTESIAN_POINT ( 'NONE',  ( 117.9583881442453048, 0.1319031606808879209, -14.10382304977623669 ) ) ;
#815=CARTESIAN_POINT ( 'NONE',  ( 125.5030348109119558, -3.383040157471821630, -19.15922257007629170 ) ) ;
#817=CARTESIAN_POINT ( 'NONE',  ( 136.9115742440160659, -9.061375133822513916, -9.797515867730091088 ) ) ;
#818=CARTESIAN_POINT ( 'NONE',  ( 123.8012348109119642, 0.2603800115204892296, -16.42320221600525088 ) ) ;
#820=CARTESIAN_POINT ( 'NONE',  ( 119.7736414775786358, 0.1319031606808879209, -14.10382304977623669 ) ) ;
#821=CARTESIAN_POINT ( 'NONE',  ( 115.7460481442453357, -10.15424416112533912, -14.75197769757731336 ) ) ;
#824=CARTESIAN_POINT ( 'NONE',  ( 119.3765548109119834, -10.15424416112533912, -14.75197769757731336 ) ) ;
#826=CARTESIAN_POINT ( 'NONE',  ( 124.8790414775786246, -8.899110576539710493, -16.42337572283490132 ) ) ;
#827=CARTESIAN_POINT ( 'NONE',  ( 114.8384214775786489, -10.15424416112534267, -14.75197769757730804 ) ) ;
#833=CARTESIAN_POINT ( 'NONE',  ( 118.8660148109119774, -10.30919188438810075, -12.61870101168855918 ) ) ;
#834=CARTESIAN_POINT ( 'NONE',  ( 118.2420214775786320, -3.383040157471821630, -19.15922257007629170 ) ) ;
#836=CARTESIAN_POINT ( 'NONE',  ( 112.5693548109119888, -10.63000616557722466, -14.87417383870573495 ) ) ;
#839=CARTESIAN_POINT ( 'NONE',  ( 115.5758681442453053, -1.561330072975668060, -17.79121239304076951 ) ) ;
#840=CARTESIAN_POINT ( 'NONE',  ( 120.3409081442453044, -8.899110576539710493, -16.42337572283490132 ) ) ;
#842=CARTESIAN_POINT ( 'NONE',  ( 124.7088614775786226, 0.2603800115204892296, -16.42320221600525088 ) ) ;
#843=CARTESIAN_POINT ( 'NONE',  ( 121.1918081442452859, 0.9020085738987339008, -11.91225656197089222 ) ) ;
#844=EDGE_CURVE ( 'NONE', #21157, #21529, #40068, .T. ) ;
#846=CARTESIAN_POINT ( 'NONE',  ( 117.6180281442453150, -8.899110576539710493, -16.42337572283490132 ) ) ;
#851=EDGE_CURVE ( 'NONE', #28482, #19616, #5453, .T. ) ;
#853=CARTESIAN_POINT ( 'NONE',  ( 120.3976348109119812, -1.834011780172310813, -8.268836392978581529 ) ) ;
#856=CARTESIAN_POINT ( 'NONE',  ( 128.0511146350389993, -7.187744967641459759, -18.83419938739690025 ) ) ;
#859=CARTESIAN_POINT ( 'NONE',  ( 117.1642148109119859, -0.8288870151387760510, -10.36305467784173118 ) ) ;
#863=CARTESIAN_POINT ( 'NONE',  ( 119.6601881442453106, -1.833838273342659253, -17.42832698103878286 ) ) ;
#864=CARTESIAN_POINT ( 'NONE',  ( 121.5888948109119809, -10.30919188438809364, -12.61870101168852187 ) ) ;
#865=CARTESIAN_POINT ( 'NONE',  ( 123.0070614775786169, -10.15424416112533912, -14.75197769757731336 ) ) ;
#867=CARTESIAN_POINT ( 'NONE',  ( 118.7525614775786380, -1.833838273342659253, -17.42832698103878286 ) ) ;
#868=CARTESIAN_POINT ( 'NONE',  ( 114.8384214775786489, 0.9020085738987339008, -11.91225656197089222 ) ) ;
#869=CARTESIAN_POINT ( 'NONE',  ( 120.6812681442452941, -10.30919188438810075, -12.61870101168855918 ) ) ;
#870=CARTESIAN_POINT ( 'NONE',  ( 112.1722681442453222, -0.4660016031367893996, -10.09054647747474043 ) ) ;
#872=CARTESIAN_POINT ( 'NONE',  ( 120.2274548109119934, -9.859900752359374465, -12.68260735090039404 ) ) ;
#874=CARTESIAN_POINT ( 'NONE',  ( 122.0427081442452817, 0.5811942927096110934, -14.16772938898807510 ) ) ;
#881=ORIENTED_EDGE ( 'NONE', *, *, #16520, .F. ) ;
#883=CARTESIAN_POINT ( 'NONE',  ( 123.2906948109119867, -1.833838273342659697, -17.42832698103878286 ) ) ;
#888=ORIENTED_EDGE ( 'NONE', *, *, #41925, .F. ) ;
#889=CARTESIAN_POINT ( 'NONE',  ( 113.6471614775786492, -5.638512984488999180, -18.83840828888717311 ) ) ;
#891=CARTESIAN_POINT ( 'NONE',  ( 114.6682414775786469, -1.561330072975668060, -17.79121239304076596 ) ) ;
#893=CARTESIAN_POINT ( 'NONE',  ( 122.3263414775786373, -3.505236298600246325, -18.68346056562440793 ) ) ;
#894=CARTESIAN_POINT ( 'NONE',  ( 126.2471382750707818, -3.957262863412609022, -8.461457090771025591 ) ) ;
#896=CARTESIAN_POINT ( 'NONE',  ( 122.8368814775786291, -1.561330072975668948, -17.79121239304076951 ) ) ;
#900=CARTESIAN_POINT ( 'NONE',  ( 112.2289948109119848, -1.834011780172310813, -8.268836392978581529 ) ) ;
#904=CARTESIAN_POINT ( 'NONE',  ( 118.8092881442453290, -9.988377603198976828, -10.36322818467138340 ) ) ;
#908=CARTESIAN_POINT ( 'NONE',  ( 111.3780948109119890, -5.574606645277164318, -18.38911715685844683 ) ) ;
#911=CARTESIAN_POINT ( 'NONE',  ( 121.9859814775786333, -9.565557343593413364, -10.61323700422348004 ) ) ;
#912=ORIENTED_EDGE ( 'NONE', *, *, #22583, .T. ) ;
#913=CARTESIAN_POINT ( 'NONE',  ( 116.6536748109119941, 0.9020085738987339008, -11.91225656197089222 ) ) ;
#914=EDGE_CURVE ( 'NONE', #29459, #28588, #42750, .T. ) ;
#916=CARTESIAN_POINT ( 'NONE',  ( 112.7156220163423512, -1.087735405160637603, -17.17288456429614030 ) ) ;
#919=CARTESIAN_POINT ( 'NONE',  ( 111.3780948109119890, -5.574606645277164318, -18.38911715685844683 ) ) ;
#920=DIRECTION ( 'NONE',  ( 0.000000000000000000, -0.6004852223388327248, 0.7996358532186277346 ) ) ;
#922=CARTESIAN_POINT ( 'NONE',  ( 125.2761281442453054, -10.63000616557722466, -14.87417383870573495 ) ) ;
#923=CARTESIAN_POINT ( 'NONE',  ( 124.0848681442452772, -4.089484607189486809, -7.948022111789456723 ) ) ;
#924=CARTESIAN_POINT ( 'NONE',  ( 122.2696148109119889, -5.574606645277164318, -18.38911715685844683 ) ) ;
#926=CARTESIAN_POINT ( 'NONE',  ( 122.0427081442452817, -9.859900752359378018, -12.68260735090039759 ) ) ;
#927=CARTESIAN_POINT ( 'NONE',  ( 113.6471614775786492, -4.153390946401321671, -8.397313243818183892 ) ) ;
#928=CARTESIAN_POINT ( 'NONE',  ( 120.6812681442452941, -10.30919188438810075, -12.61870101168855918 ) ) ;
#929=ORIENTED_EDGE ( 'NONE', *, *, #41606, .T. ) ;
#936=CARTESIAN_POINT ( 'NONE',  ( 126.0135748109119902, -8.166667518702819706, -8.995218007635861213 ) ) ;
#937=CARTESIAN_POINT ( 'NONE',  ( 114.3278814775786429, -10.30919188438810075, -12.61870101168855918 ) ) ;
#939=CARTESIAN_POINT ( 'NONE',  ( 111.5482748109120053, -0.1624402480850797581, -16.17319339645315424 ) ) ;
#941=CARTESIAN_POINT ( 'NONE',  ( 122.0427081442452817, -9.859900752359374465, -12.68260735090038693 ) ) ;
#945=CARTESIAN_POINT ( 'NONE',  ( 115.8027748109119841, -0.4660016031367893996, -10.09054647747474043 ) ) ;
#949=ORIENTED_EDGE ( 'NONE', *, *, #17087, .T. ) ;
#950=CARTESIAN_POINT ( 'NONE',  ( 126.2184548109105435, -7.866424907533402511, -9.395035934245175469 ) ) ;
#951=CARTESIAN_POINT ( 'NONE',  ( 117.5045748109119756, -9.859900752359374465, -12.68260735090039404 ) ) ;
#953=CARTESIAN_POINT ( 'NONE',  ( 116.7104014775786425, -0.4660016031367893996, -10.09054647747474043 ) ) ;
#954=CARTESIAN_POINT ( 'NONE',  ( 113.5904348109119866, -7.893985811506177619, -18.51759400769804742 ) ) ;
#955=CARTESIAN_POINT ( 'NONE',  ( 125.1059481442452750, -1.833838273342660141, -17.42832698103878286 ) ) ;
#957=CARTESIAN_POINT ( 'NONE',  ( 120.6245414775786458, -0.1624402480850797581, -16.17319339645315424 ) ) ;
#958=CARTESIAN_POINT ( 'NONE',  ( 117.4478481442453131, -9.565557343593413364, -10.61323700422348004 ) ) ;
#962=CARTESIAN_POINT ( 'NONE',  ( 111.7184548109119788, -9.142054238649166109, -15.98131134002176523 ) ) ;
#963=CARTESIAN_POINT ( 'NONE',  ( 116.8805814775786445, -3.505236298600246325, -18.68346056562440793 ) ) ;
#966=CARTESIAN_POINT ( 'NONE',  ( 115.5191414775786569, -3.383040157471821630, -19.15922257007629170 ) ) ;
#968=CARTESIAN_POINT ( 'NONE',  ( 114.2144281442453178, -1.833838273342658809, -17.42832698103878286 ) ) ;
#971=CARTESIAN_POINT ( 'NONE',  ( 123.9146881442452894, -10.15424416112533912, -14.75197769757731336 ) ) ;
#972=EDGE_CURVE ( 'NONE', #3055, #38119, #11731, .T. ) ;
#973=CARTESIAN_POINT ( 'NONE',  ( 116.3700414775786527, -4.153390946401321671, -8.397313243818183892 ) ) ;
#974=CARTESIAN_POINT ( 'NONE',  ( 110.2184548109119788, -3.104384172016180887, -16.98539509221845734 ) ) ;
#976=ORIENTED_EDGE ( 'NONE', *, *, #851, .T. ) ;
#982=CARTESIAN_POINT ( 'NONE',  ( 111.8319081442453182, -5.638512984488999180, -18.83840828888717311 ) ) ;
#983=CARTESIAN_POINT ( 'NONE',  ( 112.8529881442453302, -1.561330072975668060, -17.79121239304076596 ) ) ;
#984=CARTESIAN_POINT ( 'NONE',  ( 122.6667014775786413, -2.084020599724406786, -8.691656652584148546 ) ) ;
#985=FACE_OUTER_BOUND ( 'NONE', #8311, .T. ) ;
#987=CARTESIAN_POINT ( 'NONE',  ( 119.6601881442453106, -1.833838273342659253, -17.42832698103878286 ) ) ;
#992=CARTESIAN_POINT ( 'NONE',  ( 113.8740681442453138, 0.5811942927096154232, -14.16772938898807155 ) ) ;
#994=CARTESIAN_POINT ( 'NONE',  ( 118.1852948109119836, -5.638512984488999180, -18.83840828888717311 ) ) ;
#995=CARTESIAN_POINT ( 'NONE',  ( 114.0442481442453300, -1.834011780172303929, -8.268836392978592187 ) ) ;
#997=CARTESIAN_POINT ( 'NONE',  ( 115.8027748109119841, -0.4660016031367893996, -10.09054647747474043 ) ) ;
#998=CARTESIAN_POINT ( 'NONE',  ( 117.4478481442453131, 0.2603800115204892296, -16.42320221600525088 ) ) ;
#999=CARTESIAN_POINT ( 'NONE',  ( 127.4620922276734092, -10.46289306240577588, -13.90154686030524189 ) ) ;
#1003=LINE ( 'NONE', #43187, #23766 ) ;
#1005=CARTESIAN_POINT ( 'NONE',  ( 118.9794681442453026, -0.8288870151387760510, -10.36305467784173118 ) ) ;
#1009=CARTESIAN_POINT ( 'NONE',  ( 126.3975136127440919, -4.653777249196778598, -8.307659966040843003 ) ) ;
#1010=CARTESIAN_POINT ( 'NONE',  ( 113.9307948109119764, -10.15424416112533912, -14.75197769757731336 ) ) ;
#1012=CARTESIAN_POINT ( 'NONE',  ( 122.5532481442453019, -10.63000616557722466, -14.87417383870573495 ) ) ;
#1013=CARTESIAN_POINT ( 'NONE',  ( 120.0572748109119772, -3.383040157471821630, -19.15922257007629170 ) ) ;
#1015=CARTESIAN_POINT ( 'NONE',  ( 119.8303681442453126, 0.4262465694468514643, -12.03445270309931736 ) ) ;
#1016=CARTESIAN_POINT ( 'NONE',  ( 125.9568481442452850, -6.344957434206665248, -7.627207830600338134 ) ) ;
#1017=CARTESIAN_POINT ( 'NONE',  ( 116.8805814775786445, -6.344957434206662583, -7.627207830600332805 ) ) ;
#1018=CARTESIAN_POINT ( 'NONE',  ( 120.3976348109119812, -7.643976991954077427, -18.09477374809248928 ) ) ;
#1020=CARTESIAN_POINT ( 'NONE',  ( 125.2194014775786286, 0.1319031606808879209, -14.10382304977623669 ) ) ;
#1021=CARTESIAN_POINT ( 'NONE',  ( 121.9859814775786333, 0.2603800115204892296, -16.42320221600525088 ) ) ;
#1028=CARTESIAN_POINT ( 'NONE',  ( 116.8805814775786445, -6.344957434206662583, -7.627207830600332805 ) ) ;
#1029=CARTESIAN_POINT ( 'NONE',  ( 137.4945747549981547, -9.790276493893014020, -12.42916563457901269 ) ) ;
#1030=CARTESIAN_POINT ( 'NONE',  ( 117.3343948109119737, -6.222761293078241884, -8.102969835052219238 ) ) ;
#1031=CARTESIAN_POINT ( 'NONE',  ( 126.2333338125975217, -0.7732851963037252752, -10.50508471548512190 ) ) ;
#1032=CARTESIAN_POINT ( 'NONE',  ( 117.3911214775786505, -7.894159318335806752, -9.358103419637833653 ) ) ;
#1034=CARTESIAN_POINT ( 'NONE',  ( 113.2500748109119968, -3.505236298600246325, -18.68346056562440793 ) ) ;
#1036=CARTESIAN_POINT ( 'NONE',  ( 111.6276609221557550, -2.372251574601221158, -17.96033910819751966 ) ) ;
#1038=CARTESIAN_POINT ( 'NONE',  ( 119.4900081442453086, -1.834011780172310813, -8.268836392978581529 ) ) ;
#1039=B_SPLINE_CURVE_WITH_KNOTS ( 'NONE', 3,
 ( #24514, #35194, #31789, #561, #42073, #10831, #7621, #32236, #7172, #14471 ),
 .UNSPECIFIED., .F., .F.,
 ( 4, 3, 3, 4 ),
 ( 0.000000000000000000, 0.0001671877560958060112, 0.0003343755126086500086, 0.0006438490228505489759 ),
 .UNSPECIFIED. ) ;
#1040=CARTESIAN_POINT ( 'NONE',  ( 119.2063748109119814, -7.894159318335828068, -9.358103419637847864 ) ) ;
#1041=CARTESIAN_POINT ( 'NONE',  ( 112.7395348109119766, -4.153390946401321671, -8.397313243818183892 ) ) ;
#1044=CARTESIAN_POINT ( 'NONE',  ( 121.5321681442453183, -9.988377603198976828, -10.36322818467138340 ) ) ;
#1046=CARTESIAN_POINT ( 'NONE',  ( 118.2420214775786320, -6.222761293078241884, -8.102969835052219238 ) ) ;
#1048=CARTESIAN_POINT ( 'NONE',  ( 116.3133148109120043, -2.084020599724406786, -8.691656652584148546 ) ) ;
#1051=CARTESIAN_POINT ( 'NONE',  ( 123.2339681442453241, -3.505236298600246325, -18.68346056562440793 ) ) ;
#1052=CARTESIAN_POINT ( 'NONE',  ( 122.3263414775786373, -3.505236298600246325, -18.68346056562440793 ) ) ;
#1053=CARTESIAN_POINT ( 'NONE',  ( 114.7816948109119863, -9.859900752359374465, -12.68260735090037983 ) ) ;
#1060=CARTESIAN_POINT ( 'NONE',  ( 116.1998614775786507, -10.63000616557722466, -14.87417383870573495 ) ) ;
#1061=CARTESIAN_POINT ( 'NONE',  ( 117.7314814775786260, -4.089484607189486809, -7.948022111789456723 ) ) ;
#1063=CARTESIAN_POINT ( 'NONE',  ( 112.7962614775786676, -3.383040157471821630, -19.15922257007629170 ) ) ;
#1069=CARTESIAN_POINT ( 'NONE',  ( 115.5191414775786569, -3.383040157471821630, -19.15922257007629170 ) ) ;
#1070=CARTESIAN_POINT ( 'NONE',  ( 123.5743281442453139, -2.084020599724406786, -8.691656652584148546 ) ) ;
#1072=CARTESIAN_POINT ( 'NONE',  ( 124.6521348109119884, -1.561330072975668948, -17.79121239304076951 ) ) ;
#1073=CARTESIAN_POINT ( 'NONE',  ( 121.2485348109119769, -0.4660016031367893996, -10.09054647747474043 ) ) ;
#1076=CARTESIAN_POINT ( 'NONE',  ( 118.0718414775786442, -0.8288870151387760510, -10.36305467784173118 ) ) ;
#1081=CARTESIAN_POINT ( 'NONE',  ( 119.7736414775786358, -10.30919188438810075, -12.61870101168855918 ) ) ;
#1085=CARTESIAN_POINT ( 'NONE',  ( 121.9100498793805230, -2.191907684172563986, -18.20049396185734025 ) ) ;
#1086=CARTESIAN_POINT ( 'NONE',  ( 115.7460481442453357, -10.15424416112533912, -14.75197769757731336 ) ) ;
#1089=CARTESIAN_POINT ( 'NONE',  ( 123.1205148109119563, -7.643976991954077427, -18.09477374809248928 ) ) ;
#1091=CARTESIAN_POINT ( 'NONE',  ( 121.0783548109119749, -9.565557343593413364, -10.61323700422348004 ) ) ;
#1094=CARTESIAN_POINT ( 'NONE',  ( 123.5743281442453139, -2.084020599724406786, -8.691656652584148546 ) ) ;
#1095=CARTESIAN_POINT ( 'NONE',  ( 112.7962614775786676, -3.383040157471821630, -19.15922257007629170 ) ) ;
#1096=CARTESIAN_POINT ( 'NONE',  ( 117.6747548109119919, -1.834011780172310813, -8.268836392978581529 ) ) ;
#1097=CARTESIAN_POINT ( 'NONE',  ( 125.5597614775786326, -7.894159318335828068, -9.358103419637847864 ) ) ;
#1100=CARTESIAN_POINT ( 'NONE',  ( 121.0783548109119749, -9.565557343593413364, -10.61323700422348004 ) ) ;
#1102=CARTESIAN_POINT ( 'NONE',  ( 120.3409081442453044, -0.4660016031367893996, -10.09054647747474043 ) ) ;
#1109=CARTESIAN_POINT ( 'NONE',  ( 121.4754414775786131, -1.833838273342659697, -17.42832698103878286 ) ) ;
#1116=CARTESIAN_POINT ( 'NONE',  ( 114.7816948109119863, 0.5811942927096154232, -14.16772938898807155 ) ) ;
#1118=CARTESIAN_POINT ( 'NONE',  ( 120.8514481442452961, -2.084020599724406786, -8.691656652584148546 ) ) ;
#1119=CARTESIAN_POINT ( 'NONE',  ( 112.5126281442453120, 0.1319031606808879209, -14.10382304977623669 ) ) ;
#1120=CARTESIAN_POINT ( 'NONE',  ( 123.8012348109119785, -9.565557343593409811, -10.61323700422347649 ) ) ;
#1127=B_SPLINE_CURVE_WITH_KNOTS ( 'NONE', 3,
 ( #18016, #8205, #28064, #17795, #21663, #18476, #15050, #10739, #18244, #25088 ),
 .UNSPECIFIED., .F., .F.,
 ( 4, 3, 3, 4 ),
 ( 0.000000000000000000, 0.0001671877560958114864, 0.0003343755126086585196, 0.0006438490228507209303 ),
 .UNSPECIFIED. ) ;
#1128=CARTESIAN_POINT ( 'NONE',  ( 122.1561614775786353, -0.4660016031367893996, -10.09054647747474043 ) ) ;
#1129=CARTESIAN_POINT ( 'NONE',  ( 137.3802547664382985, -9.320531758105950360, -15.95367587447831248 ) ) ;
#1132=CARTESIAN_POINT ( 'NONE',  ( 125.3328548109119964, -9.261995988541697145, -16.69588392320189030 ) ) ;
#1134=CARTESIAN_POINT ( 'NONE',  ( 127.0400190879707480, -4.559358201214624096, -18.79541519429530538 ) ) ;
#1135=CARTESIAN_POINT ( 'NONE',  ( 124.9924948109119924, -5.574606645277164318, -18.38911715685844683 ) ) ;
#1137=CARTESIAN_POINT ( 'NONE',  ( 116.3700414775786527, -5.638512984488999180, -18.83840828888717311 ) ) ;
#1138=B_SPLINE_CURVE_WITH_KNOTS ( 'NONE', 3,
 ( #17671, #28612, #42521, #11282, #39316, #7174, #21084, #21986, #4646, #31567 ),
 .UNSPECIFIED., .F., .F.,
 ( 4, 3, 3, 4 ),
 ( 0.000000000000000000, 0.0001671877560958085049, 0.0003343755126086540201, 0.0006438490228505489759 ),
 .UNSPECIFIED. ) ;
#1139=PLANE ( 'NONE',  #37208 ) ;
#1141=CARTESIAN_POINT ( 'NONE',  ( 135.8419766445523464, -5.597291064638494795, -7.485280051629364273 ) ) ;
#1142=CARTESIAN_POINT ( 'NONE',  ( 125.1626748109119802, -9.988377603198980381, -10.36322818467138518 ) ) ;
#1146=CARTESIAN_POINT ( 'NONE',  ( 111.9453614775786434, -7.894159318335828068, -9.358103419637847864 ) ) ;
#1147=CARTESIAN_POINT ( 'NONE',  ( 124.6521348109119884, -7.894159318335828068, -9.358103419637847864 ) ) ;
#1149=CARTESIAN_POINT ( 'NONE',  ( 123.8012348109119642, -9.565557343593413364, -10.61323700422348004 ) ) ;
#1151=CARTESIAN_POINT ( 'NONE',  ( 120.9081748109119872, -5.638512984488999180, -18.83840828888717311 ) ) ;
#1159=CARTESIAN_POINT ( 'NONE',  ( 126.2597653975822709, -9.794341843349942067, -12.44453272831780311 ) ) ;
#1160=CARTESIAN_POINT ( 'NONE',  ( 114.3846081442453197, -10.63000616557722466, -14.87417383870573495 ) ) ;
#1162=CARTESIAN_POINT ( 'NONE',  ( 112.3991748109119868, -1.833838273342658809, -17.42832698103878286 ) ) ;
#1165=CARTESIAN_POINT ( 'NONE',  ( 112.3991748109119868, -1.833838273342658809, -17.42832698103878286 ) ) ;
#1170=CARTESIAN_POINT ( 'NONE',  ( 115.6325948109119821, 0.2603800115204892296, -16.42320221600525088 ) ) ;
#1174=CARTESIAN_POINT ( 'NONE',  ( 126.9733055311805856, -7.218567762708847368, -8.558672424457089534 ) ) ;
#1175=CARTESIAN_POINT ( 'NONE',  ( 118.9227414775786542, 0.4262465694468514643, -12.03445270309931736 ) ) ;
#1176=CARTESIAN_POINT ( 'NONE',  ( 114.8384214775786489, 0.9020085738987339008, -11.91225656197089222 ) ) ;
#1177=EDGE_CURVE ( 'NONE', #1359, #5980, #25246, .T. ) ;
#1180=CARTESIAN_POINT ( 'NONE',  ( 111.7184548109119788, -9.261995988541697145, -16.69588392320189030 ) ) ;
#1181=CARTESIAN_POINT ( 'NONE',  ( 124.7655881442452852, -9.859900752359378018, -12.68260735090039759 ) ) ;
#1182=CARTESIAN_POINT ( 'NONE',  ( 123.1205148109119563, -7.643976991954077427, -18.09477374809248928 ) ) ;
#1183=CARTESIAN_POINT ( 'NONE',  ( 114.8951481442453115, -8.899110576539710493, -16.42337572283490132 ) ) ;
#1189=CARTESIAN_POINT ( 'NONE',  ( 118.1285681442453068, -2.084020599724406786, -8.691656652584148546 ) ) ;
#1190=ORIENTED_EDGE ( 'NONE', *, *, #8994, .T. ) ;
#1192=CARTESIAN_POINT ( 'NONE',  ( 114.9518748109119883, -1.834011780172310813, -8.268836392978581529 ) ) ;
#1194=CARTESIAN_POINT ( 'NONE',  ( 119.1472854349294579, -1.040089454026966287, -17.23633227186632766 ) ) ;
#1197=CARTESIAN_POINT ( 'NONE',  ( 122.7234281442452755, -4.153390946401325223, -8.397313243818185668 ) ) ;
#1198=CARTESIAN_POINT ( 'NONE',  ( 116.7671281442453335, -7.643976991954077427, -18.09477374809248928 ) ) ;
#1200=VECTOR ( 'NONE', #23710, 1000.000000000000114 ) ;
#1202=VERTEX_POINT ( 'NONE', #11813 ) ;
#1207=CARTESIAN_POINT ( 'NONE',  ( 114.1577014775786552, -6.344957434206662583, -7.627207830600332805 ) ) ;
#1208=CARTESIAN_POINT ( 'NONE',  ( 126.0703014775786102, -0.1624402480850797581, -16.17319339645315424 ) ) ;
#1209=CARTESIAN_POINT ( 'NONE',  ( 122.1561614775786353, -8.899110576539710493, -16.42337572283490132 ) ) ;
#1212=CARTESIAN_POINT ( 'NONE',  ( 119.2631014775786298, -9.565557343593413364, -10.61323700422348004 ) ) ;
#1214=CARTESIAN_POINT ( 'NONE',  ( 114.0783153663348770, -1.172797794773246416, -17.05961127468924587 ) ) ;
#1217=CARTESIAN_POINT ( 'NONE',  ( 118.7525614775786380, -8.166667518702819706, -8.995218007635861213 ) ) ;
#1219=CARTESIAN_POINT ( 'NONE',  ( 115.7460481442453357, 0.9020085738987339008, -11.91225656197089222 ) ) ;
#1220=CARTESIAN_POINT ( 'NONE',  ( 111.2184548109119788, -4.863998795839242995, -13.39321520033831447 ) ) ;
#1222=CARTESIAN_POINT ( 'NONE',  ( 115.8595014775786609, -1.834011780172310813, -8.268836392978581529 ) ) ;
#1223=CARTESIAN_POINT ( 'NONE',  ( 117.6747548109119919, -1.834011780172310813, -8.268836392978581529 ) ) ;
#1224=CARTESIAN_POINT ( 'NONE',  ( 126.3063647503472566, -9.895249910033488305, -13.03518212827709988 ) ) ;
#1231=CARTESIAN_POINT ( 'NONE',  ( 121.7590748109119687, -2.084020599724406786, -8.691656652584148546 ) ) ;
#1235=CARTESIAN_POINT ( 'NONE',  ( 114.3278814775786429, 0.1319031606808879209, -14.10382304977623669 ) ) ;
#1236=CARTESIAN_POINT ( 'NONE',  ( 114.1577014775786552, -3.505236298600246325, -18.68346056562440793 ) ) ;
#1238=CARTESIAN_POINT ( 'NONE',  ( 124.0281414775786146, -1.834011780172310813, -8.268836392978581529 ) ) ;
#1239=CARTESIAN_POINT ( 'NONE',  ( 120.6812681442452941, -10.30919188438810075, -12.61870101168855918 ) ) ;
#1242=CARTESIAN_POINT ( 'NONE',  ( 119.4900081442453086, -7.643976991954077427, -18.09477374809248928 ) ) ;
#1243=CARTESIAN_POINT ( 'NONE',  ( 112.6260814775786514, -9.261995988541697145, -16.69588392320189030 ) ) ;
#1244=CARTESIAN_POINT ( 'NONE',  ( 122.0427081442452817, 0.5811942927096110934, -14.16772938898807510 ) ) ;
#1245=CARTESIAN_POINT ( 'NONE',  ( 118.6391081442452986, -5.574606645277164318, -18.38911715685844683 ) ) ;
#1246=VERTEX_POINT ( 'NONE', #1315 ) ;
#1247=CARTESIAN_POINT ( 'NONE',  ( 125.7299414775786346, -10.15424416112533912, -14.75197769757731336 ) ) ;
#1248=CARTESIAN_POINT ( 'NONE',  ( 121.4187148109119789, -6.344957434206665248, -7.627207830600338134 ) ) ;
#1252=CARTESIAN_POINT ( 'NONE',  ( 126.3807372594939125, 0.2118326779918614511, -13.62869614777685001 ) ) ;
#1254=CARTESIAN_POINT ( 'NONE',  ( 119.5467348109119712, -4.089484607189486809, -7.948022111789456723 ) ) ;
#1255=CARTESIAN_POINT ( 'NONE',  ( 136.1332990479119189, -10.28161693900162810, -11.09901496658777376 ) ) ;
#1256=CARTESIAN_POINT ( 'NONE',  ( 116.6536748109119941, -10.15424416112533912, -14.75197769757731336 ) ) ;
#1257=CARTESIAN_POINT ( 'NONE',  ( 125.1059481442452750, -8.166667518702819706, -8.995218007635861213 ) ) ;
#1259=CARTESIAN_POINT ( 'NONE',  ( 117.0056648082055801, -0.1020945015694922492, -15.74893487844867401 ) ) ;
#1262=CARTESIAN_POINT ( 'NONE',  ( 112.3424481442453384, -3.505236298600246325, -18.68346056562440793 ) ) ;
#1266=CARTESIAN_POINT ( 'NONE',  ( 120.7947214775786193, -9.261995988541697145, -16.69588392320189030 ) ) ;
#1267=CARTESIAN_POINT ( 'NONE',  ( 120.2274548109119934, -9.859900752359374465, -12.68260735090039404 ) ) ;
#1268=CARTESIAN_POINT ( 'NONE',  ( 114.1009748109119784, -5.574606645277164318, -18.38911715685844683 ) ) ;
#1269=ORIENTED_EDGE ( 'NONE', *, *, #42780, .T. ) ;
#1270=CARTESIAN_POINT ( 'NONE',  ( 136.1673833308529424, -7.073431297710629728, -7.951451023228969461 ) ) ;
#1273=CARTESIAN_POINT ( 'NONE',  ( 119.3765548109119834, -10.15424416112533912, -14.75197769757731336 ) ) ;
#1274=CARTESIAN_POINT ( 'NONE',  ( 120.0005481442453146, -4.153390946401325223, -8.397313243818185668 ) ) ;
#1275=CARTESIAN_POINT ( 'NONE',  ( 116.1431348109119881, 0.1319031606808879209, -14.10382304977623669 ) ) ;
#1278=CARTESIAN_POINT ( 'NONE',  ( 123.1772414775786189, -5.574606645277164318, -18.38911715685844683 ) ) ;
#1279=CARTESIAN_POINT ( 'NONE',  ( 123.6310548109119765, -4.153390946401325223, -8.397313243818185668 ) ) ;
#1281=CARTESIAN_POINT ( 'NONE',  ( 112.5126281442453120, 0.1319031606808870605, -14.10382304977625090 ) ) ;
#1287=CARTESIAN_POINT ( 'NONE',  ( 115.8027748109119841, -0.4660016031367893996, -10.09054647747474043 ) ) ;
#1288=CARTESIAN_POINT ( 'NONE',  ( 118.2987481442453088, -1.561330072975668504, -17.79121239304076951 ) ) ;
#1290=CARTESIAN_POINT ( 'NONE',  ( 114.2711548109119803, -9.988377603198976828, -10.36322818467138340 ) ) ;
#1294=CARTESIAN_POINT ( 'NONE',  ( 118.1285681442453068, -7.893985811506177619, -18.51759400769804742 ) ) ;
#1295=CARTESIAN_POINT ( 'NONE',  ( 122.8368814775786291, -7.894159318335828068, -9.358103419637847864 ) ) ;
#1297=CARTESIAN_POINT ( 'NONE',  ( 114.8951481442453115, -8.899110576539710493, -16.42337572283490132 ) ) ;
#1298=CARTESIAN_POINT ( 'NONE',  ( 122.7234281442452755, -5.638512984488999180, -18.83840828888717311 ) ) ;
#1300=CARTESIAN_POINT ( 'NONE',  ( 118.1852948109119836, -4.153390946401325223, -8.397313243818185668 ) ) ;
#1305=CARTESIAN_POINT ( 'NONE',  ( 117.5613014775786525, 0.9020085738987339008, -11.91225656197089222 ) ) ;
#1307=CARTESIAN_POINT ( 'NONE',  ( 125.5030348109119558, -6.222761293078241884, -8.102969835052219238 ) ) ;
#1310=CARTESIAN_POINT ( 'NONE',  ( 116.5402214775786405, -9.565557343593413364, -10.61323700422348004 ) ) ;
#1311=CARTESIAN_POINT ( 'NONE',  ( 112.0127758072985529, 0.3208234527006404435, -15.99825685930877661 ) ) ;
#1313=CARTESIAN_POINT ( 'NONE',  ( 122.7801548109119665, -6.222761293078241884, -8.102969835052219238 ) ) ;
#1315=CARTESIAN_POINT ( 'NONE',  ( 128.2184548109119930, -3.719473736431747390, -16.16631137400202078 ) ) ;
#1316=CARTESIAN_POINT ( 'NONE',  ( 124.4819548109119722, -2.084020599724406786, -8.691656652584148546 ) ) ;
#1318=CARTESIAN_POINT ( 'NONE',  ( 124.5386814775786206, -4.153390946401325223, -8.397313243818185668 ) ) ;
#1319=CARTESIAN_POINT ( 'NONE',  ( 114.3846081442453197, -10.63000616557722466, -14.87417383870573495 ) ) ;
#1320=CARTESIAN_POINT ( 'NONE',  ( 121.1918081442452859, 0.9020085738987339008, -11.91225656197089222 ) ) ;
#1321=CARTESIAN_POINT ( 'NONE',  ( 126.4106614775786284, -6.222761293078241884, -8.102969835052219238 ) ) ;
#1323=CARTESIAN_POINT ( 'NONE',  ( 118.9794681442453026, -0.8288870151387760510, -10.36305467784173118 ) ) ;
#1325=CARTESIAN_POINT ( 'NONE',  ( 120.1707281442453166, 0.2603800115204892296, -16.42320221600525088 ) ) ;
#1328=CARTESIAN_POINT ( 'NONE',  ( 114.2144281442453178, -1.833838273342658809, -17.42832698103878286 ) ) ;
#1331=ORIENTED_EDGE ( 'NONE', *, *, #39829, .F. ) ;
#1332=CARTESIAN_POINT ( 'NONE',  ( 121.8158014775786171, -4.153390946401325223, -8.397313243818185668 ) ) ;
#1335=CARTESIAN_POINT ( 'NONE',  ( 112.1234697116520920, -8.918491192341182483, -16.31914947962552631 ) ) ;
#1339=CARTESIAN_POINT ( 'NONE',  ( 113.4202548109119846, -10.30919188438810075, -12.61870101168855918 ) ) ;
#1341=CARTESIAN_POINT ( 'NONE',  ( 118.9794681442453026, -0.8288870151387760510, -10.36305467784173118 ) ) ;
#1342=CARTESIAN_POINT ( 'NONE',  ( 126.2184548109108420, -4.131345727441387616, -8.447100459282841811 ) ) ;
#1345=CARTESIAN_POINT ( 'NONE',  ( 114.8447400025837197, -2.311015703046749081, -18.04188382666269064 ) ) ;
#1347=CARTESIAN_POINT ( 'NONE',  ( 111.8886348109120092, -3.383040157471821630, -19.15922257007629170 ) ) ;
#1348=ORIENTED_EDGE ( 'NONE', *, *, #972, .F. ) ;
#1351=CARTESIAN_POINT ( 'NONE',  ( 119.5467348109119712, -4.089484607189486809, -7.948022111789456723 ) ) ;
#1352=CARTESIAN_POINT ( 'NONE',  ( 137.1399781294032039, -8.476060746497974918, -17.35023159224490996 ) ) ;
#1355=CARTESIAN_POINT ( 'NONE',  ( 125.0492214775786266, -6.344957434206665248, -7.627207830600338134 ) ) ;
#1358=CARTESIAN_POINT ( 'NONE',  ( 124.0281414775786146, -7.643976991954077427, -18.09477374809248928 ) ) ;
#1359=VERTEX_POINT ( 'NONE', #24815 ) ;
#1360=CARTESIAN_POINT ( 'NONE',  ( 117.2776681442452968, -5.638512984488999180, -18.83840828888717311 ) ) ;
#1364=CARTESIAN_POINT ( 'NONE',  ( 112.0020881442453344, -9.565557343593402706, -10.61323700422347649 ) ) ;
#1367=CARTESIAN_POINT ( 'NONE',  ( 136.7478768735726931, -5.372037007781774953, -7.792893957613936884 ) ) ;
#1368=CARTESIAN_POINT ( 'NONE',  ( 124.8223148109119762, 0.9020085738987339008, -11.91225656197089222 ) ) ;
#1369=DIRECTION ( 'NONE',  ( 0.000000000000000000, 0.6004852223388321697, -0.7996358532186279566 ) ) ;
#1371=CARTESIAN_POINT ( 'NONE',  ( 112.0588148109119828, -9.859900752359374465, -12.68260735090039404 ) ) ;
#1372=CARTESIAN_POINT ( 'NONE',  ( 125.2194014775786286, 0.1319031606808879209, -14.10382304977623669 ) ) ;
#1373=CARTESIAN_POINT ( 'NONE',  ( 123.9146881442452894, -10.15424416112533912, -14.75197769757731336 ) ) ;
#1375=CARTESIAN_POINT ( 'NONE',  ( 118.5823814775786360, -1.834011780172310813, -8.268836392978581529 ) ) ;
#1380=CARTESIAN_POINT ( 'NONE',  ( 126.2940345447968156, -9.794764728668093667, -12.36025030967080163 ) ) ;
#1381=CARTESIAN_POINT ( 'NONE',  ( 114.6115148109119986, -3.383040157471821630, -19.15922257007629170 ) ) ;
#1383=CARTESIAN_POINT ( 'NONE',  ( 115.4056881442453459, -2.084020599724406786, -8.691656652584148546 ) ) ;
#1389=DIRECTION ( 'NONE',  ( 1.000000000000000000, 0.000000000000000000, 0.000000000000000000 ) ) ;
#1390=CARTESIAN_POINT ( 'NONE',  ( 117.2209414775786485, -7.893985811506177619, -18.51759400769804742 ) ) ;
#1395=CARTESIAN_POINT ( 'NONE',  ( 118.1285681442453068, -2.084020599724406786, -8.691656652584148546 ) ) ;
#1396=CARTESIAN_POINT ( 'NONE',  ( 116.1431348109119881, -10.30919188438810075, -12.61870101168855918 ) ) ;
#1398=CARTESIAN_POINT ( 'NONE',  ( 125.2194014775786286, 0.1319031606808879209, -14.10382304977623669 ) ) ;
#1399=CARTESIAN_POINT ( 'NONE',  ( 124.9924948109119924, -5.574606645277164318, -18.38911715685844683 ) ) ;
#1400=CARTESIAN_POINT ( 'NONE',  ( 116.6536748109119941, -10.15424416112533912, -14.75197769757731336 ) ) ;
#1404=CARTESIAN_POINT ( 'NONE',  ( 116.4267681442453153, -6.222761293078241884, -8.102969835052219238 ) ) ;
#1408=CARTESIAN_POINT ( 'NONE',  ( 114.7816948109119863, 0.5811942927096154232, -14.16772938898807155 ) ) ;
#1410=CARTESIAN_POINT ( 'NONE',  ( 112.2857214775786474, -5.574606645277164318, -18.38911715685844683 ) ) ;
#1413=CARTESIAN_POINT ( 'NONE',  ( 121.5888948109119809, 0.1319031606808879209, -14.10382304977623669 ) ) ;
#1414=CARTESIAN_POINT ( 'NONE',  ( 117.3911214775786505, -7.894159318335828068, -9.358103419637847864 ) ) ;
#1416=CARTESIAN_POINT ( 'NONE',  ( 116.0980381415389218, -0.1020945015694922492, -15.74893487844867401 ) ) ;
#1421=CARTESIAN_POINT ( 'NONE',  ( 116.8238548109119819, -4.089484607189486809, -7.948022111789456723 ) ) ;
#1422=CARTESIAN_POINT ( 'NONE',  ( 125.1059481442452750, -1.833838273342660141, -17.42832698103878286 ) ) ;
#1423=CARTESIAN_POINT ( 'NONE',  ( 115.3489614775786407, -0.8288870151387760510, -10.36305467784173118 ) ) ;
#1425=CARTESIAN_POINT ( 'NONE',  ( 121.0216281442452981, -7.894159318335828068, -9.358103419637847864 ) ) ;
#1428=CARTESIAN_POINT ( 'NONE',  ( 118.2987481442453088, -7.894159318335828068, -9.358103419637847864 ) ) ;
#1429=CARTESIAN_POINT ( 'NONE',  ( 125.3328548109119964, -0.8288870151387760510, -10.36305467784173118 ) ) ;
#1434=CARTESIAN_POINT ( 'NONE',  ( 118.1285681442453068, -7.893985811506177619, -18.51759400769804742 ) ) ;
#1436=CARTESIAN_POINT ( 'NONE',  ( 122.1561614775786353, -0.4660016031367893996, -10.09054647747474043 ) ) ;
#1439=CARTESIAN_POINT ( 'NONE',  ( 116.3700414775786527, -5.638512984488999180, -18.83840828888717311 ) ) ;
#1440=CARTESIAN_POINT ( 'NONE',  ( 118.9227414775786400, -10.63000616557722466, -14.87417383870573495 ) ) ;
#1441=CARTESIAN_POINT ( 'NONE',  ( 126.5010429760475574, -10.00445151461793536, -13.30003832786311513 ) ) ;
#1448=CARTESIAN_POINT ( 'NONE',  ( 118.7525614775786380, -1.833838273342659253, -17.42832698103878286 ) ) ;
#1452=CARTESIAN_POINT ( 'NONE',  ( 112.5126281442453120, 0.1319031606808879209, -14.10382304977623669 ) ) ;
#1454=CARTESIAN_POINT ( 'NONE',  ( 112.7962614775786676, -6.222761293078241884, -8.102969835052219238 ) ) ;
#1455=CARTESIAN_POINT ( 'NONE',  ( 119.2631014775786298, 0.2603800115204892296, -16.42320221600525088 ) ) ;
#1457=CARTESIAN_POINT ( 'NONE',  ( 117.8449348109119938, -1.833838273342659253, -17.42832698103878286 ) ) ;
#1458=CARTESIAN_POINT ( 'NONE',  ( 116.8805814775786445, -6.344957434206662583, -7.627207830600332805 ) ) ;
#1459=CARTESIAN_POINT ( 'NONE',  ( 120.9649014775786355, -3.383040157471821630, -19.15922257007629170 ) ) ;
#1460=CARTESIAN_POINT ( 'NONE',  ( 121.4187148109119789, -3.505236298600246325, -18.68346056562440793 ) ) ;
#1462=CARTESIAN_POINT ( 'NONE',  ( 123.6310548109119765, -4.153390946401325223, -8.397313243818185668 ) ) ;
#1463=CARTESIAN_POINT ( 'NONE',  ( 121.0216281442452981, -1.561330072975668948, -17.79121239304076951 ) ) ;
#1464=CARTESIAN_POINT ( 'NONE',  ( 112.7962614775786676, -6.222761293078241884, -8.102969835052219238 ) ) ;
#1465=CARTESIAN_POINT ( 'NONE',  ( 120.8514481442452961, -7.893985811506177619, -18.51759400769804742 ) ) ;
#1470=EDGE_CURVE ( 'NONE', #38601, #45059, #39401, .T. ) ;
#1473=CARTESIAN_POINT ( 'NONE',  ( 136.4173705901605160, -10.21087619983626560, -11.18524563227092017 ) ) ;
#1474=CARTESIAN_POINT ( 'NONE',  ( 114.7249681442453237, -9.565557343593413364, -10.61323700422348004 ) ) ;
#1475=CARTESIAN_POINT ( 'NONE',  ( 125.6164881442453094, 0.2603800115204892296, -16.42320221600525088 ) ) ;
#1480=CARTESIAN_POINT ( 'NONE',  ( 115.1787814775786387, -0.1624402480850797581, -16.17319339645315424 ) ) ;
#1484=CARTESIAN_POINT ( 'NONE',  ( 118.6958348109119754, -6.344957434206665248, -7.627207830600338134 ) ) ;
#1485=CARTESIAN_POINT ( 'NONE',  ( 121.2485348109119769, -8.899110576539710493, -16.42337572283490132 ) ) ;
#1487=CARTESIAN_POINT ( 'NONE',  ( 137.1886586612212113, -7.251019100340859502, -8.638848605701541672 ) ) ;
#1490=CARTESIAN_POINT ( 'NONE',  ( 120.5110881442453206, -3.505236298600246325, -18.68346056562440793 ) ) ;
#1491=CARTESIAN_POINT ( 'NONE',  ( 123.5176014775786228, -0.8288870151387760510, -10.36305467784173118 ) ) ;
#1492=CARTESIAN_POINT ( 'NONE',  ( 117.3911214775786505, -7.894159318335828068, -9.358103419637847864 ) ) ;
#1493=CARTESIAN_POINT ( 'NONE',  ( 121.0016831242421773, -1.016270020561755860, -17.26805140881366896 ) ) ;
#1495=CARTESIAN_POINT ( 'NONE',  ( 122.8936081442453059, -9.565557343593413364, -10.61323700422348004 ) ) ;
#1496=CARTESIAN_POINT ( 'NONE',  ( 123.0070614775786169, -10.15424416112533912, -14.75197769757731336 ) ) ;
#1499=CARTESIAN_POINT ( 'NONE',  ( 112.5693548109119888, 0.4262465694468579591, -12.03445270309932802 ) ) ;
#1503=CYLINDRICAL_SURFACE ( 'NONE', #31356, 5.999999999999997335 ) ;
#1505=CARTESIAN_POINT ( 'NONE',  ( 120.7379948109119709, -10.63000616557722466, -14.87417383870573495 ) ) ;
#1506=CARTESIAN_POINT ( 'NONE',  ( 117.0507614775786465, -10.30919188438810075, -12.61870101168855918 ) ) ;
#1508=CARTESIAN_POINT ( 'NONE',  ( 117.1642148109119859, -9.261995988541697145, -16.69588392320189030 ) ) ;
#1512=AXIS2_PLACEMENT_3D ( 'NONE', #9948, #2860, #9716 ) ;
#1513=CARTESIAN_POINT ( 'NONE',  ( 119.3765548109119834, 0.9020085738987339008, -11.91225656197089222 ) ) ;
#1514=CARTESIAN_POINT ( 'NONE',  ( 112.0588148109119828, 0.5811942927096154232, -14.16772938898807155 ) ) ;
#1516=CARTESIAN_POINT ( 'NONE',  ( 113.0798948109119948, -8.899110576539710493, -16.42337572283490132 ) ) ;
#1517=CARTESIAN_POINT ( 'NONE',  ( 125.3895814775786448, -7.893985811506177619, -18.51759400769804742 ) ) ;
#1519=CARTESIAN_POINT ( 'NONE',  ( 121.5321681442453183, -0.1624402480850797581, -16.17319339645315424 ) ) ;
#1524=CARTESIAN_POINT ( 'NONE',  ( 122.6667014775786413, -7.893985811506177619, -18.51759400769804742 ) ) ;
#1529=CARTESIAN_POINT ( 'NONE',  ( 118.8660148109119774, 0.1319031606808879209, -14.10382304977623669 ) ) ;
#1532=CARTESIAN_POINT ( 'NONE',  ( 121.7590748109119687, -2.084020599724406786, -8.691656652584148546 ) ) ;
#1534=CARTESIAN_POINT ( 'NONE',  ( 124.5386814775786206, -4.153390946401325223, -8.397313243818185668 ) ) ;
#1537=CARTESIAN_POINT ( 'NONE',  ( 118.4122014775786340, -9.859900752359374465, -12.68260735090039404 ) ) ;
#1538=CARTESIAN_POINT ( 'NONE',  ( 122.6099748109119929, -0.8288870151387760510, -10.36305467784173118 ) ) ;
#1540=CARTESIAN_POINT ( 'NONE',  ( 118.6391081442452986, -4.089484607189486809, -7.948022111789456723 ) ) ;
#1541=CARTESIAN_POINT ( 'NONE',  ( 117.5045748109119756, 0.5811942927096110934, -14.16772938898807510 ) ) ;
#1543=CARTESIAN_POINT ( 'NONE',  ( 124.0281414775786146, -7.643976991954077427, -18.09477374809248928 ) ) ;
#1545=CARTESIAN_POINT ( 'NONE',  ( 121.8158014775786171, -5.638512984488999180, -18.83840828888717311 ) ) ;
#1549=CARTESIAN_POINT ( 'NONE',  ( 113.3068014775786594, -1.833838273342658809, -17.42832698103878286 ) ) ;
#1550=CARTESIAN_POINT ( 'NONE',  ( 137.8451516969511204, -2.777385826612674524, -17.42084227926059015 ) ) ;
#1551=CARTESIAN_POINT ( 'NONE',  ( 125.4463081442452932, -5.638512984488999180, -18.83840828888717311 ) ) ;
#1553=CARTESIAN_POINT ( 'NONE',  ( 124.2550481442452792, -0.1624402480850797581, -16.17319339645315424 ) ) ;
#1558=VERTEX_POINT ( 'NONE', #5408 ) ;
#1559=CARTESIAN_POINT ( 'NONE',  ( 115.6325948109119821, 0.2603800115204892296, -16.42320221600525088 ) ) ;
#1560=CARTESIAN_POINT ( 'NONE',  ( 126.0135748109119902, -8.166667518702819706, -8.995218007635861213 ) ) ;
#1562=CARTESIAN_POINT ( 'NONE',  ( 121.4187148109119789, -3.505236298600246325, -18.68346056562440793 ) ) ;
#1563=CARTESIAN_POINT ( 'NONE',  ( 115.5191414775786569, -6.222761293078241884, -8.102969835052219238 ) ) ;
#1566=CARTESIAN_POINT ( 'NONE',  ( 113.0798948109119948, -0.4660016031367893996, -10.09054647747474043 ) ) ;
#1570=CARTESIAN_POINT ( 'NONE',  ( 124.1983214775786166, -8.166667518702819706, -8.995218007635861213 ) ) ;
#1573=CARTESIAN_POINT ( 'NONE',  ( 113.4769814775786330, -10.63000616557722466, -14.87417383870573495 ) ) ;
#1574=CARTESIAN_POINT ( 'NONE',  ( 126.1837548109119211, -10.63000616557722466, -14.87417383870573495 ) ) ;
#1576=CARTESIAN_POINT ( 'NONE',  ( 122.9503348109119827, -9.859900752359378018, -12.68260735090039759 ) ) ;
#1578=CARTESIAN_POINT ( 'NONE',  ( 118.7525614775786380, -8.166667518702819706, -8.995218007635861213 ) ) ;
#1581=CARTESIAN_POINT ( 'NONE',  ( 137.4443952029541265, -4.676119418685644291, -8.312370287078346465 ) ) ;
#1582=CARTESIAN_POINT ( 'NONE',  ( 114.7249681442453237, -9.565557343593413364, -10.61323700422348004 ) ) ;
#1587=CARTESIAN_POINT ( 'NONE',  ( 126.2404814775786264, -9.261995988541697145, -16.69588392320189030 ) ) ;
#1588=CARTESIAN_POINT ( 'NONE',  ( 113.0798948109119948, -0.4660016031367893996, -10.09054647747474043 ) ) ;
#1590=CARTESIAN_POINT ( 'NONE',  ( 125.2761281442453054, 0.4262465694468514643, -12.03445270309931736 ) ) ;
#1592=CARTESIAN_POINT ( 'NONE',  ( 119.5467348109119712, -4.089484607189486809, -7.948022111789456723 ) ) ;
#1594=CARTESIAN_POINT ( 'NONE',  ( 120.0572748109119772, -3.383040157471821630, -19.15922257007629170 ) ) ;
#1600=CARTESIAN_POINT ( 'NONE',  ( 124.9924948109119924, -5.574606645276184658, -18.38911715685858539 ) ) ;
#1601=CARTESIAN_POINT ( 'NONE',  ( 115.2355081442453155, -10.30919188438810075, -12.61870101168855918 ) ) ;
#1605=CARTESIAN_POINT ( 'NONE',  ( 135.3184548109119874, -7.067465109756605912, -7.812468278694988832 ) ) ;
#1606=CARTESIAN_POINT ( 'NONE',  ( 112.9512158961590558, -2.263366209404213958, -18.10533625161307114 ) ) ;
#1607=CARTESIAN_POINT ( 'NONE',  ( 121.1918081442452859, 0.9020085738987339008, -11.91225656197089222 ) ) ;
#1608=EDGE_CURVE ( 'NONE', #11237, #43860, #16131, .T. ) ;
#1612=CARTESIAN_POINT ( 'NONE',  ( 121.3052614775786395, -7.643976991954073874, -18.09477374809249284 ) ) ;
#1613=CARTESIAN_POINT ( 'NONE',  ( 119.2063748109119814, -7.894159318335828068, -9.358103419637847864 ) ) ;
#1614=CARTESIAN_POINT ( 'NONE',  ( 117.7314814775786260, -4.089484607189486809, -7.948022111789456723 ) ) ;
#1616=EDGE_CURVE ( 'NONE', #2614, #30875, #3558, .T. ) ;
#1617=CARTESIAN_POINT ( 'NONE',  ( 118.1222496192402218, -1.111561923218658210, -17.14115599315433158 ) ) ;
#1618=CARTESIAN_POINT ( 'NONE',  ( 123.1772414775786189, -5.574606645277164318, -18.38911715685844683 ) ) ;
#1619=CARTESIAN_POINT ( 'NONE',  ( 116.4834948109119779, -7.894159318335828068, -9.358103419637847864 ) ) ;
#1625=CARTESIAN_POINT ( 'NONE',  ( 117.7314814775786260, -5.574606645277164318, -18.38911715685844683 ) ) ;
#1627=CARTESIAN_POINT ( 'NONE',  ( 127.0150841466607403, -9.727352494953397155, -15.73620462677915377 ) ) ;
#1628=CARTESIAN_POINT ( 'NONE',  ( 116.7104014775786425, -0.4660016031367893996, -10.09054647747474043 ) ) ;
#1630=CARTESIAN_POINT ( 'NONE',  ( 119.0298762859068944, -1.111561923218657322, -17.14115599315433158 ) ) ;
#1633=VERTEX_POINT ( 'NONE', #32980 ) ;
#1634=CARTESIAN_POINT ( 'NONE',  ( 122.5532481442453019, 0.4262465694468514643, -12.03445270309931736 ) ) ;
#1635=CARTESIAN_POINT ( 'NONE',  ( 118.1285681442453068, -2.084020599724406786, -8.691656652584148546 ) ) ;
#1637=DIRECTION ( 'NONE',  ( 0.000000000000000000, 0.6004852223388321697, -0.7996358532186279566 ) ) ;
#1640=CARTESIAN_POINT ( 'NONE',  ( 117.7882081442453170, -6.344957434206665248, -7.627207830600338134 ) ) ;
#1641=CARTESIAN_POINT ( 'NONE',  ( 115.2922348109119781, -10.63000616557722466, -14.87417383870573495 ) ) ;
#1642=CARTESIAN_POINT ( 'NONE',  ( 116.5969481442453031, -9.859900752359374465, -12.68260735090039404 ) ) ;
#1644=CARTESIAN_POINT ( 'NONE',  ( 122.0994348109119443, -10.15424416112533912, -14.75197769757731336 ) ) ;
#1648=CARTESIAN_POINT ( 'NONE',  ( 120.9081748109119872, -4.153390946401325223, -8.397313243818185668 ) ) ;
#1651=DIRECTION ( 'NONE',  ( 0.000000000000000000, -0.6004852223388320587, 0.7996358532186281787 ) ) ;
#1656=CARTESIAN_POINT ( 'NONE',  ( 120.3976348109119812, -1.834011780172310813, -8.268836392978581529 ) ) ;
#1658=CARTESIAN_POINT ( 'NONE',  ( 121.3619881442452879, -4.089484607189486809, -7.948022111789456723 ) ) ;
#1659=CARTESIAN_POINT ( 'NONE',  ( 115.5566632127138575, -2.191907684172563986, -18.20049396185734025 ) ) ;
#1661=CARTESIAN_POINT ( 'NONE',  ( 116.6536748109119941, 0.9020085738987339008, -11.91225656197089222 ) ) ;
#1662=CARTESIAN_POINT ( 'NONE',  ( 117.0507614775786465, -10.30919188438810075, -12.61870101168855918 ) ) ;
#1663=CARTESIAN_POINT ( 'NONE',  ( 111.3319081442453182, -5.568102603702657305, -18.34339073538273013 ) ) ;
#1669=CARTESIAN_POINT ( 'NONE',  ( 118.9227414775786542, 0.4262465694468514643, -12.03445270309931736 ) ) ;
#1672=CARTESIAN_POINT ( 'NONE',  ( 112.8529881442453160, -7.894159318335828068, -9.358103419637847864 ) ) ;
#1675=CARTESIAN_POINT ( 'NONE',  ( 113.3068014775786594, -1.833838273342658809, -17.42832698103878286 ) ) ;
#1676=CARTESIAN_POINT ( 'NONE',  ( 118.5256548109119876, -0.4660016031367893996, -10.09054647747474043 ) ) ;
#1679=CARTESIAN_POINT ( 'NONE',  ( 120.0005481442453146, -4.153390946401325223, -8.397313243818185668 ) ) ;
#1680=CARTESIAN_POINT ( 'NONE',  ( 115.3489614775786407, -9.261995988541697145, -16.69588392320189030 ) ) ;
#1681=CARTESIAN_POINT ( 'NONE',  ( 123.1205148109119563, -1.834011780172310813, -8.268836392978581529 ) ) ;
#1682=CARTESIAN_POINT ( 'NONE',  ( 119.3765548109119834, -10.15424416112533912, -14.75197769757731336 ) ) ;
#1684=EDGE_CURVE ( 'NONE', #41948, #6181, #25963, .T. ) ;
#1685=CARTESIAN_POINT ( 'NONE',  ( 124.0281414775786146, -7.643976991954077427, -18.09477374809248928 ) ) ;
#1688=CARTESIAN_POINT ( 'NONE',  ( 120.1140014775786398, -1.561330072975668504, -17.79121239304076951 ) ) ;
#1690=CARTESIAN_POINT ( 'NONE',  ( 120.0572748109119772, -3.383040157471821630, -19.15922257007629170 ) ) ;
#1698=CARTESIAN_POINT ( 'NONE',  ( 119.6034614775786196, -3.505236298600246325, -18.68346056562440793 ) ) ;
#1699=CARTESIAN_POINT ( 'NONE',  ( 124.8223148109119762, 0.9020085738987339008, -11.91225656197089222 ) ) ;
#1700=CARTESIAN_POINT ( 'NONE',  ( 111.8534302567928478, -9.072100856114243328, -16.09694245754784347 ) ) ;
#1704=CARTESIAN_POINT ( 'NONE',  ( 117.1642148109119859, -0.8288870151387760510, -10.36305467784173118 ) ) ;
#1709=CARTESIAN_POINT ( 'NONE',  ( 123.6310548109119765, -5.638512984488999180, -18.83840828888717311 ) ) ;
#1710=CARTESIAN_POINT ( 'NONE',  ( 123.5176014775786228, -0.8288870151387760510, -10.36305467784173118 ) ) ;
#1712=CARTESIAN_POINT ( 'NONE',  ( 126.1270281442452870, -10.30919188438810075, -12.61870101168855918 ) ) ;
#1714=CARTESIAN_POINT ( 'NONE',  ( 124.3117748109119844, 0.1319031606808879209, -14.10382304977623669 ) ) ;
#1716=CARTESIAN_POINT ( 'NONE',  ( 121.4754414775786131, -1.833838273342659697, -17.42832698103878286 ) ) ;
#1717=CARTESIAN_POINT ( 'NONE',  ( 114.7249681442453237, -9.565557343593413364, -10.61323700422348004 ) ) ;
#1727=CARTESIAN_POINT ( 'NONE',  ( 120.7947214775786193, -9.261995988541697145, -16.69588392320189030 ) ) ;
#1728=CARTESIAN_POINT ( 'NONE',  ( 117.6747548109119919, -1.834011780172310813, -8.268836392978581529 ) ) ;
#1730=CARTESIAN_POINT ( 'NONE',  ( 117.7314814775786260, -4.089484607189486809, -7.948022111789456723 ) ) ;
#1735=CARTESIAN_POINT ( 'NONE',  ( 121.3619881442452879, -4.089484607189486809, -7.948022111789456723 ) ) ;
#1736=CARTESIAN_POINT ( 'NONE',  ( 120.7947214775786193, -9.261995988541697145, -16.69588392320189030 ) ) ;
#1738=CARTESIAN_POINT ( 'NONE',  ( 124.4819548109119722, -2.084020599724406786, -8.691656652584148546 ) ) ;
#1740=CARTESIAN_POINT ( 'NONE',  ( 112.8529881442453160, -7.894159318335828068, -9.358103419637847864 ) ) ;
#1741=CARTESIAN_POINT ( 'NONE',  ( 112.1155414775786454, -10.15424416112533912, -14.75197769757731336 ) ) ;
#1743=CARTESIAN_POINT ( 'NONE',  ( 120.6812681442452941, 0.1319031606808879209, -14.10382304977623669 ) ) ;
#1749=CARTESIAN_POINT ( 'NONE',  ( 123.8579614775786126, 0.5811942927096110934, -14.16772938898807510 ) ) ;
#1752=CARTESIAN_POINT ( 'NONE',  ( 118.5256548109119876, -8.899110576539710493, -16.42337572283490132 ) ) ;
#1755=CARTESIAN_POINT ( 'NONE',  ( 125.2194014775786286, 0.1319031606808879209, -14.10382304977623669 ) ) ;
#1757=CARTESIAN_POINT ( 'NONE',  ( 124.0848681442452772, -5.574606645277164318, -18.38911715685844683 ) ) ;
#1759=CARTESIAN_POINT ( 'NONE',  ( 121.4754414775786131, -8.166667518702819706, -8.995218007635861213 ) ) ;
#1760=CARTESIAN_POINT ( 'NONE',  ( 116.2565881442453133, -0.8288870151387760510, -10.36305467784173118 ) ) ;
#1761=CARTESIAN_POINT ( 'NONE',  ( 121.7590748109119687, -2.084020599724406786, -8.691656652584148546 ) ) ;
#1763=CARTESIAN_POINT ( 'NONE',  ( 124.2550481442452792, -9.988377603198980381, -10.36322818467138518 ) ) ;
#1764=CARTESIAN_POINT ( 'NONE',  ( 117.4478481442453131, 0.2603800115204892296, -16.42320221600525088 ) ) ;
#1766=CARTESIAN_POINT ( 'NONE',  ( 113.6471614775786492, -4.153390946401321671, -8.397313243818183892 ) ) ;
#1767=CARTESIAN_POINT ( 'NONE',  ( 124.2550481442452792, -0.1624402480850797581, -16.17319339645315424 ) ) ;
#1768=CARTESIAN_POINT ( 'NONE',  ( 120.2274548109119934, 0.5811942927096110934, -14.16772938898807510 ) ) ;
#1773=CARTESIAN_POINT ( 'NONE',  ( 114.7816948109119863, -9.859900752359374465, -12.68260735090039404 ) ) ;
#1775=CARTESIAN_POINT ( 'NONE',  ( 125.3895814775786448, -7.893985811506177619, -18.51759400769804742 ) ) ;
#1776=EDGE_LOOP ( 'NONE', ( #20608, #11474, #27163, #35151 ) ) ;
#1777=CARTESIAN_POINT ( 'NONE',  ( 125.2194014775786286, 0.1319031606808879209, -14.10382304977623669 ) ) ;
#1784=CARTESIAN_POINT ( 'NONE',  ( 113.9307948109119906, 0.9020085738987339008, -11.91225656197089222 ) ) ;
#1785=CARTESIAN_POINT ( 'NONE',  ( 113.1933481442453058, -4.089484607189490362, -7.948022111789460276 ) ) ;
#1786=CARTESIAN_POINT ( 'NONE',  ( 124.8790414775786246, -8.899110576539710493, -16.42337572283490132 ) ) ;
#1787=CARTESIAN_POINT ( 'NONE',  ( 116.0864081442453113, -0.1624402480850797581, -16.17319339645315424 ) ) ;
#1791=CARTESIAN_POINT ( 'NONE',  ( 115.4624148109119943, -5.638512984488999180, -18.83840828888717311 ) ) ;
#1793=CARTESIAN_POINT ( 'NONE',  ( 125.3328548109119964, -9.261995988541697145, -16.69588392320189030 ) ) ;
#1796=CARTESIAN_POINT ( 'NONE',  ( 113.7038881442453402, -3.383040157471821630, -19.15922257007629170 ) ) ;
#1797=CARTESIAN_POINT ( 'NONE',  ( 111.2646414775786496, -8.899110576539710493, -16.42337572283490132 ) ) ;
#1799=CARTESIAN_POINT ( 'NONE',  ( 112.9664414775786412, 0.5811942927096154232, -14.16772938898807155 ) ) ;
#1800=CIRCLE ( 'NONE', #6933, 4.999999999999998224 ) ;
#1802=CARTESIAN_POINT ( 'NONE',  ( 118.3554748109119998, 0.2603800115204892296, -16.42320221600525088 ) ) ;
#1805=CARTESIAN_POINT ( 'NONE',  ( 126.2184548109119788, -4.863998795839242995, -13.39321520033831447 ) ) ;
#1806=CARTESIAN_POINT ( 'NONE',  ( 123.6001203708216423, -4.367669542124009929, -15.30311642213100143 ) ) ;
#1808=CARTESIAN_POINT ( 'NONE',  ( 113.0798948109119948, -8.899110576539710493, -16.42337572283490132 ) ) ;
#1811=CARTESIAN_POINT ( 'NONE',  ( 112.0020881442453344, -9.565557343593413364, -10.61323700422348004 ) ) ;
#1812=CARTESIAN_POINT ( 'NONE',  ( 112.8529881442453302, -1.561330072975668060, -17.79121239304076596 ) ) ;
#1814=CARTESIAN_POINT ( 'NONE',  ( 122.4397948109119767, -0.1624402480850797581, -16.17319339645315424 ) ) ;
#1816=CARTESIAN_POINT ( 'NONE',  ( 124.2550481442452792, -9.988377603198980381, -10.36322818467138518 ) ) ;
#1817=CARTESIAN_POINT ( 'NONE',  ( 122.4397948109119767, -9.988377603198976828, -10.36322818467138340 ) ) ;
#1823=CARTESIAN_POINT ( 'NONE',  ( 125.4924948109119924, -4.159894987976798575, -8.443039665293765594 ) ) ;
#1824=CARTESIAN_POINT ( 'NONE',  ( 114.4413348109119823, -9.261995988541697145, -16.69588392320189030 ) ) ;
#1828=CARTESIAN_POINT ( 'NONE',  ( 115.6893214775786447, -9.859900752359374465, -12.68260735090039404 ) ) ;
#1829=CARTESIAN_POINT ( 'NONE',  ( 122.8176765460471813, -2.191907684172563986, -18.20049396185734025 ) ) ;
#1830=CARTESIAN_POINT ( 'NONE',  ( 119.7736414775786358, -10.30919188438810075, -12.61870101168855918 ) ) ;
#1834=ORIENTED_EDGE ( 'NONE', *, *, #21963, .F. ) ;
#1836=CARTESIAN_POINT ( 'NONE',  ( 117.7882081442453170, -3.505236298600246325, -18.68346056562440793 ) ) ;
#1837=CARTESIAN_POINT ( 'NONE',  ( 116.2565881442452991, -9.261995988541697145, -16.69588392320189030 ) ) ;
#1838=CARTESIAN_POINT ( 'NONE',  ( 115.5191414775786569, -3.383040157471821630, -19.15922257007629170 ) ) ;
#1839=CARTESIAN_POINT ( 'NONE',  ( 118.2788031242421596, -1.016270020561755860, -17.26805140881366896 ) ) ;
#1840=CARTESIAN_POINT ( 'NONE',  ( 123.0070614775786169, -10.15424416112533912, -14.75197769757731336 ) ) ;
#1841=CARTESIAN_POINT ( 'NONE',  ( 117.8449348109119938, -1.833838273342659253, -17.42832698103878286 ) ) ;
#1845=CARTESIAN_POINT ( 'NONE',  ( 114.2711548109119803, -9.988377603198976828, -10.36322818467138340 ) ) ;
#1846=CARTESIAN_POINT ( 'NONE',  ( 116.3700414775786527, -4.153390946401321671, -8.397313243818183892 ) ) ;
#1849=CARTESIAN_POINT ( 'NONE',  ( 114.8384214775786489, 0.9020085738987339008, -11.91225656197089222 ) ) ;
#1852=CARTESIAN_POINT ( 'NONE',  ( 117.3343948109119737, -6.222761293078241884, -8.102969835052219238 ) ) ;
#1855=CARTESIAN_POINT ( 'NONE',  ( 123.3474214775786209, -0.1624402480850797581, -16.17319339645315424 ) ) ;
#1856=CARTESIAN_POINT ( 'NONE',  ( 120.7947214775786193, -0.8288870151387760510, -10.36305467784173118 ) ) ;
#1862=CARTESIAN_POINT ( 'NONE',  ( 117.0507614775786465, -10.30919188438810075, -12.61870101168855918 ) ) ;
#1864=CARTESIAN_POINT ( 'NONE',  ( 115.4056881442453459, -7.893985811506177619, -18.51759400769804742 ) ) ;
#1865=CARTESIAN_POINT ( 'NONE',  ( 117.5613014775786525, -10.15424416112533912, -14.75197769757731336 ) ) ;
#1866=CARTESIAN_POINT ( 'NONE',  ( 121.6456214775786293, 0.4262465694468514643, -12.03445270309931736 ) ) ;
#1867=CARTESIAN_POINT ( 'NONE',  ( 112.2237824678160933, -1.149058757900094818, -17.09122335155389294 ) ) ;
#1869=EDGE_CURVE ( 'NONE', #30875, #2648, #15615, .T. ) ;
#1871=CARTESIAN_POINT ( 'NONE',  ( 118.1285681442453068, -2.084020599724406786, -8.691656652584148546 ) ) ;
#1877=CARTESIAN_POINT ( 'NONE',  ( 119.3198281442452924, 0.5811942927096110934, -14.16772938898807510 ) ) ;
#1879=CARTESIAN_POINT ( 'NONE',  ( 122.6099748109119929, -9.261995988541697145, -16.69588392320189030 ) ) ;
#1882=CARTESIAN_POINT ( 'NONE',  ( 119.8303681442453126, -10.63000616557722466, -14.87417383870573495 ) ) ;
#1883=CARTESIAN_POINT ( 'NONE',  ( 116.6536748109119941, 0.9020085738987339008, -11.91225656197089222 ) ) ;
#1889=CARTESIAN_POINT ( 'NONE',  ( 121.3052614775786111, -7.643976991954077427, -18.09477374809248928 ) ) ;
#1893=CARTESIAN_POINT ( 'NONE',  ( 116.7104014775786425, -8.899110576539710493, -16.42337572283490132 ) ) ;
#1896=CARTESIAN_POINT ( 'NONE',  ( 126.0703014775786102, -9.988377603198980381, -10.36322818467138518 ) ) ;
#1897=CARTESIAN_POINT ( 'NONE',  ( 124.2550481442452792, -9.988377603198980381, -10.36322818467138518 ) ) ;
#1900=CARTESIAN_POINT ( 'NONE',  ( 120.3976348109119812, -7.643976991954077427, -18.09477374809248928 ) ) ;
#1901=CARTESIAN_POINT ( 'NONE',  ( 114.3846081442453197, -10.63000616557722466, -14.87417383870573495 ) ) ;
#1902=CARTESIAN_POINT ( 'NONE',  ( 121.0216281442452981, -1.561330072975668948, -17.79121239304076951 ) ) ;
#1903=CARTESIAN_POINT ( 'NONE',  ( 123.1772414775786189, -5.574606645277164318, -18.38911715685844683 ) ) ;
#1905=CARTESIAN_POINT ( 'NONE',  ( 123.3474214775786209, -0.1624402480850797581, -16.17319339645315424 ) ) ;
#1908=ADVANCED_FACE ( 'NONE', ( #17919 ), #25142, .T. ) ;
#1909=CARTESIAN_POINT ( 'NONE',  ( 123.9146881442452894, 0.9020085738987339008, -11.91225656197089222 ) ) ;
#1910=CARTESIAN_POINT ( 'NONE',  ( 112.5126281442453120, 0.1319031606808879209, -14.10382304977623669 ) ) ;
#1911=CARTESIAN_POINT ( 'NONE',  ( 125.9001214775786224, -4.089484607189486809, -7.948022111789456723 ) ) ;
#1914=CARTESIAN_POINT ( 'NONE',  ( 110.2184548109119788, -4.863998795839242995, -13.39321520033831447 ) ) ;
#1915=CARTESIAN_POINT ( 'NONE',  ( 138.0698945632798882, -1.891928339825783345, -16.10198143539211202 ) ) ;
#1920=CARTESIAN_POINT ( 'NONE',  ( 137.3019930433563331, -10.07954145175000349, -13.43736401499259614 ) ) ;
#1921=CARTESIAN_POINT ( 'NONE',  ( 117.8449348109119938, -1.833838273342659253, -17.42832698103878286 ) ) ;
#1922=CARTESIAN_POINT ( 'NONE',  ( 126.1837548109119211, -10.63000616557722466, -14.87417383870573495 ) ) ;
#1929=CARTESIAN_POINT ( 'NONE',  ( 116.4267681442453153, -6.222761293078241884, -8.102969835052219238 ) ) ;
#1930=CARTESIAN_POINT ( 'NONE',  ( 113.2858169107182249, -2.467220198592768199, -17.83387418641523325 ) ) ;
#1933=CARTESIAN_POINT ( 'NONE',  ( 124.2193060444391790, -1.267766418764731728, -16.93314635290706605 ) ) ;
#1935=CARTESIAN_POINT ( 'NONE',  ( 122.4397948109119767, -9.988377603198976828, -10.36322818467138340 ) ) ;
#1936=CARTESIAN_POINT ( 'NONE',  ( 121.0216281442452981, -7.894159318335828068, -9.358103419637847864 ) ) ;
#1939=CARTESIAN_POINT ( 'NONE',  ( 126.2471382750665043, 0.06775931372756542614, -14.29995113275557372 ) ) ;
#1941=CARTESIAN_POINT ( 'NONE',  ( 121.3052614775786111, -7.643976991954077427, -18.09477374809248928 ) ) ;
#1943=CARTESIAN_POINT ( 'NONE',  ( 121.0216281442452981, -7.894159318335828068, -9.358103419637847864 ) ) ;
#1952=CARTESIAN_POINT ( 'NONE',  ( 120.1140014775786398, -1.561330072975668504, -17.79121239304076951 ) ) ;
#1953=CARTESIAN_POINT ( 'NONE',  ( 121.0783548109119749, 0.2603800115204892296, -16.42320221600525088 ) ) ;
#1955=CARTESIAN_POINT ( 'NONE',  ( 115.8595014775786609, -1.834011780172310813, -8.268836392978581529 ) ) ;
#1956=LINE ( 'NONE', #39601, #14096 ) ;
#1959=CARTESIAN_POINT ( 'NONE',  ( 122.9503348109119827, 0.5811942927096110934, -14.16772938898807510 ) ) ;
#1960=CARTESIAN_POINT ( 'NONE',  ( 119.4332814775786318, -0.4660016031367893996, -10.09054647747474043 ) ) ;
#1961=CARTESIAN_POINT ( 'NONE',  ( 124.9924948109119924, -5.574606645277164318, -18.38911715685844683 ) ) ;
#1965=CARTESIAN_POINT ( 'NONE',  ( 113.1366214775786432, -7.643976991954077427, -18.09477374809248928 ) ) ;
#1966=CARTESIAN_POINT ( 'NONE',  ( 124.2550481442452792, -9.988377603198980381, -10.36322818467138518 ) ) ;
#1969=CARTESIAN_POINT ( 'NONE',  ( 119.0929214775786278, -4.153390946401325223, -8.397313243818185668 ) ) ;
#1976=CARTESIAN_POINT ( 'NONE',  ( 122.8936081442453059, 0.2603800115204892296, -16.42320221600525088 ) ) ;
#1977=CARTESIAN_POINT ( 'NONE',  ( 114.6874464091100947, -0.9924539043446216624, -17.29976612834909133 ) ) ;
#1980=CARTESIAN_POINT ( 'NONE',  ( 119.0929214775786278, -4.153390946401325223, -8.397313243818185668 ) ) ;
#1983=CARTESIAN_POINT ( 'NONE',  ( 122.4397948109119767, -0.1624402480850797581, -16.17319339645315424 ) ) ;
#1985=CARTESIAN_POINT ( 'NONE',  ( 135.3184548109119874, -4.105398160058917334, -19.34506575923121474 ) ) ;
#1987=VECTOR ( 'NONE', #43432, 1000.000000000000000 ) ;
#1988=CARTESIAN_POINT ( 'NONE',  ( 124.5954081442453116, -3.383040157471821630, -19.15922257007629170 ) ) ;
#1989=CARTESIAN_POINT ( 'NONE',  ( 117.3343948109119737, -6.222761293078241884, -8.102969835052219238 ) ) ;
#1990=CARTESIAN_POINT ( 'NONE',  ( 123.9146881442452894, -10.15424416112533912, -14.75197769757731336 ) ) ;
#1992=CARTESIAN_POINT ( 'NONE',  ( 124.1983214775786166, -8.166667518702819706, -8.995218007635861213 ) ) ;
#1994=CARTESIAN_POINT ( 'NONE',  ( 114.8951481442453115, -0.4660016031367893996, -10.09054647747474043 ) ) ;
#1996=CARTESIAN_POINT ( 'NONE',  ( 113.6471614775786492, -5.638512984488995627, -18.83840828888717311 ) ) ;
#1997=CARTESIAN_POINT ( 'NONE',  ( 123.9714148109119805, -8.899110576539710493, -16.42337572283490132 ) ) ;
#1998=CARTESIAN_POINT ( 'NONE',  ( 125.6164881442453094, 0.2603800115204892296, -16.42320221600525088 ) ) ;
#2002=CARTESIAN_POINT ( 'NONE',  ( 114.8384214775786489, -10.15424416112533912, -14.75197769757731336 ) ) ;
#2006=CARTESIAN_POINT ( 'NONE',  ( 124.0281414775786146, -7.643976991954077427, -18.09477374809248928 ) ) ;
#2009=ORIENTED_EDGE ( 'NONE', *, *, #44122, .T. ) ;
#2014=CARTESIAN_POINT ( 'NONE',  ( 119.3765548109119834, 0.9020085738987339008, -11.91225656197089222 ) ) ;
#2015=CARTESIAN_POINT ( 'NONE',  ( 125.2194014775786286, 0.1319031606808879209, -14.10382304977623669 ) ) ;
#2016=CARTESIAN_POINT ( 'NONE',  ( 116.4267681442453153, -6.222761293078241884, -8.102969835052219238 ) ) ;
#2020=CARTESIAN_POINT ( 'NONE',  ( 115.6325948109119821, 0.2603800115204892296, -16.42320221600525088 ) ) ;
#2023=CARTESIAN_POINT ( 'NONE',  ( 123.3474214775786209, -9.988377603198976828, -10.36322818467138340 ) ) ;
#2025=CARTESIAN_POINT ( 'NONE',  ( 116.0296814775786345, -8.166667518702817929, -8.995218007635861213 ) ) ;
#2026=CARTESIAN_POINT ( 'NONE',  ( 115.0653281442453277, -3.505236298600246325, -18.68346056562440793 ) ) ;
#2028=CARTESIAN_POINT ( 'NONE',  ( 111.7751814775786556, -7.893985811506177619, -18.51759400769804742 ) ) ;
#2030=CARTESIAN_POINT ( 'NONE',  ( 121.6456214775786293, -10.63000616557722466, -14.87417383870573495 ) ) ;
#2032=CARTESIAN_POINT ( 'NONE',  ( 115.7417048073892687, -1.081026697600512732, -17.18181821144401056 ) ) ;
#2035=CARTESIAN_POINT ( 'NONE',  ( 114.2711548109119803, -0.1624402480850797581, -16.17319339645315424 ) ) ;
#2040=CARTESIAN_POINT ( 'NONE',  ( 112.1155414775786454, -10.15424416112533912, -14.75197769757731336 ) ) ;
#2042=CARTESIAN_POINT ( 'NONE',  ( 112.4559014775786494, -9.988377603198976828, -10.36322818467138340 ) ) ;
#2044=CARTESIAN_POINT ( 'NONE',  ( 113.5904348109119866, -7.893985811506177619, -18.51759400769804742 ) ) ;
#2045=CARTESIAN_POINT ( 'NONE',  ( 115.0653281442453277, -3.505236298600246325, -18.68346056562440793 ) ) ;
#2046=CARTESIAN_POINT ( 'NONE',  ( 124.4819548109119722, -7.893985811506177619, -18.51759400769804742 ) ) ;
#2047=CARTESIAN_POINT ( 'NONE',  ( 123.0637881442452937, -0.4660016031367893996, -10.09054647747474043 ) ) ;
#2049=CARTESIAN_POINT ( 'NONE',  ( 112.8529881442453302, -1.561330072975668060, -17.79121239304076596 ) ) ;
#2054=CARTESIAN_POINT ( 'NONE',  ( 126.2872529661378564, -9.794462782700913195, -12.37543279432376231 ) ) ;
#2055=CARTESIAN_POINT ( 'NONE',  ( 119.9438214775786378, -7.893985811506177619, -18.51759400769804742 ) ) ;
#2057=CARTESIAN_POINT ( 'NONE',  ( 125.3895814775786448, -7.893985811506177619, -18.51759400769804742 ) ) ;
#2060=CARTESIAN_POINT ( 'NONE',  ( 114.3846081442453197, 0.4262465694468514643, -12.03445270309931736 ) ) ;
#2061=CARTESIAN_POINT ( 'NONE',  ( 119.6034614775786196, -6.344957434206665248, -7.627207830600338134 ) ) ;
#2065=CARTESIAN_POINT ( 'NONE',  ( 121.0783548109119749, -9.565557343593393824, -10.61323700422344274 ) ) ;
#2066=CARTESIAN_POINT ( 'NONE',  ( 122.4965214775786251, 0.1319031606808879209, -14.10382304977623669 ) ) ;
#2067=CARTESIAN_POINT ( 'NONE',  ( 120.4543614775786295, -4.089484607189486809, -7.948022111789456723 ) ) ;
#2070=CARTESIAN_POINT ( 'NONE',  ( 115.3489614775786407, -9.261995988541697145, -16.69588392320189030 ) ) ;
#2071=CARTESIAN_POINT ( 'NONE',  ( 135.7171320688292724, -7.236526375436695524, -18.88165896190640680 ) ) ;
#2072=CARTESIAN_POINT ( 'NONE',  ( 124.3117748109119844, 0.1319031606808879209, -14.10382304977623669 ) ) ;
#2073=CARTESIAN_POINT ( 'NONE',  ( 119.2063748109119814, -7.894159318335828068, -9.358103419637847864 ) ) ;
#2076=CARTESIAN_POINT ( 'NONE',  ( 111.8886348109120092, -3.383040157471821630, -19.15922257007629170 ) ) ;
#2077=CARTESIAN_POINT ( 'NONE',  ( 119.7736414775786358, 0.1319031606808879209, -14.10382304977623669 ) ) ;
#2080=CARTESIAN_POINT ( 'NONE',  ( 120.5110881442453206, -6.344957434206665248, -7.627207830600338134 ) ) ;
#2082=CARTESIAN_POINT ( 'NONE',  ( 114.9518748109119883, -7.643976991954077427, -18.09477374809248928 ) ) ;
#2084=ORIENTED_EDGE ( 'NONE', *, *, #27230, .T. ) ;
#2085=CARTESIAN_POINT ( 'NONE',  ( 124.5386814775786206, -4.153390946401325223, -8.397313243818185668 ) ) ;
#2086=CARTESIAN_POINT ( 'NONE',  ( 120.6812681442452941, 0.1319031606808879209, -14.10382304977623669 ) ) ;
#2089=CARTESIAN_POINT ( 'NONE',  ( 118.5256548109119876, -0.4660016031367893996, -10.09054647747474043 ) ) ;
#2091=CARTESIAN_POINT ( 'NONE',  ( 116.1998614775786507, -10.63000616557722466, -14.87417383870573495 ) ) ;
#2092=CARTESIAN_POINT ( 'NONE',  ( 114.0442481442453300, -1.834011780172310813, -8.268836392978581529 ) ) ;
#2093=CARTESIAN_POINT ( 'NONE',  ( 117.9016614775786280, -0.1624402480850797581, -16.17319339645315424 ) ) ;
#2094=CARTESIAN_POINT ( 'NONE',  ( 124.9357681442453014, -7.643976991954077427, -18.09477374809248928 ) ) ;
#2095=CARTESIAN_POINT ( 'NONE',  ( 112.7962614775786676, -3.383040157471821630, -19.15922257007629170 ) ) ;
#2097=CARTESIAN_POINT ( 'NONE',  ( 122.4965214775786251, 0.1319031606808879209, -14.10382304977623669 ) ) ;
#2098=CARTESIAN_POINT ( 'NONE',  ( 114.1210660817262550, -2.423081321603721694, -17.89265170041262465 ) ) ;
#2102=CARTESIAN_POINT ( 'NONE',  ( 117.0507614775786465, -10.30919188438810075, -12.61870101168855918 ) ) ;
#2103=ORIENTED_EDGE ( 'NONE', *, *, #8142, .T. ) ;
#2104=CARTESIAN_POINT ( 'NONE',  ( 121.7023481442452777, -9.261995988541697145, -16.69588392320189030 ) ) ;
#2107=CARTESIAN_POINT ( 'NONE',  ( 119.5467348109119712, -4.089484607189486809, -7.948022111789456723 ) ) ;
#2108=CARTESIAN_POINT ( 'NONE',  ( 121.4187148109119789, -6.344957434206665248, -7.627207830600338134 ) ) ;
#2112=DIRECTION ( 'NONE',  ( 0.000000000000000000, 0.6004852223388321697, -0.7996358532186279566 ) ) ;
#2114=CARTESIAN_POINT ( 'NONE',  ( 125.6164881442453094, -9.565557343593413364, -10.61323700422348004 ) ) ;
#2117=CARTESIAN_POINT ( 'NONE',  ( 116.8805814775786445, -3.505236298600246325, -18.68346056562440793 ) ) ;
#2121=CARTESIAN_POINT ( 'NONE',  ( 111.2646414775786496, -8.899110576539710493, -16.42337572283490132 ) ) ;
#2122=CARTESIAN_POINT ( 'NONE',  ( 124.9924948109119924, -4.089484607189486809, -7.948022111789456723 ) ) ;
#2124=CARTESIAN_POINT ( 'NONE',  ( 121.0216281442452981, -7.894159318335828068, -9.358103419637847864 ) ) ;
#2125=CARTESIAN_POINT ( 'NONE',  ( 116.5969481442453031, 0.5811942927096154232, -14.16772938898807155 ) ) ;
#2126=CARTESIAN_POINT ( 'NONE',  ( 122.4965214775786251, -10.30919188438810075, -12.61870101168855918 ) ) ;
#2127=CARTESIAN_POINT ( 'NONE',  ( 124.4252281442452812, -0.8288870151387760510, -10.36305467784173118 ) ) ;
#2130=EDGE_CURVE ( 'NONE', #30086, #40322, #14182, .T. ) ;
#2131=CARTESIAN_POINT ( 'NONE',  ( 123.2339681442453241, -6.344957434206665248, -7.627207830600338134 ) ) ;
#2132=CARTESIAN_POINT ( 'NONE',  ( 112.9097148109120070, -9.565557343593413364, -10.61323700422348004 ) ) ;
#2133=CARTESIAN_POINT ( 'NONE',  ( 111.6617281442453304, 0.4262465694468514643, -12.03445270309931736 ) ) ;
#2136=CARTESIAN_POINT ( 'NONE',  ( 138.2184548109119930, -2.458068653496962686, -15.34808096303632396 ) ) ;
#2140=CARTESIAN_POINT ( 'NONE',  ( 118.3554748109119998, -9.565557343593413364, -10.61323700422348004 ) ) ;
#2141=CARTESIAN_POINT ( 'NONE',  ( 111.3780948109119890, -5.574606645277164318, -18.38911715685844683 ) ) ;
#2142=CARTESIAN_POINT ( 'NONE',  ( 126.2889637360267159, -5.888109775029882975, -18.32339328746833473 ) ) ;
#2143=ORIENTED_EDGE ( 'NONE', *, *, #28955, .T. ) ;
#2145=CARTESIAN_POINT ( 'NONE',  ( 117.5613014775786525, -10.15424416112533912, -14.75197769757731336 ) ) ;
#2146=CARTESIAN_POINT ( 'NONE',  ( 113.4821938206745386, -2.348512537728063787, -17.99195118506216318 ) ) ;
#2151=CARTESIAN_POINT ( 'NONE',  ( 123.2339681442453241, -6.344957434206665248, -7.627207830600338134 ) ) ;
#2152=CARTESIAN_POINT ( 'NONE',  ( 123.6877814775786533, -6.222761293078241884, -8.102969835052219238 ) ) ;
#2159=CARTESIAN_POINT ( 'NONE',  ( 122.9503348109119827, -9.859900752359378018, -12.68260735090039759 ) ) ;
#2160=CARTESIAN_POINT ( 'NONE',  ( 119.8870948109119752, -0.8288870151387760510, -10.36305467784173118 ) ) ;
#2161=EDGE_CURVE ( 'NONE', #34050, #35601, #31920, .T. ) ;
#2164=CARTESIAN_POINT ( 'NONE',  ( 116.5026997424434114, -0.9924539043446216624, -17.29976612834909133 ) ) ;
#2170=CARTESIAN_POINT ( 'NONE',  ( 120.2841814775786276, 0.9020085738987339008, -11.91225656197089222 ) ) ;
#2171=CARTESIAN_POINT ( 'NONE',  ( 123.1205148109119563, -1.834011780172310813, -8.268836392978581529 ) ) ;
#2173=CARTESIAN_POINT ( 'NONE',  ( 116.4267681442453153, -3.383040157471821630, -19.15922257007629170 ) ) ;
#2174=CARTESIAN_POINT ( 'NONE',  ( 114.2144281442453178, -8.166667518702817929, -8.995218007635859436 ) ) ;
#2178=CARTESIAN_POINT ( 'NONE',  ( 112.2857214775786474, -5.574606645277164318, -18.38911715685844683 ) ) ;
#2179=CARTESIAN_POINT ( 'NONE',  ( 119.4900081442453086, -1.834011780172310813, -8.268836392978581529 ) ) ;
#2181=CARTESIAN_POINT ( 'NONE',  ( 124.3685014775786328, 0.4262465694468514643, -12.03445270309931736 ) ) ;
#2182=CARTESIAN_POINT ( 'NONE',  ( 112.3424481442453384, -3.505236298600246325, -18.68346056562440793 ) ) ;
#2185=CARTESIAN_POINT ( 'NONE',  ( 113.4202548109119846, 0.1319031606808879209, -14.10382304977623669 ) ) ;
#2186=CARTESIAN_POINT ( 'NONE',  ( 125.8433948109119456, -1.834011780172310813, -8.268836392978581529 ) ) ;
#2188=EDGE_CURVE ( 'NONE', #18093, #38601, #5278, .T. ) ;
#2191=CARTESIAN_POINT ( 'NONE',  ( 120.5678148109119832, -1.833838273342659253, -17.42832698103878286 ) ) ;
#2197=CARTESIAN_POINT ( 'NONE',  ( 123.7445081442452874, -1.561330072975668948, -17.79121239304076951 ) ) ;
#2198=CARTESIAN_POINT ( 'NONE',  ( 138.2184548109119930, -5.622599431619523358, -7.441364641445410655 ) ) ;
#2208=CARTESIAN_POINT ( 'NONE',  ( 115.9162281442453093, -5.574606645277164318, -18.38911715685844683 ) ) ;
#2211=CARTESIAN_POINT ( 'NONE',  ( 121.8158014775786171, -5.638512984488999180, -18.83840828888717311 ) ) ;
#2212=CARTESIAN_POINT ( 'NONE',  ( 114.3278814775786429, -10.30919188438810075, -12.61870101168855918 ) ) ;
#2214=DIRECTION ( 'NONE',  ( 0.000000000000000000, 0.6004852223388322807, -0.7996358532186279566 ) ) ;
#2215=CARTESIAN_POINT ( 'NONE',  ( 122.8368814775786291, -7.894159318335828068, -9.358103419637847864 ) ) ;
#2216=CARTESIAN_POINT ( 'NONE',  ( 124.1983214775786166, -8.166667518702819706, -8.995218007635861213 ) ) ;
#2220=CARTESIAN_POINT ( 'NONE',  ( 114.4413348109119823, -0.8288870151387760510, -10.36305467784173118 ) ) ;
#2221=VECTOR ( 'NONE', #16331, 1000.000000000000000 ) ;
#2222=CARTESIAN_POINT ( 'NONE',  ( 115.1220548109119761, -1.833838273342658809, -17.42832698103878286 ) ) ;
#2228=CARTESIAN_POINT ( 'NONE',  ( 124.5386814775786206, -4.153390946401325223, -8.397313243818185668 ) ) ;
#2231=ORIENTED_EDGE ( 'NONE', *, *, #41365, .T. ) ;
#2235=CARTESIAN_POINT ( 'NONE',  ( 119.2063748109119814, -1.561330072975668504, -17.79121239304076951 ) ) ;
#2236=CARTESIAN_POINT ( 'NONE',  ( 125.5597614775786326, -7.894159318335828068, -9.358103419637847864 ) ) ;
#2237=CARTESIAN_POINT ( 'NONE',  ( 113.1366214775786432, -7.643976991954077427, -18.09477374809248928 ) ) ;
#2240=CARTESIAN_POINT ( 'NONE',  ( 111.7184548109119788, -9.162420673101799196, -15.99582338542316151 ) ) ;
#2241=CARTESIAN_POINT ( 'NONE',  ( 116.0864081442453113, -9.988377603198976828, -10.36322818467138340 ) ) ;
#2245=CARTESIAN_POINT ( 'NONE',  ( 124.3117748109119844, -10.30919188438810075, -12.61870101168855918 ) ) ;
#2249=CARTESIAN_POINT ( 'NONE',  ( 114.7816948109119863, 0.5811942927096154232, -14.16772938898807155 ) ) ;
#2250=CARTESIAN_POINT ( 'NONE',  ( 115.2922348109119781, 0.4262465694468514643, -12.03445270309931736 ) ) ;
#2251=CARTESIAN_POINT ( 'NONE',  ( 126.2184548109119788, -5.568102603702699049, -18.34339073538272302 ) ) ;
#2252=CARTESIAN_POINT ( 'NONE',  ( 125.4463081442452932, -4.153390946401325223, -8.397313243818185668 ) ) ;
#2255=CARTESIAN_POINT ( 'NONE',  ( 120.3409081442453044, -0.4660016031367893996, -10.09054647747474043 ) ) ;
#2259=CARTESIAN_POINT ( 'NONE',  ( 112.1155012242753344, -10.15403529472779809, -14.75050927016698310 ) ) ;
#2260=CARTESIAN_POINT ( 'NONE',  ( 136.3568202015705992, -2.634417929066116937, -8.029337161656213695 ) ) ;
#2261=CARTESIAN_POINT ( 'NONE',  ( 113.7606148109119886, -7.894159318335828068, -9.358103419637847864 ) ) ;
#2262=CARTESIAN_POINT ( 'NONE',  ( 111.2184548109119788, -1.295815253274133161, -16.89579513612386563 ) ) ;
#2264=CARTESIAN_POINT ( 'NONE',  ( 114.7249681442453237, -9.565557343593413364, -10.61323700422348004 ) ) ;
#2265=CARTESIAN_POINT ( 'NONE',  ( 115.0086014775786509, -4.089484607189486809, -7.948022111789456723 ) ) ;
#2267=CARTESIAN_POINT ( 'NONE',  ( 113.8173414775786512, 0.2603800115204892296, -16.42320221600525088 ) ) ;
#2268=CARTESIAN_POINT ( 'NONE',  ( 117.3343948109119737, -6.222761293078241884, -8.102969835052219238 ) ) ;
#2269=CARTESIAN_POINT ( 'NONE',  ( 123.2339681442453241, -6.344957434206665248, -7.627207830600338134 ) ) ;
#2270=CARTESIAN_POINT ( 'NONE',  ( 123.4041481442452834, -10.30919188438810075, -12.61870101168855918 ) ) ;
#2272=CARTESIAN_POINT ( 'NONE',  ( 114.4980614775786592, -7.893985811506177619, -18.51759400769804742 ) ) ;
#2278=CARTESIAN_POINT ( 'NONE',  ( 119.8870948109119752, -9.261995988541697145, -16.69588392320189030 ) ) ;
#2282=CARTESIAN_POINT ( 'NONE',  ( 120.6253743740715407, -2.419733177069661512, -17.89711025544711376 ) ) ;
#2283=CARTESIAN_POINT ( 'NONE',  ( 115.0653281442453277, -3.505236298600246325, -18.68346056562440793 ) ) ;
#2286=CARTESIAN_POINT ( 'NONE',  ( 118.6958348109119754, -6.344957434206665248, -7.627207830600338134 ) ) ;
#2292=CARTESIAN_POINT ( 'NONE',  ( 121.4754414775786131, -1.833838273342659697, -17.42832698103878286 ) ) ;
#2293=CARTESIAN_POINT ( 'NONE',  ( 120.3409081442453044, -0.4660016031367893996, -10.09054647747474043 ) ) ;
#2294=CARTESIAN_POINT ( 'NONE',  ( 115.2355081442453155, 0.1319031606808879209, -14.10382304977623669 ) ) ;
#2295=CARTESIAN_POINT ( 'NONE',  ( 113.7606148109119886, -1.561330072975668060, -17.79121239304076596 ) ) ;
#2296=CARTESIAN_POINT ( 'NONE',  ( 117.8659193777725278, -1.267766418764730840, -16.93314635290706605 ) ) ;
#2297=CARTESIAN_POINT ( 'NONE',  ( 126.2455040230451289, -0.9944417698632344038, -10.20348866579734448 ) ) ;
#2298=CARTESIAN_POINT ( 'NONE',  ( 119.3765548109119834, -10.15424416112533912, -14.75197769757731336 ) ) ;
#2299=VERTEX_POINT ( 'NONE', #6494 ) ;
#2300=CARTESIAN_POINT ( 'NONE',  ( 119.6601881442453106, -8.166667518702801942, -8.995218007635848778 ) ) ;
#2302=CARTESIAN_POINT ( 'NONE',  ( 113.0231681442453322, 0.9020085738987339008, -11.91225656197089222 ) ) ;
#2303=CARTESIAN_POINT ( 'NONE',  ( 121.3619881442452879, -5.574606645277164318, -18.38911715685844683 ) ) ;
#2306=CARTESIAN_POINT ( 'NONE',  ( 120.2841814775786276, 0.9020085738987339008, -11.91225656197089222 ) ) ;
#2308=CARTESIAN_POINT ( 'NONE',  ( 114.8384214775786489, -10.15424416112533912, -14.75197769757731336 ) ) ;
#2309=ORIENTED_EDGE ( 'NONE', *, *, #2188, .T. ) ;
#2310=ORIENTED_EDGE ( 'NONE', *, *, #8142, .F. ) ;
#2312=CARTESIAN_POINT ( 'NONE',  ( 126.2972081442452890, -2.084020599724406786, -8.691656652584148546 ) ) ;
#2313=CARTESIAN_POINT ( 'NONE',  ( 121.2485348109119769, -8.899110576539710493, -16.42337572283490132 ) ) ;
#2316=CARTESIAN_POINT ( 'NONE',  ( 120.1707281442453166, 0.2603800115204892296, -16.42320221600525088 ) ) ;
#2319=EDGE_CURVE ( 'NONE', #21889, #31663, #36791, .T. ) ;
#2320=CARTESIAN_POINT ( 'NONE',  ( 116.5969481442453031, 0.5811942927096154232, -14.16772938898807155 ) ) ;
#2321=CARTESIAN_POINT ( 'NONE',  ( 116.2565881442452991, -9.261995988541697145, -16.69588392320189030 ) ) ;
#2322=CARTESIAN_POINT ( 'NONE',  ( 114.4980614775786734, -2.084020599724406786, -8.691656652584148546 ) ) ;
#2323=CARTESIAN_POINT ( 'NONE',  ( 125.0492214775786266, -3.505236298600246325, -18.68346056562440793 ) ) ;
#2324=CARTESIAN_POINT ( 'NONE',  ( 113.9875214775786532, -0.4660016031367893996, -10.09054647747474043 ) ) ;
#2326=CARTESIAN_POINT ( 'NONE',  ( 124.9924948109119924, -5.574606645277164318, -18.38911715685844683 ) ) ;
#2327=DIRECTION ( 'NONE',  ( 0.000000000000000000, 0.6004852223388321697, -0.7996358532186279566 ) ) ;
#2332=CARTESIAN_POINT ( 'NONE',  ( 121.9292548109119849, -1.561330072975668948, -17.79121239304076951 ) ) ;
#2334=CARTESIAN_POINT ( 'NONE',  ( 119.1496481442453046, -3.383040157471821630, -19.15922257007629170 ) ) ;
#2335=CARTESIAN_POINT ( 'NONE',  ( 112.6260814775786514, -0.8288870151387760510, -10.36305467784173118 ) ) ;
#2337=CARTESIAN_POINT ( 'NONE',  ( 119.4332814775786318, -0.4660016031367893996, -10.09054647747474043 ) ) ;
#2338=CARTESIAN_POINT ( 'NONE',  ( 119.7736414775786358, -10.30919188438810075, -12.61870101168855918 ) ) ;
#2340=CARTESIAN_POINT ( 'NONE',  ( 124.1415948109119540, -3.505236298600246325, -18.68346056562440793 ) ) ;
#2345=CARTESIAN_POINT ( 'NONE',  ( 114.4291028165343960, -2.324775150319240868, -18.02356106541842351 ) ) ;
#2346=CARTESIAN_POINT ( 'NONE',  ( 123.2339681442453241, -3.505236298600246325, -18.68346056562440793 ) ) ;
#2349=CARTESIAN_POINT ( 'NONE',  ( 116.6536748109119941, -10.15424416112533912, -14.75197769757731336 ) ) ;
#2351=CARTESIAN_POINT ( 'NONE',  ( 113.4202548109119846, 0.1319031606808879209, -14.10382304977623669 ) ) ;
#2352=CARTESIAN_POINT ( 'NONE',  ( 123.8579614775786126, 0.5811942927096110934, -14.16772938898807510 ) ) ;
#2353=ORIENTED_EDGE ( 'NONE', *, *, #972, .T. ) ;
#2354=CARTESIAN_POINT ( 'NONE',  ( 122.4965214775786251, 0.1319031606808879209, -14.10382304977623669 ) ) ;
#2356=CARTESIAN_POINT ( 'NONE',  ( 116.8238548109119819, -4.089484607189486809, -7.948022111789456723 ) ) ;
#2357=CARTESIAN_POINT ( 'NONE',  ( 124.3117748109119844, -10.30919188438810075, -12.61870101168855918 ) ) ;
#2359=B_SPLINE_CURVE_WITH_KNOTS ( 'NONE', 3,
 ( #13125, #9933, #40711, #30444, #20419, #10158, #23846, #9471, #34302, #33847 ),
 .UNSPECIFIED., .F., .F.,
 ( 4, 3, 3, 4 ),
 ( 0.000000000000000000, 0.0001671877560958089928, 0.0003343755126086545080, 0.0006438490228505469159 ),
 .UNSPECIFIED. ) ;
#2360=CARTESIAN_POINT ( 'NONE',  ( 123.7445081442452874, -7.894159318335828068, -9.358103419637847864 ) ) ;
#2363=CARTESIAN_POINT ( 'NONE',  ( 123.4608748109119745, -10.63000616557722466, -14.87417383870573495 ) ) ;
#2364=CARTESIAN_POINT ( 'NONE',  ( 113.7606148109119886, -7.894159318335828068, -9.358103419637847864 ) ) ;
#2365=CARTESIAN_POINT ( 'NONE',  ( 126.0703014775786102, -9.988377603198980381, -10.36322818467138518 ) ) ;
#2366=LINE ( 'NONE', #22448, #1987 ) ;
#2369=CARTESIAN_POINT ( 'NONE',  ( 128.2184548109119930, -2.520019956603805511, -15.26558354049377009 ) ) ;
#2373=CARTESIAN_POINT ( 'NONE',  ( 118.0151148109119816, 0.4262465694468514643, -12.03445270309931736 ) ) ;
#2374=CARTESIAN_POINT ( 'NONE',  ( 113.1366214775786432, -7.643976991954077427, -18.09477374809248928 ) ) ;
#2375=CARTESIAN_POINT ( 'NONE',  ( 126.3858199398357982, -6.059226663227516241, -18.33441212318943769 ) ) ;
#2379=CARTESIAN_POINT ( 'NONE',  ( 115.6325948109119821, -9.565557343593413364, -10.61323700422348004 ) ) ;
#2380=CARTESIAN_POINT ( 'NONE',  ( 113.0798948109119948, -8.899110576539710493, -16.42337572283490132 ) ) ;
#2381=CONICAL_SURFACE ( 'NONE', #205, 3.999999999999997780, 0.7853981633974476129 ) ;
#2383=CARTESIAN_POINT ( 'NONE',  ( 112.0588148109119828, -9.859900752359374465, -12.68260735090039404 ) ) ;
#2385=CARTESIAN_POINT ( 'NONE',  ( 123.8579614775786126, 0.5811942927096110934, -14.16772938898807510 ) ) ;
#2386=CARTESIAN_POINT ( 'NONE',  ( 112.1722681442453222, -0.4660016031367893996, -10.09054647747474043 ) ) ;
#2391=CARTESIAN_POINT ( 'NONE',  ( 123.5743281442453139, -2.084020599724406786, -8.691656652584148546 ) ) ;
#2392=CARTESIAN_POINT ( 'NONE',  ( 118.3554748109119998, -9.565557343593413364, -10.61323700422348004 ) ) ;
#2397=CARTESIAN_POINT ( 'NONE',  ( 114.6682414775786469, -7.894159318335828068, -9.358103419637847864 ) ) ;
#2401=CARTESIAN_POINT ( 'NONE',  ( 121.5321681442453183, -9.988377603198976828, -10.36322818467138340 ) ) ;
#2402=CARTESIAN_POINT ( 'NONE',  ( 123.3474214775786209, -9.988377603198976828, -10.36322818467138340 ) ) ;
#2404=CARTESIAN_POINT ( 'NONE',  ( 118.0718414775786300, -9.261995988541697145, -16.69588392320189030 ) ) ;
#2405=CARTESIAN_POINT ( 'NONE',  ( 114.4413348109119823, -9.261995988541697145, -16.69588392320189030 ) ) ;
#2407=CARTESIAN_POINT ( 'NONE',  ( 113.7606148109119886, -7.894159318335828068, -9.358103419637847864 ) ) ;
#2409=CARTESIAN_POINT ( 'NONE',  ( 112.1722681442453222, -8.899110576539710493, -16.42337572283490132 ) ) ;
#2410=CARTESIAN_POINT ( 'NONE',  ( 121.9859814775786333, 0.2603800115204892296, -16.42320221600525088 ) ) ;
#2411=CARTESIAN_POINT ( 'NONE',  ( 124.9357681442453014, -7.643976991954077427, -18.09477374809248928 ) ) ;
#2413=CARTESIAN_POINT ( 'NONE',  ( 112.4559014775786778, -0.1624402480850797581, -16.17319339645315424 ) ) ;
#2415=CARTESIAN_POINT ( 'NONE',  ( 119.2631014775786298, -9.565557343593413364, -10.61323700422348004 ) ) ;
#2416=CARTESIAN_POINT ( 'NONE',  ( 126.1837548109119211, -10.63000616557722466, -14.87417383870573495 ) ) ;
#2420=CARTESIAN_POINT ( 'NONE',  ( 119.4900081442453086, -7.643976991954077427, -18.09477374809248928 ) ) ;
#2422=CARTESIAN_POINT ( 'NONE',  ( 124.2558810407382026, -2.419733177069661512, -17.89711025544711376 ) ) ;
#2425=EDGE_CURVE ( 'NONE', #6914, #43250, #15665, .T. ) ;
#2426=CARTESIAN_POINT ( 'NONE',  ( 123.9714148109119805, -0.4660016031367893996, -10.09054647747474043 ) ) ;
#2434=CARTESIAN_POINT ( 'NONE',  ( 137.3593431606284696, -4.917112010162052016, -18.55357672982330541 ) ) ;
#2436=CARTESIAN_POINT ( 'NONE',  ( 125.1088394146763818, -2.481781793725739593, -17.81448324536422234 ) ) ;
#2437=CARTESIAN_POINT ( 'NONE',  ( 125.2761281442453054, -10.63000616557722466, -14.87417383870573495 ) ) ;
#2438=CARTESIAN_POINT ( 'NONE',  ( 118.9794681442453026, -0.8288870151387760510, -10.36305467784173118 ) ) ;
#2442=CARTESIAN_POINT ( 'NONE',  ( 124.3117748109119844, -10.30919188438810075, -12.61870101168855918 ) ) ;
#2443=CARTESIAN_POINT ( 'NONE',  ( 115.7460481442453357, 0.9020085738987339008, -11.91225656197089222 ) ) ;
#2445=CARTESIAN_POINT ( 'NONE',  ( 113.5904348109119866, -7.893985811506177619, -18.51759400769804742 ) ) ;
#2448=CARTESIAN_POINT ( 'NONE',  ( 125.0492214775786266, -3.505236298600246325, -18.68346056562440793 ) ) ;
#2449=CARTESIAN_POINT ( 'NONE',  ( 123.5743281442453139, -7.893985811506177619, -18.51759400769804742 ) ) ;
#2452=CARTESIAN_POINT ( 'NONE',  ( 115.4056881442453459, -2.084020599724406786, -8.691656652584148546 ) ) ;
#2453=CARTESIAN_POINT ( 'NONE',  ( 117.2776681442452968, -4.153390946401325223, -8.397313243818185668 ) ) ;
#2458=CARTESIAN_POINT ( 'NONE',  ( 124.9924948109119924, -5.574606645277164318, -18.38911715685844683 ) ) ;
#2465=CARTESIAN_POINT ( 'NONE',  ( 116.8805814775786445, -6.344957434206662583, -7.627207830600332805 ) ) ;
#2466=CARTESIAN_POINT ( 'NONE',  ( 124.5954081442453116, -6.222761293078241884, -8.102969835052219238 ) ) ;
#2467=CARTESIAN_POINT ( 'NONE',  ( 115.1220548109119761, -1.833838273342658809, -17.42832698103878286 ) ) ;
#2468=CARTESIAN_POINT ( 'NONE',  ( 112.1260814775786514, -8.862178061932382889, -16.39564131203247399 ) ) ;
#2469=CARTESIAN_POINT ( 'NONE',  ( 121.9292548109119849, -1.561330072975668948, -17.79121239304076951 ) ) ;
#2470=CARTESIAN_POINT ( 'NONE',  ( 114.8951481442453115, -0.4660016031367893996, -10.09054647747474043 ) ) ;
#2472=EDGE_CURVE ( 'NONE', #1202, #29255, #30661, .T. ) ;
#2474=CARTESIAN_POINT ( 'NONE',  ( 125.7866681442452688, -0.4660016031367893996, -10.09054647747474043 ) ) ;
#2477=CARTESIAN_POINT ( 'NONE',  ( 116.3700414775786527, -5.638512984488999180, -18.83840828888717311 ) ) ;
#2478=CARTESIAN_POINT ( 'NONE',  ( 115.3489614775786407, -0.8288870151387760510, -10.36305467784173118 ) ) ;
#2481=CARTESIAN_POINT ( 'NONE',  ( 126.5808414775786446, -9.859900752359378018, -12.68260735090039759 ) ) ;
#2483=CARTESIAN_POINT ( 'NONE',  ( 120.9649014775786355, -3.383040157471821630, -19.15922257007629170 ) ) ;
#2486=CARTESIAN_POINT ( 'NONE',  ( 125.0876622310133399, -1.244021962887375432, -16.96476564598603431 ) ) ;
#2487=CARTESIAN_POINT ( 'NONE',  ( 116.8238548109119819, -5.574606645277164318, -18.38911715685844683 ) ) ;
#2488=CARTESIAN_POINT ( 'NONE',  ( 112.4960109814547309, -2.395992375830773291, -17.92872468182854462 ) ) ;
#2489=CARTESIAN_POINT ( 'NONE',  ( 117.8449348109119938, -1.833838273342659253, -17.42832698103878286 ) ) ;
#2492=CARTESIAN_POINT ( 'NONE',  ( 115.9162281442453093, -5.574606645277164318, -18.38911715685844683 ) ) ;
#2493=CARTESIAN_POINT ( 'NONE',  ( 117.2776681442452968, -5.638512984488999180, -18.83840828888717311 ) ) ;
#2495=CARTESIAN_POINT ( 'NONE',  ( 125.6164881442453094, -9.565557343593413364, -10.61323700422348004 ) ) ;
#2496=CARTESIAN_POINT ( 'NONE',  ( 114.3846081442453197, 0.4262465694468514643, -12.03445270309931736 ) ) ;
#2497=CARTESIAN_POINT ( 'NONE',  ( 122.2696148109119889, -4.089484607189486809, -7.948022111789456723 ) ) ;
#2498=EDGE_CURVE ( 'NONE', #31245, #40595, #41393, .T. ) ;
#2500=CARTESIAN_POINT ( 'NONE',  ( 121.3619881442452879, -4.089484607189486809, -7.948022111789456723 ) ) ;
#2502=CARTESIAN_POINT ( 'NONE',  ( 114.3278814775786429, -10.30919188438810075, -12.61870101168855918 ) ) ;
#2506=CARTESIAN_POINT ( 'NONE',  ( 128.0593593558783425, -4.017378915256145433, -15.76970282473099516 ) ) ;
#2507=CARTESIAN_POINT ( 'NONE',  ( 119.3765548109119834, 0.9020085738987339008, -11.91225656197089222 ) ) ;
#2512=CARTESIAN_POINT ( 'NONE',  ( 114.7249681442453237, -9.565557343593413364, -10.61323700422348004 ) ) ;
#2514=CARTESIAN_POINT ( 'NONE',  ( 119.2063748109119814, -1.561330072975668504, -17.79121239304076951 ) ) ;
#2519=CARTESIAN_POINT ( 'NONE',  ( 123.8012348109119642, -9.565557343593413364, -10.61323700422348004 ) ) ;
#2520=CARTESIAN_POINT ( 'NONE',  ( 121.1918081442452859, 0.9020085738987339008, -11.91225656197089222 ) ) ;
#2521=CARTESIAN_POINT ( 'NONE',  ( 113.2500748109119968, -3.505236298600246325, -18.68346056562440793 ) ) ;
#2522=CARTESIAN_POINT ( 'NONE',  ( 114.4980614775786592, -7.893985811506177619, -18.51759400769804742 ) ) ;
#2523=CARTESIAN_POINT ( 'NONE',  ( 118.7315769107182177, -2.467220198592778413, -17.83387418641524391 ) ) ;
#2524=CARTESIAN_POINT ( 'NONE',  ( 126.5010429760475574, -1.163263821645348584, -9.824252222897710496 ) ) ;
#2525=CARTESIAN_POINT ( 'NONE',  ( 118.3554748109119998, -9.565557343593413364, -10.61323700422348004 ) ) ;
#2528=CARTESIAN_POINT ( 'NONE',  ( 120.0465871478583466, -3.807985514183269693, -19.09877912889401230 ) ) ;
#2529=CARTESIAN_POINT ( 'NONE',  ( 112.9664414775786412, 0.5811942927096154232, -14.16772938898807155 ) ) ;
#2530=CARTESIAN_POINT ( 'NONE',  ( 121.8158014775786171, -4.153390946401325223, -8.397313243818185668 ) ) ;
#2533=CARTESIAN_POINT ( 'NONE',  ( 118.9794681442453026, -9.261995988541697145, -16.69588392320189030 ) ) ;
#2536=CARTESIAN_POINT ( 'NONE',  ( 116.5969481442453031, -9.859900752359374465, -12.68260735090039404 ) ) ;
#2538=VERTEX_POINT ( 'NONE', #20632 ) ;
#2539=CARTESIAN_POINT ( 'NONE',  ( 112.0588148109119828, 0.5811942927096154232, -14.16772938898807155 ) ) ;
#2540=CARTESIAN_POINT ( 'NONE',  ( 121.7023481442452777, -0.8288870151387760510, -10.36305467784173118 ) ) ;
#2544=CARTESIAN_POINT ( 'NONE',  ( 118.4689281442453392, 0.9020085738987339008, -11.91225656197089222 ) ) ;
#2546=CARTESIAN_POINT ( 'NONE',  ( 119.0929214775786278, -5.638512984488999180, -18.83840828888717311 ) ) ;
#2547=CARTESIAN_POINT ( 'NONE',  ( 114.5547881442453217, -5.638512984488999180, -18.83840828888717311 ) ) ;
#2548=CARTESIAN_POINT ( 'NONE',  ( 118.8660148109119774, 0.1319031606808879209, -14.10382304977623669 ) ) ;
#2549=CARTESIAN_POINT ( 'NONE',  ( 124.7088614775786226, -9.565557343593413364, -10.61323700422348004 ) ) ;
#2550=CARTESIAN_POINT ( 'NONE',  ( 112.0588148109119828, 0.5811942927096154232, -14.16772938898807155 ) ) ;
#2552=CARTESIAN_POINT ( 'NONE',  ( 125.1626748109119802, -0.1624402480850797581, -16.17319339645315424 ) ) ;
#2554=CARTESIAN_POINT ( 'NONE',  ( 135.3184548109119874, -9.609004340414083245, -9.721032963308941177 ) ) ;
#2560=CARTESIAN_POINT ( 'NONE',  ( 122.5532481442453019, -10.63000616557722466, -14.87417383870573495 ) ) ;
#2561=CARTESIAN_POINT ( 'NONE',  ( 123.1205148109119563, -7.643976991954077427, -18.09477374809248928 ) ) ;
#2563=CARTESIAN_POINT ( 'NONE',  ( 125.1059481442452750, -8.166667518702819706, -8.995218007635861213 ) ) ;
#2564=CARTESIAN_POINT ( 'NONE',  ( 113.9307948109119764, -10.15424416112533912, -14.75197769757731336 ) ) ;
#2566=CARTESIAN_POINT ( 'NONE',  ( 121.1918081442452859, 0.9020085738987339008, -11.91225656197089222 ) ) ;
#2567=CARTESIAN_POINT ( 'NONE',  ( 122.6099748109119929, -9.261995988541697145, -16.69588392320189030 ) ) ;
#2569=CARTESIAN_POINT ( 'NONE',  ( 124.2550481442452792, -0.1624402480850797581, -16.17319339645315424 ) ) ;
#2574=CARTESIAN_POINT ( 'NONE',  ( 112.5693548109119888, 0.4262465694468514643, -12.03445270309931736 ) ) ;
#2575=CARTESIAN_POINT ( 'NONE',  ( 125.0492214775786266, -3.505236298600246325, -18.68346056562440793 ) ) ;
#2578=CARTESIAN_POINT ( 'NONE',  ( 117.4478481442453131, -9.565557343593413364, -10.61323700422348004 ) ) ;
#2580=CARTESIAN_POINT ( 'NONE',  ( 115.8027748109119841, -8.899110576539710493, -16.42337572283490132 ) ) ;
#2581=CARTESIAN_POINT ( 'NONE',  ( 123.1772414775786189, -4.089484607189486809, -7.948022111789456723 ) ) ;
#2583=CARTESIAN_POINT ( 'NONE',  ( 121.3619881442452879, -5.574606645277164318, -18.38911715685844683 ) ) ;
#2584=CARTESIAN_POINT ( 'NONE',  ( 118.0718414775786300, -9.261995988541697145, -16.69588392320189030 ) ) ;
#2585=CARTESIAN_POINT ( 'NONE',  ( 123.9714148109119805, -0.4660016031367893996, -10.09054647747474043 ) ) ;
#2586=CARTESIAN_POINT ( 'NONE',  ( 124.1415948109119540, -3.505236298600246325, -18.68346056562440793 ) ) ;
#2591=CARTESIAN_POINT ( 'NONE',  ( 125.1626748109119802, -9.988377603198980381, -10.36322818467138518 ) ) ;
#2592=CARTESIAN_POINT ( 'NONE',  ( 116.1431348109119881, 0.1319031606808879209, -14.10382304977623669 ) ) ;
#2593=CARTESIAN_POINT ( 'NONE',  ( 124.3117748109119844, -10.30919188438810075, -12.61870101168855918 ) ) ;
#2601=CARTESIAN_POINT ( 'NONE',  ( 117.7882081442453170, -3.505236298600246325, -18.68346056562440793 ) ) ;
#2602=CARTESIAN_POINT ( 'NONE',  ( 114.4980614775786734, -2.084020599724406786, -8.691656652584148546 ) ) ;
#2603=CARTESIAN_POINT ( 'NONE',  ( 125.5597614775786326, -7.894159318335813857, -9.358103419637837206 ) ) ;
#2606=CARTESIAN_POINT ( 'NONE',  ( 119.2631014775786298, -9.565557343593413364, -10.61323700422348004 ) ) ;
#2607=CARTESIAN_POINT ( 'NONE',  ( 113.9307948109119764, -10.15424416112533912, -14.75197769757731336 ) ) ;
#2609=CARTESIAN_POINT ( 'NONE',  ( 111.5020881442453202, -0.2054726073303936307, -16.14774885094461965 ) ) ;
#2611=CARTESIAN_POINT ( 'NONE',  ( 123.1205148109119563, -1.834011780172310813, -8.268836392978581529 ) ) ;
#2613=CARTESIAN_POINT ( 'NONE',  ( 112.5126281442453120, -10.30919188438810075, -12.61870101168855918 ) ) ;
#2614=VERTEX_POINT ( 'NONE', #11645 ) ;
#2618=CARTESIAN_POINT ( 'NONE',  ( 111.8886348109120092, -3.383040157471821630, -19.15922257007629170 ) ) ;
#2619=CARTESIAN_POINT ( 'NONE',  ( 120.7947214775786193, -0.8288870151387760510, -10.36305467784173118 ) ) ;
#2623=CARTESIAN_POINT ( 'NONE',  ( 128.2184548109119930, -4.863998795839242995, -13.39321520033831447 ) ) ;
#2624=CARTESIAN_POINT ( 'NONE',  ( 112.6260814775786514, -0.8288870151387760510, -10.36305467784173118 ) ) ;
#2628=CARTESIAN_POINT ( 'NONE',  ( 125.8433948109119456, -1.834011780172310813, -8.268836392978581529 ) ) ;
#2629=CARTESIAN_POINT ( 'NONE',  ( 123.2339681442453241, -6.344957434206665248, -7.627207830600338134 ) ) ;
#2632=CARTESIAN_POINT ( 'NONE',  ( 119.4900081442453086, -1.834011780172310813, -8.268836392978581529 ) ) ;
#2633=CARTESIAN_POINT ( 'NONE',  ( 114.0442481442453300, -1.834011780172310813, -8.268836392978581529 ) ) ;
#2634=VERTEX_POINT ( 'NONE', #7773 ) ;
#2635=CARTESIAN_POINT ( 'NONE',  ( 114.6115148109119986, -6.222761293078241884, -8.102969835052219238 ) ) ;
#2636=CARTESIAN_POINT ( 'NONE',  ( 112.9097148109120070, -9.565557343593413364, -10.61323700422348004 ) ) ;
#2637=CARTESIAN_POINT ( 'NONE',  ( 124.7655881442452852, 0.5811942927096110934, -14.16772938898807510 ) ) ;
#2638=CARTESIAN_POINT ( 'NONE',  ( 113.4202548109119846, -10.30919188438810075, -12.61870101168855918 ) ) ;
#2640=CARTESIAN_POINT ( 'NONE',  ( 113.1366214775786432, -7.643976991954077427, -18.09477374809248928 ) ) ;
#2642=CARTESIAN_POINT ( 'NONE',  ( 116.0296814775786345, -1.833838273342658809, -17.42832698103878286 ) ) ;
#2643=CARTESIAN_POINT ( 'NONE',  ( 112.5693548109119888, -10.63000616557722466, -14.87417383870573495 ) ) ;
#2645=CARTESIAN_POINT ( 'NONE',  ( 123.1772414775786189, -5.574606645277164318, -18.38911715685844683 ) ) ;
#2648=VERTEX_POINT ( 'NONE', #25778 ) ;
#2650=CARTESIAN_POINT ( 'NONE',  ( 125.9568481442452850, -6.344957434206665248, -7.627207830600338134 ) ) ;
#2658=AXIS2_PLACEMENT_3D ( 'NONE', #38258, #38475, #4506 ) ;
#2659=CARTESIAN_POINT ( 'NONE',  ( 117.9016614775786280, -9.988377603198976828, -10.36322818467138340 ) ) ;
#2662=( BOUNDED_SURFACE ( )  B_SPLINE_SURFACE ( 1, 2, ( 
 ( #28413, #808, #17921, #1262, #18378, #42101, #42546, #25667, #32266, #4457, #10864, #38648, #15172, #21340, #590, #3774, #28639, #14500, #32041, #1034, #14951, #14726, #29078, #35225, #39572, #22014, #28862, #17698, #21565, #31596, #365, #7419, #14276, #42322, #24759, #42990, #35909, #11084, #4674, #24986, #38880, #7650, #15625, #37029, #15856, #32707, #29980, #26108, #29305, #15401, #22234, #8780, #18816, #1480, #12666, #19716, #33602, #32928, #40477, #33153, #40015, #2379, #19496, #29751, #43218, #25887, #16308, #8560, #5125, #40702, #43663, #19041, #19274, #22911, #12439, #1929, #5797, #22460, #12895, #9238, #33375, #36130, #22684, #4900, #11986, #39789, #36354, #29531, #1704, #30209, #36804, #43446, #44130, #12211, #26793, #2145, #36582, #5358, #26338, #40246, #43898, #9014, #5571, #16076, #26564, #23147, #6026, #19949, #477, #7540, #21457, #20185, #28302, #21010, #27862, #35340, #4112, #256, #27021, #33837, #34070, #21233, #14615, #28083, #16765, #2606, #40936, #18033, #42214, #695, #14165, #24654, #3893, #10975, #31930, #17593, #28532, #31707, #34884, #23606, #38539, #30435, #3672, #2836, #24878, #31487, #14390, #16538, #6265, #35112, #37491, #38770, #9460, #23372, #7314, #17813, #44354, #37253, #24431, #41991, #37, #13114, #9689, #30662, #13950, #41772, #10532, #38323, #7100, #10756, #11202, #25336, #26005, #12101, #926, #11646, #8225, #22131, #4568, #36475, #19158, #1814, #35796, #36024, #11431, #8670, #25779, #35569, #4792, #33039, #25555, #32604, #18713, #15741, #28755, #42438, #36248, #39909, #22573, #25107, #32382, #5242, #39004, #18262, #39461, #1149, #7774, #1373, #11875, #39229, #21681, #39686, #18933, #15286, #29193, #43105, #4342, #32158, #7994, #18492, #14845, #8451, #22354, #5015, #15066, #42885, #15511, #42660, #28980, #21902, #32820, #1590, #29418, #43332, #20070, #26225, #19381, #2495, #30320, #44246, #37142, #44015, #36691, #5686, #33725, #40360, #16424, #5916, #22797, #29643, #23721, #27131, #33489, #41055, #29871, #43557, #9349 ),
 ( #13004, #36915, #40134, #15968, #9812, #16649, #20293, #26903, #40823, #23494, #30544, #37611, #19838, #6385, #6150, #23259, #43786, #9578, #5461, #37380, #9124, #44465, #40590, #33956, #33269, #26458, #2723, #12551, #13230, #34178, #2953, #12326, #8899, #2044, #23028, #12777, #19605, #2267, #16195, #30099, #26679, #41501, #37829, #38486, #31213, #7261, #17103, #30771, #44921, #421, #31653, #20519, #45137, #13678, #28029, #27587, #21178, #10921, #35281, #197, #14113, #10041, #16880, #13896, #3617, #6834, #6606, #38713, #17756, #10257, #34399, #35053, #27802, #3836, #30995, #44697, #24164, #14337, #28251, #3180, #41716, #10481, #24382, #38056, #24822, #7482, #21401, #20739, #38268, #34619, #42160, #41937, #23948, #7049, #13457, #10700, #20960, #3406, #17323, #27361, #34832, #17535, #41281, #31430, #24603, #1096, #4739, #25503, #15012, #32766, #35513, #39857, #22301, #15231, #22520, #35745, #17979, #31879, #21625, #644, #42607, #14559, #1540, #18660, #38944, #18875, #39174, #15461, #29140, #11372, #29367, #42832, #28478, #11819, #7938, #11146, #42382, #4055, #4518, #25050, #7712, #39634, #43278, #12047, #14788, #36198, #28925, #21849, #25950, #8622, #39408, #4285, #18204, #28702, #43053, #32102, #22081, #25278, #869, #18441, #32330, #4963, #11593, #8171, #32551, #25727, #35969, #1320, #8397, #13178, #12954, #16140, #5416, #5860, #12277, #30042, #15918, #23437, #2211, #26850, #43509, #9755, #12721, #19332, #33218, #2666, #40763, #9519, #40308, #37321, #6092, #19782, #26173, #44192, #27080, #20011, #5634, #26624, #36417, #22741, #19554, #33432, #40538, #43958, #41001, #36643, #5185, #30266, #33896, #16599, #19102, #26398, #30492, #32989, #40079, #9299, #9072, #44412, #23207, #33664, #1992, #1763, #2442, #15689, #37085, #16364, #29591, #8842, #29816, #43732, #12501, #22974, #36864, #13840, #6999, #27533, #24113, #41886, #20243, #10205, #34129, #38007, #13623, #374, #2898, #14063, #16827, #13406, #41671, #24336, #38220, #31162, #6781, #30720, #44867, #27756, #34349 ) ),
 .UNSPECIFIED., .F., .F., .T. ) 
 B_SPLINE_SURFACE_WITH_KNOTS ( ( 2, 2 ),
 ( 3, 2, 2, 2, 2, 2, 2, 2, 2, 2, 2, 2, 2, 2, 2, 2, 2, 2, 2, 2, 2, 2, 2, 2, 2, 2, 2, 2, 2, 2, 2, 2, 2, 2, 2, 2, 2, 2, 2, 2, 2, 2, 2, 2, 2, 2, 2, 2, 2, 2, 2, 2, 2, 2, 2, 2, 2, 2, 2, 2, 2, 2, 2, 2, 2, 2, 2, 2, 2, 2, 2, 2, 2, 2, 2, 2, 2, 2, 2, 2, 2, 2, 2, 2, 2, 2, 2, 2, 2, 2, 2, 2, 2, 2, 2, 2, 2, 2, 2, 2, 2, 2, 2, 2, 2, 2, 2, 2, 2, 2, 2, 2, 2, 2, 2, 2, 2, 2, 2, 2, 2, 2, 2, 2, 2, 2, 2, 2, 3 ),
 ( 0.000000000000000000, 1.000000000000000000 ),
 ( 0.000000000000000000, 0.007812500000000000000, 0.01562500000000000000, 0.02343750000000000000, 0.03125000000000000000, 0.03906250000000000000, 0.04687500000000000000, 0.05468750000000000000, 0.06250000000000000000, 0.07031250000000000000, 0.07812500000000000000, 0.08593750000000000000, 0.09375000000000000000, 0.1015625000000000000, 0.1093750000000000000, 0.1171875000000000000, 0.1250000000000000000, 0.1328125000000000000, 0.1406250000000000000, 0.1484375000000000000, 0.1562500000000000000, 0.1640625000000000000, 0.1718750000000000000, 0.1796875000000000000, 0.1875000000000000000, 0.1953125000000000000, 0.2031250000000000000, 0.2109375000000000000, 0.2187500000000000000, 0.2265625000000000000, 0.2343750000000000000, 0.2421875000000000000, 0.2500000000000000000, 0.2578125000000000000, 0.2656250000000000000, 0.2734375000000000000, 0.2812500000000000000, 0.2890625000000000000, 0.2968750000000000000, 0.3046875000000000000, 0.3125000000000000000, 0.3203125000000000000, 0.3281250000000000000, 0.3359375000000000000, 0.3437500000000000000, 0.3515625000000000000, 0.3593750000000000000, 0.3671875000000000000, 0.3750000000000000000, 0.3828125000000000000, 0.3906250000000000000, 0.3984375000000000000, 0.4062500000000000000, 0.4140625000000000000, 0.4218750000000000000, 0.4296875000000000000, 0.4375000000000000000, 0.4453125000000000000, 0.4531250000000000000, 0.4609375000000000000, 0.4687500000000000000, 0.4765625000000000000, 0.4843750000000000000, 0.4921875000000000000, 0.5000000000000000000, 0.5078125000000000000, 0.5156250000000000000, 0.5234375000000000000, 0.5312500000000000000, 0.5390625000000000000, 0.5468750000000000000, 0.5546875000000000000, 0.5625000000000000000, 0.5703125000000000000, 0.5781250000000000000, 0.5859375000000000000, 0.5937500000000000000, 0.6015625000000000000, 0.6093750000000000000, 0.6171875000000000000, 0.6250000000000000000, 0.6328125000000000000, 0.6406250000000000000, 0.6484375000000000000, 0.6562500000000000000, 0.6640625000000000000, 0.6718750000000000000, 0.6796875000000000000, 0.6875000000000000000, 0.6953125000000000000, 0.7031250000000000000, 0.7109375000000000000, 0.7187500000000000000, 0.7265625000000000000, 0.7343750000000000000, 0.7421875000000000000, 0.7500000000000000000, 0.7578125000000000000, 0.7656250000000000000, 0.7734375000000000000, 0.7812500000000000000, 0.7890625000000000000, 0.7968750000000000000, 0.8046875000000000000, 0.8125000000000000000, 0.8203125000000000000, 0.8281250000000000000, 0.8359375000000000000, 0.8437500000000000000, 0.8515625000000000000, 0.8593750000000000000, 0.8671875000000000000, 0.8750000000000000000, 0.8828125000000000000, 0.8906250000000000000, 0.8984375000000000000, 0.9062500000000000000, 0.9140625000000000000, 0.9218750000000000000, 0.9296875000000000000, 0.9375000000000000000, 0.9453125000000000000, 0.9531250000000000000, 0.9609375000000000000, 0.9687500000000000000, 0.9765625000000000000, 0.9843750000000000000, 0.9921875000000000000, 1.000000000000000000 ),
 .UNSPECIFIED. ) 
 GEOMETRIC_REPRESENTATION_ITEM ( )  RATIONAL_B_SPLINE_SURFACE ( (
 ( 1.000000000000000000, 0.9238795325112869605, 1.000000000000000000, 0.9238795325112869605, 1.000000000000000000, 0.9238795325112869605, 1.000000000000000000, 0.9238795325112869605, 1.000000000000000000, 0.9238795325112869605, 1.000000000000000000, 0.9238795325112869605, 1.000000000000000000, 0.9238795325112869605, 1.000000000000000000, 0.9238795325112869605, 1.000000000000000000, 0.9238795325112869605, 1.000000000000000000, 0.9238795325112869605, 1.000000000000000000, 0.9238795325112869605, 1.000000000000000000, 0.9238795325112869605, 1.000000000000000000, 0.9238795325112869605, 1.000000000000000000, 0.9238795325112869605, 1.000000000000000000, 0.9238795325112869605, 1.000000000000000000, 0.9238795325112869605, 1.000000000000000000, 0.9238795325112869605, 1.000000000000000000, 0.9238795325112869605, 1.000000000000000000, 0.9238795325112869605, 1.000000000000000000, 0.9238795325112869605, 1.000000000000000000, 0.9238795325112869605, 1.000000000000000000, 0.9238795325112869605, 1.000000000000000000, 0.9238795325112869605, 1.000000000000000000, 0.9238795325112869605, 1.000000000000000000, 0.9238795325112869605, 1.000000000000000000, 0.9238795325112869605, 1.000000000000000000, 0.9238795325112869605, 1.000000000000000000, 0.9238795325112869605, 1.000000000000000000, 0.9238795325112869605, 1.000000000000000000, 0.9238795325112869605, 1.000000000000000000, 0.9238795325112869605, 1.000000000000000000, 0.9238795325112869605, 1.000000000000000000, 0.9238795325112869605, 1.000000000000000000, 0.9238795325112869605, 1.000000000000000000, 0.9238795325112869605, 1.000000000000000000, 0.9238795325112869605, 1.000000000000000000, 0.9238795325112869605, 1.000000000000000000, 0.9238795325112869605, 1.000000000000000000, 0.9238795325112869605, 1.000000000000000000, 0.9238795325112869605, 1.000000000000000000, 0.9238795325112869605, 1.000000000000000000, 0.9238795325112869605, 1.000000000000000000, 0.9238795325112869605, 1.000000000000000000, 0.9238795325112869605, 1.000000000000000000, 0.9238795325112869605, 1.000000000000000000, 0.9238795325112869605, 1.000000000000000000, 0.9238795325112869605, 1.000000000000000000, 0.9238795325112869605, 1.000000000000000000, 0.9238795325112869605, 1.000000000000000000, 0.9238795325112869605, 1.000000000000000000, 0.9238795325112869605, 1.000000000000000000, 0.9238795325112869605, 1.000000000000000000, 0.9238795325112869605, 1.000000000000000000, 0.9238795325112869605, 1.000000000000000000, 0.9238795325112869605, 1.000000000000000000, 0.9238795325112869605, 1.000000000000000000, 0.9238795325112869605, 1.000000000000000000, 0.9238795325112869605, 1.000000000000000000, 0.9238795325112869605, 1.000000000000000000, 0.9238795325112869605, 1.000000000000000000, 0.9238795325112869605, 1.000000000000000000, 0.9238795325112869605, 1.000000000000000000, 0.9238795325112869605, 1.000000000000000000, 0.9238795325112869605, 1.000000000000000000, 0.9238795325112869605, 1.000000000000000000, 0.9238795325112869605, 1.000000000000000000, 0.9238795325112869605, 1.000000000000000000, 0.9238795325112869605, 1.000000000000000000, 0.9238795325112869605, 1.000000000000000000, 0.9238795325112869605, 1.000000000000000000, 0.9238795325112869605, 1.000000000000000000, 0.9238795325112869605, 1.000000000000000000, 0.9238795325112869605, 1.000000000000000000, 0.9238795325112869605, 1.000000000000000000, 0.9238795325112869605, 1.000000000000000000, 0.9238795325112869605, 1.000000000000000000, 0.9238795325112869605, 1.000000000000000000, 0.9238795325112869605, 1.000000000000000000, 0.9238795325112869605, 1.000000000000000000, 0.9238795325112869605, 1.000000000000000000, 0.9238795325112869605, 1.000000000000000000, 0.9238795325112869605, 1.000000000000000000, 0.9238795325112869605, 1.000000000000000000, 0.9238795325112869605, 1.000000000000000000, 0.9238795325112869605, 1.000000000000000000, 0.9238795325112869605, 1.000000000000000000, 0.9238795325112869605, 1.000000000000000000, 0.9238795325112869605, 1.000000000000000000, 0.9238795325112869605, 1.000000000000000000, 0.9238795325112869605, 1.000000000000000000, 0.9238795325112869605, 1.000000000000000000, 0.9238795325112869605, 1.000000000000000000, 0.9238795325112869605, 1.000000000000000000, 0.9238795325112869605, 1.000000000000000000, 0.9238795325112869605, 1.000000000000000000, 0.9238795325112869605, 1.000000000000000000, 0.9238795325112869605, 1.000000000000000000, 0.9238795325112869605, 1.000000000000000000, 0.9238795325112869605, 1.000000000000000000, 0.9238795325112869605, 1.000000000000000000, 0.9238795325112869605, 1.000000000000000000, 0.9238795325112869605, 1.000000000000000000, 0.9238795325112869605, 1.000000000000000000, 0.9238795325112869605, 1.000000000000000000, 0.9238795325112869605, 1.000000000000000000, 0.9238795325112869605, 1.000000000000000000, 0.9238795325112869605, 1.000000000000000000, 0.9238795325112869605, 1.000000000000000000, 0.9238795325112869605, 1.000000000000000000, 0.9238795325112869605, 1.000000000000000000, 0.9238795325112869605, 1.000000000000000000, 0.9238795325112869605, 1.000000000000000000, 0.9238795325112869605, 1.000000000000000000, 0.9238795325112869605, 1.000000000000000000, 0.9238795325112869605, 1.000000000000000000, 0.9238795325112869605, 1.000000000000000000, 0.9238795325112869605, 1.000000000000000000, 0.9238795325112869605, 1.000000000000000000, 0.9238795325112869605, 1.000000000000000000, 0.9238795325112869605, 1.000000000000000000, 0.9238795325112869605, 1.000000000000000000, 0.9238795325112869605, 1.000000000000000000, 0.9238795325112869605, 1.000000000000000000, 0.9238795325112869605, 1.000000000000000000, 0.9238795325112869605, 1.000000000000000000, 0.9238795325112869605, 1.000000000000000000, 0.9238795325112869605, 1.000000000000000000, 0.9238795325112869605, 1.000000000000000000),
 ( 1.000000000000000000, 0.9238795325112869605, 1.000000000000000000, 0.9238795325112869605, 1.000000000000000000, 0.9238795325112869605, 1.000000000000000000, 0.9238795325112869605, 1.000000000000000000, 0.9238795325112869605, 1.000000000000000000, 0.9238795325112869605, 1.000000000000000000, 0.9238795325112869605, 1.000000000000000000, 0.9238795325112869605, 1.000000000000000000, 0.9238795325112869605, 1.000000000000000000, 0.9238795325112869605, 1.000000000000000000, 0.9238795325112869605, 1.000000000000000000, 0.9238795325112869605, 1.000000000000000000, 0.9238795325112869605, 1.000000000000000000, 0.9238795325112869605, 1.000000000000000000, 0.9238795325112869605, 1.000000000000000000, 0.9238795325112869605, 1.000000000000000000, 0.9238795325112869605, 1.000000000000000000, 0.9238795325112869605, 1.000000000000000000, 0.9238795325112869605, 1.000000000000000000, 0.9238795325112869605, 1.000000000000000000, 0.9238795325112869605, 1.000000000000000000, 0.9238795325112869605, 1.000000000000000000, 0.9238795325112869605, 1.000000000000000000, 0.9238795325112869605, 1.000000000000000000, 0.9238795325112869605, 1.000000000000000000, 0.9238795325112869605, 1.000000000000000000, 0.9238795325112869605, 1.000000000000000000, 0.9238795325112869605, 1.000000000000000000, 0.9238795325112869605, 1.000000000000000000, 0.9238795325112869605, 1.000000000000000000, 0.9238795325112869605, 1.000000000000000000, 0.9238795325112869605, 1.000000000000000000, 0.9238795325112869605, 1.000000000000000000, 0.9238795325112869605, 1.000000000000000000, 0.9238795325112869605, 1.000000000000000000, 0.9238795325112869605, 1.000000000000000000, 0.9238795325112869605, 1.000000000000000000, 0.9238795325112869605, 1.000000000000000000, 0.9238795325112869605, 1.000000000000000000, 0.9238795325112869605, 1.000000000000000000, 0.9238795325112869605, 1.000000000000000000, 0.9238795325112869605, 1.000000000000000000, 0.9238795325112869605, 1.000000000000000000, 0.9238795325112869605, 1.000000000000000000, 0.9238795325112869605, 1.000000000000000000, 0.9238795325112869605, 1.000000000000000000, 0.9238795325112869605, 1.000000000000000000, 0.9238795325112869605, 1.000000000000000000, 0.9238795325112869605, 1.000000000000000000, 0.9238795325112869605, 1.000000000000000000, 0.9238795325112869605, 1.000000000000000000, 0.9238795325112869605, 1.000000000000000000, 0.9238795325112869605, 1.000000000000000000, 0.9238795325112869605, 1.000000000000000000, 0.9238795325112869605, 1.000000000000000000, 0.9238795325112869605, 1.000000000000000000, 0.9238795325112869605, 1.000000000000000000, 0.9238795325112869605, 1.000000000000000000, 0.9238795325112869605, 1.000000000000000000, 0.9238795325112869605, 1.000000000000000000, 0.9238795325112869605, 1.000000000000000000, 0.9238795325112869605, 1.000000000000000000, 0.9238795325112869605, 1.000000000000000000, 0.9238795325112869605, 1.000000000000000000, 0.9238795325112869605, 1.000000000000000000, 0.9238795325112869605, 1.000000000000000000, 0.9238795325112869605, 1.000000000000000000, 0.9238795325112869605, 1.000000000000000000, 0.9238795325112869605, 1.000000000000000000, 0.9238795325112869605, 1.000000000000000000, 0.9238795325112869605, 1.000000000000000000, 0.9238795325112869605, 1.000000000000000000, 0.9238795325112869605, 1.000000000000000000, 0.9238795325112869605, 1.000000000000000000, 0.9238795325112869605, 1.000000000000000000, 0.9238795325112869605, 1.000000000000000000, 0.9238795325112869605, 1.000000000000000000, 0.9238795325112869605, 1.000000000000000000, 0.9238795325112869605, 1.000000000000000000, 0.9238795325112869605, 1.000000000000000000, 0.9238795325112869605, 1.000000000000000000, 0.9238795325112869605, 1.000000000000000000, 0.9238795325112869605, 1.000000000000000000, 0.9238795325112869605, 1.000000000000000000, 0.9238795325112869605, 1.000000000000000000, 0.9238795325112869605, 1.000000000000000000, 0.9238795325112869605, 1.000000000000000000, 0.9238795325112869605, 1.000000000000000000, 0.9238795325112869605, 1.000000000000000000, 0.9238795325112869605, 1.000000000000000000, 0.9238795325112869605, 1.000000000000000000, 0.9238795325112869605, 1.000000000000000000, 0.9238795325112869605, 1.000000000000000000, 0.9238795325112869605, 1.000000000000000000, 0.9238795325112869605, 1.000000000000000000, 0.9238795325112869605, 1.000000000000000000, 0.9238795325112869605, 1.000000000000000000, 0.9238795325112869605, 1.000000000000000000, 0.9238795325112869605, 1.000000000000000000, 0.9238795325112869605, 1.000000000000000000, 0.9238795325112869605, 1.000000000000000000, 0.9238795325112869605, 1.000000000000000000, 0.9238795325112869605, 1.000000000000000000, 0.9238795325112869605, 1.000000000000000000, 0.9238795325112869605, 1.000000000000000000, 0.9238795325112869605, 1.000000000000000000, 0.9238795325112869605, 1.000000000000000000, 0.9238795325112869605, 1.000000000000000000, 0.9238795325112869605, 1.000000000000000000, 0.9238795325112869605, 1.000000000000000000, 0.9238795325112869605, 1.000000000000000000, 0.9238795325112869605, 1.000000000000000000, 0.9238795325112869605, 1.000000000000000000, 0.9238795325112869605, 1.000000000000000000, 0.9238795325112869605, 1.000000000000000000, 0.9238795325112869605, 1.000000000000000000, 0.9238795325112869605, 1.000000000000000000, 0.9238795325112869605, 1.000000000000000000, 0.9238795325112869605, 1.000000000000000000, 0.9238795325112869605, 1.000000000000000000, 0.9238795325112869605, 1.000000000000000000, 0.9238795325112869605, 1.000000000000000000, 0.9238795325112869605, 1.000000000000000000, 0.9238795325112869605, 1.000000000000000000, 0.9238795325112869605, 1.000000000000000000, 0.9238795325112869605, 1.000000000000000000, 0.9238795325112869605, 1.000000000000000000, 0.9238795325112869605, 1.000000000000000000) ) ) 
 REPRESENTATION_ITEM ( '' )  SURFACE ( )  );
#2663=CARTESIAN_POINT ( 'NONE',  ( 121.0783548109119749, -9.565557343593413364, -10.61323700422348004 ) ) ;
#2666=CARTESIAN_POINT ( 'NONE',  ( 122.2128881442453263, -1.834011780172310813, -8.268836392978581529 ) ) ;
#2667=CARTESIAN_POINT ( 'NONE',  ( 120.9081748109119872, -5.638512984488999180, -18.83840828888717311 ) ) ;
#2668=CARTESIAN_POINT ( 'NONE',  ( 126.0135748109119902, -8.166667518702819706, -8.995218007635861213 ) ) ;
#2669=CARTESIAN_POINT ( 'NONE',  ( 112.2857214775786474, -5.574606645277164318, -18.38911715685844683 ) ) ;
#2670=CARTESIAN_POINT ( 'NONE',  ( 113.8740681442453138, 0.5811942927096154232, -14.16772938898807155 ) ) ;
#2671=CARTESIAN_POINT ( 'NONE',  ( 125.3328548109119964, -9.261995988541697145, -16.69588392320189030 ) ) ;
#2675=CARTESIAN_POINT ( 'NONE',  ( 115.9729548109119861, -3.505236298600246325, -18.68346056562440793 ) ) ;
#2676=CARTESIAN_POINT ( 'NONE',  ( 115.2922348109119781, 0.4262465694468514643, -12.03445270309931736 ) ) ;
#2681=CARTESIAN_POINT ( 'NONE',  ( 124.0281414775786146, -7.643976991954092526, -18.09477374809249284 ) ) ;
#2682=CARTESIAN_POINT ( 'NONE',  ( 113.5904348109119866, -7.893985811506177619, -18.51759400769804742 ) ) ;
#2683=CARTESIAN_POINT ( 'NONE',  ( 113.2134394150595966, -2.423081321603721694, -17.89265170041262465 ) ) ;
#2687=CARTESIAN_POINT ( 'NONE',  ( 123.5196897444113517, -2.961643921203012564, -14.67744431876825928 ) ) ;
#2691=CARTESIAN_POINT ( 'NONE',  ( 118.5823814775786360, -1.834011780172310813, -8.268836392978581529 ) ) ;
#2692=CARTESIAN_POINT ( 'NONE',  ( 123.5176014775786228, -0.8288870151387760510, -10.36305467784173118 ) ) ;
#2693=CARTESIAN_POINT ( 'NONE',  ( 119.3198281442452924, -9.859900752359374465, -12.68260735090039404 ) ) ;
#2696=CARTESIAN_POINT ( 'NONE',  ( 121.6456214775786293, -10.63000616557722466, -14.87417383870573495 ) ) ;
#2697=CARTESIAN_POINT ( 'NONE',  ( 119.6034614775786196, -6.344957434206665248, -7.627207830600338134 ) ) ;
#2700=CARTESIAN_POINT ( 'NONE',  ( 112.6828081442453282, -2.084020599724406786, -8.691656652584148546 ) ) ;
#2703=CARTESIAN_POINT ( 'NONE',  ( 117.7882081442453170, -6.344957434206665248, -7.627207830600338134 ) ) ;
#2705=B_SPLINE_CURVE_WITH_KNOTS ( 'NONE', 3,
 ( #25216, #28195, #39346, #32487, #35683, #39116, #3999, #25444, #8113, #34988 ),
 .UNSPECIFIED., .F., .F.,
 ( 4, 3, 3, 4 ),
 ( 0.000000000000000000, 0.0001671877560958114864, 0.0003343755126086559717, 0.0006438490228507209303 ),
 .UNSPECIFIED. ) ;
#2706=CARTESIAN_POINT ( 'NONE',  ( 114.3846081442453197, 0.4262465694468514643, -12.03445270309931736 ) ) ;
#2708=CARTESIAN_POINT ( 'NONE',  ( 125.6164881442453094, -9.565557343593413364, -10.61323700422348004 ) ) ;
#2710=CARTESIAN_POINT ( 'NONE',  ( 122.0994348109119443, 0.9020085738987339008, -11.91225656197089222 ) ) ;
#2713=CARTESIAN_POINT ( 'NONE',  ( 113.6471614775786492, -4.153390946401321671, -8.397313243818183892 ) ) ;
#2716=CARTESIAN_POINT ( 'NONE',  ( 116.0864081442453113, -0.1624402480850797581, -16.17319339645315424 ) ) ;
#2717=CARTESIAN_POINT ( 'NONE',  ( 123.4043428172204386, -3.870068077801122719, -15.96576694716182310 ) ) ;
#2718=CARTESIAN_POINT ( 'NONE',  ( 118.2987481442453088, -7.894159318335828068, -9.358103419637847864 ) ) ;
#2720=CARTESIAN_POINT ( 'NONE',  ( 117.3343948109119737, -6.222761293078241884, -8.102969835052219238 ) ) ;
#2721=CARTESIAN_POINT ( 'NONE',  ( 117.0507614775786465, -10.30919188438810075, -12.61870101168855918 ) ) ;
#2723=CARTESIAN_POINT ( 'NONE',  ( 113.1933481442453058, -4.089484607189486809, -7.948022111789456723 ) ) ;
#2724=CARTESIAN_POINT ( 'NONE',  ( 114.2711548109119803, -0.1624402480850797581, -16.17319339645315424 ) ) ;
#2725=CARTESIAN_POINT ( 'NONE',  ( 122.8368814775786291, -1.561330072975668948, -17.79121239304076951 ) ) ;
#2727=CARTESIAN_POINT ( 'NONE',  ( 117.5045748109119756, -9.859900752359374465, -12.68260735090039404 ) ) ;
#2729=CARTESIAN_POINT ( 'NONE',  ( 112.0020881442453344, 0.2603800115204892296, -16.42320221600525088 ) ) ;
#2735=CARTESIAN_POINT ( 'NONE',  ( 119.2063748109119814, -1.561330072975668504, -17.79121239304076951 ) ) ;
#2737=CARTESIAN_POINT ( 'NONE',  ( 125.5030348109119558, -3.383040157471821630, -19.15922257007629170 ) ) ;
#2738=CARTESIAN_POINT ( 'NONE',  ( 125.3328548109119964, -9.261995988541379177, -16.69588392320231307 ) ) ;
#2739=CARTESIAN_POINT ( 'NONE',  ( 113.8173414775786512, -9.565557343593413364, -10.61323700422348004 ) ) ;
#2740=ADVANCED_FACE ( 'NONE', ( #41500 ), #7791, .T. ) ;
#2741=CARTESIAN_POINT ( 'NONE',  ( 124.7088614775786226, 0.2603800115204892296, -16.42320221600525088 ) ) ;
#2746=FACE_OUTER_BOUND ( 'NONE', #2770, .T. ) ;
#2747=CARTESIAN_POINT ( 'NONE',  ( 124.0848681442452772, -5.574606645277164318, -18.38911715685844683 ) ) ;
#2748=CARTESIAN_POINT ( 'NONE',  ( 118.4122014775786340, 0.5811942927096110934, -14.16772938898807510 ) ) ;
#2750=CARTESIAN_POINT ( 'NONE',  ( 113.7606148109119886, -7.894159318335828068, -9.358103419637847864 ) ) ;
#2751=CARTESIAN_POINT ( 'NONE',  ( 116.9373081442452929, -8.166667518702817929, -8.995218007635861213 ) ) ;
#2754=CARTESIAN_POINT ( 'NONE',  ( 118.8660148109119774, 0.1319031606808879209, -14.10382304977623669 ) ) ;
#2758=CARTESIAN_POINT ( 'NONE',  ( 112.3991748109119868, -8.166667518702817929, -8.995218007635859436 ) ) ;
#2759=CARTESIAN_POINT ( 'NONE',  ( 122.8936081442453059, -9.565557343593413364, -10.61323700422348004 ) ) ;
#2763=CARTESIAN_POINT ( 'NONE',  ( 137.3374356171238730, -0.3302559494014912223, -10.88373700413916900 ) ) ;
#2766=CARTESIAN_POINT ( 'NONE',  ( 117.7314814775786260, -4.089484607189486809, -7.948022111789456723 ) ) ;
#2768=CARTESIAN_POINT ( 'NONE',  ( 116.0864081442453113, -0.1624402480850797581, -16.17319339645315424 ) ) ;
#2770=EDGE_LOOP ( 'NONE', ( #24436, #33308, #33257, #30830 ) ) ;
#2771=CARTESIAN_POINT ( 'NONE',  ( 124.3685014775786328, 0.4262465694468514643, -12.03445270309931736 ) ) ;
#2772=CARTESIAN_POINT ( 'NONE',  ( 120.9649014775786355, -6.222761293078241884, -8.102969835052219238 ) ) ;
#2775=CARTESIAN_POINT ( 'NONE',  ( 121.8158014775786171, -5.638512984488999180, -18.83840828888717311 ) ) ;
#2776=CARTESIAN_POINT ( 'NONE',  ( 111.5672066102589213, -9.129161674847271257, -16.62002394948158113 ) ) ;
#2778=CARTESIAN_POINT ( 'NONE',  ( 117.1127004873411863, -2.348512537728064675, -17.99195118506216318 ) ) ;
#2779=CARTESIAN_POINT ( 'NONE',  ( 119.2063748109119814, -1.561330072975668504, -17.79121239304076951 ) ) ;
#2780=CARTESIAN_POINT ( 'NONE',  ( 119.2063748109119814, -1.561330072975668504, -17.79121239304076951 ) ) ;
#2781=CARTESIAN_POINT ( 'NONE',  ( 120.1140014775786398, -7.894159318335828068, -9.358103419637847864 ) ) ;
#2782=CARTESIAN_POINT ( 'NONE',  ( 125.2761281442453054, 0.4262465694468514643, -12.03445270309931736 ) ) ;
#2783=CARTESIAN_POINT ( 'NONE',  ( 112.9097148109120070, 0.2603800115204892296, -16.42320221600525088 ) ) ;
#2785=CARTESIAN_POINT ( 'NONE',  ( 121.8725281442453223, -6.222761293078241884, -8.102969835052219238 ) ) ;
#2791=CARTESIAN_POINT ( 'NONE',  ( 121.5888948109119809, -10.30919188438810075, -12.61870101168855918 ) ) ;
#2792=CARTESIAN_POINT ( 'NONE',  ( 122.0994348109119443, -10.15424416112533912, -14.75197769757731336 ) ) ;
#2794=CARTESIAN_POINT ( 'NONE',  ( 125.0492214775786266, -6.344957434206665248, -7.627207830600338134 ) ) ;
#2795=CARTESIAN_POINT ( 'NONE',  ( 113.7038881442453402, -6.222761293078241884, -8.102969835052219238 ) ) ;
#2796=CARTESIAN_POINT ( 'NONE',  ( 121.7023481442452919, -0.8288870151387517371, -10.36305467784176315 ) ) ;
#2797=CARTESIAN_POINT ( 'NONE',  ( 119.2631014775786298, 0.2603800115204892296, -16.42320221600525088 ) ) ;
#2799=CARTESIAN_POINT ( 'NONE',  ( 122.3263414775786373, -6.344957434206665248, -7.627207830600338134 ) ) ;
#2801=CARTESIAN_POINT ( 'NONE',  ( 126.1270281442452870, 0.1319031606808879209, -14.10382304977623669 ) ) ;
#2802=CARTESIAN_POINT ( 'NONE',  ( 111.9645664091100912, -0.9924539043446216624, -17.29976612834909133 ) ) ;
#2805=CARTESIAN_POINT ( 'NONE',  ( 112.8529881442453302, -7.894159318335828068, -9.358103419637847864 ) ) ;
#2806=CARTESIAN_POINT ( 'NONE',  ( 122.5532481442453019, 0.4262465694468514643, -12.03445270309931736 ) ) ;
#2809=CARTESIAN_POINT ( 'NONE',  ( 118.5823814775786360, -7.643976991954077427, -18.09477374809248928 ) ) ;
#2810=CARTESIAN_POINT ( 'NONE',  ( 114.6115148109119986, -6.222761293078241884, -8.102969835052219238 ) ) ;
#2811=CARTESIAN_POINT ( 'NONE',  ( 124.7655881442452852, 0.5811942927096110934, -14.16772938898807510 ) ) ;
#2814=CARTESIAN_POINT ( 'NONE',  ( 122.3830681442452857, -1.833838273342659697, -17.42832698103878286 ) ) ;
#2815=CARTESIAN_POINT ( 'NONE',  ( 118.5256548109119876, -0.4660016031367893996, -10.09054647747474043 ) ) ;
#2816=CARTESIAN_POINT ( 'NONE',  ( 125.5030348109119558, -3.383040157471821630, -19.15922257007629170 ) ) ;
#2817=CARTESIAN_POINT ( 'NONE',  ( 125.1626748109119802, -0.1624402480850797581, -16.17319339645315424 ) ) ;
#2820=CARTESIAN_POINT ( 'NONE',  ( 123.3474214775786209, -9.988377603198976828, -10.36322818467138340 ) ) ;
#2821=CARTESIAN_POINT ( 'NONE',  ( 115.2922348109119781, 0.4262465694468514643, -12.03445270309931736 ) ) ;
#2822=CARTESIAN_POINT ( 'NONE',  ( 125.3895814775786448, -7.893985811506177619, -18.51759400769804742 ) ) ;
#2831=CARTESIAN_POINT ( 'NONE',  ( 123.4608748109119745, 0.4262465694468514643, -12.03445270309931736 ) ) ;
#2832=CARTESIAN_POINT ( 'NONE',  ( 114.9518748109119883, -7.643976991954077427, -18.09477374809248928 ) ) ;
#2833=CARTESIAN_POINT ( 'NONE',  ( 126.7702028005115125, -0.1768172365690781900, -10.97118840898372660 ) ) ;
#2835=CARTESIAN_POINT ( 'NONE',  ( 128.2184548109119930, -1.889072916127989776, -18.60376373290417362 ) ) ;
#2836=CARTESIAN_POINT ( 'NONE',  ( 120.2841814775786276, -10.15424416112533912, -14.75197769757731336 ) ) ;
#2837=CARTESIAN_POINT ( 'NONE',  ( 112.7962614775786676, -6.222761293078241884, -8.102969835052219238 ) ) ;
#2841=CARTESIAN_POINT ( 'NONE',  ( 124.9357681442453014, -1.834011780172310813, -8.268836392978581529 ) ) ;
#2843=CARTESIAN_POINT ( 'NONE',  ( 112.3991748109119868, -8.166667518702817929, -8.995218007635859436 ) ) ;
#2845=CARTESIAN_POINT ( 'NONE',  ( 113.8740681442453138, 0.5811942927096154232, -14.16772938898807155 ) ) ;
#2846=CARTESIAN_POINT ( 'NONE',  ( 128.2184548109119930, 0.6402711692277476274, -15.78131322003126868 ) ) ;
#2848=CARTESIAN_POINT ( 'NONE',  ( 124.3685014775786328, 0.4262465694468514643, -12.03445270309931736 ) ) ;
#2849=CARTESIAN_POINT ( 'NONE',  ( 122.8368814775786291, -7.894159318335828068, -9.358103419637847864 ) ) ;
#2854=FACE_OUTER_BOUND ( 'NONE', #2897, .T. ) ;
#2858=CARTESIAN_POINT ( 'NONE',  ( 125.4463081442452932, -5.638512984488999180, -18.83840828888717311 ) ) ;
#2859=CARTESIAN_POINT ( 'NONE',  ( 123.5176014775786228, -9.261995988541697145, -16.69588392320189030 ) ) ;
#2860=DIRECTION ( 'NONE',  ( 1.000000000000000000, 0.000000000000000000, 0.000000000000000000 ) ) ;
#2862=CARTESIAN_POINT ( 'NONE',  ( 118.6958348109119754, -6.344957434206665248, -7.627207830600338134 ) ) ;
#2866=CARTESIAN_POINT ( 'NONE',  ( 114.1009748109119784, -5.574606645277164318, -18.38911715685844683 ) ) ;
#2867=CARTESIAN_POINT ( 'NONE',  ( 112.1155414775786454, -10.15424416112533912, -14.75197769757731336 ) ) ;
#2868=CARTESIAN_POINT ( 'NONE',  ( 122.8368814775786291, -1.561330072975668948, -17.79121239304076951 ) ) ;
#2869=CARTESIAN_POINT ( 'NONE',  ( 115.9729548109119861, -6.344957434206662583, -7.627207830600332805 ) ) ;
#2871=CARTESIAN_POINT ( 'NONE',  ( 126.0135748109119902, -8.166667518702819706, -8.995218007635861213 ) ) ;
#2873=CARTESIAN_POINT ( 'NONE',  ( 116.4267681442453153, -6.222761293078241884, -8.102969835052219238 ) ) ;
#2874=CARTESIAN_POINT ( 'NONE',  ( 112.7395348109119766, -5.638512984488999180, -18.83840828888717311 ) ) ;
#2878=CARTESIAN_POINT ( 'NONE',  ( 122.3830681442452857, -1.833838273342659697, -17.42832698103878286 ) ) ;
#2882=CIRCLE ( 'NONE', #32701, 4.999999999999998224 ) ;
#2885=LINE ( 'NONE', #2198, #24754 ) ;
#2891=CARTESIAN_POINT ( 'NONE',  ( 119.7736414775786358, -10.30919188438810075, -12.61870101168855918 ) ) ;
#2892=CARTESIAN_POINT ( 'NONE',  ( 136.7407071004454338, -4.349533742155984761, -18.99919027275945282 ) ) ;
#2896=CARTESIAN_POINT ( 'NONE',  ( 121.1918081442452859, -10.15424416112533912, -14.75197769757731336 ) ) ;
#2897=EDGE_LOOP ( 'NONE', ( #25166, #9378, #14886, #18310 ) ) ;
#2898=CARTESIAN_POINT ( 'NONE',  ( 125.5597614775786326, -1.561330072975669392, -17.79121239304076951 ) ) ;
#2899=CARTESIAN_POINT ( 'NONE',  ( 120.5110881442453206, -6.344957434206665248, -7.627207830600338134 ) ) ;
#2901=CARTESIAN_POINT ( 'NONE',  ( 116.3700414775786527, -4.153390946401321671, -8.397313243818183892 ) ) ;
#2902=CARTESIAN_POINT ( 'NONE',  ( 123.8012348109119642, 0.2603800115204892296, -16.42320221600525088 ) ) ;
#2906=CARTESIAN_POINT ( 'NONE',  ( 116.0296814775786345, -1.833838273342658809, -17.42832698103878286 ) ) ;
#2907=CARTESIAN_POINT ( 'NONE',  ( 117.7314814775786260, -5.574606645277164318, -18.38911715685844683 ) ) ;
#2912=CARTESIAN_POINT ( 'NONE',  ( 114.6115148109119986, -3.383040157471821630, -19.15922257007629170 ) ) ;
#2920=CARTESIAN_POINT ( 'NONE',  ( 119.1496481442453046, -3.383040157471821630, -19.15922257007629170 ) ) ;
#2922=CARTESIAN_POINT ( 'NONE',  ( 114.4413348109119823, -9.261995988541697145, -16.69588392320189030 ) ) ;
#2923=CARTESIAN_POINT ( 'NONE',  ( 118.0151148109119816, 0.4262465694468514643, -12.03445270309931736 ) ) ;
#2927=CARTESIAN_POINT ( 'NONE',  ( 120.0572748109119772, -3.383040157471821630, -19.15922257007629170 ) ) ;
#2928=CARTESIAN_POINT ( 'NONE',  ( 116.8805814775786445, -6.344957434206662583, -7.627207830600332805 ) ) ;
#2931=CARTESIAN_POINT ( 'NONE',  ( 112.5693548109119888, 0.4262465694468514643, -12.03445270309931736 ) ) ;
#2932=CARTESIAN_POINT ( 'NONE',  ( 125.0849635773846842, -2.467220198597905867, -17.83387418641800437 ) ) ;
#2934=CARTESIAN_POINT ( 'NONE',  ( 117.1074881442453233, -10.63000616557722466, -14.87417383870573495 ) ) ;
#2936=CARTESIAN_POINT ( 'NONE',  ( 116.3133148109119759, -7.893985811506177619, -18.51759400769804742 ) ) ;
#2938=CARTESIAN_POINT ( 'NONE',  ( 122.4397948109119767, -9.988377603198976828, -10.36322818467138340 ) ) ;
#2941=CARTESIAN_POINT ( 'NONE',  ( 113.1933481442453058, -5.574606645277164318, -18.38911715685844683 ) ) ;
#2942=( BOUNDED_SURFACE ( )  B_SPLINE_SURFACE ( 1, 2, ( 
 ( #21336, #41213, #24103, #41660, #44858, #10860, #14053, #38643, #20458, #3116, #30935, #20900, #13612, #27522, #10196, #6771, #34557, #27969, #10636, #3341, #27745, #24540, #7197, #24325, #17260, #31149, #45070, #3770, #21108, #34984, #17694, #361, #31814, #35448, #585, #11303, #28409, #15396, #32482, #7646, #32703, #7879, #29300, #42985, #25212, #1474, #11533, #42318, #25661, #21787, #24982, #11079, #17917, #4452, #14495, #38876, #8330, #43213, #11980, #28635, #36125, #28858, #35678, #25882, #39784, #8107, #4223, #21561, #42542, #29074, #22454, #35904, #39111, #18141, #32036, #8553, #4894, #36348, #22008, #1256, #11752, #18811, #804, #25440, #14722, #39566, #42770, #18374, #15167, #32262, #39341, #1030, #14947, #4669, #22229, #18591, #12890, #33832, #19944, #2601, #1921, #33370, #29744, #2373, #43440, #23601, #19488, #19711, #12661, #2140, #12204, #26332, #9233, #15849, #37022, #26559, #26102, #5119, #44349, #16533, #9008, #30430, #5352, #19035, #29975, #32922, #40009, #13109, #30204, #33597, #8774, #1698, #15618, #22678, #29524, #16071, #36576, #40472, #9684, #6021, #19268, #33147, #43657, #5792, #27014, #22905, #36798, #12433, #40239, #40697, #5566, #43892, #23142, #16303, #44125, #26788, #40931, #9453, #23367, #37248, #44575, #3505, #7147, #10142, #14001, #10587, #10807, #13781, #6490, #20404, #3723, #27917, #41827, #41389, #24487, #38375, #21058, #42047, #309, #34936, #17642, #6717, #27693, #37486, #23833, #20628, #34505, #41610, #3283, #14223, #37719, #6260, #31314, #31540, #28138, #20180, #10365, #34065, #34289, #2831, #17205, #27469, #16760, #31098, #27244, #24273, #20843, #30657, #13340, #45023, #38161, #6937, #41158, #9919, #3061, #44800, #16989, #34722, #17422, #89, #24051, #37944, #30880, #13559, #11254, #35168, #25163, #14671, #1422, #3944, #15122, #21282, #14446, #42718, #25390, #22180, #11701, #15342, #28809, #39286, #18542, #25612, #4847, #32209, #29251, #1208, #4401, #38827, #8053, #536, #18317, #4173, #39515, #35626, #29028, #7831, #32434 ),
 ( #17867, #43160, #39060, #11484, #28585, #28353, #24702, #8278, #18091, #42266, #42939, #35847, #21509, #21959, #36076, #7595, #18766, #32655, #11031, #21737, #983, #14898, #31984, #38592, #7369, #31764, #747, #4621, #35397, #24930, #42495, #9397, #19890, #5067, #29469, #19433, #18983, #15565, #23308, #39959, #22627, #2092, #9177, #8721, #8954, #12607, #33318, #22854, #40642, #43384, #2547, #30152, #23084, #30377, #43606, #25826, #39733, #12152, #8502, #5298, #22406, #37192, #26509, #1641, #26734, #1864, #5966, #36965, #19214, #33777, #5513, #36299, #19655, #15793, #32872, #26055, #11928, #12382, #36525, #33094, #2321, #16474, #29695, #26280, #44068, #36745, #40188, #16018, #29926, #43840, #40417, #5736, #33542, #16249, #12834, #17156, #6441, #9628, #30599, #10530, #13508, #34234, #41770, #27416, #34009, #20572, #27639, #26953, #20791, #37886, #31043, #6662, #21008, #3670, #41107, #20350, #6202, #23998, #34449, #41553, #3008, #44749, #17374, #40875, #30825, #23549, #41336, #16930, #34882, #37432, #34671, #20124, #2780, #44973, #13730, #10313, #3230, #10095, #16705, #24215, #38106, #9865, #6881, #3457, #44516, #44299, #38321, #24429, #31262, #7098, #13281, #13054, #35, #17591, #27187, #23774, #13947, #27860, #37666, #28081, #254, #38537, #14163, #14613, #41989, #39001, #36639, #32985, #7312, #21231, #17811, #32155, #1759, #4110, #35338, #42212, #10754, #22516, #24876, #21455, #4339, #35566, #5412, #11428, #15685, #38768, #22737, #18031, #35110, #42657, #29587, #31928, #8619, #5181, #31484, #7771, #475, #14388, #43505, #36412, #19098, #693, #12272, #26169, #40074, #24652, #8838, #3891, #31705, #28530, #21678, #28300, #10973, #42436, #11200, #18259, #25105, #7538, #923, #14842, #25947, #28752, #39854, #33214, #9515, #16824, #33428, #1988, #44188, #37775, #26394, #30717, #44408, #33892, #40304, #15914, #29812, #9067, #43728, #2437, #12496, #26846, #23892, #20239, #22970, #36860, #5630, #20006, #34125, #37081, #23203, #30037, #19550, #9751, #12717, #9295, #37317 ) ),
 .UNSPECIFIED., .F., .F., .F. ) 
 B_SPLINE_SURFACE_WITH_KNOTS ( ( 2, 2 ),
 ( 3, 2, 2, 2, 2, 2, 2, 2, 2, 2, 2, 2, 2, 2, 2, 2, 2, 2, 2, 2, 2, 2, 2, 2, 2, 2, 2, 2, 2, 2, 2, 2, 2, 2, 2, 2, 2, 2, 2, 2, 2, 2, 2, 2, 2, 2, 2, 2, 2, 2, 2, 2, 2, 2, 2, 2, 2, 2, 2, 2, 2, 2, 2, 2, 2, 2, 2, 2, 2, 2, 2, 2, 2, 2, 2, 2, 2, 2, 2, 2, 2, 2, 2, 2, 2, 2, 2, 2, 2, 2, 2, 2, 2, 2, 2, 2, 2, 2, 2, 2, 2, 2, 2, 2, 2, 2, 2, 2, 2, 2, 2, 2, 2, 2, 2, 2, 2, 2, 2, 2, 2, 2, 2, 2, 2, 2, 2, 2, 3 ),
 ( 0.000000000000000000, 1.000000000000000000 ),
 ( 0.000000000000000000, 0.007812500000000000000, 0.01562500000000000000, 0.02343750000000000000, 0.03125000000000000000, 0.03906250000000000000, 0.04687500000000000000, 0.05468750000000000000, 0.06250000000000000000, 0.07031250000000000000, 0.07812500000000000000, 0.08593750000000000000, 0.09375000000000000000, 0.1015625000000000000, 0.1093750000000000000, 0.1171875000000000000, 0.1250000000000000000, 0.1328125000000000000, 0.1406250000000000000, 0.1484375000000000000, 0.1562500000000000000, 0.1640625000000000000, 0.1718750000000000000, 0.1796875000000000000, 0.1875000000000000000, 0.1953125000000000000, 0.2031250000000000000, 0.2109375000000000000, 0.2187500000000000000, 0.2265625000000000000, 0.2343750000000000000, 0.2421875000000000000, 0.2500000000000000000, 0.2578125000000000000, 0.2656250000000000000, 0.2734375000000000000, 0.2812500000000000000, 0.2890625000000000000, 0.2968750000000000000, 0.3046875000000000000, 0.3125000000000000000, 0.3203125000000000000, 0.3281250000000000000, 0.3359375000000000000, 0.3437500000000000000, 0.3515625000000000000, 0.3593750000000000000, 0.3671875000000000000, 0.3750000000000000000, 0.3828125000000000000, 0.3906250000000000000, 0.3984375000000000000, 0.4062500000000000000, 0.4140625000000000000, 0.4218750000000000000, 0.4296875000000000000, 0.4375000000000000000, 0.4453125000000000000, 0.4531250000000000000, 0.4609375000000000000, 0.4687500000000000000, 0.4765625000000000000, 0.4843750000000000000, 0.4921875000000000000, 0.5000000000000000000, 0.5078125000000000000, 0.5156250000000000000, 0.5234375000000000000, 0.5312500000000000000, 0.5390625000000000000, 0.5468750000000000000, 0.5546875000000000000, 0.5625000000000000000, 0.5703125000000000000, 0.5781250000000000000, 0.5859375000000000000, 0.5937500000000000000, 0.6015625000000000000, 0.6093750000000000000, 0.6171875000000000000, 0.6250000000000000000, 0.6328125000000000000, 0.6406250000000000000, 0.6484375000000000000, 0.6562500000000000000, 0.6640625000000000000, 0.6718750000000000000, 0.6796875000000000000, 0.6875000000000000000, 0.6953125000000000000, 0.7031250000000000000, 0.7109375000000000000, 0.7187500000000000000, 0.7265625000000000000, 0.7343750000000000000, 0.7421875000000000000, 0.7500000000000000000, 0.7578125000000000000, 0.7656250000000000000, 0.7734375000000000000, 0.7812500000000000000, 0.7890625000000000000, 0.7968750000000000000, 0.8046875000000000000, 0.8125000000000000000, 0.8203125000000000000, 0.8281250000000000000, 0.8359375000000000000, 0.8437500000000000000, 0.8515625000000000000, 0.8593750000000000000, 0.8671875000000000000, 0.8750000000000000000, 0.8828125000000000000, 0.8906250000000000000, 0.8984375000000000000, 0.9062500000000000000, 0.9140625000000000000, 0.9218750000000000000, 0.9296875000000000000, 0.9375000000000000000, 0.9453125000000000000, 0.9531250000000000000, 0.9609375000000000000, 0.9687500000000000000, 0.9765625000000000000, 0.9843750000000000000, 0.9921875000000000000, 1.000000000000000000 ),
 .UNSPECIFIED. ) 
 GEOMETRIC_REPRESENTATION_ITEM ( )  RATIONAL_B_SPLINE_SURFACE ( (
 ( 1.000000000000000000, 0.9238795325112869605, 1.000000000000000000, 0.9238795325112869605, 1.000000000000000000, 0.9238795325112869605, 1.000000000000000000, 0.9238795325112869605, 1.000000000000000000, 0.9238795325112869605, 1.000000000000000000, 0.9238795325112869605, 1.000000000000000000, 0.9238795325112869605, 1.000000000000000000, 0.9238795325112869605, 1.000000000000000000, 0.9238795325112869605, 1.000000000000000000, 0.9238795325112869605, 1.000000000000000000, 0.9238795325112869605, 1.000000000000000000, 0.9238795325112869605, 1.000000000000000000, 0.9238795325112869605, 1.000000000000000000, 0.9238795325112869605, 1.000000000000000000, 0.9238795325112869605, 1.000000000000000000, 0.9238795325112869605, 1.000000000000000000, 0.9238795325112869605, 1.000000000000000000, 0.9238795325112869605, 1.000000000000000000, 0.9238795325112869605, 1.000000000000000000, 0.9238795325112869605, 1.000000000000000000, 0.9238795325112869605, 1.000000000000000000, 0.9238795325112869605, 1.000000000000000000, 0.9238795325112869605, 1.000000000000000000, 0.9238795325112869605, 1.000000000000000000, 0.9238795325112869605, 1.000000000000000000, 0.9238795325112869605, 1.000000000000000000, 0.9238795325112869605, 1.000000000000000000, 0.9238795325112869605, 1.000000000000000000, 0.9238795325112869605, 1.000000000000000000, 0.9238795325112869605, 1.000000000000000000, 0.9238795325112869605, 1.000000000000000000, 0.9238795325112869605, 1.000000000000000000, 0.9238795325112869605, 1.000000000000000000, 0.9238795325112869605, 1.000000000000000000, 0.9238795325112869605, 1.000000000000000000, 0.9238795325112869605, 1.000000000000000000, 0.9238795325112869605, 1.000000000000000000, 0.9238795325112869605, 1.000000000000000000, 0.9238795325112869605, 1.000000000000000000, 0.9238795325112869605, 1.000000000000000000, 0.9238795325112869605, 1.000000000000000000, 0.9238795325112869605, 1.000000000000000000, 0.9238795325112869605, 1.000000000000000000, 0.9238795325112869605, 1.000000000000000000, 0.9238795325112869605, 1.000000000000000000, 0.9238795325112869605, 1.000000000000000000, 0.9238795325112869605, 1.000000000000000000, 0.9238795325112869605, 1.000000000000000000, 0.9238795325112869605, 1.000000000000000000, 0.9238795325112869605, 1.000000000000000000, 0.9238795325112869605, 1.000000000000000000, 0.9238795325112869605, 1.000000000000000000, 0.9238795325112869605, 1.000000000000000000, 0.9238795325112869605, 1.000000000000000000, 0.9238795325112869605, 1.000000000000000000, 0.9238795325112869605, 1.000000000000000000, 0.9238795325112869605, 1.000000000000000000, 0.9238795325112869605, 1.000000000000000000, 0.9238795325112869605, 1.000000000000000000, 0.9238795325112869605, 1.000000000000000000, 0.9238795325112869605, 1.000000000000000000, 0.9238795325112869605, 1.000000000000000000, 0.9238795325112869605, 1.000000000000000000, 0.9238795325112869605, 1.000000000000000000, 0.9238795325112869605, 1.000000000000000000, 0.9238795325112869605, 1.000000000000000000, 0.9238795325112869605, 1.000000000000000000, 0.9238795325112869605, 1.000000000000000000, 0.9238795325112869605, 1.000000000000000000, 0.9238795325112869605, 1.000000000000000000, 0.9238795325112869605, 1.000000000000000000, 0.9238795325112869605, 1.000000000000000000, 0.9238795325112869605, 1.000000000000000000, 0.9238795325112869605, 1.000000000000000000, 0.9238795325112869605, 1.000000000000000000, 0.9238795325112869605, 1.000000000000000000, 0.9238795325112869605, 1.000000000000000000, 0.9238795325112869605, 1.000000000000000000, 0.9238795325112869605, 1.000000000000000000, 0.9238795325112869605, 1.000000000000000000, 0.9238795325112869605, 1.000000000000000000, 0.9238795325112869605, 1.000000000000000000, 0.9238795325112869605, 1.000000000000000000, 0.9238795325112869605, 1.000000000000000000, 0.9238795325112869605, 1.000000000000000000, 0.9238795325112869605, 1.000000000000000000, 0.9238795325112869605, 1.000000000000000000, 0.9238795325112869605, 1.000000000000000000, 0.9238795325112869605, 1.000000000000000000, 0.9238795325112869605, 1.000000000000000000, 0.9238795325112869605, 1.000000000000000000, 0.9238795325112869605, 1.000000000000000000, 0.9238795325112869605, 1.000000000000000000, 0.9238795325112869605, 1.000000000000000000, 0.9238795325112869605, 1.000000000000000000, 0.9238795325112869605, 1.000000000000000000, 0.9238795325112869605, 1.000000000000000000, 0.9238795325112869605, 1.000000000000000000, 0.9238795325112869605, 1.000000000000000000, 0.9238795325112869605, 1.000000000000000000, 0.9238795325112869605, 1.000000000000000000, 0.9238795325112869605, 1.000000000000000000, 0.9238795325112869605, 1.000000000000000000, 0.9238795325112869605, 1.000000000000000000, 0.9238795325112869605, 1.000000000000000000, 0.9238795325112869605, 1.000000000000000000, 0.9238795325112869605, 1.000000000000000000, 0.9238795325112869605, 1.000000000000000000, 0.9238795325112869605, 1.000000000000000000, 0.9238795325112869605, 1.000000000000000000, 0.9238795325112869605, 1.000000000000000000, 0.9238795325112869605, 1.000000000000000000, 0.9238795325112869605, 1.000000000000000000, 0.9238795325112869605, 1.000000000000000000, 0.9238795325112869605, 1.000000000000000000, 0.9238795325112869605, 1.000000000000000000, 0.9238795325112869605, 1.000000000000000000, 0.9238795325112869605, 1.000000000000000000, 0.9238795325112869605, 1.000000000000000000, 0.9238795325112869605, 1.000000000000000000, 0.9238795325112869605, 1.000000000000000000, 0.9238795325112869605, 1.000000000000000000, 0.9238795325112869605, 1.000000000000000000, 0.9238795325112869605, 1.000000000000000000, 0.9238795325112869605, 1.000000000000000000, 0.9238795325112869605, 1.000000000000000000, 0.9238795325112869605, 1.000000000000000000, 0.9238795325112869605, 1.000000000000000000),
 ( 1.000000000000000000, 0.9238795325112869605, 1.000000000000000000, 0.9238795325112869605, 1.000000000000000000, 0.9238795325112869605, 1.000000000000000000, 0.9238795325112869605, 1.000000000000000000, 0.9238795325112869605, 1.000000000000000000, 0.9238795325112869605, 1.000000000000000000, 0.9238795325112869605, 1.000000000000000000, 0.9238795325112869605, 1.000000000000000000, 0.9238795325112869605, 1.000000000000000000, 0.9238795325112869605, 1.000000000000000000, 0.9238795325112869605, 1.000000000000000000, 0.9238795325112869605, 1.000000000000000000, 0.9238795325112869605, 1.000000000000000000, 0.9238795325112869605, 1.000000000000000000, 0.9238795325112869605, 1.000000000000000000, 0.9238795325112869605, 1.000000000000000000, 0.9238795325112869605, 1.000000000000000000, 0.9238795325112869605, 1.000000000000000000, 0.9238795325112869605, 1.000000000000000000, 0.9238795325112869605, 1.000000000000000000, 0.9238795325112869605, 1.000000000000000000, 0.9238795325112869605, 1.000000000000000000, 0.9238795325112869605, 1.000000000000000000, 0.9238795325112869605, 1.000000000000000000, 0.9238795325112869605, 1.000000000000000000, 0.9238795325112869605, 1.000000000000000000, 0.9238795325112869605, 1.000000000000000000, 0.9238795325112869605, 1.000000000000000000, 0.9238795325112869605, 1.000000000000000000, 0.9238795325112869605, 1.000000000000000000, 0.9238795325112869605, 1.000000000000000000, 0.9238795325112869605, 1.000000000000000000, 0.9238795325112869605, 1.000000000000000000, 0.9238795325112869605, 1.000000000000000000, 0.9238795325112869605, 1.000000000000000000, 0.9238795325112869605, 1.000000000000000000, 0.9238795325112869605, 1.000000000000000000, 0.9238795325112869605, 1.000000000000000000, 0.9238795325112869605, 1.000000000000000000, 0.9238795325112869605, 1.000000000000000000, 0.9238795325112869605, 1.000000000000000000, 0.9238795325112869605, 1.000000000000000000, 0.9238795325112869605, 1.000000000000000000, 0.9238795325112869605, 1.000000000000000000, 0.9238795325112869605, 1.000000000000000000, 0.9238795325112869605, 1.000000000000000000, 0.9238795325112869605, 1.000000000000000000, 0.9238795325112869605, 1.000000000000000000, 0.9238795325112869605, 1.000000000000000000, 0.9238795325112869605, 1.000000000000000000, 0.9238795325112869605, 1.000000000000000000, 0.9238795325112869605, 1.000000000000000000, 0.9238795325112869605, 1.000000000000000000, 0.9238795325112869605, 1.000000000000000000, 0.9238795325112869605, 1.000000000000000000, 0.9238795325112869605, 1.000000000000000000, 0.9238795325112869605, 1.000000000000000000, 0.9238795325112869605, 1.000000000000000000, 0.9238795325112869605, 1.000000000000000000, 0.9238795325112869605, 1.000000000000000000, 0.9238795325112869605, 1.000000000000000000, 0.9238795325112869605, 1.000000000000000000, 0.9238795325112869605, 1.000000000000000000, 0.9238795325112869605, 1.000000000000000000, 0.9238795325112869605, 1.000000000000000000, 0.9238795325112869605, 1.000000000000000000, 0.9238795325112869605, 1.000000000000000000, 0.9238795325112869605, 1.000000000000000000, 0.9238795325112869605, 1.000000000000000000, 0.9238795325112869605, 1.000000000000000000, 0.9238795325112869605, 1.000000000000000000, 0.9238795325112869605, 1.000000000000000000, 0.9238795325112869605, 1.000000000000000000, 0.9238795325112869605, 1.000000000000000000, 0.9238795325112869605, 1.000000000000000000, 0.9238795325112869605, 1.000000000000000000, 0.9238795325112869605, 1.000000000000000000, 0.9238795325112869605, 1.000000000000000000, 0.9238795325112869605, 1.000000000000000000, 0.9238795325112869605, 1.000000000000000000, 0.9238795325112869605, 1.000000000000000000, 0.9238795325112869605, 1.000000000000000000, 0.9238795325112869605, 1.000000000000000000, 0.9238795325112869605, 1.000000000000000000, 0.9238795325112869605, 1.000000000000000000, 0.9238795325112869605, 1.000000000000000000, 0.9238795325112869605, 1.000000000000000000, 0.9238795325112869605, 1.000000000000000000, 0.9238795325112869605, 1.000000000000000000, 0.9238795325112869605, 1.000000000000000000, 0.9238795325112869605, 1.000000000000000000, 0.9238795325112869605, 1.000000000000000000, 0.9238795325112869605, 1.000000000000000000, 0.9238795325112869605, 1.000000000000000000, 0.9238795325112869605, 1.000000000000000000, 0.9238795325112869605, 1.000000000000000000, 0.9238795325112869605, 1.000000000000000000, 0.9238795325112869605, 1.000000000000000000, 0.9238795325112869605, 1.000000000000000000, 0.9238795325112869605, 1.000000000000000000, 0.9238795325112869605, 1.000000000000000000, 0.9238795325112869605, 1.000000000000000000, 0.9238795325112869605, 1.000000000000000000, 0.9238795325112869605, 1.000000000000000000, 0.9238795325112869605, 1.000000000000000000, 0.9238795325112869605, 1.000000000000000000, 0.9238795325112869605, 1.000000000000000000, 0.9238795325112869605, 1.000000000000000000, 0.9238795325112869605, 1.000000000000000000, 0.9238795325112869605, 1.000000000000000000, 0.9238795325112869605, 1.000000000000000000, 0.9238795325112869605, 1.000000000000000000, 0.9238795325112869605, 1.000000000000000000, 0.9238795325112869605, 1.000000000000000000, 0.9238795325112869605, 1.000000000000000000, 0.9238795325112869605, 1.000000000000000000, 0.9238795325112869605, 1.000000000000000000, 0.9238795325112869605, 1.000000000000000000, 0.9238795325112869605, 1.000000000000000000, 0.9238795325112869605, 1.000000000000000000, 0.9238795325112869605, 1.000000000000000000, 0.9238795325112869605, 1.000000000000000000, 0.9238795325112869605, 1.000000000000000000, 0.9238795325112869605, 1.000000000000000000, 0.9238795325112869605, 1.000000000000000000, 0.9238795325112869605, 1.000000000000000000, 0.9238795325112869605, 1.000000000000000000, 0.9238795325112869605, 1.000000000000000000) ) ) 
 REPRESENTATION_ITEM ( '' )  SURFACE ( )  );
#2943=DIRECTION ( 'NONE',  ( 0.000000000000000000, 0.6004852223388321697, -0.7996358532186279566 ) ) ;
#2944=CARTESIAN_POINT ( 'NONE',  ( 115.2922348109119781, 0.4262465694468514643, -12.03445270309931736 ) ) ;
#2945=CARTESIAN_POINT ( 'NONE',  ( 120.2905000025837126, -2.311015703046761072, -18.04188382666269774 ) ) ;
#2946=CARTESIAN_POINT ( 'NONE',  ( 118.0718414775786442, -0.8288870151387760510, -10.36305467784173118 ) ) ;
#2949=CARTESIAN_POINT ( 'NONE',  ( 117.2209414775786485, -2.084020599724406786, -8.691656652584148546 ) ) ;
#2951=CARTESIAN_POINT ( 'NONE',  ( 114.3846081442453197, -10.63000616557722466, -14.87417383870573495 ) ) ;
#2953=CARTESIAN_POINT ( 'NONE',  ( 113.4202548109119846, -10.30919188438810075, -12.61870101168855918 ) ) ;
#2954=CARTESIAN_POINT ( 'NONE',  ( 115.8027748109119841, -8.899110576539710493, -16.42337572283490132 ) ) ;
#2955=CARTESIAN_POINT ( 'NONE',  ( 113.5337081442453240, -0.8288870151387760510, -10.36305467784173118 ) ) ;
#2956=CARTESIAN_POINT ( 'NONE',  ( 115.9162281442453235, -5.574606645277164318, -18.38911715685844683 ) ) ;
#2958=CARTESIAN_POINT ( 'NONE',  ( 114.0442481442453300, -1.834011780172310813, -8.268836392978581529 ) ) ;
#2963=CARTESIAN_POINT ( 'NONE',  ( 117.2776681442452968, -5.638512984488999180, -18.83840828888717311 ) ) ;
#2965=DIRECTION ( 'NONE',  ( 1.000000000000000000, 0.000000000000000000, 0.000000000000000000 ) ) ;
#2966=CARTESIAN_POINT ( 'NONE',  ( 120.7824894832010472, -2.324775150319219108, -18.02356106541841996 ) ) ;
#2967=CARTESIAN_POINT ( 'NONE',  ( 118.8660148109119774, 0.1319031606808879209, -14.10382304977623669 ) ) ;
#2968=CARTESIAN_POINT ( 'NONE',  ( 127.7425183523501744, 0.8652765085452543969, -12.77968882490997338 ) ) ;
#2969=CARTESIAN_POINT ( 'NONE',  ( 124.1415948109119540, -6.344957434206665248, -7.627207830600338134 ) ) ;
#2973=CARTESIAN_POINT ( 'NONE',  ( 112.1155414775786454, 0.9020085738987339008, -11.91225656197089222 ) ) ;
#2974=CARTESIAN_POINT ( 'NONE',  ( 120.9081748109119872, -4.153390946401325223, -8.397313243818185668 ) ) ;
#2975=CARTESIAN_POINT ( 'NONE',  ( 120.7379948109119709, -10.63000616557722466, -14.87417383870573495 ) ) ;
#2977=CARTESIAN_POINT ( 'NONE',  ( 116.6536748109119941, -10.15424416112533912, -14.75197769757731336 ) ) ;
#2978=CARTESIAN_POINT ( 'NONE',  ( 119.3198281442452924, 0.5811942927096110934, -14.16772938898807510 ) ) ;
#2981=CARTESIAN_POINT ( 'NONE',  ( 124.8223148109119762, -10.15424416112533912, -14.75197769757731336 ) ) ;
#2985=CARTESIAN_POINT ( 'NONE',  ( 118.5256548109119876, -0.4660016031367893996, -10.09054647747474043 ) ) ;
#2986=CARTESIAN_POINT ( 'NONE',  ( 125.0492214775786266, -3.505236298600246325, -18.68346056562440793 ) ) ;
#2991=CARTESIAN_POINT ( 'NONE',  ( 119.6601881442453106, -8.166667518702819706, -8.995218007635861213 ) ) ;
#2993=CARTESIAN_POINT ( 'NONE',  ( 118.5256548109119876, -8.899110576539710493, -16.42337572283490132 ) ) ;
#2997=CARTESIAN_POINT ( 'NONE',  ( 125.2194014775786286, 0.1319031606808879209, -14.10382304977623669 ) ) ;
#2998=CARTESIAN_POINT ( 'NONE',  ( 123.6877814775786533, -6.222761293078241884, -8.102969835052219238 ) ) ;
#3003=CARTESIAN_POINT ( 'NONE',  ( 122.5532481442453019, -10.63000616557722466, -14.87417383870573495 ) ) ;
#3007=CARTESIAN_POINT ( 'NONE',  ( 121.1918081442452859, 0.9020085738987339008, -11.91225656197089222 ) ) ;
#3008=CARTESIAN_POINT ( 'NONE',  ( 118.5256548109119876, -0.4660016031367893996, -10.09054647747474043 ) ) ;
#3009=CARTESIAN_POINT ( 'NONE',  ( 120.9081748109119872, -4.153390946401325223, -8.397313243818185668 ) ) ;
#3011=CARTESIAN_POINT ( 'NONE',  ( 116.2565881442452991, -9.261995988541697145, -16.69588392320189030 ) ) ;
#3013=CARTESIAN_POINT ( 'NONE',  ( 124.8790414775786246, -8.899110576539710493, -16.42337572283490132 ) ) ;
#3014=CARTESIAN_POINT ( 'NONE',  ( 125.0492214775786408, -3.505236298599212041, -18.68346056562414859 ) ) ;
#3019=CARTESIAN_POINT ( 'NONE',  ( 120.8514481442452961, -7.893985811506177619, -18.51759400769804742 ) ) ;
#3020=CARTESIAN_POINT ( 'NONE',  ( 123.2906948109119867, -1.833838273342659697, -17.42832698103878286 ) ) ;
#3023=CARTESIAN_POINT ( 'NONE',  ( 122.9503348109119827, 0.5811942927096110934, -14.16772938898807510 ) ) ;
#3024=CARTESIAN_POINT ( 'NONE',  ( 112.6828081442453282, -2.084020599724406786, -8.691656652584148546 ) ) ;
#3026=CARTESIAN_POINT ( 'NONE',  ( 123.3474214775786209, -9.988377603198976828, -10.36322818467138340 ) ) ;
#3027=ADVANCED_FACE ( 'NONE', ( #8257 ), #28066, .T. ) ;
#3029=CARTESIAN_POINT ( 'NONE',  ( 120.3976348109119812, -1.834011780172310813, -8.268836392978581529 ) ) ;
#3031=CARTESIAN_POINT ( 'NONE',  ( 126.6942948109119840, -8.899110576539710493, -16.42337572283490132 ) ) ;
#3032=CARTESIAN_POINT ( 'NONE',  ( 111.9254164575755226, -1.016270020561755860, -17.26805140881366896 ) ) ;
#3036=CARTESIAN_POINT ( 'NONE',  ( 113.3635281442453504, -0.1624402480850797581, -16.17319339645315424 ) ) ;
#3037=CARTESIAN_POINT ( 'NONE',  ( 123.5176014775786228, -0.8288870151387760510, -10.36305467784173118 ) ) ;
#3040=CARTESIAN_POINT ( 'NONE',  ( 121.4754414775786131, -1.833838273342659697, -17.42832698103878286 ) ) ;
#3041=CARTESIAN_POINT ( 'NONE',  ( 116.8238548109119819, -5.574606645277164318, -18.38911715685844683 ) ) ;
#3042=CARTESIAN_POINT ( 'NONE',  ( 111.8319081442453182, -4.153390946401321671, -8.397313243818183892 ) ) ;
#3044=CARTESIAN_POINT ( 'NONE',  ( 123.9146881442452894, -10.15424416112533912, -14.75197769757731336 ) ) ;
#3045=CARTESIAN_POINT ( 'NONE',  ( 119.2063748109119814, -1.561330072975668504, -17.79121239304076951 ) ) ;
#3051=CARTESIAN_POINT ( 'NONE',  ( 115.6893214775786447, -9.859900752359374465, -12.68260735090039404 ) ) ;
#3052=CARTESIAN_POINT ( 'NONE',  ( 112.6260814775786514, -0.8288870151387760510, -10.36305467784173118 ) ) ;
#3055=VERTEX_POINT ( 'NONE', #962 ) ;
#3061=CARTESIAN_POINT ( 'NONE',  ( 124.3117748109119844, 0.1319031606808879209, -14.10382304977623669 ) ) ;
#3063=CARTESIAN_POINT ( 'NONE',  ( 112.6260814775786514, -0.8288870151387760510, -10.36305467784173118 ) ) ;
#3064=CARTESIAN_POINT ( 'NONE',  ( 126.4082675373902873, -6.091288680381572007, -18.33809601120119481 ) ) ;
#3069=CARTESIAN_POINT ( 'NONE',  ( 128.2184548109119930, 0.6402711692277476274, -15.78131322003126868 ) ) ;
#3072=CARTESIAN_POINT ( 'NONE',  ( 111.9453614775786434, -1.561330072975668060, -17.79121239304076596 ) ) ;
#3074=CARTESIAN_POINT ( 'NONE',  ( 115.0086014775786509, -4.089484607189486809, -7.948022111789456723 ) ) ;
#3077=EDGE_CURVE ( 'NONE', #39008, #5980, #30316, .T. ) ;
#3078=CARTESIAN_POINT ( 'NONE',  ( 125.0492214775786266, -3.505236298600246325, -18.68346056562440793 ) ) ;
#3079=CARTESIAN_POINT ( 'NONE',  ( 124.7655881442452852, -9.859900752359378018, -12.68260735090039759 ) ) ;
#3084=CARTESIAN_POINT ( 'NONE',  ( 112.5126281442453120, 0.1319031606808879209, -14.10382304977623669 ) ) ;
#3086=DIRECTION ( 'NONE',  ( 0.000000000000000000, 0.6004852223388321697, -0.7996358532186279566 ) ) ;
#3088=CARTESIAN_POINT ( 'NONE',  ( 125.2194014775786286, -10.30919188438810075, -12.61870101168855918 ) ) ;
#3089=CARTESIAN_POINT ( 'NONE',  ( 111.8319081442453182, -4.153390946401321671, -8.397313243818183892 ) ) ;
#3092=CARTESIAN_POINT ( 'NONE',  ( 119.2063748109119814, -1.561330072975668504, -17.79121239304076951 ) ) ;
#3093=CARTESIAN_POINT ( 'NONE',  ( 113.5904348109119866, -7.893985811506177619, -18.51759400769804742 ) ) ;
#3095=CARTESIAN_POINT ( 'NONE',  ( 112.7962614775786676, -6.222761293078241884, -8.102969835052219238 ) ) ;
#3096=CARTESIAN_POINT ( 'NONE',  ( 125.6164881442453094, 0.2603800115204892296, -16.42320221600525088 ) ) ;
#3097=CARTESIAN_POINT ( 'NONE',  ( 124.9357681442453014, -1.834011780172310813, -8.268836392978581529 ) ) ;
#3098=CARTESIAN_POINT ( 'NONE',  ( 115.4056881442453459, -7.893985811506177619, -18.51759400769804742 ) ) ;
#3099=CARTESIAN_POINT ( 'NONE',  ( 113.8173414775786512, -9.565557343593413364, -10.61323700422348004 ) ) ;
#3101=CARTESIAN_POINT ( 'NONE',  ( 116.7671281442453335, -7.643976991954077427, -18.09477374809248928 ) ) ;
#3103=CARTESIAN_POINT ( 'NONE',  ( 112.3424481442453384, -6.344957434206662583, -7.627207830600332805 ) ) ;
#3105=CARTESIAN_POINT ( 'NONE',  ( 123.7445081442452874, -7.894159318335828068, -9.358103419637847864 ) ) ;
#3116=CARTESIAN_POINT ( 'NONE',  ( 112.6828081442453282, -2.084020599724406786, -8.691656652584148546 ) ) ;
#3121=CARTESIAN_POINT ( 'NONE',  ( 120.0005481442453146, -5.638512984488999180, -18.83840828888717311 ) ) ;
#3122=CARTESIAN_POINT ( 'NONE',  ( 137.2844488807198502, -4.793161434092606754, -18.62470134987731640 ) ) ;
#3125=CARTESIAN_POINT ( 'NONE',  ( 120.3976348109119812, -7.643976991954077427, -18.09477374809248928 ) ) ;
#3127=CARTESIAN_POINT ( 'NONE',  ( 135.9690293846493319, -9.531372520637221513, -9.741219538532039479 ) ) ;
#3128=CARTESIAN_POINT ( 'NONE',  ( 118.9794681442453026, -9.261995988541697145, -16.69588392320189030 ) ) ;
#3130=CARTESIAN_POINT ( 'NONE',  ( 117.0507614775786465, 0.1319031606808879209, -14.10382304977623669 ) ) ;
#3133=CARTESIAN_POINT ( 'NONE',  ( 113.8740681442453138, -9.859900752359374465, -12.68260735090039404 ) ) ;
#3137=CARTESIAN_POINT ( 'NONE',  ( 118.2420214775786320, -6.222761293078241884, -8.102969835052219238 ) ) ;
#3139=CARTESIAN_POINT ( 'NONE',  ( 120.0005481442453146, -4.153390946401325223, -8.397313243818185668 ) ) ;
#3144=ORIENTED_EDGE ( 'NONE', *, *, #616, .F. ) ;
#3146=CARTESIAN_POINT ( 'NONE',  ( 112.8529881442453302, -1.561330072975668060, -17.79121239304076596 ) ) ;
#3147=CARTESIAN_POINT ( 'NONE',  ( 112.1155414775786454, 0.9020085738987339008, -11.91225656197089222 ) ) ;
#3151=CARTESIAN_POINT ( 'NONE',  ( 123.3995567976525365, -2.659420626585511371, -15.07970544296840210 ) ) ;
#3154=CARTESIAN_POINT ( 'NONE',  ( 120.2841814775786276, 0.9020085738987339008, -11.91225656197089222 ) ) ;
#3155=CARTESIAN_POINT ( 'NONE',  ( 126.3539348109119800, -4.153390946401325223, -8.397313243818185668 ) ) ;
#3156=CARTESIAN_POINT ( 'NONE',  ( 117.7882081442453170, -3.505236298600246325, -18.68346056562440793 ) ) ;
#3158=CARTESIAN_POINT ( 'NONE',  ( 121.4754414775786131, -8.166667518702819706, -8.995218007635861213 ) ) ;
#3159=CARTESIAN_POINT ( 'NONE',  ( 118.7525614775786380, -8.166667518702819706, -8.995218007635861213 ) ) ;
#3161=CARTESIAN_POINT ( 'NONE',  ( 111.2646414775786496, -8.899110576539710493, -16.42337572283490132 ) ) ;
#3164=CARTESIAN_POINT ( 'NONE',  ( 119.0361948109119652, -7.893985811506177619, -18.51759400769804742 ) ) ;
#3167=CARTESIAN_POINT ( 'NONE',  ( 114.1009748109119784, -4.089484607189486809, -7.948022111789456723 ) ) ;
#3170=CARTESIAN_POINT ( 'NONE',  ( 125.1059481442452750, -8.166667518702819706, -8.995218007635861213 ) ) ;
#3172=CARTESIAN_POINT ( 'NONE',  ( 113.5904348109119866, -2.084020599724406786, -8.691656652584148546 ) ) ;
#3174=CARTESIAN_POINT ( 'NONE',  ( 116.4834948109119779, -7.894159318335828068, -9.358103419637847864 ) ) ;
#3176=CARTESIAN_POINT ( 'NONE',  ( 119.4900081442453086, -7.643976991954077427, -18.09477374809248928 ) ) ;
#3178=CARTESIAN_POINT ( 'NONE',  ( 117.5045748109119756, -9.859900752359374465, -12.68260735090039404 ) ) ;
#3180=CARTESIAN_POINT ( 'NONE',  ( 116.1998614775786507, -10.63000616557722466, -14.87417383870573495 ) ) ;
#3181=CARTESIAN_POINT ( 'NONE',  ( 113.6471614775786492, -4.153390946401321671, -8.397313243818183892 ) ) ;
#3182=CARTESIAN_POINT ( 'NONE',  ( 116.7104014775786425, -8.899110576539710493, -16.42337572283490132 ) ) ;
#3184=CARTESIAN_POINT ( 'NONE',  ( 117.2776681442452968, -5.638512984488999180, -18.83840828888717311 ) ) ;
#3190=CARTESIAN_POINT ( 'NONE',  ( 123.5743281442453139, -7.893985811506177619, -18.51759400769804742 ) ) ;
#3192=DIRECTION ( 'NONE',  ( 0.000000000000000000, 0.6004852223388321697, -0.7996358532186279566 ) ) ;
#3193=CARTESIAN_POINT ( 'NONE',  ( 119.0929214775786278, -4.153390946401325223, -8.397313243818185668 ) ) ;
#3195=CARTESIAN_POINT ( 'NONE',  ( 123.2339681442453241, -6.344957434206665248, -7.627207830600338134 ) ) ;
#3197=DIRECTION ( 'NONE',  ( 0.000000000000000000, 0.6004852223388323917, -0.7996358532186279566 ) ) ;
#3200=CARTESIAN_POINT ( 'NONE',  ( 125.7299414775786346, -10.15424416112533912, -14.75197769757731336 ) ) ;
#3201=CARTESIAN_POINT ( 'NONE',  ( 122.8936081442453059, 0.2603800115204892296, -16.42320221600525088 ) ) ;
#3202=CARTESIAN_POINT ( 'NONE',  ( 117.4478481442453131, -9.565557343593413364, -10.61323700422348004 ) ) ;
#3204=CARTESIAN_POINT ( 'NONE',  ( 120.4543614775786295, -4.089484607189486809, -7.948022111789456723 ) ) ;
#3206=CARTESIAN_POINT ( 'NONE',  ( 125.6732148109119862, -9.859900752359378018, -12.68260735090039759 ) ) ;
#3207=CARTESIAN_POINT ( 'NONE',  ( 121.3052614775786111, -7.643976991954077427, -18.09477374809248928 ) ) ;
#3210=CARTESIAN_POINT ( 'NONE',  ( 117.6747548109119919, -1.834011780172310813, -8.268836392978581529 ) ) ;
#3211=CARTESIAN_POINT ( 'NONE',  ( 124.7088614775786226, -9.565557343593413364, -10.61323700422348004 ) ) ;
#3214=CARTESIAN_POINT ( 'NONE',  ( 135.8419766445667278, -1.204973725236484716, -8.697158258016544963 ) ) ;
#3215=CARTESIAN_POINT ( 'NONE',  ( 121.0216281442452981, -1.561330072975668948, -17.79121239304076951 ) ) ;
#3217=CARTESIAN_POINT ( 'NONE',  ( 119.4332814775786318, -8.899110576539710493, -16.42337572283490132 ) ) ;
#3220=CARTESIAN_POINT ( 'NONE',  ( 115.6893214775786447, 0.5811942927096154232, -14.16772938898807155 ) ) ;
#3221=CARTESIAN_POINT ( 'NONE',  ( 123.9714148109119805, -8.899110576539710493, -16.42337572283490132 ) ) ;
#3225=CARTESIAN_POINT ( 'NONE',  ( 122.6667014775786413, -7.893985811506177619, -18.51759400769804742 ) ) ;
#3229=CARTESIAN_POINT ( 'NONE',  ( 118.5823814775786360, -1.834011780172310813, -8.268836392978581529 ) ) ;
#3230=CARTESIAN_POINT ( 'NONE',  ( 119.4332814775786318, -0.4660016031367893996, -10.09054647747474043 ) ) ;
#3231=CARTESIAN_POINT ( 'NONE',  ( 119.0929214775786278, -4.153390946401325223, -8.397313243818185668 ) ) ;
#3233=CARTESIAN_POINT ( 'NONE',  ( 116.9373081442452929, -8.166667518702817929, -8.995218007635861213 ) ) ;
#3234=ORIENTED_EDGE ( 'NONE', *, *, #35618, .T. ) ;
#3235=CARTESIAN_POINT ( 'NONE',  ( 112.2289948109119848, -1.834011780172310813, -8.268836392978581529 ) ) ;
#3236=CARTESIAN_POINT ( 'NONE',  ( 125.7761281442453196, -10.10582367741896093, -14.73954123521881066 ) ) ;
#3240=CARTESIAN_POINT ( 'NONE',  ( 122.7801548109119665, -3.383040157471821630, -19.15922257007629170 ) ) ;
#3241=CARTESIAN_POINT ( 'NONE',  ( 122.2696148109119889, -5.574606645277164318, -18.38911715685844683 ) ) ;
#3243=CARTESIAN_POINT ( 'NONE',  ( 124.7655881442452852, 0.5811942927096110934, -14.16772938898807510 ) ) ;
#3246=CARTESIAN_POINT ( 'NONE',  ( 123.5176014775786228, -9.261995988541697145, -16.69588392320189030 ) ) ;
#3249=CARTESIAN_POINT ( 'NONE',  ( 114.1009748109119784, -4.089484607189486809, -7.948022111789456723 ) ) ;
#3255=CARTESIAN_POINT ( 'NONE',  ( 113.3068014775786594, -1.833838273342658809, -17.42832698103878286 ) ) ;
#3256=CARTESIAN_POINT ( 'NONE',  ( 112.5126281442453120, -10.30919188438810075, -12.61870101168855918 ) ) ;
#3259=CARTESIAN_POINT ( 'NONE',  ( 121.7590748109119687, -2.084020599724406786, -8.691656652584148546 ) ) ;
#3260=CARTESIAN_POINT ( 'NONE',  ( 115.0086014775786509, -5.574606645277164318, -18.38911715685844683 ) ) ;
#3261=CARTESIAN_POINT ( 'NONE',  ( 113.7606148109119886, -7.894159318335828068, -9.358103419637847864 ) ) ;
#3263=CARTESIAN_POINT ( 'NONE',  ( 124.3685014775786328, 0.4262465694468514643, -12.03445270309931736 ) ) ;
#3264=CARTESIAN_POINT ( 'NONE',  ( 117.7882081442453170, -6.344957434206665248, -7.627207830600338134 ) ) ;
#3266=CARTESIAN_POINT ( 'NONE',  ( 114.8384214775786489, -10.15424416112533912, -14.75197769757731336 ) ) ;
#3270=CARTESIAN_POINT ( 'NONE',  ( 116.7104014775786425, -8.899110576539710493, -16.42337572283490132 ) ) ;
#3271=CARTESIAN_POINT ( 'NONE',  ( 115.1787814775786387, -0.1624402480850797581, -16.17319339645315424 ) ) ;
#3283=CARTESIAN_POINT ( 'NONE',  ( 122.8368814775786291, -7.894159318335828068, -9.358103419637847864 ) ) ;
#3284=CARTESIAN_POINT ( 'NONE',  ( 113.8173414775786512, -9.565557343593413364, -10.61323700422348004 ) ) ;
#3285=CARTESIAN_POINT ( 'NONE',  ( 113.5904348109119866, -2.084020599724388578, -8.691656652584157428 ) ) ;
#3289=CARTESIAN_POINT ( 'NONE',  ( 116.3700414775786527, -4.153390946401321671, -8.397313243818183892 ) ) ;
#3290=CARTESIAN_POINT ( 'NONE',  ( 122.5977428165343781, -2.324775150319219108, -18.02356106541841996 ) ) ;
#3293=CARTESIAN_POINT ( 'NONE',  ( 116.8797485810857069, -1.220279397241700758, -16.99638242193885063 ) ) ;
#3294=CARTESIAN_POINT ( 'NONE',  ( 125.3895814775786448, -2.084020599724406786, -8.691656652584148546 ) ) ;
#3296=CARTESIAN_POINT ( 'NONE',  ( 114.4413348109119823, -9.261995988541697145, -16.69588392320189030 ) ) ;
#3299=CARTESIAN_POINT ( 'NONE',  ( 124.9357681442453014, -7.643976991954077427, -18.09477374809248928 ) ) ;
#3300=CARTESIAN_POINT ( 'NONE',  ( 124.8790414775786246, -8.899110576539710493, -16.42337572283490132 ) ) ;
#3303=ADVANCED_FACE ( 'NONE', ( #26260 ), #26708, .T. ) ;
#3306=CARTESIAN_POINT ( 'NONE',  ( 114.4980614775786734, -2.084020599724406786, -8.691656652584148546 ) ) ;
#3308=CARTESIAN_POINT ( 'NONE',  ( 123.7184548109119788, -3.484218720211407661, -13.98160872758045770 ) ) ;
#3310=CARTESIAN_POINT ( 'NONE',  ( 123.5176014775786228, -9.261995988541697145, -16.69588392320189030 ) ) ;
#3311=CARTESIAN_POINT ( 'NONE',  ( 112.1155414775786454, -10.15424416112533912, -14.75197769757731336 ) ) ;
#3314=CARTESIAN_POINT ( 'NONE',  ( 121.6456214775786293, -10.63000616557722466, -14.87417383870573495 ) ) ;
#3315=CARTESIAN_POINT ( 'NONE',  ( 115.5758681442453053, -1.561330072975668060, -17.79121239304076951 ) ) ;
#3319=CARTESIAN_POINT ( 'NONE',  ( 115.1220548109119761, -1.833838273342658809, -17.42832698103878286 ) ) ;
#3320=CARTESIAN_POINT ( 'NONE',  ( 122.1561614775786353, -0.4660016031367893996, -10.09054647747474043 ) ) ;
#3321=CARTESIAN_POINT ( 'NONE',  ( 114.4413348109119823, -9.261995988541697145, -16.69588392320189030 ) ) ;
#3322=B_SPLINE_CURVE_WITH_KNOTS ( 'NONE', 3,
 ( #9850, #41320, #20332, #27841, #3214, #31247, #23982, #3440, #20992, #34866, #37868, #27398, #16688, #13265, #20775, #33994, #14149, #27622, #30581, #41536, #10297, #19, #44734, #13932, #41754, #3654, #40861, #17575, #31467, #9614, #23533, #37419, #6188, #41092, #20108, #2763, #6424, #34217, #14374, #10957, #679, #38983, #42196, #39445, #11411, #25538, #36004, #21217, #459, #35551, #35092, #31690, #3875, #41974, #11186, #11626 ),
 .UNSPECIFIED., .F., .F.,
 ( 4, 2, 2, 2, 2, 2, 2, 1, 2, 2, 2, 2, 2, 2, 2, 2, 2, 2, 2, 2, 2, 1, 2, 2, 2, 2, 2, 2, 4 ),
 ( 0.000000000000000000, 0.06250000000001902645, 0.09375000000003509693, 0.1093750000000366374, 0.1250000000000381917, 0.1875000000000199285, 0.2187500000000047462, 0.2343749999999969469, 0.2421874999999932554, 0.2499999999999895917, 0.3125000000000103251, 0.3437500000000163203, 0.3593750000000197065, 0.3750000000000230371, 0.5000000000000551781, 0.5625000000000714984, 0.5937500000000812683, 0.6093750000000863754, 0.6250000000000914824, 0.6875000000001173506, 0.7187500000001303402, 0.7343750000001322276, 0.7421875000001330047, 0.7500000000001337819, 0.8125000000000972555, 0.8437500000000790479, 0.8593750000000698330, 0.8750000000000607292, 1.000000000000000000 ),
 .UNSPECIFIED. ) ;
#3323=CARTESIAN_POINT ( 'NONE',  ( 117.1642148109119859, -0.8288870151387760510, -10.36305467784173118 ) ) ;
#3325=CARTESIAN_POINT ( 'NONE',  ( 117.1074881442453233, 0.4262465694468514643, -12.03445270309931736 ) ) ;
#3327=CARTESIAN_POINT ( 'NONE',  ( 117.1642148109119859, -9.261995988541697145, -16.69588392320189030 ) ) ;
#3328=CARTESIAN_POINT ( 'NONE',  ( 123.1205148109119563, -7.643976991954077427, -18.09477374809248928 ) ) ;
#3333=EDGE_CURVE ( 'NONE', #40981, #11839, #5747, .T. ) ;
#3334=ADVANCED_FACE ( 'NONE', ( #25376 ), #6329, .T. ) ;
#3339=CARTESIAN_POINT ( 'NONE',  ( 115.6325948109119821, 0.2603800115204892296, -16.42320221600525088 ) ) ;
#3341=CARTESIAN_POINT ( 'NONE',  ( 113.2500748109119968, -3.505236298600246325, -18.68346056562440793 ) ) ;
#3343=CARTESIAN_POINT ( 'NONE',  ( 123.1938586403692000, -1.196538596002817867, -17.02799684832028504 ) ) ;
#3345=CARTESIAN_POINT ( 'NONE',  ( 118.2987481442453088, -1.561330072975668504, -17.79121239304076951 ) ) ;
#3346=CARTESIAN_POINT ( 'NONE',  ( 137.1428665321213884, -6.586308144700341316, -18.46356886511411943 ) ) ;
#3350=CARTESIAN_POINT ( 'NONE',  ( 121.7023481442452777, -0.8288870151387760510, -10.36305467784173118 ) ) ;
#3353=CARTESIAN_POINT ( 'NONE',  ( 118.4689281442453392, 0.9020085738987339008, -11.91225656197089222 ) ) ;
#3355=CARTESIAN_POINT ( 'NONE',  ( 116.5402214775786405, -9.565557343593413364, -10.61323700422348004 ) ) ;
#3356=AXIS2_PLACEMENT_3D ( 'NONE', #28804, #39055, #34931 ) ;
#3357=CARTESIAN_POINT ( 'NONE',  ( 112.9664414775786412, -9.859900752359374465, -12.68260735090039404 ) ) ;
#3361=CARTESIAN_POINT ( 'NONE',  ( 116.7104014775786425, -8.899110576539710493, -16.42337572283490132 ) ) ;
#3362=CARTESIAN_POINT ( 'NONE',  ( 118.8660148109119774, 0.1319031606808879209, -14.10382304977623669 ) ) ;
#3366=PRODUCT ( 'Barrel Adjuster Screw', 'Barrel Adjuster Screw', '', ( #38914 ) ) ;
#3368=CARTESIAN_POINT ( 'NONE',  ( 115.6893214775786447, 0.5811942927096154232, -14.16772938898807155 ) ) ;
#3369=CARTESIAN_POINT ( 'NONE',  ( 113.5337081442453240, -9.261995988541697145, -16.69588392320189030 ) ) ;
#3374=CARTESIAN_POINT ( 'NONE',  ( 123.1772414775786189, -4.089484607189486809, -7.948022111789456723 ) ) ;
#3375=CARTESIAN_POINT ( 'NONE',  ( 126.1837548109119496, 0.4262465694468514643, -12.03445270309931736 ) ) ;
#3376=CARTESIAN_POINT ( 'NONE',  ( 116.8238548109119819, -5.574606645277164318, -18.38911715685844683 ) ) ;
#3379=CYLINDRICAL_SURFACE ( 'NONE', #39557, 5.999999999999997335 ) ;
#3380=CARTESIAN_POINT ( 'NONE',  ( 120.6812681442452941, -10.30919188438810075, -12.61870101168855918 ) ) ;
#3381=CARTESIAN_POINT ( 'NONE',  ( 119.0361948109119652, -7.893985811506177619, -18.51759400769804742 ) ) ;
#3384=CARTESIAN_POINT ( 'NONE',  ( 114.0442481442453300, -7.643976991954077427, -18.09477374809248928 ) ) ;
#3387=CARTESIAN_POINT ( 'NONE',  ( 118.2987481442453088, -1.561330072975668504, -17.79121239304076951 ) ) ;
#3390=CARTESIAN_POINT ( 'NONE',  ( 114.4413348109119823, -9.261995988541697145, -16.69588392320189030 ) ) ;
#3395=CARTESIAN_POINT ( 'NONE',  ( 112.6260814775786514, -0.8288870151387760510, -10.36305467784173118 ) ) ;
#3399=CARTESIAN_POINT ( 'NONE',  ( 117.5045748109119756, -9.859900752359374465, -12.68260735090039404 ) ) ;
#3401=CARTESIAN_POINT ( 'NONE',  ( 118.6391081442452986, -5.574606645277164318, -18.38911715685844683 ) ) ;
#3404=CARTESIAN_POINT ( 'NONE',  ( 120.5678148109119832, -1.833838273342659253, -17.42832698103878286 ) ) ;
#3406=CARTESIAN_POINT ( 'NONE',  ( 117.2209414775786485, -7.893985811506177619, -18.51759400769804742 ) ) ;
#3407=CARTESIAN_POINT ( 'NONE',  ( 117.7882081442453170, -3.505236298600246325, -18.68346056562440793 ) ) ;
#3409=CARTESIAN_POINT ( 'NONE',  ( 116.3700414775786527, -5.638512984488999180, -18.83840828888717311 ) ) ;
#3415=CARTESIAN_POINT ( 'NONE',  ( 121.5321681442453183, -9.988377603198976828, -10.36322818467138340 ) ) ;
#3416=ORIENTED_EDGE ( 'NONE', *, *, #42304, .F. ) ;
#3417=CARTESIAN_POINT ( 'NONE',  ( 118.3186931642484438, -2.215723800389698184, -18.16877924232191788 ) ) ;
#3418=CARTESIAN_POINT ( 'NONE',  ( 118.5256548109119876, -8.899110576539710493, -16.42337572283490132 ) ) ;
#3421=CARTESIAN_POINT ( 'NONE',  ( 121.7590748109119687, -7.893985811506177619, -18.51759400769804742 ) ) ;
#3426=CARTESIAN_POINT ( 'NONE',  ( 112.4559014775786494, -9.988377603198976828, -10.36322818467138340 ) ) ;
#3427=CARTESIAN_POINT ( 'NONE',  ( 124.4819548109119722, -7.893985811506177619, -18.51759400769804742 ) ) ;
#3428=CARTESIAN_POINT ( 'NONE',  ( 118.6958348109119754, -3.505236298600246325, -18.68346056562440793 ) ) ;
#3430=CARTESIAN_POINT ( 'NONE',  ( 120.9081748109119872, -5.638512984488999180, -18.83840828888717311 ) ) ;
#3432=CARTESIAN_POINT ( 'NONE',  ( 122.6099748109119929, -0.8288870151387760510, -10.36305467784173118 ) ) ;
#3434=CARTESIAN_POINT ( 'NONE',  ( 151.2860562277021472, -4.683672500039348208, -14.88233656108870662 ) ) ;
#3436=CARTESIAN_POINT ( 'NONE',  ( 116.4834948109119779, -1.561330072975668504, -17.79121239304076951 ) ) ;
#3437=CARTESIAN_POINT ( 'NONE',  ( 123.4608748109119745, 0.4262465694468514643, -12.03445270309931736 ) ) ;
#3440=CARTESIAN_POINT ( 'NONE',  ( 136.0320772899241604, -1.215848289962678130, -8.742271026892920460 ) ) ;
#3441=CARTESIAN_POINT ( 'NONE',  ( 120.8514481442452961, -7.893985811506177619, -18.51759400769804742 ) ) ;
#3443=CARTESIAN_POINT ( 'NONE',  ( 120.4543614775786295, -5.574606645277164318, -18.38911715685844683 ) ) ;
#3447=CARTESIAN_POINT ( 'NONE',  ( 113.2500748109119968, -6.344957434206662583, -7.627207830600332805 ) ) ;
#3453=CARTESIAN_POINT ( 'NONE',  ( 122.0427081442452817, 0.5811942927096110934, -14.16772938898807510 ) ) ;
#3456=CARTESIAN_POINT ( 'NONE',  ( 119.5467348109119712, -4.089484607189486809, -7.948022111789456723 ) ) ;
#3457=CARTESIAN_POINT ( 'NONE',  ( 119.8303681442453126, -10.63000616557722466, -14.87417383870573495 ) ) ;
#3458=CARTESIAN_POINT ( 'NONE',  ( 120.5110881442453206, -3.505236298600246325, -18.68346056562440793 ) ) ;
#3460=CARTESIAN_POINT ( 'NONE',  ( 115.5191414775786569, -3.383040157471821630, -19.15922257007629170 ) ) ;
#3467=AXIS2_PLACEMENT_3D ( 'NONE', #13774, #34281, #20173 ) ;
#3468=CARTESIAN_POINT ( 'NONE',  ( 124.4252281442452812, -9.261995988541697145, -16.69588392320189030 ) ) ;
#3469=CARTESIAN_POINT ( 'NONE',  ( 124.8223148109119762, -10.15424416112533912, -14.75197769757731336 ) ) ;
#3471=CARTESIAN_POINT ( 'NONE',  ( 123.4608748109119745, -10.63000616557722466, -14.87417383870573495 ) ) ;
#3474=CARTESIAN_POINT ( 'NONE',  ( 124.7655881442452852, 0.5811942927096110934, -14.16772938898807510 ) ) ;
#3475=CARTESIAN_POINT ( 'NONE',  ( 124.4252281442452812, -9.261995988541697145, -16.69588392320189030 ) ) ;
#3477=CARTESIAN_POINT ( 'NONE',  ( 126.4106614775786284, -6.222761293078241884, -8.102969835052219238 ) ) ;
#3481=CARTESIAN_POINT ( 'NONE',  ( 138.2184548109119930, -2.475900776146298110, -7.888945235271312306 ) ) ;
#3482=CARTESIAN_POINT ( 'NONE',  ( 114.8384214775786489, -10.15424416112533912, -14.75197769757731336 ) ) ;
#3483=CARTESIAN_POINT ( 'NONE',  ( 112.3991748109119868, -8.166667518702817929, -8.995218007635859436 ) ) ;
#3486=CARTESIAN_POINT ( 'NONE',  ( 119.7736414775786358, 0.1319031606808879209, -14.10382304977623669 ) ) ;
#3487=CARTESIAN_POINT ( 'NONE',  ( 115.8595014775786609, -7.643976991954077427, -18.09477374809248928 ) ) ;
#3488=CARTESIAN_POINT ( 'NONE',  ( 113.8173414775786512, -9.565557343593413364, -10.61323700422348004 ) ) ;
#3490=CARTESIAN_POINT ( 'NONE',  ( 124.1983214775786166, -1.833838273342659697, -17.42832698103878286 ) ) ;
#3492=CARTESIAN_POINT ( 'NONE',  ( 114.7816948109119863, -9.859900752359374465, -12.68260735090039404 ) ) ;
#3495=VERTEX_POINT ( 'NONE', #16813 ) ;
#3496=CARTESIAN_POINT ( 'NONE',  ( 120.0572748109119772, -6.222761293078241884, -8.102969835052219238 ) ) ;
#3497=CARTESIAN_POINT ( 'NONE',  ( 112.7962614775786676, -6.222761293078241884, -8.102969835052219238 ) ) ;
#3505=CARTESIAN_POINT ( 'NONE',  ( 121.3052614775786111, -7.643976991954077427, -18.09477374809248928 ) ) ;
#3506=CARTESIAN_POINT ( 'NONE',  ( 118.7525614775786380, -1.833838273342659253, -17.42832698103878286 ) ) ;
#3510=CARTESIAN_POINT ( 'NONE',  ( 115.9162281442453235, -5.574606645277164318, -18.38911715685844683 ) ) ;
#3513=CARTESIAN_POINT ( 'NONE',  ( 124.8223148109119762, 0.9020085738987339008, -11.91225656197089222 ) ) ;
#3514=CARTESIAN_POINT ( 'NONE',  ( 114.8384214775786489, 0.9020085738987339008, -11.91225656197089222 ) ) ;
#3515=VERTEX_POINT ( 'NONE', #45066 ) ;
#3516=CARTESIAN_POINT ( 'NONE',  ( 114.7249681442453237, 0.2603800115204892296, -16.42320221600525088 ) ) ;
#3519=CARTESIAN_POINT ( 'NONE',  ( 112.2289948109119848, -1.834011780172310813, -8.268836392978581529 ) ) ;
#3520=CARTESIAN_POINT ( 'NONE',  ( 113.5337081442453240, -9.261995988541697145, -16.69588392320189030 ) ) ;
#3521=CARTESIAN_POINT ( 'NONE',  ( 123.9146881442452894, -10.15424416112533912, -14.75197769757731336 ) ) ;
#3526=CARTESIAN_POINT ( 'NONE',  ( 117.2209414775786485, -2.084020599724406786, -8.691656652584148546 ) ) ;
#3528=AXIS2_PLACEMENT_3D ( 'NONE', #44929, #10487, #31887 ) ;
#3531=CARTESIAN_POINT ( 'NONE',  ( 123.9714148109119805, -0.4660016031367893996, -10.09054647747474043 ) ) ;
#3532=CARTESIAN_POINT ( 'NONE',  ( 111.4348214775786801, -3.505236298600246325, -18.68346056562440793 ) ) ;
#3533=CARTESIAN_POINT ( 'NONE',  ( 120.0572748109119772, -6.222761293078222344, -8.102969835052219238 ) ) ;
#3534=CARTESIAN_POINT ( 'NONE',  ( 119.0361948109119652, -7.893985811506177619, -18.51759400769804742 ) ) ;
#3536=CARTESIAN_POINT ( 'NONE',  ( 115.3489614775786407, -9.261995988541697145, -16.69588392320189030 ) ) ;
#3538=CARTESIAN_POINT ( 'NONE',  ( 114.9518748109119883, -7.643976991954077427, -18.09477374809248928 ) ) ;
#3539=CARTESIAN_POINT ( 'NONE',  ( 123.6310548109119765, -5.638512984488999180, -18.83840828888717311 ) ) ;
#3540=CARTESIAN_POINT ( 'NONE',  ( 119.2631014775786298, 0.2603800115204892296, -16.42320221600525088 ) ) ;
#3541=CARTESIAN_POINT ( 'NONE',  ( 115.9162281442453093, -5.574606645277164318, -18.38911715685844683 ) ) ;
#3543=CARTESIAN_POINT ( 'NONE',  ( 121.1350814775786233, -9.859900752359378018, -12.68260735090039759 ) ) ;
#3544=CARTESIAN_POINT ( 'NONE',  ( 116.3700414775786527, -5.638512984488999180, -18.83840828888717311 ) ) ;
#3545=CARTESIAN_POINT ( 'NONE',  ( 136.9735043287622318, 0.6043515321839462162, -13.01395506536901436 ) ) ;
#3552=CARTESIAN_POINT ( 'NONE',  ( 113.2500748109119968, -6.344957434206662583, -7.627207830600332805 ) ) ;
#3553=TOROIDAL_SURFACE ( 'NONE', #29051, 3.100000000000000089, 2.899999999999999911 ) ;
#3558=B_SPLINE_CURVE_WITH_KNOTS ( 'NONE', 3,
 ( #8834, #25943, #36634, #26843, #9512, #12492, #40300, #9064, #23429, #43501 ),
 .UNSPECIFIED., .F., .F.,
 ( 4, 3, 3, 4 ),
 ( 0.000000000000000000, 0.0001671877560958105107, 0.0003343755126086549959, 0.0006438490228505499516 ),
 .UNSPECIFIED. ) ;
#3561=CARTESIAN_POINT ( 'NONE',  ( 118.9227414775786400, -10.63000616557722466, -14.87417383870573495 ) ) ;
#3563=ADVANCED_FACE ( 'NONE', ( #35217 ), #21555, .F. ) ;
#3566=CARTESIAN_POINT ( 'NONE',  ( 125.1059481442452750, -1.833838273342660141, -17.42832698103878286 ) ) ;
#3569=CARTESIAN_POINT ( 'NONE',  ( 120.3409081442453044, -0.4660016031367893996, -10.09054647747474043 ) ) ;
#3571=CARTESIAN_POINT ( 'NONE',  ( 114.4413348109119823, -0.8288870151387760510, -10.36305467784173118 ) ) ;
#3573=CARTESIAN_POINT ( 'NONE',  ( 112.0020881442453344, -9.565557343593413364, -10.61323700422348004 ) ) ;
#3576=CARTESIAN_POINT ( 'NONE',  ( 119.8303681442453126, 0.4262465694468514643, -12.03445270309931736 ) ) ;
#3577=CARTESIAN_POINT ( 'NONE',  ( 120.7379948109119709, 0.4262465694468514643, -12.03445270309931736 ) ) ;
#3583=CARTESIAN_POINT ( 'NONE',  ( 112.9097148109120070, 0.2603800115204892296, -16.42320221600525088 ) ) ;
#3584=CARTESIAN_POINT ( 'NONE',  ( 116.2565881442452991, -9.261995988541697145, -16.69588392320189030 ) ) ;
#3590=DIRECTION ( 'NONE',  ( 0.000000000000000000, 0.6004852223388321697, -0.7996358532186279566 ) ) ;
#3591=CARTESIAN_POINT ( 'NONE',  ( 122.4397948109119767, -9.988377603198976828, -10.36322818467138340 ) ) ;
#3592=CARTESIAN_POINT ( 'NONE',  ( 113.9875214775786532, -0.4660016031367893996, -10.09054647747474043 ) ) ;
#3593=CARTESIAN_POINT ( 'NONE',  ( 118.3554748109119998, -9.565557343593413364, -10.61323700422348004 ) ) ;
#3594=CARTESIAN_POINT ( 'NONE',  ( 123.6877814775786533, -3.383040157471821630, -19.15922257007629170 ) ) ;
#3595=CARTESIAN_POINT ( 'NONE',  ( 119.2063748109119814, -1.561330072975668504, -17.79121239304076951 ) ) ;
#3597=CARTESIAN_POINT ( 'NONE',  ( 113.1366214775786432, -7.643976991954077427, -18.09477374809248928 ) ) ;
#3600=CARTESIAN_POINT ( 'NONE',  ( 122.8368814775786291, -1.561330072975668948, -17.79121239304076951 ) ) ;
#3602=CARTESIAN_POINT ( 'NONE',  ( 115.9729548109119861, -6.344957434206662583, -7.627207830600332805 ) ) ;
#3605=CARTESIAN_POINT ( 'NONE',  ( 138.2184548109119930, -7.050714571525749541, -18.72418924296322729 ) ) ;
#3606=CARTESIAN_POINT ( 'NONE',  ( 122.4397948109119767, -9.988377603198980381, -10.36322818467138518 ) ) ;
#3609=CARTESIAN_POINT ( 'NONE',  ( 119.1496481442453046, -6.222761293078241884, -8.102969835052219238 ) ) ;
#3610=CARTESIAN_POINT ( 'NONE',  ( 120.5468302440515203, -2.467220198592778413, -17.83387418641524391 ) ) ;
#3611=CARTESIAN_POINT ( 'NONE',  ( 121.4754414775786131, -1.833838273342659697, -17.42832698103878286 ) ) ;
#3615=CARTESIAN_POINT ( 'NONE',  ( 121.0216281442452981, -7.894159318335828068, -9.358103419637847864 ) ) ;
#3617=CARTESIAN_POINT ( 'NONE',  ( 115.3489614775786407, -9.261995988541697145, -16.69588392320189030 ) ) ;
#3618=CARTESIAN_POINT ( 'NONE',  ( 123.1772414775786189, -4.089484607189477039, -7.948022111789462052 ) ) ;
#3619=CARTESIAN_POINT ( 'NONE',  ( 116.9373081442452929, -1.833838273342659253, -17.42832698103878286 ) ) ;
#3621=CARTESIAN_POINT ( 'NONE',  ( 116.7104014775786425, -0.4660016031367893996, -10.09054647747474043 ) ) ;
#3627=CARTESIAN_POINT ( 'NONE',  ( 120.7947214775786193, -9.261995988541697145, -16.69588392320189030 ) ) ;
#3631=CARTESIAN_POINT ( 'NONE',  ( 117.5613014775786525, -10.15424416112533912, -14.75197769757731336 ) ) ;
#3633=EDGE_CURVE ( 'NONE', #12590, #43250, #35717, .T. ) ;
#3634=CARTESIAN_POINT ( 'NONE',  ( 123.5176014775786228, -9.261995988541697145, -16.69588392320189030 ) ) ;
#3637=ORIENTED_EDGE ( 'NONE', *, *, #18352, .T. ) ;
#3638=CARTESIAN_POINT ( 'NONE',  ( 115.6893214775786447, 0.5811942927096154232, -14.16772938898807155 ) ) ;
#3639=CARTESIAN_POINT ( 'NONE',  ( 126.4106614775786284, -6.222761293078241884, -8.102969835052219238 ) ) ;
#3640=CARTESIAN_POINT ( 'NONE',  ( 123.9146881442452894, 0.9020085738987339008, -11.91225656197089222 ) ) ;
#3641=CARTESIAN_POINT ( 'NONE',  ( 117.6747548109119919, -7.643976991954077427, -18.09477374809248928 ) ) ;
#3644=CARTESIAN_POINT ( 'NONE',  ( 119.4332814775786318, -0.4660016031367893996, -10.09054647747474043 ) ) ;
#3647=CARTESIAN_POINT ( 'NONE',  ( 124.0281414775786146, -7.643976991954077427, -18.09477374809248928 ) ) ;
#3649=CARTESIAN_POINT ( 'NONE',  ( 120.0947965460471920, -2.191907684172563986, -18.20049396185734025 ) ) ;
#3650=CARTESIAN_POINT ( 'NONE',  ( 117.3343948109119737, -3.383040157471821630, -19.15922257007629170 ) ) ;
#3651=CARTESIAN_POINT ( 'NONE',  ( 125.6164881442453094, -9.565557343593413364, -10.61323700422348004 ) ) ;
#3653=( BOUNDED_SURFACE ( )  B_SPLINE_SURFACE ( 1, 2, ( 
 ( #18052, #8009, #21918, #35811, #1165, #18506, #32396, #15082, #43572, #12342, #37155, #40605, #29659, #16438, #5931, #6166, #30116, #13018, #23273, #5257, #26241, #43803, #15758, #26019, #44262, #5703, #40152, #20086, #33285, #2739, #39924, #33504, #8915, #36708, #22813, #5476, #19396, #19853, #9364, #2060, #30336, #33740, #33971, #44031, #26917, #2512, #19174, #15983, #12569, #29886, #8685, #2283, #16664, #43346, #36931, #26474, #12116, #33054, #40377, #9140, #23044, #40838, #1828, #9593, #19620, #23509, #37394, #22590, #16213, #36490, #12792, #26694, #37627, #27373, #41515, #7062, #27601, #34844, #24177, #38498, #27148, #30558, #10270, #6401, #7275, #27815, #41729, #38282, #13906, #20753, #24615, #17549, #20972, #17117, #35068, #3631, #6619, #31443, #21190, #44479, #20307, #20532, #14125, #211, #38069, #34412, #28042, #41950, #16895, #23960, #6846, #34632, #3418, #41295, #3849, #41069, #9826, #17334, #2967, #31224, #34193, #10492, #3193, #24278, #30788, #24394, #10057, #10714, #13246, #31007, #23737, #44711, #13472, #37843, #44934, #13692, #11606, #25517, #4069, #39420, #35527, #39187, #31892, #43066, #11385, #28264, #8411, #42622, #14350, #22094, #42173, #8185, #31665, #35759, #434, #24835, #35981, #4752, #25065, #38958, #7726, #25293, #38726, #11160, #1109, #18673, #4530, #10933, #15027, #14574, #1332, #7498, #15246, #32565, #35296, #28491, #4299, #7953, #18454, #21414, #17993, #11834, #36211, #29154, #25742, #42396, #28937, #39648, #659, #22316, #42846, #21639, #17769, #18220, #32115, #21864, #883, #14802, #28715, #32342, #22536, #9087, #8855, #5649, #43748, #12515, #26865, #8635, #33003, #2006, #22756, #22989, #33683, #1553, #36879, #40554, #15475, #19346, #2228, #29605, #36433, #43521, #16380, #23453, #26640, #26413, #2458, #19569, #40096, #40323, #1777, #4978, #32781, #12289, #30282, #26187, #29831, #5200, #25965, #18890, #36656, #19119, #33448, #5429, #16157, #15932, #30061, #33233, #29381, #44208, #43974, #9314, #12738, #23223, #37102, #43293, #5877 ),
 ( #19798, #12969, #12063, #15703, #40780, #9538, #39870, #27549, #41901, #10666, #30959, #27325, #14078, #27095, #9771, #41242, #41683, #23910, #34799, #31178, #3146, #3583, #45098, #16843, #13855, #27770, #23683, #10444, #10001, #13640, #6342, #17494, #44883, #2682, #27996, #17067, #33911, #24348, #16613, #38235, #7015, #41461, #20257, #162, #37793, #37338, #30506, #10220, #37572, #30735, #34143, #2912, #44658, #20925, #34584, #13421, #31393, #6110, #20029, #24129, #44427, #17287, #13195, #6567, #20485, #34364, #41017, #38021, #6797, #20706, #3368, #14524, #1287, #14301, #42126, #28437, #42350, #32295, #28219, #1060, #25011, #35706, #14975, #4482, #38677, #22040, #25243, #35934, #31619, #21363, #35477, #28888, #21590, #42800, #18168, #32512, #21139, #24569, #4251, #388, #15199, #21813, #18403, #11561, #7906, #14752, #18622, #25468, #39372, #11109, #29103, #8139, #613, #4702, #43014, #38454, #10886, #38904, #7225, #35015, #32065, #7675, #3795, #17721, #24785, #17945, #833, #28665, #42569, #35246, #7443, #4023, #31844, #11332, #39141, #5380, #32731, #22933, #29553, #19297, #18839, #33175, #22484, #26587, #9036, #36826, #19519, #40269, #1952, #5821, #43919, #2170, #43470, #16329, #33396, #32950, #30003, #19741, #11783, #1505, #1727, #40500, #16100, #22707, #15649, #12688, #9261, #43244, #5149, #15878, #36605, #29775, #8584, #2401, #8358, #22262, #43686, #29330, #12461, #15425, #5595, #12236, #26362, #12010, #23171, #36378, #37050, #33625, #26133, #30231, #25690, #39597, #36156, #4925, #19066, #25912, #39817, #40037, #8803, #16789, #20431, #13138, #24300, #37746, #9482, #34749, #23860, #40725, #3310, #23395, #37970, #45049, #6516, #27042, #6964, #34092, #3531, #37281, #34315, #16561, #37513, #40959, #44376, #9714, #6746, #41416, #30456, #17233, #20655, #20871, #30906, #13809, #24077, #6048, #23627, #44604, #6286, #26814, #3088, #17447, #44153, #17015, #2858, #12918, #33859, #20207, #30685, #13367, #34532, #2628, #31124, #27272, #10170, #27720, #41635, #41186, #10391 ) ),
 .UNSPECIFIED., .F., .F., .F. ) 
 B_SPLINE_SURFACE_WITH_KNOTS ( ( 2, 2 ),
 ( 3, 2, 2, 2, 2, 2, 2, 2, 2, 2, 2, 2, 2, 2, 2, 2, 2, 2, 2, 2, 2, 2, 2, 2, 2, 2, 2, 2, 2, 2, 2, 2, 2, 2, 2, 2, 2, 2, 2, 2, 2, 2, 2, 2, 2, 2, 2, 2, 2, 2, 2, 2, 2, 2, 2, 2, 2, 2, 2, 2, 2, 2, 2, 2, 2, 2, 2, 2, 2, 2, 2, 2, 2, 2, 2, 2, 2, 2, 2, 2, 2, 2, 2, 2, 2, 2, 2, 2, 2, 2, 2, 2, 2, 2, 2, 2, 2, 2, 2, 2, 2, 2, 2, 2, 2, 2, 2, 2, 2, 2, 2, 2, 2, 2, 2, 2, 2, 2, 2, 2, 2, 2, 2, 2, 2, 2, 2, 2, 3 ),
 ( 0.000000000000000000, 1.000000000000000000 ),
 ( 0.000000000000000000, 0.007812500000000000000, 0.01562500000000000000, 0.02343750000000000000, 0.03125000000000000000, 0.03906250000000000000, 0.04687500000000000000, 0.05468750000000000000, 0.06250000000000000000, 0.07031250000000000000, 0.07812500000000000000, 0.08593750000000000000, 0.09375000000000000000, 0.1015625000000000000, 0.1093750000000000000, 0.1171875000000000000, 0.1250000000000000000, 0.1328125000000000000, 0.1406250000000000000, 0.1484375000000000000, 0.1562500000000000000, 0.1640625000000000000, 0.1718750000000000000, 0.1796875000000000000, 0.1875000000000000000, 0.1953125000000000000, 0.2031250000000000000, 0.2109375000000000000, 0.2187500000000000000, 0.2265625000000000000, 0.2343750000000000000, 0.2421875000000000000, 0.2500000000000000000, 0.2578125000000000000, 0.2656250000000000000, 0.2734375000000000000, 0.2812500000000000000, 0.2890625000000000000, 0.2968750000000000000, 0.3046875000000000000, 0.3125000000000000000, 0.3203125000000000000, 0.3281250000000000000, 0.3359375000000000000, 0.3437500000000000000, 0.3515625000000000000, 0.3593750000000000000, 0.3671875000000000000, 0.3750000000000000000, 0.3828125000000000000, 0.3906250000000000000, 0.3984375000000000000, 0.4062500000000000000, 0.4140625000000000000, 0.4218750000000000000, 0.4296875000000000000, 0.4375000000000000000, 0.4453125000000000000, 0.4531250000000000000, 0.4609375000000000000, 0.4687500000000000000, 0.4765625000000000000, 0.4843750000000000000, 0.4921875000000000000, 0.5000000000000000000, 0.5078125000000000000, 0.5156250000000000000, 0.5234375000000000000, 0.5312500000000000000, 0.5390625000000000000, 0.5468750000000000000, 0.5546875000000000000, 0.5625000000000000000, 0.5703125000000000000, 0.5781250000000000000, 0.5859375000000000000, 0.5937500000000000000, 0.6015625000000000000, 0.6093750000000000000, 0.6171875000000000000, 0.6250000000000000000, 0.6328125000000000000, 0.6406250000000000000, 0.6484375000000000000, 0.6562500000000000000, 0.6640625000000000000, 0.6718750000000000000, 0.6796875000000000000, 0.6875000000000000000, 0.6953125000000000000, 0.7031250000000000000, 0.7109375000000000000, 0.7187500000000000000, 0.7265625000000000000, 0.7343750000000000000, 0.7421875000000000000, 0.7500000000000000000, 0.7578125000000000000, 0.7656250000000000000, 0.7734375000000000000, 0.7812500000000000000, 0.7890625000000000000, 0.7968750000000000000, 0.8046875000000000000, 0.8125000000000000000, 0.8203125000000000000, 0.8281250000000000000, 0.8359375000000000000, 0.8437500000000000000, 0.8515625000000000000, 0.8593750000000000000, 0.8671875000000000000, 0.8750000000000000000, 0.8828125000000000000, 0.8906250000000000000, 0.8984375000000000000, 0.9062500000000000000, 0.9140625000000000000, 0.9218750000000000000, 0.9296875000000000000, 0.9375000000000000000, 0.9453125000000000000, 0.9531250000000000000, 0.9609375000000000000, 0.9687500000000000000, 0.9765625000000000000, 0.9843750000000000000, 0.9921875000000000000, 1.000000000000000000 ),
 .UNSPECIFIED. ) 
 GEOMETRIC_REPRESENTATION_ITEM ( )  RATIONAL_B_SPLINE_SURFACE ( (
 ( 1.000000000000000000, 0.9238795325112869605, 1.000000000000000000, 0.9238795325112869605, 1.000000000000000000, 0.9238795325112869605, 1.000000000000000000, 0.9238795325112869605, 1.000000000000000000, 0.9238795325112869605, 1.000000000000000000, 0.9238795325112869605, 1.000000000000000000, 0.9238795325112869605, 1.000000000000000000, 0.9238795325112869605, 1.000000000000000000, 0.9238795325112869605, 1.000000000000000000, 0.9238795325112869605, 1.000000000000000000, 0.9238795325112869605, 1.000000000000000000, 0.9238795325112869605, 1.000000000000000000, 0.9238795325112869605, 1.000000000000000000, 0.9238795325112869605, 1.000000000000000000, 0.9238795325112869605, 1.000000000000000000, 0.9238795325112869605, 1.000000000000000000, 0.9238795325112869605, 1.000000000000000000, 0.9238795325112869605, 1.000000000000000000, 0.9238795325112869605, 1.000000000000000000, 0.9238795325112869605, 1.000000000000000000, 0.9238795325112869605, 1.000000000000000000, 0.9238795325112869605, 1.000000000000000000, 0.9238795325112869605, 1.000000000000000000, 0.9238795325112869605, 1.000000000000000000, 0.9238795325112869605, 1.000000000000000000, 0.9238795325112869605, 1.000000000000000000, 0.9238795325112869605, 1.000000000000000000, 0.9238795325112869605, 1.000000000000000000, 0.9238795325112869605, 1.000000000000000000, 0.9238795325112869605, 1.000000000000000000, 0.9238795325112869605, 1.000000000000000000, 0.9238795325112869605, 1.000000000000000000, 0.9238795325112869605, 1.000000000000000000, 0.9238795325112869605, 1.000000000000000000, 0.9238795325112869605, 1.000000000000000000, 0.9238795325112869605, 1.000000000000000000, 0.9238795325112869605, 1.000000000000000000, 0.9238795325112869605, 1.000000000000000000, 0.9238795325112869605, 1.000000000000000000, 0.9238795325112869605, 1.000000000000000000, 0.9238795325112869605, 1.000000000000000000, 0.9238795325112869605, 1.000000000000000000, 0.9238795325112869605, 1.000000000000000000, 0.9238795325112869605, 1.000000000000000000, 0.9238795325112869605, 1.000000000000000000, 0.9238795325112869605, 1.000000000000000000, 0.9238795325112869605, 1.000000000000000000, 0.9238795325112869605, 1.000000000000000000, 0.9238795325112869605, 1.000000000000000000, 0.9238795325112869605, 1.000000000000000000, 0.9238795325112869605, 1.000000000000000000, 0.9238795325112869605, 1.000000000000000000, 0.9238795325112869605, 1.000000000000000000, 0.9238795325112869605, 1.000000000000000000, 0.9238795325112869605, 1.000000000000000000, 0.9238795325112869605, 1.000000000000000000, 0.9238795325112869605, 1.000000000000000000, 0.9238795325112869605, 1.000000000000000000, 0.9238795325112869605, 1.000000000000000000, 0.9238795325112869605, 1.000000000000000000, 0.9238795325112869605, 1.000000000000000000, 0.9238795325112869605, 1.000000000000000000, 0.9238795325112869605, 1.000000000000000000, 0.9238795325112869605, 1.000000000000000000, 0.9238795325112869605, 1.000000000000000000, 0.9238795325112869605, 1.000000000000000000, 0.9238795325112869605, 1.000000000000000000, 0.9238795325112869605, 1.000000000000000000, 0.9238795325112869605, 1.000000000000000000, 0.9238795325112869605, 1.000000000000000000, 0.9238795325112869605, 1.000000000000000000, 0.9238795325112869605, 1.000000000000000000, 0.9238795325112869605, 1.000000000000000000, 0.9238795325112869605, 1.000000000000000000, 0.9238795325112869605, 1.000000000000000000, 0.9238795325112869605, 1.000000000000000000, 0.9238795325112869605, 1.000000000000000000, 0.9238795325112869605, 1.000000000000000000, 0.9238795325112869605, 1.000000000000000000, 0.9238795325112869605, 1.000000000000000000, 0.9238795325112869605, 1.000000000000000000, 0.9238795325112869605, 1.000000000000000000, 0.9238795325112869605, 1.000000000000000000, 0.9238795325112869605, 1.000000000000000000, 0.9238795325112869605, 1.000000000000000000, 0.9238795325112869605, 1.000000000000000000, 0.9238795325112869605, 1.000000000000000000, 0.9238795325112869605, 1.000000000000000000, 0.9238795325112869605, 1.000000000000000000, 0.9238795325112869605, 1.000000000000000000, 0.9238795325112869605, 1.000000000000000000, 0.9238795325112869605, 1.000000000000000000, 0.9238795325112869605, 1.000000000000000000, 0.9238795325112869605, 1.000000000000000000, 0.9238795325112869605, 1.000000000000000000, 0.9238795325112869605, 1.000000000000000000, 0.9238795325112869605, 1.000000000000000000, 0.9238795325112869605, 1.000000000000000000, 0.9238795325112869605, 1.000000000000000000, 0.9238795325112869605, 1.000000000000000000, 0.9238795325112869605, 1.000000000000000000, 0.9238795325112869605, 1.000000000000000000, 0.9238795325112869605, 1.000000000000000000, 0.9238795325112869605, 1.000000000000000000, 0.9238795325112869605, 1.000000000000000000, 0.9238795325112869605, 1.000000000000000000, 0.9238795325112869605, 1.000000000000000000, 0.9238795325112869605, 1.000000000000000000, 0.9238795325112869605, 1.000000000000000000, 0.9238795325112869605, 1.000000000000000000, 0.9238795325112869605, 1.000000000000000000, 0.9238795325112869605, 1.000000000000000000, 0.9238795325112869605, 1.000000000000000000, 0.9238795325112869605, 1.000000000000000000, 0.9238795325112869605, 1.000000000000000000, 0.9238795325112869605, 1.000000000000000000, 0.9238795325112869605, 1.000000000000000000, 0.9238795325112869605, 1.000000000000000000, 0.9238795325112869605, 1.000000000000000000, 0.9238795325112869605, 1.000000000000000000, 0.9238795325112869605, 1.000000000000000000, 0.9238795325112869605, 1.000000000000000000, 0.9238795325112869605, 1.000000000000000000, 0.9238795325112869605, 1.000000000000000000, 0.9238795325112869605, 1.000000000000000000, 0.9238795325112869605, 1.000000000000000000, 0.9238795325112869605, 1.000000000000000000, 0.9238795325112869605, 1.000000000000000000),
 ( 1.000000000000000000, 0.9238795325112869605, 1.000000000000000000, 0.9238795325112869605, 1.000000000000000000, 0.9238795325112869605, 1.000000000000000000, 0.9238795325112869605, 1.000000000000000000, 0.9238795325112869605, 1.000000000000000000, 0.9238795325112869605, 1.000000000000000000, 0.9238795325112869605, 1.000000000000000000, 0.9238795325112869605, 1.000000000000000000, 0.9238795325112869605, 1.000000000000000000, 0.9238795325112869605, 1.000000000000000000, 0.9238795325112869605, 1.000000000000000000, 0.9238795325112869605, 1.000000000000000000, 0.9238795325112869605, 1.000000000000000000, 0.9238795325112869605, 1.000000000000000000, 0.9238795325112869605, 1.000000000000000000, 0.9238795325112869605, 1.000000000000000000, 0.9238795325112869605, 1.000000000000000000, 0.9238795325112869605, 1.000000000000000000, 0.9238795325112869605, 1.000000000000000000, 0.9238795325112869605, 1.000000000000000000, 0.9238795325112869605, 1.000000000000000000, 0.9238795325112869605, 1.000000000000000000, 0.9238795325112869605, 1.000000000000000000, 0.9238795325112869605, 1.000000000000000000, 0.9238795325112869605, 1.000000000000000000, 0.9238795325112869605, 1.000000000000000000, 0.9238795325112869605, 1.000000000000000000, 0.9238795325112869605, 1.000000000000000000, 0.9238795325112869605, 1.000000000000000000, 0.9238795325112869605, 1.000000000000000000, 0.9238795325112869605, 1.000000000000000000, 0.9238795325112869605, 1.000000000000000000, 0.9238795325112869605, 1.000000000000000000, 0.9238795325112869605, 1.000000000000000000, 0.9238795325112869605, 1.000000000000000000, 0.9238795325112869605, 1.000000000000000000, 0.9238795325112869605, 1.000000000000000000, 0.9238795325112869605, 1.000000000000000000, 0.9238795325112869605, 1.000000000000000000, 0.9238795325112869605, 1.000000000000000000, 0.9238795325112869605, 1.000000000000000000, 0.9238795325112869605, 1.000000000000000000, 0.9238795325112869605, 1.000000000000000000, 0.9238795325112869605, 1.000000000000000000, 0.9238795325112869605, 1.000000000000000000, 0.9238795325112869605, 1.000000000000000000, 0.9238795325112869605, 1.000000000000000000, 0.9238795325112869605, 1.000000000000000000, 0.9238795325112869605, 1.000000000000000000, 0.9238795325112869605, 1.000000000000000000, 0.9238795325112869605, 1.000000000000000000, 0.9238795325112869605, 1.000000000000000000, 0.9238795325112869605, 1.000000000000000000, 0.9238795325112869605, 1.000000000000000000, 0.9238795325112869605, 1.000000000000000000, 0.9238795325112869605, 1.000000000000000000, 0.9238795325112869605, 1.000000000000000000, 0.9238795325112869605, 1.000000000000000000, 0.9238795325112869605, 1.000000000000000000, 0.9238795325112869605, 1.000000000000000000, 0.9238795325112869605, 1.000000000000000000, 0.9238795325112869605, 1.000000000000000000, 0.9238795325112869605, 1.000000000000000000, 0.9238795325112869605, 1.000000000000000000, 0.9238795325112869605, 1.000000000000000000, 0.9238795325112869605, 1.000000000000000000, 0.9238795325112869605, 1.000000000000000000, 0.9238795325112869605, 1.000000000000000000, 0.9238795325112869605, 1.000000000000000000, 0.9238795325112869605, 1.000000000000000000, 0.9238795325112869605, 1.000000000000000000, 0.9238795325112869605, 1.000000000000000000, 0.9238795325112869605, 1.000000000000000000, 0.9238795325112869605, 1.000000000000000000, 0.9238795325112869605, 1.000000000000000000, 0.9238795325112869605, 1.000000000000000000, 0.9238795325112869605, 1.000000000000000000, 0.9238795325112869605, 1.000000000000000000, 0.9238795325112869605, 1.000000000000000000, 0.9238795325112869605, 1.000000000000000000, 0.9238795325112869605, 1.000000000000000000, 0.9238795325112869605, 1.000000000000000000, 0.9238795325112869605, 1.000000000000000000, 0.9238795325112869605, 1.000000000000000000, 0.9238795325112869605, 1.000000000000000000, 0.9238795325112869605, 1.000000000000000000, 0.9238795325112869605, 1.000000000000000000, 0.9238795325112869605, 1.000000000000000000, 0.9238795325112869605, 1.000000000000000000, 0.9238795325112869605, 1.000000000000000000, 0.9238795325112869605, 1.000000000000000000, 0.9238795325112869605, 1.000000000000000000, 0.9238795325112869605, 1.000000000000000000, 0.9238795325112869605, 1.000000000000000000, 0.9238795325112869605, 1.000000000000000000, 0.9238795325112869605, 1.000000000000000000, 0.9238795325112869605, 1.000000000000000000, 0.9238795325112869605, 1.000000000000000000, 0.9238795325112869605, 1.000000000000000000, 0.9238795325112869605, 1.000000000000000000, 0.9238795325112869605, 1.000000000000000000, 0.9238795325112869605, 1.000000000000000000, 0.9238795325112869605, 1.000000000000000000, 0.9238795325112869605, 1.000000000000000000, 0.9238795325112869605, 1.000000000000000000, 0.9238795325112869605, 1.000000000000000000, 0.9238795325112869605, 1.000000000000000000, 0.9238795325112869605, 1.000000000000000000, 0.9238795325112869605, 1.000000000000000000, 0.9238795325112869605, 1.000000000000000000, 0.9238795325112869605, 1.000000000000000000, 0.9238795325112869605, 1.000000000000000000, 0.9238795325112869605, 1.000000000000000000, 0.9238795325112869605, 1.000000000000000000, 0.9238795325112869605, 1.000000000000000000, 0.9238795325112869605, 1.000000000000000000, 0.9238795325112869605, 1.000000000000000000, 0.9238795325112869605, 1.000000000000000000, 0.9238795325112869605, 1.000000000000000000, 0.9238795325112869605, 1.000000000000000000, 0.9238795325112869605, 1.000000000000000000, 0.9238795325112869605, 1.000000000000000000, 0.9238795325112869605, 1.000000000000000000, 0.9238795325112869605, 1.000000000000000000, 0.9238795325112869605, 1.000000000000000000, 0.9238795325112869605, 1.000000000000000000, 0.9238795325112869605, 1.000000000000000000, 0.9238795325112869605, 1.000000000000000000) ) ) 
 REPRESENTATION_ITEM ( '' )  SURFACE ( )  );
#3654=CARTESIAN_POINT ( 'NONE',  ( 137.3019930433552815, -1.207271142501472161, -9.674051694548802871 ) ) ;
#3655=CARTESIAN_POINT ( 'NONE',  ( 123.0637881442452937, -0.4660016031367893996, -10.09054647747474043 ) ) ;
#3657=CARTESIAN_POINT ( 'NONE',  ( 120.1707281442453166, -9.565557343593413364, -10.61323700422348004 ) ) ;
#3661=CARTESIAN_POINT ( 'NONE',  ( 115.5191414775786569, -3.383040157471821630, -19.15922257007629170 ) ) ;
#3662=CARTESIAN_POINT ( 'NONE',  ( 125.0492214775786266, -3.505236298600246325, -18.68346056562440793 ) ) ;
#3664=CARTESIAN_POINT ( 'NONE',  ( 120.7379948109119709, -10.63000616557722466, -14.87417383870573495 ) ) ;
#3666=CARTESIAN_POINT ( 'NONE',  ( 123.1205148109119563, -1.834011780172310813, -8.268836392978581529 ) ) ;
#3669=CARTESIAN_POINT ( 'NONE',  ( 124.1415948109119540, -6.344957434206665248, -7.627207830600338134 ) ) ;
#3670=CARTESIAN_POINT ( 'NONE',  ( 118.1285681442453068, -7.893985811506177619, -18.51759400769804742 ) ) ;
#3671=CARTESIAN_POINT ( 'NONE',  ( 123.0637881442452937, -8.899110576539710493, -16.42337572283490132 ) ) ;
#3672=CARTESIAN_POINT ( 'NONE',  ( 120.2274548109119934, -9.859900752359374465, -12.68260735090039404 ) ) ;
#3674=CARTESIAN_POINT ( 'NONE',  ( 116.8805814775786445, -6.344957434206662583, -7.627207830600332805 ) ) ;
#3677=CARTESIAN_POINT ( 'NONE',  ( 125.2088614775786510, -0.2054726073298613620, -16.14774885094370660 ) ) ;
#3681=CARTESIAN_POINT ( 'NONE',  ( 125.2655881442453278, 0.08617673920530924403, -14.09731900820076334 ) ) ;
#3682=CARTESIAN_POINT ( 'NONE',  ( 125.6732148109119862, -9.859900752359378018, -12.68260735090039759 ) ) ;
#3684=CARTESIAN_POINT ( 'NONE',  ( 114.2711548109119803, -0.1624402480850797581, -16.17319339645315424 ) ) ;
#3687=CARTESIAN_POINT ( 'NONE',  ( 125.1059481442452750, -8.166667518702819706, -8.995218007635861213 ) ) ;
#3688=CARTESIAN_POINT ( 'NONE',  ( 124.8223148109119762, 0.9020085738987339008, -11.91225656197089222 ) ) ;
#3690=CARTESIAN_POINT ( 'NONE',  ( 114.1577014775786552, -6.344957434206662583, -7.627207830600332805 ) ) ;
#3696=CARTESIAN_POINT ( 'NONE',  ( 115.0086014775786509, -5.574606645277164318, -18.38911715685844683 ) ) ;
#3697=CARTESIAN_POINT ( 'NONE',  ( 112.9097148109120070, 0.2603800115204892296, -16.42320221600525088 ) ) ;
#3698=EDGE_CURVE ( 'NONE', #4879, #19315, #6339, .T. ) ;
#3702=CARTESIAN_POINT ( 'NONE',  ( 121.2485348109119769, -8.899110576539710493, -16.42337572283490132 ) ) ;
#3703=CARTESIAN_POINT ( 'NONE',  ( 119.7169148109119874, -0.1624402480850797581, -16.17319339645315424 ) ) ;
#3704=CARTESIAN_POINT ( 'NONE',  ( 113.5337081442453240, -0.8288870151387760510, -10.36305467784173118 ) ) ;
#3706=CARTESIAN_POINT ( 'NONE',  ( 125.7299414775786346, -10.15424416112533912, -14.75197769757731336 ) ) ;
#3707=CARTESIAN_POINT ( 'NONE',  ( 114.5547881442453217, -4.153390946401321671, -8.397313243818183892 ) ) ;
#3713=CARTESIAN_POINT ( 'NONE',  ( 117.3343948109119737, -6.222761293078241884, -8.102969835052219238 ) ) ;
#3714=CARTESIAN_POINT ( 'NONE',  ( 112.5693548109119888, 0.4262465694468514643, -12.03445270309931736 ) ) ;
#3723=CARTESIAN_POINT ( 'NONE',  ( 121.8158014775786171, -4.153390946401325223, -8.397313243818185668 ) ) ;
#3724=CARTESIAN_POINT ( 'NONE',  ( 119.0361948109119652, -2.084020599724406786, -8.691656652584148546 ) ) ;
#3725=CYLINDRICAL_SURFACE ( 'NONE', #25045, 1.999999999999999556 ) ;
#3727=CARTESIAN_POINT ( 'NONE',  ( 116.8238548109119819, -5.574606645277164318, -18.38911715685844683 ) ) ;
#3729=CARTESIAN_POINT ( 'NONE',  ( 112.1260814775786514, -8.862178061932382889, -16.39564131203247399 ) ) ;
#3730=CARTESIAN_POINT ( 'NONE',  ( 125.6732148109119862, 0.5811942927096110934, -14.16772938898807510 ) ) ;
#3731=CARTESIAN_POINT ( 'NONE',  ( 116.1998614775786507, -10.63000616557722466, -14.87417383870573495 ) ) ;
#3732=ORIENTED_EDGE ( 'NONE', *, *, #29013, .F. ) ;
#3733=CARTESIAN_POINT ( 'NONE',  ( 111.8886348109120092, -3.383040157471821630, -19.15922257007629170 ) ) ;
#3736=CARTESIAN_POINT ( 'NONE',  ( 113.4202548109119846, -10.30919188438810075, -12.61870101168855918 ) ) ;
#3737=CARTESIAN_POINT ( 'NONE',  ( 115.0653281442453277, -6.344957434206662583, -7.627207830600332805 ) ) ;
#3738=CARTESIAN_POINT ( 'NONE',  ( 122.1561614775786353, -8.899110576539710493, -16.42337572283490132 ) ) ;
#3744=CARTESIAN_POINT ( 'NONE',  ( 115.4624148109119943, -4.153390946401321671, -8.397313243818183892 ) ) ;
#3749=CARTESIAN_POINT ( 'NONE',  ( 127.4620922277129580, -5.372330455815395922, -7.794320933752800329 ) ) ;
#3750=CARTESIAN_POINT ( 'NONE',  ( 124.9357681442453014, -1.834011780172310813, -8.268836392978581529 ) ) ;
#3752=CARTESIAN_POINT ( 'NONE',  ( 125.0492214775786266, -6.344957434206665248, -7.627207830600338134 ) ) ;
#3753=CARTESIAN_POINT ( 'NONE',  ( 114.7816948109119863, 0.5811942927096154232, -14.16772938898807155 ) ) ;
#3755=CARTESIAN_POINT ( 'NONE',  ( 114.6682414775786469, -7.894159318335828068, -9.358103419637847864 ) ) ;
#3758=CARTESIAN_POINT ( 'NONE',  ( 118.5256548109119876, -0.4660016031367893996, -10.09054647747474043 ) ) ;
#3759=CARTESIAN_POINT ( 'NONE',  ( 114.7249681442453237, -9.565557343593413364, -10.61323700422348004 ) ) ;
#3761=CARTESIAN_POINT ( 'NONE',  ( 121.3619881442452879, -5.574606645277164318, -18.38911715685844683 ) ) ;
#3762=CARTESIAN_POINT ( 'NONE',  ( 117.7314814775786260, -4.089484607189486809, -7.948022111789456723 ) ) ;
#3763=CARTESIAN_POINT ( 'NONE',  ( 137.0805771145923870, 0.2345801235192398748, -15.18230913089962186 ) ) ;
#3765=CARTESIAN_POINT ( 'NONE',  ( 114.6091521015961376, -1.040089454026971172, -17.23633227186634187 ) ) ;
#3768=CARTESIAN_POINT ( 'NONE',  ( 113.1366214775786432, -1.834011780172310813, -8.268836392978581529 ) ) ;
#3770=CARTESIAN_POINT ( 'NONE',  ( 113.7038881442453402, -6.222761293078241884, -8.102969835052219238 ) ) ;
#3771=CARTESIAN_POINT ( 'NONE',  ( 135.3184548109119874, -10.44474571748257041, -15.59668151425567650 ) ) ;
#3774=CARTESIAN_POINT ( 'NONE',  ( 113.0231681442453180, -10.15424416112533912, -14.75197769757731336 ) ) ;
#3776=CARTESIAN_POINT ( 'NONE',  ( 118.9227414775786400, -10.63000616557722466, -14.87417383870573495 ) ) ;
#3777=CARTESIAN_POINT ( 'NONE',  ( 115.7460481442453357, 0.9020085738987339008, -11.91225656197089222 ) ) ;
#3778=CARTESIAN_POINT ( 'NONE',  ( 123.8012348109119642, -9.565557343593413364, -10.61323700422348004 ) ) ;
#3779=CARTESIAN_POINT ( 'NONE',  ( 118.1285681442453068, -2.084020599724406786, -8.691656652584148546 ) ) ;
#3782=CARTESIAN_POINT ( 'NONE',  ( 124.0281414775786146, -1.834011780172310813, -8.268836392978581529 ) ) ;
#3784=CARTESIAN_POINT ( 'NONE',  ( 114.8951481442453115, -8.899110576539710493, -16.42337572283490132 ) ) ;
#3785=CARTESIAN_POINT ( 'NONE',  ( 112.6828081442453282, -2.084020599724406786, -8.691656652584148546 ) ) ;
#3788=CARTESIAN_POINT ( 'NONE',  ( 118.6391081442452986, -5.574606645277164318, -18.38911715685844683 ) ) ;
#3789=CARTESIAN_POINT ( 'NONE',  ( 121.0783548109119749, -9.565557343593413364, -10.61323700422348004 ) ) ;
#3795=CARTESIAN_POINT ( 'NONE',  ( 118.6391081442452986, -4.089484607189486809, -7.948022111789456723 ) ) ;
#3796=CARTESIAN_POINT ( 'NONE',  ( 115.2922348109119781, -10.63000616557722466, -14.87417383870573495 ) ) ;
#3803=CARTESIAN_POINT ( 'NONE',  ( 122.7234281442452755, -5.638512984488999180, -18.83840828888717311 ) ) ;
#3805=CARTESIAN_POINT ( 'NONE',  ( 112.7395348109119766, -5.638512984488999180, -18.83840828888717311 ) ) ;
#3806=CARTESIAN_POINT ( 'NONE',  ( 121.6456214775786293, 0.4262465694468514643, -12.03445270309931736 ) ) ;
#3807=FILL_AREA_STYLE_COLOUR ( '', #31518 ) ;
#3808=CARTESIAN_POINT ( 'NONE',  ( 125.0492214775786266, -6.344957434206665248, -7.627207830600338134 ) ) ;
#3809=CARTESIAN_POINT ( 'NONE',  ( 120.2274548109119934, 0.5811942927096110934, -14.16772938898807510 ) ) ;
#3813=CARTESIAN_POINT ( 'NONE',  ( 115.3489614775786407, -0.8288870151387760510, -10.36305467784173118 ) ) ;
#3816=CARTESIAN_POINT ( 'NONE',  ( 122.0427081442452817, 0.5811942927096110934, -14.16772938898807510 ) ) ;
#3817=CARTESIAN_POINT ( 'NONE',  ( 110.2184548109119788, -3.104384172016180887, -16.98539509221845734 ) ) ;
#3818=CARTESIAN_POINT ( 'NONE',  ( 116.1998614775786507, -10.63000616557722466, -14.87417383870573495 ) ) ;
#3821=CARTESIAN_POINT ( 'NONE',  ( 124.8790414775786246, -0.4660016031367893996, -10.09054647747474043 ) ) ;
#3823=CARTESIAN_POINT ( 'NONE',  ( 114.1009748109119784, -5.574606645277164318, -18.38911715685844683 ) ) ;
#3826=CARTESIAN_POINT ( 'NONE',  ( 121.1350814775786233, -9.859900752359378018, -12.68260735090039759 ) ) ;
#3827=EDGE_CURVE ( 'NONE', #12347, #30023, #27583, .T. ) ;
#3829=EDGE_CURVE ( 'NONE', #19616, #19203, #30806, .T. ) ;
#3831=CARTESIAN_POINT ( 'NONE',  ( 122.4397948109119767, -0.1624402480850797581, -16.17319339645315424 ) ) ;
#3834=CARTESIAN_POINT ( 'NONE',  ( 118.6391081442452986, -5.574606645277164318, -18.38911715685844683 ) ) ;
#3836=CARTESIAN_POINT ( 'NONE',  ( 115.8595014775786609, -1.834011780172310813, -8.268836392978581529 ) ) ;
#3838=CARTESIAN_POINT ( 'NONE',  ( 119.9438214775786378, -2.084020599724406786, -8.691656652584148546 ) ) ;
#3839=VERTEX_POINT ( 'NONE', #44570 ) ;
#3840=CARTESIAN_POINT ( 'NONE',  ( 118.1285681442453068, -7.893985811506177619, -18.51759400769804742 ) ) ;
#3846=CARTESIAN_POINT ( 'NONE',  ( 122.2128881442453263, -1.834011780172310813, -8.268836392978581529 ) ) ;
#3848=CARTESIAN_POINT ( 'NONE',  ( 126.5041214912228327, -8.436341138087987801, -9.693603847840460475 ) ) ;
#3849=CARTESIAN_POINT ( 'NONE',  ( 118.6391081442452986, -5.574606645277164318, -18.38911715685844683 ) ) ;
#3857=CARTESIAN_POINT ( 'NONE',  ( 113.9875214775786532, -0.4660016031367893996, -10.09054647747474043 ) ) ;
#3858=CARTESIAN_POINT ( 'NONE',  ( 112.7962614775786676, -3.383040157471821630, -19.15922257007629170 ) ) ;
#3859=CARTESIAN_POINT ( 'NONE',  ( 124.8790414775786246, -0.4660016031367893996, -10.09054647747474043 ) ) ;
#3860=CARTESIAN_POINT ( 'NONE',  ( 115.6325948109119821, -9.565557343593413364, -10.61323700422348004 ) ) ;
#3861=CARTESIAN_POINT ( 'NONE',  ( 126.4915402333600696, -3.531116461040918697, -8.432618951126483964 ) ) ;
#3862=CARTESIAN_POINT ( 'NONE',  ( 117.3343948109119737, -3.383040157471821630, -19.15922257007629170 ) ) ;
#3863=CARTESIAN_POINT ( 'NONE',  ( 111.6155414775786596, 0.3778260857407392814, -12.04688916545883792 ) ) ;
#3864=CARTESIAN_POINT ( 'NONE',  ( 123.2184548109119788, -4.863998795839242995, -13.39321520033831447 ) ) ;
#3866=CARTESIAN_POINT ( 'NONE',  ( 123.3474214775786209, -0.1624402480850797581, -16.17319339645315424 ) ) ;
#3872=CARTESIAN_POINT ( 'NONE',  ( 117.6180281442453150, -0.4660016031367893996, -10.09054647747474043 ) ) ;
#3873=CARTESIAN_POINT ( 'NONE',  ( 136.7082020370466751, -8.466464675110531246, -17.74021297388502560 ) ) ;
#3875=CARTESIAN_POINT ( 'NONE',  ( 136.1332990479133684, 0.5890802737549483137, -11.18462521611371940 ) ) ;
#3876=CARTESIAN_POINT ( 'NONE',  ( 121.5888948109119809, -10.30919188438810075, -12.61870101168855918 ) ) ;
#3878=CARTESIAN_POINT ( 'NONE',  ( 119.7736414775786358, 0.1319031606808879209, -14.10382304977623669 ) ) ;
#3881=CARTESIAN_POINT ( 'NONE',  ( 116.0864081442453113, -9.988377603198976828, -10.36322818467138340 ) ) ;
#3882=B_SPLINE_CURVE_WITH_KNOTS ( 'NONE', 3,
 ( #8003, #21912, #4801, #8909, #32614, #8460, #1159, #4575, #2054, #1380, #32390, #43341, #43113, #5026, #22363, #18941, #11656, #5470, #11883, #33279, #18500, #32831, #22584, #8233, #28987, #33049, #26014, #39919, #8680, #43566 ),
 .UNSPECIFIED., .F., .F.,
 ( 4, 2, 2, 1, 2, 2, 2, 1, 1, 2, 2, 2, 1, 1, 1, 2, 2, 4 ),
 ( 0.000000000000000000, 0.03124999999998964717, 0.06249999999997929434, 0.09374999999996894151, 0.1093749999999579364, 0.1249999999999469313, 0.1874999999999130695, 0.2187499999998872013, 0.2343749999998742672, 0.2421874999998592792, 0.2499999999998443190, 0.3749999999997088995, 0.4374999999996524447, 0.4687499999996350142, 0.4843749999996257993, 0.4921874999996208033, 0.4999999999996157518, 1.000000000000000000 ),
 .UNSPECIFIED. ) ;
#3883=CARTESIAN_POINT ( 'NONE',  ( 116.4642898793805443, -2.191907684172563986, -18.20049396185734025 ) ) ;
#3884=CARTESIAN_POINT ( 'NONE',  ( 112.8330431242421810, -1.016270020561755860, -17.26805140881366896 ) ) ;
#3887=CARTESIAN_POINT ( 'NONE',  ( 124.1415948109119540, -6.344957434206665248, -7.627207830600338134 ) ) ;
#3890=CARTESIAN_POINT ( 'NONE',  ( 124.0281414775786146, -1.834011780172310813, -8.268836392978581529 ) ) ;
#3891=CARTESIAN_POINT ( 'NONE',  ( 123.4608748109119745, -10.63000616557722466, -14.87417383870573495 ) ) ;
#3892=CARTESIAN_POINT ( 'NONE',  ( 122.4397948109119767, -0.1624402480850797581, -16.17319339645315424 ) ) ;
#3893=CARTESIAN_POINT ( 'NONE',  ( 119.6601881442453106, -1.833838273342659253, -17.42832698103878286 ) ) ;
#3895=CARTESIAN_POINT ( 'NONE',  ( 115.2355081442453155, -10.30919188438810075, -12.61870101168855918 ) ) ;
#3904=CARTESIAN_POINT ( 'NONE',  ( 126.4673881442452910, -7.894159318335828068, -9.358103419637847864 ) ) ;
#3906=CARTESIAN_POINT ( 'NONE',  ( 114.3846081442453197, 0.4262465694468514643, -12.03445270309931736 ) ) ;
#3908=CARTESIAN_POINT ( 'NONE',  ( 122.3147114802850410, -3.929494816604749641, -18.62311481910883870 ) ) ;
#3909=CARTESIAN_POINT ( 'NONE',  ( 124.5386814775786206, -5.638512984488999180, -18.83840828888717311 ) ) ;
#3910=CARTESIAN_POINT ( 'NONE',  ( 123.6877814775786533, -3.383040157471821630, -19.15922257007629170 ) ) ;
#3912=CARTESIAN_POINT ( 'NONE',  ( 116.9940348109119839, -9.988377603198976828, -10.36322818467138340 ) ) ;
#3918=CARTESIAN_POINT ( 'NONE',  ( 117.0507614775786465, 0.1319031606808879209, -14.10382304977623669 ) ) ;
#3919=CARTESIAN_POINT ( 'NONE',  ( 112.3424481442453384, -6.344957434206662583, -7.627207830600332805 ) ) ;
#3922=CARTESIAN_POINT ( 'NONE',  ( 119.8870948109119752, -0.8288870151387760510, -10.36305467784173118 ) ) ;
#3923=CARTESIAN_POINT ( 'NONE',  ( 120.9081748109119872, -4.153390946401325223, -8.397313243818185668 ) ) ;
#3924=CARTESIAN_POINT ( 'NONE',  ( 111.4348214775786801, -3.505236298600246325, -18.68346056562440793 ) ) ;
#3926=CARTESIAN_POINT ( 'NONE',  ( 124.7655881442452852, -9.859900752359378018, -12.68260735090039759 ) ) ;
#3928=CARTESIAN_POINT ( 'NONE',  ( 112.7395348109119766, -4.153390946401321671, -8.397313243818183892 ) ) ;
#3929=ORIENTED_EDGE ( 'NONE', *, *, #28917, .F. ) ;
#3930=LINE ( 'NONE', #294, #34696 ) ;
#3932=CARTESIAN_POINT ( 'NONE',  ( 112.6260814775786514, -9.261995988541697145, -16.69588392320189030 ) ) ;
#3936=CARTESIAN_POINT ( 'NONE',  ( 118.2420214775786320, -6.222761293078241884, -8.102969835052219238 ) ) ;
#3937=CARTESIAN_POINT ( 'NONE',  ( 114.8951481442453115, -8.899110576539710493, -16.42337572283490132 ) ) ;
#3940=FACE_OUTER_BOUND ( 'NONE', #7724, .T. ) ;
#3943=CARTESIAN_POINT ( 'NONE',  ( 112.8529881442453302, -1.561330072975668060, -17.79121239304076596 ) ) ;
#3944=CARTESIAN_POINT ( 'NONE',  ( 125.1626748109119802, -0.1624402480850797581, -16.17319339645315424 ) ) ;
#3946=CARTESIAN_POINT ( 'NONE',  ( 117.0507614775786465, 0.1319031606808879209, -14.10382304977623669 ) ) ;
#3947=CARTESIAN_POINT ( 'NONE',  ( 113.5337081442453240, -0.8288870151387690566, -10.36305467784174006 ) ) ;
#3949=CARTESIAN_POINT ( 'NONE',  ( 116.4267681442453153, -6.222761293078241884, -8.102969835052219238 ) ) ;
#3954=CARTESIAN_POINT ( 'NONE',  ( 113.5904348109119866, -7.893985811506177619, -18.51759400769804742 ) ) ;
#3956=CARTESIAN_POINT ( 'NONE',  ( 117.3911214775786505, -1.561330072975668504, -17.79121239304076951 ) ) ;
#3959=CARTESIAN_POINT ( 'NONE',  ( 113.3635281442453504, -9.988377603198976828, -10.36322818467138340 ) ) ;
#3960=CARTESIAN_POINT ( 'NONE',  ( 113.7606148109119886, -1.561330072975668060, -17.79121239304076596 ) ) ;
#3968=CARTESIAN_POINT ( 'NONE',  ( 115.6893214775786447, -9.859900752359374465, -12.68260735090039404 ) ) ;
#3972=CARTESIAN_POINT ( 'NONE',  ( 126.8137406967953211, -5.033017579089364979, -8.097877628942260486 ) ) ;
#3973=CARTESIAN_POINT ( 'NONE',  ( 123.9146881442452894, 0.9020085738987339008, -11.91225656197089222 ) ) ;
#3975=CARTESIAN_POINT ( 'NONE',  ( 123.0637881442452937, -0.4660016031367893996, -10.09054647747474043 ) ) ;
#3976=CARTESIAN_POINT ( 'NONE',  ( 115.8027748109119841, -0.4660016031367893996, -10.09054647747474043 ) ) ;
#3978=CARTESIAN_POINT ( 'NONE',  ( 114.8951481442453115, -8.899110576539710493, -16.42337572283490132 ) ) ;
#3980=CARTESIAN_POINT ( 'NONE',  ( 118.0718414775786300, -9.261995988541697145, -16.69588392320189030 ) ) ;
#3981=CARTESIAN_POINT ( 'NONE',  ( 116.7671281442453335, -7.643976991954077427, -18.09477374809248928 ) ) ;
#3983=CARTESIAN_POINT ( 'NONE',  ( 121.7590748109119687, -2.084020599724406786, -8.691656652584148546 ) ) ;
#3985=CARTESIAN_POINT ( 'NONE',  ( 117.1074881442453233, -10.63000616557722466, -14.87417383870573495 ) ) ;
#3986=CARTESIAN_POINT ( 'NONE',  ( 137.1434659109582128, 0.4862668849895840917, -13.14961857006992219 ) ) ;
#3990=DIRECTION ( 'NONE',  ( -1.000000000000000000, 0.000000000000000000, 0.000000000000000000 ) ) ;
#3992=CARTESIAN_POINT ( 'NONE',  ( 114.8384214775786489, 0.9020085738987339008, -11.91225656197089222 ) ) ;
#3997=CARTESIAN_POINT ( 'NONE',  ( 117.7765781469516924, -3.929494816604741203, -18.62311481910882804 ) ) ;
#3999=CARTESIAN_POINT ( 'NONE',  ( 122.1448793335884204, -2.334846009198419559, -18.01015021110789505 ) ) ;
#4003=CARTESIAN_POINT ( 'NONE',  ( 118.4122014775786340, 0.5811942927096110934, -14.16772938898807510 ) ) ;
#4004=CARTESIAN_POINT ( 'NONE',  ( 123.2339681442453241, -3.505236298600246325, -18.68346056562440793 ) ) ;
#4005=CARTESIAN_POINT ( 'NONE',  ( 120.4543614775786295, -5.574606645277164318, -18.38911715685844683 ) ) ;
#4006=CARTESIAN_POINT ( 'NONE',  ( 125.2194014775786286, -10.30919188438810075, -12.61870101168855918 ) ) ;
#4008=CARTESIAN_POINT ( 'NONE',  ( 137.2528433483957713, -8.663841125622667505, -9.754824023745433337 ) ) ;
#4009=CARTESIAN_POINT ( 'NONE',  ( 124.3685014775786328, -10.63000616557722466, -14.87417383870573495 ) ) ;
#4011=CARTESIAN_POINT ( 'NONE',  ( 117.9016614775786280, -0.1624402480850797581, -16.17319339645315424 ) ) ;
#4012=CARTESIAN_POINT ( 'NONE',  ( 113.5337081442453240, -0.8288870151387760510, -10.36305467784173118 ) ) ;
#4016=CARTESIAN_POINT ( 'NONE',  ( 119.4900081442453086, -7.643976991954077427, -18.09477374809248928 ) ) ;
#4017=CARTESIAN_POINT ( 'NONE',  ( 119.8870948109119752, -0.8288870151387760510, -10.36305467784173118 ) ) ;
#4023=CARTESIAN_POINT ( 'NONE',  ( 119.1496481442453046, -3.383040157471821630, -19.15922257007629170 ) ) ;
#4024=CARTESIAN_POINT ( 'NONE',  ( 116.4834948109119779, -1.561330072975668504, -17.79121239304076951 ) ) ;
#4026=CARTESIAN_POINT ( 'NONE',  ( 114.6682414775786469, -1.561330072975668060, -17.79121239304076596 ) ) ;
#4028=CARTESIAN_POINT ( 'NONE',  ( 113.0921268052895527, -1.125321370491273454, -17.12283323191015683 ) ) ;
#4030=CARTESIAN_POINT ( 'NONE',  ( 122.8368814775786291, -1.561330072975668948, -17.79121239304076951 ) ) ;
#4031=CARTESIAN_POINT ( 'NONE',  ( 115.4624148109119943, -5.638512984488999180, -18.83840828888717311 ) ) ;
#4032=CARTESIAN_POINT ( 'NONE',  ( 120.8514481442452961, -2.084020599724406786, -8.691656652584148546 ) ) ;
#4033=CARTESIAN_POINT ( 'NONE',  ( 124.7655881442452852, 0.5811942927096110934, -14.16772938898807510 ) ) ;
#4034=CARTESIAN_POINT ( 'NONE',  ( 123.4041481442452834, -10.30919188438810075, -12.61870101168855918 ) ) ;
#4036=CARTESIAN_POINT ( 'NONE',  ( 117.5045748109119756, -9.859900752359374465, -12.68260735090039404 ) ) ;
#4041=CARTESIAN_POINT ( 'NONE',  ( 122.2696148109119889, -4.089484607189486809, -7.948022111789456723 ) ) ;
#4043=CARTESIAN_POINT ( 'NONE',  ( 118.0718414775786300, -9.261995988541697145, -16.69588392320189030 ) ) ;
#4046=CARTESIAN_POINT ( 'NONE',  ( 124.8223148109119762, 0.9020085738987339008, -11.91225656197089222 ) ) ;
#4048=CARTESIAN_POINT ( 'NONE',  ( 114.7816948109119863, -9.859900752359374465, -12.68260735090039404 ) ) ;
#4049=CARTESIAN_POINT ( 'NONE',  ( 118.5256548109119876, -8.899110576539710493, -16.42337572283490132 ) ) ;
#4051=CARTESIAN_POINT ( 'NONE',  ( 120.3409081442453044, -8.899110576539710493, -16.42337572283490132 ) ) ;
#4053=CARTESIAN_POINT ( 'NONE',  ( 118.8660148109119774, 0.1319031606808879209, -14.10382304977623669 ) ) ;
#4054=CARTESIAN_POINT ( 'NONE',  ( 112.1155414775786454, 0.9020085738987339008, -11.91225656197089222 ) ) ;
#4055=CARTESIAN_POINT ( 'NONE',  ( 119.4900081442453086, -1.834011780172310813, -8.268836392978581529 ) ) ;
#4056=CARTESIAN_POINT ( 'NONE',  ( 112.0588148109119828, 0.5811942927096154232, -14.16772938898807155 ) ) ;
#4058=CARTESIAN_POINT ( 'NONE',  ( 120.6245414775786458, -0.1624402480850797581, -16.17319339645315424 ) ) ;
#4059=ORIENTED_EDGE ( 'NONE', *, *, #43434, .F. ) ;
#4060=CARTESIAN_POINT ( 'NONE',  ( 116.9373081442452929, -8.166667518702817929, -8.995218007635861213 ) ) ;
#4062=CARTESIAN_POINT ( 'NONE',  ( 115.2355081442453155, 0.1319031606808870605, -14.10382304977625090 ) ) ;
#4066=CARTESIAN_POINT ( 'NONE',  ( 120.6812681442452941, -10.30919188438810075, -12.61870101168855918 ) ) ;
#4069=CARTESIAN_POINT ( 'NONE',  ( 120.0005481442453146, -4.153390946401325223, -8.397313243818185668 ) ) ;
#4076=CARTESIAN_POINT ( 'NONE',  ( 114.9518748109119883, -1.834011780172310813, -8.268836392978581529 ) ) ;
#4077=CARTESIAN_POINT ( 'NONE',  ( 126.0703014775786102, -0.1624402480850797581, -16.17319339645315424 ) ) ;
#4078=CARTESIAN_POINT ( 'NONE',  ( 124.9924948109119924, -4.089484607189486809, -7.948022111789456723 ) ) ;
#4079=CARTESIAN_POINT ( 'NONE',  ( 120.4543614775786295, -5.574606645277164318, -18.38911715685844683 ) ) ;
#4080=CARTESIAN_POINT ( 'NONE',  ( 126.4262034846925786, -3.611341894066276481, -8.445358815182457235 ) ) ;
#4081=CARTESIAN_POINT ( 'NONE',  ( 121.8725281442453223, -3.383040157471821630, -19.15922257007629170 ) ) ;
#4082=CARTESIAN_POINT ( 'NONE',  ( 112.1155414775786454, -10.15424416112533912, -14.75197769757731336 ) ) ;
#4085=CARTESIAN_POINT ( 'NONE',  ( 112.1155414775786454, 0.9020085738987339008, -11.91225656197089222 ) ) ;
#4090=CARTESIAN_POINT ( 'NONE',  ( 121.5888948109119809, -10.30919188438810075, -12.61870101168855918 ) ) ;
#4094=CARTESIAN_POINT ( 'NONE',  ( 111.7184548109119788, -9.261995988541697145, -16.69588392320189030 ) ) ;
#4095=CARTESIAN_POINT ( 'NONE',  ( 122.8936081442453059, 0.2603800115204892296, -16.42320221600525088 ) ) ;
#4097=CARTESIAN_POINT ( 'NONE',  ( 123.4041481442452834, 0.1319031606808879209, -14.10382304977623669 ) ) ;
#4099=CARTESIAN_POINT ( 'NONE',  ( 113.7038881442453402, -3.383040157471821630, -19.15922257007629170 ) ) ;
#4102=CARTESIAN_POINT ( 'NONE',  ( 120.9081748109119872, -5.638512984489026714, -18.83840828888716956 ) ) ;
#4103=CARTESIAN_POINT ( 'NONE',  ( 136.6675107540880845, -5.407613336693704476, -7.751903229841559551 ) ) ;
#4104=CARTESIAN_POINT ( 'NONE',  ( 124.7088614775786226, 0.2603800115204892296, -16.42320221600525088 ) ) ;
#4106=AXIS2_PLACEMENT_3D ( 'NONE', #9030, #4695, #18615 ) ;
#4109=CARTESIAN_POINT ( 'NONE',  ( 123.2339681442453241, -6.344957434206665248, -7.627207830600338134 ) ) ;
#4110=CARTESIAN_POINT ( 'NONE',  ( 121.5321681442453183, -9.988377603198976828, -10.36322818467138340 ) ) ;
#4111=CARTESIAN_POINT ( 'NONE',  ( 124.0848681442452772, -5.574606645277164318, -18.38911715685844683 ) ) ;
#4112=CARTESIAN_POINT ( 'NONE',  ( 118.7525614775786380, -1.833838273342659253, -17.42832698103878286 ) ) ;
#4114=CARTESIAN_POINT ( 'NONE',  ( 118.8660148109119774, -10.30919188438810075, -12.61870101168855918 ) ) ;
#4125=CARTESIAN_POINT ( 'NONE',  ( 124.1415948109119540, -6.344957434206665248, -7.627207830600338134 ) ) ;
#4126=CARTESIAN_POINT ( 'NONE',  ( 112.9664414775786412, 0.5811942927096154232, -14.16772938898807155 ) ) ;
#4129=CARTESIAN_POINT ( 'NONE',  ( 113.5904348109119866, -2.084020599724406786, -8.691656652584148546 ) ) ;
#4131=CARTESIAN_POINT ( 'NONE',  ( 119.2063748109119814, -7.894159318335806752, -9.358103419637831877 ) ) ;
#4132=FACE_OUTER_BOUND ( 'NONE', #40700, .T. ) ;
#4133=CARTESIAN_POINT ( 'NONE',  ( 124.6521348109119884, -1.561330072975668948, -17.79121239304076951 ) ) ;
#4135=CARTESIAN_POINT ( 'NONE',  ( 117.9016614775786280, -9.988377603198976828, -10.36322818467138340 ) ) ;
#4141=CARTESIAN_POINT ( 'NONE',  ( 116.3133148109120043, -2.084020599724406786, -8.691656652584148546 ) ) ;
#4142=CARTESIAN_POINT ( 'NONE',  ( 125.9568481442452850, -3.505236298600246325, -18.68346056562440793 ) ) ;
#4144=CARTESIAN_POINT ( 'NONE',  ( 113.2500748109119968, -6.344957434206662583, -7.627207830600332805 ) ) ;
#4146=CARTESIAN_POINT ( 'NONE',  ( 123.9146881442452894, -10.15424416112533912, -14.75197769757731336 ) ) ;
#4148=CARTESIAN_POINT ( 'NONE',  ( 121.3619881442452879, -5.574606645277164318, -18.38911715685844683 ) ) ;
#4149=CARTESIAN_POINT ( 'NONE',  ( 117.0507614775786465, 0.1319031606808879209, -14.10382304977623669 ) ) ;
#4150=ORIENTED_EDGE ( 'NONE', *, *, #29223, .F. ) ;
#4154=CARTESIAN_POINT ( 'NONE',  ( 121.8367297606643262, -2.236191541394346061, -18.14152338500401029 ) ) ;
#4155=CARTESIAN_POINT ( 'NONE',  ( 115.1220548109119761, -1.833838273342658809, -17.42832698103878286 ) ) ;
#4157=CARTESIAN_POINT ( 'NONE',  ( 126.8396850857591289, -9.603614909541551725, -15.78910935443854768 ) ) ;
#4161=CARTESIAN_POINT ( 'NONE',  ( 124.9924948109119924, -5.574606645277164318, -18.38911715685844683 ) ) ;
#4163=CARTESIAN_POINT ( 'NONE',  ( 117.2209414775786485, -2.084020599724406786, -8.691656652584148546 ) ) ;
#4164=CARTESIAN_POINT ( 'NONE',  ( 115.6325948109119821, -9.565557343593413364, -10.61323700422348004 ) ) ;
#4172=CARTESIAN_POINT ( 'NONE',  ( 113.4202548109119846, -10.30919188438810075, -12.61870101168855918 ) ) ;
#4173=CARTESIAN_POINT ( 'NONE',  ( 126.4106614775786284, -6.222761293078241884, -8.102969835052219238 ) ) ;
#4174=CARTESIAN_POINT ( 'NONE',  ( 116.8238548109119819, -5.574606645277164318, -18.38911715685844683 ) ) ;
#4175=CARTESIAN_POINT ( 'NONE',  ( 113.4769814775786614, 0.4262465694468579591, -12.03445270309932802 ) ) ;
#4177=CARTESIAN_POINT ( 'NONE',  ( 117.7882081442453170, -3.505236298600246325, -18.68346056562440793 ) ) ;
#4181=CARTESIAN_POINT ( 'NONE',  ( 115.2355081442453155, -10.30919188438810075, -12.61870101168855918 ) ) ;
#4183=CARTESIAN_POINT ( 'NONE',  ( 116.1998614775786507, -10.63000616557722466, -14.87417383870573495 ) ) ;
#4186=CARTESIAN_POINT ( 'NONE',  ( 115.1787814775786387, -9.988377603198976828, -10.36322818467138340 ) ) ;
#4187=CARTESIAN_POINT ( 'NONE',  ( 113.8173414775786512, 0.2603800115204892296, -16.42320221600525088 ) ) ;
#4192=ADVANCED_FACE ( 'NONE', ( #3940 ), #743, .T. ) ;
#4196=CARTESIAN_POINT ( 'NONE',  ( 115.6325948109119821, -9.565557343593413364, -10.61323700422348004 ) ) ;
#4198=CARTESIAN_POINT ( 'NONE',  ( 117.9583881442453048, -10.30919188438809719, -12.61870101168856273 ) ) ;
#4200=CARTESIAN_POINT ( 'NONE',  ( 126.6827570900409796, -4.935151780043032232, -8.161448820960071515 ) ) ;
#4201=CARTESIAN_POINT ( 'NONE',  ( 113.5337081442453240, -0.8288870151387760510, -10.36305467784173118 ) ) ;
#4203=CARTESIAN_POINT ( 'NONE',  ( 123.3474214775786209, -9.988377603198976828, -10.36322818467138340 ) ) ;
#4204=CARTESIAN_POINT ( 'NONE',  ( 116.9940348109119839, -9.988377603198976828, -10.36322818467138340 ) ) ;
#4206=CARTESIAN_POINT ( 'NONE',  ( 116.0296814775786345, -1.833838273342658809, -17.42832698103878286 ) ) ;
#4207=CARTESIAN_POINT ( 'NONE',  ( 112.5126281442453120, -10.30919188438810075, -12.61870101168855918 ) ) ;
#4208=EDGE_CURVE ( 'NONE', #42235, #1359, #8513, .T. ) ;
#4209=CARTESIAN_POINT ( 'NONE',  ( 117.7314814775786260, -4.089484607189486809, -7.948022111789456723 ) ) ;
#4211=CARTESIAN_POINT ( 'NONE',  ( 118.6958348109119754, -3.505236298600246325, -18.68346056562440793 ) ) ;
#4214=CARTESIAN_POINT ( 'NONE',  ( 122.4965214775786251, 0.1319031606808879209, -14.10382304977623669 ) ) ;
#4215=CARTESIAN_POINT ( 'NONE',  ( 115.3489614775786407, -9.261995988541697145, -16.69588392320189030 ) ) ;
#4216=CARTESIAN_POINT ( 'NONE',  ( 137.3409837554746105, 0.3147047579545037554, -13.41223745296854730 ) ) ;
#4221=CARTESIAN_POINT ( 'NONE',  ( 114.3846081442453197, -10.63000616557722466, -14.87417383870573495 ) ) ;
#4222=CARTESIAN_POINT ( 'NONE',  ( 136.6675107540953604, -10.50531076633295768, -13.93682974119022866 ) ) ;
#4223=CARTESIAN_POINT ( 'NONE',  ( 115.9162281442453235, -5.574606645277164318, -18.38911715685844683 ) ) ;
#4225=CARTESIAN_POINT ( 'NONE',  ( 117.2209414775786485, -2.084020599724404121, -8.691656652584155651 ) ) ;
#4227=CARTESIAN_POINT ( 'NONE',  ( 115.4624148109119943, -5.638512984488999180, -18.83840828888717311 ) ) ;
#4231=CARTESIAN_POINT ( 'NONE',  ( 119.8303681442453126, -10.63000616557722466, -14.87417383870573495 ) ) ;
#4233=CARTESIAN_POINT ( 'NONE',  ( 117.5613014775786525, -10.15424416112533912, -14.75197769757731336 ) ) ;
#4234=CARTESIAN_POINT ( 'NONE',  ( 125.9568481442452850, -6.344957434206665248, -7.627207830600338134 ) ) ;
#4237=CARTESIAN_POINT ( 'NONE',  ( 123.1772414775786189, -4.089484607189486809, -7.948022111789456723 ) ) ;
#4239=CARTESIAN_POINT ( 'NONE',  ( 120.2274548109119934, -9.859900752359374465, -12.68260735090039404 ) ) ;
#4241=CARTESIAN_POINT ( 'NONE',  ( 116.5402214775786405, -9.565557343593413364, -10.61323700422348004 ) ) ;
#4244=CARTESIAN_POINT ( 'NONE',  ( 121.6456214775786293, 0.4262465694468514643, -12.03445270309931736 ) ) ;
#4245=CARTESIAN_POINT ( 'NONE',  ( 125.6732148109119862, -9.859900752359378018, -12.68260735090039759 ) ) ;
#4251=CARTESIAN_POINT ( 'NONE',  ( 117.2776681442452968, -5.638512984488999180, -18.83840828888717311 ) ) ;
#4252=CARTESIAN_POINT ( 'NONE',  ( 117.6180281442453150, -0.4660016031367893996, -10.09054647747474043 ) ) ;
#4254=CARTESIAN_POINT ( 'NONE',  ( 112.7395348109119766, -5.638512984488999180, -18.83840828888717311 ) ) ;
#4256=DIRECTION ( 'NONE',  ( -1.000000000000000000, 0.000000000000000000, 0.000000000000000000 ) ) ;
#4257=CARTESIAN_POINT ( 'NONE',  ( 117.6747548109119919, -1.834011780172310813, -8.268836392978581529 ) ) ;
#4259=CARTESIAN_POINT ( 'NONE',  ( 121.5888948109119809, 0.1319031606808879209, -14.10382304977623669 ) ) ;
#4261=CARTESIAN_POINT ( 'NONE',  ( 125.2761281442453054, -10.63000616557722466, -14.87417383870573495 ) ) ;
#4262=CARTESIAN_POINT ( 'NONE',  ( 122.0427081442452817, 0.5811942927096110934, -14.16772938898807510 ) ) ;
#4264=CARTESIAN_POINT ( 'NONE',  ( 117.5613014775786525, -10.15424416112533912, -14.75197769757731336 ) ) ;
#4268=CARTESIAN_POINT ( 'NONE',  ( 121.5321681442453183, -9.988377603198976828, -10.36322818467138340 ) ) ;
#4270=CARTESIAN_POINT ( 'NONE',  ( 120.1707281442453166, 0.2603800115204892296, -16.42320221600525088 ) ) ;
#4272=CARTESIAN_POINT ( 'NONE',  ( 125.4463081442452932, -4.153390946401325223, -8.397313243818185668 ) ) ;
#4276=CARTESIAN_POINT ( 'NONE',  ( 114.8951481442453115, -8.899110576539710493, -16.42337572283490132 ) ) ;
#4278=CARTESIAN_POINT ( 'NONE',  ( 123.8427358961590130, -2.263366209404226392, -18.10533625161308180 ) ) ;
#4279=CARTESIAN_POINT ( 'NONE',  ( 119.4900081442453086, -7.643976991954077427, -18.09477374809248928 ) ) ;
#4281=CARTESIAN_POINT ( 'NONE',  ( 121.1918081442452859, -10.15424416112533912, -14.75197769757731336 ) ) ;
#4283=CARTESIAN_POINT ( 'NONE',  ( 119.7736414775786358, 0.1319031606808879209, -14.10382304977623669 ) ) ;
#4284=CARTESIAN_POINT ( 'NONE',  ( 114.5547881442453217, -5.638512984488999180, -18.83840828888717311 ) ) ;
#4285=CARTESIAN_POINT ( 'NONE',  ( 120.2841814775786276, 0.9020085738987339008, -11.91225656197089222 ) ) ;
#4286=CARTESIAN_POINT ( 'NONE',  ( 113.3635281442453504, -9.988377603198976828, -10.36322818467138340 ) ) ;
#4288=CARTESIAN_POINT ( 'NONE',  ( 118.7525614775786380, -1.833838273342659253, -17.42832698103878286 ) ) ;
#4290=CARTESIAN_POINT ( 'NONE',  ( 119.5467348109119712, -4.089484607189486809, -7.948022111789456723 ) ) ;
#4292=DIRECTION ( 'NONE',  ( -1.000000000000000000, 0.000000000000000000, 0.000000000000000000 ) ) ;
#4295=CARTESIAN_POINT ( 'NONE',  ( 125.7866681442452688, -0.4660016031367893996, -10.09054647747474043 ) ) ;
#4299=CARTESIAN_POINT ( 'NONE',  ( 122.1561614775786353, -8.899110576539710493, -16.42337572283490132 ) ) ;
#4305=CARTESIAN_POINT ( 'NONE',  ( 114.7816948109119863, 0.5811942927096154232, -14.16772938898807155 ) ) ;
#4306=CARTESIAN_POINT ( 'NONE',  ( 113.1366214775786432, -1.834011780172310813, -8.268836392978581529 ) ) ;
#4308=CARTESIAN_POINT ( 'NONE',  ( 121.0216281442452981, -7.894159318335828068, -9.358103419637847864 ) ) ;
#4310=CARTESIAN_POINT ( 'NONE',  ( 126.2333338125921074, -4.013644120520951653, -8.458427223423711894 ) ) ;
#4312=CARTESIAN_POINT ( 'NONE',  ( 122.4397948109119767, -9.988377603198976828, -10.36322818467138340 ) ) ;
#4313=CARTESIAN_POINT ( 'NONE',  ( 123.5176014775786228, -0.8288870151387499607, -10.36305467784176493 ) ) ;
#4314=( BOUNDED_CURVE ( )  B_SPLINE_CURVE ( 2, ( #28140, #24704, #42268, #4175, #3947, #3285, #27919, #42049, #31100, #20630, #17424, #31316, #24489, #38377, #17207, #38594, #7371 ),
 .UNSPECIFIED., .F., .F. ) 
 B_SPLINE_CURVE_WITH_KNOTS ( ( 3, 2, 2, 2, 2, 2, 2, 2, 3 ),
 ( 0.1421282416568590001, 0.1484375000000000000, 0.1562500000000000000, 0.1640625000000000000, 0.1718750000000000000, 0.1796875000000000000, 0.1875000000000000000, 0.1953125000000000000, 0.2016217583431409999 ),
 .UNSPECIFIED. ) 
 CURVE ( )  GEOMETRIC_REPRESENTATION_ITEM ( )  RATIONAL_B_SPLINE_CURVE ( ( 0.9763430640195970289, 0.9385262470928680267, 1.000000000000000000, 0.9238795325112869605, 1.000000000000000000, 0.9238795325112869605, 1.000000000000000000, 0.9238795325112869605, 1.000000000000000000, 0.9238795325112869605, 1.000000000000000000, 0.9238795325112869605, 1.000000000000000000, 0.9238795325112869605, 1.000000000000000000, 0.9385262470928680267, 0.9763430640195970289 ) ) 
 REPRESENTATION_ITEM ( '' )  );
#4320=CARTESIAN_POINT ( 'NONE',  ( 120.8514481442452961, -7.893985811506177619, -18.51759400769804742 ) ) ;
#4321=CARTESIAN_POINT ( 'NONE',  ( 136.2632467228247037, -10.27097813662025416, -15.60566243075115977 ) ) ;
#4324=CARTESIAN_POINT ( 'NONE',  ( 112.1155414775786454, -10.15424416112533912, -14.75197769757731336 ) ) ;
#4326=CARTESIAN_POINT ( 'NONE',  ( 124.5954081442453116, -6.222761293078241884, -8.102969835052219238 ) ) ;
#4328=CARTESIAN_POINT ( 'NONE',  ( 119.8870948109119752, -9.261995988541697145, -16.69588392320189030 ) ) ;
#4334=CARTESIAN_POINT ( 'NONE',  ( 111.4915481442453142, -1.833838273342658365, -17.42832698103878286 ) ) ;
#4337=CARTESIAN_POINT ( 'NONE',  ( 125.0492214775786266, -6.344957434206665248, -7.627207830600338134 ) ) ;
#4339=CARTESIAN_POINT ( 'NONE',  ( 121.9292548109119849, -1.561330072975668948, -17.79121239304076951 ) ) ;
#4340=CARTESIAN_POINT ( 'NONE',  ( 121.8158014775786171, -4.153390946401325223, -8.397313243818185668 ) ) ;
#4342=CARTESIAN_POINT ( 'NONE',  ( 124.4252281442452812, -0.8288870151387760510, -10.36305467784173118 ) ) ;
#4344=CARTESIAN_POINT ( 'NONE',  ( 121.3052614775786111, -1.834011780172310813, -8.268836392978581529 ) ) ;
#4347=CARTESIAN_POINT ( 'NONE',  ( 122.7443564273309988, -2.236191541394346061, -18.14152338500401029 ) ) ;
#4351=CARTESIAN_POINT ( 'NONE',  ( 125.1626748109119802, -9.988377603198980381, -10.36322818467138518 ) ) ;
#4352=CARTESIAN_POINT ( 'NONE',  ( 125.2194014775786286, 0.1319031606808879209, -14.10382304977623669 ) ) ;
#4354=CARTESIAN_POINT ( 'NONE',  ( 114.5547881442453217, -4.153390946401321671, -8.397313243818183892 ) ) ;
#4357=CARTESIAN_POINT ( 'NONE',  ( 125.5597614775786326, -1.561330072975669392, -17.79121239304076951 ) ) ;
#4360=CARTESIAN_POINT ( 'NONE',  ( 115.5758681442453053, -1.561330072975668060, -17.79121239304076951 ) ) ;
#4364=CARTESIAN_POINT ( 'NONE',  ( 126.2184548109108420, -7.843366116849215253, -9.377719973493116257 ) ) ;
#4365=CARTESIAN_POINT ( 'NONE',  ( 120.5678148109119832, -1.833838273342659253, -17.42832698103878286 ) ) ;
#4366=CARTESIAN_POINT ( 'NONE',  ( 117.7882081442453170, -6.344957434206665248, -7.627207830600338134 ) ) ;
#4370=CARTESIAN_POINT ( 'NONE',  ( 125.5030348109119558, -6.222761293078241884, -8.102969835052219238 ) ) ;
#4371=CARTESIAN_POINT ( 'NONE',  ( 118.8092881442453290, -0.1624402480850797581, -16.17319339645315424 ) ) ;
#4372=CARTESIAN_POINT ( 'NONE',  ( 115.1787814775786387, -0.1624402480850797581, -16.17319339645315424 ) ) ;
#4378=CARTESIAN_POINT ( 'NONE',  ( 118.8092881442453290, -0.1624402480850797581, -16.17319339645315424 ) ) ;
#4379=ORIENTED_EDGE ( 'NONE', *, *, #34764, .F. ) ;
#4383=CARTESIAN_POINT ( 'NONE',  ( 114.1577014775786552, -6.344957434206662583, -7.627207830600332805 ) ) ;
#4386=CARTESIAN_POINT ( 'NONE',  ( 113.8173414775786512, -9.565557343593413364, -10.61323700422348004 ) ) ;
#4389=CARTESIAN_POINT ( 'NONE',  ( 119.4900081442453086, -7.643976991954077427, -18.09477374809248928 ) ) ;
#4390=CARTESIAN_POINT ( 'NONE',  ( 116.9940348109119839, -0.1624402480850797581, -16.17319339645315424 ) ) ;
#4394=CARTESIAN_POINT ( 'NONE',  ( 121.1874648073892615, -1.081026697600536046, -17.18181821144402832 ) ) ;
#4398=( BOUNDED_CURVE ( )  B_SPLINE_CURVE ( 2, ( #7422, #31375, #21343, #146, #14280, #35227, #593, #14503, #31159, #14060, #45077, #3776, #44864, #6548, #27978, #38436, #41882 ),
 .UNSPECIFIED., .F., .F. ) 
 B_SPLINE_CURVE_WITH_KNOTS ( ( 3, 2, 2, 2, 2, 2, 2, 2, 3 ),
 ( 0.4545046674808919662, 0.4609375000000000000, 0.4687500000000000000, 0.4765625000000000000, 0.4843750000000000000, 0.4921875000000000000, 0.5000000000000000000, 0.5078125000000000000, 0.5142453325190590174 ),
 .UNSPECIFIED. ) 
 CURVE ( )  GEOMETRIC_REPRESENTATION_ITEM ( )  RATIONAL_B_SPLINE_CURVE ( ( 0.9778625265006459788, 0.9373222120152210346, 1.000000000000000000, 0.9238795325112869605, 1.000000000000000000, 0.9238795325112869605, 1.000000000000000000, 0.9238795325112869605, 1.000000000000000000, 0.9238795325112869605, 1.000000000000000000, 0.9238795325112869605, 1.000000000000000000, 0.9238795325112869605, 1.000000000000000000, 0.9373222120157009840, 0.9778625265000250311 ) ) 
 REPRESENTATION_ITEM ( '' )  );
#4399=CARTESIAN_POINT ( 'NONE',  ( 113.8173414775786512, 0.2603800115204892296, -16.42320221600525088 ) ) ;
#4401=CARTESIAN_POINT ( 'NONE',  ( 126.1270281442452870, 0.1319031606808879209, -14.10382304977623669 ) ) ;
#4402=CARTESIAN_POINT ( 'NONE',  ( 117.3343948109119737, -6.222761293078241884, -8.102969835052219238 ) ) ;
#4404=EDGE_CURVE ( 'NONE', #38601, #11611, #35139, .T. ) ;
#4407=CARTESIAN_POINT ( 'NONE',  ( 118.8660148109119774, 0.1319031606808879209, -14.10382304977623669 ) ) ;
#4409=AXIS2_PLACEMENT_3D ( 'NONE', #10168, #13365, #3086 ) ;
#4411=CARTESIAN_POINT ( 'NONE',  ( 116.6536748109119941, 0.9020085738987339008, -11.91225656197089222 ) ) ;
#4414=CARTESIAN_POINT ( 'NONE',  ( 118.5256548109119876, -0.4660016031367893996, -10.09054647747474043 ) ) ;
#4417=CARTESIAN_POINT ( 'NONE',  ( 117.2776681442452968, -5.638512984488999180, -18.83840828888717311 ) ) ;
#4418=CARTESIAN_POINT ( 'NONE',  ( 115.4056881442453459, -7.893985811506177619, -18.51759400769804742 ) ) ;
#4425=CARTESIAN_POINT ( 'NONE',  ( 115.9729548109119861, -3.505236298600246325, -18.68346056562440793 ) ) ;
#4429=CARTESIAN_POINT ( 'NONE',  ( 126.3444272079776454, -4.573690577007555547, -8.338462930989205546 ) ) ;
#4430=CARTESIAN_POINT ( 'NONE',  ( 114.8384214775786489, -10.15424416112533912, -14.75197769757731336 ) ) ;
#4431=CARTESIAN_POINT ( 'NONE',  ( 135.8113403534200074, 1.048617111794840628, -12.65718902849948435 ) ) ;
#4432=CARTESIAN_POINT ( 'NONE',  ( 122.2128881442453263, -1.834011780172310813, -8.268836392978581529 ) ) ;
#4433=CARTESIAN_POINT ( 'NONE',  ( 120.4543614775786295, -4.089484607189486809, -7.948022111789456723 ) ) ;
#4435=CARTESIAN_POINT ( 'NONE',  ( 118.3554748109119998, -9.565557343593413364, -10.61323700422348004 ) ) ;
#4436=CARTESIAN_POINT ( 'NONE',  ( 126.0135748109119902, -8.166667518702819706, -8.995218007635861213 ) ) ;
#4438=CARTESIAN_POINT ( 'NONE',  ( 119.4332814775786318, -0.4660016031367893996, -10.09054647747474043 ) ) ;
#4439=CARTESIAN_POINT ( 'NONE',  ( 118.7525614775786380, -1.833838273342659253, -17.42832698103878286 ) ) ;
#4441=CARTESIAN_POINT ( 'NONE',  ( 120.2274548109119934, -9.859900752359378018, -12.68260735090039759 ) ) ;
#4443=CARTESIAN_POINT ( 'NONE',  ( 121.7590748109119687, -7.893985811506177619, -18.51759400769804742 ) ) ;
#4444=CARTESIAN_POINT ( 'NONE',  ( 135.3184548109119874, 0.6402711692277546218, -15.78131322003127579 ) ) ;
#4450=CARTESIAN_POINT ( 'NONE',  ( 116.7671281442453335, -1.834011780172310813, -8.268836392978581529 ) ) ;
#4452=CARTESIAN_POINT ( 'NONE',  ( 115.1787814775786387, -0.1624402480850797581, -16.17319339645315424 ) ) ;
#4457=CARTESIAN_POINT ( 'NONE',  ( 112.6828081442453282, -2.084020599724406786, -8.691656652584148546 ) ) ;
#4462=CARTESIAN_POINT ( 'NONE',  ( 118.6391081442452986, -4.089484607189486809, -7.948022111789456723 ) ) ;
#4463=CARTESIAN_POINT ( 'NONE',  ( 119.0361948109119652, -2.084020599724406786, -8.691656652584148546 ) ) ;
#4464=CARTESIAN_POINT ( 'NONE',  ( 112.5126281442453120, 0.1319031606808879209, -14.10382304977623669 ) ) ;
#4465=ORIENTED_EDGE ( 'NONE', *, *, #10351, .T. ) ;
#4466=CARTESIAN_POINT ( 'NONE',  ( 137.4945747550013095, -7.665717176805711297, -9.228124848700741012 ) ) ;
#4468=CARTESIAN_POINT ( 'NONE',  ( 122.6667014775786413, -7.893985811506177619, -18.51759400769804742 ) ) ;
#4470=CARTESIAN_POINT ( 'NONE',  ( 118.1852948109119836, -4.153390946401325223, -8.397313243818185668 ) ) ;
#4471=CARTESIAN_POINT ( 'NONE',  ( 117.7314814775786260, -5.574606645277164318, -18.38911715685844683 ) ) ;
#4474=CARTESIAN_POINT ( 'NONE',  ( 122.1561614775786353, -8.899110576539710493, -16.42337572283490132 ) ) ;
#4475=CARTESIAN_POINT ( 'NONE',  ( 124.5386814775786206, -4.153390946401325223, -8.397313243818185668 ) ) ;
#4476=CARTESIAN_POINT ( 'NONE',  ( 114.2354127111058659, -1.267766418764742387, -16.93314635290707315 ) ) ;
#4482=CARTESIAN_POINT ( 'NONE',  ( 116.4267681442453153, -3.383040157471821630, -19.15922257007629170 ) ) ;
#4483=CARTESIAN_POINT ( 'NONE',  ( 119.8303681442453126, -10.63000616557722466, -14.87417383870573495 ) ) ;
#4485=CARTESIAN_POINT ( 'NONE',  ( 112.6828081442453282, -7.893985811506177619, -18.51759400769804742 ) ) ;
#4487=CARTESIAN_POINT ( 'NONE',  ( 117.3711764575755012, -1.016270020561755860, -17.26805140881366896 ) ) ;
#4488=CARTESIAN_POINT ( 'NONE',  ( 117.3343948109119737, -3.383040157471821630, -19.15922257007629170 ) ) ;
#4489=CARTESIAN_POINT ( 'NONE',  ( 123.4041481442452834, 0.1319031606808879209, -14.10382304977623669 ) ) ;
#4491=CARTESIAN_POINT ( 'NONE',  ( 124.5386814775786206, -5.638512984488999180, -18.83840828888717311 ) ) ;
#4492=CARTESIAN_POINT ( 'NONE',  ( 121.7023481442452777, -9.261995988541697145, -16.69588392320189030 ) ) ;
#4493=B_SPLINE_CURVE_WITH_KNOTS ( 'NONE', 3,
 ( #8164, #35735, #8388, #4278, #11137, #25495, #43043, #11586, #14779, #32978 ),
 .UNSPECIFIED., .F., .F.,
 ( 4, 3, 3, 4 ),
 ( 0.000000000000000000, 0.0001671877560958130043, 0.0003343755126086565138, 0.0006438490228507229903 ),
 .UNSPECIFIED. ) ;
#4495=CARTESIAN_POINT ( 'NONE',  ( 114.7249681442453237, -9.565557343593413364, -10.61323700422348004 ) ) ;
#4498=EDGE_LOOP ( 'NONE', ( #2231, #31266, #34221, #2103 ) ) ;
#4499=EDGE_CURVE ( 'NONE', #19842, #38747, #7745, .T. ) ;
#4501=CARTESIAN_POINT ( 'NONE',  ( 119.5467348109119712, -4.089484607189486809, -7.948022111789456723 ) ) ;
#4502=EDGE_LOOP ( 'NONE', ( #4996, #1834, #5293, #16106 ) ) ;
#4506=DIRECTION ( 'NONE',  ( 0.000000000000000000, 0.6004852223388321697, -0.7996358532186279566 ) ) ;
#4507=CARTESIAN_POINT ( 'NONE',  ( 114.0442481442453300, -7.643976991954077427, -18.09477374809248928 ) ) ;
#4510=CARTESIAN_POINT ( 'NONE',  ( 120.7947214775786193, -0.8288870151387760510, -10.36305467784173118 ) ) ;
#4512=CARTESIAN_POINT ( 'NONE',  ( 122.6667014775786413, -2.084020599724406786, -8.691656652584148546 ) ) ;
#4516=CARTESIAN_POINT ( 'NONE',  ( 122.7801548109119665, -6.222761293078241884, -8.102969835052219238 ) ) ;
#4517=CARTESIAN_POINT ( 'NONE',  ( 112.2289948109119848, -1.834011780172310813, -8.268836392978581529 ) ) ;
#4518=CARTESIAN_POINT ( 'NONE',  ( 119.5467348109119712, -4.089484607189486809, -7.948022111789456723 ) ) ;
#4519=CARTESIAN_POINT ( 'NONE',  ( 126.4673881442452910, -7.894159318335828068, -9.358103419637847864 ) ) ;
#4521=CARTESIAN_POINT ( 'NONE',  ( 119.6601881442453106, -1.833838273342659253, -17.42832698103878286 ) ) ;
#4523=CARTESIAN_POINT ( 'NONE',  ( 122.1561614775786353, -0.4660016031367893996, -10.09054647747474043 ) ) ;
#4530=CARTESIAN_POINT ( 'NONE',  ( 121.5888948109119809, 0.1319031606808879209, -14.10382304977623669 ) ) ;
#4531=CARTESIAN_POINT ( 'NONE',  ( 124.4252281442453238, -9.261995988541050551, -16.69588392320275361 ) ) ;
#4536=CARTESIAN_POINT ( 'NONE',  ( 114.4413348109119823, -9.261995988541697145, -16.69588392320189030 ) ) ;
#4537=CARTESIAN_POINT ( 'NONE',  ( 125.7866681442452688, -0.4660016031367893996, -10.09054647747474043 ) ) ;
#4538=CARTESIAN_POINT ( 'NONE',  ( 119.7736414775786358, 0.1319031606808879209, -14.10382304977623669 ) ) ;
#4539=CARTESIAN_POINT ( 'NONE',  ( 128.2184548109119930, -2.475900776146301219, -7.888945235271306977 ) ) ;
#4540=CARTESIAN_POINT ( 'NONE',  ( 123.0637881442452937, -0.4660016031367893996, -10.09054647747474043 ) ) ;
#4546=CARTESIAN_POINT ( 'NONE',  ( 120.3409081442453044, -0.4660016031367893996, -10.09054647747474043 ) ) ;
#4550=CARTESIAN_POINT ( 'NONE',  ( 111.7184548109119788, -0.8288870151387760510, -10.36305467784173118 ) ) ;
#4552=CARTESIAN_POINT ( 'NONE',  ( 127.1653849502244498, -4.492243868911367066, -18.85410977821037548 ) ) ;
#4553=CARTESIAN_POINT ( 'NONE',  ( 124.7088614775786226, -9.565557343593413364, -10.61323700422348004 ) ) ;
#4555=CARTESIAN_POINT ( 'NONE',  ( 117.3343948109119737, -3.383040157471821630, -19.15922257007629170 ) ) ;
#4560=CARTESIAN_POINT ( 'NONE',  ( 112.0020881442453344, -9.565557343593413364, -10.61323700422348004 ) ) ;
#4561=CYLINDRICAL_SURFACE ( 'NONE', #23339, 4.999999999999998224 ) ;
#4565=CARTESIAN_POINT ( 'NONE',  ( 125.5030348109119558, -3.383040157471821630, -19.15922257007629170 ) ) ;
#4566=CARTESIAN_POINT ( 'NONE',  ( 124.2550481442452792, -0.1624402480850797581, -16.17319339645315424 ) ) ;
#4568=CARTESIAN_POINT ( 'NONE',  ( 122.2696148109119889, -5.574606645277164318, -18.38911715685844683 ) ) ;
#4569=CARTESIAN_POINT ( 'NONE',  ( 112.7395348109119766, -4.153390946401321671, -8.397313243818183892 ) ) ;
#4570=CARTESIAN_POINT ( 'NONE',  ( 118.0151148109119816, -10.63000616557722466, -14.87417383870573495 ) ) ;
#4571=CARTESIAN_POINT ( 'NONE',  ( 126.3063647503475693, -8.674798189681249383, -16.69767936789492069 ) ) ;
#4575=CARTESIAN_POINT ( 'NONE',  ( 126.2758031835838608, -9.794238051865816530, -12.40301975007665192 ) ) ;
#4576=CARTESIAN_POINT ( 'NONE',  ( 115.0086014775786509, -4.089484607189486809, -7.948022111789456723 ) ) ;
#4577=ORIENTED_EDGE ( 'NONE', *, *, #31338, .T. ) ;
#4578=CARTESIAN_POINT ( 'NONE',  ( 113.2500748109119968, -3.505236298600246325, -18.68346056562440793 ) ) ;
#4580=CARTESIAN_POINT ( 'NONE',  ( 119.4900081442453086, -7.643976991954101408, -18.09477374809246797 ) ) ;
#4585=CARTESIAN_POINT ( 'NONE',  ( 117.2776681442452968, -5.638512984488999180, -18.83840828888717311 ) ) ;
#4590=CARTESIAN_POINT ( 'NONE',  ( 126.2758031835833918, -7.650030489068367245, -9.206835671950464928 ) ) ;
#4591=CARTESIAN_POINT ( 'NONE',  ( 120.2841814775786276, -10.15424416112533912, -14.75197769757731336 ) ) ;
#4593=CARTESIAN_POINT ( 'NONE',  ( 115.9729548109119861, -6.344957434206662583, -7.627207830600332805 ) ) ;
#4595=CARTESIAN_POINT ( 'NONE',  ( 124.8223148109119762, -10.15424416112533912, -14.75197769757731336 ) ) ;
#4597=CARTESIAN_POINT ( 'NONE',  ( 121.0216281442452981, -7.894159318335828068, -9.358103419637847864 ) ) ;
#4598=CARTESIAN_POINT ( 'NONE',  ( 116.0864081442453113, -0.1624402480850797581, -16.17319339645315424 ) ) ;
#4603=CARTESIAN_POINT ( 'NONE',  ( 117.5613014775786525, -10.15424416112533912, -14.75197769757731336 ) ) ;
#4606=CARTESIAN_POINT ( 'NONE',  ( 116.1431348109119881, -10.30919188438810075, -12.61870101168855918 ) ) ;
#4608=CARTESIAN_POINT ( 'NONE',  ( 113.9875214775786532, -8.899110576539710493, -16.42337572283490132 ) ) ;
#4610=ORIENTED_EDGE ( 'NONE', *, *, #44845, .T. ) ;
#4611=CARTESIAN_POINT ( 'NONE',  ( 123.5176014775786228, -0.8288870151387760510, -10.36305467784173118 ) ) ;
#4612=CARTESIAN_POINT ( 'NONE',  ( 118.6391081442452986, -5.574606645277164318, -18.38911715685844683 ) ) ;
#4617=CARTESIAN_POINT ( 'NONE',  ( 112.1391434465618318, -8.920658433412334887, -16.34206577034920471 ) ) ;
#4620=FACE_OUTER_BOUND ( 'NONE', #22616, .T. ) ;
#4621=CARTESIAN_POINT ( 'NONE',  ( 113.2500748109119968, -6.344957434206662583, -7.627207830600332805 ) ) ;
#4622=CARTESIAN_POINT ( 'NONE',  ( 122.0427081442452817, -9.859900752359378018, -12.68260735090039759 ) ) ;
#4625=CARTESIAN_POINT ( 'NONE',  ( 121.5888948109119809, 0.1319031606808879209, -14.10382304977623669 ) ) ;
#4630=CARTESIAN_POINT ( 'NONE',  ( 117.2776681442452968, -5.638512984488999180, -18.83840828888717311 ) ) ;
#4631=ORIENTED_EDGE ( 'NONE', *, *, #34388, .T. ) ;
#4632=CARTESIAN_POINT ( 'NONE',  ( 117.5045748109119756, 0.5811942927096110934, -14.16772938898807510 ) ) ;
#4635=CARTESIAN_POINT ( 'NONE',  ( 117.1642148109119859, -9.261995988541697145, -16.69588392320189030 ) ) ;
#4636=CARTESIAN_POINT ( 'NONE',  ( 118.5823814775786360, -1.834011780172310813, -8.268836392978581529 ) ) ;
#4637=CARTESIAN_POINT ( 'NONE',  ( 126.5125895482211718, -10.01042591126173598, -13.31191545708816371 ) ) ;
#4640=ORIENTED_EDGE ( 'NONE', *, *, #40451, .T. ) ;
#4643=CARTESIAN_POINT ( 'NONE',  ( 121.0216281442452981, -7.894159318335828068, -9.358103419637847864 ) ) ;
#4646=CARTESIAN_POINT ( 'NONE',  ( 121.5688035400977611, -1.223627541775709426, -16.99192386690442547 ) ) ;
#4647=CARTESIAN_POINT ( 'NONE',  ( 115.4056881442453459, -2.084020599724406786, -8.691656652584148546 ) ) ;
#4649=CARTESIAN_POINT ( 'NONE',  ( 122.3263414775786373, -6.344957434206665248, -7.627207830600338134 ) ) ;
#4650=CARTESIAN_POINT ( 'NONE',  ( 119.4900081442453086, -1.834011780172310813, -8.268836392978581529 ) ) ;
#4653=CARTESIAN_POINT ( 'NONE',  ( 118.0718414775786442, -0.8288870151387760510, -10.36305467784173118 ) ) ;
#4654=CARTESIAN_POINT ( 'NONE',  ( 112.4559014775786494, -9.988377603198976828, -10.36322818467138340 ) ) ;
#4655=CARTESIAN_POINT ( 'NONE',  ( 120.1140014775786398, -1.561330072975668504, -17.79121239304076951 ) ) ;
#4656=CARTESIAN_POINT ( 'NONE',  ( 118.1852948109119836, -4.153390946401325223, -8.397313243818185668 ) ) ;
#4658=CARTESIAN_POINT ( 'NONE',  ( 123.5743281442453139, -2.084020599724406786, -8.691656652584148546 ) ) ;
#4660=ADVANCED_FACE ( 'NONE', ( #6141 ), #18761, .T. ) ;
#4661=CARTESIAN_POINT ( 'NONE',  ( 121.3619881442452879, -4.089484607189486809, -7.948022111789456723 ) ) ;
#4667=CARTESIAN_POINT ( 'NONE',  ( 118.8660148109119774, -10.30919188438810075, -12.61870101168855918 ) ) ;
#4668=DIRECTION ( 'NONE',  ( 1.000000000000000000, 0.000000000000000000, 0.000000000000000000 ) ) ;
#4669=CARTESIAN_POINT ( 'NONE',  ( 117.4478481442453131, -9.565557343593413364, -10.61323700422348004 ) ) ;
#4670=CARTESIAN_POINT ( 'NONE',  ( 124.6521348109119884, -1.561330072975668948, -17.79121239304076951 ) ) ;
#4671=CARTESIAN_POINT ( 'NONE',  ( 126.2872529661351848, -0.6579534352730314062, -10.62653152189244388 ) ) ;
#4674=CARTESIAN_POINT ( 'NONE',  ( 114.3278814775786429, 0.1319031606808879209, -14.10382304977623669 ) ) ;
#4679=CARTESIAN_POINT ( 'NONE',  ( 120.3409081442453044, -0.4660016031367893996, -10.09054647747474043 ) ) ;
#4680=CARTESIAN_POINT ( 'NONE',  ( 120.6812681442452941, 0.1319031606808879209, -14.10382304977623669 ) ) ;
#4681=CARTESIAN_POINT ( 'NONE',  ( 114.1577014775786552, -3.505236298600246325, -18.68346056562440793 ) ) ;
#4683=CARTESIAN_POINT ( 'NONE',  ( 136.7082020370380349, -9.210996569390418998, -9.790749321066718025 ) ) ;
#4684=CARTESIAN_POINT ( 'NONE',  ( 126.1837548109119211, -10.63000616557722466, -14.87417383870573495 ) ) ;
#4686=CARTESIAN_POINT ( 'NONE',  ( 120.1707281442453166, -9.565557343593413364, -10.61323700422348004 ) ) ;
#4688=CARTESIAN_POINT ( 'NONE',  ( 123.0637881442452937, -8.899110576539710493, -16.42337572283490132 ) ) ;
#4689=CARTESIAN_POINT ( 'NONE',  ( 116.4267681442453153, -6.222761293078241884, -8.102969835052219238 ) ) ;
#4693=CARTESIAN_POINT ( 'NONE',  ( 124.7655881442452852, -9.859900752359378018, -12.68260735090039759 ) ) ;
#4694=CARTESIAN_POINT ( 'NONE',  ( 123.9714148109119805, -8.899110576539710493, -16.42337572283490132 ) ) ;
#4695=DIRECTION ( 'NONE',  ( 1.000000000000000000, 0.000000000000000000, 0.000000000000000000 ) ) ;
#4699=B_SPLINE_CURVE_WITH_KNOTS ( 'NONE', 3,
 ( #33056, #34144, #20258, #1606, #19175, #15759, #44659, #5260, #2683, #6111 ),
 .UNSPECIFIED., .F., .F.,
 ( 4, 3, 3, 4 ),
 ( 0.000000000000000000, 0.0001671877560958105107, 0.0003343755126086574896, 0.0006438490228507220145 ),
 .UNSPECIFIED. ) ;
#4702=CARTESIAN_POINT ( 'NONE',  ( 118.1285681442453068, -7.893985811506177619, -18.51759400769804742 ) ) ;
#4703=CARTESIAN_POINT ( 'NONE',  ( 118.7525614775786380, -8.166667518702819706, -8.995218007635861213 ) ) ;
#4705=CARTESIAN_POINT ( 'NONE',  ( 114.0442481442453300, -1.834011780172310813, -8.268836392978581529 ) ) ;
#4711=CARTESIAN_POINT ( 'NONE',  ( 116.0296814775786345, -8.166667518702817929, -8.995218007635861213 ) ) ;
#4712=CARTESIAN_POINT ( 'NONE',  ( 121.4187148109119789, -3.505236298600246325, -18.68346056562440793 ) ) ;
#4714=CARTESIAN_POINT ( 'NONE',  ( 115.1787814775786387, -0.1624402480850797581, -16.17319339645315424 ) ) ;
#4715=CARTESIAN_POINT ( 'NONE',  ( 122.1561614775786353, -0.4660016031367893996, -10.09054647747474043 ) ) ;
#4716=EDGE_CURVE ( 'NONE', #35115, #21529, #43427, .T. ) ;
#4720=CARTESIAN_POINT ( 'NONE',  ( 116.7671281442453335, -7.643976991954077427, -18.09477374809248928 ) ) ;
#4723=ORIENTED_EDGE ( 'NONE', *, *, #29098, .F. ) ;
#4725=CARTESIAN_POINT ( 'NONE',  ( 118.9227414775786400, -10.63000616557722466, -14.87417383870573495 ) ) ;
#4728=CARTESIAN_POINT ( 'NONE',  ( 128.2184548109119930, -7.252096815532139473, -18.89748516540533529 ) ) ;
#4730=CARTESIAN_POINT ( 'NONE',  ( 115.6325948109119821, -9.565557343593413364, -10.61323700422348004 ) ) ;
#4733=CARTESIAN_POINT ( 'NONE',  ( 122.5532481442453019, 0.4262465694468514643, -12.03445270309931736 ) ) ;
#4734=CARTESIAN_POINT ( 'NONE',  ( 121.1918081442452859, 0.9020085738987244639, -11.91225656197088156 ) ) ;
#4735=CARTESIAN_POINT ( 'NONE',  ( 125.1059481442452750, -1.833838273342660141, -17.42832698103878286 ) ) ;
#4737=CARTESIAN_POINT ( 'NONE',  ( 124.0281414775786146, -7.643976991954077427, -18.09477374809248928 ) ) ;
#4738=CARTESIAN_POINT ( 'NONE',  ( 114.3278814775786429, -10.30919188438810075, -12.61870101168855918 ) ) ;
#4739=CARTESIAN_POINT ( 'NONE',  ( 117.7314814775786260, -4.089484607189486809, -7.948022111789456723 ) ) ;
#4740=CARTESIAN_POINT ( 'NONE',  ( 125.7299414775786346, -10.15424416112533912, -14.75197769757731336 ) ) ;
#4743=CARTESIAN_POINT ( 'NONE',  ( 118.8660148109119774, 0.1319031606808879209, -14.10382304977623669 ) ) ;
#4745=CARTESIAN_POINT ( 'NONE',  ( 121.4754414775786131, -8.166667518702819706, -8.995218007635861213 ) ) ;
#4748=CARTESIAN_POINT ( 'NONE',  ( 113.2500748109119968, -3.505236298600246325, -18.68346056562440793 ) ) ;
#4750=CARTESIAN_POINT ( 'NONE',  ( 125.1626748109119802, -9.988377603198980381, -10.36322818467138518 ) ) ;
#4752=CARTESIAN_POINT ( 'NONE',  ( 121.0783548109119749, -9.565557343593413364, -10.61323700422348004 ) ) ;
#4759=CARTESIAN_POINT ( 'NONE',  ( 115.0653281442453277, -6.344957434206662583, -7.627207830600332805 ) ) ;
#4761=CARTESIAN_POINT ( 'NONE',  ( 120.7379948109119709, 0.4262465694468514643, -12.03445270309931736 ) ) ;
#4762=CARTESIAN_POINT ( 'NONE',  ( 126.2202699136542066, -4.102562024790352702, -8.450529750232742998 ) ) ;
#4764=CARTESIAN_POINT ( 'NONE',  ( 111.9453614775786434, -7.894159318335828068, -9.358103419637847864 ) ) ;
#4767=CARTESIAN_POINT ( 'NONE',  ( 124.8790414775786246, -8.899110576539710493, -16.42337572283490132 ) ) ;
#4771=CARTESIAN_POINT ( 'NONE',  ( 119.8303681442453126, -10.63000616557722466, -14.87417383870573495 ) ) ;
#4772=CARTESIAN_POINT ( 'NONE',  ( 137.1886586612278052, -9.618365390465340781, -15.78023550484489235 ) ) ;
#4776=CARTESIAN_POINT ( 'NONE',  ( 124.6521348109119884, -1.561330072975668948, -17.79121239304076951 ) ) ;
#4779=CARTESIAN_POINT ( 'NONE',  ( 124.3685014775786328, 0.4262465694468514643, -12.03445270309931736 ) ) ;
#4781=CARTESIAN_POINT ( 'NONE',  ( 116.5969481442453031, 0.5811942927096154232, -14.16772938898807155 ) ) ;
#4783=CARTESIAN_POINT ( 'NONE',  ( 116.7715436525450343, -2.378957183258571639, -17.95140958770219086 ) ) ;
#4785=CARTESIAN_POINT ( 'NONE',  ( 111.4481564080329576, -2.480768857730201393, -17.81583212108824554 ) ) ;
#4786=CARTESIAN_POINT ( 'NONE',  ( 112.3991748109119868, -1.833838273342658809, -17.42832698103878286 ) ) ;
#4789=CARTESIAN_POINT ( 'NONE',  ( 112.7962614775786676, -6.222761293078241884, -8.102969835052219238 ) ) ;
#4790=CARTESIAN_POINT ( 'NONE',  ( 111.7751814775786556, -7.893985811506177619, -18.51759400769804742 ) ) ;
#4792=CARTESIAN_POINT ( 'NONE',  ( 122.8368814775786291, -7.894159318335828068, -9.358103419637847864 ) ) ;
#4793=CARTESIAN_POINT ( 'NONE',  ( 113.5337081442453240, -0.8288870151387760510, -10.36305467784173118 ) ) ;
#4794=CARTESIAN_POINT ( 'NONE',  ( 117.9583881442453048, -10.30919188438810075, -12.61870101168855918 ) ) ;
#4796=CARTESIAN_POINT ( 'NONE',  ( 117.8266488976800161, -1.244021962887374544, -16.96476564598603076 ) ) ;
#4801=CARTESIAN_POINT ( 'NONE',  ( 126.2202699136542350, -9.806684245945831435, -12.63177842929600203 ) ) ;
#4802=CARTESIAN_POINT ( 'NONE',  ( 116.3133148109119759, -7.893985811506177619, -18.51759400769804742 ) ) ;
#4804=CARTESIAN_POINT ( 'NONE',  ( 116.0864081442453113, -0.1624402480850797581, -16.17319339645315424 ) ) ;
#4807=CARTESIAN_POINT ( 'NONE',  ( 125.7866681442452688, -0.4660016031367893996, -10.09054647747474043 ) ) ;
#4808=CARTESIAN_POINT ( 'NONE',  ( 123.1772414775786189, -5.574606645277164318, -18.38911715685844683 ) ) ;
#4810=CARTESIAN_POINT ( 'NONE',  ( 116.4834948109119779, -1.561330072975668504, -17.79121239304076951 ) ) ;
#4815=CARTESIAN_POINT ( 'NONE',  ( 119.3198281442452924, -9.859900752359374465, -12.68260735090039404 ) ) ;
#4816=CARTESIAN_POINT ( 'NONE',  ( 114.7249681442453237, 0.2603800115204892296, -16.42320221600525088 ) ) ;
#4817=CARTESIAN_POINT ( 'NONE',  ( 113.5337081442453240, -9.261995988541697145, -16.69588392320189030 ) ) ;
#4818=CARTESIAN_POINT ( 'NONE',  ( 124.9357681442453014, -7.643976991954077427, -18.09477374809248928 ) ) ;
#4819=CARTESIAN_POINT ( 'NONE',  ( 123.6877814775786533, -6.222761293078241884, -8.102969835052219238 ) ) ;
#4820=CARTESIAN_POINT ( 'NONE',  ( 115.4624148109119943, -4.153390946401321671, -8.397313243818183892 ) ) ;
#4826=CARTESIAN_POINT ( 'NONE',  ( 118.6391081442452986, -5.574606645277164318, -18.38911715685844683 ) ) ;
#4829=CARTESIAN_POINT ( 'NONE',  ( 116.0864081442453113, -9.988377603198976828, -10.36322818467138340 ) ) ;
#4831=CARTESIAN_POINT ( 'NONE',  ( 113.0798948109119948, -8.899110576539710493, -16.42337572283490132 ) ) ;
#4833=ORIENTED_EDGE ( 'NONE', *, *, #23174, .T. ) ;
#4835=CARTESIAN_POINT ( 'NONE',  ( 121.6456214775786293, 0.4262465694468514643, -12.03445270309931736 ) ) ;
#4836=B_SPLINE_CURVE_WITH_KNOTS ( 'NONE', 3,
 ( #24961, #35426, #42523, #7859, #565, #4431, #777, #7397, #14700, #41855 ),
 .UNSPECIFIED., .F., .F.,
 ( 4, 2, 2, 2, 4 ),
 ( 0.000000000000000000, 0.2499999999999472644, 0.3749999999999558686, 0.4999999999999644729, 1.000000000000000000 ),
 .UNSPECIFIED. ) ;
#4837=CARTESIAN_POINT ( 'NONE',  ( 116.1431348109119881, 0.1319031606808879209, -14.10382304977623669 ) ) ;
#4840=CARTESIAN_POINT ( 'NONE',  ( 116.1998614775786649, 0.4262465694468561273, -12.03445270309934223 ) ) ;
#4846=CARTESIAN_POINT ( 'NONE',  ( 115.6893214775786447, 0.5811942927096154232, -14.16772938898807155 ) ) ;
#4847=CARTESIAN_POINT ( 'NONE',  ( 125.9001214775786224, -5.574606645277164318, -18.38911715685844683 ) ) ;
#4848=CARTESIAN_POINT ( 'NONE',  ( 115.4056881442453459, -2.084020599724406786, -8.691656652584148546 ) ) ;
#4849=( BOUNDED_SURFACE ( )  B_SPLINE_SURFACE ( 1, 2, ( 
 ( #44806, #13564, #24056, #37949, #23374, #37254, #23607, #19717, #9461, #44582, #6722, #2837, #26566, #27249, #12896, #16077, #2380, #29981, #37724, #30211, #6027, #33839, #26794, #43899, #19950, #40478, #9239, #27022, #40937, #9690, #40703, #2607, #16539, #6266, #20186, #34071, #16766, #30663, #9924, #23837, #35401, #24706, #31319, #38831, #28589, #31545, #7835, #21287, #10370, #21741, #21062, #31990, #11035, #313, #34727, #24279, #42270, #20848, #41615, #31768, #540, #14006, #27698, #34940, #7151, #27922, #3510, #38166, #7599, #38596, #14452, #42499, #25167, #31103, #3289, #3949, #17647, #21515, #6945, #14228, #28142, #17427, #3727, #39065, #24934, #17210, #94, #17872, #7373, #41832, #42053, #10811, #10592, #45028, #13786, #24494, #28357, #38379, #35172, #4177, #18094, #751, #14675, #11259, #36304, #1871, #42722, #32439, #1428, #12157, #32660, #39964, #29256, #43612, #32213, #35630, #11935, #18771, #4407, #43165, #25831, #39739, #22185, #12387, #5072, #1212, #15347, #26285, #36531, #15570, #15126, #29033, #987, #5303, #42943, #11705, #40193, #15798, #8507, #21965, #26060, #8726, #18546, #19219, #29700, #22411, #8959, #8283, #33099, #18989, #11489, #36082, #32877, #22632, #1648, #8058, #18322, #14902, #28814, #29476, #43390, #25616, #25394, #39521, #39290, #35851, #4625, #4853, #16023, #16482, #40647, #2785, #20355, #13513, #30382, #36750, #23781, #23089, #12612, #37198, #6447, #19660, #2097, #41112, #40880, #9870, #13059, #30157, #41343, #37437, #27192, #44304, #19440, #43845, #9634, #12840, #26515, #23554, #37671, #16254, #44075, #26959, #29931, #26739, #30831, #6208, #34240, #16711, #40423, #9183, #23313, #36972, #5519, #20130, #27422, #22859, #9403, #5741, #19895, #33323, #33547, #5971, #33782, #30604, #3013, #34016, #2326, #44522, #13286, #2552, #16936, #44754, #14560, #35282, #10318, #17161, #1097, #32103, #39175, #4740, #32552, #37891, #10100, #11373, #25051, #15013, #13736, #7713, #21626, #44978, #42383, #1321, #4519, #24004, #34455, #25279, #14789 ),
 ( #31049, #28703, #645, #27645, #7939, #42833, #4056, #17980, #870, #3235, #31880, #18661, #42608, #25504, #35746, #41559, #24221, #11147, #38714, #6668, #21850, #15232, #29141, #28479, #7483, #35514, #20577, #21402, #38945, #4286, #18442, #28926, #32331, #11594, #18205, #39409, #8172, #22082, #35970, #43733, #9300, #4964, #39858, #8843, #19556, #40080, #2212, #36644, #5861, #39635, #43054, #19333, #26174, #11820, #5417, #33219, #1994, #29593, #19783, #12502, #8623, #22742, #33665, #43959, #22975, #22521, #36418, #8398, #12722, #5186, #19103, #2443, #23208, #15919, #29368, #33433, #16141, #25951, #26625, #37087, #29817, #16365, #15690, #40539, #26399, #18876, #43510, #40309, #30043, #9073, #12278, #15462, #25728, #36865, #22302, #36199, #32990, #12049, #5635, #32767, #43279, #1764, #1541, #38008, #34570, #20469, #6552, #44193, #20692, #41448, #44413, #27757, #30945, #41672, #37322, #27082, #41226, #6782, #27309, #3353, #23896, #38221, #26851, #30267, #34350, #13407, #12955, #37779, #3128, #17053, #16828, #7001, #44868, #41002, #9985, #20912, #31163, #10206, #9756, #23667, #40764, #45082, #37555, #6326, #34786, #10429, #13624, #16600, #17272, #13841, #13179, #24337, #3569, #27534, #9521, #2899, #23438, #24114, #6093, #30721, #20012, #33897, #2667, #30493, #20244, #34130, #44644, #42334, #14511, #28205, #27983, #375, #17481, #1044, #22025, #600, #10649, #11095, #35233, #42555, #14960, #8123, #24996, #31379, #18388, #17706, #7211, #31830, #28872, #14286, #41887, #35692, #35462, #4468, #7660, #24768, #35918, #32051, #21798, #38891, #14064, #38441, #4237, #7428, #21124, #18155, #32276, #10873, #38659, #21575, #24555, #21349, #25453, #818, #42785, #11317, #34998, #3782, #31606, #11546, #14737, #39355, #28649, #4009, #150, #25227, #42113, #39125, #17931, #28423, #7892, #39800, #8343, #5367, #36813, #43227, #11994, #40024, #42998, #25896, #12676, #36592, #19505, #29761, #11765, #36140, #5135, #22244, #32496, #8789, #9247, #23156, #8569, #18824, #1712, #4684, #4908 ) ),
 .UNSPECIFIED., .F., .F., .F. ) 
 B_SPLINE_SURFACE_WITH_KNOTS ( ( 2, 2 ),
 ( 3, 2, 2, 2, 2, 2, 2, 2, 2, 2, 2, 2, 2, 2, 2, 2, 2, 2, 2, 2, 2, 2, 2, 2, 2, 2, 2, 2, 2, 2, 2, 2, 2, 2, 2, 2, 2, 2, 2, 2, 2, 2, 2, 2, 2, 2, 2, 2, 2, 2, 2, 2, 2, 2, 2, 2, 2, 2, 2, 2, 2, 2, 2, 2, 2, 2, 2, 2, 2, 2, 2, 2, 2, 2, 2, 2, 2, 2, 2, 2, 2, 2, 2, 2, 2, 2, 2, 2, 2, 2, 2, 2, 2, 2, 2, 2, 2, 2, 2, 2, 2, 2, 2, 2, 2, 2, 2, 2, 2, 2, 2, 2, 2, 2, 2, 2, 2, 2, 2, 2, 2, 2, 2, 2, 2, 2, 2, 2, 3 ),
 ( 0.000000000000000000, 1.000000000000000000 ),
 ( 0.000000000000000000, 0.007812500000000000000, 0.01562500000000000000, 0.02343750000000000000, 0.03125000000000000000, 0.03906250000000000000, 0.04687500000000000000, 0.05468750000000000000, 0.06250000000000000000, 0.07031250000000000000, 0.07812500000000000000, 0.08593750000000000000, 0.09375000000000000000, 0.1015625000000000000, 0.1093750000000000000, 0.1171875000000000000, 0.1250000000000000000, 0.1328125000000000000, 0.1406250000000000000, 0.1484375000000000000, 0.1562500000000000000, 0.1640625000000000000, 0.1718750000000000000, 0.1796875000000000000, 0.1875000000000000000, 0.1953125000000000000, 0.2031250000000000000, 0.2109375000000000000, 0.2187500000000000000, 0.2265625000000000000, 0.2343750000000000000, 0.2421875000000000000, 0.2500000000000000000, 0.2578125000000000000, 0.2656250000000000000, 0.2734375000000000000, 0.2812500000000000000, 0.2890625000000000000, 0.2968750000000000000, 0.3046875000000000000, 0.3125000000000000000, 0.3203125000000000000, 0.3281250000000000000, 0.3359375000000000000, 0.3437500000000000000, 0.3515625000000000000, 0.3593750000000000000, 0.3671875000000000000, 0.3750000000000000000, 0.3828125000000000000, 0.3906250000000000000, 0.3984375000000000000, 0.4062500000000000000, 0.4140625000000000000, 0.4218750000000000000, 0.4296875000000000000, 0.4375000000000000000, 0.4453125000000000000, 0.4531250000000000000, 0.4609375000000000000, 0.4687500000000000000, 0.4765625000000000000, 0.4843750000000000000, 0.4921875000000000000, 0.5000000000000000000, 0.5078125000000000000, 0.5156250000000000000, 0.5234375000000000000, 0.5312500000000000000, 0.5390625000000000000, 0.5468750000000000000, 0.5546875000000000000, 0.5625000000000000000, 0.5703125000000000000, 0.5781250000000000000, 0.5859375000000000000, 0.5937500000000000000, 0.6015625000000000000, 0.6093750000000000000, 0.6171875000000000000, 0.6250000000000000000, 0.6328125000000000000, 0.6406250000000000000, 0.6484375000000000000, 0.6562500000000000000, 0.6640625000000000000, 0.6718750000000000000, 0.6796875000000000000, 0.6875000000000000000, 0.6953125000000000000, 0.7031250000000000000, 0.7109375000000000000, 0.7187500000000000000, 0.7265625000000000000, 0.7343750000000000000, 0.7421875000000000000, 0.7500000000000000000, 0.7578125000000000000, 0.7656250000000000000, 0.7734375000000000000, 0.7812500000000000000, 0.7890625000000000000, 0.7968750000000000000, 0.8046875000000000000, 0.8125000000000000000, 0.8203125000000000000, 0.8281250000000000000, 0.8359375000000000000, 0.8437500000000000000, 0.8515625000000000000, 0.8593750000000000000, 0.8671875000000000000, 0.8750000000000000000, 0.8828125000000000000, 0.8906250000000000000, 0.8984375000000000000, 0.9062500000000000000, 0.9140625000000000000, 0.9218750000000000000, 0.9296875000000000000, 0.9375000000000000000, 0.9453125000000000000, 0.9531250000000000000, 0.9609375000000000000, 0.9687500000000000000, 0.9765625000000000000, 0.9843750000000000000, 0.9921875000000000000, 1.000000000000000000 ),
 .UNSPECIFIED. ) 
 GEOMETRIC_REPRESENTATION_ITEM ( )  RATIONAL_B_SPLINE_SURFACE ( (
 ( 1.000000000000000000, 0.9238795325112869605, 1.000000000000000000, 0.9238795325112869605, 1.000000000000000000, 0.9238795325112869605, 1.000000000000000000, 0.9238795325112869605, 1.000000000000000000, 0.9238795325112869605, 1.000000000000000000, 0.9238795325112869605, 1.000000000000000000, 0.9238795325112869605, 1.000000000000000000, 0.9238795325112869605, 1.000000000000000000, 0.9238795325112869605, 1.000000000000000000, 0.9238795325112869605, 1.000000000000000000, 0.9238795325112869605, 1.000000000000000000, 0.9238795325112869605, 1.000000000000000000, 0.9238795325112869605, 1.000000000000000000, 0.9238795325112869605, 1.000000000000000000, 0.9238795325112869605, 1.000000000000000000, 0.9238795325112869605, 1.000000000000000000, 0.9238795325112869605, 1.000000000000000000, 0.9238795325112869605, 1.000000000000000000, 0.9238795325112869605, 1.000000000000000000, 0.9238795325112869605, 1.000000000000000000, 0.9238795325112869605, 1.000000000000000000, 0.9238795325112869605, 1.000000000000000000, 0.9238795325112869605, 1.000000000000000000, 0.9238795325112869605, 1.000000000000000000, 0.9238795325112869605, 1.000000000000000000, 0.9238795325112869605, 1.000000000000000000, 0.9238795325112869605, 1.000000000000000000, 0.9238795325112869605, 1.000000000000000000, 0.9238795325112869605, 1.000000000000000000, 0.9238795325112869605, 1.000000000000000000, 0.9238795325112869605, 1.000000000000000000, 0.9238795325112869605, 1.000000000000000000, 0.9238795325112869605, 1.000000000000000000, 0.9238795325112869605, 1.000000000000000000, 0.9238795325112869605, 1.000000000000000000, 0.9238795325112869605, 1.000000000000000000, 0.9238795325112869605, 1.000000000000000000, 0.9238795325112869605, 1.000000000000000000, 0.9238795325112869605, 1.000000000000000000, 0.9238795325112869605, 1.000000000000000000, 0.9238795325112869605, 1.000000000000000000, 0.9238795325112869605, 1.000000000000000000, 0.9238795325112869605, 1.000000000000000000, 0.9238795325112869605, 1.000000000000000000, 0.9238795325112869605, 1.000000000000000000, 0.9238795325112869605, 1.000000000000000000, 0.9238795325112869605, 1.000000000000000000, 0.9238795325112869605, 1.000000000000000000, 0.9238795325112869605, 1.000000000000000000, 0.9238795325112869605, 1.000000000000000000, 0.9238795325112869605, 1.000000000000000000, 0.9238795325112869605, 1.000000000000000000, 0.9238795325112869605, 1.000000000000000000, 0.9238795325112869605, 1.000000000000000000, 0.9238795325112869605, 1.000000000000000000, 0.9238795325112869605, 1.000000000000000000, 0.9238795325112869605, 1.000000000000000000, 0.9238795325112869605, 1.000000000000000000, 0.9238795325112869605, 1.000000000000000000, 0.9238795325112869605, 1.000000000000000000, 0.9238795325112869605, 1.000000000000000000, 0.9238795325112869605, 1.000000000000000000, 0.9238795325112869605, 1.000000000000000000, 0.9238795325112869605, 1.000000000000000000, 0.9238795325112869605, 1.000000000000000000, 0.9238795325112869605, 1.000000000000000000, 0.9238795325112869605, 1.000000000000000000, 0.9238795325112869605, 1.000000000000000000, 0.9238795325112869605, 1.000000000000000000, 0.9238795325112869605, 1.000000000000000000, 0.9238795325112869605, 1.000000000000000000, 0.9238795325112869605, 1.000000000000000000, 0.9238795325112869605, 1.000000000000000000, 0.9238795325112869605, 1.000000000000000000, 0.9238795325112869605, 1.000000000000000000, 0.9238795325112869605, 1.000000000000000000, 0.9238795325112869605, 1.000000000000000000, 0.9238795325112869605, 1.000000000000000000, 0.9238795325112869605, 1.000000000000000000, 0.9238795325112869605, 1.000000000000000000, 0.9238795325112869605, 1.000000000000000000, 0.9238795325112869605, 1.000000000000000000, 0.9238795325112869605, 1.000000000000000000, 0.9238795325112869605, 1.000000000000000000, 0.9238795325112869605, 1.000000000000000000, 0.9238795325112869605, 1.000000000000000000, 0.9238795325112869605, 1.000000000000000000, 0.9238795325112869605, 1.000000000000000000, 0.9238795325112869605, 1.000000000000000000, 0.9238795325112869605, 1.000000000000000000, 0.9238795325112869605, 1.000000000000000000, 0.9238795325112869605, 1.000000000000000000, 0.9238795325112869605, 1.000000000000000000, 0.9238795325112869605, 1.000000000000000000, 0.9238795325112869605, 1.000000000000000000, 0.9238795325112869605, 1.000000000000000000, 0.9238795325112869605, 1.000000000000000000, 0.9238795325112869605, 1.000000000000000000, 0.9238795325112869605, 1.000000000000000000, 0.9238795325112869605, 1.000000000000000000, 0.9238795325112869605, 1.000000000000000000, 0.9238795325112869605, 1.000000000000000000, 0.9238795325112869605, 1.000000000000000000, 0.9238795325112869605, 1.000000000000000000, 0.9238795325112869605, 1.000000000000000000, 0.9238795325112869605, 1.000000000000000000, 0.9238795325112869605, 1.000000000000000000, 0.9238795325112869605, 1.000000000000000000, 0.9238795325112869605, 1.000000000000000000, 0.9238795325112869605, 1.000000000000000000, 0.9238795325112869605, 1.000000000000000000, 0.9238795325112869605, 1.000000000000000000, 0.9238795325112869605, 1.000000000000000000, 0.9238795325112869605, 1.000000000000000000, 0.9238795325112869605, 1.000000000000000000, 0.9238795325112869605, 1.000000000000000000, 0.9238795325112869605, 1.000000000000000000, 0.9238795325112869605, 1.000000000000000000, 0.9238795325112869605, 1.000000000000000000, 0.9238795325112869605, 1.000000000000000000, 0.9238795325112869605, 1.000000000000000000, 0.9238795325112869605, 1.000000000000000000, 0.9238795325112869605, 1.000000000000000000, 0.9238795325112869605, 1.000000000000000000, 0.9238795325112869605, 1.000000000000000000, 0.9238795325112869605, 1.000000000000000000, 0.9238795325112869605, 1.000000000000000000, 0.9238795325112869605, 1.000000000000000000),
 ( 1.000000000000000000, 0.9238795325112869605, 1.000000000000000000, 0.9238795325112869605, 1.000000000000000000, 0.9238795325112869605, 1.000000000000000000, 0.9238795325112869605, 1.000000000000000000, 0.9238795325112869605, 1.000000000000000000, 0.9238795325112869605, 1.000000000000000000, 0.9238795325112869605, 1.000000000000000000, 0.9238795325112869605, 1.000000000000000000, 0.9238795325112869605, 1.000000000000000000, 0.9238795325112869605, 1.000000000000000000, 0.9238795325112869605, 1.000000000000000000, 0.9238795325112869605, 1.000000000000000000, 0.9238795325112869605, 1.000000000000000000, 0.9238795325112869605, 1.000000000000000000, 0.9238795325112869605, 1.000000000000000000, 0.9238795325112869605, 1.000000000000000000, 0.9238795325112869605, 1.000000000000000000, 0.9238795325112869605, 1.000000000000000000, 0.9238795325112869605, 1.000000000000000000, 0.9238795325112869605, 1.000000000000000000, 0.9238795325112869605, 1.000000000000000000, 0.9238795325112869605, 1.000000000000000000, 0.9238795325112869605, 1.000000000000000000, 0.9238795325112869605, 1.000000000000000000, 0.9238795325112869605, 1.000000000000000000, 0.9238795325112869605, 1.000000000000000000, 0.9238795325112869605, 1.000000000000000000, 0.9238795325112869605, 1.000000000000000000, 0.9238795325112869605, 1.000000000000000000, 0.9238795325112869605, 1.000000000000000000, 0.9238795325112869605, 1.000000000000000000, 0.9238795325112869605, 1.000000000000000000, 0.9238795325112869605, 1.000000000000000000, 0.9238795325112869605, 1.000000000000000000, 0.9238795325112869605, 1.000000000000000000, 0.9238795325112869605, 1.000000000000000000, 0.9238795325112869605, 1.000000000000000000, 0.9238795325112869605, 1.000000000000000000, 0.9238795325112869605, 1.000000000000000000, 0.9238795325112869605, 1.000000000000000000, 0.9238795325112869605, 1.000000000000000000, 0.9238795325112869605, 1.000000000000000000, 0.9238795325112869605, 1.000000000000000000, 0.9238795325112869605, 1.000000000000000000, 0.9238795325112869605, 1.000000000000000000, 0.9238795325112869605, 1.000000000000000000, 0.9238795325112869605, 1.000000000000000000, 0.9238795325112869605, 1.000000000000000000, 0.9238795325112869605, 1.000000000000000000, 0.9238795325112869605, 1.000000000000000000, 0.9238795325112869605, 1.000000000000000000, 0.9238795325112869605, 1.000000000000000000, 0.9238795325112869605, 1.000000000000000000, 0.9238795325112869605, 1.000000000000000000, 0.9238795325112869605, 1.000000000000000000, 0.9238795325112869605, 1.000000000000000000, 0.9238795325112869605, 1.000000000000000000, 0.9238795325112869605, 1.000000000000000000, 0.9238795325112869605, 1.000000000000000000, 0.9238795325112869605, 1.000000000000000000, 0.9238795325112869605, 1.000000000000000000, 0.9238795325112869605, 1.000000000000000000, 0.9238795325112869605, 1.000000000000000000, 0.9238795325112869605, 1.000000000000000000, 0.9238795325112869605, 1.000000000000000000, 0.9238795325112869605, 1.000000000000000000, 0.9238795325112869605, 1.000000000000000000, 0.9238795325112869605, 1.000000000000000000, 0.9238795325112869605, 1.000000000000000000, 0.9238795325112869605, 1.000000000000000000, 0.9238795325112869605, 1.000000000000000000, 0.9238795325112869605, 1.000000000000000000, 0.9238795325112869605, 1.000000000000000000, 0.9238795325112869605, 1.000000000000000000, 0.9238795325112869605, 1.000000000000000000, 0.9238795325112869605, 1.000000000000000000, 0.9238795325112869605, 1.000000000000000000, 0.9238795325112869605, 1.000000000000000000, 0.9238795325112869605, 1.000000000000000000, 0.9238795325112869605, 1.000000000000000000, 0.9238795325112869605, 1.000000000000000000, 0.9238795325112869605, 1.000000000000000000, 0.9238795325112869605, 1.000000000000000000, 0.9238795325112869605, 1.000000000000000000, 0.9238795325112869605, 1.000000000000000000, 0.9238795325112869605, 1.000000000000000000, 0.9238795325112869605, 1.000000000000000000, 0.9238795325112869605, 1.000000000000000000, 0.9238795325112869605, 1.000000000000000000, 0.9238795325112869605, 1.000000000000000000, 0.9238795325112869605, 1.000000000000000000, 0.9238795325112869605, 1.000000000000000000, 0.9238795325112869605, 1.000000000000000000, 0.9238795325112869605, 1.000000000000000000, 0.9238795325112869605, 1.000000000000000000, 0.9238795325112869605, 1.000000000000000000, 0.9238795325112869605, 1.000000000000000000, 0.9238795325112869605, 1.000000000000000000, 0.9238795325112869605, 1.000000000000000000, 0.9238795325112869605, 1.000000000000000000, 0.9238795325112869605, 1.000000000000000000, 0.9238795325112869605, 1.000000000000000000, 0.9238795325112869605, 1.000000000000000000, 0.9238795325112869605, 1.000000000000000000, 0.9238795325112869605, 1.000000000000000000, 0.9238795325112869605, 1.000000000000000000, 0.9238795325112869605, 1.000000000000000000, 0.9238795325112869605, 1.000000000000000000, 0.9238795325112869605, 1.000000000000000000, 0.9238795325112869605, 1.000000000000000000, 0.9238795325112869605, 1.000000000000000000, 0.9238795325112869605, 1.000000000000000000, 0.9238795325112869605, 1.000000000000000000, 0.9238795325112869605, 1.000000000000000000, 0.9238795325112869605, 1.000000000000000000, 0.9238795325112869605, 1.000000000000000000, 0.9238795325112869605, 1.000000000000000000, 0.9238795325112869605, 1.000000000000000000, 0.9238795325112869605, 1.000000000000000000, 0.9238795325112869605, 1.000000000000000000, 0.9238795325112869605, 1.000000000000000000, 0.9238795325112869605, 1.000000000000000000, 0.9238795325112869605, 1.000000000000000000, 0.9238795325112869605, 1.000000000000000000, 0.9238795325112869605, 1.000000000000000000, 0.9238795325112869605, 1.000000000000000000, 0.9238795325112869605, 1.000000000000000000, 0.9238795325112869605, 1.000000000000000000) ) ) 
 REPRESENTATION_ITEM ( '' )  SURFACE ( )  );
#4850=CARTESIAN_POINT ( 'NONE',  ( 122.5532481442453019, 0.4262465694468514643, -12.03445270309931736 ) ) ;
#4853=CARTESIAN_POINT ( 'NONE',  ( 121.6456214775786293, 0.4262465694468514643, -12.03445270309931736 ) ) ;
#4854=CARTESIAN_POINT ( 'NONE',  ( 124.4819548109119722, -2.084020599724406786, -8.691656652584148546 ) ) ;
#4858=CARTESIAN_POINT ( 'NONE',  ( 119.2063748109119814, -1.561330072975668504, -17.79121239304076951 ) ) ;
#4859=ORIENTED_EDGE ( 'NONE', *, *, #8994, .F. ) ;
#4860=CARTESIAN_POINT ( 'NONE',  ( 121.5888948109119809, -10.30919188438810075, -12.61870101168855918 ) ) ;
#4863=CARTESIAN_POINT ( 'NONE',  ( 115.5191414775786569, -3.383040157471821630, -19.15922257007629170 ) ) ;
#4864=CARTESIAN_POINT ( 'NONE',  ( 116.4267681442453153, -3.383040157471821630, -19.15922257007629170 ) ) ;
#4872=CARTESIAN_POINT ( 'NONE',  ( 122.0427081442452817, -9.859900752359378018, -12.68260735090039759 ) ) ;
#4875=CARTESIAN_POINT ( 'NONE',  ( 116.0296814775786345, -1.833838273342658809, -17.42832698103878286 ) ) ;
#4877=CARTESIAN_POINT ( 'NONE',  ( 126.1270281442452870, -10.30919188438810075, -12.61870101168855918 ) ) ;
#4878=CARTESIAN_POINT ( 'NONE',  ( 118.3554748109119998, 0.2603800115204892296, -16.42320221600525088 ) ) ;
#4879=VERTEX_POINT ( 'NONE', #38972 ) ;
#4881=CARTESIAN_POINT ( 'NONE',  ( 120.1707281442453166, -9.565557343593413364, -10.61323700422348004 ) ) ;
#4882=CARTESIAN_POINT ( 'NONE',  ( 113.6471614775786492, -5.638512984488999180, -18.83840828888717311 ) ) ;
#4883=CARTESIAN_POINT ( 'NONE',  ( 121.7590748109119687, -7.893985811506177619, -18.51759400769804742 ) ) ;
#4884=CARTESIAN_POINT ( 'NONE',  ( 120.7379948109119709, 0.4262465694468514643, -12.03445270309931736 ) ) ;
#4886=CARTESIAN_POINT ( 'NONE',  ( 116.1230435400977825, -1.223627541775731631, -16.99192386690444323 ) ) ;
#4887=CARTESIAN_POINT ( 'NONE',  ( 119.8870948109119752, -9.261995988541697145, -16.69588392320189030 ) ) ;
#4890=CARTESIAN_POINT ( 'NONE',  ( 137.5098279454183796, -1.294660118266357296, -16.89733337109311861 ) ) ;
#4894=CARTESIAN_POINT ( 'NONE',  ( 116.4834948109119779, -7.894159318335828068, -9.358103419637847864 ) ) ;
#4895=CARTESIAN_POINT ( 'NONE',  ( 125.2194014775786286, -10.30919188438810075, -12.61870101168855918 ) ) ;
#4897=CARTESIAN_POINT ( 'NONE',  ( 115.9363194150596001, -2.423081321603731020, -17.89265170041263175 ) ) ;
#4900=CARTESIAN_POINT ( 'NONE',  ( 116.8805814775786445, -3.505236298600246325, -18.68346056562440793 ) ) ;
#4901=CARTESIAN_POINT ( 'NONE',  ( 114.6874464091100947, -0.9924539043446216624, -17.29976612834909133 ) ) ;
#4904=CARTESIAN_POINT ( 'NONE',  ( 120.4543614775786295, -4.089484607189486809, -7.948022111789456723 ) ) ;
#4905=CARTESIAN_POINT ( 'NONE',  ( 123.0070614775786169, -10.15424416112533912, -14.75197769757731336 ) ) ;
#4908=CARTESIAN_POINT ( 'NONE',  ( 126.2404814775786264, -9.261995988541697145, -16.69588392320189030 ) ) ;
#4910=CARTESIAN_POINT ( 'NONE',  ( 120.9649014775786355, -6.222761293078241884, -8.102969835052219238 ) ) ;
#4912=CARTESIAN_POINT ( 'NONE',  ( 123.2906948109119867, -1.833838273342659697, -17.42832698103878286 ) ) ;
#4913=CARTESIAN_POINT ( 'NONE',  ( 117.1074881442453233, 0.4262465694468514643, -12.03445270309931736 ) ) ;
#4914=CARTESIAN_POINT ( 'NONE',  ( 119.5240753663348556, -1.172797794773259072, -17.05961127468926719 ) ) ;
#4916=CARTESIAN_POINT ( 'NONE',  ( 122.4397948109119767, -0.1624402480850797581, -16.17319339645315424 ) ) ;
#4917=CARTESIAN_POINT ( 'NONE',  ( 124.6521348109119884, -7.894159318335828068, -9.358103419637847864 ) ) ;
#4921=B_SPLINE_CURVE_WITH_KNOTS ( 'NONE', 3,
 ( #3883, #7984, #8214, #39452, #7762, #36014, #25545, #4783, #8441, #39675 ),
 .UNSPECIFIED., .F., .F.,
 ( 4, 3, 3, 4 ),
 ( 0.000000000000000000, 0.0001671877560958109985, 0.0003343755126086545080, 0.0006438490228507220145 ),
 .UNSPECIFIED. ) ;
#4925=CARTESIAN_POINT ( 'NONE',  ( 122.6667014775786413, -7.893985811506177619, -18.51759400769804742 ) ) ;
#4926=CARTESIAN_POINT ( 'NONE',  ( 116.6536748109119941, 0.9020085738987339008, -11.91225656197089222 ) ) ;
#4928=CARTESIAN_POINT ( 'NONE',  ( 113.8740681442453138, 0.5811942927096154232, -14.16772938898807155 ) ) ;
#4932=CARTESIAN_POINT ( 'NONE',  ( 116.4267681442453153, -3.383040157471821630, -19.15922257007629170 ) ) ;
#4933=CARTESIAN_POINT ( 'NONE',  ( 126.1837548109119496, 0.4262465694468514643, -12.03445270309931736 ) ) ;
#4935=CARTESIAN_POINT ( 'NONE',  ( 115.6893214775786447, -9.859900752359374465, -12.68260735090039404 ) ) ;
#4936=CARTESIAN_POINT ( 'NONE',  ( 125.5030348109119558, -3.383040157471821630, -19.15922257007629170 ) ) ;
#4939=CARTESIAN_POINT ( 'NONE',  ( 121.1350814775786233, -9.859900752359378018, -12.68260735090039759 ) ) ;
#4942=ORIENTED_EDGE ( 'NONE', *, *, #7164, .F. ) ;
#4946=CARTESIAN_POINT ( 'NONE',  ( 119.9438214775786378, -7.893985811506177619, -18.51759400769804742 ) ) ;
#4951=CARTESIAN_POINT ( 'NONE',  ( 118.0718414775786442, -0.8288870151387760510, -10.36305467784173118 ) ) ;
#4954=CARTESIAN_POINT ( 'NONE',  ( 125.0492214775786266, -3.505236298600246325, -18.68346056562440793 ) ) ;
#4957=CARTESIAN_POINT ( 'NONE',  ( 124.2550481442452792, -0.1624402480850797581, -16.17319339645315424 ) ) ;
#4959=CARTESIAN_POINT ( 'NONE',  ( 118.2987481442453088, -7.894159318335828068, -9.358103419637847864 ) ) ;
#4960=CARTESIAN_POINT ( 'NONE',  ( 121.3052614775786111, -7.643976991954077427, -18.09477374809248928 ) ) ;
#4962=CARTESIAN_POINT ( 'NONE',  ( 113.7038881442453402, -3.383040157471821630, -19.15922257007629170 ) ) ;
#4963=CARTESIAN_POINT ( 'NONE',  ( 120.8514481442452961, -7.893985811506177619, -18.51759400769804742 ) ) ;
#4964=CARTESIAN_POINT ( 'NONE',  ( 114.0442481442453300, -1.834011780172310813, -8.268836392978581529 ) ) ;
#4968=CARTESIAN_POINT ( 'NONE',  ( 124.1415948109119540, -3.505236298600246325, -18.68346056562440793 ) ) ;
#4970=CARTESIAN_POINT ( 'NONE',  ( 121.3619881442452879, -4.089484607189486809, -7.948022111789456723 ) ) ;
#4974=CARTESIAN_POINT ( 'NONE',  ( 113.0798948109119948, -8.899110576539710493, -16.42337572283490132 ) ) ;
#4976=CARTESIAN_POINT ( 'NONE',  ( 125.2194014775786286, -10.30919188438810075, -12.61870101168855918 ) ) ;
#4978=CARTESIAN_POINT ( 'NONE',  ( 125.2761281442453054, 0.4262465694468514643, -12.03445270309931736 ) ) ;
#4984=CARTESIAN_POINT ( 'NONE',  ( 116.3700414775786527, -5.638512984488999180, -18.83840828888717311 ) ) ;
#4985=CARTESIAN_POINT ( 'NONE',  ( 125.2761281442453054, -10.63000616557722466, -14.87417383870573495 ) ) ;
#4986=CARTESIAN_POINT ( 'NONE',  ( 121.1350814775786233, -9.859900752359378018, -12.68260735090039759 ) ) ;
#4987=CARTESIAN_POINT ( 'NONE',  ( 113.5337081442453240, -0.8288870151387760510, -10.36305467784173118 ) ) ;
#4990=CARTESIAN_POINT ( 'NONE',  ( 123.8119224739651969, 0.3208234527006275094, -15.99825685930878194 ) ) ;
#4991=CARTESIAN_POINT ( 'NONE',  ( 112.0020881442453344, 0.2603800115204892296, -16.42320221600525088 ) ) ;
#4994=CARTESIAN_POINT ( 'NONE',  ( 123.0637881442452937, -0.4660016031367893996, -10.09054647747474043 ) ) ;
#4995=CARTESIAN_POINT ( 'NONE',  ( 136.8611794030194346, -9.932755188769407440, -15.66772631836134444 ) ) ;
#4996=ORIENTED_EDGE ( 'NONE', *, *, #17087, .F. ) ;
#4997=CARTESIAN_POINT ( 'NONE',  ( 114.2144281442453178, -8.166667518702817929, -8.995218007635859436 ) ) ;
#4998=CARTESIAN_POINT ( 'NONE',  ( 124.4252281442452812, -9.261995988541697145, -16.69588392320189030 ) ) ;
#5001=CARTESIAN_POINT ( 'NONE',  ( 125.1626748109119802, -0.1624402480850797581, -16.17319339645315424 ) ) ;
#5003=CARTESIAN_POINT ( 'NONE',  ( 116.8238548109119819, -4.089484607189486809, -7.948022111789456723 ) ) ;
#5007=CARTESIAN_POINT ( 'NONE',  ( 111.4630944056972623, -2.471736349583551817, -17.82786025615278191 ) ) ;
#5008=CARTESIAN_POINT ( 'NONE',  ( 115.6325948109119821, -9.565557343593413364, -10.61323700422348004 ) ) ;
#5012=CARTESIAN_POINT ( 'NONE',  ( 113.5904348109119866, -2.084020599724406786, -8.691656652584148546 ) ) ;
#5013=CARTESIAN_POINT ( 'NONE',  ( 112.1155414775786454, 0.9020085738987339008, -11.91225656197089222 ) ) ;
#5015=CARTESIAN_POINT ( 'NONE',  ( 124.8223148109119762, -10.15424416112533912, -14.75197769757731336 ) ) ;
#5016=CARTESIAN_POINT ( 'NONE',  ( 112.9664414775786412, -9.859900752359374465, -12.68260735090039404 ) ) ;
#5017=CARTESIAN_POINT ( 'NONE',  ( 118.2987481442453088, -1.561330072975668504, -17.79121239304076951 ) ) ;
#5019=CARTESIAN_POINT ( 'NONE',  ( 120.9081748109119872, -5.638512984488999180, -18.83840828888717311 ) ) ;
#5026=CARTESIAN_POINT ( 'NONE',  ( 126.4262034846940708, -9.811855180994648151, -12.14055829856050472 ) ) ;
#5027=CARTESIAN_POINT ( 'NONE',  ( 114.8951481442453115, -0.4660016031367893996, -10.09054647747474043 ) ) ;
#5030=CARTESIAN_POINT ( 'NONE',  ( 119.3198281442452924, -9.859900752359374465, -12.68260735090039404 ) ) ;
#5033=CARTESIAN_POINT ( 'NONE',  ( 122.6667014775786413, -2.084020599724391687, -8.691656652584152098 ) ) ;
#5034=CARTESIAN_POINT ( 'NONE',  ( 112.5693548109119888, -10.63000616557722466, -14.87417383870573495 ) ) ;
#5035=CARTESIAN_POINT ( 'NONE',  ( 119.8870948109119752, -9.261995988541697145, -16.69588392320189030 ) ) ;
#5039=CARTESIAN_POINT ( 'NONE',  ( 120.9649014775786497, -6.222761293078217903, -8.102969835052215686 ) ) ;
#5040=CARTESIAN_POINT ( 'NONE',  ( 119.6034614775786196, -3.505236298600246325, -18.68346056562440793 ) ) ;
#5041=CARTESIAN_POINT ( 'NONE',  ( 117.3343948109119737, -3.383040157471821630, -19.15922257007629170 ) ) ;
#5044=CARTESIAN_POINT ( 'NONE',  ( 121.9292548109119849, -7.894159318335828068, -9.358103419637847864 ) ) ;
#5045=CARTESIAN_POINT ( 'NONE',  ( 114.2144281442453178, -1.833838273342658809, -17.42832698103878286 ) ) ;
#5050=CARTESIAN_POINT ( 'NONE',  ( 117.2209414775786485, -2.084020599724406786, -8.691656652584148546 ) ) ;
#5054=CARTESIAN_POINT ( 'NONE',  ( 115.6325948109119821, 0.2603800115204892296, -16.42320221600525088 ) ) ;
#5056=CARTESIAN_POINT ( 'NONE',  ( 112.5126281442453120, 0.1319031606808879209, -14.10382304977623669 ) ) ;
#5059=CARTESIAN_POINT ( 'NONE',  ( 122.6099748109119929, -0.8288870151387760510, -10.36305467784173118 ) ) ;
#5060=CARTESIAN_POINT ( 'NONE',  ( 118.0151148109119816, 0.4262465694468514643, -12.03445270309931736 ) ) ;
#5066=CARTESIAN_POINT ( 'NONE',  ( 114.6115148109119986, -3.383040157471821630, -19.15922257007629170 ) ) ;
#5067=CARTESIAN_POINT ( 'NONE',  ( 113.5904348109119866, -7.893985811506177619, -18.51759400769804742 ) ) ;
#5068=CARTESIAN_POINT ( 'NONE',  ( 115.9162281442453235, -5.574606645277164318, -18.38911715685844683 ) ) ;
#5069=CARTESIAN_POINT ( 'NONE',  ( 121.2485348109119769, -8.899110576539710493, -16.42337572283490132 ) ) ;
#5072=CARTESIAN_POINT ( 'NONE',  ( 119.2063748109119814, -7.894159318335828068, -9.358103419637847864 ) ) ;
#5073=CARTESIAN_POINT ( 'NONE',  ( 123.6310548109119765, -4.153390946401325223, -8.397313243818185668 ) ) ;
#5079=CARTESIAN_POINT ( 'NONE',  ( 120.0005481442453146, -5.638512984488999180, -18.83840828888717311 ) ) ;
#5081=CARTESIAN_POINT ( 'NONE',  ( 122.3263414775786373, -6.344957434206665248, -7.627207830600338134 ) ) ;
#5084=CARTESIAN_POINT ( 'NONE',  ( 114.8951481442453115, -0.4660016031367893996, -10.09054647747474043 ) ) ;
#5085=CARTESIAN_POINT ( 'NONE',  ( 117.5613014775786525, 0.9020085738987339008, -11.91225656197089222 ) ) ;
#5091=CARTESIAN_POINT ( 'NONE',  ( 120.4543614775786295, -5.574606645277164318, -18.38911715685844683 ) ) ;
#5095=CARTESIAN_POINT ( 'NONE',  ( 115.0653281442453277, -3.505236298600246325, -18.68346056562440793 ) ) ;
#5098=CARTESIAN_POINT ( 'NONE',  ( 113.1366214775786432, -7.643976991954077427, -18.09477374809248928 ) ) ;
#5099=CARTESIAN_POINT ( 'NONE',  ( 119.5467348109119712, -4.089484607189486809, -7.948022111789456723 ) ) ;
#5100=ORIENTED_EDGE ( 'NONE', *, *, #41365, .F. ) ;
#5101=CARTESIAN_POINT ( 'NONE',  ( 117.0507614775786465, 0.1319031606808879209, -14.10382304977623669 ) ) ;
#5102=CARTESIAN_POINT ( 'NONE',  ( 115.8595014775786609, -1.834011780172310813, -8.268836392978581529 ) ) ;
#5103=CARTESIAN_POINT ( 'NONE',  ( 122.8936081442453059, 0.2603800115204892296, -16.42320221600525088 ) ) ;
#5104=CARTESIAN_POINT ( 'NONE',  ( 121.1350814775786233, -9.859900752359378018, -12.68260735090039759 ) ) ;
#5106=CARTESIAN_POINT ( 'NONE',  ( 125.3895814775786448, -2.084020599724406786, -8.691656652584148546 ) ) ;
#5107=CARTESIAN_POINT ( 'NONE',  ( 119.3198281442452924, 0.5811942927096110934, -14.16772938898807510 ) ) ;
#5110=CARTESIAN_POINT ( 'NONE',  ( 122.3263414775786373, -6.344957434206665248, -7.627207830600338134 ) ) ;
#5111=( BOUNDED_CURVE ( )  B_SPLINE_CURVE ( 2, ( #45144, #21633, #4062, #25287, #17987, #35061, #31886, #28036, #13901, #27808, #38492, #39181, #7267, #651, #31436, #20966, #41722 ),
 .UNSPECIFIED., .F., .T. ) 
 B_SPLINE_CURVE_WITH_KNOTS ( ( 3, 2, 2, 2, 2, 2, 2, 2, 3 ),
 ( 0.2671282416568590001, 0.2734375000000000000, 0.2812500000000000000, 0.2890625000000000000, 0.2968750000000000000, 0.3046875000000000000, 0.3125000000000000000, 0.3203125000000000000, 0.3266217583431409999 ),
 .UNSPECIFIED. ) 
 CURVE ( )  GEOMETRIC_REPRESENTATION_ITEM ( )  RATIONAL_B_SPLINE_CURVE ( ( 0.9763430640195970289, 0.9385262470928680267, 1.000000000000000000, 0.9238795325112869605, 1.000000000000000000, 0.9238795325112869605, 1.000000000000000000, 0.9238795325112869605, 1.000000000000000000, 0.9238795325112869605, 1.000000000000000000, 0.9238795325112869605, 1.000000000000000000, 0.9238795325112869605, 1.000000000000000000, 0.9385262470928680267, 0.9763430640195970289 ) ) 
 REPRESENTATION_ITEM ( '' )  );
#5119=CARTESIAN_POINT ( 'NONE',  ( 118.8092881442453290, -0.1624402480850797581, -16.17319339645315424 ) ) ;
#5120=CARTESIAN_POINT ( 'NONE',  ( 123.9714148109119805, -0.4660016031367893996, -10.09054647747474043 ) ) ;
#5125=CARTESIAN_POINT ( 'NONE',  ( 116.0296814775786345, -1.833838273342658809, -17.42832698103878286 ) ) ;
#5126=CARTESIAN_POINT ( 'NONE',  ( 126.2184548109119788, -1.295815253274133161, -16.89579513612386563 ) ) ;
#5130=CARTESIAN_POINT ( 'NONE',  ( 121.5888948109119809, -10.30919188438810075, -12.61870101168855918 ) ) ;
#5132=CARTESIAN_POINT ( 'NONE',  ( 122.8936081442453059, -9.565557343593413364, -10.61323700422348004 ) ) ;
#5135=CARTESIAN_POINT ( 'NONE',  ( 125.6732148109119862, 0.5811942927096110934, -14.16772938898807510 ) ) ;
#5137=CARTESIAN_POINT ( 'NONE',  ( 122.3830681442452857, -1.833838273342659697, -17.42832698103878286 ) ) ;
#5138=CARTESIAN_POINT ( 'NONE',  ( 123.3474214775786209, -0.1624402480850797581, -16.17319339645315424 ) ) ;
#5139=CARTESIAN_POINT ( 'NONE',  ( 116.0864081442453113, -0.1624402480850797581, -16.17319339645315424 ) ) ;
#5142=CARTESIAN_POINT ( 'NONE',  ( 125.0492214775786266, -3.505236298600246325, -18.68346056562440793 ) ) ;
#5143=CARTESIAN_POINT ( 'NONE',  ( 122.4397948109119767, -0.1624402480850797581, -16.17319339645315424 ) ) ;
#5149=CARTESIAN_POINT ( 'NONE',  ( 121.2485348109119769, -0.4660016031367893996, -10.09054647747474043 ) ) ;
#5150=CARTESIAN_POINT ( 'NONE',  ( 119.1496481442453046, -3.383040157471821630, -19.15922257007629170 ) ) ;
#5152=CARTESIAN_POINT ( 'NONE',  ( 117.4478481442453131, 0.2603800115204892296, -16.42320221600525088 ) ) ;
#5157=CARTESIAN_POINT ( 'NONE',  ( 119.2631014775786298, 0.2603800115204892296, -16.42320221600525088 ) ) ;
#5158=CARTESIAN_POINT ( 'NONE',  ( 126.1270281442452870, 0.1319031606808879209, -14.10382304977623669 ) ) ;
#5160=CARTESIAN_POINT ( 'NONE',  ( 112.3424481442453384, -3.505236298600246325, -18.68346056562440793 ) ) ;
#5161=CARTESIAN_POINT ( 'NONE',  ( 125.1059481442452750, -8.166667518702819706, -8.995218007635861213 ) ) ;
#5164=CARTESIAN_POINT ( 'NONE',  ( 119.7169148109119874, -0.1624402480850797581, -16.17319339645315424 ) ) ;
#5169=CARTESIAN_POINT ( 'NONE',  ( 123.6310548109119765, -5.638512984488999180, -18.83840828888717311 ) ) ;
#5171=CARTESIAN_POINT ( 'NONE',  ( 111.4231914802848422, -3.929494816611151631, -18.62311481910791144 ) ) ;
#5173=CARTESIAN_POINT ( 'NONE',  ( 118.4689281442453392, -10.15424416112533912, -14.75197769757731336 ) ) ;
#5176=CARTESIAN_POINT ( 'NONE',  ( 124.3685014775786328, 0.4262465694468514643, -12.03445270309931736 ) ) ;
#5178=CARTESIAN_POINT ( 'NONE',  ( 124.1415948109119540, -3.505236298600246325, -18.68346056562440793 ) ) ;
#5181=CARTESIAN_POINT ( 'NONE',  ( 122.6667014775786413, -7.893985811506177619, -18.51759400769804742 ) ) ;
#5182=CARTESIAN_POINT ( 'NONE',  ( 118.8092881442453290, -0.1624402480850797581, -16.17319339645315424 ) ) ;
#5183=CARTESIAN_POINT ( 'NONE',  ( 121.4187148109119789, -3.505236298600246325, -18.68346056562440793 ) ) ;
#5185=CARTESIAN_POINT ( 'NONE',  ( 123.4041481442452834, -10.30919188438810075, -12.61870101168855918 ) ) ;
#5186=CARTESIAN_POINT ( 'NONE',  ( 115.6325948109119821, 0.2603800115204892296, -16.42320221600525088 ) ) ;
#5188=CYLINDRICAL_SURFACE ( 'NONE', #18927, 3.499999999999998668 ) ;
#5190=CARTESIAN_POINT ( 'NONE',  ( 122.7801548109119665, -6.222761293078241884, -8.102969835052219238 ) ) ;
#5192=CARTESIAN_POINT ( 'NONE',  ( 121.3052614775786111, -1.834011780172310813, -8.268836392978581529 ) ) ;
#5196=CARTESIAN_POINT ( 'NONE',  ( 113.1933481442453058, -5.574606645277164318, -18.38911715685844683 ) ) ;
#5200=CARTESIAN_POINT ( 'NONE',  ( 125.6164881442453094, -9.565557343593413364, -10.61323700422348004 ) ) ;
#5207=CARTESIAN_POINT ( 'NONE',  ( 115.0086014775786509, -4.089484607189486809, -7.948022111789456723 ) ) ;
#5208=CARTESIAN_POINT ( 'NONE',  ( 125.3895814775786448, -7.893985811506177619, -18.51759400769804742 ) ) ;
#5210=CARTESIAN_POINT ( 'NONE',  ( 125.7299414775786346, -10.15424416112533912, -14.75197769757731336 ) ) ;
#5211=CARTESIAN_POINT ( 'NONE',  ( 116.0296814775786345, -1.833838273342658809, -17.42832698103878286 ) ) ;
#5214=B_SPLINE_CURVE_WITH_KNOTS ( 'NONE', 3,
 ( #43337, #21907, #26231, #8455, #12331, #22579, #39690, #40140, #33045, #39465, #15746, #29648, #15071, #15290, #8904, #29198, #28983, #36697, #26010, #39234, #5466, #22136, #18496, #39914, #43109, #43562, #35801, #4571, #36028, #42889, #25558 ),
 .UNSPECIFIED., .F., .F.,
 ( 4, 2, 2, 1, 1, 1, 2, 2, 2, 1, 1, 1, 2, 2, 2, 1, 2, 2, 4 ),
 ( 0.000000000000000000, 0.2499999999998858691, 0.3749999999998160916, 0.4374999999997945532, 0.4687499999997689626, 0.4843749999997562505, 0.4921874999997510325, 0.4999999999997458699, 0.6249999999996926903, 0.6874999999996759259, 0.7187499999996675992, 0.7343749999996631583, 0.7421874999996734834, 0.7499999999996838085, 0.8124999999997638556, 0.8437499999997956079, 0.8593749999998111511, 0.8749999999998266942, 1.000000000000000000 ),
 .UNSPECIFIED. ) ;
#5216=CARTESIAN_POINT ( 'NONE',  ( 115.9162281442453235, -4.089484607189486809, -7.948022111789456723 ) ) ;
#5219=CARTESIAN_POINT ( 'NONE',  ( 122.6099748109119929, -9.261995988541697145, -16.69588392320189030 ) ) ;
#5221=ORIENTED_EDGE ( 'NONE', *, *, #29199, .T. ) ;
#5223=CARTESIAN_POINT ( 'NONE',  ( 114.3278814775786429, -10.30919188438810075, -12.61870101168855918 ) ) ;
#5226=CARTESIAN_POINT ( 'NONE',  ( 112.2289948109119848, -7.643976991954077427, -18.09477374809248928 ) ) ;
#5228=CARTESIAN_POINT ( 'NONE',  ( 112.2289948109119848, -1.834011780172310813, -8.268836392978581529 ) ) ;
#5229=ORIENTED_EDGE ( 'NONE', *, *, #23105, .F. ) ;
#5230=CARTESIAN_POINT ( 'NONE',  ( 118.1852948109119836, -5.638512984488999180, -18.83840828888717311 ) ) ;
#5234=CARTESIAN_POINT ( 'NONE',  ( 136.2315975805971959, -2.595879224868264945, -7.997781276090496938 ) ) ;
#5235=CARTESIAN_POINT ( 'NONE',  ( 114.7816948109119863, -9.859900752359374465, -12.68260735090039404 ) ) ;
#5239=CARTESIAN_POINT ( 'NONE',  ( 112.5693548109119888, 0.4262465694468514643, -12.03445270309931736 ) ) ;
#5240=CARTESIAN_POINT ( 'NONE',  ( 112.2857214775786474, -4.089484607189486809, -7.948022111789456723 ) ) ;
#5242=CARTESIAN_POINT ( 'NONE',  ( 123.5743281442453139, -2.084020599724406786, -8.691656652584148546 ) ) ;
#5244=CARTESIAN_POINT ( 'NONE',  ( 124.0848681442452772, -4.089484607189486809, -7.948022111789456723 ) ) ;
#5245=CARTESIAN_POINT ( 'NONE',  ( 122.5532481442453019, -10.63000616557722466, -14.87417383870573495 ) ) ;
#5247=CARTESIAN_POINT ( 'NONE',  ( 117.5569581407225996, -1.081026697600512732, -17.18181821144401056 ) ) ;
#5252=CARTESIAN_POINT ( 'NONE',  ( 125.2194014775786286, 0.1319031606810284196, -14.10382304977525614 ) ) ;
#5253=CARTESIAN_POINT ( 'NONE',  ( 116.8238548109119819, -4.089484607189486809, -7.948022111789456723 ) ) ;
#5257=CARTESIAN_POINT ( 'NONE',  ( 113.2500748109119968, -3.505236298600246325, -18.68346056562440793 ) ) ;
#5259=B_SPLINE_CURVE_WITH_KNOTS ( 'NONE', 3,
 ( #16416, #9570, #40353, #2488, #26217, #26670, #12543, #6143, #23485, #20064 ),
 .UNSPECIFIED., .F., .F.,
 ( 4, 3, 3, 4 ),
 ( 0.000000000000000000, 0.0001671877548681254834, 0.0003343755096277680285, 0.0006463528481650619413 ),
 .UNSPECIFIED. ) ;
#5260=CARTESIAN_POINT ( 'NONE',  ( 113.1410369858783724, -2.378957183258581853, -17.95140958770220152 ) ) ;
#5261=CARTESIAN_POINT ( 'NONE',  ( 120.0572748109119772, -3.383040157471821630, -19.15922257007629170 ) ) ;
#5267=CARTESIAN_POINT ( 'NONE',  ( 120.3976348109119812, -7.643976991954077427, -18.09477374809248928 ) ) ;
#5268=CARTESIAN_POINT ( 'NONE',  ( 115.1787814775786387, -9.988377603198976828, -10.36322818467138340 ) ) ;
#5269=CARTESIAN_POINT ( 'NONE',  ( 117.2209414775786485, -7.893985811506177619, -18.51759400769804742 ) ) ;
#5270=CARTESIAN_POINT ( 'NONE',  ( 136.2916311807211400, -7.115752929798599524, -18.77480778557723440 ) ) ;
#5271=CARTESIAN_POINT ( 'NONE',  ( 122.5532481442453019, 0.4262465694468514643, -12.03445270309931736 ) ) ;
#5272=CARTESIAN_POINT ( 'NONE',  ( 120.3976348109119812, -7.643976991954077427, -18.09477374809248928 ) ) ;
#5277=CARTESIAN_POINT ( 'NONE',  ( 112.0588148109119828, 0.5811942927096154232, -14.16772938898807155 ) ) ;
#5278=B_SPLINE_CURVE_WITH_KNOTS ( 'NONE', 3,
 ( #39787, #36580, #19715, #19039 ),
 .UNSPECIFIED., .F., .F.,
 ( 4, 4 ),
 ( 0.000000000000000000, 1.568264261493034943E-06 ),
 .UNSPECIFIED. ) ;
#5279=CARTESIAN_POINT ( 'NONE',  ( 117.1642148109119859, -0.8288870151387760510, -10.36305467784173118 ) ) ;
#5282=B_SPLINE_CURVE_WITH_KNOTS ( 'NONE', 3,
 ( #11356, #21837, #856, #4728 ),
 .UNSPECIFIED., .F., .F.,
 ( 4, 4 ),
 ( 0.000000000000000000, 1.000000000000000000 ),
 .UNSPECIFIED. ) ;
#5284=CARTESIAN_POINT ( 'NONE',  ( 115.8595014775786609, -1.834011780172310813, -8.268836392978581529 ) ) ;
#5286=CARTESIAN_POINT ( 'NONE',  ( 114.1577014775786552, -3.505236298600246325, -18.68346056562440793 ) ) ;
#5290=CARTESIAN_POINT ( 'NONE',  ( 121.8158014775786171, -4.153390946401325223, -8.397313243818185668 ) ) ;
#5291=CARTESIAN_POINT ( 'NONE',  ( 120.7379948109119709, 0.4262465694468514643, -12.03445270309931736 ) ) ;
#5293=ORIENTED_EDGE ( 'NONE', *, *, #550, .T. ) ;
#5294=DIRECTION ( 'NONE',  ( 1.000000000000000000, 0.000000000000000000, 0.000000000000000000 ) ) ;
#5297=CARTESIAN_POINT ( 'NONE',  ( 115.8027748109119841, -0.4660016031367893996, -10.09054647747474043 ) ) ;
#5298=CARTESIAN_POINT ( 'NONE',  ( 115.0653281442453277, -6.344957434206662583, -7.627207830600332805 ) ) ;
#5299=CARTESIAN_POINT ( 'NONE',  ( 115.6325948109119821, -9.565557343593413364, -10.61323700422348004 ) ) ;
#5300=CARTESIAN_POINT ( 'NONE',  ( 120.3409081442453044, -8.899110576539710493, -16.42337572283490132 ) ) ;
#5303=CARTESIAN_POINT ( 'NONE',  ( 119.7169148109119874, -0.1624402480850797581, -16.17319339645315424 ) ) ;
#5310=CARTESIAN_POINT ( 'NONE',  ( 117.8449348109119938, -8.166667518702817929, -8.995218007635861213 ) ) ;
#5312=CARTESIAN_POINT ( 'NONE',  ( 122.5532481442453019, -10.63000616557722466, -14.87417383870573495 ) ) ;
#5315=CARTESIAN_POINT ( 'NONE',  ( 118.8660148109119774, -10.30919188438810075, -12.61870101168855918 ) ) ;
#5316=CARTESIAN_POINT ( 'NONE',  ( 115.9162281442453235, -4.089484607189486809, -7.948022111789456723 ) ) ;
#5322=CARTESIAN_POINT ( 'NONE',  ( 120.9081748109119872, -4.153390946401325223, -8.397313243818185668 ) ) ;
#5325=CARTESIAN_POINT ( 'NONE',  ( 116.1431348109119881, 0.1319031606808879209, -14.10382304977623669 ) ) ;
#5328=CARTESIAN_POINT ( 'NONE',  ( 111.3213681442453264, -7.643976991954077427, -18.09477374809248928 ) ) ;
#5329=CARTESIAN_POINT ( 'NONE',  ( 119.3198281442452924, 0.5811942927096110934, -14.16772938898807510 ) ) ;
#5332=CARTESIAN_POINT ( 'NONE',  ( 116.9940348109119839, -0.1624402480850797581, -16.17319339645315424 ) ) ;
#5333=CARTESIAN_POINT ( 'NONE',  ( 116.4834948109119779, -1.561330072975668504, -17.79121239304076951 ) ) ;
#5334=CARTESIAN_POINT ( 'NONE',  ( 119.9438214775786378, -7.893985811506177619, -18.51759400769804742 ) ) ;
#5336=CARTESIAN_POINT ( 'NONE',  ( 123.5743281442453139, -2.084020599724406786, -8.691656652584148546 ) ) ;
#5341=CARTESIAN_POINT ( 'NONE',  ( 120.9649014775786355, -3.383040157471821630, -19.15922257007629170 ) ) ;
#5343=CARTESIAN_POINT ( 'NONE',  ( 125.1059481442452750, -8.166667518702819706, -8.995218007635861213 ) ) ;
#5347=CARTESIAN_POINT ( 'NONE',  ( 136.0826545884683583, -0.7358842820514963634, -17.64142694063895433 ) ) ;
#5352=CARTESIAN_POINT ( 'NONE',  ( 119.0929214775786278, -4.153390946401325223, -8.397313243818185668 ) ) ;
#5353=CARTESIAN_POINT ( 'NONE',  ( 124.9357681442453014, -1.834011780172310813, -8.268836392978581529 ) ) ;
#5355=EDGE_LOOP ( 'NONE', ( #44589, #10268, #23473, #9664 ) ) ;
#5358=CARTESIAN_POINT ( 'NONE',  ( 117.6747548109119919, -7.643976991954077427, -18.09477374809248928 ) ) ;
#5363=CARTESIAN_POINT ( 'NONE',  ( 123.4041481442452834, -10.30919188438810075, -12.61870101168855918 ) ) ;
#5364=CARTESIAN_POINT ( 'NONE',  ( 121.4754414775786131, -1.833838273342659697, -17.42832698103878286 ) ) ;
#5367=CARTESIAN_POINT ( 'NONE',  ( 124.9357681442453014, -1.834011780172310813, -8.268836392978581529 ) ) ;
#5369=CARTESIAN_POINT ( 'NONE',  ( 120.7947214775786193, -0.8288870151387760510, -10.36305467784173118 ) ) ;
#5371=CARTESIAN_POINT ( 'NONE',  ( 120.1140014775786398, -7.894159318335828068, -9.358103419637847864 ) ) ;
#5380=CARTESIAN_POINT ( 'NONE',  ( 119.3765548109119834, 0.9020085738987339008, -11.91225656197089222 ) ) ;
#5381=CARTESIAN_POINT ( 'NONE',  ( 123.7445081442452874, -1.561330072975668948, -17.79121239304076951 ) ) ;
#5382=CARTESIAN_POINT ( 'NONE',  ( 151.2860562277021472, -2.520019956603805511, -15.26558354049377009 ) ) ;
#5383=CARTESIAN_POINT ( 'NONE',  ( 118.2987481442453088, -1.561330072975668504, -17.79121239304076951 ) ) ;
#5387=AXIS2_PLACEMENT_3D ( 'NONE', #43261, #26833, #26151 ) ;
#5388=CARTESIAN_POINT ( 'NONE',  ( 124.4252281442452812, -9.261995988541697145, -16.69588392320189030 ) ) ;
#5389=CARTESIAN_POINT ( 'NONE',  ( 121.5321681442453183, -9.988377603198976828, -10.36322818467138340 ) ) ;
#5390=CARTESIAN_POINT ( 'NONE',  ( 125.5597614775786326, -7.894159318335828068, -9.358103419637847864 ) ) ;
#5391=CARTESIAN_POINT ( 'NONE',  ( 115.0086014775786509, -5.574606645277164318, -18.38911715685844683 ) ) ;
#5392=CARTESIAN_POINT ( 'NONE',  ( 123.8012348109119642, 0.2603800115204892296, -16.42320221600525088 ) ) ;
#5395=CARTESIAN_POINT ( 'NONE',  ( 118.6391081442452986, -5.574606645277164318, -18.38911715685844683 ) ) ;
#5400=CARTESIAN_POINT ( 'NONE',  ( 122.3830681442452857, -8.166667518702819706, -8.995218007635861213 ) ) ;
#5404=CARTESIAN_POINT ( 'NONE',  ( 117.8449348109119938, -1.833838273342659253, -17.42832698103878286 ) ) ;
#5407=CARTESIAN_POINT ( 'NONE',  ( 123.0070614775786169, -10.15424416112533912, -14.75197769757731336 ) ) ;
#5408=CARTESIAN_POINT ( 'NONE',  ( 116.4642898793805443, -2.191907684172563986, -18.20049396185734025 ) ) ;
#5409=CARTESIAN_POINT ( 'NONE',  ( 124.9357681442453014, -7.643976991954077427, -18.09477374809248928 ) ) ;
#5410=CARTESIAN_POINT ( 'NONE',  ( 110.2184548109119788, -2.211393927326565922, -15.67656524173425403 ) ) ;
#5412=CARTESIAN_POINT ( 'NONE',  ( 122.0427081442452817, 0.5811942927096110934, -14.16772938898807510 ) ) ;
#5413=CARTESIAN_POINT ( 'NONE',  ( 116.3133148109120043, -2.084020599724406786, -8.691656652584148546 ) ) ;
#5414=CARTESIAN_POINT ( 'NONE',  ( 122.9503348109119827, -9.859900752359378018, -12.68260735090039759 ) ) ;
#5416=CARTESIAN_POINT ( 'NONE',  ( 121.4754414775786131, -8.166667518702819706, -8.995218007635861213 ) ) ;
#5417=CARTESIAN_POINT ( 'NONE',  ( 114.7816948109119863, 0.5811942927096154232, -14.16772938898807155 ) ) ;
#5419=FACE_OUTER_BOUND ( 'NONE', #6364, .T. ) ;
#5420=CARTESIAN_POINT ( 'NONE',  ( 123.5743281442453139, -2.084020599724406786, -8.691656652584148546 ) ) ;
#5421=CARTESIAN_POINT ( 'NONE',  ( 123.0070614775786169, 0.9020085738987339008, -11.91225656197089222 ) ) ;
#5425=CARTESIAN_POINT ( 'NONE',  ( 112.4559014775786778, -0.1624402480850797581, -16.17319339645315424 ) ) ;
#5429=CARTESIAN_POINT ( 'NONE',  ( 125.9568481442452850, -3.505236298600246325, -18.68346056562440793 ) ) ;
#5434=ORIENTED_EDGE ( 'NONE', *, *, #42931, .T. ) ;
#5435=CARTESIAN_POINT ( 'NONE',  ( 120.1140014775786398, -1.561330072975668504, -17.79121239304076951 ) ) ;
#5436=CARTESIAN_POINT ( 'NONE',  ( 123.9146881442452894, -10.15424416112533912, -14.75197769757731336 ) ) ;
#5437=CARTESIAN_POINT ( 'NONE',  ( 113.5904348109119866, -2.084020599724406786, -8.691656652584148546 ) ) ;
#5440=CARTESIAN_POINT ( 'NONE',  ( 116.1998614775786507, -10.63000616557722466, -14.87417383870573495 ) ) ;
#5442=CARTESIAN_POINT ( 'NONE',  ( 125.5597614775786326, -1.561330072975669392, -17.79121239304076951 ) ) ;
#5443=ORIENTED_EDGE ( 'NONE', *, *, #40728, .F. ) ;
#5444=CARTESIAN_POINT ( 'NONE',  ( 113.0231681442453322, 0.9020085738987339008, -11.91225656197089222 ) ) ;
#5445=CARTESIAN_POINT ( 'NONE',  ( 114.8384214775786489, -10.15424416112533912, -14.75197769757731336 ) ) ;
#5447=CARTESIAN_POINT ( 'NONE',  ( 126.2404814775786264, -0.8288870151387760510, -10.36305467784173118 ) ) ;
#5449=CARTESIAN_POINT ( 'NONE',  ( 120.3976348109119812, -1.834011780172310813, -8.268836392978581529 ) ) ;
#5453=LINE ( 'NONE', #19373, #38178 ) ;
#5455=CARTESIAN_POINT ( 'NONE',  ( 115.5191414775786569, -6.222761293078241884, -8.102969835052219238 ) ) ;
#5458=CARTESIAN_POINT ( 'NONE',  ( 113.0798948109119948, -8.899110576539710493, -16.42337572283490132 ) ) ;
#5459=CARTESIAN_POINT ( 'NONE',  ( 126.0135748109119902, -1.833838273342660141, -17.42832698103878286 ) ) ;
#5461=CARTESIAN_POINT ( 'NONE',  ( 112.7395348109119766, -5.638512984488999180, -18.83840828888717311 ) ) ;
#5462=CARTESIAN_POINT ( 'NONE',  ( 116.6536748109119941, -10.15424416112533912, -14.75197769757731336 ) ) ;
#5463=CARTESIAN_POINT ( 'NONE',  ( 123.5176014775786228, -9.261995988541697145, -16.69588392320189030 ) ) ;
#5464=CARTESIAN_POINT ( 'NONE',  ( 120.7947214775786193, -9.261995988541697145, -16.69588392320189030 ) ) ;
#5466=CARTESIAN_POINT ( 'NONE',  ( 126.5010429760476995, -8.564733770033562621, -16.96217817777857917 ) ) ;
#5470=CARTESIAN_POINT ( 'NONE',  ( 126.4915402333597001, -9.824595045050944719, -12.06033286554019135 ) ) ;
#5471=CARTESIAN_POINT ( 'NONE',  ( 119.3198281442452924, 0.5811942927096110934, -14.16772938898807510 ) ) ;
#5475=CARTESIAN_POINT ( 'NONE',  ( 124.6329298793804981, -2.191907684172563986, -18.20049396185734025 ) ) ;
#5476=CARTESIAN_POINT ( 'NONE',  ( 114.1577014775786552, -3.505236298600246325, -18.68346056562440793 ) ) ;
#5477=EDGE_CURVE ( 'NONE', #15102, #32667, #17093, .T. ) ;
#5478=CARTESIAN_POINT ( 'NONE',  ( 119.0929214775786278, -5.638512984488999180, -18.83840828888717311 ) ) ;
#5480=CARTESIAN_POINT ( 'NONE',  ( 119.3437409388149462, -2.287189184988710267, -18.07361239780447448 ) ) ;
#5483=CARTESIAN_POINT ( 'NONE',  ( 120.7947214775786193, -0.8288870151387742746, -10.36305467784173473 ) ) ;
#5484=CARTESIAN_POINT ( 'NONE',  ( 121.0216281442452981, -7.894159318335828068, -9.358103419637847864 ) ) ;
#5485=CARTESIAN_POINT ( 'NONE',  ( 120.2274548109119934, 0.5811942927096110934, -14.16772938898807510 ) ) ;
#5487=CARTESIAN_POINT ( 'NONE',  ( 113.8740681442453138, 0.5811942927096154232, -14.16772938898807155 ) ) ;
#5488=CARTESIAN_POINT ( 'NONE',  ( 136.4689272580752686, -7.050714571525749541, -18.72418924296322729 ) ) ;
#5489=CARTESIAN_POINT ( 'NONE',  ( 124.1415948109119540, -3.505236298600246325, -18.68346056562440793 ) ) ;
#5490=CARTESIAN_POINT ( 'NONE',  ( 118.6391081442452986, -5.574606645277164318, -18.38911715685844683 ) ) ;
#5493=CARTESIAN_POINT ( 'NONE',  ( 114.3846081442453197, -10.63000616557722466, -14.87417383870573495 ) ) ;
#5494=CARTESIAN_POINT ( 'NONE',  ( 122.6667014775786413, -2.084020599724406786, -8.691656652584148546 ) ) ;
#5497=CARTESIAN_POINT ( 'NONE',  ( 119.0929214775786278, -5.638512984488999180, -18.83840828888717311 ) ) ;
#5499=CARTESIAN_POINT ( 'NONE',  ( 116.2565881442453133, -0.8288870151387760510, -10.36305467784173118 ) ) ;
#5503=CARTESIAN_POINT ( 'NONE',  ( 120.8514481442452961, -2.084020599724406786, -8.691656652584148546 ) ) ;
#5504=CARTESIAN_POINT ( 'NONE',  ( 122.1561614775786353, -8.899110576539710493, -16.42337572283490132 ) ) ;
#5510=CARTESIAN_POINT ( 'NONE',  ( 118.2420214775786320, -3.383040157471821630, -19.15922257007629170 ) ) ;
#5512=CARTESIAN_POINT ( 'NONE',  ( 116.4834948109119779, -1.561330072975668504, -17.79121239304076951 ) ) ;
#5513=CARTESIAN_POINT ( 'NONE',  ( 115.6893214775786447, 0.5811942927096154232, -14.16772938898807155 ) ) ;
#5514=CARTESIAN_POINT ( 'NONE',  ( 116.8805814775786445, -3.505236298600246325, -18.68346056562440793 ) ) ;
#5515=CARTESIAN_POINT ( 'NONE',  ( 121.3619881442452879, -5.574606645277164318, -18.38911715685844683 ) ) ;
#5516=CARTESIAN_POINT ( 'NONE',  ( 112.6828081442453282, -7.893985811506177619, -18.51759400769804742 ) ) ;
#5519=CARTESIAN_POINT ( 'NONE',  ( 124.1983214775786166, -1.833838273342659697, -17.42832698103878286 ) ) ;
#5521=CARTESIAN_POINT ( 'NONE',  ( 113.9371133359170614, -2.311015703046748193, -18.04188382666269064 ) ) ;
#5525=CARTESIAN_POINT ( 'NONE',  ( 118.1852948109119836, -5.638512984488999180, -18.83840828888717311 ) ) ;
#5528=CARTESIAN_POINT ( 'NONE',  ( 122.6667014775786413, -7.893985811506177619, -18.51759400769804742 ) ) ;
#5531=CARTESIAN_POINT ( 'NONE',  ( 120.9649014775786355, -3.383040157471821630, -19.15922257007629170 ) ) ;
#5534=CARTESIAN_POINT ( 'NONE',  ( 116.0296814775786345, -8.166667518702817929, -8.995218007635861213 ) ) ;
#5540=CARTESIAN_POINT ( 'NONE',  ( 125.4463081442452932, -4.153390946401325223, -8.397313243818185668 ) ) ;
#5544=CARTESIAN_POINT ( 'NONE',  ( 119.6601881442453106, -1.833838273342659253, -17.42832698103878286 ) ) ;
#5547=CARTESIAN_POINT ( 'NONE',  ( 114.2711548109119803, -0.1624402480850797581, -16.17319339645315424 ) ) ;
#5548=CARTESIAN_POINT ( 'NONE',  ( 124.4819548109119722, -7.893985811506177619, -18.51759400769804742 ) ) ;
#5551=CARTESIAN_POINT ( 'NONE',  ( 120.7379948109119709, 0.4262465694468514643, -12.03445270309931736 ) ) ;
#5552=CARTESIAN_POINT ( 'NONE',  ( 113.5904348109119866, -7.893985811506177619, -18.51759400769804742 ) ) ;
#5553=CARTESIAN_POINT ( 'NONE',  ( 120.7947214775786193, -9.261995988541697145, -16.69588392320189030 ) ) ;
#5554=CARTESIAN_POINT ( 'NONE',  ( 123.4608748109119745, 0.4262465694468514643, -12.03445270309931736 ) ) ;
#5555=ORIENTED_EDGE ( 'NONE', *, *, #11905, .T. ) ;
#5558=CARTESIAN_POINT ( 'NONE',  ( 124.8790414775786246, -0.4660016031367893996, -10.09054647747474043 ) ) ;
#5560=CARTESIAN_POINT ( 'NONE',  ( 111.5482748109120053, -0.1624402480850797581, -16.17319339645315424 ) ) ;
#5563=CARTESIAN_POINT ( 'NONE',  ( 127.9028083230502375, -3.116567687765117167, -14.47105017736742205 ) ) ;
#5566=CARTESIAN_POINT ( 'NONE',  ( 120.6812681442452941, 0.1319031606808879209, -14.10382304977623669 ) ) ;
#5567=CARTESIAN_POINT ( 'NONE',  ( 125.4463081442452932, -5.638512984488999180, -18.83840828888717311 ) ) ;
#5568=CARTESIAN_POINT ( 'NONE',  ( 126.3965902706515578, -6.074779341511876041, -18.33615407855781854 ) ) ;
#5571=CARTESIAN_POINT ( 'NONE',  ( 117.9583881442453048, 0.1319031606808879209, -14.10382304977623669 ) ) ;
#5573=EDGE_CURVE ( 'NONE', #40242, #25201, #37817, .T. ) ;
#5576=CARTESIAN_POINT ( 'NONE',  ( 124.1407619144190306, -1.220279397241718966, -16.99638242193886484 ) ) ;
#5577=CARTESIAN_POINT ( 'NONE',  ( 123.1772414775786189, -4.089484607189486809, -7.948022111789456723 ) ) ;
#5578=CARTESIAN_POINT ( 'NONE',  ( 123.2339681442453241, -3.505236298600246325, -18.68346056562440793 ) ) ;
#5581=CARTESIAN_POINT ( 'NONE',  ( 126.3230600034192292, 0.06859183521943734707, -14.48755961147212368 ) ) ;
#5584=CARTESIAN_POINT ( 'NONE',  ( 122.1561614775786353, -8.899110576539710493, -16.42337572283490132 ) ) ;
#5586=CARTESIAN_POINT ( 'NONE',  ( 120.1707281442453166, -9.565557343593413364, -10.61323700422348004 ) ) ;
#5595=CARTESIAN_POINT ( 'NONE',  ( 121.9292548109119849, -1.561330072975668948, -17.79121239304076951 ) ) ;
#5596=CARTESIAN_POINT ( 'NONE',  ( 121.3619881442452879, -4.089484607189486809, -7.948022111789456723 ) ) ;
#5599=CARTESIAN_POINT ( 'NONE',  ( 115.4056881442453459, -7.893985811506177619, -18.51759400769804742 ) ) ;
#5600=CARTESIAN_POINT ( 'NONE',  ( 113.8740681442453138, 0.5811942927096154232, -14.16772938898807155 ) ) ;
#5603=CARTESIAN_POINT ( 'NONE',  ( 123.1205148109119563, -1.834011780172310813, -8.268836392978581529 ) ) ;
#5604=CARTESIAN_POINT ( 'NONE',  ( 120.2841814775786276, 0.9020085738987339008, -11.91225656197089222 ) ) ;
#5605=CARTESIAN_POINT ( 'NONE',  ( 125.7299414775786346, -10.15424416112533912, -14.75197769757731336 ) ) ;
#5606=AXIS2_PLACEMENT_3D ( 'NONE', #14939, #20888, #34766 ) ;
#5607=CARTESIAN_POINT ( 'NONE',  ( 112.1722681442453222, -8.899110576539710493, -16.42337572283490132 ) ) ;
#5608=CARTESIAN_POINT ( 'NONE',  ( 115.8027748109119841, -8.899110576539710493, -16.42337572283490132 ) ) ;
#5609=CARTESIAN_POINT ( 'NONE',  ( 124.4252281442452812, -9.261995988541697145, -16.69588392320189030 ) ) ;
#5612=CARTESIAN_POINT ( 'NONE',  ( 120.9649014775786355, -6.222761293078241884, -8.102969835052219238 ) ) ;
#5617=CARTESIAN_POINT ( 'NONE',  ( 121.0024232127138504, -2.191907684172563986, -18.20049396185734025 ) ) ;
#5618=CARTESIAN_POINT ( 'NONE',  ( 123.1772414775786189, -4.089484607189486809, -7.948022111789456723 ) ) ;
#5624=CARTESIAN_POINT ( 'NONE',  ( 122.9503348109119827, -9.859900752359378018, -12.68260735090039759 ) ) ;
#5627=CARTESIAN_POINT ( 'NONE',  ( 123.3474214775786209, -0.1624402480850797581, -16.17319339645315424 ) ) ;
#5630=CARTESIAN_POINT ( 'NONE',  ( 125.6732148109119862, 0.5811942927096110934, -14.16772938898807510 ) ) ;
#5631=CARTESIAN_POINT ( 'NONE',  ( 117.0507614775786465, 0.1319031606808879209, -14.10382304977623669 ) ) ;
#5634=CARTESIAN_POINT ( 'NONE',  ( 122.8368814775786291, -1.561330072975668948, -17.79121239304076951 ) ) ;
#5635=CARTESIAN_POINT ( 'NONE',  ( 117.2776681442452968, -5.638512984488999180, -18.83840828888717311 ) ) ;
#5637=DIRECTION ( 'NONE',  ( 1.000000000000000000, 0.000000000000000000, 0.000000000000000000 ) ) ;
#5638=CARTESIAN_POINT ( 'NONE',  ( 122.7234281442452755, -4.153390946401325223, -8.397313243818185668 ) ) ;
#5639=CARTESIAN_POINT ( 'NONE',  ( 123.1205148109119563, -1.834011780172310813, -8.268836392978581529 ) ) ;
#5643=CARTESIAN_POINT ( 'NONE',  ( 112.2289948109119848, -7.643976991954077427, -18.09477374809248928 ) ) ;
#5644=CARTESIAN_POINT ( 'NONE',  ( 117.7882081442453170, -3.505236298600246325, -18.68346056562440793 ) ) ;
#5646=CARTESIAN_POINT ( 'NONE',  ( 135.3184548109119874, -1.889072916127989776, -18.60376373290417362 ) ) ;
#5649=CARTESIAN_POINT ( 'NONE',  ( 123.6877814775786533, -6.222761293078241884, -8.102969835052219238 ) ) ;
#5653=CIRCLE ( 'NONE', #11500, 4.999999999999998224 ) ;
#5657=CARTESIAN_POINT ( 'NONE',  ( 118.6958348109119754, -6.344957434206665248, -7.627207830600338134 ) ) ;
#5658=CARTESIAN_POINT ( 'NONE',  ( 125.4463081442452932, -4.153390946401325223, -8.397313243818185668 ) ) ;
#5659=CARTESIAN_POINT ( 'NONE',  ( 114.4980614775786734, -2.084020599724406786, -8.691656652584148546 ) ) ;
#5663=CARTESIAN_POINT ( 'NONE',  ( 116.3133148109119759, -7.893985811506177619, -18.51759400769804742 ) ) ;
#5666=CARTESIAN_POINT ( 'NONE',  ( 123.1205148109119563, -1.834011780172310813, -8.268836392978581529 ) ) ;
#5670=CARTESIAN_POINT ( 'NONE',  ( 115.4624148109119943, -5.638512984488999180, -18.83840828888717311 ) ) ;
#5671=CARTESIAN_POINT ( 'NONE',  ( 114.6115148109119986, -6.222761293078241884, -8.102969835052219238 ) ) ;
#5672=CARTESIAN_POINT ( 'NONE',  ( 126.3243314201013305, -5.189031759765639684, -18.43570266033291460 ) ) ;
#5673=CARTESIAN_POINT ( 'NONE',  ( 112.0588148109119828, 0.5811942927096154232, -14.16772938898807155 ) ) ;
#5675=CARTESIAN_POINT ( 'NONE',  ( 120.1140014775786398, -1.561330072975668504, -17.79121239304076951 ) ) ;
#5677=CARTESIAN_POINT ( 'NONE',  ( 115.8935686996681937, -1.172797794773246416, -17.05961127468924587 ) ) ;
#5678=CARTESIAN_POINT ( 'NONE',  ( 112.1721994132789320, -8.900630651041904429, -16.42135045828372597 ) ) ;
#5679=CARTESIAN_POINT ( 'NONE',  ( 136.5935259641903201, -2.727577936221012855, -8.099885892359873552 ) ) ;
#5680=CARTESIAN_POINT ( 'NONE',  ( 113.7038881442453402, -6.222761293078241884, -8.102969835052219238 ) ) ;
#5683=CARTESIAN_POINT ( 'NONE',  ( 117.0507614775786465, 0.1319031606808879209, -14.10382304977623669 ) ) ;
#5684=CARTESIAN_POINT ( 'NONE',  ( 112.7962614775786676, -3.383040157471821630, -19.15922257007629170 ) ) ;
#5686=CARTESIAN_POINT ( 'NONE',  ( 125.9568481442452850, -3.505236298600246325, -18.68346056562440793 ) ) ;
#5687=CARTESIAN_POINT ( 'NONE',  ( 117.1642148109119859, -0.8288870151387760510, -10.36305467784173118 ) ) ;
#5688=CARTESIAN_POINT ( 'NONE',  ( 122.8936081442453059, 0.2603800115204892296, -16.42320221600525088 ) ) ;
#5689=CARTESIAN_POINT ( 'NONE',  ( 122.1561614775786353, -0.4660016031367893996, -10.09054647747474043 ) ) ;
#5690=ORIENTED_EDGE ( 'NONE', *, *, #18587, .F. ) ;
#5691=CARTESIAN_POINT ( 'NONE',  ( 115.0086014775786509, -4.089484607189486809, -7.948022111789456723 ) ) ;
#5698=CARTESIAN_POINT ( 'NONE',  ( 118.0151148109119816, -10.63000616557722466, -14.87417383870573495 ) ) ;
#5702=CARTESIAN_POINT ( 'NONE',  ( 120.6646509814547130, -2.395992375830759524, -17.92872468182853396 ) ) ;
#5703=CARTESIAN_POINT ( 'NONE',  ( 113.5904348109119866, -2.084020599724406786, -8.691656652584148546 ) ) ;
#5705=CARTESIAN_POINT ( 'NONE',  ( 118.3554748109119998, 0.2603800115204892296, -16.42320221600525088 ) ) ;
#5710=CARTESIAN_POINT ( 'NONE',  ( 121.9859814775786333, -9.565557343593413364, -10.61323700422348004 ) ) ;
#5711=CARTESIAN_POINT ( 'NONE',  ( 119.2063748109119814, -1.561330072975668504, -17.79121239304076951 ) ) ;
#5712=CARTESIAN_POINT ( 'NONE',  ( 113.5337081442453240, -0.8288870151387760510, -10.36305467784173118 ) ) ;
#5713=CARTESIAN_POINT ( 'NONE',  ( 116.4267681442453153, -3.383040157471821630, -19.15922257007629170 ) ) ;
#5714=CARTESIAN_POINT ( 'NONE',  ( 125.3328548109119964, -9.261995988541029234, -16.69588392320277848 ) ) ;
#5715=CARTESIAN_POINT ( 'NONE',  ( 122.6099748109119929, -0.8288870151387760510, -10.36305467784173118 ) ) ;
#5716=CARTESIAN_POINT ( 'NONE',  ( 119.8870948109119752, -0.8288870151387760510, -10.36305467784173118 ) ) ;
#5719=CARTESIAN_POINT ( 'NONE',  ( 114.4413348109119823, -9.261995988541697145, -16.69588392320189030 ) ) ;
#5720=CARTESIAN_POINT ( 'NONE',  ( 122.4397948109119767, -0.1624402480850797581, -16.17319339645315424 ) ) ;
#5723=CARTESIAN_POINT ( 'NONE',  ( 118.6958348109119754, -6.344957434206665248, -7.627207830600338134 ) ) ;
#5725=CARTESIAN_POINT ( 'NONE',  ( 115.0653281442453277, -3.505236298600246325, -18.68346056562440793 ) ) ;
#5728=CARTESIAN_POINT ( 'NONE',  ( 125.0492214775786266, -3.505236298600246325, -18.68346056562440793 ) ) ;
#5729=CARTESIAN_POINT ( 'NONE',  ( 119.7169148109119874, -0.1624402480850797581, -16.17319339645315424 ) ) ;
#5733=CARTESIAN_POINT ( 'NONE',  ( 119.6034614775786196, -6.344957434206665248, -7.627207830600338134 ) ) ;
#5735=CARTESIAN_POINT ( 'NONE',  ( 117.3911214775786505, -1.561330072975668504, -17.79121239304076951 ) ) ;
#5736=CARTESIAN_POINT ( 'NONE',  ( 116.8805814775786445, -6.344957434206662583, -7.627207830600332805 ) ) ;
#5737=CARTESIAN_POINT ( 'NONE',  ( 116.1431348109119881, 0.1319031606808879209, -14.10382304977623669 ) ) ;
#5738=CARTESIAN_POINT ( 'NONE',  ( 123.6310548109119765, -4.153390946401325223, -8.397313243818185668 ) ) ;
#5739=CARTESIAN_POINT ( 'NONE',  ( 111.9645664091100912, -0.9924539043446216624, -17.29976612834909133 ) ) ;
#5740=ORIENTED_EDGE ( 'NONE', *, *, #19748, .F. ) ;
#5741=CARTESIAN_POINT ( 'NONE',  ( 124.4819548109119722, -2.084020599724406786, -8.691656652584148546 ) ) ;
#5746=CARTESIAN_POINT ( 'NONE',  ( 120.6245414775786458, -9.988377603198976828, -10.36322818467138340 ) ) ;
#5747=B_SPLINE_CURVE_WITH_KNOTS ( 'NONE', 3,
 ( #11472, #26042, #1194, #11915, #32421, #1630, #42480, #29237, #12139, #15107 ),
 .UNSPECIFIED., .F., .F.,
 ( 4, 3, 3, 4 ),
 ( 0.000000000000000000, 0.0001671877560958109985, 0.0003343755126086570017, 0.0006438490228505480001 ),
 .UNSPECIFIED. ) ;
#5749=CARTESIAN_POINT ( 'NONE',  ( 120.5110881442453206, -6.344957434206665248, -7.627207830600338134 ) ) ;
#5750=CARTESIAN_POINT ( 'NONE',  ( 112.3991748109119868, -1.833838273342658809, -17.42832698103878286 ) ) ;
#5752=CARTESIAN_POINT ( 'NONE',  ( 118.9227414775786400, -10.63000616557722466, -14.87417383870573495 ) ) ;
#5753=CARTESIAN_POINT ( 'NONE',  ( 121.1350814775786233, 0.5811942927096110934, -14.16772938898807510 ) ) ;
#5758=ORIENTED_EDGE ( 'NONE', *, *, #21801, .T. ) ;
#5759=CARTESIAN_POINT ( 'NONE',  ( 151.2860562277021472, -4.863998795839242995, -13.39321520033831447 ) ) ;
#5760=CARTESIAN_POINT ( 'NONE',  ( 112.7395348109119766, -4.153390946401321671, -8.397313243818183892 ) ) ;
#5761=CARTESIAN_POINT ( 'NONE',  ( 124.0848681442452772, -5.574606645277164318, -18.38911715685844683 ) ) ;
#5764=CARTESIAN_POINT ( 'NONE',  ( 118.8092881442453290, -0.1624402480850797581, -16.17319339645315424 ) ) ;
#5768=CARTESIAN_POINT ( 'NONE',  ( 111.7751814775786556, -2.084020599724406786, -8.691656652584148546 ) ) ;
#5769=CARTESIAN_POINT ( 'NONE',  ( 125.2761281442453054, -10.63000616557722466, -14.87417383870573495 ) ) ;
#5772=CARTESIAN_POINT ( 'NONE',  ( 120.6812681442452941, 0.1319031606808879209, -14.10382304977623669 ) ) ;
#5773=CARTESIAN_POINT ( 'NONE',  ( 113.5337081442453240, -9.261995988541697145, -16.69588392320189030 ) ) ;
#5774=CARTESIAN_POINT ( 'NONE',  ( 125.1626748109119802, -9.988377603198980381, -10.36322818467138518 ) ) ;
#5775=CARTESIAN_POINT ( 'NONE',  ( 123.4041481442452834, 0.1319031606808879209, -14.10382304977623669 ) ) ;
#5778=( BOUNDED_SURFACE ( )  B_SPLINE_SURFACE ( 1, 2, ( 
 ( #20486, #34365, #12970, #29660, #26866, #40781, #23454, #3147, #29212, #43122, #11891, #25793, #39702, #8467, #8686, #5034, #36266, #26020, #32838, #15527, #29433, #12117, #39926, #38022, #17946, #41902, #21591, #7676, #163, #38236, #35016, #28438, #3369, #38455, #14525, #35247, #24349, #42351, #25012, #10221, #34585, #24570, #24130, #20707, #11110, #45099, #27771, #7226, #14302, #13856, #38905, #31179, #35478, #31394, #7016, #17068, #14079, #6798, #21140, #389, #44884, #38678, #10667, #3796, #17722, #30960, #13641, #41684, #20926, #17288, #31620, #28220, #42127, #31845, #27550, #7444, #10445, #17495, #10887, #34800, #3584, #27997, #24786, #21364, #4024, #614, #41462, #4926, #18840, #39818, #29554, #43015, #25913, #39598, #1506, #25691, #35707, #32732, #32513, #15426, #18623, #22708, #12011, #32951, #4252, #1728, #1061, #18169, #29331, #8359, #40038, #42570, #8804, #32066, #11333, #834, #1288, #15650, #36157, #22263, #8585, #19067, #15200, #22485, #4703, #43471, #22041, #8140, #14976, #36379, #43245, #5150, #12237, #26134, #14753, #28666, #25244, #39142, #11562, #7907, #39373, #11784, #21814, #4483, #29104, #18404, #32296, #28889, #42801, #25469, #35935, #41187, #9947, #27043, #40501, #40960, #13139, #9037, #26588, #9262, #44377, #12689, #26815, #44154, #36827, #1953, #6049, #26363, #12462, #22934, #5596, #19520, #23172, #16562, #30004, #29776, #23628, #40726, #5822, #37051, #34093, #19742, #40270, #12919, #19972, #19298, #9715, #30232, #9483, #23396, #13368, #36606, #33397, #43920, #43687, #16330, #37282, #33860, #37514, #44605, #6287, #2171, #33626, #2629, #16101, #2402, #30457, #20208, #2859, #16790, #30686, #27273, #5381, #33176, #15879, #3973, #17448, #337, #14030, #21085, #117, #10171, #7175, #6965, #24517, #38188, #42295, #31568, #7396, #23861, #21314, #20656, #37747, #3750, #27944, #14474, #17016, #28382, #6517, #30907, #20432, #20872, #35197, #10614, #41854, #14250, #38619, #34750, #28166, #24301, #17895, #41636, #27721, #34533, #42076, #38402, #34962 ),
 ( #31792, #564, #17672, #3532, #10392, #31343, #10834, #24731, #34316, #17234, #3089, #44829, #13587, #27497, #41417, #3311, #24078, #37971, #31125, #6747, #45050, #13810, #1452, #21987, #32013, #11956, #35876, #15595, #1672, #39317, #32239, #29054, #22432, #42522, #32461, #8530, #29276, #18346, #36325, #19010, #4201, #29498, #15372, #14926, #43192, #32682, #28613, #1010, #28837, #18793, #42747, #1236, #18569, #11283, #21538, #25642, #776, #14699, #25191, #39089, #7858, #11512, #36104, #4430, #18119, #25854, #15148, #5095, #21764, #32896, #25416, #8085, #11057, #4647, #35657, #42962, #39545, #38856, #39760, #11728, #8306, #22208, #24960, #7624, #4875, #35425, #5325, #23117, #33573, #26765, #44329, #6235, #19921, #19241, #43868, #2349, #1893, #36551, #33344, #2117, #40446, #9208, #33124, #16280, #44100, #12865, #33807, #23580, #36994, #2578, #30182, #40674, #19686, #29720, #9426, #26536, #23340, #12640, #16736, #5998, #26987, #43412, #40906, #40216, #12179, #37224, #16508, #34040, #15821, #2809, #26080, #43633, #39984, #5764, #9660, #30407, #13088, #37462, #20157, #8750, #22655, #12408, #26308, #16047, #29953, #8981, #22879, #36773, #5544, #19461, #3486, #34699, #3922, #10562, #31514, #37917, #21262, #20605, #38139, #286, #20820, #41584, #31291, #14197, #44548, #24247, #13312, #17402, #35142, #27670, #65, #6910, #10342, #28114, #16962, #30633, #3702, #41805, #27219, #17184, #3040, #13977, #31074, #34911, #42018, #3259, #45001, #27890, #41137, #24459, #38351, #7127, #21038, #24027, #10783, #17621, #24679, #10124, #34480, #9896, #38567, #7344, #20379, #23808, #30856, #37696, #6469, #44779, #34266, #13538, #27446, #41368, #6694, #13761, #15314, #22379, #29004, #28560, #24905, #36275, #35822, #25137, #28329, #4146, #25802, #11230, #17841, #31739, #35369, #42690, #42912, #11675, #25363, #39712, #39486, #11458, #42466, #22157, #1181, #4595, #39032, #4818, #28783, #8250, #955, #25584, #1398, #32632, #15094, #14872, #35597, #4370, #39258, #18289, #36050, #7803, #18741 ) ),
 .UNSPECIFIED., .F., .F., .F. ) 
 B_SPLINE_SURFACE_WITH_KNOTS ( ( 2, 2 ),
 ( 3, 2, 2, 2, 2, 2, 2, 2, 2, 2, 2, 2, 2, 2, 2, 2, 2, 2, 2, 2, 2, 2, 2, 2, 2, 2, 2, 2, 2, 2, 2, 2, 2, 2, 2, 2, 2, 2, 2, 2, 2, 2, 2, 2, 2, 2, 2, 2, 2, 2, 2, 2, 2, 2, 2, 2, 2, 2, 2, 2, 2, 2, 2, 2, 2, 2, 2, 2, 2, 2, 2, 2, 2, 2, 2, 2, 2, 2, 2, 2, 2, 2, 2, 2, 2, 2, 2, 2, 2, 2, 2, 2, 2, 2, 2, 2, 2, 2, 2, 2, 2, 2, 2, 2, 2, 2, 2, 2, 2, 2, 2, 2, 2, 2, 2, 2, 2, 2, 2, 2, 2, 2, 2, 2, 2, 2, 2, 2, 3 ),
 ( 0.000000000000000000, 1.000000000000000000 ),
 ( 0.000000000000000000, 0.007812500000000000000, 0.01562500000000000000, 0.02343750000000000000, 0.03125000000000000000, 0.03906250000000000000, 0.04687500000000000000, 0.05468750000000000000, 0.06250000000000000000, 0.07031250000000000000, 0.07812500000000000000, 0.08593750000000000000, 0.09375000000000000000, 0.1015625000000000000, 0.1093750000000000000, 0.1171875000000000000, 0.1250000000000000000, 0.1328125000000000000, 0.1406250000000000000, 0.1484375000000000000, 0.1562500000000000000, 0.1640625000000000000, 0.1718750000000000000, 0.1796875000000000000, 0.1875000000000000000, 0.1953125000000000000, 0.2031250000000000000, 0.2109375000000000000, 0.2187500000000000000, 0.2265625000000000000, 0.2343750000000000000, 0.2421875000000000000, 0.2500000000000000000, 0.2578125000000000000, 0.2656250000000000000, 0.2734375000000000000, 0.2812500000000000000, 0.2890625000000000000, 0.2968750000000000000, 0.3046875000000000000, 0.3125000000000000000, 0.3203125000000000000, 0.3281250000000000000, 0.3359375000000000000, 0.3437500000000000000, 0.3515625000000000000, 0.3593750000000000000, 0.3671875000000000000, 0.3750000000000000000, 0.3828125000000000000, 0.3906250000000000000, 0.3984375000000000000, 0.4062500000000000000, 0.4140625000000000000, 0.4218750000000000000, 0.4296875000000000000, 0.4375000000000000000, 0.4453125000000000000, 0.4531250000000000000, 0.4609375000000000000, 0.4687500000000000000, 0.4765625000000000000, 0.4843750000000000000, 0.4921875000000000000, 0.5000000000000000000, 0.5078125000000000000, 0.5156250000000000000, 0.5234375000000000000, 0.5312500000000000000, 0.5390625000000000000, 0.5468750000000000000, 0.5546875000000000000, 0.5625000000000000000, 0.5703125000000000000, 0.5781250000000000000, 0.5859375000000000000, 0.5937500000000000000, 0.6015625000000000000, 0.6093750000000000000, 0.6171875000000000000, 0.6250000000000000000, 0.6328125000000000000, 0.6406250000000000000, 0.6484375000000000000, 0.6562500000000000000, 0.6640625000000000000, 0.6718750000000000000, 0.6796875000000000000, 0.6875000000000000000, 0.6953125000000000000, 0.7031250000000000000, 0.7109375000000000000, 0.7187500000000000000, 0.7265625000000000000, 0.7343750000000000000, 0.7421875000000000000, 0.7500000000000000000, 0.7578125000000000000, 0.7656250000000000000, 0.7734375000000000000, 0.7812500000000000000, 0.7890625000000000000, 0.7968750000000000000, 0.8046875000000000000, 0.8125000000000000000, 0.8203125000000000000, 0.8281250000000000000, 0.8359375000000000000, 0.8437500000000000000, 0.8515625000000000000, 0.8593750000000000000, 0.8671875000000000000, 0.8750000000000000000, 0.8828125000000000000, 0.8906250000000000000, 0.8984375000000000000, 0.9062500000000000000, 0.9140625000000000000, 0.9218750000000000000, 0.9296875000000000000, 0.9375000000000000000, 0.9453125000000000000, 0.9531250000000000000, 0.9609375000000000000, 0.9687500000000000000, 0.9765625000000000000, 0.9843750000000000000, 0.9921875000000000000, 1.000000000000000000 ),
 .UNSPECIFIED. ) 
 GEOMETRIC_REPRESENTATION_ITEM ( )  RATIONAL_B_SPLINE_SURFACE ( (
 ( 1.000000000000000000, 0.9238795325112869605, 1.000000000000000000, 0.9238795325112869605, 1.000000000000000000, 0.9238795325112869605, 1.000000000000000000, 0.9238795325112869605, 1.000000000000000000, 0.9238795325112869605, 1.000000000000000000, 0.9238795325112869605, 1.000000000000000000, 0.9238795325112869605, 1.000000000000000000, 0.9238795325112869605, 1.000000000000000000, 0.9238795325112869605, 1.000000000000000000, 0.9238795325112869605, 1.000000000000000000, 0.9238795325112869605, 1.000000000000000000, 0.9238795325112869605, 1.000000000000000000, 0.9238795325112869605, 1.000000000000000000, 0.9238795325112869605, 1.000000000000000000, 0.9238795325112869605, 1.000000000000000000, 0.9238795325112869605, 1.000000000000000000, 0.9238795325112869605, 1.000000000000000000, 0.9238795325112869605, 1.000000000000000000, 0.9238795325112869605, 1.000000000000000000, 0.9238795325112869605, 1.000000000000000000, 0.9238795325112869605, 1.000000000000000000, 0.9238795325112869605, 1.000000000000000000, 0.9238795325112869605, 1.000000000000000000, 0.9238795325112869605, 1.000000000000000000, 0.9238795325112869605, 1.000000000000000000, 0.9238795325112869605, 1.000000000000000000, 0.9238795325112869605, 1.000000000000000000, 0.9238795325112869605, 1.000000000000000000, 0.9238795325112869605, 1.000000000000000000, 0.9238795325112869605, 1.000000000000000000, 0.9238795325112869605, 1.000000000000000000, 0.9238795325112869605, 1.000000000000000000, 0.9238795325112869605, 1.000000000000000000, 0.9238795325112869605, 1.000000000000000000, 0.9238795325112869605, 1.000000000000000000, 0.9238795325112869605, 1.000000000000000000, 0.9238795325112869605, 1.000000000000000000, 0.9238795325112869605, 1.000000000000000000, 0.9238795325112869605, 1.000000000000000000, 0.9238795325112869605, 1.000000000000000000, 0.9238795325112869605, 1.000000000000000000, 0.9238795325112869605, 1.000000000000000000, 0.9238795325112869605, 1.000000000000000000, 0.9238795325112869605, 1.000000000000000000, 0.9238795325112869605, 1.000000000000000000, 0.9238795325112869605, 1.000000000000000000, 0.9238795325112869605, 1.000000000000000000, 0.9238795325112869605, 1.000000000000000000, 0.9238795325112869605, 1.000000000000000000, 0.9238795325112869605, 1.000000000000000000, 0.9238795325112869605, 1.000000000000000000, 0.9238795325112869605, 1.000000000000000000, 0.9238795325112869605, 1.000000000000000000, 0.9238795325112869605, 1.000000000000000000, 0.9238795325112869605, 1.000000000000000000, 0.9238795325112869605, 1.000000000000000000, 0.9238795325112869605, 1.000000000000000000, 0.9238795325112869605, 1.000000000000000000, 0.9238795325112869605, 1.000000000000000000, 0.9238795325112869605, 1.000000000000000000, 0.9238795325112869605, 1.000000000000000000, 0.9238795325112869605, 1.000000000000000000, 0.9238795325112869605, 1.000000000000000000, 0.9238795325112869605, 1.000000000000000000, 0.9238795325112869605, 1.000000000000000000, 0.9238795325112869605, 1.000000000000000000, 0.9238795325112869605, 1.000000000000000000, 0.9238795325112869605, 1.000000000000000000, 0.9238795325112869605, 1.000000000000000000, 0.9238795325112869605, 1.000000000000000000, 0.9238795325112869605, 1.000000000000000000, 0.9238795325112869605, 1.000000000000000000, 0.9238795325112869605, 1.000000000000000000, 0.9238795325112869605, 1.000000000000000000, 0.9238795325112869605, 1.000000000000000000, 0.9238795325112869605, 1.000000000000000000, 0.9238795325112869605, 1.000000000000000000, 0.9238795325112869605, 1.000000000000000000, 0.9238795325112869605, 1.000000000000000000, 0.9238795325112869605, 1.000000000000000000, 0.9238795325112869605, 1.000000000000000000, 0.9238795325112869605, 1.000000000000000000, 0.9238795325112869605, 1.000000000000000000, 0.9238795325112869605, 1.000000000000000000, 0.9238795325112869605, 1.000000000000000000, 0.9238795325112869605, 1.000000000000000000, 0.9238795325112869605, 1.000000000000000000, 0.9238795325112869605, 1.000000000000000000, 0.9238795325112869605, 1.000000000000000000, 0.9238795325112869605, 1.000000000000000000, 0.9238795325112869605, 1.000000000000000000, 0.9238795325112869605, 1.000000000000000000, 0.9238795325112869605, 1.000000000000000000, 0.9238795325112869605, 1.000000000000000000, 0.9238795325112869605, 1.000000000000000000, 0.9238795325112869605, 1.000000000000000000, 0.9238795325112869605, 1.000000000000000000, 0.9238795325112869605, 1.000000000000000000, 0.9238795325112869605, 1.000000000000000000, 0.9238795325112869605, 1.000000000000000000, 0.9238795325112869605, 1.000000000000000000, 0.9238795325112869605, 1.000000000000000000, 0.9238795325112869605, 1.000000000000000000, 0.9238795325112869605, 1.000000000000000000, 0.9238795325112869605, 1.000000000000000000, 0.9238795325112869605, 1.000000000000000000, 0.9238795325112869605, 1.000000000000000000, 0.9238795325112869605, 1.000000000000000000, 0.9238795325112869605, 1.000000000000000000, 0.9238795325112869605, 1.000000000000000000, 0.9238795325112869605, 1.000000000000000000, 0.9238795325112869605, 1.000000000000000000, 0.9238795325112869605, 1.000000000000000000, 0.9238795325112869605, 1.000000000000000000, 0.9238795325112869605, 1.000000000000000000, 0.9238795325112869605, 1.000000000000000000, 0.9238795325112869605, 1.000000000000000000, 0.9238795325112869605, 1.000000000000000000, 0.9238795325112869605, 1.000000000000000000, 0.9238795325112869605, 1.000000000000000000, 0.9238795325112869605, 1.000000000000000000, 0.9238795325112869605, 1.000000000000000000, 0.9238795325112869605, 1.000000000000000000, 0.9238795325112869605, 1.000000000000000000, 0.9238795325112869605, 1.000000000000000000, 0.9238795325112869605, 1.000000000000000000, 0.9238795325112869605, 1.000000000000000000, 0.9238795325112869605, 1.000000000000000000),
 ( 1.000000000000000000, 0.9238795325112869605, 1.000000000000000000, 0.9238795325112869605, 1.000000000000000000, 0.9238795325112869605, 1.000000000000000000, 0.9238795325112869605, 1.000000000000000000, 0.9238795325112869605, 1.000000000000000000, 0.9238795325112869605, 1.000000000000000000, 0.9238795325112869605, 1.000000000000000000, 0.9238795325112869605, 1.000000000000000000, 0.9238795325112869605, 1.000000000000000000, 0.9238795325112869605, 1.000000000000000000, 0.9238795325112869605, 1.000000000000000000, 0.9238795325112869605, 1.000000000000000000, 0.9238795325112869605, 1.000000000000000000, 0.9238795325112869605, 1.000000000000000000, 0.9238795325112869605, 1.000000000000000000, 0.9238795325112869605, 1.000000000000000000, 0.9238795325112869605, 1.000000000000000000, 0.9238795325112869605, 1.000000000000000000, 0.9238795325112869605, 1.000000000000000000, 0.9238795325112869605, 1.000000000000000000, 0.9238795325112869605, 1.000000000000000000, 0.9238795325112869605, 1.000000000000000000, 0.9238795325112869605, 1.000000000000000000, 0.9238795325112869605, 1.000000000000000000, 0.9238795325112869605, 1.000000000000000000, 0.9238795325112869605, 1.000000000000000000, 0.9238795325112869605, 1.000000000000000000, 0.9238795325112869605, 1.000000000000000000, 0.9238795325112869605, 1.000000000000000000, 0.9238795325112869605, 1.000000000000000000, 0.9238795325112869605, 1.000000000000000000, 0.9238795325112869605, 1.000000000000000000, 0.9238795325112869605, 1.000000000000000000, 0.9238795325112869605, 1.000000000000000000, 0.9238795325112869605, 1.000000000000000000, 0.9238795325112869605, 1.000000000000000000, 0.9238795325112869605, 1.000000000000000000, 0.9238795325112869605, 1.000000000000000000, 0.9238795325112869605, 1.000000000000000000, 0.9238795325112869605, 1.000000000000000000, 0.9238795325112869605, 1.000000000000000000, 0.9238795325112869605, 1.000000000000000000, 0.9238795325112869605, 1.000000000000000000, 0.9238795325112869605, 1.000000000000000000, 0.9238795325112869605, 1.000000000000000000, 0.9238795325112869605, 1.000000000000000000, 0.9238795325112869605, 1.000000000000000000, 0.9238795325112869605, 1.000000000000000000, 0.9238795325112869605, 1.000000000000000000, 0.9238795325112869605, 1.000000000000000000, 0.9238795325112869605, 1.000000000000000000, 0.9238795325112869605, 1.000000000000000000, 0.9238795325112869605, 1.000000000000000000, 0.9238795325112869605, 1.000000000000000000, 0.9238795325112869605, 1.000000000000000000, 0.9238795325112869605, 1.000000000000000000, 0.9238795325112869605, 1.000000000000000000, 0.9238795325112869605, 1.000000000000000000, 0.9238795325112869605, 1.000000000000000000, 0.9238795325112869605, 1.000000000000000000, 0.9238795325112869605, 1.000000000000000000, 0.9238795325112869605, 1.000000000000000000, 0.9238795325112869605, 1.000000000000000000, 0.9238795325112869605, 1.000000000000000000, 0.9238795325112869605, 1.000000000000000000, 0.9238795325112869605, 1.000000000000000000, 0.9238795325112869605, 1.000000000000000000, 0.9238795325112869605, 1.000000000000000000, 0.9238795325112869605, 1.000000000000000000, 0.9238795325112869605, 1.000000000000000000, 0.9238795325112869605, 1.000000000000000000, 0.9238795325112869605, 1.000000000000000000, 0.9238795325112869605, 1.000000000000000000, 0.9238795325112869605, 1.000000000000000000, 0.9238795325112869605, 1.000000000000000000, 0.9238795325112869605, 1.000000000000000000, 0.9238795325112869605, 1.000000000000000000, 0.9238795325112869605, 1.000000000000000000, 0.9238795325112869605, 1.000000000000000000, 0.9238795325112869605, 1.000000000000000000, 0.9238795325112869605, 1.000000000000000000, 0.9238795325112869605, 1.000000000000000000, 0.9238795325112869605, 1.000000000000000000, 0.9238795325112869605, 1.000000000000000000, 0.9238795325112869605, 1.000000000000000000, 0.9238795325112869605, 1.000000000000000000, 0.9238795325112869605, 1.000000000000000000, 0.9238795325112869605, 1.000000000000000000, 0.9238795325112869605, 1.000000000000000000, 0.9238795325112869605, 1.000000000000000000, 0.9238795325112869605, 1.000000000000000000, 0.9238795325112869605, 1.000000000000000000, 0.9238795325112869605, 1.000000000000000000, 0.9238795325112869605, 1.000000000000000000, 0.9238795325112869605, 1.000000000000000000, 0.9238795325112869605, 1.000000000000000000, 0.9238795325112869605, 1.000000000000000000, 0.9238795325112869605, 1.000000000000000000, 0.9238795325112869605, 1.000000000000000000, 0.9238795325112869605, 1.000000000000000000, 0.9238795325112869605, 1.000000000000000000, 0.9238795325112869605, 1.000000000000000000, 0.9238795325112869605, 1.000000000000000000, 0.9238795325112869605, 1.000000000000000000, 0.9238795325112869605, 1.000000000000000000, 0.9238795325112869605, 1.000000000000000000, 0.9238795325112869605, 1.000000000000000000, 0.9238795325112869605, 1.000000000000000000, 0.9238795325112869605, 1.000000000000000000, 0.9238795325112869605, 1.000000000000000000, 0.9238795325112869605, 1.000000000000000000, 0.9238795325112869605, 1.000000000000000000, 0.9238795325112869605, 1.000000000000000000, 0.9238795325112869605, 1.000000000000000000, 0.9238795325112869605, 1.000000000000000000, 0.9238795325112869605, 1.000000000000000000, 0.9238795325112869605, 1.000000000000000000, 0.9238795325112869605, 1.000000000000000000, 0.9238795325112869605, 1.000000000000000000, 0.9238795325112869605, 1.000000000000000000, 0.9238795325112869605, 1.000000000000000000, 0.9238795325112869605, 1.000000000000000000, 0.9238795325112869605, 1.000000000000000000, 0.9238795325112869605, 1.000000000000000000, 0.9238795325112869605, 1.000000000000000000, 0.9238795325112869605, 1.000000000000000000, 0.9238795325112869605, 1.000000000000000000, 0.9238795325112869605, 1.000000000000000000) ) ) 
 REPRESENTATION_ITEM ( '' )  SURFACE ( )  );
#5779=CARTESIAN_POINT ( 'NONE',  ( 123.6310548109119765, -5.638512984488999180, -18.83840828888717311 ) ) ;
#5780=CARTESIAN_POINT ( 'NONE',  ( 114.1009748109119784, -5.574606645277164318, -18.38911715685844683 ) ) ;
#5781=CARTESIAN_POINT ( 'NONE',  ( 125.7866681442452688, -0.4660016031367893996, -10.09054647747474043 ) ) ;
#5792=CARTESIAN_POINT ( 'NONE',  ( 120.2841814775786276, -10.15424416112533912, -14.75197769757731336 ) ) ;
#5793=CARTESIAN_POINT ( 'NONE',  ( 115.5191414775786569, -6.222761293078241884, -8.102969835052219238 ) ) ;
#5794=CARTESIAN_POINT ( 'NONE',  ( 126.2687745536026398, -5.836013449744841708, -18.32348129158890870 ) ) ;
#5797=CARTESIAN_POINT ( 'NONE',  ( 116.4834948109119779, -7.894159318335828068, -9.358103419637847864 ) ) ;
#5801=CARTESIAN_POINT ( 'NONE',  ( 122.8176765460471813, -2.191907684172563986, -18.20049396185734025 ) ) ;
#5803=CARTESIAN_POINT ( 'NONE',  ( 122.1561614775786353, -0.4660016031367893996, -10.09054647747474043 ) ) ;
#5804=CARTESIAN_POINT ( 'NONE',  ( 124.2550481442452792, -0.1624402480850797581, -16.17319339645315424 ) ) ;
#5808=CARTESIAN_POINT ( 'NONE',  ( 126.4915402333596575, 0.09659745337240860374, -14.72609753513648201 ) ) ;
#5810=CARTESIAN_POINT ( 'NONE',  ( 124.8790414775786246, -8.899110576539710493, -16.42337572283490132 ) ) ;
#5811=CARTESIAN_POINT ( 'NONE',  ( 119.4900081442453086, -7.643976991954077427, -18.09477374809248928 ) ) ;
#5815=CARTESIAN_POINT ( 'NONE',  ( 116.8238548109119819, -4.089484607189483256, -7.948022111789462052 ) ) ;
#5817=CARTESIAN_POINT ( 'NONE',  ( 114.5547881442453217, -4.153390946401321671, -8.397313243818183892 ) ) ;
#5821=CARTESIAN_POINT ( 'NONE',  ( 120.1707281442453166, 0.2603800115204892296, -16.42320221600525088 ) ) ;
#5822=CARTESIAN_POINT ( 'NONE',  ( 121.8158014775786171, -5.638512984488999180, -18.83840828888717311 ) ) ;
#5823=CARTESIAN_POINT ( 'NONE',  ( 119.7736414775786358, 0.1319031606808853119, -14.10382304977625800 ) ) ;
#5824=CARTESIAN_POINT ( 'NONE',  ( 116.6536748109119941, 0.9020085738987339008, -11.91225656197089222 ) ) ;
#5825=CARTESIAN_POINT ( 'NONE',  ( 113.0798948109119948, -0.4660016031367893996, -10.09054647747474043 ) ) ;
#5827=CARTESIAN_POINT ( 'NONE',  ( 114.8951481442453115, -8.899110576539710493, -16.42337572283490132 ) ) ;
#5828=EDGE_CURVE ( 'NONE', #30808, #29459, #22551, .T. ) ;
#5829=CARTESIAN_POINT ( 'NONE',  ( 125.9568481442452850, -6.344957434206665248, -7.627207830600338134 ) ) ;
#5830=CARTESIAN_POINT ( 'NONE',  ( 119.7169148109119874, -9.988377603198976828, -10.36322818467138340 ) ) ;
#5832=CARTESIAN_POINT ( 'NONE',  ( 125.2194014775786286, 0.1319031606808879209, -14.10382304977623669 ) ) ;
#5833=CARTESIAN_POINT ( 'NONE',  ( 111.5482748109120053, -0.1624402480850797581, -16.17319339645315424 ) ) ;
#5835=CARTESIAN_POINT ( 'NONE',  ( 118.1285681442453068, -2.084020599724406786, -8.691656652584148546 ) ) ;
#5836=CARTESIAN_POINT ( 'NONE',  ( 125.0492214775786266, -6.344957434206665248, -7.627207830600338134 ) ) ;
#5838=CARTESIAN_POINT ( 'NONE',  ( 120.8514481442452961, -2.084020599724406786, -8.691656652584148546 ) ) ;
#5845=CARTESIAN_POINT ( 'NONE',  ( 123.1205148109119563, -1.834011780172310813, -8.268836392978581529 ) ) ;
#5848=CARTESIAN_POINT ( 'NONE',  ( 112.4559014775786494, -9.988377603198976828, -10.36322818467138340 ) ) ;
#5854=CARTESIAN_POINT ( 'NONE',  ( 125.0929224177872783, -2.472073928853079305, -17.82741071888329643 ) ) ;
#5856=( BOUNDED_CURVE ( )  B_SPLINE_CURVE ( 2, ( #42876, #467, #34876, #687, #21001, #41982, #11634, #14836, #35558, #10747, #17583, #3664, #42205, #10967, #4102, #24869, #25097 ),
 .UNSPECIFIED., .F., .T. ) 
 B_SPLINE_CURVE_WITH_KNOTS ( ( 3, 2, 2, 2, 2, 2, 2, 2, 3 ),
 ( 0.5795046674808920217, 0.5859375000000000000, 0.5937500000000000000, 0.6015625000000000000, 0.6093750000000000000, 0.6171875000000000000, 0.6250000000000000000, 0.6328125000000000000, 0.6392453325190590174 ),
 .UNSPECIFIED. ) 
 CURVE ( )  GEOMETRIC_REPRESENTATION_ITEM ( )  RATIONAL_B_SPLINE_CURVE ( ( 0.9778625265006459788, 0.9373222120152210346, 1.000000000000000000, 0.9238795325112869605, 1.000000000000000000, 0.9238795325112869605, 1.000000000000000000, 0.9238795325112869605, 1.000000000000000000, 0.9238795325112869605, 1.000000000000000000, 0.9238795325112869605, 1.000000000000000000, 0.9238795325112869605, 1.000000000000000000, 0.9373222120157009840, 0.9778625265000250311 ) ) 
 REPRESENTATION_ITEM ( '' )  );
#5857=CARTESIAN_POINT ( 'NONE',  ( 118.8660148109119774, 0.1319031606808879209, -14.10382304977623669 ) ) ;
#5858=DIRECTION ( 'NONE',  ( -1.000000000000000000, 0.000000000000000000, 0.000000000000000000 ) ) ;
#5860=CARTESIAN_POINT ( 'NONE',  ( 121.5321681442453183, -9.988377603198976828, -10.36322818467138340 ) ) ;
#5861=CARTESIAN_POINT ( 'NONE',  ( 114.4413348109119823, -9.261995988541697145, -16.69588392320189030 ) ) ;
#5863=CARTESIAN_POINT ( 'NONE',  ( 112.9664414775786412, -9.859900752359374465, -12.68260735090039404 ) ) ;
#5864=CARTESIAN_POINT ( 'NONE',  ( 124.9924948109119924, -5.574606645277164318, -18.38911715685844683 ) ) ;
#5865=CARTESIAN_POINT ( 'NONE',  ( 125.8433948109119456, -1.834011780172310813, -8.268836392978581529 ) ) ;
#5869=CARTESIAN_POINT ( 'NONE',  ( 117.5613014775786525, -10.15424416112533912, -14.75197769757731336 ) ) ;
#5871=CARTESIAN_POINT ( 'NONE',  ( 117.9583881442453048, 0.1319031606808879209, -14.10382304977623669 ) ) ;
#5876=CARTESIAN_POINT ( 'NONE',  ( 123.0070614775786311, -10.15424416112535155, -14.75197769757726185 ) ) ;
#5877=CARTESIAN_POINT ( 'NONE',  ( 126.6942948109119840, -8.899110576539710493, -16.42337572283490132 ) ) ;
#5881=CARTESIAN_POINT ( 'NONE',  ( 138.2184548109119930, -1.191816558809784876, -8.648209655763537285 ) ) ;
#5884=CARTESIAN_POINT ( 'NONE',  ( 117.1642148109119859, -9.261995988541697145, -16.69588392320189030 ) ) ;
#5885=CARTESIAN_POINT ( 'NONE',  ( 123.6877814775786533, -6.222761293078241884, -8.102969835052219238 ) ) ;
#5886=CARTESIAN_POINT ( 'NONE',  ( 113.6471614775786492, -4.153390946401321671, -8.397313243818183892 ) ) ;
#5888=CARTESIAN_POINT ( 'NONE',  ( 122.8368814775786291, -1.561330072975668948, -17.79121239304076951 ) ) ;
#5889=CARTESIAN_POINT ( 'NONE',  ( 114.4413348109119823, -9.261995988541697145, -16.69588392320189030 ) ) ;
#5890=EDGE_CURVE ( 'NONE', #8490, #25201, #43460, .T. ) ;
#5893=CARTESIAN_POINT ( 'NONE',  ( 124.9924948109119924, -4.089484607189486809, -7.948022111789456723 ) ) ;
#5896=CARTESIAN_POINT ( 'NONE',  ( 113.5337081442453240, -9.261995988541697145, -16.69588392320189030 ) ) ;
#5897=CARTESIAN_POINT ( 'NONE',  ( 113.6471614775786492, -4.153390946401321671, -8.397313243818183892 ) ) ;
#5899=CARTESIAN_POINT ( 'NONE',  ( 125.9568481442452850, -3.505236298600246325, -18.68346056562440793 ) ) ;
#5902=CARTESIAN_POINT ( 'NONE',  ( 121.5321681442453183, -9.988377603198976828, -10.36322818467138340 ) ) ;
#5904=EDGE_CURVE ( 'NONE', #39007, #39913, #15654, .T. ) ;
#5908=CARTESIAN_POINT ( 'NONE',  ( 117.7882081442453170, -3.505236298600246325, -18.68346056562440793 ) ) ;
#5909=CARTESIAN_POINT ( 'NONE',  ( 123.4801383079017967, -4.061106116276376632, -15.71137846253180292 ) ) ;
#5910=CARTESIAN_POINT ( 'NONE',  ( 115.1220548109119761, -1.833838273342658809, -17.42832698103878286 ) ) ;
#5913=CARTESIAN_POINT ( 'NONE',  ( 114.7816948109119863, -9.859900752359374465, -12.68260735090039404 ) ) ;
#5914=CARTESIAN_POINT ( 'NONE',  ( 117.1642148109119859, -9.261995988541697145, -16.69588392320189030 ) ) ;
#5916=CARTESIAN_POINT ( 'NONE',  ( 126.1837548109119496, 0.4262465694468514643, -12.03445270309931736 ) ) ;
#5917=CARTESIAN_POINT ( 'NONE',  ( 115.5191414775786569, -6.222761293078241884, -8.102969835052219238 ) ) ;
#5918=CARTESIAN_POINT ( 'NONE',  ( 124.9357681442453014, -1.834011780172310813, -8.268836392978581529 ) ) ;
#5919=CARTESIAN_POINT ( 'NONE',  ( 120.5678148109119832, -8.166667518702819706, -8.995218007635861213 ) ) ;
#5921=CARTESIAN_POINT ( 'NONE',  ( 113.3635281442453504, -9.988377603198976828, -10.36322818467138340 ) ) ;
#5927=CARTESIAN_POINT ( 'NONE',  ( 118.4689281442453392, 0.9020085738987339008, -11.91225656197089222 ) ) ;
#5928=ORIENTED_EDGE ( 'NONE', *, *, #616, .T. ) ;
#5929=CARTESIAN_POINT ( 'NONE',  ( 124.8790414775786246, -0.4660016031367893996, -10.09054647747474043 ) ) ;
#5931=CARTESIAN_POINT ( 'NONE',  ( 112.9664414775786412, -9.859900752359374465, -12.68260735090039404 ) ) ;
#5933=CARTESIAN_POINT ( 'NONE',  ( 120.2841814775786276, 0.9020085738987339008, -11.91225656197089222 ) ) ;
#5939=CARTESIAN_POINT ( 'NONE',  ( 123.5743281442453139, -2.084020599724406786, -8.691656652584148546 ) ) ;
#5940=CARTESIAN_POINT ( 'NONE',  ( 119.7736414775786358, -10.30919188438810075, -12.61870101168855918 ) ) ;
#5941=CARTESIAN_POINT ( 'NONE',  ( 114.6115148109119986, -6.222761293078241884, -8.102969835052219238 ) ) ;
#5942=CARTESIAN_POINT ( 'NONE',  ( 114.1009748109119784, -4.089484607189486809, -7.948022111789456723 ) ) ;
#5943=DIRECTION ( 'NONE',  ( 1.000000000000000000, 0.000000000000000000, 0.000000000000000000 ) ) ;
#5945=CARTESIAN_POINT ( 'NONE',  ( 120.0572748109119772, -6.222761293078241884, -8.102969835052219238 ) ) ;
#5948=CARTESIAN_POINT ( 'NONE',  ( 112.9097148109120070, 0.2603800115204892296, -16.42320221600525088 ) ) ;
#5949=CARTESIAN_POINT ( 'NONE',  ( 120.6245414775786458, -0.1624402480850797581, -16.17319339645315424 ) ) ;
#5952=CARTESIAN_POINT ( 'NONE',  ( 117.7882081442453170, -6.344957434206665248, -7.627207830600338134 ) ) ;
#5954=CARTESIAN_POINT ( 'NONE',  ( 117.6747548109119919, -7.643976991954077427, -18.09477374809248928 ) ) ;
#5957=CARTESIAN_POINT ( 'NONE',  ( 125.2761281442453054, 0.4262465694468514643, -12.03445270309931736 ) ) ;
#5959=CARTESIAN_POINT ( 'NONE',  ( 119.8870948109119752, -0.8288870151387760510, -10.36305467784173118 ) ) ;
#5962=CARTESIAN_POINT ( 'NONE',  ( 119.0929214775786278, -5.638512984488999180, -18.83840828888717311 ) ) ;
#5965=CARTESIAN_POINT ( 'NONE',  ( 118.9227414775786400, -10.63000616557722466, -14.87417383870573495 ) ) ;
#5966=CARTESIAN_POINT ( 'NONE',  ( 115.4624148109119943, -5.638512984488999180, -18.83840828888717311 ) ) ;
#5967=CARTESIAN_POINT ( 'NONE',  ( 121.1350814775786233, -9.859900752359378018, -12.68260735090039759 ) ) ;
#5968=CARTESIAN_POINT ( 'NONE',  ( 123.7445081442452874, -7.894159318335828068, -9.358103419637847864 ) ) ;
#5969=CARTESIAN_POINT ( 'NONE',  ( 112.1845001386228944, -1.125321370491271677, -17.12283323191015683 ) ) ;
#5971=CARTESIAN_POINT ( 'NONE',  ( 124.7088614775786226, -9.565557343593413364, -10.61323700422348004 ) ) ;
#5972=CARTESIAN_POINT ( 'NONE',  ( 123.6310548109119765, -5.638512984488995627, -18.83840828888717311 ) ) ;
#5977=B_SPLINE_CURVE_WITH_KNOTS ( 'NONE', 3,
 ( #32777, #28934, #11602, #25513, #22091, #39417, #1550, #15472, #33000, #16376, #30278, #44654, #26410, #5646 ),
 .UNSPECIFIED., .F., .F.,
 ( 4, 2, 2, 2, 2, 2, 4 ),
 ( 0.000000000000000000, 0.1250000000000003331, 0.2500000000000006661, 0.3750000000000009992, 0.5000000000000013323, 0.7500000000000006661, 1.000000000000000000 ),
 .UNSPECIFIED. ) ;
#5978=CARTESIAN_POINT ( 'NONE',  ( 122.6099748109119929, -9.261995988541697145, -16.69588392320189030 ) ) ;
#5979=CARTESIAN_POINT ( 'NONE',  ( 123.7445081442452874, -7.894159318335828068, -9.358103419637847864 ) ) ;
#5980=VERTEX_POINT ( 'NONE', #1085 ) ;
#5981=CARTESIAN_POINT ( 'NONE',  ( 124.8223148109119762, 0.9020085738987339008, -11.91225656197089222 ) ) ;
#5982=CARTESIAN_POINT ( 'NONE',  ( 113.6471614775786492, -4.153390946401321671, -8.397313243818183892 ) ) ;
#5984=CARTESIAN_POINT ( 'NONE',  ( 118.9794681442453026, -9.261995988541697145, -16.69588392320189030 ) ) ;
#5985=CARTESIAN_POINT ( 'NONE',  ( 119.5467348109119712, -4.089484607189486809, -7.948022111789456723 ) ) ;
#5987=CARTESIAN_POINT ( 'NONE',  ( 123.5176014775786228, -0.8288870151387760510, -10.36305467784173118 ) ) ;
#5993=FACE_OUTER_BOUND ( 'NONE', #38949, .T. ) ;
#5995=CARTESIAN_POINT ( 'NONE',  ( 122.3263414775786373, -3.505236298600246325, -18.68346056562440793 ) ) ;
#5998=CARTESIAN_POINT ( 'NONE',  ( 118.0151148109119816, 0.4262465694468514643, -12.03445270309931736 ) ) ;
#6000=CARTESIAN_POINT ( 'NONE',  ( 117.2209414775786485, -2.084020599724406786, -8.691656652584148546 ) ) ;
#6001=CARTESIAN_POINT ( 'NONE',  ( 121.7590748109119687, -7.893985811506177619, -18.51759400769804742 ) ) ;
#6003=CARTESIAN_POINT ( 'NONE',  ( 120.5678148109119832, -1.833838273342659253, -17.42832698103878286 ) ) ;
#6005=CARTESIAN_POINT ( 'NONE',  ( 118.1285681442453068, -7.893985811506177619, -18.51759400769804742 ) ) ;
#6006=CARTESIAN_POINT ( 'NONE',  ( 123.4608748109119745, -10.63000616557722466, -14.87417383870573495 ) ) ;
#6007=CARTESIAN_POINT ( 'NONE',  ( 123.9146881442452894, -10.15424416112533912, -14.75197769757731336 ) ) ;
#6010=CARTESIAN_POINT ( 'NONE',  ( 122.4397948109119767, -9.988377603198976828, -10.36322818467138340 ) ) ;
#6011=CARTESIAN_POINT ( 'NONE',  ( 115.8595014775786609, -7.643976991954077427, -18.09477374809248928 ) ) ;
#6012=CARTESIAN_POINT ( 'NONE',  ( 124.0848681442452772, -4.089484607189486809, -7.948022111789456723 ) ) ;
#6021=CARTESIAN_POINT ( 'NONE',  ( 120.0572748109119772, -6.222761293078241884, -8.102969835052219238 ) ) ;
#6022=CARTESIAN_POINT ( 'NONE',  ( 115.7460481442453357, -10.15424416112533912, -14.75197769757731336 ) ) ;
#6023=CARTESIAN_POINT ( 'NONE',  ( 126.4915402333614480, -0.4138374118321233586, -10.82803409125247107 ) ) ;
#6026=CARTESIAN_POINT ( 'NONE',  ( 118.1852948109119836, -4.153390946401325223, -8.397313243818185668 ) ) ;
#6027=CARTESIAN_POINT ( 'NONE',  ( 113.3068014775786594, -1.833838273342658809, -17.42832698103878286 ) ) ;
#6028=CIRCLE ( 'NONE', #41288, 4.999999999999998224 ) ;
#6030=CARTESIAN_POINT ( 'NONE',  ( 111.3886348109119808, -3.517672760959766887, -18.63504008191830508 ) ) ;
#6032=CARTESIAN_POINT ( 'NONE',  ( 121.6456214775786293, -10.63000616557722466, -14.87417383870573495 ) ) ;
#6033=CARTESIAN_POINT ( 'NONE',  ( 112.7395348109119766, -5.638512984488999180, -18.83840828888717311 ) ) ;
#6038=CARTESIAN_POINT ( 'NONE',  ( 126.3539348109119800, -4.153390946401325223, -8.397313243818185668 ) ) ;
#6039=CARTESIAN_POINT ( 'NONE',  ( 119.3198281442452924, -9.859900752359374465, -12.68260735090039404 ) ) ;
#6042=CARTESIAN_POINT ( 'NONE',  ( 116.9940348109119697, -9.988377603198960841, -10.36322818467135853 ) ) ;
#6044=CARTESIAN_POINT ( 'NONE',  ( 114.7249681442453237, -9.565557343593413364, -10.61323700422348004 ) ) ;
#6048=CARTESIAN_POINT ( 'NONE',  ( 124.9357681442453014, -1.834011780172310813, -8.268836392978581529 ) ) ;
#6049=CARTESIAN_POINT ( 'NONE',  ( 121.1350814775786233, 0.5811942927096110934, -14.16772938898807510 ) ) ;
#6051=( BOUNDED_CURVE ( )  B_SPLINE_CURVE ( 2, ( #19908, #34028, #26971, #13297, #2796, #16723, #44535, #41123, #9882, #17826, #941, #28769, #21024, #31500, #31277, #3908, #14406 ),
 .UNSPECIFIED., .F., .T. ) 
 B_SPLINE_CURVE_WITH_KNOTS ( ( 3, 2, 2, 2, 2, 2, 2, 2, 3 ),
 ( 0.7046282416568590001, 0.7109375000000000000, 0.7187500000000000000, 0.7265625000000000000, 0.7343750000000000000, 0.7421875000000000000, 0.7500000000000000000, 0.7578125000000000000, 0.7641217583431409999 ),
 .UNSPECIFIED. ) 
 CURVE ( )  GEOMETRIC_REPRESENTATION_ITEM ( )  RATIONAL_B_SPLINE_CURVE ( ( 0.9763430640195970289, 0.9385262470928680267, 1.000000000000000000, 0.9238795325112869605, 1.000000000000000000, 0.9238795325112869605, 1.000000000000000000, 0.9238795325112869605, 1.000000000000000000, 0.9238795325112869605, 1.000000000000000000, 0.9238795325112869605, 1.000000000000000000, 0.9238795325112869605, 1.000000000000000000, 0.9385262470928670275, 0.9763430640195980281 ) ) 
 REPRESENTATION_ITEM ( '' )  );
#6052=CARTESIAN_POINT ( 'NONE',  ( 116.1431348109119881, -10.30919188438810075, -12.61870101168855918 ) ) ;
#6054=CARTESIAN_POINT ( 'NONE',  ( 113.9307948109119906, 0.9020085738987339008, -11.91225656197089222 ) ) ;
#6055=ORIENTED_EDGE ( 'NONE', *, *, #39358, .F. ) ;
#6056=CARTESIAN_POINT ( 'NONE',  ( 114.1577014775786552, -3.505236298600246325, -18.68346056562440793 ) ) ;
#6058=CARTESIAN_POINT ( 'NONE',  ( 125.1059481442452750, -8.166667518702819706, -8.995218007635861213 ) ) ;
#6059=CARTESIAN_POINT ( 'NONE',  ( 119.2063748109119814, -1.561330072975668504, -17.79121239304076951 ) ) ;
#6060=CARTESIAN_POINT ( 'NONE',  ( 115.1787814775786387, -9.988377603198976828, -10.36322818467138340 ) ) ;
#6062=CARTESIAN_POINT ( 'NONE',  ( 112.8529881442453160, -7.894159318335828068, -9.358103419637847864 ) ) ;
#6064=CARTESIAN_POINT ( 'NONE',  ( 118.0718414775786442, -0.8288870151387760510, -10.36305467784173118 ) ) ;
#6065=CARTESIAN_POINT ( 'NONE',  ( 113.0231681442453180, -10.15424416112533912, -14.75197769757731336 ) ) ;
#6069=CARTESIAN_POINT ( 'NONE',  ( 121.8725281442453223, -6.222761293078241884, -8.102969835052219238 ) ) ;
#6072=VERTEX_POINT ( 'NONE', #43040 ) ;
#6074=CARTESIAN_POINT ( 'NONE',  ( 121.5888948109119809, -10.30919188438810075, -12.61870101168855918 ) ) ;
#6077=CARTESIAN_POINT ( 'NONE',  ( 112.3991748109119868, -8.166667518702817929, -8.995218007635859436 ) ) ;
#6084=CARTESIAN_POINT ( 'NONE',  ( 135.8491221887209690, -4.131696503738900184, -19.29954514867480597 ) ) ;
#6089=CARTESIAN_POINT ( 'NONE',  ( 122.2128881442453263, -7.643976991954077427, -18.09477374809248928 ) ) ;
#6091=ORIENTED_EDGE ( 'NONE', *, *, #44122, .F. ) ;
#6092=CARTESIAN_POINT ( 'NONE',  ( 122.4965214775786251, -10.30919188438810075, -12.61870101168855918 ) ) ;
#6093=CARTESIAN_POINT ( 'NONE',  ( 120.6812681442452941, -10.30919188438810075, -12.61870101168855918 ) ) ;
#6095=CARTESIAN_POINT ( 'NONE',  ( 113.8173414775786512, -9.565557343593413364, -10.61323700422348004 ) ) ;
#6096=CARTESIAN_POINT ( 'NONE',  ( 113.7038881442453402, -3.383040157471821630, -19.15922257007629170 ) ) ;
#6098=CARTESIAN_POINT ( 'NONE',  ( 124.0848681442452772, -4.089484607189486809, -7.948022111789456723 ) ) ;
#6103=CARTESIAN_POINT ( 'NONE',  ( 117.2776681442452968, -4.153390946401321671, -8.397313243818183892 ) ) ;
#6104=CARTESIAN_POINT ( 'NONE',  ( 118.1285681442453068, -2.084020599724406786, -8.691656652584148546 ) ) ;
#6110=CARTESIAN_POINT ( 'NONE',  ( 114.9518748109119883, -1.834011780172310813, -8.268836392978581529 ) ) ;
#6111=CARTESIAN_POINT ( 'NONE',  ( 113.2858169107182249, -2.467220198592768199, -17.83387418641523325 ) ) ;
#6117=CARTESIAN_POINT ( 'NONE',  ( 123.2687479366341421, -2.335067861339664486, -15.51187490787343215 ) ) ;
#6120=CARTESIAN_POINT ( 'NONE',  ( 117.9016614775786280, -9.988377603198976828, -10.36322818467138340 ) ) ;
#6121=CARTESIAN_POINT ( 'NONE',  ( 126.0703014775786102, -0.1624402480850797581, -16.17319339645315424 ) ) ;
#6122=CARTESIAN_POINT ( 'NONE',  ( 118.1285681442453068, -2.084020599724406786, -8.691656652584148546 ) ) ;
#6124=CARTESIAN_POINT ( 'NONE',  ( 122.7801548109119665, -3.383040157471821630, -19.15922257007629170 ) ) ;
#6125=CARTESIAN_POINT ( 'NONE',  ( 112.9097148109120070, 0.2603800115204892296, -16.42320221600525088 ) ) ;
#6128=CARTESIAN_POINT ( 'NONE',  ( 111.8886348109120092, -6.222761293078241884, -8.102969835052219238 ) ) ;
#6131=CARTESIAN_POINT ( 'NONE',  ( 118.4122014775786340, 0.5811942927096110934, -14.16772938898807510 ) ) ;
#6133=CARTESIAN_POINT ( 'NONE',  ( 114.8951481442453115, -8.899110576539710493, -16.42337572283490132 ) ) ;
#6135=CARTESIAN_POINT ( 'NONE',  ( 113.0231681442453322, 0.9020085738987339008, -11.91225656197089222 ) ) ;
#6137=CARTESIAN_POINT ( 'NONE',  ( 120.1707281442453166, 0.2603800115204892296, -16.42320221600525088 ) ) ;
#6138=DIRECTION ( 'NONE',  ( -1.000000000000000000, 0.000000000000000000, 0.000000000000000000 ) ) ;
#6140=CARTESIAN_POINT ( 'NONE',  ( 124.9698353663348342, -1.172797794773259072, -17.05961127468926719 ) ) ;
#6141=FACE_OUTER_BOUND ( 'NONE', #35087, .T. ) ;
#6142=CARTESIAN_POINT ( 'NONE',  ( 117.0507614775786465, 0.1319031606808879209, -14.10382304977623669 ) ) ;
#6143=CARTESIAN_POINT ( 'NONE',  ( 112.6871514811013526, -2.280480477428480146, -18.08254604495227724 ) ) ;
#6144=CARTESIAN_POINT ( 'NONE',  ( 118.3554748109119998, -9.565557343593413364, -10.61323700422348004 ) ) ;
#6147=CARTESIAN_POINT ( 'NONE',  ( 117.2776681442452968, -4.153390946401325223, -8.397313243818185668 ) ) ;
#6148=CARTESIAN_POINT ( 'NONE',  ( 113.8173414775786512, 0.2603800115204892296, -16.42320221600525088 ) ) ;
#6150=CARTESIAN_POINT ( 'NONE',  ( 112.5126281442453120, -10.30919188438810075, -12.61870101168855918 ) ) ;
#6151=CARTESIAN_POINT ( 'NONE',  ( 115.0086014775786509, -5.574606645277164318, -18.38911715685844683 ) ) ;
#6152=CARTESIAN_POINT ( 'NONE',  ( 122.3830681442452857, -8.166667518702819706, -8.995218007635861213 ) ) ;
#6154=CARTESIAN_POINT ( 'NONE',  ( 116.1431348109119881, 0.1319031606808879209, -14.10382304977623669 ) ) ;
#6156=CARTESIAN_POINT ( 'NONE',  ( 113.3068014775786594, -8.166667518702817929, -8.995218007635859436 ) ) ;
#6161=CARTESIAN_POINT ( 'NONE',  ( 127.9787496859519393, -4.170178312457123226, -15.56602175589793191 ) ) ;
#6162=CARTESIAN_POINT ( 'NONE',  ( 120.3976348109119812, -1.834011780172310813, -8.268836392978581529 ) ) ;
#6165=DIRECTION ( 'NONE',  ( 0.000000000000000000, 0.6004852223388319477, -0.7996358532186282897 ) ) ;
#6166=CARTESIAN_POINT ( 'NONE',  ( 113.0231681442453180, -10.15424416112533912, -14.75197769757731336 ) ) ;
#6168=CARTESIAN_POINT ( 'NONE',  ( 122.2696148109119889, -4.089484607189486809, -7.948022111789456723 ) ) ;
#6172=CARTESIAN_POINT ( 'NONE',  ( 111.7184548109119788, -9.261995988541697145, -16.69588392320189030 ) ) ;
#6173=CARTESIAN_POINT ( 'NONE',  ( 122.3830681442452857, -1.833838273342659697, -17.42832698103878286 ) ) ;
#6174=CARTESIAN_POINT ( 'NONE',  ( 118.2420214775786320, -3.383040157471821630, -19.15922257007629170 ) ) ;
#6175=CARTESIAN_POINT ( 'NONE',  ( 113.4202548109119846, 0.1319031606808879209, -14.10382304977623669 ) ) ;
#6176=CARTESIAN_POINT ( 'NONE',  ( 116.8805814775786445, -6.344957434206662583, -7.627207830600332805 ) ) ;
#6180=CARTESIAN_POINT ( 'NONE',  ( 119.4332814775786318, -8.899110576539710493, -16.42337572283490132 ) ) ;
#6181=VERTEX_POINT ( 'NONE', #34338 ) ;
#6185=CARTESIAN_POINT ( 'NONE',  ( 122.8368814775786291, -7.894159318335828068, -9.358103419637847864 ) ) ;
#6188=CARTESIAN_POINT ( 'NONE',  ( 137.3930029278033658, -0.4326168857421066605, -10.81500932932321035 ) ) ;
#6189=CARTESIAN_POINT ( 'NONE',  ( 119.3765548109119834, 0.9020085738987339008, -11.91225656197089222 ) ) ;
#6192=CARTESIAN_POINT ( 'NONE',  ( 117.5613014775786525, -10.15424416112533912, -14.75197769757731336 ) ) ;
#6195=CARTESIAN_POINT ( 'NONE',  ( 125.6732148109119862, -9.859900752359378018, -12.68260735090039759 ) ) ;
#6196=CARTESIAN_POINT ( 'NONE',  ( 122.3263414775786373, -3.505236298600246325, -18.68346056562440793 ) ) ;
#6199=CARTESIAN_POINT ( 'NONE',  ( 123.8012348109119642, 0.2603800115204892296, -16.42320221600525088 ) ) ;
#6200=CARTESIAN_POINT ( 'NONE',  ( 112.1722337524184070, -8.900133558646924570, -16.42203216583235204 ) ) ;
#6201=CARTESIAN_POINT ( 'NONE',  ( 120.1140014775786398, -1.561330072975668504, -17.79121239304076951 ) ) ;
#6202=CARTESIAN_POINT ( 'NONE',  ( 118.2987481442453088, -1.561330072975668504, -17.79121239304076951 ) ) ;
#6203=CARTESIAN_POINT ( 'NONE',  ( 118.1852948109119836, -4.153390946401325223, -8.397313243818185668 ) ) ;
#6205=CARTESIAN_POINT ( 'NONE',  ( 112.1111981407226210, -1.081026697600516950, -17.18181821144401411 ) ) ;
#6208=CARTESIAN_POINT ( 'NONE',  ( 123.8012348109119642, -9.565557343593413364, -10.61323700422348004 ) ) ;
#6215=CARTESIAN_POINT ( 'NONE',  ( 123.9146881442452894, 0.9020085738987339008, -11.91225656197089222 ) ) ;
#6216=CARTESIAN_POINT ( 'NONE',  ( 121.8158014775786171, -4.153390946401325223, -8.397313243818185668 ) ) ;
#6217=VERTEX_POINT ( 'NONE', #16126 ) ;
#6218=CARTESIAN_POINT ( 'NONE',  ( 123.4041481442452834, -10.30919188438810075, -12.61870101168855918 ) ) ;
#6219=CARTESIAN_POINT ( 'NONE',  ( 112.4559014775786778, -0.1624402480850797581, -16.17319339645315424 ) ) ;
#6221=CARTESIAN_POINT ( 'NONE',  ( 121.4754414775786131, -8.166667518702819706, -8.995218007635861213 ) ) ;
#6222=CARTESIAN_POINT ( 'NONE',  ( 121.8725281442453223, -3.383040157471821630, -19.15922257007629170 ) ) ;
#6225=CARTESIAN_POINT ( 'NONE',  ( 114.3278814775786429, -10.30919188438810075, -12.61870101168855918 ) ) ;
#6226=CARTESIAN_POINT ( 'NONE',  ( 115.9162281442453235, -4.089484607189486809, -7.948022111789456723 ) ) ;
#6230=DIRECTION ( 'NONE',  ( 0.000000000000000000, 0.6004852223388321697, -0.7996358532186279566 ) ) ;
#6231=CARTESIAN_POINT ( 'NONE',  ( 124.9357681442453014, -7.643976991954077427, -18.09477374809248928 ) ) ;
#6235=CARTESIAN_POINT ( 'NONE',  ( 116.4267681442453153, -6.222761293078241884, -8.102969835052219238 ) ) ;
#6237=CARTESIAN_POINT ( 'NONE',  ( 117.9016614775786280, -0.1624402480850797581, -16.17319339645315424 ) ) ;
#6238=CARTESIAN_POINT ( 'NONE',  ( 124.3117748109119844, -10.30919188438810075, -12.61870101168855918 ) ) ;
#6240=CARTESIAN_POINT ( 'NONE',  ( 124.0281414775786146, -7.643976991954077427, -18.09477374809248928 ) ) ;
#6241=CARTESIAN_POINT ( 'NONE',  ( 119.0929214775786278, -5.638512984488999180, -18.83840828888717311 ) ) ;
#6242=CARTESIAN_POINT ( 'NONE',  ( 125.4463081442452932, -5.638512984488999180, -18.83840828888717311 ) ) ;
#6244=CARTESIAN_POINT ( 'NONE',  ( 122.7234281442452755, -4.153390946401325223, -8.397313243818185668 ) ) ;
#6248=CARTESIAN_POINT ( 'NONE',  ( 124.4819548109119722, -7.893985811506177619, -18.51759400769804742 ) ) ;
#6250=CARTESIAN_POINT ( 'NONE',  ( 113.4202548109119846, 0.1319031606808879209, -14.10382304977623669 ) ) ;
#6251=CARTESIAN_POINT ( 'NONE',  ( 123.6877814775786533, -3.383040157471821630, -19.15922257007629170 ) ) ;
#6252=CARTESIAN_POINT ( 'NONE',  ( 117.5284876054816152, -2.287189184988681401, -18.07361239780446738 ) ) ;
#6260=CARTESIAN_POINT ( 'NONE',  ( 123.0070614775786169, -10.15424416112533912, -14.75197769757731336 ) ) ;
#6261=CARTESIAN_POINT ( 'NONE',  ( 113.7038881442453402, -6.222761293078241884, -8.102969835052219238 ) ) ;
#6262=CARTESIAN_POINT ( 'NONE',  ( 126.2640359059496973, -5.823073642834863506, -18.32360385354721544 ) ) ;
#6265=CARTESIAN_POINT ( 'NONE',  ( 120.5678148109119832, -1.833838273342659253, -17.42832698103878286 ) ) ;
#6266=CARTESIAN_POINT ( 'NONE',  ( 114.0442481442453300, -7.643976991954077427, -18.09477374809248928 ) ) ;
#6272=CARTESIAN_POINT ( 'NONE',  ( 112.0020881442453344, 0.2603800115204892296, -16.42320221600525088 ) ) ;
#6274=CARTESIAN_POINT ( 'NONE',  ( 112.1155414775786454, 0.9020085738987339008, -11.91225656197089222 ) ) ;
#6275=CARTESIAN_POINT ( 'NONE',  ( 127.7429221096626151, 0.4604311707933653741, -15.59844375728449073 ) ) ;
#6277=CARTESIAN_POINT ( 'NONE',  ( 123.8579614775786126, -9.859900752359378018, -12.68260735090039759 ) ) ;
#6278=CARTESIAN_POINT ( 'NONE',  ( 121.6456214775786293, 0.4262465694468514643, -12.03445270309931736 ) ) ;
#6282=DIRECTION ( 'NONE',  ( -1.000000000000000000, 0.000000000000000000, 0.000000000000000000 ) ) ;
#6286=CARTESIAN_POINT ( 'NONE',  ( 125.1059481442452750, -8.166667518702819706, -8.995218007635861213 ) ) ;
#6287=CARTESIAN_POINT ( 'NONE',  ( 123.0637881442452937, -0.4660016031367893996, -10.09054647747474043 ) ) ;
#6289=CARTESIAN_POINT ( 'NONE',  ( 118.8660148109119774, -10.30919188438810075, -12.61870101168855918 ) ) ;
#6290=CARTESIAN_POINT ( 'NONE',  ( 112.6260814775786514, -9.261995988541697145, -16.69588392320189030 ) ) ;
#6291=VERTEX_POINT ( 'NONE', #37994 ) ;
#6294=CARTESIAN_POINT ( 'NONE',  ( 111.6617281442453304, 0.4262465694468514643, -12.03445270309931736 ) ) ;
#6295=CARTESIAN_POINT ( 'NONE',  ( 124.0848681442452772, -4.089484607189486809, -7.948022111789456723 ) ) ;
#6296=CARTESIAN_POINT ( 'NONE',  ( 115.5758681442453053, -1.561330072975668060, -17.79121239304076951 ) ) ;
#6298=CARTESIAN_POINT ( 'NONE',  ( 112.2857214775786474, -5.574606645277164318, -18.38911715685844683 ) ) ;
#6300=CARTESIAN_POINT ( 'NONE',  ( 117.8449348109119938, -1.833838273342659253, -17.42832698103878286 ) ) ;
#6301=CARTESIAN_POINT ( 'NONE',  ( 111.7751814775786556, -7.893985811506177619, -18.51759400769804742 ) ) ;
#6303=CARTESIAN_POINT ( 'NONE',  ( 124.3685014775786328, 0.4262465694468514643, -12.03445270309931736 ) ) ;
#6311=CARTESIAN_POINT ( 'NONE',  ( 112.7395348109119766, -5.638512984488999180, -18.83840828888717311 ) ) ;
#6318=CARTESIAN_POINT ( 'NONE',  ( 119.3765548109119834, 0.9020085738987339008, -11.91225656197089222 ) ) ;
#6322=CARTESIAN_POINT ( 'NONE',  ( 122.7234281442452755, -4.153390946401325223, -8.397313243818185668 ) ) ;
#6326=CARTESIAN_POINT ( 'NONE',  ( 119.8303681442453126, -10.63000616557722466, -14.87417383870573495 ) ) ;
#6328=CARTESIAN_POINT ( 'NONE',  ( 115.5758681442453053, -7.894159318335828068, -9.358103419637847864 ) ) ;
#6329=( BOUNDED_SURFACE ( )  B_SPLINE_SURFACE ( 1, 2, ( 
 ( #31972, #25595, #1410, #39501, #25150, #14656, #5056, #43370, #8263, #22168, #39274, #22393, #36288, #36062, #8037, #734, #4831, #39045, #15550, #18971, #32860, #29457, #21943, #35834, #18753, #7817, #39947, #8709, #43144, #4386, #18300, #15328, #4608, #36512, #32195, #5286, #968, #14885, #32642, #25814, #29914, #33080, #12595, #20111, #37422, #33530, #44056, #2308, #30584, #2082, #9617, #5725, #9166, #43594, #43828, #13268, #16238, #44288, #19643, #33997, #15780, #16462, #44505, #30141, #23762, #37181, #26267, #37652, #36954, #2768, #26940, #12822, #5499, #40174, #30366, #33307, #26498, #29683, #2536, #40406, #12367, #26720, #23070, #40629, #19420, #8939, #23537, #9386, #13041, #27174, #41095, #1852, #19202, #19879, #23296, #6192, #22842, #5954, #33767, #36734, #40864, #9854, #16692, #16006, #30813, #7086, #10517, #27401, #20779, #17362, #44737, #14377, #2993, #27625, #34869, #10082, #16919, #13718, #31250, #24865, #10742, #17800, #13496, #20995, #34438, #24641, #23985, #35096, #3217, #21220, #31694, #22, #42199, #24203, #3878, #38309, #41323, #6870, #17144, #10302, #44961, #3657, #6427, #462, #37873, #13935, #3443, #31030, #6649, #41539, #20337, #28290, #10960, #34658, #20557, #27847, #38094, #31470, #34220, #41757, #24419, #17578, #7301, #243, #14152, #28068, #41977, #38523, #18019, #11859, #11629, #25765, #28965, #911, #14600, #43316, #28741, #21442, #35328, #28520, #25541, #42646, #42425, #39448, #39671, #32143, #14831, #42872, #31917, #11414, #1576, #8210, #8435, #18698, #682, #25092, #39216, #11189, #4097, #22117, #12085, #38756, #25323, #7758, #35784, #7526, #38987, #7980, #21888, #1358, #43091, #36007, #15054, #21666, #29178, #4779, #35554, #36235, #29404, #4326, #18247, #4553, #18479, #15270, #32368, #22340, #1135, #15497, #32589, #5001, #18914, #32806, #25990, #33472, #2252, #16181, #12537, #2708, #26662, #22783, #23011, #16635, #26886, #5899, #36677, #19367, #36458, #40805, #5447, #33256, #36901, #29628, #8882, #39895, #2481, #16405, #19591 ),
 ( #29856, #2028, #12762, #44450, #23477, #22557, #5673, #30085, #15953, #5228, #43771, #8656, #9561, #30529, #9108, #19142, #43999, #26440, #19822, #37363, #33025, #40575, #1799, #6135, #26210, #15727, #40347, #20055, #9335, #43543, #44230, #23244, #12990, #37125, #33709, #12313, #40118, #30305, #33938, #9796, #34164, #31199, #3167, #16866, #13877, #181, #6589, #20506, #3390, #6368, #34385, #21160, #45121, #28015, #38253, #20279, #44681, #13663, #30757, #41040, #17309, #17742, #31638, #17089, #27347, #10242, #13217, #13442, #30980, #44906, #20945, #17517, #27788, #34605, #27116, #3602, #24367, #41267, #10686, #3818, #23706, #2936, #24150, #38042, #34819, #6818, #31414, #20725, #35037, #37598, #10026, #41701, #41484, #23933, #10466, #7035, #14098, #27572, #37814, #41920, #24588, #38471, #7247, #1305, #25488, #42369, #38925, #10906, #15217, #11130, #7695, #11352, #4043, #28461, #407, #22062, #35954, #25033, #29124, #25711, #14544, #43035, #36179, #14323, #21383, #25263, #39159, #4725, #42591, #18642, #7924, #8379, #42146, #28237, #21834, #28687, #24806, #35727, #4501, #18424, #32084, #22286, #1081, #21611, #32316, #4946, #11803, #39391, #35498, #4270, #38698, #39618, #18189, #853, #14995, #17965, #14772, #7466, #32535, #18859, #28908, #35266, #31864, #42817, #631, #11579, #8157, #19541, #39842, #33200, #29575, #36625, #26154, #33418, #6074, #30251, #29351, #12484, #29801, #43492, #43265, #15672, #32751, #16350, #37308, #15901, #25934, #26382, #5400, #12708, #44176, #23421, #40293, #1524, #33648, #32972, #22506, #1976, #12939, #12260, #12031, #5845, #5618, #19767, #22957, #40061, #8604, #15445, #22726, #36399, #5169, #19086, #2197, #19316, #1749, #16123, #2426, #8824, #43713, #36849, #9057, #30027, #40749, #43943, #26836, #26608, #40523, #9285, #23192, #37072, #9506, #10191, #24535, #38425, #9970, #34114, #17037, #19997, #37537, #23881, #37766, #27741, #24321, #24098, #41434, #33881, #10413, #31144, #37991, #27295, #40985, #2650, #6536, #16582, #30477, #9739, #6767 ) ),
 .UNSPECIFIED., .F., .F., .F. ) 
 B_SPLINE_SURFACE_WITH_KNOTS ( ( 2, 2 ),
 ( 3, 2, 2, 2, 2, 2, 2, 2, 2, 2, 2, 2, 2, 2, 2, 2, 2, 2, 2, 2, 2, 2, 2, 2, 2, 2, 2, 2, 2, 2, 2, 2, 2, 2, 2, 2, 2, 2, 2, 2, 2, 2, 2, 2, 2, 2, 2, 2, 2, 2, 2, 2, 2, 2, 2, 2, 2, 2, 2, 2, 2, 2, 2, 2, 2, 2, 2, 2, 2, 2, 2, 2, 2, 2, 2, 2, 2, 2, 2, 2, 2, 2, 2, 2, 2, 2, 2, 2, 2, 2, 2, 2, 2, 2, 2, 2, 2, 2, 2, 2, 2, 2, 2, 2, 2, 2, 2, 2, 2, 2, 2, 2, 2, 2, 2, 2, 2, 2, 2, 2, 2, 2, 2, 2, 2, 2, 2, 2, 3 ),
 ( 0.000000000000000000, 1.000000000000000000 ),
 ( 0.000000000000000000, 0.007812500000000000000, 0.01562500000000000000, 0.02343750000000000000, 0.03125000000000000000, 0.03906250000000000000, 0.04687500000000000000, 0.05468750000000000000, 0.06250000000000000000, 0.07031250000000000000, 0.07812500000000000000, 0.08593750000000000000, 0.09375000000000000000, 0.1015625000000000000, 0.1093750000000000000, 0.1171875000000000000, 0.1250000000000000000, 0.1328125000000000000, 0.1406250000000000000, 0.1484375000000000000, 0.1562500000000000000, 0.1640625000000000000, 0.1718750000000000000, 0.1796875000000000000, 0.1875000000000000000, 0.1953125000000000000, 0.2031250000000000000, 0.2109375000000000000, 0.2187500000000000000, 0.2265625000000000000, 0.2343750000000000000, 0.2421875000000000000, 0.2500000000000000000, 0.2578125000000000000, 0.2656250000000000000, 0.2734375000000000000, 0.2812500000000000000, 0.2890625000000000000, 0.2968750000000000000, 0.3046875000000000000, 0.3125000000000000000, 0.3203125000000000000, 0.3281250000000000000, 0.3359375000000000000, 0.3437500000000000000, 0.3515625000000000000, 0.3593750000000000000, 0.3671875000000000000, 0.3750000000000000000, 0.3828125000000000000, 0.3906250000000000000, 0.3984375000000000000, 0.4062500000000000000, 0.4140625000000000000, 0.4218750000000000000, 0.4296875000000000000, 0.4375000000000000000, 0.4453125000000000000, 0.4531250000000000000, 0.4609375000000000000, 0.4687500000000000000, 0.4765625000000000000, 0.4843750000000000000, 0.4921875000000000000, 0.5000000000000000000, 0.5078125000000000000, 0.5156250000000000000, 0.5234375000000000000, 0.5312500000000000000, 0.5390625000000000000, 0.5468750000000000000, 0.5546875000000000000, 0.5625000000000000000, 0.5703125000000000000, 0.5781250000000000000, 0.5859375000000000000, 0.5937500000000000000, 0.6015625000000000000, 0.6093750000000000000, 0.6171875000000000000, 0.6250000000000000000, 0.6328125000000000000, 0.6406250000000000000, 0.6484375000000000000, 0.6562500000000000000, 0.6640625000000000000, 0.6718750000000000000, 0.6796875000000000000, 0.6875000000000000000, 0.6953125000000000000, 0.7031250000000000000, 0.7109375000000000000, 0.7187500000000000000, 0.7265625000000000000, 0.7343750000000000000, 0.7421875000000000000, 0.7500000000000000000, 0.7578125000000000000, 0.7656250000000000000, 0.7734375000000000000, 0.7812500000000000000, 0.7890625000000000000, 0.7968750000000000000, 0.8046875000000000000, 0.8125000000000000000, 0.8203125000000000000, 0.8281250000000000000, 0.8359375000000000000, 0.8437500000000000000, 0.8515625000000000000, 0.8593750000000000000, 0.8671875000000000000, 0.8750000000000000000, 0.8828125000000000000, 0.8906250000000000000, 0.8984375000000000000, 0.9062500000000000000, 0.9140625000000000000, 0.9218750000000000000, 0.9296875000000000000, 0.9375000000000000000, 0.9453125000000000000, 0.9531250000000000000, 0.9609375000000000000, 0.9687500000000000000, 0.9765625000000000000, 0.9843750000000000000, 0.9921875000000000000, 1.000000000000000000 ),
 .UNSPECIFIED. ) 
 GEOMETRIC_REPRESENTATION_ITEM ( )  RATIONAL_B_SPLINE_SURFACE ( (
 ( 1.000000000000000000, 0.9238795325112869605, 1.000000000000000000, 0.9238795325112869605, 1.000000000000000000, 0.9238795325112869605, 1.000000000000000000, 0.9238795325112869605, 1.000000000000000000, 0.9238795325112869605, 1.000000000000000000, 0.9238795325112869605, 1.000000000000000000, 0.9238795325112869605, 1.000000000000000000, 0.9238795325112869605, 1.000000000000000000, 0.9238795325112869605, 1.000000000000000000, 0.9238795325112869605, 1.000000000000000000, 0.9238795325112869605, 1.000000000000000000, 0.9238795325112869605, 1.000000000000000000, 0.9238795325112869605, 1.000000000000000000, 0.9238795325112869605, 1.000000000000000000, 0.9238795325112869605, 1.000000000000000000, 0.9238795325112869605, 1.000000000000000000, 0.9238795325112869605, 1.000000000000000000, 0.9238795325112869605, 1.000000000000000000, 0.9238795325112869605, 1.000000000000000000, 0.9238795325112869605, 1.000000000000000000, 0.9238795325112869605, 1.000000000000000000, 0.9238795325112869605, 1.000000000000000000, 0.9238795325112869605, 1.000000000000000000, 0.9238795325112869605, 1.000000000000000000, 0.9238795325112869605, 1.000000000000000000, 0.9238795325112869605, 1.000000000000000000, 0.9238795325112869605, 1.000000000000000000, 0.9238795325112869605, 1.000000000000000000, 0.9238795325112869605, 1.000000000000000000, 0.9238795325112869605, 1.000000000000000000, 0.9238795325112869605, 1.000000000000000000, 0.9238795325112869605, 1.000000000000000000, 0.9238795325112869605, 1.000000000000000000, 0.9238795325112869605, 1.000000000000000000, 0.9238795325112869605, 1.000000000000000000, 0.9238795325112869605, 1.000000000000000000, 0.9238795325112869605, 1.000000000000000000, 0.9238795325112869605, 1.000000000000000000, 0.9238795325112869605, 1.000000000000000000, 0.9238795325112869605, 1.000000000000000000, 0.9238795325112869605, 1.000000000000000000, 0.9238795325112869605, 1.000000000000000000, 0.9238795325112869605, 1.000000000000000000, 0.9238795325112869605, 1.000000000000000000, 0.9238795325112869605, 1.000000000000000000, 0.9238795325112869605, 1.000000000000000000, 0.9238795325112869605, 1.000000000000000000, 0.9238795325112869605, 1.000000000000000000, 0.9238795325112869605, 1.000000000000000000, 0.9238795325112869605, 1.000000000000000000, 0.9238795325112869605, 1.000000000000000000, 0.9238795325112869605, 1.000000000000000000, 0.9238795325112869605, 1.000000000000000000, 0.9238795325112869605, 1.000000000000000000, 0.9238795325112869605, 1.000000000000000000, 0.9238795325112869605, 1.000000000000000000, 0.9238795325112869605, 1.000000000000000000, 0.9238795325112869605, 1.000000000000000000, 0.9238795325112869605, 1.000000000000000000, 0.9238795325112869605, 1.000000000000000000, 0.9238795325112869605, 1.000000000000000000, 0.9238795325112869605, 1.000000000000000000, 0.9238795325112869605, 1.000000000000000000, 0.9238795325112869605, 1.000000000000000000, 0.9238795325112869605, 1.000000000000000000, 0.9238795325112869605, 1.000000000000000000, 0.9238795325112869605, 1.000000000000000000, 0.9238795325112869605, 1.000000000000000000, 0.9238795325112869605, 1.000000000000000000, 0.9238795325112869605, 1.000000000000000000, 0.9238795325112869605, 1.000000000000000000, 0.9238795325112869605, 1.000000000000000000, 0.9238795325112869605, 1.000000000000000000, 0.9238795325112869605, 1.000000000000000000, 0.9238795325112869605, 1.000000000000000000, 0.9238795325112869605, 1.000000000000000000, 0.9238795325112869605, 1.000000000000000000, 0.9238795325112869605, 1.000000000000000000, 0.9238795325112869605, 1.000000000000000000, 0.9238795325112869605, 1.000000000000000000, 0.9238795325112869605, 1.000000000000000000, 0.9238795325112869605, 1.000000000000000000, 0.9238795325112869605, 1.000000000000000000, 0.9238795325112869605, 1.000000000000000000, 0.9238795325112869605, 1.000000000000000000, 0.9238795325112869605, 1.000000000000000000, 0.9238795325112869605, 1.000000000000000000, 0.9238795325112869605, 1.000000000000000000, 0.9238795325112869605, 1.000000000000000000, 0.9238795325112869605, 1.000000000000000000, 0.9238795325112869605, 1.000000000000000000, 0.9238795325112869605, 1.000000000000000000, 0.9238795325112869605, 1.000000000000000000, 0.9238795325112869605, 1.000000000000000000, 0.9238795325112869605, 1.000000000000000000, 0.9238795325112869605, 1.000000000000000000, 0.9238795325112869605, 1.000000000000000000, 0.9238795325112869605, 1.000000000000000000, 0.9238795325112869605, 1.000000000000000000, 0.9238795325112869605, 1.000000000000000000, 0.9238795325112869605, 1.000000000000000000, 0.9238795325112869605, 1.000000000000000000, 0.9238795325112869605, 1.000000000000000000, 0.9238795325112869605, 1.000000000000000000, 0.9238795325112869605, 1.000000000000000000, 0.9238795325112869605, 1.000000000000000000, 0.9238795325112869605, 1.000000000000000000, 0.9238795325112869605, 1.000000000000000000, 0.9238795325112869605, 1.000000000000000000, 0.9238795325112869605, 1.000000000000000000, 0.9238795325112869605, 1.000000000000000000, 0.9238795325112869605, 1.000000000000000000, 0.9238795325112869605, 1.000000000000000000, 0.9238795325112869605, 1.000000000000000000, 0.9238795325112869605, 1.000000000000000000, 0.9238795325112869605, 1.000000000000000000, 0.9238795325112869605, 1.000000000000000000, 0.9238795325112869605, 1.000000000000000000, 0.9238795325112869605, 1.000000000000000000, 0.9238795325112869605, 1.000000000000000000, 0.9238795325112869605, 1.000000000000000000, 0.9238795325112869605, 1.000000000000000000, 0.9238795325112869605, 1.000000000000000000, 0.9238795325112869605, 1.000000000000000000, 0.9238795325112869605, 1.000000000000000000, 0.9238795325112869605, 1.000000000000000000, 0.9238795325112869605, 1.000000000000000000, 0.9238795325112869605, 1.000000000000000000),
 ( 1.000000000000000000, 0.9238795325112869605, 1.000000000000000000, 0.9238795325112869605, 1.000000000000000000, 0.9238795325112869605, 1.000000000000000000, 0.9238795325112869605, 1.000000000000000000, 0.9238795325112869605, 1.000000000000000000, 0.9238795325112869605, 1.000000000000000000, 0.9238795325112869605, 1.000000000000000000, 0.9238795325112869605, 1.000000000000000000, 0.9238795325112869605, 1.000000000000000000, 0.9238795325112869605, 1.000000000000000000, 0.9238795325112869605, 1.000000000000000000, 0.9238795325112869605, 1.000000000000000000, 0.9238795325112869605, 1.000000000000000000, 0.9238795325112869605, 1.000000000000000000, 0.9238795325112869605, 1.000000000000000000, 0.9238795325112869605, 1.000000000000000000, 0.9238795325112869605, 1.000000000000000000, 0.9238795325112869605, 1.000000000000000000, 0.9238795325112869605, 1.000000000000000000, 0.9238795325112869605, 1.000000000000000000, 0.9238795325112869605, 1.000000000000000000, 0.9238795325112869605, 1.000000000000000000, 0.9238795325112869605, 1.000000000000000000, 0.9238795325112869605, 1.000000000000000000, 0.9238795325112869605, 1.000000000000000000, 0.9238795325112869605, 1.000000000000000000, 0.9238795325112869605, 1.000000000000000000, 0.9238795325112869605, 1.000000000000000000, 0.9238795325112869605, 1.000000000000000000, 0.9238795325112869605, 1.000000000000000000, 0.9238795325112869605, 1.000000000000000000, 0.9238795325112869605, 1.000000000000000000, 0.9238795325112869605, 1.000000000000000000, 0.9238795325112869605, 1.000000000000000000, 0.9238795325112869605, 1.000000000000000000, 0.9238795325112869605, 1.000000000000000000, 0.9238795325112869605, 1.000000000000000000, 0.9238795325112869605, 1.000000000000000000, 0.9238795325112869605, 1.000000000000000000, 0.9238795325112869605, 1.000000000000000000, 0.9238795325112869605, 1.000000000000000000, 0.9238795325112869605, 1.000000000000000000, 0.9238795325112869605, 1.000000000000000000, 0.9238795325112869605, 1.000000000000000000, 0.9238795325112869605, 1.000000000000000000, 0.9238795325112869605, 1.000000000000000000, 0.9238795325112869605, 1.000000000000000000, 0.9238795325112869605, 1.000000000000000000, 0.9238795325112869605, 1.000000000000000000, 0.9238795325112869605, 1.000000000000000000, 0.9238795325112869605, 1.000000000000000000, 0.9238795325112869605, 1.000000000000000000, 0.9238795325112869605, 1.000000000000000000, 0.9238795325112869605, 1.000000000000000000, 0.9238795325112869605, 1.000000000000000000, 0.9238795325112869605, 1.000000000000000000, 0.9238795325112869605, 1.000000000000000000, 0.9238795325112869605, 1.000000000000000000, 0.9238795325112869605, 1.000000000000000000, 0.9238795325112869605, 1.000000000000000000, 0.9238795325112869605, 1.000000000000000000, 0.9238795325112869605, 1.000000000000000000, 0.9238795325112869605, 1.000000000000000000, 0.9238795325112869605, 1.000000000000000000, 0.9238795325112869605, 1.000000000000000000, 0.9238795325112869605, 1.000000000000000000, 0.9238795325112869605, 1.000000000000000000, 0.9238795325112869605, 1.000000000000000000, 0.9238795325112869605, 1.000000000000000000, 0.9238795325112869605, 1.000000000000000000, 0.9238795325112869605, 1.000000000000000000, 0.9238795325112869605, 1.000000000000000000, 0.9238795325112869605, 1.000000000000000000, 0.9238795325112869605, 1.000000000000000000, 0.9238795325112869605, 1.000000000000000000, 0.9238795325112869605, 1.000000000000000000, 0.9238795325112869605, 1.000000000000000000, 0.9238795325112869605, 1.000000000000000000, 0.9238795325112869605, 1.000000000000000000, 0.9238795325112869605, 1.000000000000000000, 0.9238795325112869605, 1.000000000000000000, 0.9238795325112869605, 1.000000000000000000, 0.9238795325112869605, 1.000000000000000000, 0.9238795325112869605, 1.000000000000000000, 0.9238795325112869605, 1.000000000000000000, 0.9238795325112869605, 1.000000000000000000, 0.9238795325112869605, 1.000000000000000000, 0.9238795325112869605, 1.000000000000000000, 0.9238795325112869605, 1.000000000000000000, 0.9238795325112869605, 1.000000000000000000, 0.9238795325112869605, 1.000000000000000000, 0.9238795325112869605, 1.000000000000000000, 0.9238795325112869605, 1.000000000000000000, 0.9238795325112869605, 1.000000000000000000, 0.9238795325112869605, 1.000000000000000000, 0.9238795325112869605, 1.000000000000000000, 0.9238795325112869605, 1.000000000000000000, 0.9238795325112869605, 1.000000000000000000, 0.9238795325112869605, 1.000000000000000000, 0.9238795325112869605, 1.000000000000000000, 0.9238795325112869605, 1.000000000000000000, 0.9238795325112869605, 1.000000000000000000, 0.9238795325112869605, 1.000000000000000000, 0.9238795325112869605, 1.000000000000000000, 0.9238795325112869605, 1.000000000000000000, 0.9238795325112869605, 1.000000000000000000, 0.9238795325112869605, 1.000000000000000000, 0.9238795325112869605, 1.000000000000000000, 0.9238795325112869605, 1.000000000000000000, 0.9238795325112869605, 1.000000000000000000, 0.9238795325112869605, 1.000000000000000000, 0.9238795325112869605, 1.000000000000000000, 0.9238795325112869605, 1.000000000000000000, 0.9238795325112869605, 1.000000000000000000, 0.9238795325112869605, 1.000000000000000000, 0.9238795325112869605, 1.000000000000000000, 0.9238795325112869605, 1.000000000000000000, 0.9238795325112869605, 1.000000000000000000, 0.9238795325112869605, 1.000000000000000000, 0.9238795325112869605, 1.000000000000000000, 0.9238795325112869605, 1.000000000000000000, 0.9238795325112869605, 1.000000000000000000, 0.9238795325112869605, 1.000000000000000000, 0.9238795325112869605, 1.000000000000000000, 0.9238795325112869605, 1.000000000000000000, 0.9238795325112869605, 1.000000000000000000, 0.9238795325112869605, 1.000000000000000000, 0.9238795325112869605, 1.000000000000000000) ) ) 
 REPRESENTATION_ITEM ( '' )  SURFACE ( )  );
#6330=CARTESIAN_POINT ( 'NONE',  ( 123.2906948109119867, -8.166667518702819706, -8.995218007635861213 ) ) ;
#6334=CARTESIAN_POINT ( 'NONE',  ( 115.6893214775786447, -9.859900752359374465, -12.68260735090039404 ) ) ;
#6335=CARTESIAN_POINT ( 'NONE',  ( 116.1998614775786507, 0.4262465694468514643, -12.03445270309931736 ) ) ;
#6339=B_SPLINE_CURVE_WITH_KNOTS ( 'NONE', 3,
 ( #16066, #11975, #29520, #12200, #19030, #8326, #32917, #9229, #12658, #8768 ),
 .UNSPECIFIED., .F., .F.,
 ( 4, 3, 3, 4 ),
 ( 0.000000000000000000, 0.0001671877548681280042, 0.0003343755096277700343, 0.0006463528481650609656 ),
 .UNSPECIFIED. ) ;
#6342=CARTESIAN_POINT ( 'NONE',  ( 113.4202548109119846, -10.30919188438810075, -12.61870101168855918 ) ) ;
#6348=CARTESIAN_POINT ( 'NONE',  ( 123.5508514527377315, -3.041208495916663423, -14.57149963527472103 ) ) ;
#6349=CARTESIAN_POINT ( 'NONE',  ( 111.5005945643030856, -1.275047081438759111, -16.92345106201108251 ) ) ;
#6350=ADVANCED_FACE ( 'NONE', ( #6769 ), #12464, .T. ) ;
#6352=ORIENTED_EDGE ( 'NONE', *, *, #32499, .F. ) ;
#6353=CARTESIAN_POINT ( 'NONE',  ( 118.7525614775786380, -8.166667518702819706, -8.995218007635861213 ) ) ;
#6354=CARTESIAN_POINT ( 'NONE',  ( 114.0442481442453300, -1.834011780172310813, -8.268836392978581529 ) ) ;
#6355=CARTESIAN_POINT ( 'NONE',  ( 118.6958348109119754, -3.505236298600246325, -18.68346056562440793 ) ) ;
#6357=CARTESIAN_POINT ( 'NONE',  ( 123.2339681442453241, -6.344957434206665248, -7.627207830600338134 ) ) ;
#6359=CARTESIAN_POINT ( 'NONE',  ( 117.2209414775786485, -7.893985811506177619, -18.51759400769804742 ) ) ;
#6362=CARTESIAN_POINT ( 'NONE',  ( 114.5547881442453217, -4.153390946401321671, -8.397313243818183892 ) ) ;
#6364=EDGE_LOOP ( 'NONE', ( #24925, #949, #28706, #7528, #30199 ) ) ;
#6365=B_SPLINE_CURVE_WITH_KNOTS ( 'NONE', 3,
 ( #20187, #39009, #7780, #6723, #20635, #21687, #3290, #14395, #4347, #28306 ),
 .UNSPECIFIED., .F., .F.,
 ( 4, 3, 3, 4 ),
 ( 0.000000000000000000, 0.0001671877548681309858, 0.0003343755096277739917, 0.0006463528481650629171 ),
 .UNSPECIFIED. ) ;
#6366=CARTESIAN_POINT ( 'NONE',  ( 119.2063748109119814, -1.561330072975668504, -17.79121239304076951 ) ) ;
#6368=CARTESIAN_POINT ( 'NONE',  ( 114.4980614775786592, -7.893985811506177619, -18.51759400769804742 ) ) ;
#6370=CARTESIAN_POINT ( 'NONE',  ( 122.1561614775786353, -0.4660016031367893996, -10.09054647747474043 ) ) ;
#6373=DIRECTION ( 'NONE',  ( 1.000000000000000000, 0.000000000000000000, 0.000000000000000000 ) ) ;
#6376=CARTESIAN_POINT ( 'NONE',  ( 115.8595014775786609, -7.643976991954077427, -18.09477374809248928 ) ) ;
#6378=EDGE_CURVE ( 'NONE', #7925, #23072, #37240, .T. ) ;
#6380=CARTESIAN_POINT ( 'NONE',  ( 117.2776681442452968, -4.153390946401325223, -8.397313243818185668 ) ) ;
#6382=CARTESIAN_POINT ( 'NONE',  ( 116.8805814775786445, -3.505236298600246325, -18.68346056562440793 ) ) ;
#6383=CARTESIAN_POINT ( 'NONE',  ( 115.0653281442453277, -6.344957434206662583, -7.627207830600332805 ) ) ;
#6385=CARTESIAN_POINT ( 'NONE',  ( 112.4559014775786494, -9.988377603198976828, -10.36322818467138340 ) ) ;
#6386=CARTESIAN_POINT ( 'NONE',  ( 115.3489614775786407, -0.8288870151387760510, -10.36305467784173118 ) ) ;
#6387=CARTESIAN_POINT ( 'NONE',  ( 112.0020881442453344, -9.565557343593413364, -10.61323700422348004 ) ) ;
#6389=CARTESIAN_POINT ( 'NONE',  ( 115.2355081442453155, 0.1319031606808879209, -14.10382304977623669 ) ) ;
#6391=CARTESIAN_POINT ( 'NONE',  ( 113.8740681442453138, 0.5811942927096154232, -14.16772938898807155 ) ) ;
#6395=B_SPLINE_CURVE_WITH_KNOTS ( 'NONE', 3,
 ( #23092, #26286, #22860, #12615, #36752, #5521, #19441, #33324, #2098, #29933 ),
 .UNSPECIFIED., .F., .F.,
 ( 4, 3, 3, 4 ),
 ( 0.000000000000000000, 0.0001671877560958114864, 0.0003343755126086574896, 0.0006438490228507209303 ),
 .UNSPECIFIED. ) ;
#6397=CARTESIAN_POINT ( 'NONE',  ( 118.6958348109119754, -6.344957434206665248, -7.627207830600338134 ) ) ;
#6399=CARTESIAN_POINT ( 'NONE',  ( 125.5597614775786326, -1.561330072975669392, -17.79121239304076951 ) ) ;
#6400=CARTESIAN_POINT ( 'NONE',  ( 125.1059481442452750, -8.166667518702794837, -8.995218007635845225 ) ) ;
#6401=CARTESIAN_POINT ( 'NONE',  ( 116.8805814775786445, -3.505236298600246325, -18.68346056562440793 ) ) ;
#6402=CARTESIAN_POINT ( 'NONE',  ( 124.5386814775786206, -4.153390946401287032, -8.397313243818187445 ) ) ;
#6403=CARTESIAN_POINT ( 'NONE',  ( 124.9924948109119924, -4.089484607189486809, -7.948022111789456723 ) ) ;
#6407=CARTESIAN_POINT ( 'NONE',  ( 111.9261565460471957, -2.191907684172563986, -18.20049396185734025 ) ) ;
#6408=CARTESIAN_POINT ( 'NONE',  ( 123.2339681442453241, -3.505236298600246325, -18.68346056562440793 ) ) ;
#6409=CARTESIAN_POINT ( 'NONE',  ( 118.2987481442453088, -1.561330072975668504, -17.79121239304076951 ) ) ;
#6411=CARTESIAN_POINT ( 'NONE',  ( 117.9016614775786280, -0.1624402480850797581, -16.17319339645315424 ) ) ;
#6412=CARTESIAN_POINT ( 'NONE',  ( 117.9583881442453048, -10.30919188438810075, -12.61870101168855918 ) ) ;
#6413=CARTESIAN_POINT ( 'NONE',  ( 123.4041481442452834, 0.1319031606808844515, -14.10382304977626511 ) ) ;
#6414=CARTESIAN_POINT ( 'NONE',  ( 126.4536383592487141, -1.145462627196077721, -9.876933969119310319 ) ) ;
#6415=CARTESIAN_POINT ( 'NONE',  ( 124.1983214775786166, -1.833838273342659697, -17.42832698103878286 ) ) ;
#6419=CARTESIAN_POINT ( 'NONE',  ( 115.3489614775786407, -9.261995988541697145, -16.69588392320189030 ) ) ;
#6420=CARTESIAN_POINT ( 'NONE',  ( 121.1350814775786233, -9.859900752359378018, -12.68260735090039759 ) ) ;
#6424=CARTESIAN_POINT ( 'NONE',  ( 137.2618751061050375, -0.2068468655711039328, -10.95876972476207989 ) ) ;
#6425=CARTESIAN_POINT ( 'NONE',  ( 119.7169148109119874, -9.988377603198976828, -10.36322818467138340 ) ) ;
#6427=CARTESIAN_POINT ( 'NONE',  ( 120.2274548109119934, -9.859900752359374465, -12.68260735090039404 ) ) ;
#6430=CARTESIAN_POINT ( 'NONE',  ( 126.4106614775786284, -6.222761293078241884, -8.102969835052219238 ) ) ;
#6431=CARTESIAN_POINT ( 'NONE',  ( 124.4819548109119722, -2.084020599724406786, -8.691656652584148546 ) ) ;
#6435=CARTESIAN_POINT ( 'NONE',  ( 120.3409081442453044, -0.4660016031367893996, -10.09054647747474043 ) ) ;
#6440=CARTESIAN_POINT ( 'NONE',  ( 120.7947214775786193, -9.261995988541697145, -16.69588392320189030 ) ) ;
#6441=CARTESIAN_POINT ( 'NONE',  ( 117.1642148109119859, -9.261995988541697145, -16.69588392320189030 ) ) ;
#6442=CARTESIAN_POINT ( 'NONE',  ( 120.0572748109119772, -6.222761293078241884, -8.102969835052219238 ) ) ;
#6444=CARTESIAN_POINT ( 'NONE',  ( 125.5030348109119558, -6.222761293078241884, -8.102969835052219238 ) ) ;
#6445=CARTESIAN_POINT ( 'NONE',  ( 112.3991748109119868, -8.166667518702817929, -8.995218007635859436 ) ) ;
#6447=CARTESIAN_POINT ( 'NONE',  ( 122.3830681442452857, -1.833838273342659697, -17.42832698103878286 ) ) ;
#6452=CARTESIAN_POINT ( 'NONE',  ( 122.8368814775786291, -1.561330072975668948, -17.79121239304076951 ) ) ;
#6453=CARTESIAN_POINT ( 'NONE',  ( 122.8936081442453059, -9.565557343593413364, -10.61323700422348004 ) ) ;
#6455=CARTESIAN_POINT ( 'NONE',  ( 122.8936081442453059, 0.2603800115204892296, -16.42320221600525088 ) ) ;
#6457=CARTESIAN_POINT ( 'NONE',  ( 125.3328548109119964, -9.261995988541697145, -16.69588392320189030 ) ) ;
#6458=CARTESIAN_POINT ( 'NONE',  ( 121.7590748109119687, -7.893985811506177619, -18.51759400769804742 ) ) ;
#6460=CARTESIAN_POINT ( 'NONE',  ( 112.1722681442453222, -0.4660016031367893996, -10.09054647747474043 ) ) ;
#6463=ORIENTED_EDGE ( 'NONE', *, *, #26706, .T. ) ;
#6464=CARTESIAN_POINT ( 'NONE',  ( 124.9401836525450022, -2.378957183258596064, -17.95140958770220863 ) ) ;
#6465=CARTESIAN_POINT ( 'NONE',  ( 118.6557253070358939, -1.196538596002800103, -17.02799684832027083 ) ) ;
#6466=CARTESIAN_POINT ( 'NONE',  ( 123.0070614775786169, -10.15424416112533912, -14.75197769757731336 ) ) ;
#6469=CARTESIAN_POINT ( 'NONE',  ( 122.9503348109119827, -9.859900752359378018, -12.68260735090039759 ) ) ;
#6470=CARTESIAN_POINT ( 'NONE',  ( 115.7460481442453357, -10.15424416112533912, -14.75197769757731336 ) ) ;
#6471=CARTESIAN_POINT ( 'NONE',  ( 123.9146881442452894, 0.9020085738987339008, -11.91225656197089222 ) ) ;
#6473=CARTESIAN_POINT ( 'NONE',  ( 123.2906948109119867, -1.833838273342659697, -17.42832698103878286 ) ) ;
#6474=CARTESIAN_POINT ( 'NONE',  ( 118.3554748109119998, 0.2603800115204892296, -16.42320221600525088 ) ) ;
#6477=DIRECTION ( 'NONE',  ( 1.000000000000000000, 0.000000000000000000, 0.000000000000000000 ) ) ;
#6480=CARTESIAN_POINT ( 'NONE',  ( 113.6471614775786492, -4.153390946401321671, -8.397313243818183892 ) ) ;
#6481=CARTESIAN_POINT ( 'NONE',  ( 113.9307948109119764, -10.15424416112533912, -14.75197769757731336 ) ) ;
#6482=CARTESIAN_POINT ( 'NONE',  ( 115.1010702440515558, -2.467220198592777525, -17.83387418641524391 ) ) ;
#6490=CARTESIAN_POINT ( 'NONE',  ( 121.7023481442452919, -0.8288870151387760510, -10.36305467784173118 ) ) ;
#6491=CARTESIAN_POINT ( 'NONE',  ( 113.9307948109119764, -10.15424416112533912, -14.75197769757731336 ) ) ;
#6492=CARTESIAN_POINT ( 'NONE',  ( 126.2450673757166442, -5.764848433121719573, -18.32501366739699122 ) ) ;
#6494=CARTESIAN_POINT ( 'NONE',  ( 124.8790414775786246, -8.899110576539426276, -16.42337572283528146 ) ) ;
#6500=CARTESIAN_POINT ( 'NONE',  ( 126.1270281442452870, 0.1319031606808879209, -14.10382304977623669 ) ) ;
#6502=CARTESIAN_POINT ( 'NONE',  ( 114.2711548109119803, -9.988377603198976828, -10.36322818467138340 ) ) ;
#6506=CARTESIAN_POINT ( 'NONE',  ( 125.3895814775786448, -2.084020599724406786, -8.691656652584148546 ) ) ;
#6507=CARTESIAN_POINT ( 'NONE',  ( 123.5176014775786228, -0.8288870151387760510, -10.36305467784173118 ) ) ;
#6512=CARTESIAN_POINT ( 'NONE',  ( 112.9664414775786412, -9.859900752359374465, -12.68260735090039404 ) ) ;
#6516=CARTESIAN_POINT ( 'NONE',  ( 123.7445081442452874, -1.561330072975668948, -17.79121239304076951 ) ) ;
#6517=CARTESIAN_POINT ( 'NONE',  ( 125.2194014775786286, -10.30919188438810075, -12.61870101168855918 ) ) ;
#6519=CARTESIAN_POINT ( 'NONE',  ( 120.5110881442453206, -6.344957434206665248, -7.627207830600338134 ) ) ;
#6520=CARTESIAN_POINT ( 'NONE',  ( 112.3424481442453384, -6.344957434206662583, -7.627207830600332805 ) ) ;
#6522=CARTESIAN_POINT ( 'NONE',  ( 114.0442481442453300, -7.643976991954077427, -18.09477374809248928 ) ) ;
#6523=CARTESIAN_POINT ( 'NONE',  ( 124.9924948109119924, -4.089484607189486809, -7.948022111789456723 ) ) ;
#6524=CARTESIAN_POINT ( 'NONE',  ( 122.8936081442453059, 0.2603800115204892296, -16.42320221600525088 ) ) ;
#6525=CARTESIAN_POINT ( 'NONE',  ( 114.9518748109119883, -1.834011780172310813, -8.268836392978581529 ) ) ;
#6526=CARTESIAN_POINT ( 'NONE',  ( 113.2500748109119968, -3.505236298600246325, -18.68346056562440793 ) ) ;
#6528=CARTESIAN_POINT ( 'NONE',  ( 118.7525614775786380, -1.833838273342659253, -17.42832698103878286 ) ) ;
#6530=CARTESIAN_POINT ( 'NONE',  ( 125.1626748109119802, -0.1624402480850797581, -16.17319339645315424 ) ) ;
#6536=CARTESIAN_POINT ( 'NONE',  ( 126.0135748109119902, -8.166667518702819706, -8.995218007635861213 ) ) ;
#6545=CARTESIAN_POINT ( 'NONE',  ( 116.8805814775786445, -6.344957434206662583, -7.627207830600332805 ) ) ;
#6546=CARTESIAN_POINT ( 'NONE',  ( 137.4783527756549972, -5.189670303016769459, -18.42458730202076467 ) ) ;
#6548=CARTESIAN_POINT ( 'NONE',  ( 119.0361948109119794, -7.893985811506194494, -18.51759400769804031 ) ) ;
#6549=CARTESIAN_POINT ( 'NONE',  ( 119.6034614775786196, -3.505236298600246325, -18.68346056562440793 ) ) ;
#6552=CARTESIAN_POINT ( 'NONE',  ( 117.7314814775786260, -4.089484607189486809, -7.948022111789456723 ) ) ;
#6554=CARTESIAN_POINT ( 'NONE',  ( 113.9307948109119764, -10.15424416112533912, -14.75197769757731336 ) ) ;
#6555=CARTESIAN_POINT ( 'NONE',  ( 111.5482748109120053, -0.1624402480850797581, -16.17319339645315424 ) ) ;
#6559=CARTESIAN_POINT ( 'NONE',  ( 116.7671281442453335, -7.643976991954077427, -18.09477374809248928 ) ) ;
#6560=CARTESIAN_POINT ( 'NONE',  ( 119.2063748109119814, -7.894159318335828068, -9.358103419637847864 ) ) ;
#6563=B_SPLINE_CURVE_WITH_KNOTS ( 'NONE', 3,
 ( #2802, #3032, #13752, #26758, #44770, #20596, #40667, #44540, #27437, #44993 ),
 .UNSPECIFIED., .F., .F.,
 ( 4, 3, 3, 4 ),
 ( 0.000000000000000000, 0.0001671877560958075020, 0.0003343755126086529902, 0.0006438490228507220145 ),
 .UNSPECIFIED. ) ;
#6567=CARTESIAN_POINT ( 'NONE',  ( 115.2922348109119781, -10.63000616557722466, -14.87417383870573495 ) ) ;
#6572=CARTESIAN_POINT ( 'NONE',  ( 123.4699442700021308, -2.835955651089761442, -14.84486572726433806 ) ) ;
#6574=CARTESIAN_POINT ( 'NONE',  ( 123.7445081442452874, -1.561330072975668948, -17.79121239304076951 ) ) ;
#6576=CARTESIAN_POINT ( 'NONE',  ( 112.7962614775786676, -3.383040157471821630, -19.15922257007629170 ) ) ;
#6577=CARTESIAN_POINT ( 'NONE',  ( 119.0929214775786278, -4.153390946401325223, -8.397313243818185668 ) ) ;
#6580=CARTESIAN_POINT ( 'NONE',  ( 122.0427081442452817, 0.5811942927096110934, -14.16772938898807510 ) ) ;
#6581=CARTESIAN_POINT ( 'NONE',  ( 118.6958348109119754, -6.344957434206665248, -7.627207830600338134 ) ) ;
#6583=CARTESIAN_POINT ( 'NONE',  ( 114.1577014775786552, -3.505236298600246325, -18.68346056562440793 ) ) ;
#6586=CARTESIAN_POINT ( 'NONE',  ( 118.2420214775786320, -3.383040157471821630, -19.15922257007629170 ) ) ;
#6589=CARTESIAN_POINT ( 'NONE',  ( 114.3278814775786429, -10.30919188438810075, -12.61870101168855918 ) ) ;
#6591=CARTESIAN_POINT ( 'NONE',  ( 123.8579614775786126, 0.5811942927096110934, -14.16772938898807510 ) ) ;
#6594=CARTESIAN_POINT ( 'NONE',  ( 113.9307948109119764, -10.15424416112533912, -14.75197769757731336 ) ) ;
#6597=CARTESIAN_POINT ( 'NONE',  ( 115.5191414775786569, -6.222761293078241884, -8.102969835052219238 ) ) ;
#6600=CARTESIAN_POINT ( 'NONE',  ( 119.5467348109119712, -5.574606645277164318, -18.38911715685844683 ) ) ;
#6603=CARTESIAN_POINT ( 'NONE',  ( 117.4478481442453131, -9.565557343593413364, -10.61323700422348004 ) ) ;
#6606=CARTESIAN_POINT ( 'NONE',  ( 115.4624148109119943, -5.638512984488999180, -18.83840828888717311 ) ) ;
#6607=CARTESIAN_POINT ( 'NONE',  ( 113.5904348109119866, -2.084020599724406786, -8.691656652584148546 ) ) ;
#6608=CARTESIAN_POINT ( 'NONE',  ( 118.5256548109119876, -8.899110576539710493, -16.42337572283490132 ) ) ;
#6610=CARTESIAN_POINT ( 'NONE',  ( 114.8951481442453115, -0.4660016031367893996, -10.09054647747474043 ) ) ;
#6614=CARTESIAN_POINT ( 'NONE',  ( 110.8846330289902369, -1.498564202500827669, -16.62580459685196743 ) ) ;
#6616=CARTESIAN_POINT ( 'NONE',  ( 123.1772414775786189, -4.089484607189486809, -7.948022111789456723 ) ) ;
#6619=CARTESIAN_POINT ( 'NONE',  ( 117.6180281442453150, -8.899110576539710493, -16.42337572283490132 ) ) ;
#6620=CARTESIAN_POINT ( 'NONE',  ( 124.5954081442453116, -6.222761293078269418, -8.102969835052228120 ) ) ;
#6621=CARTESIAN_POINT ( 'NONE',  ( 121.8725281442453223, -3.383040157471821630, -19.15922257007629170 ) ) ;
#6626=CARTESIAN_POINT ( 'NONE',  ( 126.5241148109119393, -9.565557343593413364, -10.61323700422348004 ) ) ;
#6627=CARTESIAN_POINT ( 'NONE',  ( 124.2550481442452792, -9.988377603198980381, -10.36322818467138518 ) ) ;
#6629=CARTESIAN_POINT ( 'NONE',  ( 117.5045748109119756, -9.859900752359374465, -12.68260735090039404 ) ) ;
#6631=CARTESIAN_POINT ( 'NONE',  ( 118.2420214775786320, -3.383040157471821630, -19.15922257007629170 ) ) ;
#6634=CARTESIAN_POINT ( 'NONE',  ( 126.9115046738272241, -1.250902631998696668, -9.451862355402859350 ) ) ;
#6635=CARTESIAN_POINT ( 'NONE',  ( 123.1205148109119563, -7.643976991954077427, -18.09477374809248928 ) ) ;
#6637=EDGE_CURVE ( 'NONE', #43185, #21157, #15105, .T. ) ;
#6641=CARTESIAN_POINT ( 'NONE',  ( 117.3911214775786505, -1.561330072975668504, -17.79121239304076951 ) ) ;
#6642=CARTESIAN_POINT ( 'NONE',  ( 135.4522060580516438, -8.536173890036971912, -18.13819535414095085 ) ) ;
#6647=CARTESIAN_POINT ( 'NONE',  ( 123.6310548109119765, -5.638512984488999180, -18.83840828888717311 ) ) ;
#6649=CARTESIAN_POINT ( 'NONE',  ( 120.5678148109119832, -1.833838273342659253, -17.42832698103878286 ) ) ;
#6652=CARTESIAN_POINT ( 'NONE',  ( 124.1415948109119540, -3.505236298600246325, -18.68346056562440793 ) ) ;
#6653=CARTESIAN_POINT ( 'NONE',  ( 124.5954081442453116, -6.222761293078241884, -8.102969835052219238 ) ) ;
#6655=CARTESIAN_POINT ( 'NONE',  ( 135.3184548109119874, -4.863998795839242995, -13.39321520033831447 ) ) ;
#6656=CARTESIAN_POINT ( 'NONE',  ( 121.6456214775786293, -10.63000616557722466, -14.87417383870573495 ) ) ;
#6661=CARTESIAN_POINT ( 'NONE',  ( 119.0361948109119652, -7.893985811506177619, -18.51759400769804742 ) ) ;
#6662=CARTESIAN_POINT ( 'NONE',  ( 118.0151148109119816, -10.63000616557722466, -14.87417383870573495 ) ) ;
#6663=CARTESIAN_POINT ( 'NONE',  ( 121.3619881442452879, -5.574606645277164318, -18.38911715685844683 ) ) ;
#6664=CARTESIAN_POINT ( 'NONE',  ( 123.3474214775786209, -0.1624402480850797581, -16.17319339645315424 ) ) ;
#6665=CARTESIAN_POINT ( 'NONE',  ( 115.4624148109119943, -5.638512984488999180, -18.83840828888717311 ) ) ;
#6668=CARTESIAN_POINT ( 'NONE',  ( 112.7962614775786676, -3.383040157471821630, -19.15922257007629170 ) ) ;
#6670=CARTESIAN_POINT ( 'NONE',  ( 125.3223148109119904, 0.3778260857404745487, -12.04688916545782185 ) ) ;
#6675=CARTESIAN_POINT ( 'NONE',  ( 120.7947214775786193, -9.261995988541697145, -16.69588392320189030 ) ) ;
#6676=CARTESIAN_POINT ( 'NONE',  ( 124.1415948109119540, -3.505236298600246325, -18.68346056562440793 ) ) ;
#6678=CARTESIAN_POINT ( 'NONE',  ( 125.3328548109119964, -9.261995988541697145, -16.69588392320189030 ) ) ;
#6681=CARTESIAN_POINT ( 'NONE',  ( 122.3263414775786373, -6.344957434206665248, -7.627207830600338134 ) ) ;
#6682=CARTESIAN_POINT ( 'NONE',  ( 126.0703014775786102, -9.988377603198980381, -10.36322818467138518 ) ) ;
#6684=CARTESIAN_POINT ( 'NONE',  ( 113.5904348109119866, -7.893985811506177619, -18.51759400769804742 ) ) ;
#6689=CARTESIAN_POINT ( 'NONE',  ( 112.3424481442453384, -3.505236298600246325, -18.68346056562440793 ) ) ;
#6690=CARTESIAN_POINT ( 'NONE',  ( 112.1722681442453222, -0.4660016031367893996, -10.09054647747474043 ) ) ;
#6694=CARTESIAN_POINT ( 'NONE',  ( 123.2906948109119867, -1.833838273342659697, -17.42832698103878286 ) ) ;
#6695=CARTESIAN_POINT ( 'NONE',  ( 116.6536748109119941, -10.15424416112533912, -14.75197769757731336 ) ) ;
#6696=CARTESIAN_POINT ( 'NONE',  ( 113.6471614775786492, -4.153390946401321671, -8.397313243818183892 ) ) ;
#6701=CARTESIAN_POINT ( 'NONE',  ( 119.6034614775786196, -6.344957434206665248, -7.627207830600338134 ) ) ;
#6708=CARTESIAN_POINT ( 'NONE',  ( 115.9729548109119861, -3.505236298600246325, -18.68346056562440793 ) ) ;
#6709=CARTESIAN_POINT ( 'NONE',  ( 112.9664414775786412, -9.859900752359374465, -12.68260735090039404 ) ) ;
#6710=CARTESIAN_POINT ( 'NONE',  ( 114.7356558072985564, 0.3208234527006404435, -15.99825685930877661 ) ) ;
#6717=CARTESIAN_POINT ( 'NONE',  ( 122.4397948109119767, -0.1624402480850797581, -16.17319339645315424 ) ) ;
#6718=CARTESIAN_POINT ( 'NONE',  ( 114.6682414775786469, -7.894159318335828068, -9.358103419637847864 ) ) ;
#6719=CARTESIAN_POINT ( 'NONE',  ( 119.9375029525735670, -1.111561923218657322, -17.14115599315433158 ) ) ;
#6722=CARTESIAN_POINT ( 'NONE',  ( 112.7395348109119766, -4.153390946401321671, -8.397313243818183892 ) ) ;
#6723=CARTESIAN_POINT ( 'NONE',  ( 122.4799043147880440, -2.395992375830759524, -17.92872468182853396 ) ) ;
#6727=CARTESIAN_POINT ( 'NONE',  ( 126.1270281442452870, -10.30919188438810075, -12.61870101168855918 ) ) ;
#6728=CARTESIAN_POINT ( 'NONE',  ( 125.6164881442453094, -9.565557343593413364, -10.61323700422348004 ) ) ;
#6730=ORIENTED_EDGE ( 'NONE', *, *, #24760, .F. ) ;
#6731=CARTESIAN_POINT ( 'NONE',  ( 113.8173414775786512, 0.2603800115204892296, -16.42320221600525088 ) ) ;
#6735=CARTESIAN_POINT ( 'NONE',  ( 126.2972081442452890, -2.084020599724406786, -8.691656652584148546 ) ) ;
#6736=CARTESIAN_POINT ( 'NONE',  ( 124.7088614775786226, -9.565557343593413364, -10.61323700422348004 ) ) ;
#6737=CARTESIAN_POINT ( 'NONE',  ( 124.9252281442453096, -8.862178061932084461, -16.39564131203287545 ) ) ;
#6742=CARTESIAN_POINT ( 'NONE',  ( 114.2711548109119803, -0.1624402480850797581, -16.17319339645315424 ) ) ;
#6746=CARTESIAN_POINT ( 'NONE',  ( 124.4252281442452812, -9.261995988541697145, -16.69588392320189030 ) ) ;
#6747=CARTESIAN_POINT ( 'NONE',  ( 112.3424481442453384, -3.505236298600246325, -18.68346056562440793 ) ) ;
#6749=CARTESIAN_POINT ( 'NONE',  ( 120.4543614775786295, -4.089484607189486809, -7.948022111789456723 ) ) ;
#6750=CARTESIAN_POINT ( 'NONE',  ( 115.2922348109119781, -10.63000616557722466, -14.87417383870573495 ) ) ;
#6752=CARTESIAN_POINT ( 'NONE',  ( 113.9307948109119764, -10.15424416112533912, -14.75197769757731336 ) ) ;
#6753=CARTESIAN_POINT ( 'NONE',  ( 123.7445081442452874, -1.561330072975668948, -17.79121239304076951 ) ) ;
#6754=CARTESIAN_POINT ( 'NONE',  ( 114.5547881442453217, -5.638512984488999180, -18.83840828888717311 ) ) ;
#6755=CARTESIAN_POINT ( 'NONE',  ( 116.3700414775786527, -4.153390946401321671, -8.397313243818183892 ) ) ;
#6756=VERTEX_POINT ( 'NONE', #8114 ) ;
#6757=EDGE_CURVE ( 'NONE', #17138, #14254, #33931, .T. ) ;
#6758=CARTESIAN_POINT ( 'NONE',  ( 116.5969481442453031, -9.859900752359374465, -12.68260735090039404 ) ) ;
#6761=CARTESIAN_POINT ( 'NONE',  ( 115.4624148109119943, -5.638512984488999180, -18.83840828888717311 ) ) ;
#6762=CARTESIAN_POINT ( 'NONE',  ( 124.7088614775786226, -9.565557343593413364, -10.61323700422348004 ) ) ;
#6766=CARTESIAN_POINT ( 'NONE',  ( 128.2184548109119930, -4.863998795839242995, -13.39321520033831447 ) ) ;
#6767=CARTESIAN_POINT ( 'NONE',  ( 126.2404814775786264, -9.261995988541697145, -16.69588392320189030 ) ) ;
#6769=FACE_OUTER_BOUND ( 'NONE', #5355, .T. ) ;
#6771=CARTESIAN_POINT ( 'NONE',  ( 113.0231681442453180, -10.15424416112533912, -14.75197769757731336 ) ) ;
#6773=CARTESIAN_POINT ( 'NONE',  ( 123.1545820330015317, -1.172797794773259072, -17.05961127468926719 ) ) ;
#6775=CARTESIAN_POINT ( 'NONE',  ( 118.3554748109119998, 0.2603800115204892296, -16.42320221600525088 ) ) ;
#6776=CARTESIAN_POINT ( 'NONE',  ( 136.9861655118718886, -4.492900143882628150, -18.85368254081607375 ) ) ;
#6779=CARTESIAN_POINT ( 'NONE',  ( 121.0216281442452981, -7.894159318335828068, -9.358103419637847864 ) ) ;
#6781=CARTESIAN_POINT ( 'NONE',  ( 126.0135748109119902, -8.166667518702819706, -8.995218007635861213 ) ) ;
#6782=CARTESIAN_POINT ( 'NONE',  ( 118.3554748109119998, 0.2603800115204892296, -16.42320221600525088 ) ) ;
#6784=CARTESIAN_POINT ( 'NONE',  ( 117.2209414775786485, -2.084020599724406786, -8.691656652584148546 ) ) ;
#6785=CIRCLE ( 'NONE', #12614, 1.499999999999999334 ) ;
#6786=CARTESIAN_POINT ( 'NONE',  ( 112.5126281442453120, 0.1319031606808879209, -14.10382304977623669 ) ) ;
#6790=CARTESIAN_POINT ( 'NONE',  ( 115.0086014775786509, -5.574606645277164318, -18.38911715685844683 ) ) ;
#6792=CARTESIAN_POINT ( 'NONE',  ( 121.4754414775786131, -1.833838273342659697, -17.42832698103878286 ) ) ;
#6797=CARTESIAN_POINT ( 'NONE',  ( 115.5758681442453053, -1.561330072975668060, -17.79121239304076951 ) ) ;
#6798=CARTESIAN_POINT ( 'NONE',  ( 114.9518748109119883, -1.834011780172310813, -8.268836392978581529 ) ) ;
#6801=CARTESIAN_POINT ( 'NONE',  ( 123.6849955490782804, -3.391418706753638546, -14.10518582020394618 ) ) ;
#6803=CARTESIAN_POINT ( 'NONE',  ( 122.2696148109119889, -4.089484607189486809, -7.948022111789456723 ) ) ;
#6804=CARTESIAN_POINT ( 'NONE',  ( 111.8319081442453182, -5.638512984488999180, -18.83840828888717311 ) ) ;
#6806=CARTESIAN_POINT ( 'NONE',  ( 118.6391081442452986, -5.574606645277164318, -18.38911715685844683 ) ) ;
#6807=SURFACE_SIDE_STYLE ('',( #397 ) ) ;
#6809=CARTESIAN_POINT ( 'NONE',  ( 122.1561614775786353, -0.4660016031367893996, -10.09054647747474043 ) ) ;
#6810=CARTESIAN_POINT ( 'NONE',  ( 116.6536748109119941, 0.9020085738987339008, -11.91225656197089222 ) ) ;
#6812=CARTESIAN_POINT ( 'NONE',  ( 113.2500748109119968, -3.505236298600246325, -18.68346056562440793 ) ) ;
#6813=DIRECTION ( 'NONE',  ( 1.000000000000000000, 0.000000000000000000, 0.000000000000000000 ) ) ;
#6814=ORIENTED_EDGE ( 'NONE', *, *, #23941, .F. ) ;
#6815=CARTESIAN_POINT ( 'NONE',  ( 118.4689281442453392, 0.9020085738987339008, -11.91225656197089222 ) ) ;
#6818=CARTESIAN_POINT ( 'NONE',  ( 116.5402214775786405, 0.2603800115204892296, -16.42320221600525088 ) ) ;
#6821=CIRCLE ( 'NONE', #12652, 5.999999999999997335 ) ;
#6822=CARTESIAN_POINT ( 'NONE',  ( 125.2194014775786286, -10.30919188438810075, -12.61870101168855918 ) ) ;
#6827=CARTESIAN_POINT ( 'NONE',  ( 116.4267681442453153, -6.222761293078241884, -8.102969835052219238 ) ) ;
#6829=CARTESIAN_POINT ( 'NONE',  ( 117.6747548109119919, -7.643976991954077427, -18.09477374809248928 ) ) ;
#6832=CARTESIAN_POINT ( 'NONE',  ( 120.4543614775786295, -5.574606645277164318, -18.38911715685844683 ) ) ;
#6834=CARTESIAN_POINT ( 'NONE',  ( 115.4056881442453459, -7.893985811506177619, -18.51759400769804742 ) ) ;
#6835=CARTESIAN_POINT ( 'NONE',  ( 125.7866681442452688, -0.4660016031367893996, -10.09054647747474043 ) ) ;
#6836=CARTESIAN_POINT ( 'NONE',  ( 116.1998614775786507, 0.4262465694468514643, -12.03445270309931736 ) ) ;
#6838=CARTESIAN_POINT ( 'NONE',  ( 115.4624148109119943, -5.638512984488999180, -18.83840828888717311 ) ) ;
#6843=CARTESIAN_POINT ( 'NONE',  ( 120.8514481442452961, -7.893985811506177619, -18.51759400769804742 ) ) ;
#6845=CARTESIAN_POINT ( 'NONE',  ( 118.4361142721482878, -2.287189184988681401, -18.07361239780446738 ) ) ;
#6846=CARTESIAN_POINT ( 'NONE',  ( 118.4122014775786340, -9.859900752359374465, -12.68260735090039404 ) ) ;
#6848=CARTESIAN_POINT ( 'NONE',  ( 121.6456214775786293, -10.63000616557722466, -14.87417383870573495 ) ) ;
#6853=CARTESIAN_POINT ( 'NONE',  ( 113.0798948109119948, -0.4660016031367893996, -10.09054647747474043 ) ) ;
#6854=CARTESIAN_POINT ( 'NONE',  ( 112.2289948109119848, -1.834011780172310813, -8.268836392978581529 ) ) ;
#6855=CARTESIAN_POINT ( 'NONE',  ( 123.6310548109119765, -5.638512984488999180, -18.83840828888717311 ) ) ;
#6856=CARTESIAN_POINT ( 'NONE',  ( 118.2420214775786320, -6.222761293078241884, -8.102969835052219238 ) ) ;
#6858=CARTESIAN_POINT ( 'NONE',  ( 118.8660148109119774, -10.30919188438810075, -12.61870101168855918 ) ) ;
#6860=CARTESIAN_POINT ( 'NONE',  ( 122.6667014775786413, -2.084020599724406786, -8.691656652584148546 ) ) ;
#6863=CARTESIAN_POINT ( 'NONE',  ( 115.9162281442453235, -4.089484607189486809, -7.948022111789456723 ) ) ;
#6864=CARTESIAN_POINT ( 'NONE',  ( 136.0320772899191297, -8.512149301715753680, -18.04415937378387724 ) ) ;
#6868=CARTESIAN_POINT ( 'NONE',  ( 123.9146881442452894, 0.9020085738987339008, -11.91225656197089222 ) ) ;
#6870=CARTESIAN_POINT ( 'NONE',  ( 119.9438214775786378, -2.084020599724406786, -8.691656652584148546 ) ) ;
#6873=CARTESIAN_POINT ( 'NONE',  ( 113.1933481442453058, -4.089484607189486809, -7.948022111789456723 ) ) ;
#6874=CARTESIAN_POINT ( 'NONE',  ( 123.2339681442453241, -3.505236298600246325, -18.68346056562440793 ) ) ;
#6877=CARTESIAN_POINT ( 'NONE',  ( 123.0637881442452937, -0.4660016031367893996, -10.09054647747474043 ) ) ;
#6880=CARTESIAN_POINT ( 'NONE',  ( 120.2274548109119934, 0.5811942927096110934, -14.16772938898807510 ) ) ;
#6881=CARTESIAN_POINT ( 'NONE',  ( 119.7736414775786358, -10.30919188438810075, -12.61870101168855918 ) ) ;
#6882=CARTESIAN_POINT ( 'NONE',  ( 120.7379948109119709, 0.4262465694468514643, -12.03445270309931736 ) ) ;
#6884=CARTESIAN_POINT ( 'NONE',  ( 115.3489614775786407, -9.261995988541697145, -16.69588392320189030 ) ) ;
#6887=CARTESIAN_POINT ( 'NONE',  ( 125.2761281442453338, 0.4262465694465857324, -12.03445270309828175 ) ) ;
#6892=CARTESIAN_POINT ( 'NONE',  ( 113.3068014775786594, -8.166667518702817929, -8.995218007635859436 ) ) ;
#6894=CARTESIAN_POINT ( 'NONE',  ( 122.7801548109119665, -3.383040157471821630, -19.15922257007629170 ) ) ;
#6897=CARTESIAN_POINT ( 'NONE',  ( 125.4463081442452932, -5.638512984488999180, -18.83840828888717311 ) ) ;
#6898=CARTESIAN_POINT ( 'NONE',  ( 125.2194014775786286, -10.30919188438810075, -12.61870101168855918 ) ) ;
#6900=CARTESIAN_POINT ( 'NONE',  ( 113.1366214775786432, -1.834011780172310813, -8.268836392978581529 ) ) ;
#6904=EDGE_LOOP ( 'NONE', ( #6091, #35097, #32843, #26335 ) ) ;
#6906=CARTESIAN_POINT ( 'NONE',  ( 114.7249681442453237, -9.565557343593413364, -10.61323700422348004 ) ) ;
#6907=CARTESIAN_POINT ( 'NONE',  ( 113.5904348109119866, -7.893985811506177619, -18.51759400769804742 ) ) ;
#6910=CARTESIAN_POINT ( 'NONE',  ( 120.9649014775786355, -6.222761293078241884, -8.102969835052219238 ) ) ;
#6912=CARTESIAN_POINT ( 'NONE',  ( 116.7671281442453335, -7.643976991954077427, -18.09477374809248928 ) ) ;
#6913=CARTESIAN_POINT ( 'NONE',  ( 111.3213681442453264, -7.643976991954077427, -18.09477374809248928 ) ) ;
#6914=VERTEX_POINT ( 'NONE', #5126 ) ;
#6915=VECTOR ( 'NONE', #22072, 1000.000000000000114 ) ;
#6916=EDGE_CURVE ( 'NONE', #6181, #24205, #42107, .T. ) ;
#6919=CARTESIAN_POINT ( 'NONE',  ( 115.2355081442453155, 0.1319031606808879209, -14.10382304977623669 ) ) ;
#6921=CARTESIAN_POINT ( 'NONE',  ( 126.3509913982019413, -9.162490483930437080, -16.07503793292245931 ) ) ;
#6925=CARTESIAN_POINT ( 'NONE',  ( 117.7314814775786260, -5.574606645277164318, -18.38911715685844683 ) ) ;
#6926=CARTESIAN_POINT ( 'NONE',  ( 115.5758681442453053, -7.894159318335828068, -9.358103419637847864 ) ) ;
#6933=AXIS2_PLACEMENT_3D ( 'NONE', #1805, #36682, #26447 ) ;
#6937=CARTESIAN_POINT ( 'NONE',  ( 124.1415948109119540, -3.505236298600246325, -18.68346056562440793 ) ) ;
#6938=CARTESIAN_POINT ( 'NONE',  ( 118.6958348109119754, -3.505236298600246325, -18.68346056562440793 ) ) ;
#6944=VECTOR ( 'NONE', #9688, 1000.000000000000114 ) ;
#6945=CARTESIAN_POINT ( 'NONE',  ( 116.5969481442453031, -9.859900752359374465, -12.68260735090039404 ) ) ;
#6947=CARTESIAN_POINT ( 'NONE',  ( 125.0492214775786266, -6.344957434206665248, -7.627207830600338134 ) ) ;
#6948=CARTESIAN_POINT ( 'NONE',  ( 125.1059481442452750, -1.833838273342660141, -17.42832698103878286 ) ) ;
#6950=CARTESIAN_POINT ( 'NONE',  ( 112.3991748109119868, -8.166667518702817929, -8.995218007635859436 ) ) ;
#6951=CARTESIAN_POINT ( 'NONE',  ( 114.1009748109119784, -4.089484607189490362, -7.948022111789460276 ) ) ;
#6953=CARTESIAN_POINT ( 'NONE',  ( 126.2972081442452890, -2.084020599724406786, -8.691656652584148546 ) ) ;
#6954=CARTESIAN_POINT ( 'NONE',  ( 114.8951481442453115, -0.4660016031367893996, -10.09054647747474043 ) ) ;
#6955=CARTESIAN_POINT ( 'NONE',  ( 125.2194014775786286, 0.1319031606808879209, -14.10382304977623669 ) ) ;
#6958=CARTESIAN_POINT ( 'NONE',  ( 117.3237071478583573, -3.807985514183284348, -19.09877912889400520 ) ) ;
#6960=CARTESIAN_POINT ( 'NONE',  ( 118.1852948109119836, -4.153390946401325223, -8.397313243818185668 ) ) ;
#6964=CARTESIAN_POINT ( 'NONE',  ( 123.8579614775786126, 0.5811942927096110934, -14.16772938898807510 ) ) ;
#6965=CARTESIAN_POINT ( 'NONE',  ( 124.3685014775786328, -10.63000616557722466, -14.87417383870573495 ) ) ;
#6967=CARTESIAN_POINT ( 'NONE',  ( 120.5678148109119832, -8.166667518702819706, -8.995218007635861213 ) ) ;
#6968=CARTESIAN_POINT ( 'NONE',  ( 118.0151148109119816, -10.63000616557722466, -14.87417383870573495 ) ) ;
#6971=CARTESIAN_POINT ( 'NONE',  ( 115.8595014775786609, -7.643976991954077427, -18.09477374809248928 ) ) ;
#6972=CARTESIAN_POINT ( 'NONE',  ( 122.2128881442453263, -1.834011780172310813, -8.268836392978581529 ) ) ;
#6973=CARTESIAN_POINT ( 'NONE',  ( 115.5191414775786569, -3.383040157471821630, -19.15922257007629170 ) ) ;
#6974=CARTESIAN_POINT ( 'NONE',  ( 117.0507614775786465, 0.1319031606808879209, -14.10382304977623669 ) ) ;
#6976=CARTESIAN_POINT ( 'NONE',  ( 120.5110881442453206, -3.505236298600246325, -18.68346056562440793 ) ) ;
#6979=CARTESIAN_POINT ( 'NONE',  ( 118.0718414775786300, -9.261995988541697145, -16.69588392320189030 ) ) ;
#6986=CARTESIAN_POINT ( 'NONE',  ( 114.5547881442453217, -5.638512984488999180, -18.83840828888717311 ) ) ;
#6991=CARTESIAN_POINT ( 'NONE',  ( 123.3116793777725064, -1.267766418764731728, -16.93314635290706605 ) ) ;
#6993=CARTESIAN_POINT ( 'NONE',  ( 118.1852948109119836, -5.638512984488999180, -18.83840828888717311 ) ) ;
#6997=CARTESIAN_POINT ( 'NONE',  ( 121.5321681442453183, -0.1624402480850797581, -16.17319339645315424 ) ) ;
#6999=CARTESIAN_POINT ( 'NONE',  ( 124.9924948109119924, -4.089484607189486809, -7.948022111789456723 ) ) ;
#7000=ADVANCED_FACE ( 'NONE', ( #37030 ), #4849, .T. ) ;
#7001=CARTESIAN_POINT ( 'NONE',  ( 119.1496481442453046, -3.383040157471821630, -19.15922257007629170 ) ) ;
#7003=CARTESIAN_POINT ( 'NONE',  ( 116.9373081442452929, -1.833838273342659253, -17.42832698103878286 ) ) ;
#7006=CARTESIAN_POINT ( 'NONE',  ( 113.2500748109119968, -3.505236298600246325, -18.68346056562440793 ) ) ;
#7009=CARTESIAN_POINT ( 'NONE',  ( 122.0427081442452817, -9.859900752359378018, -12.68260735090039759 ) ) ;
#7010=CARTESIAN_POINT ( 'NONE',  ( 119.8303681442453126, 0.4262465694468514643, -12.03445270309931736 ) ) ;
#7015=CARTESIAN_POINT ( 'NONE',  ( 113.9875214775786532, -0.4660016031367893996, -10.09054647747474043 ) ) ;
#7016=CARTESIAN_POINT ( 'NONE',  ( 114.7816948109119863, 0.5811942927096154232, -14.16772938898807155 ) ) ;
#7020=CARTESIAN_POINT ( 'NONE',  ( 121.8158014775786171, -5.638512984488999180, -18.83840828888717311 ) ) ;
#7021=CARTESIAN_POINT ( 'NONE',  ( 113.9307948109119906, 0.9020085738987339008, -11.91225656197089222 ) ) ;
#7022=CARTESIAN_POINT ( 'NONE',  ( 117.1074881442453233, 0.4262465694468514643, -12.03445270309931736 ) ) ;
#7024=CARTESIAN_POINT ( 'NONE',  ( 126.1270281442452870, -10.30919188438810075, -12.61870101168855918 ) ) ;
#7025=CARTESIAN_POINT ( 'NONE',  ( 118.1852948109119836, -5.638512984488999180, -18.83840828888717311 ) ) ;
#7028=CARTESIAN_POINT ( 'NONE',  ( 112.7395348109119766, -4.153390946401321671, -8.397313243818183892 ) ) ;
#7031=CARTESIAN_POINT ( 'NONE',  ( 119.4900081442453086, -1.834011780172310813, -8.268836392978581529 ) ) ;
#7035=CARTESIAN_POINT ( 'NONE',  ( 117.1074881442453233, -10.63000616557722466, -14.87417383870573495 ) ) ;
#7038=CARTESIAN_POINT ( 'NONE',  ( 124.9357681442453014, -1.834011780172310813, -8.268836392978581529 ) ) ;
#7039=CARTESIAN_POINT ( 'NONE',  ( 122.1561614775786353, -0.4660016031367685829, -10.09054647747476885 ) ) ;
#7040=DIRECTION ( 'NONE',  ( 0.000000000000000000, 0.6004852223388321697, -0.7996358532186279566 ) ) ;
#7042=CARTESIAN_POINT ( 'NONE',  ( 120.2841814775786276, -10.15424416112533912, -14.75197769757731336 ) ) ;
#7044=CARTESIAN_POINT ( 'NONE',  ( 116.2565881442453133, -0.8288870151387760510, -10.36305467784173118 ) ) ;
#7047=CARTESIAN_POINT ( 'NONE',  ( 120.9649014775786355, -6.222761293078241884, -8.102969835052219238 ) ) ;
#7049=CARTESIAN_POINT ( 'NONE',  ( 116.9940348109119839, -9.988377603198976828, -10.36322818467138340 ) ) ;
#7051=CARTESIAN_POINT ( 'NONE',  ( 116.4267681442453153, -6.222761293078241884, -8.102969835052219238 ) ) ;
#7053=CARTESIAN_POINT ( 'NONE',  ( 116.0864081442453113, -9.988377603198976828, -10.36322818467138340 ) ) ;
#7055=CIRCLE ( 'NONE', #29610, 2.999999999999998668 ) ;
#7059=CARTESIAN_POINT ( 'NONE',  ( 123.9714148109119805, -0.4660016031367893996, -10.09054647747474043 ) ) ;
#7060=ORIENTED_EDGE ( 'NONE', *, *, #27562, .F. ) ;
#7061=CARTESIAN_POINT ( 'NONE',  ( 127.0400190879708049, -8.899344475176020453, -9.788696381569236493 ) ) ;
#7062=CARTESIAN_POINT ( 'NONE',  ( 116.4267681442453153, -6.222761293078241884, -8.102969835052219238 ) ) ;
#7063=CARTESIAN_POINT ( 'NONE',  ( 116.1431348109119881, -10.30919188438809542, -12.61870101168854852 ) ) ;
#7064=CARTESIAN_POINT ( 'NONE',  ( 122.6667014775786413, -7.893985811506177619, -18.51759400769804742 ) ) ;
#7068=CARTESIAN_POINT ( 'NONE',  ( 114.8951481442453115, -0.4660016031367893996, -10.09054647747474043 ) ) ;
#7069=CARTESIAN_POINT ( 'NONE',  ( 124.6521348109119884, -7.894159318335828068, -9.358103419637847864 ) ) ;
#7070=CARTESIAN_POINT ( 'NONE',  ( 123.5743281442453139, -7.893985811506177619, -18.51759400769804742 ) ) ;
#7072=CARTESIAN_POINT ( 'NONE',  ( 118.5823814775786360, -7.643976991954077427, -18.09477374809248928 ) ) ;
#7074=CARTESIAN_POINT ( 'NONE',  ( 119.3765548109119834, 0.9020085738987339008, -11.91225656197089222 ) ) ;
#7076=CARTESIAN_POINT ( 'NONE',  ( 123.6310548109119765, -4.153390946401325223, -8.397313243818185668 ) ) ;
#7077=ORIENTED_EDGE ( 'NONE', *, *, #18100, .F. ) ;
#7080=CARTESIAN_POINT ( 'NONE',  ( 115.5191414775786569, -3.383040157471821630, -19.15922257007629170 ) ) ;
#7081=CARTESIAN_POINT ( 'NONE',  ( 123.9714148109119805, -8.899110576539710493, -16.42337572283490132 ) ) ;
#7084=CARTESIAN_POINT ( 'NONE',  ( 122.6099748109119929, -9.261995988541697145, -16.69588392320189030 ) ) ;
#7086=CARTESIAN_POINT ( 'NONE',  ( 118.1285681442453068, -2.084020599724406786, -8.691656652584148546 ) ) ;
#7089=CARTESIAN_POINT ( 'NONE',  ( 114.0442481442453300, -1.834011780172310813, -8.268836392978581529 ) ) ;
#7090=CARTESIAN_POINT ( 'NONE',  ( 125.7299414775786346, -10.15424416112533912, -14.75197769757731336 ) ) ;
#7093=CARTESIAN_POINT ( 'NONE',  ( 120.7947214775786193, -9.261995988541697145, -16.69588392320189030 ) ) ;
#7097=CARTESIAN_POINT ( 'NONE',  ( 124.1983214775786166, -8.166667518702819706, -8.995218007635861213 ) ) ;
#7098=CARTESIAN_POINT ( 'NONE',  ( 120.1707281442453166, 0.2603800115204892296, -16.42320221600525088 ) ) ;
#7099=CARTESIAN_POINT ( 'NONE',  ( 124.1415948109119540, -3.505236298600246325, -18.68346056562440793 ) ) ;
#7100=CARTESIAN_POINT ( 'NONE',  ( 121.7023481442452919, -0.8288870151387760510, -10.36305467784173118 ) ) ;
#7102=CARTESIAN_POINT ( 'NONE',  ( 114.7816948109119863, 0.5811942927096154232, -14.16772938898807155 ) ) ;
#7103=ORIENTED_EDGE ( 'NONE', *, *, #23332, .T. ) ;
#7109=CARTESIAN_POINT ( 'NONE',  ( 125.0386814775786490, -5.568102603701690967, -18.34339073538286513 ) ) ;
#7110=CARTESIAN_POINT ( 'NONE',  ( 112.1155414775786454, 0.9020085738987339008, -11.91225656197089222 ) ) ;
#7112=CARTESIAN_POINT ( 'NONE',  ( 113.4769814775786330, 0.4262465694468514643, -12.03445270309931736 ) ) ;
#7115=CARTESIAN_POINT ( 'NONE',  ( 124.5954081442453116, -3.383040157471821630, -19.15922257007629170 ) ) ;
#7116=CARTESIAN_POINT ( 'NONE',  ( 123.4608748109119745, -10.63000616557722466, -14.87417383870573495 ) ) ;
#7118=CARTESIAN_POINT ( 'NONE',  ( 113.6471614775786492, -5.638512984488999180, -18.83840828888717311 ) ) ;
#7122=CARTESIAN_POINT ( 'NONE',  ( 124.7112241868944693, -2.239543233855045834, -18.13706010537467606 ) ) ;
#7123=CARTESIAN_POINT ( 'NONE',  ( 115.3489614775786407, -0.8288870151387760510, -10.36305467784173118 ) ) ;
#7124=CARTESIAN_POINT ( 'NONE',  ( 113.3068014775786594, -8.166667518702817929, -8.995218007635859436 ) ) ;
#7127=CARTESIAN_POINT ( 'NONE',  ( 122.0994348109119443, -10.15424416112533912, -14.75197769757731336 ) ) ;
#7128=CARTESIAN_POINT ( 'NONE',  ( 118.0151148109119816, 0.4262465694468514643, -12.03445270309931736 ) ) ;
#7129=CARTESIAN_POINT ( 'NONE',  ( 125.7299414775786346, 0.9020085738987339008, -11.91225656197089222 ) ) ;
#7131=CARTESIAN_POINT ( 'NONE',  ( 125.2761281442453054, 0.4262465694468514643, -12.03445270309931736 ) ) ;
#7133=CARTESIAN_POINT ( 'NONE',  ( 115.2922348109119781, 0.4262465694468514643, -12.03445270309931736 ) ) ;
#7138=CARTESIAN_POINT ( 'NONE',  ( 117.2776681442452968, -4.153390946401321671, -8.397313243818183892 ) ) ;
#7139=CARTESIAN_POINT ( 'NONE',  ( 114.1009748109119784, -5.574606645277164318, -18.38911715685844683 ) ) ;
#7146=CARTESIAN_POINT ( 'NONE',  ( 111.7184548109119788, -9.261995988541697145, -16.69588392320189030 ) ) ;
#7147=CARTESIAN_POINT ( 'NONE',  ( 121.3619881442452879, -5.574606645277164318, -18.38911715685844683 ) ) ;
#7148=CARTESIAN_POINT ( 'NONE',  ( 119.2631014775786298, -9.565557343593413364, -10.61323700422348004 ) ) ;
#7151=CARTESIAN_POINT ( 'NONE',  ( 115.8027748109119841, -8.899110576539710493, -16.42337572283490132 ) ) ;
#7153=CARTESIAN_POINT ( 'NONE',  ( 125.7866681442452688, -8.899110576539710493, -16.42337572283490132 ) ) ;
#7154=CARTESIAN_POINT ( 'NONE',  ( 125.1693226804736980, -1.293398517294378713, -16.89901338141164899 ) ) ;
#7156=CARTESIAN_POINT ( 'NONE',  ( 114.7249681442453237, 0.2603800115204892296, -16.42320221600525088 ) ) ;
#7158=CARTESIAN_POINT ( 'NONE',  ( 112.1722681442453222, -0.4660016031367893996, -10.09054647747474043 ) ) ;
#7159=CARTESIAN_POINT ( 'NONE',  ( 114.6008271478583822, -3.807985514183293230, -19.09877912889401230 ) ) ;
#7161=CARTESIAN_POINT ( 'NONE',  ( 126.4673881442452910, -7.894159318335828068, -9.358103419637847864 ) ) ;
#7162=CARTESIAN_POINT ( 'NONE',  ( 114.2711548109119803, -9.988377603198976828, -10.36322818467138340 ) ) ;
#7163=CARTESIAN_POINT ( 'NONE',  ( 123.6310548109119765, -4.153390946401325223, -8.397313243818185668 ) ) ;
#7164=EDGE_CURVE ( 'NONE', #43250, #39978, #19253, .T. ) ;
#7167=CARTESIAN_POINT ( 'NONE',  ( 112.0044508535611527, -2.239543233855026738, -18.13706010537467606 ) ) ;
#7169=CARTESIAN_POINT ( 'NONE',  ( 118.4689281442453392, -10.15424416112533912, -14.75197769757731336 ) ) ;
#7172=CARTESIAN_POINT ( 'NONE',  ( 122.4764302067644195, -1.223627541775709426, -16.99192386690442547 ) ) ;
#7174=CARTESIAN_POINT ( 'NONE',  ( 121.7527562859068837, -1.111561923218658210, -17.14115599315433158 ) ) ;
#7175=CARTESIAN_POINT ( 'NONE',  ( 124.3117748109119844, -10.30919188438810075, -12.61870101168855918 ) ) ;
#7177=CARTESIAN_POINT ( 'NONE',  ( 125.1059481442452750, -8.166667518702819706, -8.995218007635861213 ) ) ;
#7178=CARTESIAN_POINT ( 'NONE',  ( 115.9162281442453235, -4.089484607189486809, -7.948022111789456723 ) ) ;
#7180=CARTESIAN_POINT ( 'NONE',  ( 113.7038881442453402, -6.222761293078241884, -8.102969835052219238 ) ) ;
#7181=CARTESIAN_POINT ( 'NONE',  ( 111.8319081442453182, -5.638512984488999180, -18.83840828888717311 ) ) ;
#7182=CARTESIAN_POINT ( 'NONE',  ( 116.1431348109119881, -10.30919188438810075, -12.61870101168855918 ) ) ;
#7183=CARTESIAN_POINT ( 'NONE',  ( 116.8238548109119819, -5.574606645277164318, -18.38911715685844683 ) ) ;
#7186=CARTESIAN_POINT ( 'NONE',  ( 122.6667014775786413, -2.084020599724406786, -8.691656652584148546 ) ) ;
#7187=EDGE_CURVE ( 'NONE', #2634, #17999, #5653, .T. ) ;
#7189=CARTESIAN_POINT ( 'NONE',  ( 117.8449348109119938, -8.166667518702817929, -8.995218007635861213 ) ) ;
#7190=CARTESIAN_POINT ( 'NONE',  ( 136.0105862893745439, 0.5780522297147454580, -15.71516581483972352 ) ) ;
#7192=CARTESIAN_POINT ( 'NONE',  ( 114.6482964575754977, -1.016270020561755860, -17.26805140881366896 ) ) ;
#7193=CARTESIAN_POINT ( 'NONE',  ( 126.3410021428612566, 0.1890319226722280144, -13.68675727894937388 ) ) ;
#7195=CARTESIAN_POINT ( 'NONE',  ( 113.3635281442453504, -9.988377603198976828, -10.36322818467138340 ) ) ;
#7196=CARTESIAN_POINT ( 'NONE',  ( 136.9115742440160375, -10.37453544881151757, -13.81866509092029105 ) ) ;
#7197=CARTESIAN_POINT ( 'NONE',  ( 113.4202548109119846, 0.1319031606808879209, -14.10382304977623669 ) ) ;
#7199=CARTESIAN_POINT ( 'NONE',  ( 115.3602436215688414, -1.135392229370332462, -17.10942237759954665 ) ) ;
#7201=CARTESIAN_POINT ( 'NONE',  ( 116.7104014775786425, -0.4660016031367893996, -10.09054647747474043 ) ) ;
#7206=CARTESIAN_POINT ( 'NONE',  ( 113.9307948109119906, 0.9020085738987339008, -11.91225656197089222 ) ) ;
#7207=CARTESIAN_POINT ( 'NONE',  ( 124.5954081442453116, -6.222761293078241884, -8.102969835052219238 ) ) ;
#7208=CARTESIAN_POINT ( 'NONE',  ( 119.5467348109119712, -5.574606645277164318, -18.38911715685844683 ) ) ;
#7211=CARTESIAN_POINT ( 'NONE',  ( 122.2696148109119889, -4.089484607189486809, -7.948022111789456723 ) ) ;
#7213=CARTESIAN_POINT ( 'NONE',  ( 114.5547881442453217, -4.153390946401321671, -8.397313243818183892 ) ) ;
#7214=CARTESIAN_POINT ( 'NONE',  ( 114.4413348109119823, -0.8288870151387760510, -10.36305467784173118 ) ) ;
#7218=CARTESIAN_POINT ( 'NONE',  ( 120.2841814775786276, -10.15424416112533912, -14.75197769757731336 ) ) ;
#7219=CARTESIAN_POINT ( 'NONE',  ( 122.1561614775786353, -8.899110576539710493, -16.42337572283490132 ) ) ;
#7225=CARTESIAN_POINT ( 'NONE',  ( 118.4122014775786340, 0.5811942927096110934, -14.16772938898807510 ) ) ;
#7226=CARTESIAN_POINT ( 'NONE',  ( 114.3846081442453197, -10.63000616557722466, -14.87417383870573495 ) ) ;
#7230=DIRECTION ( 'NONE',  ( 0.000000000000000000, -0.6004852223388320587, 0.7996358532186281787 ) ) ;
#7231=CARTESIAN_POINT ( 'NONE',  ( 120.3976348109119812, -1.834011780172310813, -8.268836392978581529 ) ) ;
#7232=CARTESIAN_POINT ( 'NONE',  ( 126.2404814775786264, -0.8288870151387760510, -10.36305467784173118 ) ) ;
#7234=CARTESIAN_POINT ( 'NONE',  ( 123.6310548109119765, -4.153390946401325223, -8.397313243818185668 ) ) ;
#7235=PRESENTATION_STYLE_ASSIGNMENT (( #7453 ) ) ;
#7236=CARTESIAN_POINT ( 'NONE',  ( 126.1837548109119211, -10.63000616557722466, -14.87417383870573495 ) ) ;
#7237=CARTESIAN_POINT ( 'NONE',  ( 118.2987481442453088, -1.561330072975668504, -17.79121239304076951 ) ) ;
#7240=CARTESIAN_POINT ( 'NONE',  ( 115.8595014775786609, -7.643976991954077427, -18.09477374809248928 ) ) ;
#7245=CARTESIAN_POINT ( 'NONE',  ( 119.8303681442453126, -10.63000616557722466, -14.87417383870573495 ) ) ;
#7247=CARTESIAN_POINT ( 'NONE',  ( 117.5045748109119756, 0.5811942927096110934, -14.16772938898807510 ) ) ;
#7250=CARTESIAN_POINT ( 'NONE',  ( 125.5597614775786326, -1.561330072975669392, -17.79121239304076951 ) ) ;
#7251=CARTESIAN_POINT ( 'NONE',  ( 122.6667014775786413, -7.893985811506198047, -18.51759400769803676 ) ) ;
#7252=CARTESIAN_POINT ( 'NONE',  ( 116.0296814775786345, -1.833838273342658809, -17.42832698103878286 ) ) ;
#7254=CARTESIAN_POINT ( 'NONE',  ( 118.6391081442452986, -5.574606645277164318, -18.38911715685844683 ) ) ;
#7255=CARTESIAN_POINT ( 'NONE',  ( 120.4744527483928920, -2.423081321603731908, -17.89265170041263175 ) ) ;
#7256=CARTESIAN_POINT ( 'NONE',  ( 121.3619881442452879, -5.574606645277164318, -18.38911715685844683 ) ) ;
#7259=CARTESIAN_POINT ( 'NONE',  ( 121.1918081442452859, -10.15424416112533912, -14.75197769757731336 ) ) ;
#7261=CARTESIAN_POINT ( 'NONE',  ( 114.2711548109119803, -9.988377603198976828, -10.36322818467138340 ) ) ;
#7262=CARTESIAN_POINT ( 'NONE',  ( 121.9484597424434043, -0.9924539043446216624, -17.29976612834909133 ) ) ;
#7263=CARTESIAN_POINT ( 'NONE',  ( 121.8725281442453223, -6.222761293078241884, -8.102969835052219238 ) ) ;
#7265=CARTESIAN_POINT ( 'NONE',  ( 116.8238548109119819, -4.089484607189486809, -7.948022111789456723 ) ) ;
#7267=CARTESIAN_POINT ( 'NONE',  ( 115.8027748109119841, -8.899110576539719375, -16.42337572283489067 ) ) ;
#7271=CARTESIAN_POINT ( 'NONE',  ( 123.2906948109119867, -8.166667518702819706, -8.995218007635861213 ) ) ;
#7274=CARTESIAN_POINT ( 'NONE',  ( 126.2455040230451004, -8.053725330373652014, -9.523658174356643968 ) ) ;
#7275=CARTESIAN_POINT ( 'NONE',  ( 116.9373081442452929, -1.833838273342659253, -17.42832698103878286 ) ) ;
#7278=EDGE_CURVE ( 'NONE', #452, #24392, #2359, .T. ) ;
#7282=CARTESIAN_POINT ( 'NONE',  ( 115.0086014775786509, -4.089484607189486809, -7.948022111789456723 ) ) ;
#7283=CARTESIAN_POINT ( 'NONE',  ( 112.9097148109120070, 0.2603800115204892296, -16.42320221600525088 ) ) ;
#7284=CARTESIAN_POINT ( 'NONE',  ( 121.9292548109119849, -1.561330072975668948, -17.79121239304076951 ) ) ;
#7285=CARTESIAN_POINT ( 'NONE',  ( 116.8238548109119819, -5.574606645277164318, -18.38911715685844683 ) ) ;
#7287=CARTESIAN_POINT ( 'NONE',  ( 119.6601881442453106, -8.166667518702819706, -8.995218007635861213 ) ) ;
#7288=CARTESIAN_POINT ( 'NONE',  ( 111.3886348109119808, -3.517672760959766887, -18.63504008191830508 ) ) ;
#7291=CARTESIAN_POINT ( 'NONE',  ( 121.6456214775786293, 0.4262465694468514643, -12.03445270309931736 ) ) ;
#7295=CARTESIAN_POINT ( 'NONE',  ( 116.3133148109119759, -7.893985811506177619, -18.51759400769804742 ) ) ;
#7296=CARTESIAN_POINT ( 'NONE',  ( 123.5176014775786228, -0.8288870151387760510, -10.36305467784173118 ) ) ;
#7298=CARTESIAN_POINT ( 'NONE',  ( 112.4559014775786494, -9.988377603198976828, -10.36322818467138340 ) ) ;
#7299=CARTESIAN_POINT ( 'NONE',  ( 122.0994348109119443, 0.9020085738987339008, -11.91225656197089222 ) ) ;
#7301=CARTESIAN_POINT ( 'NONE',  ( 121.3619881442452879, -5.574606645277164318, -18.38911715685844683 ) ) ;
#7304=CARTESIAN_POINT ( 'NONE',  ( 115.0653281442453277, -6.344957434206662583, -7.627207830600332805 ) ) ;
#7305=CARTESIAN_POINT ( 'NONE',  ( 123.7445081442452874, -7.894159318335828068, -9.358103419637847864 ) ) ;
#7308=CARTESIAN_POINT ( 'NONE',  ( 123.9714148109119805, -0.4660016031367893996, -10.09054647747474043 ) ) ;
#7310=CARTESIAN_POINT ( 'NONE',  ( 135.3184548109119874, -10.81584935473217080, -14.15181583611863303 ) ) ;
#7311=CARTESIAN_POINT ( 'NONE',  ( 122.1561614775786353, -0.4660016031367893996, -10.09054647747474043 ) ) ;
#7312=CARTESIAN_POINT ( 'NONE',  ( 121.2485348109119769, -0.4660016031367893996, -10.09054647747474043 ) ) ;
#7313=CARTESIAN_POINT ( 'NONE',  ( 122.9503348109119827, -9.859900752359378018, -12.68260735090039759 ) ) ;
#7314=CARTESIAN_POINT ( 'NONE',  ( 120.9081748109119872, -4.153390946401325223, -8.397313243818185668 ) ) ;
#7315=CARTESIAN_POINT ( 'NONE',  ( 125.2205968368549946, -0.1451374939622062654, -15.72356508888822191 ) ) ;
#7316=CARTESIAN_POINT ( 'NONE',  ( 116.1431348109119881, -10.30919188438810075, -12.61870101168855918 ) ) ;
#7317=ORIENTED_EDGE ( 'NONE', *, *, #40378, .F. ) ;
#7318=CARTESIAN_POINT ( 'NONE',  ( 125.3895814775786590, -2.084020599725330491, -8.691656652583604981 ) ) ;
#7323=CARTESIAN_POINT ( 'NONE',  ( 124.8790414775786246, -0.4660016031367893996, -10.09054647747474043 ) ) ;
#7324=CARTESIAN_POINT ( 'NONE',  ( 125.1626748109119802, -0.1624402480850797581, -16.17319339645315424 ) ) ;
#7326=ORIENTED_EDGE ( 'NONE', *, *, #9969, .F. ) ;
#7327=CARTESIAN_POINT ( 'NONE',  ( 111.7751814775786556, -2.084020599724406786, -8.691656652584148546 ) ) ;
#7330=CARTESIAN_POINT ( 'NONE',  ( 123.1205148109119563, -1.834011780172310813, -8.268836392978581529 ) ) ;
#7331=CARTESIAN_POINT ( 'NONE',  ( 125.7299414775786346, 0.9020085738987339008, -11.91225656197089222 ) ) ;
#7333=CARTESIAN_POINT ( 'NONE',  ( 114.8951481442453115, -0.4660016031367893996, -10.09054647747474043 ) ) ;
#7339=CARTESIAN_POINT ( 'NONE',  ( 113.7606148109119886, -7.894159318335828068, -9.358103419637847864 ) ) ;
#7340=CARTESIAN_POINT ( 'NONE',  ( 126.6375681442452930, -10.15424416112533912, -14.75197769757731336 ) ) ;
#7344=CARTESIAN_POINT ( 'NONE',  ( 122.6667014775786413, -2.084020599724406786, -8.691656652584148546 ) ) ;
#7346=CARTESIAN_POINT ( 'NONE',  ( 120.5110881442453206, -3.505236298600246325, -18.68346056562440793 ) ) ;
#7347=CARTESIAN_POINT ( 'NONE',  ( 112.7962614775786676, -6.222761293078241884, -8.102969835052219238 ) ) ;
#7352=CARTESIAN_POINT ( 'NONE',  ( 115.5191414775786569, -6.222761293078241884, -8.102969835052219238 ) ) ;
#7358=VECTOR ( 'NONE', #4292, 1000.000000000000000 ) ;
#7359=CARTESIAN_POINT ( 'NONE',  ( 119.8870948109119752, -0.8288870151387760510, -10.36305467784173118 ) ) ;
#7360=CARTESIAN_POINT ( 'NONE',  ( 114.5547881442453217, -4.153390946401321671, -8.397313243818183892 ) ) ;
#7362=CARTESIAN_POINT ( 'NONE',  ( 116.5026997424434114, -0.9924539043446216624, -17.29976612834909133 ) ) ;
#7368=CARTESIAN_POINT ( 'NONE',  ( 112.1155414775786454, 0.9020085738987339008, -11.91225656197089222 ) ) ;
#7369=CARTESIAN_POINT ( 'NONE',  ( 113.0798948109119948, -0.4660016031367893996, -10.09054647747474043 ) ) ;
#7370=CARTESIAN_POINT ( 'NONE',  ( 117.2209414775786485, -2.084020599724406786, -8.691656652584148546 ) ) ;
#7371=CARTESIAN_POINT ( 'NONE',  ( 114.1934435773848833, -2.467220198592768199, -17.83387418641523325 ) ) ;
#7373=CARTESIAN_POINT ( 'NONE',  ( 117.1642148109119859, -0.8288870151387760510, -10.36305467784173118 ) ) ;
#7376=CARTESIAN_POINT ( 'NONE',  ( 116.7226334719562288, -1.125321370491268125, -17.12283323191015327 ) ) ;
#7377=CARTESIAN_POINT ( 'NONE',  ( 115.2922348109119781, -10.63000616557722466, -14.87417383870573495 ) ) ;
#7379=CARTESIAN_POINT ( 'NONE',  ( 117.3343948109119737, -3.383040157471821630, -19.15922257007629170 ) ) ;
#7382=CARTESIAN_POINT ( 'NONE',  ( 113.8173414775786512, 0.2603800115204892296, -16.42320221600525088 ) ) ;
#7383=CARTESIAN_POINT ( 'NONE',  ( 114.1577014775786552, -6.344957434206662583, -7.627207830600332805 ) ) ;
#7384=CARTESIAN_POINT ( 'NONE',  ( 124.8223148109119762, -10.15424416112533912, -14.75197769757731336 ) ) ;
#7385=LINE ( 'NONE', #42736, #32959 ) ;
#7388=CARTESIAN_POINT ( 'NONE',  ( 112.3781902440515665, -2.467220198592768199, -17.83387418641523325 ) ) ;
#7391=CARTESIAN_POINT ( 'NONE',  ( 116.7104014775786425, -8.899110576539710493, -16.42337572283490132 ) ) ;
#7395=CARTESIAN_POINT ( 'NONE',  ( 126.4536383592472788, -4.720982958058952406, -8.277426756250068962 ) ) ;
#7396=CARTESIAN_POINT ( 'NONE',  ( 124.6521348109119884, -1.561330072975668948, -17.79121239304076951 ) ) ;
#7397=CARTESIAN_POINT ( 'NONE',  ( 136.1067208867421243, 0.9922915268929951571, -12.69116158526661842 ) ) ;
#7398=CARTESIAN_POINT ( 'NONE',  ( 122.7801548109119665, -3.383040157471821630, -19.15922257007629170 ) ) ;
#7399=CARTESIAN_POINT ( 'NONE',  ( 116.8805814775786445, -6.344957434206662583, -7.627207830600332805 ) ) ;
#7401=CARTESIAN_POINT ( 'NONE',  ( 115.8027748109119841, -8.899110576539710493, -16.42337572283490132 ) ) ;
#7402=CARTESIAN_POINT ( 'NONE',  ( 125.8433948109119456, -1.834011780172310813, -8.268836392978581529 ) ) ;
#7403=CARTESIAN_POINT ( 'NONE',  ( 118.9227414775786400, -10.63000616557722466, -14.87417383870573495 ) ) ;
#7404=CARTESIAN_POINT ( 'NONE',  ( 117.9583881442453048, 0.1319031606808879209, -14.10382304977623669 ) ) ;
#7406=CARTESIAN_POINT ( 'NONE',  ( 119.6601881442453106, -1.833838273342659253, -17.42832698103878286 ) ) ;
#7407=CARTESIAN_POINT ( 'NONE',  ( 115.6893214775786447, 0.5811942927096154232, -14.16772938898807155 ) ) ;
#7408=CARTESIAN_POINT ( 'NONE',  ( 136.7937340014177607, 0.7122096995249440621, -12.90670490570438567 ) ) ;
#7411=CARTESIAN_POINT ( 'NONE',  ( 126.2769959775738897, 0.1476450766692196659, -13.81407022109413241 ) ) ;
#7413=CARTESIAN_POINT ( 'NONE',  ( 116.0296814775786345, -8.166667518702817929, -8.995218007635861213 ) ) ;
#7419=CARTESIAN_POINT ( 'NONE',  ( 113.9307948109119764, -10.15424416112533912, -14.75197769757731336 ) ) ;
#7422=CARTESIAN_POINT ( 'NONE',  ( 118.3179530757767566, -0.9924539043446216624, -17.29976612834909133 ) ) ;
#7423=CARTESIAN_POINT ( 'NONE',  ( 116.1998614775786507, -10.63000616557722466, -14.87417383870573495 ) ) ;
#7424=CARTESIAN_POINT ( 'NONE',  ( 123.5743281442453139, -2.084020599724406786, -8.691656652584148546 ) ) ;
#7425=CARTESIAN_POINT ( 'NONE',  ( 118.9794681442453026, -0.8288870151387760510, -10.36305467784173118 ) ) ;
#7426=ORIENTED_EDGE ( 'NONE', *, *, #33987, .T. ) ;
#7427=CARTESIAN_POINT ( 'NONE',  ( 136.8192643132362605, -7.130015825163922294, -8.292408517671104207 ) ) ;
#7428=CARTESIAN_POINT ( 'NONE',  ( 123.2339681442453241, -6.344957434206665248, -7.627207830600338134 ) ) ;
#7430=CARTESIAN_POINT ( 'NONE',  ( 120.6812681442452941, 0.1319031606808879209, -14.10382304977623669 ) ) ;
#7432=CARTESIAN_POINT ( 'NONE',  ( 111.2646414775786496, -8.899110576539710493, -16.42337572283490132 ) ) ;
#7435=CARTESIAN_POINT ( 'NONE',  ( 120.3409081442453044, -8.899110576539710493, -16.42337572283490132 ) ) ;
#7436=CARTESIAN_POINT ( 'NONE',  ( 120.9081748109119872, -4.153390946401325223, -8.397313243818185668 ) ) ;
#7441=EDGE_CURVE ( 'NONE', #452, #8883, #9524, .T. ) ;
#7443=CARTESIAN_POINT ( 'NONE',  ( 119.0929214775786278, -5.638512984488999180, -18.83840828888717311 ) ) ;
#7444=CARTESIAN_POINT ( 'NONE',  ( 115.9729548109119861, -6.344957434206662583, -7.627207830600332805 ) ) ;
#7446=CARTESIAN_POINT ( 'NONE',  ( 113.5337081442453240, -9.261995988541697145, -16.69588392320189030 ) ) ;
#7447=EDGE_LOOP ( 'NONE', ( #14154, #725, #44532, #17357, #44036 ) ) ;
#7449=AXIS2_PLACEMENT_3D ( 'NONE', #23520, #5943, #30350 ) ;
#7450=CARTESIAN_POINT ( 'NONE',  ( 123.2906948109119867, -8.166667518702819706, -8.995218007635861213 ) ) ;
#7451=CARTESIAN_POINT ( 'NONE',  ( 116.4834948109119779, -1.561330072975668504, -17.79121239304076951 ) ) ;
#7452=CARTESIAN_POINT ( 'NONE',  ( 121.8158014775786171, -4.153390946401325223, -8.397313243818185668 ) ) ;
#7453=SURFACE_STYLE_USAGE ( .BOTH. , #6807 ) ;
#7454=CARTESIAN_POINT ( 'NONE',  ( 125.9568481442452850, -6.344957434206665248, -7.627207830600338134 ) ) ;
#7455=CARTESIAN_POINT ( 'NONE',  ( 120.8514481442452961, -7.893985811506177619, -18.51759400769804742 ) ) ;
#7459=CARTESIAN_POINT ( 'NONE',  ( 117.3343948109119737, -6.222761293078241884, -8.102969835052219238 ) ) ;
#7462=CARTESIAN_POINT ( 'NONE',  ( 123.2339681442453241, -6.344957434206665248, -7.627207830600338134 ) ) ;
#7466=CARTESIAN_POINT ( 'NONE',  ( 120.6245414775786458, -9.988377603198976828, -10.36322818467138340 ) ) ;
#7469=CARTESIAN_POINT ( 'NONE',  ( 123.6310548109119765, -5.638512984488999180, -18.83840828888717311 ) ) ;
#7470=CARTESIAN_POINT ( 'NONE',  ( 119.7570243147880404, -2.395992375830759524, -17.92872468182853396 ) ) ;
#7471=CARTESIAN_POINT ( 'NONE',  ( 116.7671281442453335, -7.643976991954077427, -18.09477374809248928 ) ) ;
#7473=CARTESIAN_POINT ( 'NONE',  ( 118.7525614775786380, -1.833838273342659253, -17.42832698103878286 ) ) ;
#7476=CARTESIAN_POINT ( 'NONE',  ( 123.1772414775786189, -5.574606645277164318, -18.38911715685844683 ) ) ;
#7478=FACE_OUTER_BOUND ( 'NONE', #39647, .T. ) ;
#7479=CARTESIAN_POINT ( 'NONE',  ( 118.9794681442453026, -0.8288870151387760510, -10.36305467784173118 ) ) ;
#7482=CARTESIAN_POINT ( 'NONE',  ( 116.5402214775786405, 0.2603800115204892296, -16.42320221600525088 ) ) ;
#7483=CARTESIAN_POINT ( 'NONE',  ( 113.0798948109119948, -0.4660016031367893996, -10.09054647747474043 ) ) ;
#7487=CARTESIAN_POINT ( 'NONE',  ( 120.0005481442453146, -4.153390946401325223, -8.397313243818185668 ) ) ;
#7489=CARTESIAN_POINT ( 'NONE',  ( 115.8595014775786609, -1.834011780172310813, -8.268836392978581529 ) ) ;
#7492=VECTOR ( 'NONE', #44625, 1000.000000000000114 ) ;
#7495=CARTESIAN_POINT ( 'NONE',  ( 122.8936081442453059, 0.2603800115204892296, -16.42320221600525088 ) ) ;
#7498=CARTESIAN_POINT ( 'NONE',  ( 121.8725281442453223, -6.222761293078241884, -8.102969835052219238 ) ) ;
#7505=CARTESIAN_POINT ( 'NONE',  ( 116.3133148109119759, -7.893985811506177619, -18.51759400769804742 ) ) ;
#7506=CARTESIAN_POINT ( 'NONE',  ( 125.2761281442453054, 0.4262465694468514643, -12.03445270309931736 ) ) ;
#7507=CARTESIAN_POINT ( 'NONE',  ( 124.1415948109119540, -6.344957434206665248, -7.627207830600338134 ) ) ;
#7508=CARTESIAN_POINT ( 'NONE',  ( 121.6456214775786293, 0.4262465694468514643, -12.03445270309931736 ) ) ;
#7509=CARTESIAN_POINT ( 'NONE',  ( 126.6390922358630604, -3.374097159969326576, -8.400043106829690132 ) ) ;
#7511=CARTESIAN_POINT ( 'NONE',  ( 122.6667014775786413, -7.893985811506177619, -18.51759400769804742 ) ) ;
#7512=CARTESIAN_POINT ( 'NONE',  ( 111.9559014775786494, -9.522524984348097021, -10.63868154973201108 ) ) ;
#7520=CARTESIAN_POINT ( 'NONE',  ( 119.4332814775786318, -0.4660016031367893996, -10.09054647747474043 ) ) ;
#7521=CARTESIAN_POINT ( 'NONE',  ( 124.6521348109119884, -7.894159318335828068, -9.358103419637847864 ) ) ;
#7524=CARTESIAN_POINT ( 'NONE',  ( 122.4397948109119767, -9.988377603198976828, -10.36322818467138340 ) ) ;
#7526=CARTESIAN_POINT ( 'NONE',  ( 123.8012348109119642, -9.565557343593413364, -10.61323700422348004 ) ) ;
#7528=ORIENTED_EDGE ( 'NONE', *, *, #18352, .F. ) ;
#7529=CARTESIAN_POINT ( 'NONE',  ( 116.2565881442452991, -9.261995988541697145, -16.69588392320189030 ) ) ;
#7532=DIRECTION ( 'NONE',  ( -1.000000000000000000, 0.000000000000000000, 0.000000000000000000 ) ) ;
#7533=CARTESIAN_POINT ( 'NONE',  ( 111.6617281442453304, 0.4262465694468514643, -12.03445270309931736 ) ) ;
#7537=CARTESIAN_POINT ( 'NONE',  ( 121.7590748109119687, -7.893985811506177619, -18.51759400769804742 ) ) ;
#7538=CARTESIAN_POINT ( 'NONE',  ( 124.0281414775786146, -1.834011780172310813, -8.268836392978581529 ) ) ;
#7539=CARTESIAN_POINT ( 'NONE',  ( 123.7445081442452874, -7.894159318335828068, -9.358103419637847864 ) ) ;
#7540=CARTESIAN_POINT ( 'NONE',  ( 118.3554748109119998, -9.565557343593413364, -10.61323700422348004 ) ) ;
#7541=CARTESIAN_POINT ( 'NONE',  ( 125.7761281442453196, -10.10582367741896093, -14.73954123521881066 ) ) ;
#7542=CARTESIAN_POINT ( 'NONE',  ( 117.3911214775786505, -1.561330072975668504, -17.79121239304076951 ) ) ;
#7552=CARTESIAN_POINT ( 'NONE',  ( 124.3685014775786328, -10.63000616557722466, -14.87417383870573495 ) ) ;
#7553=CARTESIAN_POINT ( 'NONE',  ( 112.2857214775786474, -4.089484607189486809, -7.948022111789456723 ) ) ;
#7554=EDGE_LOOP ( 'NONE', ( #33129, #30401, #18640, #35038 ) ) ;
#7555=CARTESIAN_POINT ( 'NONE',  ( 112.7395348109119766, -4.153390946401321671, -8.397313243818183892 ) ) ;
#7557=CARTESIAN_POINT ( 'NONE',  ( 119.6392035773848761, -2.467220198592778413, -17.83387418641524391 ) ) ;
#7558=EDGE_CURVE ( 'NONE', #20751, #12347, #10818, .T. ) ;
#7560=CARTESIAN_POINT ( 'NONE',  ( 124.1415948109119540, -6.344957434206665248, -7.627207830600338134 ) ) ;
#7562=CARTESIAN_POINT ( 'NONE',  ( 115.2355081442453155, -10.30919188438810075, -12.61870101168855918 ) ) ;
#7568=CARTESIAN_POINT ( 'NONE',  ( 115.2355081442453155, 0.1319031606808879209, -14.10382304977623669 ) ) ;
#7569=CARTESIAN_POINT ( 'NONE',  ( 126.2404814775786264, -0.8288870151387760510, -10.36305467784173118 ) ) ;
#7570=CARTESIAN_POINT ( 'NONE',  ( 113.1933481442453058, -4.089484607189486809, -7.948022111789456723 ) ) ;
#7571=CARTESIAN_POINT ( 'NONE',  ( 118.4122014775786340, -9.859900752359374465, -12.68260735090039404 ) ) ;
#7572=CARTESIAN_POINT ( 'NONE',  ( 120.0572748109119772, -6.222761293078241884, -8.102969835052219238 ) ) ;
#7573=CARTESIAN_POINT ( 'NONE',  ( 116.9940348109119839, -0.1624402480850797581, -16.17319339645315424 ) ) ;
#7576=CARTESIAN_POINT ( 'NONE',  ( 128.2184548109119930, -4.863998795839242995, -13.39321520033831447 ) ) ;
#7577=CARTESIAN_POINT ( 'NONE',  ( 113.7606148109119886, -7.894159318335828068, -9.358103419637847864 ) ) ;
#7579=CARTESIAN_POINT ( 'NONE',  ( 126.2471382750693323, -8.992437524846883079, -16.23933567622449559 ) ) ;
#7583=CARTESIAN_POINT ( 'NONE',  ( 124.0281414775786146, -7.643976991954077427, -18.09477374809248928 ) ) ;
#7585=CARTESIAN_POINT ( 'NONE',  ( 119.6601881442453106, -1.833838273342659253, -17.42832698103878286 ) ) ;
#7586=CARTESIAN_POINT ( 'NONE',  ( 118.1852948109119836, -4.153390946401325223, -8.397313243818185668 ) ) ;
#7595=CARTESIAN_POINT ( 'NONE',  ( 112.5693548109119888, -10.63000616557722466, -14.87417383870573495 ) ) ;
#7596=CARTESIAN_POINT ( 'NONE',  ( 116.4834948109119779, -7.894159318335828068, -9.358103419637847864 ) ) ;
#7599=CARTESIAN_POINT ( 'NONE',  ( 116.0296814775786345, -1.833838273342658809, -17.42832698103878286 ) ) ;
#7605=CARTESIAN_POINT ( 'NONE',  ( 113.4202548109119846, -10.30919188438810075, -12.61870101168855918 ) ) ;
#7607=CARTESIAN_POINT ( 'NONE',  ( 115.5191414775786569, -3.383040157471821630, -19.15922257007629170 ) ) ;
#7608=CARTESIAN_POINT ( 'NONE',  ( 113.9307948109119764, 0.9020085738987376756, -11.91225656197089755 ) ) ;
#7610=CARTESIAN_POINT ( 'NONE',  ( 114.4413348109119823, -9.261995988541697145, -16.69588392320189030 ) ) ;
#7611=CARTESIAN_POINT ( 'NONE',  ( 112.5693548109119888, -10.63000616557722466, -14.87417383870573495 ) ) ;
#7619=CARTESIAN_POINT ( 'NONE',  ( 116.5402214775786405, -9.565557343593413364, -10.61323700422348004 ) ) ;
#7621=CARTESIAN_POINT ( 'NONE',  ( 122.6212569549021794, -1.135392229370309369, -17.10942237759952889 ) ) ;
#7623=CARTESIAN_POINT ( 'NONE',  ( 127.0553483106897943, -5.177147889503950218, -7.983820274244006754 ) ) ;
#7624=CARTESIAN_POINT ( 'NONE',  ( 115.9729548109119861, -3.505236298600246325, -18.68346056562440793 ) ) ;
#7626=CARTESIAN_POINT ( 'NONE',  ( 124.5386814775786206, -5.638512984488999180, -18.83840828888717311 ) ) ;
#7627=CARTESIAN_POINT ( 'NONE',  ( 117.5613014775786525, 0.9020085738987339008, -11.91225656197089222 ) ) ;
#7628=ORIENTED_EDGE ( 'NONE', *, *, #41595, .F. ) ;
#7629=CARTESIAN_POINT ( 'NONE',  ( 115.7460481442453357, -10.15424416112533912, -14.75197769757731336 ) ) ;
#7631=CARTESIAN_POINT ( 'NONE',  ( 117.6747548109119919, -1.834011780172310813, -8.268836392978581529 ) ) ;
#7633=CARTESIAN_POINT ( 'NONE',  ( 114.5547881442453217, -4.153390946401321671, -8.397313243818183892 ) ) ;
#7634=ORIENTED_EDGE ( 'NONE', *, *, #844, .T. ) ;
#7635=CARTESIAN_POINT ( 'NONE',  ( 122.4397948109119767, -0.1624402480850797581, -16.17319339645315424 ) ) ;
#7636=AXIS2_PLACEMENT_3D ( 'NONE', #16412, #12995, #2943 ) ;
#7637=CARTESIAN_POINT ( 'NONE',  ( 118.0151148109119816, -10.63000616557722466, -14.87417383870573495 ) ) ;
#7642=CARTESIAN_POINT ( 'NONE',  ( 126.3037217343607495, 0.1656680361304483373, -13.75559490932021944 ) ) ;
#7644=CARTESIAN_POINT ( 'NONE',  ( 113.7606148109119886, -1.561330072975668060, -17.79121239304076596 ) ) ;
#7646=CARTESIAN_POINT ( 'NONE',  ( 114.3846081442453197, 0.4262465694468514643, -12.03445270309931736 ) ) ;
#7650=CARTESIAN_POINT ( 'NONE',  ( 114.4980614775786734, -2.084020599724406786, -8.691656652584148546 ) ) ;
#7651=CARTESIAN_POINT ( 'NONE',  ( 123.7184548109119788, -4.863998795839242995, -13.39321520033831447 ) ) ;
#7654=CARTESIAN_POINT ( 'NONE',  ( 119.7736414775786358, -10.30919188438810075, -12.61870101168855918 ) ) ;
#7656=CARTESIAN_POINT ( 'NONE',  ( 118.8092881442453290, -0.1624402480850797581, -16.17319339645315424 ) ) ;
#7657=CARTESIAN_POINT ( 'NONE',  ( 113.4202548109119846, 0.1319031606808879209, -14.10382304977623669 ) ) ;
#7659=CARTESIAN_POINT ( 'NONE',  ( 137.4478226697682999, -7.537440151351030515, -9.085464482628538008 ) ) ;
#7660=CARTESIAN_POINT ( 'NONE',  ( 122.7234281442452755, -5.638512984488999180, -18.83840828888717311 ) ) ;
#7662=CARTESIAN_POINT ( 'NONE',  ( 118.5256548109119876, -8.899110576539710493, -16.42337572283490132 ) ) ;
#7663=CARTESIAN_POINT ( 'NONE',  ( 115.5758681442453053, -7.894159318335828068, -9.358103419637847864 ) ) ;
#7667=CARTESIAN_POINT ( 'NONE',  ( 119.5467348109119712, -5.574606645277164318, -18.38911715685844683 ) ) ;
#7668=CARTESIAN_POINT ( 'NONE',  ( 123.3474214775786209, -0.1624402480850797581, -16.17319339645315424 ) ) ;
#7669=CARTESIAN_POINT ( 'NONE',  ( 116.9163235773848726, -2.467220198592778413, -17.83387418641524391 ) ) ;
#7675=CARTESIAN_POINT ( 'NONE',  ( 118.5823814775786360, -1.834011780172310813, -8.268836392978581529 ) ) ;
#7676=CARTESIAN_POINT ( 'NONE',  ( 113.2500748109119968, -6.344957434206662583, -7.627207830600332805 ) ) ;
#7678=CARTESIAN_POINT ( 'NONE',  ( 112.3424481442453384, -6.344957434206662583, -7.627207830600332805 ) ) ;
#7682=CARTESIAN_POINT ( 'NONE',  ( 124.4252281442452812, -9.261995988541697145, -16.69588392320189030 ) ) ;
#7683=CARTESIAN_POINT ( 'NONE',  ( 115.1220548109119761, -8.166667518702817929, -8.995218007635861213 ) ) ;
#7684=CARTESIAN_POINT ( 'NONE',  ( 120.7379948109119709, 0.4262465694468514643, -12.03445270309931736 ) ) ;
#7686=CARTESIAN_POINT ( 'NONE',  ( 124.8790414775786246, -0.4660016031367893996, -10.09054647747474043 ) ) ;
#7687=CARTESIAN_POINT ( 'NONE',  ( 122.4397948109119767, -9.988377603198976828, -10.36322818467138340 ) ) ;
#7689=CARTESIAN_POINT ( 'NONE',  ( 116.9373081442452929, -1.833838273342659253, -17.42832698103878286 ) ) ;
#7693=CARTESIAN_POINT ( 'NONE',  ( 121.4754414775786131, -8.166667518702819706, -8.995218007635861213 ) ) ;
#7695=CARTESIAN_POINT ( 'NONE',  ( 117.9583881442453048, -10.30919188438810075, -12.61870101168855918 ) ) ;
#7701=CARTESIAN_POINT ( 'NONE',  ( 117.3343948109119737, -6.222761293078241884, -8.102969835052219238 ) ) ;
#7704=CARTESIAN_POINT ( 'NONE',  ( 118.5823814775786360, -7.643976991954077427, -18.09477374809248928 ) ) ;
#7707=CARTESIAN_POINT ( 'NONE',  ( 122.3830681442452857, -1.833838273342659697, -17.42832698103878286 ) ) ;
#7710=CARTESIAN_POINT ( 'NONE',  ( 119.6034614775786196, -3.505236298600246325, -18.68346056562440793 ) ) ;
#7711=CARTESIAN_POINT ( 'NONE',  ( 114.2144281442453178, -8.166667518702817929, -8.995218007635859436 ) ) ;
#7712=CARTESIAN_POINT ( 'NONE',  ( 119.6601881442453106, -8.166667518702819706, -8.995218007635861213 ) ) ;
#7713=CARTESIAN_POINT ( 'NONE',  ( 126.1837548109119496, 0.4262465694468514643, -12.03445270309931736 ) ) ;
#7715=CARTESIAN_POINT ( 'NONE',  ( 121.5321681442453183, -0.1624402480850797581, -16.17319339645315424 ) ) ;
#7717=CARTESIAN_POINT ( 'NONE',  ( 115.6893214775786447, 0.5811942927096154232, -14.16772938898807155 ) ) ;
#7723=CIRCLE ( 'NONE', #16505, 1.499999999999999334 ) ;
#7724=EDGE_LOOP ( 'NONE', ( #27738, #23789, #13591, #32692 ) ) ;
#7725=CARTESIAN_POINT ( 'NONE',  ( 126.3115243456346093, -8.177670693431501547, -9.587005482640760690 ) ) ;
#7726=CARTESIAN_POINT ( 'NONE',  ( 121.2485348109119769, -8.899110576539710493, -16.42337572283490132 ) ) ;
#7729=CARTESIAN_POINT ( 'NONE',  ( 125.9568481442452850, -6.344957434206665248, -7.627207830600338134 ) ) ;
#7734=CARTESIAN_POINT ( 'NONE',  ( 115.9729548109119861, -6.344957434206662583, -7.627207830600332805 ) ) ;
#7735=CARTESIAN_POINT ( 'NONE',  ( 114.3846081442453197, -10.63000616557722466, -14.87417383870573495 ) ) ;
#7737=CARTESIAN_POINT ( 'NONE',  ( 121.9292548109119849, -7.894159318335828068, -9.358103419637847864 ) ) ;
#7739=CARTESIAN_POINT ( 'NONE',  ( 123.7445081442452874, -1.561330072975668948, -17.79121239304076951 ) ) ;
#7740=CARTESIAN_POINT ( 'NONE',  ( 112.1722681442453222, -8.899110576539710493, -16.42337572283490132 ) ) ;
#7743=CARTESIAN_POINT ( 'NONE',  ( 125.6732148109119862, -9.859900752359378018, -12.68260735090039759 ) ) ;
#7745=CIRCLE ( 'NONE', #453, 5.999999999999997335 ) ;
#7748=CARTESIAN_POINT ( 'NONE',  ( 120.1140014775786398, -1.561330072975668504, -17.79121239304076951 ) ) ;
#7749=CARTESIAN_POINT ( 'NONE',  ( 136.8192643132354078, -9.964805478506571390, -15.65923222966296713 ) ) ;
#7752=EDGE_CURVE ( 'NONE', #38119, #3495, #2882, .T. ) ;
#7756=CARTESIAN_POINT ( 'NONE',  ( 111.8886348109120092, -6.222761293078241884, -8.102969835052219238 ) ) ;
#7758=CARTESIAN_POINT ( 'NONE',  ( 123.6877814775786533, -6.222761293078241884, -8.102969835052219238 ) ) ;
#7760=CARTESIAN_POINT ( 'NONE',  ( 117.9016614775786280, -9.988377603198976828, -10.36322818467138340 ) ) ;
#7762=CARTESIAN_POINT ( 'NONE',  ( 116.6208609388149426, -2.287189184988710267, -18.07361239780447448 ) ) ;
#7763=CARTESIAN_POINT ( 'NONE',  ( 112.6373636215688521, -1.135392229370320694, -17.10942237759953954 ) ) ;
#7764=CARTESIAN_POINT ( 'NONE',  ( 135.9690293846558404, -5.581979509648644644, -7.510532691874653999 ) ) ;
#7765=CARTESIAN_POINT ( 'NONE',  ( 124.7655881442452852, 0.5811942927096110934, -14.16772938898807510 ) ) ;
#7770=CARTESIAN_POINT ( 'NONE',  ( 123.4041481442452834, -10.30919188438810075, -12.61870101168855918 ) ) ;
#7771=CARTESIAN_POINT ( 'NONE',  ( 122.7801548109119665, -3.383040157471821630, -19.15922257007629170 ) ) ;
#7772=CARTESIAN_POINT ( 'NONE',  ( 124.3685014775786328, 0.4262465694468514643, -12.03445270309931736 ) ) ;
#7773=CARTESIAN_POINT ( 'NONE',  ( 126.2184548109105435, -9.814174330883648878, -12.68911139247483710 ) ) ;
#7774=CARTESIAN_POINT ( 'NONE',  ( 123.8579614775786126, -9.859900752359378018, -12.68260735090039759 ) ) ;
#7775=CARTESIAN_POINT ( 'NONE',  ( 113.1366214775786432, -7.643976991954077427, -18.09477374809248928 ) ) ;
#7776=CARTESIAN_POINT ( 'NONE',  ( 117.9016614775786280, -9.988377603198976828, -10.36322818467138340 ) ) ;
#7780=CARTESIAN_POINT ( 'NONE',  ( 122.4406277074048859, -2.419733177069661512, -17.89711025544711376 ) ) ;
#7784=CARTESIAN_POINT ( 'NONE',  ( 124.7088614775786226, 0.2603800115204892296, -16.42320221600525088 ) ) ;
#7785=CARTESIAN_POINT ( 'NONE',  ( 111.8886348109120092, -3.383040157471821630, -19.15922257007629170 ) ) ;
#7787=CARTESIAN_POINT ( 'NONE',  ( 113.8173414775786512, -9.565557343593413364, -10.61323700422348004 ) ) ;
#7791=( BOUNDED_SURFACE ( )  B_SPLINE_SURFACE ( 1, 2, ( 
 ( #14112, #10480, #24381, #10699, #35512, #43052, #22300, #4054, #25049, #4517, #35744, #18659, #18440, #32550, #32329, #36197, #643, #17978, #15011, #1095, #31878, #28924, #42831, #11592, #21848, #14558, #22080, #28701, #25502, #28477, #8396, #15230, #42606, #39173, #38943, #4962, #29139, #32101, #39407, #8170, #11371, #11145, #25277, #42381, #7711, #35968, #4738, #1319, #21624, #11818, #4284, #25726, #39633, #7937, #18203, #868, #14787, #24745, #130, #14486, #41428, #42088, #24973, #27959, #4215, #17685, #6761, #18131, #17459, #28396, #7407, #41867, #31137, #20670, #10848, #13821, #24316, #10184, #28180, #10406, #24091, #31357, #3544, #38201, #45061, #34546, #35213, #21096, #38633, #38868, #21550, #27510, #44848, #350, #14042, #3985, #3327, #10627, #24531, #17249, #38418, #35438, #21327, #13600, #37984, #14263, #3762, #27735, #7189, #34975, #41649, #7637, #6979, #20887, #17907, #34765, #31583, #31805, #576, #42309, #11069, #43428, #39100, #32694, #14938, #36337, #32910, #39774, #39997, #11971, #35892, #11524, #42974, #36565, #5107, #12194, #18581, #29065, #42760, #8543, #22445, #32473, #28849, #792, #4887, #14714, #15607, #19025, #1688, #29514, #39330, #8098, #39559, #7870, #26093, #8762, #29290, #11294, #28625, #15387, #25428, #22669, #21779, #5341, #1463, #21999, #11745, #32025, #42534, #25870, #4661, #1248, #25204, #35669, #15160, #25653, #8319, #4443, #22222, #18361, #32253, #1021, #36117, #18804, #43204, #12879, #9909, #37009, #16749, #6010, #26322, #19699, #16060, #23131, #12653, #19934, #37708, #30643, #15836, #44113, #16293, #29967, #29735, #2131, #19258, #2820, #23821, #2363, #12421, #26779, #5779, #44340, #44563, #33137, #40688, #1909, #20170, #19477, #8997, #33588, #13326, #43881, #43646, #37475, #37238, #6248, #9441, #26549, #40229, #22893, #9223, #36788, #5558, #33358, #33819, #30194, #40460, #2591, #34053, #23352, #16522, #30419, #13099, #27000, #27233, #40919, #41148, #9673, #23591, #44164, #22946, #12472, #2871, #41197, #16339, #26826, #40511 ),
 ( #13381, #20217, #16800, #34103, #37060, #5833, #37292, #36839, #44615, #9957, #27053, #9046, #26372, #13150, #26598, #27282, #5607, #23871, #6298, #2182, #19753, #2413, #9274, #43700, #23182, #30696, #37756, #29787, #6062, #12928, #40282, #19981, #33870, #2640, #30242, #6526, #30466, #33637, #40737, #20443, #34326, #9726, #9494, #23408, #19530, #3099, #16572, #44386, #40971, #33406, #12698, #16112, #30013, #43932, #23638, #37525, #42302, #10624, #7633, #34759, #14482, #3759, #24087, #17456, #13818, #20883, #10401, #17681, #35435, #28392, #13597, #41862, #14038, #27731, #27507, #45058, #17027, #573, #21546, #127, #10181, #24527, #3541, #42084, #11066, #30919, #38414, #44841, #17904, #17243, #6755, #31352, #24968, #41646, #41425, #35209, #34971, #3981, #7183, #24311, #37981, #20666, #6974, #34541, #3323, #31134, #31579, #27955, #38197, #346, #31801, #21093, #14259, #28176, #10844, #24739, #38864, #38629, #7404, #21322, #11291, #35666, #4656, #21774, #32022, #39554, #8759, #22665, #39326, #18357, #1245, #4211, #4439, #8094, #21996, #11966, #8540, #8316, #25650, #18128, #39769, #15382, #32247, #1682, #39994, #787, #25200, #15157, #29062, #25866, #42971, #22442, #11739, #12189, #14708, #15604, #28621, #22217, #36113, #14934, #42531, #1018, #39097, #32907, #7867, #32469, #28845, #4884, #35886, #29286, #29508, #42757, #18801, #11521, #5104, #25425, #18577, #32691, #43424, #1460, #43200, #36334, #19020, #26090, #26775, #43878, #12418, #41145, #26545, #19254, #33133, #26318, #9436, #40456, #40226, #37233, #23587, #29963, #12649, #40685, #29730, #9218, #6244, #23128, #44557, #37472, #43643, #22890, #37004, #8990, #1903, #23349, #9905, #36561, #5775, #5554, #33584, #5336, #36783, #19695, #2360, #44336, #40915, #6007, #12876, #15832, #26995, #2586, #19472, #34049, #27227, #33355, #2127, #16289, #30191, #13096, #44109, #9669, #19930, #13323, #16057, #33816, #16517, #30416, #20166, #2817, #16746, #30640, #10347, #514, #24466, #20613, #20825, #14425, #24685, #3706, #34487 ) ),
 .UNSPECIFIED., .F., .F., .F. ) 
 B_SPLINE_SURFACE_WITH_KNOTS ( ( 2, 2 ),
 ( 3, 2, 2, 2, 2, 2, 2, 2, 2, 2, 2, 2, 2, 2, 2, 2, 2, 2, 2, 2, 2, 2, 2, 2, 2, 2, 2, 2, 2, 2, 2, 2, 2, 2, 2, 2, 2, 2, 2, 2, 2, 2, 2, 2, 2, 2, 2, 2, 2, 2, 2, 2, 2, 2, 2, 2, 2, 2, 2, 2, 2, 2, 2, 2, 2, 2, 2, 2, 2, 2, 2, 2, 2, 2, 2, 2, 2, 2, 2, 2, 2, 2, 2, 2, 2, 2, 2, 2, 2, 2, 2, 2, 2, 2, 2, 2, 2, 2, 2, 2, 2, 2, 2, 2, 2, 2, 2, 2, 2, 2, 2, 2, 2, 2, 2, 2, 2, 2, 2, 2, 2, 2, 2, 2, 2, 2, 2, 2, 3 ),
 ( 0.000000000000000000, 1.000000000000000000 ),
 ( 0.000000000000000000, 0.007812500000000000000, 0.01562500000000000000, 0.02343750000000000000, 0.03125000000000000000, 0.03906250000000000000, 0.04687500000000000000, 0.05468750000000000000, 0.06250000000000000000, 0.07031250000000000000, 0.07812500000000000000, 0.08593750000000000000, 0.09375000000000000000, 0.1015625000000000000, 0.1093750000000000000, 0.1171875000000000000, 0.1250000000000000000, 0.1328125000000000000, 0.1406250000000000000, 0.1484375000000000000, 0.1562500000000000000, 0.1640625000000000000, 0.1718750000000000000, 0.1796875000000000000, 0.1875000000000000000, 0.1953125000000000000, 0.2031250000000000000, 0.2109375000000000000, 0.2187500000000000000, 0.2265625000000000000, 0.2343750000000000000, 0.2421875000000000000, 0.2500000000000000000, 0.2578125000000000000, 0.2656250000000000000, 0.2734375000000000000, 0.2812500000000000000, 0.2890625000000000000, 0.2968750000000000000, 0.3046875000000000000, 0.3125000000000000000, 0.3203125000000000000, 0.3281250000000000000, 0.3359375000000000000, 0.3437500000000000000, 0.3515625000000000000, 0.3593750000000000000, 0.3671875000000000000, 0.3750000000000000000, 0.3828125000000000000, 0.3906250000000000000, 0.3984375000000000000, 0.4062500000000000000, 0.4140625000000000000, 0.4218750000000000000, 0.4296875000000000000, 0.4375000000000000000, 0.4453125000000000000, 0.4531250000000000000, 0.4609375000000000000, 0.4687500000000000000, 0.4765625000000000000, 0.4843750000000000000, 0.4921875000000000000, 0.5000000000000000000, 0.5078125000000000000, 0.5156250000000000000, 0.5234375000000000000, 0.5312500000000000000, 0.5390625000000000000, 0.5468750000000000000, 0.5546875000000000000, 0.5625000000000000000, 0.5703125000000000000, 0.5781250000000000000, 0.5859375000000000000, 0.5937500000000000000, 0.6015625000000000000, 0.6093750000000000000, 0.6171875000000000000, 0.6250000000000000000, 0.6328125000000000000, 0.6406250000000000000, 0.6484375000000000000, 0.6562500000000000000, 0.6640625000000000000, 0.6718750000000000000, 0.6796875000000000000, 0.6875000000000000000, 0.6953125000000000000, 0.7031250000000000000, 0.7109375000000000000, 0.7187500000000000000, 0.7265625000000000000, 0.7343750000000000000, 0.7421875000000000000, 0.7500000000000000000, 0.7578125000000000000, 0.7656250000000000000, 0.7734375000000000000, 0.7812500000000000000, 0.7890625000000000000, 0.7968750000000000000, 0.8046875000000000000, 0.8125000000000000000, 0.8203125000000000000, 0.8281250000000000000, 0.8359375000000000000, 0.8437500000000000000, 0.8515625000000000000, 0.8593750000000000000, 0.8671875000000000000, 0.8750000000000000000, 0.8828125000000000000, 0.8906250000000000000, 0.8984375000000000000, 0.9062500000000000000, 0.9140625000000000000, 0.9218750000000000000, 0.9296875000000000000, 0.9375000000000000000, 0.9453125000000000000, 0.9531250000000000000, 0.9609375000000000000, 0.9687500000000000000, 0.9765625000000000000, 0.9843750000000000000, 0.9921875000000000000, 1.000000000000000000 ),
 .UNSPECIFIED. ) 
 GEOMETRIC_REPRESENTATION_ITEM ( )  RATIONAL_B_SPLINE_SURFACE ( (
 ( 1.000000000000000000, 0.9238795325112869605, 1.000000000000000000, 0.9238795325112869605, 1.000000000000000000, 0.9238795325112869605, 1.000000000000000000, 0.9238795325112869605, 1.000000000000000000, 0.9238795325112869605, 1.000000000000000000, 0.9238795325112869605, 1.000000000000000000, 0.9238795325112869605, 1.000000000000000000, 0.9238795325112869605, 1.000000000000000000, 0.9238795325112869605, 1.000000000000000000, 0.9238795325112869605, 1.000000000000000000, 0.9238795325112869605, 1.000000000000000000, 0.9238795325112869605, 1.000000000000000000, 0.9238795325112869605, 1.000000000000000000, 0.9238795325112869605, 1.000000000000000000, 0.9238795325112869605, 1.000000000000000000, 0.9238795325112869605, 1.000000000000000000, 0.9238795325112869605, 1.000000000000000000, 0.9238795325112869605, 1.000000000000000000, 0.9238795325112869605, 1.000000000000000000, 0.9238795325112869605, 1.000000000000000000, 0.9238795325112869605, 1.000000000000000000, 0.9238795325112869605, 1.000000000000000000, 0.9238795325112869605, 1.000000000000000000, 0.9238795325112869605, 1.000000000000000000, 0.9238795325112869605, 1.000000000000000000, 0.9238795325112869605, 1.000000000000000000, 0.9238795325112869605, 1.000000000000000000, 0.9238795325112869605, 1.000000000000000000, 0.9238795325112869605, 1.000000000000000000, 0.9238795325112869605, 1.000000000000000000, 0.9238795325112869605, 1.000000000000000000, 0.9238795325112869605, 1.000000000000000000, 0.9238795325112869605, 1.000000000000000000, 0.9238795325112869605, 1.000000000000000000, 0.9238795325112869605, 1.000000000000000000, 0.9238795325112869605, 1.000000000000000000, 0.9238795325112869605, 1.000000000000000000, 0.9238795325112869605, 1.000000000000000000, 0.9238795325112869605, 1.000000000000000000, 0.9238795325112869605, 1.000000000000000000, 0.9238795325112869605, 1.000000000000000000, 0.9238795325112869605, 1.000000000000000000, 0.9238795325112869605, 1.000000000000000000, 0.9238795325112869605, 1.000000000000000000, 0.9238795325112869605, 1.000000000000000000, 0.9238795325112869605, 1.000000000000000000, 0.9238795325112869605, 1.000000000000000000, 0.9238795325112869605, 1.000000000000000000, 0.9238795325112869605, 1.000000000000000000, 0.9238795325112869605, 1.000000000000000000, 0.9238795325112869605, 1.000000000000000000, 0.9238795325112869605, 1.000000000000000000, 0.9238795325112869605, 1.000000000000000000, 0.9238795325112869605, 1.000000000000000000, 0.9238795325112869605, 1.000000000000000000, 0.9238795325112869605, 1.000000000000000000, 0.9238795325112869605, 1.000000000000000000, 0.9238795325112869605, 1.000000000000000000, 0.9238795325112869605, 1.000000000000000000, 0.9238795325112869605, 1.000000000000000000, 0.9238795325112869605, 1.000000000000000000, 0.9238795325112869605, 1.000000000000000000, 0.9238795325112869605, 1.000000000000000000, 0.9238795325112869605, 1.000000000000000000, 0.9238795325112869605, 1.000000000000000000, 0.9238795325112869605, 1.000000000000000000, 0.9238795325112869605, 1.000000000000000000, 0.9238795325112869605, 1.000000000000000000, 0.9238795325112869605, 1.000000000000000000, 0.9238795325112869605, 1.000000000000000000, 0.9238795325112869605, 1.000000000000000000, 0.9238795325112869605, 1.000000000000000000, 0.9238795325112869605, 1.000000000000000000, 0.9238795325112869605, 1.000000000000000000, 0.9238795325112869605, 1.000000000000000000, 0.9238795325112869605, 1.000000000000000000, 0.9238795325112869605, 1.000000000000000000, 0.9238795325112869605, 1.000000000000000000, 0.9238795325112869605, 1.000000000000000000, 0.9238795325112869605, 1.000000000000000000, 0.9238795325112869605, 1.000000000000000000, 0.9238795325112869605, 1.000000000000000000, 0.9238795325112869605, 1.000000000000000000, 0.9238795325112869605, 1.000000000000000000, 0.9238795325112869605, 1.000000000000000000, 0.9238795325112869605, 1.000000000000000000, 0.9238795325112869605, 1.000000000000000000, 0.9238795325112869605, 1.000000000000000000, 0.9238795325112869605, 1.000000000000000000, 0.9238795325112869605, 1.000000000000000000, 0.9238795325112869605, 1.000000000000000000, 0.9238795325112869605, 1.000000000000000000, 0.9238795325112869605, 1.000000000000000000, 0.9238795325112869605, 1.000000000000000000, 0.9238795325112869605, 1.000000000000000000, 0.9238795325112869605, 1.000000000000000000, 0.9238795325112869605, 1.000000000000000000, 0.9238795325112869605, 1.000000000000000000, 0.9238795325112869605, 1.000000000000000000, 0.9238795325112869605, 1.000000000000000000, 0.9238795325112869605, 1.000000000000000000, 0.9238795325112869605, 1.000000000000000000, 0.9238795325112869605, 1.000000000000000000, 0.9238795325112869605, 1.000000000000000000, 0.9238795325112869605, 1.000000000000000000, 0.9238795325112869605, 1.000000000000000000, 0.9238795325112869605, 1.000000000000000000, 0.9238795325112869605, 1.000000000000000000, 0.9238795325112869605, 1.000000000000000000, 0.9238795325112869605, 1.000000000000000000, 0.9238795325112869605, 1.000000000000000000, 0.9238795325112869605, 1.000000000000000000, 0.9238795325112869605, 1.000000000000000000, 0.9238795325112869605, 1.000000000000000000, 0.9238795325112869605, 1.000000000000000000, 0.9238795325112869605, 1.000000000000000000, 0.9238795325112869605, 1.000000000000000000, 0.9238795325112869605, 1.000000000000000000, 0.9238795325112869605, 1.000000000000000000, 0.9238795325112869605, 1.000000000000000000, 0.9238795325112869605, 1.000000000000000000, 0.9238795325112869605, 1.000000000000000000, 0.9238795325112869605, 1.000000000000000000, 0.9238795325112869605, 1.000000000000000000, 0.9238795325112869605, 1.000000000000000000, 0.9238795325112869605, 1.000000000000000000, 0.9238795325112869605, 1.000000000000000000, 0.9238795325112869605, 1.000000000000000000),
 ( 1.000000000000000000, 0.9238795325112869605, 1.000000000000000000, 0.9238795325112869605, 1.000000000000000000, 0.9238795325112869605, 1.000000000000000000, 0.9238795325112869605, 1.000000000000000000, 0.9238795325112869605, 1.000000000000000000, 0.9238795325112869605, 1.000000000000000000, 0.9238795325112869605, 1.000000000000000000, 0.9238795325112869605, 1.000000000000000000, 0.9238795325112869605, 1.000000000000000000, 0.9238795325112869605, 1.000000000000000000, 0.9238795325112869605, 1.000000000000000000, 0.9238795325112869605, 1.000000000000000000, 0.9238795325112869605, 1.000000000000000000, 0.9238795325112869605, 1.000000000000000000, 0.9238795325112869605, 1.000000000000000000, 0.9238795325112869605, 1.000000000000000000, 0.9238795325112869605, 1.000000000000000000, 0.9238795325112869605, 1.000000000000000000, 0.9238795325112869605, 1.000000000000000000, 0.9238795325112869605, 1.000000000000000000, 0.9238795325112869605, 1.000000000000000000, 0.9238795325112869605, 1.000000000000000000, 0.9238795325112869605, 1.000000000000000000, 0.9238795325112869605, 1.000000000000000000, 0.9238795325112869605, 1.000000000000000000, 0.9238795325112869605, 1.000000000000000000, 0.9238795325112869605, 1.000000000000000000, 0.9238795325112869605, 1.000000000000000000, 0.9238795325112869605, 1.000000000000000000, 0.9238795325112869605, 1.000000000000000000, 0.9238795325112869605, 1.000000000000000000, 0.9238795325112869605, 1.000000000000000000, 0.9238795325112869605, 1.000000000000000000, 0.9238795325112869605, 1.000000000000000000, 0.9238795325112869605, 1.000000000000000000, 0.9238795325112869605, 1.000000000000000000, 0.9238795325112869605, 1.000000000000000000, 0.9238795325112869605, 1.000000000000000000, 0.9238795325112869605, 1.000000000000000000, 0.9238795325112869605, 1.000000000000000000, 0.9238795325112869605, 1.000000000000000000, 0.9238795325112869605, 1.000000000000000000, 0.9238795325112869605, 1.000000000000000000, 0.9238795325112869605, 1.000000000000000000, 0.9238795325112869605, 1.000000000000000000, 0.9238795325112869605, 1.000000000000000000, 0.9238795325112869605, 1.000000000000000000, 0.9238795325112869605, 1.000000000000000000, 0.9238795325112869605, 1.000000000000000000, 0.9238795325112869605, 1.000000000000000000, 0.9238795325112869605, 1.000000000000000000, 0.9238795325112869605, 1.000000000000000000, 0.9238795325112869605, 1.000000000000000000, 0.9238795325112869605, 1.000000000000000000, 0.9238795325112869605, 1.000000000000000000, 0.9238795325112869605, 1.000000000000000000, 0.9238795325112869605, 1.000000000000000000, 0.9238795325112869605, 1.000000000000000000, 0.9238795325112869605, 1.000000000000000000, 0.9238795325112869605, 1.000000000000000000, 0.9238795325112869605, 1.000000000000000000, 0.9238795325112869605, 1.000000000000000000, 0.9238795325112869605, 1.000000000000000000, 0.9238795325112869605, 1.000000000000000000, 0.9238795325112869605, 1.000000000000000000, 0.9238795325112869605, 1.000000000000000000, 0.9238795325112869605, 1.000000000000000000, 0.9238795325112869605, 1.000000000000000000, 0.9238795325112869605, 1.000000000000000000, 0.9238795325112869605, 1.000000000000000000, 0.9238795325112869605, 1.000000000000000000, 0.9238795325112869605, 1.000000000000000000, 0.9238795325112869605, 1.000000000000000000, 0.9238795325112869605, 1.000000000000000000, 0.9238795325112869605, 1.000000000000000000, 0.9238795325112869605, 1.000000000000000000, 0.9238795325112869605, 1.000000000000000000, 0.9238795325112869605, 1.000000000000000000, 0.9238795325112869605, 1.000000000000000000, 0.9238795325112869605, 1.000000000000000000, 0.9238795325112869605, 1.000000000000000000, 0.9238795325112869605, 1.000000000000000000, 0.9238795325112869605, 1.000000000000000000, 0.9238795325112869605, 1.000000000000000000, 0.9238795325112869605, 1.000000000000000000, 0.9238795325112869605, 1.000000000000000000, 0.9238795325112869605, 1.000000000000000000, 0.9238795325112869605, 1.000000000000000000, 0.9238795325112869605, 1.000000000000000000, 0.9238795325112869605, 1.000000000000000000, 0.9238795325112869605, 1.000000000000000000, 0.9238795325112869605, 1.000000000000000000, 0.9238795325112869605, 1.000000000000000000, 0.9238795325112869605, 1.000000000000000000, 0.9238795325112869605, 1.000000000000000000, 0.9238795325112869605, 1.000000000000000000, 0.9238795325112869605, 1.000000000000000000, 0.9238795325112869605, 1.000000000000000000, 0.9238795325112869605, 1.000000000000000000, 0.9238795325112869605, 1.000000000000000000, 0.9238795325112869605, 1.000000000000000000, 0.9238795325112869605, 1.000000000000000000, 0.9238795325112869605, 1.000000000000000000, 0.9238795325112869605, 1.000000000000000000, 0.9238795325112869605, 1.000000000000000000, 0.9238795325112869605, 1.000000000000000000, 0.9238795325112869605, 1.000000000000000000, 0.9238795325112869605, 1.000000000000000000, 0.9238795325112869605, 1.000000000000000000, 0.9238795325112869605, 1.000000000000000000, 0.9238795325112869605, 1.000000000000000000, 0.9238795325112869605, 1.000000000000000000, 0.9238795325112869605, 1.000000000000000000, 0.9238795325112869605, 1.000000000000000000, 0.9238795325112869605, 1.000000000000000000, 0.9238795325112869605, 1.000000000000000000, 0.9238795325112869605, 1.000000000000000000, 0.9238795325112869605, 1.000000000000000000, 0.9238795325112869605, 1.000000000000000000, 0.9238795325112869605, 1.000000000000000000, 0.9238795325112869605, 1.000000000000000000, 0.9238795325112869605, 1.000000000000000000, 0.9238795325112869605, 1.000000000000000000, 0.9238795325112869605, 1.000000000000000000, 0.9238795325112869605, 1.000000000000000000, 0.9238795325112869605, 1.000000000000000000, 0.9238795325112869605, 1.000000000000000000, 0.9238795325112869605, 1.000000000000000000) ) ) 
 REPRESENTATION_ITEM ( '' )  SURFACE ( )  );
#7792=CARTESIAN_POINT ( 'NONE',  ( 138.2184548109119930, -5.849744126848086090, -20.32346094940048786 ) ) ;
#7794=CARTESIAN_POINT ( 'NONE',  ( 116.0864081442453113, -9.988377603198976828, -10.36322818467138340 ) ) ;
#7799=CARTESIAN_POINT ( 'NONE',  ( 115.7460481442453357, -10.15424416112533912, -14.75197769757731336 ) ) ;
#7800=CARTESIAN_POINT ( 'NONE',  ( 117.2776681442452968, -5.638512984488999180, -18.83840828888717311 ) ) ;
#7803=CARTESIAN_POINT ( 'NONE',  ( 125.7299414775786346, -10.15424416112533912, -14.75197769757731336 ) ) ;
#7804=CARTESIAN_POINT ( 'NONE',  ( 121.4754414775786131, -1.833838273342659697, -17.42832698103878286 ) ) ;
#7805=CARTESIAN_POINT ( 'NONE',  ( 117.2209414775786485, -2.084020599724406786, -8.691656652584148546 ) ) ;
#7810=CARTESIAN_POINT ( 'NONE',  ( 118.8660148109119774, 0.1319031606808879209, -14.10382304977623669 ) ) ;
#7813=EDGE_CURVE ( 'NONE', #40452, #34050, #27414, .T. ) ;
#7814=CARTESIAN_POINT ( 'NONE',  ( 112.0020881442453344, 0.2603800115204892296, -16.42320221600525088 ) ) ;
#7817=CARTESIAN_POINT ( 'NONE',  ( 113.5904348109119866, -2.084020599724406786, -8.691656652584148546 ) ) ;
#7820=CARTESIAN_POINT ( 'NONE',  ( 118.9794681442453026, -0.8288870151387760510, -10.36305467784173118 ) ) ;
#7821=CARTESIAN_POINT ( 'NONE',  ( 116.4267681442453153, -6.222761293078241884, -8.102969835052219238 ) ) ;
#7829=AXIS2_PLACEMENT_3D ( 'NONE', #11309, #34991, #17923 ) ;
#7830=CARTESIAN_POINT ( 'NONE',  ( 112.0020881442453344, 0.2603800115204892296, -16.42320221600525088 ) ) ;
#7831=CARTESIAN_POINT ( 'NONE',  ( 126.6375681442452930, -10.15424416112533912, -14.75197769757731336 ) ) ;
#7832=CARTESIAN_POINT ( 'NONE',  ( 118.1852948109119836, -4.153390946401325223, -8.397313243818185668 ) ) ;
#7833=CYLINDRICAL_SURFACE ( 'NONE', #8286, 5.999999999999997335 ) ;
#7835=CARTESIAN_POINT ( 'NONE',  ( 114.7816948109119863, -9.859900752359374465, -12.68260735090039404 ) ) ;
#7839=CARTESIAN_POINT ( 'NONE',  ( 115.5191414775786569, -3.383040157471821630, -19.15922257007629170 ) ) ;
#7841=CARTESIAN_POINT ( 'NONE',  ( 116.8805814775786445, -6.344957434206662583, -7.627207830600332805 ) ) ;
#7844=CARTESIAN_POINT ( 'NONE',  ( 115.7460481442453357, 0.9020085738987339008, -11.91225656197089222 ) ) ;
#7845=CARTESIAN_POINT ( 'NONE',  ( 114.7816948109119863, 0.5811942927096154232, -14.16772938898807155 ) ) ;
#7847=CARTESIAN_POINT ( 'NONE',  ( 126.6827570900308473, -10.09576517521262495, -13.46436818452763973 ) ) ;
#7851=CARTESIAN_POINT ( 'NONE',  ( 112.1609860002551216, -2.334846009198400019, -18.01015021110789149 ) ) ;
#7853=CARTESIAN_POINT ( 'NONE',  ( 117.1642148109119859, -0.8288870151387760510, -10.36305467784173118 ) ) ;
#7858=CARTESIAN_POINT ( 'NONE',  ( 114.6682414775786469, -7.894159318335828068, -9.358103419637847864 ) ) ;
#7859=CARTESIAN_POINT ( 'NONE',  ( 135.6651611124131875, 1.068746826064125965, -12.64546014822358799 ) ) ;
#7860=CARTESIAN_POINT ( 'NONE',  ( 123.9714148109119805, -0.4660016031367893996, -10.09054647747474043 ) ) ;
#7861=CARTESIAN_POINT ( 'NONE',  ( 121.6456214775786293, -10.63000616557722466, -14.87417383870573495 ) ) ;
#7864=CARTESIAN_POINT ( 'NONE',  ( 117.4478481442453131, -9.565557343593413364, -10.61323700422348004 ) ) ;
#7865=CARTESIAN_POINT ( 'NONE',  ( 112.2289948109119848, -1.834011780172310813, -8.268836392978581529 ) ) ;
#7866=CARTESIAN_POINT ( 'NONE',  ( 118.6391081442452986, -4.089484607189486809, -7.948022111789456723 ) ) ;
#7867=CARTESIAN_POINT ( 'NONE',  ( 120.5678148109119832, -1.833838273342659253, -17.42832698103878286 ) ) ;
#7869=CARTESIAN_POINT ( 'NONE',  ( 122.8936081442453059, -9.565557343593413364, -10.61323700422348004 ) ) ;
#7870=CARTESIAN_POINT ( 'NONE',  ( 120.3976348109119812, -1.834011780172310813, -8.268836392978581529 ) ) ;
#7872=CARTESIAN_POINT ( 'NONE',  ( 136.4644009991209828, 0.4694575037963671926, -15.58432930555171758 ) ) ;
#7875=CARTESIAN_POINT ( 'NONE',  ( 126.8120025794041652, 0.4302159796464454788, -13.22856333804064732 ) ) ;
#7877=CARTESIAN_POINT ( 'NONE',  ( 117.7314814775786260, -4.089484607189486809, -7.948022111789456723 ) ) ;
#7879=CARTESIAN_POINT ( 'NONE',  ( 114.4980614775786734, -2.084020599724406786, -8.691656652584148546 ) ) ;
#7886=CARTESIAN_POINT ( 'NONE',  ( 118.1285681442453068, -7.893985811506177619, -18.51759400769804742 ) ) ;
#7888=CARTESIAN_POINT ( 'NONE',  ( 120.7379948109119709, 0.4262465694468514643, -12.03445270309931736 ) ) ;
#7889=CARTESIAN_POINT ( 'NONE',  ( 111.4915481442453142, -1.833838273342658365, -17.42832698103878286 ) ) ;
#7891=CARTESIAN_POINT ( 'NONE',  ( 137.4282737236246419, -7.497609102793218128, -9.036577839788058952 ) ) ;
#7892=CARTESIAN_POINT ( 'NONE',  ( 124.7655881442452852, 0.5811942927096110934, -14.16772938898807510 ) ) ;
#7894=CARTESIAN_POINT ( 'NONE',  ( 120.2841814775786276, -10.15424416112533912, -14.75197769757731336 ) ) ;
#7895=CARTESIAN_POINT ( 'NONE',  ( 117.4478481442453131, -9.565557343593413364, -10.61323700422348004 ) ) ;
#7898=CARTESIAN_POINT ( 'NONE',  ( 121.9292548109119849, -7.894159318335828068, -9.358103419637847864 ) ) ;
#7899=CARTESIAN_POINT ( 'NONE',  ( 125.7299414775786346, -10.15424416112533912, -14.75197769757731336 ) ) ;
#7900=CARTESIAN_POINT ( 'NONE',  ( 114.8951481442453115, -8.899110576539717599, -16.42337572283489067 ) ) ;
#7906=CARTESIAN_POINT ( 'NONE',  ( 117.6180281442453150, -0.4660016031367893996, -10.09054647747474043 ) ) ;
#7907=CARTESIAN_POINT ( 'NONE',  ( 119.6034614775786196, -6.344957434206665248, -7.627207830600338134 ) ) ;
#7909=CARTESIAN_POINT ( 'NONE',  ( 112.9097148109120070, 0.2603800115204892296, -16.42320221600525088 ) ) ;
#7910=ORIENTED_EDGE ( 'NONE', *, *, #7752, .F. ) ;
#7912=CARTESIAN_POINT ( 'NONE',  ( 115.6325948109119821, 0.2603800115204892296, -16.42320221600525088 ) ) ;
#7913=CARTESIAN_POINT ( 'NONE',  ( 120.2274548109119934, -9.859900752359374465, -12.68260735090039404 ) ) ;
#7915=CARTESIAN_POINT ( 'NONE',  ( 126.2404814775786264, -9.261995988541697145, -16.69588392320189030 ) ) ;
#7916=CARTESIAN_POINT ( 'NONE',  ( 121.7590748109119687, -7.893985811506177619, -18.51759400769804742 ) ) ;
#7919=CARTESIAN_POINT ( 'NONE',  ( 117.7882081442453170, -3.505236298600246325, -18.68346056562440793 ) ) ;
#7924=CARTESIAN_POINT ( 'NONE',  ( 119.0929214775786278, -5.638512984488999180, -18.83840828888717311 ) ) ;
#7925=VERTEX_POINT ( 'NONE', #40891 ) ;
#7929=CARTESIAN_POINT ( 'NONE',  ( 117.5613014775786525, -10.15424416112533912, -14.75197769757731336 ) ) ;
#7932=CARTESIAN_POINT ( 'NONE',  ( 119.5467348109119712, -5.574606645277164318, -18.38911715685844683 ) ) ;
#7934=CARTESIAN_POINT ( 'NONE',  ( 121.3052614775786111, -7.643976991954077427, -18.09477374809248928 ) ) ;
#7936=CARTESIAN_POINT ( 'NONE',  ( 123.5176014775786228, -0.8288870151387760510, -10.36305467784173118 ) ) ;
#7937=CARTESIAN_POINT ( 'NONE',  ( 114.7249681442453237, 0.2603800115204892296, -16.42320221600525088 ) ) ;
#7938=CARTESIAN_POINT ( 'NONE',  ( 119.3198281442452924, 0.5811942927096110934, -14.16772938898807510 ) ) ;
#7939=CARTESIAN_POINT ( 'NONE',  ( 111.9453614775786434, -1.561330072975668060, -17.79121239304076596 ) ) ;
#7941=CARTESIAN_POINT ( 'NONE',  ( 121.0216281442452981, -7.894159318335828068, -9.358103419637847864 ) ) ;
#7943=CARTESIAN_POINT ( 'NONE',  ( 118.8092881442453290, -9.988377603198976828, -10.36322818467138340 ) ) ;
#7949=CARTESIAN_POINT ( 'NONE',  ( 125.6732148109119862, 0.5811942927096110934, -14.16772938898807510 ) ) ;
#7950=ORIENTED_EDGE ( 'NONE', *, *, #767, .T. ) ;
#7953=CARTESIAN_POINT ( 'NONE',  ( 122.2128881442453263, -7.643976991954077427, -18.09477374809248928 ) ) ;
#7956=CARTESIAN_POINT ( 'NONE',  ( 125.7299414775786346, 0.9020085738987339008, -11.91225656197089222 ) ) ;
#7959=CARTESIAN_POINT ( 'NONE',  ( 115.4056881442453459, -7.893985811506177619, -18.51759400769804742 ) ) ;
#7960=CARTESIAN_POINT ( 'NONE',  ( 113.5337081442453240, -9.261995988541697145, -16.69588392320189030 ) ) ;
#7962=CARTESIAN_POINT ( 'NONE',  ( 121.1918081442452859, -10.15424416112533912, -14.75197769757731336 ) ) ;
#7963=CARTESIAN_POINT ( 'NONE',  ( 116.9582927111058552, -1.267766418764730840, -16.93314635290706605 ) ) ;
#7964=PRODUCT_DEFINITION ( 'UNKNOWN', '', #12593, #10563 ) ;
#7966=CARTESIAN_POINT ( 'NONE',  ( 122.1561614775786353, -0.4660016031367893996, -10.09054647747474043 ) ) ;
#7967=CARTESIAN_POINT ( 'NONE',  ( 123.6310548109119765, -4.153390946401271933, -8.397313243818190998 ) ) ;
#7974=CARTESIAN_POINT ( 'NONE',  ( 119.8870948109119752, -9.261995988541697145, -16.69588392320189030 ) ) ;
#7977=CARTESIAN_POINT ( 'NONE',  ( 111.8886348109120092, -3.383040157471821630, -19.15922257007629170 ) ) ;
#7978=CARTESIAN_POINT ( 'NONE',  ( 126.0703014775786102, -9.988377603198980381, -10.36322818467138518 ) ) ;
#7980=CARTESIAN_POINT ( 'NONE',  ( 123.9146881442452894, -10.15424416112533912, -14.75197769757731336 ) ) ;
#7982=CARTESIAN_POINT ( 'NONE',  ( 117.6747548109119919, -1.834011780172310813, -8.268836392978581529 ) ) ;
#7984=CARTESIAN_POINT ( 'NONE',  ( 116.5034398309151129, -2.215723800389698184, -18.16877924232191788 ) ) ;
#7986=CARTESIAN_POINT ( 'NONE',  ( 137.3019930433568447, -4.908147610492624935, -8.177672544428061130 ) ) ;
#7987=CARTESIAN_POINT ( 'NONE',  ( 126.0703014775786102, -9.988377603198980381, -10.36322818467138518 ) ) ;
#7991=CARTESIAN_POINT ( 'NONE',  ( 123.2906948109119867, -8.166667518702819706, -8.995218007635861213 ) ) ;
#7992=CARTESIAN_POINT ( 'NONE',  ( 123.6310548109119765, -4.153390946401325223, -8.397313243818185668 ) ) ;
#7994=CARTESIAN_POINT ( 'NONE',  ( 124.5386814775786206, -4.153390946401325223, -8.397313243818185668 ) ) ;
#7995=CARTESIAN_POINT ( 'NONE',  ( 112.7962614775786676, -6.222761293078241884, -8.102969835052219238 ) ) ;
#7996=CARTESIAN_POINT ( 'NONE',  ( 121.1918081442452859, 0.9020085738987339008, -11.91225656197089222 ) ) ;
#7997=ORIENTED_EDGE ( 'NONE', *, *, #1177, .T. ) ;
#8003=CARTESIAN_POINT ( 'NONE',  ( 126.2184548109105435, -9.814174330883648878, -12.68911139247483710 ) ) ;
#8004=CARTESIAN_POINT ( 'NONE',  ( 114.0442481442453300, -1.834011780172310813, -8.268836392978581529 ) ) ;
#8006=CARTESIAN_POINT ( 'NONE',  ( 111.3213681442453264, -7.643976991954077427, -18.09477374809248928 ) ) ;
#8009=CARTESIAN_POINT ( 'NONE',  ( 112.2289948109119848, -7.643976991954077427, -18.09477374809248928 ) ) ;
#8010=EDGE_CURVE ( 'NONE', #18562, #32667, #21070, .T. ) ;
#8011=ADVANCED_FACE ( 'NONE', ( #12626 ), #34280, .T. ) ;
#8013=DIRECTION ( 'NONE',  ( 0.000000000000000000, 0.6004852223388321697, -0.7996358532186279566 ) ) ;
#8014=CARTESIAN_POINT ( 'NONE',  ( 116.3700414775786527, -5.638512984488999180, -18.83840828888717311 ) ) ;
#8017=EDGE_LOOP ( 'NONE', ( #35997, #5690, #12699 ) ) ;
#8018=CARTESIAN_POINT ( 'NONE',  ( 126.4750299824229671, -7.440601375365601733, -8.959200753400851980 ) ) ;
#8019=CARTESIAN_POINT ( 'NONE',  ( 119.8870948109119752, -0.8288870151387760510, -10.36305467784173118 ) ) ;
#8020=CARTESIAN_POINT ( 'NONE',  ( 114.3846081442453197, -10.63000616557722466, -14.87417383870573495 ) ) ;
#8024=CARTESIAN_POINT ( 'NONE',  ( 120.2841814775786276, -10.15424416112533912, -14.75197769757731336 ) ) ;
#8025=CARTESIAN_POINT ( 'NONE',  ( 115.7460481442453357, -10.15424416112533912, -14.75197769757731336 ) ) ;
#8030=CARTESIAN_POINT ( 'NONE',  ( 117.3343948109119737, -6.222761293078241884, -8.102969835052219238 ) ) ;
#8033=CARTESIAN_POINT ( 'NONE',  ( 127.3434826497788492, -9.951987873813537888, -15.64804239197681035 ) ) ;
#8035=CARTESIAN_POINT ( 'NONE',  ( 113.4202548109119846, -10.30919188438810075, -12.61870101168855918 ) ) ;
#8037=CARTESIAN_POINT ( 'NONE',  ( 112.9664414775786412, -9.859900752359374465, -12.68260735090039404 ) ) ;
#8041=CARTESIAN_POINT ( 'NONE',  ( 121.0216281442452981, -7.894159318335828068, -9.358103419637847864 ) ) ;
#8042=CARTESIAN_POINT ( 'NONE',  ( 118.3554748109119998, -9.565557343593413364, -10.61323700422348004 ) ) ;
#8047=CARTESIAN_POINT ( 'NONE',  ( 112.1294530610591380, -8.919641830227062584, -16.32749078332169290 ) ) ;
#8052=CARTESIAN_POINT ( 'NONE',  ( 112.4559014775786494, -9.988377603198976828, -10.36322818467138340 ) ) ;
#8053=CARTESIAN_POINT ( 'NONE',  ( 126.2404814775786264, -0.8288870151387760510, -10.36305467784173118 ) ) ;
#8054=( BOUNDED_CURVE ( )  B_SPLINE_CURVE ( 2, ( #27374, #41296, #10494, #37395, #16665, #30789, #6402, #6620, #17336, #30338, #20533, #24178, #44263 ),
 .UNSPECIFIED., .F., .T. ) 
 B_SPLINE_CURVE_WITH_KNOTS ( ( 3, 2, 2, 2, 2, 2, 3 ),
 ( 0.8296282416568590001, 0.8359375000000000000, 0.8437500000000000000, 0.8515625000000000000, 0.8593750000000000000, 0.8671875000000000000, 0.8750000000000000000 ),
 .UNSPECIFIED. ) 
 CURVE ( )  GEOMETRIC_REPRESENTATION_ITEM ( )  RATIONAL_B_SPLINE_CURVE ( ( 0.9763430640195970289, 0.9385262470928680267, 1.000000000000000000, 0.9238795325112869605, 1.000000000000000000, 0.9238795325112869605, 1.000000000000000000, 0.9238795325112869605, 1.000000000000000000, 0.9238795325112869605, 1.000000000000000000, 0.9238795325112669765, 1.000000000000019984 ) ) 
 REPRESENTATION_ITEM ( '' )  );
#8055=CARTESIAN_POINT ( 'NONE',  ( 120.1140014775786398, -7.894159318335828068, -9.358103419637847864 ) ) ;
#8058=CARTESIAN_POINT ( 'NONE',  ( 120.9649014775786355, -6.222761293078241884, -8.102969835052219238 ) ) ;
#8064=CARTESIAN_POINT ( 'NONE',  ( 113.9307948109119906, 0.9020085738987339008, -11.91225656197089222 ) ) ;
#8068=CARTESIAN_POINT ( 'NONE',  ( 116.3700414775786527, -5.638512984488999180, -18.83840828888717311 ) ) ;
#8071=CARTESIAN_POINT ( 'NONE',  ( 115.4624148109119943, -5.638512984488999180, -18.83840828888717311 ) ) ;
#8074=CARTESIAN_POINT ( 'NONE',  ( 118.5256548109119876, -0.4660016031367893996, -10.09054647747474043 ) ) ;
#8075=CARTESIAN_POINT ( 'NONE',  ( 125.5597614775786326, -7.894159318335828068, -9.358103419637847864 ) ) ;
#8079=CARTESIAN_POINT ( 'NONE',  ( 111.2647102085435193, -8.897589485953298905, -16.42540022429002633 ) ) ;
#8081=CARTESIAN_POINT ( 'NONE',  ( 118.8092881442453290, -0.1624402480850797581, -16.17319339645315424 ) ) ;
#8084=CARTESIAN_POINT ( 'NONE',  ( 127.0400190879719986, -5.168639390464125682, -7.991015206380699176 ) ) ;
#8085=CARTESIAN_POINT ( 'NONE',  ( 115.2922348109119781, 0.4262465694468514643, -12.03445270309931736 ) ) ;
#8087=CARTESIAN_POINT ( 'NONE',  ( 122.7234281442452755, -5.638512984488999180, -18.83840828888717311 ) ) ;
#8088=CARTESIAN_POINT ( 'NONE',  ( 118.5823814775786360, -1.834011780172310813, -8.268836392978581529 ) ) ;
#8090=CARTESIAN_POINT ( 'NONE',  ( 116.9373081442452929, -1.833838273342659253, -17.42832698103878286 ) ) ;
#8093=CARTESIAN_POINT ( 'NONE',  ( 117.4478481442453131, 0.2603800115204892296, -16.42320221600525088 ) ) ;
#8094=CARTESIAN_POINT ( 'NONE',  ( 118.8092881442453290, -0.1624402480850797581, -16.17319339645315424 ) ) ;
#8096=CARTESIAN_POINT ( 'NONE',  ( 124.4819548109119722, -2.084020599724406786, -8.691656652584148546 ) ) ;
#8098=CARTESIAN_POINT ( 'NONE',  ( 120.2841814775786276, 0.9020085738987339008, -11.91225656197089222 ) ) ;
#8103=CARTESIAN_POINT ( 'NONE',  ( 127.5540300678602819, 0.7775483060884187392, -12.84556817354802760 ) ) ;
#8105=CARTESIAN_POINT ( 'NONE',  ( 119.4900081442453086, -1.834011780172310813, -8.268836392978581529 ) ) ;
#8106=CARTESIAN_POINT ( 'NONE',  ( 137.2618751060949762, -9.878515410958410570, -11.82152439363173357 ) ) ;
#8107=CARTESIAN_POINT ( 'NONE',  ( 115.8595014775786609, -7.643976991954077427, -18.09477374809248928 ) ) ;
#8108=CARTESIAN_POINT ( 'NONE',  ( 111.9453614775786434, -7.894159318335828068, -9.358103419637847864 ) ) ;
#8109=CARTESIAN_POINT ( 'NONE',  ( 126.2275303246276934, -0.7934555298964990344, -10.48169931380525632 ) ) ;
#8111=CARTESIAN_POINT ( 'NONE',  ( 117.7314814775786260, -5.574606645277192740, -18.38911715685844328 ) ) ;
#8113=CARTESIAN_POINT ( 'NONE',  ( 122.2897060817262513, -2.423081321603731908, -17.89265170041263175 ) ) ;
#8114=CARTESIAN_POINT ( 'NONE',  ( 112.8337832127138682, -2.191907684172563986, -18.20049396185734025 ) ) ;
#8118=CARTESIAN_POINT ( 'NONE',  ( 118.9227414775786400, -10.63000616557722466, -14.87417383870573495 ) ) ;
#8119=CARTESIAN_POINT ( 'NONE',  ( 119.4332814775786318, -8.899110576539710493, -16.42337572283490132 ) ) ;
#8120=CARTESIAN_POINT ( 'NONE',  ( 113.8740681442453138, -9.859900752359374465, -12.68260735090039404 ) ) ;
#8122=CARTESIAN_POINT ( 'NONE',  ( 137.1799701741868205, -8.769776793597710451, -9.774222394608035103 ) ) ;
#8123=CARTESIAN_POINT ( 'NONE',  ( 121.9859814775786333, 0.2603800115204892296, -16.42320221600525088 ) ) ;
#8125=CARTESIAN_POINT ( 'NONE',  ( 117.8449348109119938, -1.833838273342659253, -17.42832698103878286 ) ) ;
#8126=CARTESIAN_POINT ( 'NONE',  ( 121.5888948109119809, 0.1319031606808879209, -14.10382304977623669 ) ) ;
#8127=CARTESIAN_POINT ( 'NONE',  ( 117.7882081442453170, -3.505236298600246325, -18.68346056562440793 ) ) ;
#8130=CARTESIAN_POINT ( 'NONE',  ( 124.7088614775786226, -9.565557343593413364, -10.61323700422348004 ) ) ;
#8132=CARTESIAN_POINT ( 'NONE',  ( 122.3830681442452857, -1.833838273342659697, -17.42832698103878286 ) ) ;
#8139=CARTESIAN_POINT ( 'NONE',  ( 118.0151148109119816, -10.63000616557722466, -14.87417383870573495 ) ) ;
#8140=CARTESIAN_POINT ( 'NONE',  ( 118.9227414775786400, -10.63000616557722466, -14.87417383870573495 ) ) ;
#8142=EDGE_CURVE ( 'NONE', #30086, #33919, #40989, .T. ) ;
#8143=CARTESIAN_POINT ( 'NONE',  ( 113.8173414775786512, 0.2603800115204892296, -16.42320221600525088 ) ) ;
#8146=CARTESIAN_POINT ( 'NONE',  ( 116.3133148109119759, -7.893985811506177619, -18.51759400769804742 ) ) ;
#8147=CARTESIAN_POINT ( 'NONE',  ( 121.0216281442452981, -7.894159318335828068, -9.358103419637847864 ) ) ;
#8148=CARTESIAN_POINT ( 'NONE',  ( 113.5904348109119866, -2.084020599724406786, -8.691656652584148546 ) ) ;
#8149=CARTESIAN_POINT ( 'NONE',  ( 121.8725281442453223, -3.383040157471821630, -19.15922257007629170 ) ) ;
#8152=CARTESIAN_POINT ( 'NONE',  ( 115.2355081442453155, 0.1319031606808879209, -14.10382304977623669 ) ) ;
#8157=CARTESIAN_POINT ( 'NONE',  ( 121.1350814775786233, 0.5811942927096110934, -14.16772938898807510 ) ) ;
#8159=CARTESIAN_POINT ( 'NONE',  ( 125.7866681442452688, -8.899110576539710493, -16.42337572283490132 ) ) ;
#8162=CARTESIAN_POINT ( 'NONE',  ( 114.6682414775786469, -7.894159318335828068, -9.358103419637847864 ) ) ;
#8164=CARTESIAN_POINT ( 'NONE',  ( 123.7253032127138397, -2.191907684172563986, -18.20049396185734025 ) ) ;
#8165=CARTESIAN_POINT ( 'NONE',  ( 123.4041481442452834, 0.1319031606808879209, -14.10382304977623669 ) ) ;
#8166=CARTESIAN_POINT ( 'NONE',  ( 111.7184548109119788, -9.162420673101799196, -15.99582338542316151 ) ) ;
#8167=CARTESIAN_POINT ( 'NONE',  ( 120.9649014775786355, -6.222761293078241884, -8.102969835052219238 ) ) ;
#8169=CARTESIAN_POINT ( 'NONE',  ( 123.3474214775786209, -0.1624402480850797581, -16.17319339645315424 ) ) ;
#8170=CARTESIAN_POINT ( 'NONE',  ( 113.9307948109119906, 0.9020085738987339008, -11.91225656197089222 ) ) ;
#8171=CARTESIAN_POINT ( 'NONE',  ( 120.9649014775786355, -3.383040157471821630, -19.15922257007629170 ) ) ;
#8172=CARTESIAN_POINT ( 'NONE',  ( 113.7606148109119886, -1.561330072975668060, -17.79121239304076596 ) ) ;
#8174=CARTESIAN_POINT ( 'NONE',  ( 121.3619881442452879, -5.574606645277164318, -18.38911715685844683 ) ) ;
#8176=CARTESIAN_POINT ( 'NONE',  ( 121.7590748109119687, -7.893985811506177619, -18.51759400769804742 ) ) ;
#8185=CARTESIAN_POINT ( 'NONE',  ( 120.7379948109119709, 0.4262465694468514643, -12.03445270309931736 ) ) ;
#8190=ORIENTED_EDGE ( 'NONE', *, *, #27230, .F. ) ;
#8192=CARTESIAN_POINT ( 'NONE',  ( 113.5904348109119866, -7.893985811506177619, -18.51759400769804742 ) ) ;
#8194=CARTESIAN_POINT ( 'NONE',  ( 122.0427081442452817, -9.859900752359378018, -12.68260735090039759 ) ) ;
#8195=CARTESIAN_POINT ( 'NONE',  ( 112.7962614775786676, -6.222761293078241884, -8.102969835052219238 ) ) ;
#8197=DIRECTION ( 'NONE',  ( 0.000000000000000000, 0.6004852223388321697, -0.7996358532186279566 ) ) ;
#8202=CARTESIAN_POINT ( 'NONE',  ( 122.2696148109119889, -4.089484607189486809, -7.948022111789456723 ) ) ;
#8203=CARTESIAN_POINT ( 'NONE',  ( 137.3374356171242425, -9.397741642277191332, -15.90269339653739600 ) ) ;
#8205=CARTESIAN_POINT ( 'NONE',  ( 121.0415731642484474, -2.215723800389698184, -18.16877924232191788 ) ) ;
#8206=B_SPLINE_CURVE_WITH_KNOTS ( 'NONE', 3,
 ( #29035, #25396, #26063, #15575, #1214, #8510, #39967, #32441, #33104, #19224 ),
 .UNSPECIFIED., .F., .F.,
 ( 4, 3, 3, 4 ),
 ( 1.226634733346699927E-18, 0.0001671877548681270013, 0.0003343755096277674864, 0.0006463528481650609656 ),
 .UNSPECIFIED. ) ;
#8207=CARTESIAN_POINT ( 'NONE',  ( 124.7088614775786226, 0.2603800115204892296, -16.42320221600525088 ) ) ;
#8210=CARTESIAN_POINT ( 'NONE',  ( 123.0070614775786169, -10.15424416112533912, -14.75197769757731336 ) ) ;
#8212=CARTESIAN_POINT ( 'NONE',  ( 119.5467348109119712, -4.089484607189486809, -7.948022111789456723 ) ) ;
#8214=CARTESIAN_POINT ( 'NONE',  ( 116.5425841868944730, -2.239543233855044058, -18.13706010537467606 ) ) ;
#8215=CARTESIAN_POINT ( 'NONE',  ( 112.0588148109119828, -9.859900752359374465, -12.68260735090038693 ) ) ;
#8216=CARTESIAN_POINT ( 'NONE',  ( 116.1998614775786649, -10.63000616557722111, -14.87417383870573850 ) ) ;
#8217=CARTESIAN_POINT ( 'NONE',  ( 136.5847729262639518, -5.440308620034753240, -7.712429856759469793 ) ) ;
#8218=CARTESIAN_POINT ( 'NONE',  ( 126.1270281442452870, -10.30919188438810075, -12.61870101168855918 ) ) ;
#8222=CARTESIAN_POINT ( 'NONE',  ( 112.1722681442453222, -8.899110576539710493, -16.42337572283490132 ) ) ;
#8223=CARTESIAN_POINT ( 'NONE',  ( 125.4463081442452932, -4.153390946401325223, -8.397313243818185668 ) ) ;
#8225=CARTESIAN_POINT ( 'NONE',  ( 122.1561614775786353, -8.899110576539710493, -16.42337572283490132 ) ) ;
#8227=CARTESIAN_POINT ( 'NONE',  ( 119.1496481442453046, -3.383040157471821630, -19.15922257007629170 ) ) ;
#8230=CARTESIAN_POINT ( 'NONE',  ( 125.7299414775786488, -10.15424416112507799, -14.75197769757834543 ) ) ;
#8233=CARTESIAN_POINT ( 'NONE',  ( 126.9733055311784113, -9.947468459844838407, -11.63960890282051430 ) ) ;
#8234=CARTESIAN_POINT ( 'NONE',  ( 115.7460481442453357, 0.9020085738987339008, -11.91225656197089222 ) ) ;
#8236=CARTESIAN_POINT ( 'NONE',  ( 115.3489614775786407, -0.8288870151387760510, -10.36305467784173118 ) ) ;
#8239=CARTESIAN_POINT ( 'NONE',  ( 125.8433948109119456, -1.834011780172310813, -8.268836392978581529 ) ) ;
#8240=CARTESIAN_POINT ( 'NONE',  ( 123.1205148109119563, -7.643976991954077427, -18.09477374809248218 ) ) ;
#8242=CARTESIAN_POINT ( 'NONE',  ( 117.1642148109119859, -9.261995988541697145, -16.69588392320189030 ) ) ;
#8246=CARTESIAN_POINT ( 'NONE',  ( 126.2333338125949354, -7.752129280697795721, -9.302501600808184890 ) ) ;
#8247=CARTESIAN_POINT ( 'NONE',  ( 119.2631014775786298, -9.565557343593413364, -10.61323700422348004 ) ) ;
#8248=CARTESIAN_POINT ( 'NONE',  ( 117.3911214775786505, -1.561330072975668504, -17.79121239304076951 ) ) ;
#8250=CARTESIAN_POINT ( 'NONE',  ( 125.0492214775786266, -3.505236298600246325, -18.68346056562440793 ) ) ;
#8252=CARTESIAN_POINT ( 'NONE',  ( 124.8790414775786246, -8.899110576539710493, -16.42337572283490132 ) ) ;
#8253=CARTESIAN_POINT ( 'NONE',  ( 116.2565881442453133, -0.8288870151387760510, -10.36305467784173118 ) ) ;
#8257=FACE_OUTER_BOUND ( 'NONE', #39943, .T. ) ;
#8258=CARTESIAN_POINT ( 'NONE',  ( 116.9373081442452929, -1.833838273342659253, -17.42832698103878286 ) ) ;
#8261=CARTESIAN_POINT ( 'NONE',  ( 115.2355081442453155, -10.30919188438810075, -12.61870101168855918 ) ) ;
#8263=CARTESIAN_POINT ( 'NONE',  ( 112.6260814775786514, -0.8288870151387760510, -10.36305467784173118 ) ) ;
#8266=CARTESIAN_POINT ( 'NONE',  ( 120.9649014775786355, -6.222761293078241884, -8.102969835052219238 ) ) ;
#8267=CARTESIAN_POINT ( 'NONE',  ( 116.4834948109119779, -7.894159318335828068, -9.358103419637847864 ) ) ;
#8270=CARTESIAN_POINT ( 'NONE',  ( 116.5969481442453031, -9.859900752359374465, -12.68260735090039404 ) ) ;
#8277=CARTESIAN_POINT ( 'NONE',  ( 116.0296814775786345, -8.166667518702817929, -8.995218007635861213 ) ) ;
#8278=CARTESIAN_POINT ( 'NONE',  ( 112.1155414775786454, 0.9020085738987339008, -11.91225656197089222 ) ) ;
#8279=CARTESIAN_POINT ( 'NONE',  ( 115.1220548109119761, -1.833838273342658809, -17.42832698103878286 ) ) ;
#8280=CARTESIAN_POINT ( 'NONE',  ( 122.3263414775786373, -3.505236298600246325, -18.68346056562440793 ) ) ;
#8283=CARTESIAN_POINT ( 'NONE',  ( 120.5110881442453206, -3.505236298600246325, -18.68346056562440793 ) ) ;
#8284=CARTESIAN_POINT ( 'NONE',  ( 125.5597614775786326, -7.894159318335828068, -9.358103419637847864 ) ) ;
#8286=AXIS2_PLACEMENT_3D ( 'NONE', #19217, #28587, #21739 ) ;
#8289=CARTESIAN_POINT ( 'NONE',  ( 117.6180281442453150, -0.4660016031367893996, -10.09054647747474043 ) ) ;
#8291=CARTESIAN_POINT ( 'NONE',  ( 117.5613014775786525, 0.9020085738987339008, -11.91225656197089222 ) ) ;
#8292=DIRECTION ( 'NONE',  ( 1.000000000000000000, 0.000000000000000000, 0.000000000000000000 ) ) ;
#8294=CARTESIAN_POINT ( 'NONE',  ( 115.4056881442453459, -7.893985811506177619, -18.51759400769804742 ) ) ;
#8295=CARTESIAN_POINT ( 'NONE',  ( 118.7525614775786380, -8.166667518702819706, -8.995218007635861213 ) ) ;
#8303=CARTESIAN_POINT ( 'NONE',  ( 118.6391081442452986, -5.574606645277164318, -18.38911715685844683 ) ) ;
#8306=CARTESIAN_POINT ( 'NONE',  ( 115.8027748109119841, -8.899110576539710493, -16.42337572283490132 ) ) ;
#8309=CARTESIAN_POINT ( 'NONE',  ( 114.1009748109119784, -5.574606645277164318, -18.38911715685844683 ) ) ;
#8310=CARTESIAN_POINT ( 'NONE',  ( 118.7525614775786380, -8.166667518702819706, -8.995218007635861213 ) ) ;
#8311=EDGE_LOOP ( 'NONE', ( #33161, #14690, #16253, #17208 ) ) ;
#8313=CARTESIAN_POINT ( 'NONE',  ( 118.5823814775786360, -7.643976991954077427, -18.09477374809248928 ) ) ;
#8314=CARTESIAN_POINT ( 'NONE',  ( 115.9162281442453235, -4.089484607189486809, -7.948022111789456723 ) ) ;
#8315=CARTESIAN_POINT ( 'NONE',  ( 121.1350814775786233, 0.5811942927096110934, -14.16772938898807510 ) ) ;
#8316=CARTESIAN_POINT ( 'NONE',  ( 119.0361948109119652, -2.084020599724406786, -8.691656652584148546 ) ) ;
#8318=CARTESIAN_POINT ( 'NONE',  ( 125.0492214775786266, -3.505236298600246325, -18.68346056562440793 ) ) ;
#8319=CARTESIAN_POINT ( 'NONE',  ( 121.7023481442452777, -9.261995988541697145, -16.69588392320189030 ) ) ;
#8321=EDGE_CURVE ( 'NONE', #18562, #25347, #40410, .T. ) ;
#8326=CARTESIAN_POINT ( 'NONE',  ( 118.9279538206745315, -2.348512537728035365, -17.99195118506215252 ) ) ;
#8330=CARTESIAN_POINT ( 'NONE',  ( 115.3489614775786407, -0.8288870151387760510, -10.36305467784173118 ) ) ;
#8331=CARTESIAN_POINT ( 'NONE',  ( 111.7184548109119788, -0.8288870151387760510, -10.36305467784173118 ) ) ;
#8333=CARTESIAN_POINT ( 'NONE',  ( 117.4478481442452846, -9.565557343593393824, -10.61323700422345340 ) ) ;
#8335=CARTESIAN_POINT ( 'NONE',  ( 115.5566632127138575, -2.191907684172563986, -18.20049396185734025 ) ) ;
#8337=CARTESIAN_POINT ( 'NONE',  ( 124.1014853070358868, -1.196538596002817867, -17.02799684832028504 ) ) ;
#8339=CARTESIAN_POINT ( 'NONE',  ( 118.8660148109119774, -10.30919188438810075, -12.61870101168855918 ) ) ;
#8340=CARTESIAN_POINT ( 'NONE',  ( 124.5954081442453116, -6.222761293078241884, -8.102969835052219238 ) ) ;
#8342=CARTESIAN_POINT ( 'NONE',  ( 137.3374356171252373, -7.373476992039340594, -8.859472353902042130 ) ) ;
#8343=CARTESIAN_POINT ( 'NONE',  ( 124.8790414775786246, -0.4660016031367893996, -10.09054647747474043 ) ) ;
#8345=CARTESIAN_POINT ( 'NONE',  ( 118.8660148109119774, 0.1319031606808879209, -14.10382304977623669 ) ) ;
#8346=CARTESIAN_POINT ( 'NONE',  ( 122.7801548109119665, -6.222761293078241884, -8.102969835052219238 ) ) ;
#8347=CARTESIAN_POINT ( 'NONE',  ( 116.9373081442452929, -1.833838273342659253, -17.42832698103878286 ) ) ;
#8348=CARTESIAN_POINT ( 'NONE',  ( 111.7184548109119788, -8.862178061932382889, -16.39564131203247399 ) ) ;
#8350=CARTESIAN_POINT ( 'NONE',  ( 124.5386814775786206, -4.153390946401325223, -8.397313243818185668 ) ) ;
#8351=CARTESIAN_POINT ( 'NONE',  ( 123.8579614775786126, -9.859900752359378018, -12.68260735090039759 ) ) ;
#8358=CARTESIAN_POINT ( 'NONE',  ( 121.5888948109119809, -10.30919188438810075, -12.61870101168855918 ) ) ;
#8359=CARTESIAN_POINT ( 'NONE',  ( 117.9016614775786280, -9.988377603198976828, -10.36322818467138340 ) ) ;
#8361=CARTESIAN_POINT ( 'NONE',  ( 112.2857214775786474, -4.089484607189486809, -7.948022111789456723 ) ) ;
#8366=CARTESIAN_POINT ( 'NONE',  ( 117.5613014775786525, 0.9020085738987339008, -11.91225656197089222 ) ) ;
#8367=CARTESIAN_POINT ( 'NONE',  ( 124.7655881442452852, -9.859900752359378018, -12.68260735090039759 ) ) ;
#8369=CARTESIAN_POINT ( 'NONE',  ( 112.6260814775786514, -0.8288870151387760510, -10.36305467784173118 ) ) ;
#8370=CARTESIAN_POINT ( 'NONE',  ( 124.9924948109119924, -4.089484607189486809, -7.948022111789456723 ) ) ;
#8373=CARTESIAN_POINT ( 'NONE',  ( 118.7525614775786380, -1.833838273342659253, -17.42832698103878286 ) ) ;
#8379=CARTESIAN_POINT ( 'NONE',  ( 119.1496481442453046, -3.383040157471821630, -19.15922257007629170 ) ) ;
#8381=CARTESIAN_POINT ( 'NONE',  ( 125.6164881442453094, -9.565557343593413364, -10.61323700422348004 ) ) ;
#8385=CARTESIAN_POINT ( 'NONE',  ( 118.1852948109119836, -4.153390946401325223, -8.397313243818185668 ) ) ;
#8388=CARTESIAN_POINT ( 'NONE',  ( 123.8035975202278109, -2.239543233855044946, -18.13706010537467606 ) ) ;
#8389=CARTESIAN_POINT ( 'NONE',  ( 123.5743281442453139, -2.084020599724406786, -8.691656652584148546 ) ) ;
#8390=CARTESIAN_POINT ( 'NONE',  ( 121.4187148109119789, -6.344957434206645708, -7.627207830600334582 ) ) ;
#8394=CARTESIAN_POINT ( 'NONE',  ( 117.8449348109119938, -1.833838273342659253, -17.42832698103878286 ) ) ;
#8395=CARTESIAN_POINT ( 'NONE',  ( 123.0637881442452937, -8.899110576539710493, -16.42337572283490132 ) ) ;
#8396=CARTESIAN_POINT ( 'NONE',  ( 113.4202548109119846, -10.30919188438810075, -12.61870101168855918 ) ) ;
#8397=CARTESIAN_POINT ( 'NONE',  ( 121.2485348109119769, -0.4660016031367893996, -10.09054647747474043 ) ) ;
#8398=CARTESIAN_POINT ( 'NONE',  ( 115.5191414775786569, -3.383040157471821630, -19.15922257007629170 ) ) ;
#8401=CARTESIAN_POINT ( 'NONE',  ( 125.3328548109119964, -0.8288870151387760510, -10.36305467784173118 ) ) ;
#8403=CARTESIAN_POINT ( 'NONE',  ( 119.8303681442453126, -10.63000616557722466, -14.87417383870573495 ) ) ;
#8409=CARTESIAN_POINT ( 'NONE',  ( 126.1270281442452870, -10.30919188438810075, -12.61870101168855918 ) ) ;
#8411=CARTESIAN_POINT ( 'NONE',  ( 120.4543614775786295, -5.574606645277164318, -18.38911715685844683 ) ) ;
#8417=CARTESIAN_POINT ( 'NONE',  ( 113.4769814775786330, -10.63000616557722466, -14.87417383870573495 ) ) ;
#8419=CARTESIAN_POINT ( 'NONE',  ( 119.9438214775786378, -2.084020599724406786, -8.691656652584148546 ) ) ;
#8422=CARTESIAN_POINT ( 'NONE',  ( 115.0286927483929134, -2.423081321603721694, -17.89265170041262465 ) ) ;
#8424=ORIENTED_EDGE ( 'NONE', *, *, #34011, .F. ) ;
#8428=CARTESIAN_POINT ( 'NONE',  ( 119.1496481442453046, -3.383040157471821630, -19.15922257007629170 ) ) ;
#8429=CARTESIAN_POINT ( 'NONE',  ( 137.0105207745601774, -8.461374316958192310, -17.49868728018336483 ) ) ;
#8431=CARTESIAN_POINT ( 'NONE',  ( 112.5693548109119888, -10.63000616557722466, -14.87417383870573495 ) ) ;
#8432=CARTESIAN_POINT ( 'NONE',  ( 111.7751814775786556, -2.084020599724406786, -8.691656652584148546 ) ) ;
#8435=CARTESIAN_POINT ( 'NONE',  ( 123.0637881442452937, -8.899110576539710493, -16.42337572283490132 ) ) ;
#8437=CARTESIAN_POINT ( 'NONE',  ( 117.4478481442453131, 0.2603800115204892296, -16.42320221600525088 ) ) ;
#8441=CARTESIAN_POINT ( 'NONE',  ( 116.8439460817262585, -2.423081321603731020, -17.89265170041263175 ) ) ;
#8444=CARTESIAN_POINT ( 'NONE',  ( 112.8529881442453160, -7.894159318335828068, -9.358103419637847864 ) ) ;
#8445=CARTESIAN_POINT ( 'NONE',  ( 128.2184548109119930, 0.7167481258041193959, -11.18974888642105014 ) ) ;
#8448=CARTESIAN_POINT ( 'NONE',  ( 113.4202548109119846, 0.1319031606808879209, -14.10382304977623669 ) ) ;
#8449=CARTESIAN_POINT ( 'NONE',  ( 112.5126281442453120, -10.30919188438810075, -12.61870101168855918 ) ) ;
#8451=CARTESIAN_POINT ( 'NONE',  ( 124.7088614775786226, -9.565557343593413364, -10.61323700422348004 ) ) ;
#8453=CARTESIAN_POINT ( 'NONE',  ( 120.7947214775786193, -9.261995988541697145, -16.69588392320189030 ) ) ;
#8455=CARTESIAN_POINT ( 'NONE',  ( 127.4620922276976955, -8.463570135024619745, -17.71167606724072741 ) ) ;
#8459=ADVANCED_FACE ( 'NONE', ( #34407 ), #40684, .T. ) ;
#8460=CARTESIAN_POINT ( 'NONE',  ( 126.2471382750683659, -9.795756905406328485, -12.48647926791751139 ) ) ;
#8461=CARTESIAN_POINT ( 'NONE',  ( 113.8740681442453138, 0.5811942927096154232, -14.16772938898807155 ) ) ;
#8462=ORIENTED_EDGE ( 'NONE', *, *, #41925, .T. ) ;
#8467=CARTESIAN_POINT ( 'NONE',  ( 112.4559014775786494, -9.988377603198976828, -10.36322818467138340 ) ) ;
#8468=CARTESIAN_POINT ( 'NONE',  ( 119.3198281442452924, 0.5811942927096110934, -14.16772938898807510 ) ) ;
#8473=CARTESIAN_POINT ( 'NONE',  ( 117.9016614775786280, -0.1624402480850797581, -16.17319339645315424 ) ) ;
#8474=CARTESIAN_POINT ( 'NONE',  ( 115.2355081442453155, -10.30919188438810075, -12.61870101168855918 ) ) ;
#8476=CARTESIAN_POINT ( 'NONE',  ( 118.2420214775786462, -6.222761293078222344, -8.102969835052219238 ) ) ;
#8477=CARTESIAN_POINT ( 'NONE',  ( 123.3474214775786209, -0.1624402480850797581, -16.17319339645315424 ) ) ;
#8478=CARTESIAN_POINT ( 'NONE',  ( 115.5191414775786569, -6.222761293078241884, -8.102969835052219238 ) ) ;
#8483=CARTESIAN_POINT ( 'NONE',  ( 116.9940348109119839, -0.1624402480850797581, -16.17319339645315424 ) ) ;
#8484=ORIENTED_EDGE ( 'NONE', *, *, #34740, .F. ) ;
#8485=CARTESIAN_POINT ( 'NONE',  ( 128.2184548109119930, -4.863998795839242995, -13.39321520033831447 ) ) ;
#8486=CARTESIAN_POINT ( 'NONE',  ( 114.4413348109119823, -9.261995988541697145, -16.69588392320189030 ) ) ;
#8488=CARTESIAN_POINT ( 'NONE',  ( 125.6732148109119862, -9.859900752359378018, -12.68260735090039759 ) ) ;
#8490=VERTEX_POINT ( 'NONE', #35521 ) ;
#8492=CARTESIAN_POINT ( 'NONE',  ( 120.7379948109119709, 0.4262465694468514643, -12.03445270309931736 ) ) ;
#8494=CARTESIAN_POINT ( 'NONE',  ( 117.1642148109119859, -0.8288870151387760510, -10.36305467784173118 ) ) ;
#8501=CARTESIAN_POINT ( 'NONE',  ( 115.3489614775786407, -9.261995988541697145, -16.69588392320189030 ) ) ;
#8502=CARTESIAN_POINT ( 'NONE',  ( 115.0086014775786509, -4.089484607189486809, -7.948022111789456723 ) ) ;
#8503=CARTESIAN_POINT ( 'NONE',  ( 114.3278814775786429, 0.1319031606808879209, -14.10382304977623669 ) ) ;
#8504=CARTESIAN_POINT ( 'NONE',  ( 120.0572748109119772, -6.222761293078241884, -8.102969835052219238 ) ) ;
#8505=CARTESIAN_POINT ( 'NONE',  ( 112.3808888976800233, -1.244021962887382315, -16.96476564598603787 ) ) ;
#8507=CARTESIAN_POINT ( 'NONE',  ( 120.0005481442453146, -4.153390946401325223, -8.397313243818185668 ) ) ;
#8508=CARTESIAN_POINT ( 'NONE',  ( 124.7655881442452852, -9.859900752359378018, -12.68260735090039759 ) ) ;
#8510=CARTESIAN_POINT ( 'NONE',  ( 114.0390358011494385, -1.149058757900090377, -17.09122335155388939 ) ) ;
#8512=CARTESIAN_POINT ( 'NONE',  ( 119.7736414775786358, -10.30919188438810075, -12.61870101168855918 ) ) ;
#8513=B_SPLINE_CURVE_WITH_KNOTS ( 'NONE', 3,
 ( #24698, #38370, #530, #17862, #38586, #14217, #31535, #4394, #35393, #42489 ),
 .UNSPECIFIED., .F., .F.,
 ( 4, 3, 3, 4 ),
 ( 8.673617379884039324E-19, 0.0001671877548681294950, 0.0003343755096277725280, 0.0006463528481650619413 ),
 .UNSPECIFIED. ) ;
#8515=CARTESIAN_POINT ( 'NONE',  ( 122.2128881442453263, -1.834011780172310813, -8.268836392978581529 ) ) ;
#8518=CARTESIAN_POINT ( 'NONE',  ( 117.8449348109119938, -8.166667518702817929, -8.995218007635861213 ) ) ;
#8519=B_SPLINE_CURVE_WITH_KNOTS ( 'NONE', 3,
 ( #28626, #38634, #17460, #7408, #10849, #28850, #31358, #42535, #3545, #11295, #3986, #131, #14487, #42761, #4216, #28398, #14043, #10628, #18362, #38419, #34976, #18132, #25205, #577, #24974, #42310, #11525, #25430, #3763, #14265, #41868, #31806, #11070, #35439, #39101, #28181, #24747, #7872, #21328, #24532, #35214, #21552, #7190, #21780, #17909, #4444 ),
 .UNSPECIFIED., .F., .F.,
 ( 4, 2, 2, 2, 2, 2, 2, 2, 2, 2, 2, 2, 2, 2, 2, 2, 2, 2, 2, 2, 2, 2, 4 ),
 ( 0.000000000000000000, 0.06249999999998950839, 0.09374999999999088229, 0.1093749999999976547, 0.1250000000000044409, 0.1875000000000314748, 0.2187500000000399958, 0.2500000000000485167, 0.3750000000000693889, 0.4375000000000795475, 0.5000000000000897060, 0.5625000000000998090, 0.5937500000001049161, 0.6093750000001075806, 0.6250000000001101341, 0.6875000000001189049, 0.7187500000001230127, 0.7343750000001187939, 0.7500000000001144640, 0.8125000000000971445, 0.8437500000000810463, 0.8750000000000649480, 1.000000000000000000 ),
 .UNSPECIFIED. ) ;
#8520=CARTESIAN_POINT ( 'NONE',  ( 119.0929214775786278, -5.638512984488999180, -18.83840828888717311 ) ) ;
#8521=CARTESIAN_POINT ( 'NONE',  ( 126.3975136127465362, -9.949554030138139993, -13.18299365370083898 ) ) ;
#8525=DIRECTION ( 'NONE',  ( 1.000000000000000000, 0.000000000000000000, 0.000000000000000000 ) ) ;
#8527=CARTESIAN_POINT ( 'NONE',  ( 119.6034614775786196, -3.505236298600246325, -18.68346056562440793 ) ) ;
#8530=CARTESIAN_POINT ( 'NONE',  ( 113.2500748109119968, -3.505236298600246325, -18.68346056562440793 ) ) ;
#8533=CARTESIAN_POINT ( 'NONE',  ( 111.8886348109120092, -6.222761293078241884, -8.102969835052219238 ) ) ;
#8534=CARTESIAN_POINT ( 'NONE',  ( 119.0929214775786278, -5.638512984488999180, -18.83840828888717311 ) ) ;
#8535=ORIENTED_EDGE ( 'NONE', *, *, #34388, .F. ) ;
#8537=CARTESIAN_POINT ( 'NONE',  ( 117.1074881442453233, 0.4262465694468514643, -12.03445270309931736 ) ) ;
#8538=CARTESIAN_POINT ( 'NONE',  ( 113.4769814775786330, -10.63000616557722466, -14.87417383870573495 ) ) ;
#8539=CARTESIAN_POINT ( 'NONE',  ( 120.8514481442452961, -7.893985811506177619, -18.51759400769804742 ) ) ;
#8540=CARTESIAN_POINT ( 'NONE',  ( 118.9794681442453026, -0.8288870151387760510, -10.36305467784173118 ) ) ;
#8542=CARTESIAN_POINT ( 'NONE',  ( 123.7445081442452874, -7.894159318335828068, -9.358103419637847864 ) ) ;
#8543=CARTESIAN_POINT ( 'NONE',  ( 119.6034614775786196, -6.344957434206665248, -7.627207830600338134 ) ) ;
#8546=CARTESIAN_POINT ( 'NONE',  ( 120.7947214775786193, -9.261995988541697145, -16.69588392320189030 ) ) ;
#8549=CARTESIAN_POINT ( 'NONE',  ( 138.0385288853987049, -1.837662360184606714, -16.17424470069298081 ) ) ;
#8553=CARTESIAN_POINT ( 'NONE',  ( 116.4267681442453153, -6.222761293078241884, -8.102969835052219238 ) ) ;
#8554=CARTESIAN_POINT ( 'NONE',  ( 111.7751814775786556, -2.084020599724406786, -8.691656652584148546 ) ) ;
#8560=CARTESIAN_POINT ( 'NONE',  ( 115.9729548109119861, -3.505236298600246325, -18.68346056562440793 ) ) ;
#8563=CARTESIAN_POINT ( 'NONE',  ( 124.0229291344827516, -1.149058757900107697, -17.09122335155391781 ) ) ;
#8565=CARTESIAN_POINT ( 'NONE',  ( 119.7169148109119874, -9.988377603198976828, -10.36322818467138340 ) ) ;
#8566=CARTESIAN_POINT ( 'NONE',  ( 121.6456214775786293, 0.4262465694468514643, -12.03445270309931736 ) ) ;
#8569=CARTESIAN_POINT ( 'NONE',  ( 126.0135748109119902, -8.166667518702819706, -8.995218007635861213 ) ) ;
#8571=CARTESIAN_POINT ( 'NONE',  ( 123.9714148109119805, -8.899110576539710493, -16.42337572283490132 ) ) ;
#8572=CARTESIAN_POINT ( 'NONE',  ( 122.4965214775786251, 0.1319031606808879209, -14.10382304977623669 ) ) ;
#8573=CARTESIAN_POINT ( 'NONE',  ( 114.8384214775786489, -10.15424416112533912, -14.75197769757731336 ) ) ;
#8574=CARTESIAN_POINT ( 'NONE',  ( 120.8842620163423192, -1.087735405160626723, -17.17288456429612964 ) ) ;
#8576=CARTESIAN_POINT ( 'NONE',  ( 125.5597614775786326, -7.894159318335828068, -9.358103419637847864 ) ) ;
#8577=CARTESIAN_POINT ( 'NONE',  ( 122.2128881442453263, -7.643976991954077427, -18.09477374809248928 ) ) ;
#8578=CARTESIAN_POINT ( 'NONE',  ( 112.1722681442453222, -8.899110576539710493, -16.42337572283490132 ) ) ;
#8584=CARTESIAN_POINT ( 'NONE',  ( 121.4754414775786131, -8.166667518702819706, -8.995218007635861213 ) ) ;
#8585=CARTESIAN_POINT ( 'NONE',  ( 118.5256548109119876, -0.4660016031367893996, -10.09054647747474043 ) ) ;
#8587=CARTESIAN_POINT ( 'NONE',  ( 116.0296814775786345, -8.166667518702817929, -8.995218007635861213 ) ) ;
#8593=CARTESIAN_POINT ( 'NONE',  ( 119.0929214775786278, -5.638512984488999180, -18.83840828888717311 ) ) ;
#8594=CARTESIAN_POINT ( 'NONE',  ( 123.9714148109119805, -8.899110576539710493, -16.42337572283490132 ) ) ;
#8596=CARTESIAN_POINT ( 'NONE',  ( 114.3846081442453197, 0.4262465694468514643, -12.03445270309931736 ) ) ;
#8597=CARTESIAN_POINT ( 'NONE',  ( 111.8319081442453182, -4.153390946401321671, -8.397313243818183892 ) ) ;
#8599=CARTESIAN_POINT ( 'NONE',  ( 119.3765548109119834, -10.15424416112533912, -14.75197769757731336 ) ) ;
#8604=CARTESIAN_POINT ( 'NONE',  ( 123.4041481442452834, -10.30919188438810075, -12.61870101168855918 ) ) ;
#8606=CARTESIAN_POINT ( 'NONE',  ( 125.6732148109119862, -9.859900752359378018, -12.68260735090039759 ) ) ;
#8610=CARTESIAN_POINT ( 'NONE',  ( 118.2987481442453088, -7.894159318335828068, -9.358103419637847864 ) ) ;
#8614=CARTESIAN_POINT ( 'NONE',  ( 124.1983214775786166, -1.833838273342659697, -17.42832698103878286 ) ) ;
#8616=CARTESIAN_POINT ( 'NONE',  ( 124.3685014775786328, 0.4262465694468514643, -12.03445270309931736 ) ) ;
#8619=CARTESIAN_POINT ( 'NONE',  ( 122.6099748109119929, -9.261995988541697145, -16.69588392320189030 ) ) ;
#8620=CARTESIAN_POINT ( 'NONE',  ( 116.9940348109119839, -0.1624402480850797581, -16.17319339645315424 ) ) ;
#8621=CARTESIAN_POINT ( 'NONE',  ( 124.3117748109119844, 0.1319031606808879209, -14.10382304977623669 ) ) ;
#8622=CARTESIAN_POINT ( 'NONE',  ( 120.1707281442453166, 0.2603800115204892296, -16.42320221600525088 ) ) ;
#8623=CARTESIAN_POINT ( 'NONE',  ( 115.1220548109119761, -8.166667518702817929, -8.995218007635861213 ) ) ;
#8625=CARTESIAN_POINT ( 'NONE',  ( 125.1059481442452750, -1.833838273342660141, -17.42832698103878286 ) ) ;
#8627=CARTESIAN_POINT ( 'NONE',  ( 118.7525614775786380, -8.166667518702819706, -8.995218007635861213 ) ) ;
#8631=CARTESIAN_POINT ( 'NONE',  ( 112.3424481442453384, -3.505236298600246325, -18.68346056562440793 ) ) ;
#8635=CARTESIAN_POINT ( 'NONE',  ( 123.9146881442452894, -10.15424416112533912, -14.75197769757731336 ) ) ;
#8639=CARTESIAN_POINT ( 'NONE',  ( 111.9559014775786494, -9.522524984348095245, -10.63868154973201108 ) ) ;
#8642=CARTESIAN_POINT ( 'NONE',  ( 114.5547881442453217, -5.638512984488999180, -18.83840828888717311 ) ) ;
#8644=CARTESIAN_POINT ( 'NONE',  ( 123.9714148109119805, -8.899110576539710493, -16.42337572283490132 ) ) ;
#8645=CARTESIAN_POINT ( 'NONE',  ( 113.9875214775786532, -8.899110576539710493, -16.42337572283490132 ) ) ;
#8647=CARTESIAN_POINT ( 'NONE',  ( 124.4819548109119722, -7.893985811506201600, -18.51759400769803676 ) ) ;
#8648=CARTESIAN_POINT ( 'NONE',  ( 113.3635281442453504, -9.988377603198976828, -10.36322818467138340 ) ) ;
#8650=CARTESIAN_POINT ( 'NONE',  ( 123.2906948109119867, -8.166667518702819706, -8.995218007635861213 ) ) ;
#8651=CARTESIAN_POINT ( 'NONE',  ( 136.1332990479132263, -10.31707786543337058, -15.60180518456300547 ) ) ;
#8653=CARTESIAN_POINT ( 'NONE',  ( 114.4980614775786592, -7.893985811506177619, -18.51759400769804742 ) ) ;
#8654=CARTESIAN_POINT ( 'NONE',  ( 125.9568481442452850, -6.344957434206665248, -7.627207830600338134 ) ) ;
#8656=CARTESIAN_POINT ( 'NONE',  ( 112.3424481442453384, -6.344957434206662583, -7.627207830600332805 ) ) ;
#8658=CARTESIAN_POINT ( 'NONE',  ( 119.6601881442453106, -8.166667518702819706, -8.995218007635861213 ) ) ;
#8661=CARTESIAN_POINT ( 'NONE',  ( 120.1332064091100733, -0.9924539043446216624, -17.29976612834909133 ) ) ;
#8662=CARTESIAN_POINT ( 'NONE',  ( 136.9012041053388486, -2.916721388012065930, -8.216909731286408558 ) ) ;
#8663=CARTESIAN_POINT ( 'NONE',  ( 114.1009748109119784, -5.574606645277164318, -18.38911715685844683 ) ) ;
#8667=CARTESIAN_POINT ( 'NONE',  ( 113.8740681442453138, -9.859900752359374465, -12.68260735090039404 ) ) ;
#8668=CARTESIAN_POINT ( 'NONE',  ( 112.0588148109119828, 0.5811942927096154232, -14.16772938898807155 ) ) ;
#8670=CARTESIAN_POINT ( 'NONE',  ( 122.6667014775786413, -2.084020599724406786, -8.691656652584148546 ) ) ;
#8671=FACE_OUTER_BOUND ( 'NONE', #44083, .T. ) ;
#8672=CARTESIAN_POINT ( 'NONE',  ( 123.9714148109119805, -0.4660016031367893996, -10.09054647747474043 ) ) ;
#8674=CARTESIAN_POINT ( 'NONE',  ( 121.9292548109119849, -1.561330072975668948, -17.79121239304076951 ) ) ;
#8675=ORIENTED_EDGE ( 'NONE', *, *, #24760, .T. ) ;
#8676=CARTESIAN_POINT ( 'NONE',  ( 136.4689272580744444, 0.8652765085456386451, -12.77968882490968561 ) ) ;
#8680=CARTESIAN_POINT ( 'NONE',  ( 127.7429221096635672, -10.18842876247218499, -11.18798664339182380 ) ) ;
#8681=CARTESIAN_POINT ( 'NONE',  ( 116.6536748109119941, 0.9020085738987339008, -11.91225656197089222 ) ) ;
#8684=CARTESIAN_POINT ( 'NONE',  ( 119.4332814775786318, -8.899110576539721151, -16.42337572283488711 ) ) ;
#8685=CARTESIAN_POINT ( 'NONE',  ( 115.0086014775786509, -5.574606645277164318, -18.38911715685844683 ) ) ;
#8686=CARTESIAN_POINT ( 'NONE',  ( 112.5126281442453120, -10.30919188438810075, -12.61870101168855918 ) ) ;
#8687=CARTESIAN_POINT ( 'NONE',  ( 120.1140014775786398, -1.561330072975668504, -17.79121239304076951 ) ) ;
#8692=CARTESIAN_POINT ( 'NONE',  ( 120.1707281442453166, -9.565557343593413364, -10.61323700422348004 ) ) ;
#8693=CARTESIAN_POINT ( 'NONE',  ( 114.4413348109119823, -9.261995988541697145, -16.69588392320189030 ) ) ;
#8694=CARTESIAN_POINT ( 'NONE',  ( 113.7038881442453402, -3.383040157471821630, -19.15922257007629170 ) ) ;
#8697=CARTESIAN_POINT ( 'NONE',  ( 122.0427081442452817, -9.859900752359378018, -12.68260735090039759 ) ) ;
#8698=CARTESIAN_POINT ( 'NONE',  ( 117.7882081442453170, -3.505236298600246325, -18.68346056562440793 ) ) ;
#8702=CARTESIAN_POINT ( 'NONE',  ( 114.1009748109119784, -4.089484607189486809, -7.948022111789456723 ) ) ;
#8703=CARTESIAN_POINT ( 'NONE',  ( 118.4689281442453250, -10.15424416112533912, -14.75197769757731336 ) ) ;
#8704=ORIENTED_EDGE ( 'NONE', *, *, #31525, .F. ) ;
#8707=CARTESIAN_POINT ( 'NONE',  ( 113.3635281442453504, -9.988377603198976828, -10.36322818467138340 ) ) ;
#8709=CARTESIAN_POINT ( 'NONE',  ( 113.7038881442453402, -6.222761293078241884, -8.102969835052219238 ) ) ;
#8711=ORIENTED_EDGE ( 'NONE', *, *, #24211, .F. ) ;
#8712=CARTESIAN_POINT ( 'NONE',  ( 123.2339681442453241, -3.505236298600246325, -18.68346056562440793 ) ) ;
#8713=CARTESIAN_POINT ( 'NONE',  ( 122.8368814775786291, -7.894159318335828068, -9.358103419637847864 ) ) ;
#8716=ORIENTED_EDGE ( 'NONE', *, *, #40630, .F. ) ;
#8720=CARTESIAN_POINT ( 'NONE',  ( 115.8595014775786609, -1.834011780172310813, -8.268836392978581529 ) ) ;
#8721=CARTESIAN_POINT ( 'NONE',  ( 114.1577014775786552, -6.344957434206662583, -7.627207830600332805 ) ) ;
#8722=CARTESIAN_POINT ( 'NONE',  ( 115.1787814775786387, -0.1624402480850797581, -16.17319339645315424 ) ) ;
#8723=CARTESIAN_POINT ( 'NONE',  ( 120.6812681442452941, 0.1319031606808879209, -14.10382304977623669 ) ) ;
#8726=CARTESIAN_POINT ( 'NONE',  ( 120.1707281442453166, -9.565557343593413364, -10.61323700422348004 ) ) ;
#8727=CARTESIAN_POINT ( 'NONE',  ( 123.4608748109119745, 0.4262465694468514643, -12.03445270309931736 ) ) ;
#8732=CARTESIAN_POINT ( 'NONE',  ( 117.9583881442453048, -10.30919188438810075, -12.61870101168855918 ) ) ;
#8734=CARTESIAN_POINT ( 'NONE',  ( 122.3830681442452857, -8.166667518702819706, -8.995218007635861213 ) ) ;
#8735=CARTESIAN_POINT ( 'NONE',  ( 115.1010702440515558, -2.467220198592777525, -17.83387418641524391 ) ) ;
#8737=CARTESIAN_POINT ( 'NONE',  ( 115.1220548109119761, -8.166667518702817929, -8.995218007635861213 ) ) ;
#8738=CARTESIAN_POINT ( 'NONE',  ( 117.6180281442453150, -0.4660016031367893996, -10.09054647747474043 ) ) ;
#8745=CARTESIAN_POINT ( 'NONE',  ( 120.2841814775786276, -10.15424416112533912, -14.75197769757731336 ) ) ;
#8750=CARTESIAN_POINT ( 'NONE',  ( 119.1496481442453046, -6.222761293078241884, -8.102969835052219238 ) ) ;
#8751=DIRECTION ( 'NONE',  ( 0.000000000000000000, 0.6004852223388321697, -0.7996358532186279566 ) ) ;
#8753=CARTESIAN_POINT ( 'NONE',  ( 111.8319081442453182, -4.153390946401321671, -8.397313243818183892 ) ) ;
#8754=CARTESIAN_POINT ( 'NONE',  ( 118.2420214775786320, -3.383040157471821630, -19.15922257007629170 ) ) ;
#8755=ORIENTED_EDGE ( 'NONE', *, *, #16476, .F. ) ;
#8756=CARTESIAN_POINT ( 'NONE',  ( 118.6958348109119754, -3.505236298600246325, -18.68346056562440793 ) ) ;
#8757=CARTESIAN_POINT ( 'NONE',  ( 115.1220548109119761, -8.166667518702817929, -8.995218007635861213 ) ) ;
#8758=CARTESIAN_POINT ( 'NONE',  ( 121.2485348109119769, -0.4660016031367893996, -10.09054647747474043 ) ) ;
#8759=CARTESIAN_POINT ( 'NONE',  ( 118.4122014775786340, -9.859900752359374465, -12.68260735090039404 ) ) ;
#8761=CARTESIAN_POINT ( 'NONE',  ( 124.9357681442453014, -7.643976991954077427, -18.09477374809248928 ) ) ;
#8762=CARTESIAN_POINT ( 'NONE',  ( 120.5110881442453206, -6.344957434206665248, -7.627207830600338134 ) ) ;
#8765=CARTESIAN_POINT ( 'NONE',  ( 120.9081748109119872, -5.638512984488999180, -18.83840828888717311 ) ) ;
#8768=CARTESIAN_POINT ( 'NONE',  ( 119.1871698793805194, -2.191907684172563986, -18.20049396185734025 ) ) ;
#8773=CARTESIAN_POINT ( 'NONE',  ( 137.0596819398122932, -9.972289680933823064, -11.58104143152225163 ) ) ;
#8774=CARTESIAN_POINT ( 'NONE',  ( 119.5467348109119712, -5.574606645277164318, -18.38911715685844683 ) ) ;
#8775=CARTESIAN_POINT ( 'NONE',  ( 125.7299414775786346, 0.9020085738987339008, -11.91225656197089222 ) ) ;
#8780=CARTESIAN_POINT ( 'NONE',  ( 115.0653281442453277, -3.505236298600246325, -18.68346056562440793 ) ) ;
#8781=CARTESIAN_POINT ( 'NONE',  ( 114.9073801386228979, -1.125321370491268125, -17.12283323191015327 ) ) ;
#8785=CARTESIAN_POINT ( 'NONE',  ( 124.5386814775786206, -5.638512984488999180, -18.83840828888717311 ) ) ;
#8786=CARTESIAN_POINT ( 'NONE',  ( 122.8368814775786291, -7.894159318335828068, -9.358103419637847864 ) ) ;
#8789=CARTESIAN_POINT ( 'NONE',  ( 125.8433948109119456, -1.834011780172310813, -8.268836392978581529 ) ) ;
#8791=CARTESIAN_POINT ( 'NONE',  ( 120.5678148109119832, -1.833838273342659253, -17.42832698103878286 ) ) ;
#8792=CARTESIAN_POINT ( 'NONE',  ( 119.6601881442453106, -1.833838273342659253, -17.42832698103878286 ) ) ;
#8793=CARTESIAN_POINT ( 'NONE',  ( 120.5887993777725029, -1.267766418764730840, -16.93314635290706605 ) ) ;
#8798=CYLINDRICAL_SURFACE ( 'NONE', #12473, 4.999999999999998224 ) ;
#8800=( BOUNDED_CURVE ( )  B_SPLINE_CURVE ( 2, ( #2164, #12454, #26356, #23389, #40263, #43913, #5815, #19734, #26580, #6042, #9255, #16555, #44598, #10607, #34955, #6958, #10385 ),
 .UNSPECIFIED., .F., .T. ) 
 B_SPLINE_CURVE_WITH_KNOTS ( ( 3, 2, 2, 2, 2, 2, 2, 2, 3 ),
 ( 0.3295046674808919662, 0.3359375000000000000, 0.3437500000000000000, 0.3515625000000000000, 0.3593750000000000000, 0.3671875000000000000, 0.3750000000000000000, 0.3828125000000000000, 0.3892453325190585178 ),
 .UNSPECIFIED. ) 
 CURVE ( )  GEOMETRIC_REPRESENTATION_ITEM ( )  RATIONAL_B_SPLINE_CURVE ( ( 0.9778625265006459788, 0.9373222120152210346, 1.000000000000000000, 0.9238795325112869605, 1.000000000000000000, 0.9238795325112869605, 1.000000000000000000, 0.9238795325112869605, 1.000000000000000000, 0.9238795325112869605, 1.000000000000000000, 0.9238795325112869605, 1.000000000000000000, 0.9238795325112869605, 1.000000000000000000, 0.9373222120157019832, 0.9778625265000240319 ) ) 
 REPRESENTATION_ITEM ( '' )  );
#8803=CARTESIAN_POINT ( 'NONE',  ( 122.9503348109119827, 0.5811942927096110934, -14.16772938898807510 ) ) ;
#8804=CARTESIAN_POINT ( 'NONE',  ( 118.0718414775786300, -9.261995988541697145, -16.69588392320189030 ) ) ;
#8806=CARTESIAN_POINT ( 'NONE',  ( 115.2922348109119781, -10.63000616557722466, -14.87417383870573495 ) ) ;
#8809=CARTESIAN_POINT ( 'NONE',  ( 128.2184548109119930, -4.863998795839242995, -13.39321520033831447 ) ) ;
#8811=CARTESIAN_POINT ( 'NONE',  ( 123.2339681442453241, -6.344957434206665248, -7.627207830600338134 ) ) ;
#8813=CARTESIAN_POINT ( 'NONE',  ( 121.1918081442452859, 0.9020085738987339008, -11.91225656197089222 ) ) ;
#8814=CARTESIAN_POINT ( 'NONE',  ( 126.2404814775786264, -0.8288870151387760510, -10.36305467784173118 ) ) ;
#8816=CARTESIAN_POINT ( 'NONE',  ( 114.3278814775786429, 0.1319031606808879209, -14.10382304977623669 ) ) ;
#8817=CARTESIAN_POINT ( 'NONE',  ( 126.1270281442452870, -10.30919188438810075, -12.61870101168855918 ) ) ;
#8819=CARTESIAN_POINT ( 'NONE',  ( 118.5256548109119876, -8.899110576539710493, -16.42337572283490132 ) ) ;
#8824=CARTESIAN_POINT ( 'NONE',  ( 124.0281414775786146, -1.834011780172310813, -8.268836392978581529 ) ) ;
#8829=CARTESIAN_POINT ( 'NONE',  ( 117.6180281442453150, -8.899110576539710493, -16.42337572283490132 ) ) ;
#8832=CARTESIAN_POINT ( 'NONE',  ( 124.1415948109119540, -3.505236298600246325, -18.68346056562440793 ) ) ;
#8834=CARTESIAN_POINT ( 'NONE',  ( 123.7637130757767352, -0.9924539043446216624, -17.29976612834909133 ) ) ;
#8838=CARTESIAN_POINT ( 'NONE',  ( 123.4041481442452834, -10.30919188438810075, -12.61870101168855918 ) ) ;
#8839=CARTESIAN_POINT ( 'NONE',  ( 117.6747548109119919, -7.643976991954077427, -18.09477374809248928 ) ) ;
#8840=CARTESIAN_POINT ( 'NONE',  ( 121.3619881442452879, -5.574606645277164318, -18.38911715685844683 ) ) ;
#8842=CARTESIAN_POINT ( 'NONE',  ( 124.5954081442453116, -3.383040157471821630, -19.15922257007629170 ) ) ;
#8843=CARTESIAN_POINT ( 'NONE',  ( 114.1577014775786552, -6.344957434206662583, -7.627207830600332805 ) ) ;
#8846=CARTESIAN_POINT ( 'NONE',  ( 123.6310548109119765, -4.153390946401325223, -8.397313243818185668 ) ) ;
#8847=CARTESIAN_POINT ( 'NONE',  ( 122.5532481442453019, -10.63000616557722466, -14.87417383870573495 ) ) ;
#8855=CARTESIAN_POINT ( 'NONE',  ( 123.6310548109119765, -4.153390946401325223, -8.397313243818185668 ) ) ;
#8861=ORIENTED_EDGE ( 'NONE', *, *, #23681, .F. ) ;
#8862=CARTESIAN_POINT ( 'NONE',  ( 119.8303681442453126, -10.63000616557722466, -14.87417383870573495 ) ) ;
#8863=CARTESIAN_POINT ( 'NONE',  ( 113.0231681442453322, 0.9020085738987376756, -11.91225656197089755 ) ) ;
#8865=CARTESIAN_POINT ( 'NONE',  ( 123.0637881442452937, -8.899110576539710493, -16.42337572283490132 ) ) ;
#8866=CARTESIAN_POINT ( 'NONE',  ( 115.7460481442453357, -10.15424416112533912, -14.75197769757731336 ) ) ;
#8871=CARTESIAN_POINT ( 'NONE',  ( 113.5337081442453240, -9.261995988541697145, -16.69588392320189030 ) ) ;
#8872=ADVANCED_FACE ( 'NONE', ( #11829 ), #17390, .T. ) ;
#8875=CARTESIAN_POINT ( 'NONE',  ( 122.4965214775786251, -10.30919188438810075, -12.61870101168855918 ) ) ;
#8878=CARTESIAN_POINT ( 'NONE',  ( 114.6115148109119986, -3.383040157471821630, -19.15922257007629170 ) ) ;
#8879=CARTESIAN_POINT ( 'NONE',  ( 112.9097148109120070, -9.565557343593413364, -10.61323700422348004 ) ) ;
#8882=CARTESIAN_POINT ( 'NONE',  ( 126.4673881442452910, -7.894159318335828068, -9.358103419637847864 ) ) ;
#8883=VERTEX_POINT ( 'NONE', #35530 ) ;
#8884=CARTESIAN_POINT ( 'NONE',  ( 122.5532481442453019, -10.63000616557722466, -14.87417383870573495 ) ) ;
#8891=CARTESIAN_POINT ( 'NONE',  ( 123.4944583641427727, -4.097270811097695642, -15.66323126201896798 ) ) ;
#8892=CARTESIAN_POINT ( 'NONE',  ( 115.2355081442453155, 0.1319031606808879209, -14.10382304977623669 ) ) ;
#8896=CARTESIAN_POINT ( 'NONE',  ( 112.2857214775786474, -5.574606645277164318, -18.38911715685844683 ) ) ;
#8897=CARTESIAN_POINT ( 'NONE',  ( 125.3328548109119964, -0.8288870151387760510, -10.36305467784173118 ) ) ;
#8899=CARTESIAN_POINT ( 'NONE',  ( 113.5337081442453240, -9.261995988541697145, -16.69588392320189030 ) ) ;
#8900=CARTESIAN_POINT ( 'NONE',  ( 115.9162281442453235, -5.574606645277164318, -18.38911715685844683 ) ) ;
#8901=CARTESIAN_POINT ( 'NONE',  ( 123.6310548109119765, -5.638512984488999180, -18.83840828888717311 ) ) ;
#8902=CARTESIAN_POINT ( 'NONE',  ( 121.0783548109119749, 0.2603800115204892296, -16.42320221600525088 ) ) ;
#8904=CARTESIAN_POINT ( 'NONE',  ( 126.6827570900509130, -8.513103522651428889, -17.14294544241743523 ) ) ;
#8909=CARTESIAN_POINT ( 'NONE',  ( 126.2275303246277502, -9.801060169199397265, -12.57365908077032124 ) ) ;
#8910=CARTESIAN_POINT ( 'NONE',  ( 116.3700414775786527, -5.638512984488999180, -18.83840828888717311 ) ) ;
#8915=CARTESIAN_POINT ( 'NONE',  ( 113.9875214775786532, -8.899110576539710493, -16.42337572283490132 ) ) ;
#8916=CARTESIAN_POINT ( 'NONE',  ( 121.3052614775786111, -1.834011780172310813, -8.268836392978581529 ) ) ;
#8921=CARTESIAN_POINT ( 'NONE',  ( 118.8660148109119774, 0.1319031606808879209, -14.10382304977623669 ) ) ;
#8922=CARTESIAN_POINT ( 'NONE',  ( 119.2631014775786298, 0.2603800115204892296, -16.42320221600525088 ) ) ;
#8923=CARTESIAN_POINT ( 'NONE',  ( 112.3424481442453384, -3.505236298600246325, -18.68346056562440793 ) ) ;
#8924=CARTESIAN_POINT ( 'NONE',  ( 114.6682414775786469, -1.561330072975668060, -17.79121239304076596 ) ) ;
#8926=CARTESIAN_POINT ( 'NONE',  ( 124.0848681442452772, -5.574606645277164318, -18.38911715685844683 ) ) ;
#8927=CARTESIAN_POINT ( 'NONE',  ( 121.0216281442452981, -7.894159318335828068, -9.358103419637847864 ) ) ;
#8932=CARTESIAN_POINT ( 'NONE',  ( 113.9307948109119906, 0.9020085738987339008, -11.91225656197089222 ) ) ;
#8933=CARTESIAN_POINT ( 'NONE',  ( 120.1707281442453166, -9.565557343593413364, -10.61323700422348004 ) ) ;
#8936=CARTESIAN_POINT ( 'NONE',  ( 119.1496481442453046, -3.383040157471821630, -19.15922257007629170 ) ) ;
#8939=CARTESIAN_POINT ( 'NONE',  ( 116.9940348109119839, -0.1624402480850797581, -16.17319339645315424 ) ) ;
#8944=CARTESIAN_POINT ( 'NONE',  ( 123.8012348109119642, -9.565557343593413364, -10.61323700422348004 ) ) ;
#8945=CARTESIAN_POINT ( 'NONE',  ( 120.1707281442453166, -9.565557343593413364, -10.61323700422348004 ) ) ;
#8950=CARTESIAN_POINT ( 'NONE',  ( 117.7882081442453170, -6.344957434206665248, -7.627207830600338134 ) ) ;
#8953=CARTESIAN_POINT ( 'NONE',  ( 117.4478481442453131, 0.2603800115204892296, -16.42320221600525088 ) ) ;
#8954=CARTESIAN_POINT ( 'NONE',  ( 114.2144281442453178, -8.166667518702817929, -8.995218007635859436 ) ) ;
#8955=CARTESIAN_POINT ( 'NONE',  ( 114.8384214775786489, -10.15424416112533912, -14.75197769757731336 ) ) ;
#8957=CARTESIAN_POINT ( 'NONE',  ( 121.8725281442453223, -6.222761293078241884, -8.102969835052219238 ) ) ;
#8959=CARTESIAN_POINT ( 'NONE',  ( 120.4543614775786295, -5.574606645277164318, -18.38911715685844683 ) ) ;
#8965=CARTESIAN_POINT ( 'NONE',  ( 119.1496481442453046, -3.383040157471821630, -19.15922257007629170 ) ) ;
#8967=CARTESIAN_POINT ( 'NONE',  ( 120.3409081442453044, -0.4660016031367893996, -10.09054647747474043 ) ) ;
#8970=CARTESIAN_POINT ( 'NONE',  ( 118.7525614775786380, -8.166667518702819706, -8.995218007635861213 ) ) ;
#8971=CARTESIAN_POINT ( 'NONE',  ( 118.0718414775786300, -9.261995988541697145, -16.69588392320189030 ) ) ;
#8976=CARTESIAN_POINT ( 'NONE',  ( 115.5950730757767531, -0.9924539043446216624, -17.29976612834909133 ) ) ;
#8978=CARTESIAN_POINT ( 'NONE',  ( 120.1707281442453166, -9.565557343593413364, -10.61323700422348004 ) ) ;
#8981=CARTESIAN_POINT ( 'NONE',  ( 119.4900081442453086, -7.643976991954077427, -18.09477374809248928 ) ) ;
#8984=CARTESIAN_POINT ( 'NONE',  ( 113.9875214775786532, -8.899110576539710493, -16.42337572283490132 ) ) ;
#8985=CARTESIAN_POINT ( 'NONE',  ( 122.4965214775786251, -10.30919188438810075, -12.61870101168855918 ) ) ;
#8987=CARTESIAN_POINT ( 'NONE',  ( 121.5888948109119809, 0.1319031606808879209, -14.10382304977623669 ) ) ;
#8988=CARTESIAN_POINT ( 'NONE',  ( 115.6893214775786447, 0.5811942927096154232, -14.16772938898807155 ) ) ;
#8989=CARTESIAN_POINT ( 'NONE',  ( 121.9859814775786333, 0.2603800115204892296, -16.42320221600525088 ) ) ;
#8990=CARTESIAN_POINT ( 'NONE',  ( 123.1205148109119563, -7.643976991954077427, -18.09477374809248928 ) ) ;
#8992=CARTESIAN_POINT ( 'NONE',  ( 123.8579614775786126, -9.859900752359378018, -12.68260735090039759 ) ) ;
#8993=( BOUNDED_SURFACE ( )  B_SPLINE_SURFACE ( 1, 2, ( 
 ( #19658, #33545, #9400, #43610, #13057, #26956, #2550, #40878, #40421, #16708, #40645, #16479, #6445, #20127, #34014, #30602, #9868, #5516, #20353, #2095, #44302, #2783, #16021, #44519, #23777, #15796, #27190, #29698, #12385, #37669, #26283, #40191, #12610, #22857, #19436, #29929, #9180, #43843, #26513, #36968, #2324, #16252, #30155, #26737, #23311, #14167, #28085, #41774, #10976, #10758, #13952, #13733, #38541, #17595, #7102, #27643, #21236, #39, #24655, #17377, #41993, #17815, #3895, #34674, #6884, #10098, #6665, #3460, #31709, #31489, #20575, #24002, #10534, #27864, #24434, #35114, #41557, #37889, #7316, #31046, #3011, #21012, #41339, #38325, #34886, #258, #479, #42216, #14392, #34452, #31265, #3674, #3233, #27419, #24218, #38109, #28304, #24880, #17159, #38772, #7542, #34237, #16933, #44752, #30829, #13511, #44976, #10316, #20794, #7776, #4794, #4570, #22133, #35798, #39911, #29195, #5017, #21459, #18935, #18264, #35342, #1375, #42887, #12103, #14617, #26007, #4114, #28534, #18036, #18494, #32822, #8227, #11648, #11877, #36250, #32384, #43107, #21904, #1592, #39231, #25338, #32160, #39688, #39463, #18715, #29420, #36026, #25557, #31932, #15288, #22356, #28757, #697, #11433, #15513, #42440, #11205, #15068, #928, #25781, #8453, #43334, #1151, #25109, #32606, #39006, #21683, #7996, #35571, #4344, #14847, #28981, #42662, #16426, #37382, #23030, #30101, #27133, #19160, #23261, #43559, #29645, #26227, #40136, #36693, #26460, #2497, #23496, #6152, #22575, #44017, #20072, #22799, #33958, #36917, #43788, #2725, #5688, #12328, #12779, #37144, #36477, #30322, #2269, #26681, #16197, #30546, #13232, #5463, #15970, #8901, #40592, #44248, #19383, #13006, #16651, #8672, #26905, #5244, #33041, #44467, #1816, #19840, #33271, #15743, #2046, #9351, #29873, #12553, #40362, #9126, #19607, #33491, #5918, #33727, #40825, #9580, #21572, #4006, #18385, #18152, #20740, #20520, #815, #24993, #14507, #34400, #28646, #6835, #32047, #24165, #4234, #25224, #11314, #41502, #13679, #16882 ),
 ( #14734, #42552, #44922, #39122, #7889, #13459, #30996, #27588, #21795, #35689, #10258, #17928, #14957, #6387, #11092, #30773, #44699, #27362, #41282, #23949, #38057, #35459, #4464, #32273, #9814, #31827, #1041, #10042, #41057, #34620, #597, #23723, #28420, #37830, #42331, #38888, #37613, #20295, #7657, #34180, #2955, #6607, #3181, #17105, #25450, #42782, #8120, #22021, #35915, #18602, #1268, #4681, #11543, #32493, #28869, #39352, #19828, #16642, #30535, #23713, #37604, #16413, #44688, #27354, #41273, #23939, #37132, #13449, #20513, #16873, #37820, #2944, #12997, #10033, #40582, #6597, #9341, #9569, #10250, #41492, #30311, #6376, #31206, #17317, #9804, #2716, #34392, #38049, #26893, #20286, #40813, #6827, #3174, #24158, #34612, #33716, #44237, #34170, #2487, #23484, #20732, #37371, #6142, #30763, #17096, #20063, #30989, #44914, #13671, #27579, #3399, #33946, #45128, #26669, #23250, #5908, #13223, #44457, #27122, #41047, #18197, #25271, #31645, #414, #21392, #10474, #25041, #38935, #4049, #7704, #7254, #28695, #7473, #28470, #18433, #32092, #21618, #42599, #21842, #3609, #32324, #14106, #31873, #35507, #189, #4279, #7932, #13886, #863, #41709, #27796, #11362, #24375, #14780, #24596, #20954, #38261, #638, #21169, #7042, #28022, #35737, #35045, #34826, #17525, #31423, #38706, #39168, #4510, #35274, #41929, #10693, #17972, #38480, #3826, #42376, #14551, #17749, #14331, #24814, #28245, #42154, #10914, #11138, #15910, #1532, #18868, #22071, #18651, #15454, #29808, #43500, #32543, #35963, #22512, #39849, #36406, #1983, #25719, #4733, #22733, #43044, #36633, #1313, #40067, #40299, #5624, #5407, #28916, #1089, #43723, #19546, #12268, #11812, #8165, #15003, #19094, #8389, #11587, #15225, #9063, #39626, #42826, #25496, #29132, #25942, #26164, #8832, #8614, #22964, #19323, #5176, #22294, #33208, #29583, #32979, #36188, #12491, #12039, #26389, #29359, #36855, #39400, #4954, #43273, #32759, #1755, #15679, #22727, #25713, #4272, #1307, #18191, #8381, #8606, #39843, #8159 ) ),
 .UNSPECIFIED., .F., .F., .T. ) 
 B_SPLINE_SURFACE_WITH_KNOTS ( ( 2, 2 ),
 ( 3, 2, 2, 2, 2, 2, 2, 2, 2, 2, 2, 2, 2, 2, 2, 2, 2, 2, 2, 2, 2, 2, 2, 2, 2, 2, 2, 2, 2, 2, 2, 2, 2, 2, 2, 2, 2, 2, 2, 2, 2, 2, 2, 2, 2, 2, 2, 2, 2, 2, 2, 2, 2, 2, 2, 2, 2, 2, 2, 2, 2, 2, 2, 2, 2, 2, 2, 2, 2, 2, 2, 2, 2, 2, 2, 2, 2, 2, 2, 2, 2, 2, 2, 2, 2, 2, 2, 2, 2, 2, 2, 2, 2, 2, 2, 2, 2, 2, 2, 2, 2, 2, 2, 2, 2, 2, 2, 2, 2, 2, 2, 2, 2, 2, 2, 2, 2, 2, 2, 2, 2, 2, 2, 2, 2, 2, 2, 2, 3 ),
 ( 0.000000000000000000, 1.000000000000000000 ),
 ( 0.000000000000000000, 0.007812500000000000000, 0.01562500000000000000, 0.02343750000000000000, 0.03125000000000000000, 0.03906250000000000000, 0.04687500000000000000, 0.05468750000000000000, 0.06250000000000000000, 0.07031250000000000000, 0.07812500000000000000, 0.08593750000000000000, 0.09375000000000000000, 0.1015625000000000000, 0.1093750000000000000, 0.1171875000000000000, 0.1250000000000000000, 0.1328125000000000000, 0.1406250000000000000, 0.1484375000000000000, 0.1562500000000000000, 0.1640625000000000000, 0.1718750000000000000, 0.1796875000000000000, 0.1875000000000000000, 0.1953125000000000000, 0.2031250000000000000, 0.2109375000000000000, 0.2187500000000000000, 0.2265625000000000000, 0.2343750000000000000, 0.2421875000000000000, 0.2500000000000000000, 0.2578125000000000000, 0.2656250000000000000, 0.2734375000000000000, 0.2812500000000000000, 0.2890625000000000000, 0.2968750000000000000, 0.3046875000000000000, 0.3125000000000000000, 0.3203125000000000000, 0.3281250000000000000, 0.3359375000000000000, 0.3437500000000000000, 0.3515625000000000000, 0.3593750000000000000, 0.3671875000000000000, 0.3750000000000000000, 0.3828125000000000000, 0.3906250000000000000, 0.3984375000000000000, 0.4062500000000000000, 0.4140625000000000000, 0.4218750000000000000, 0.4296875000000000000, 0.4375000000000000000, 0.4453125000000000000, 0.4531250000000000000, 0.4609375000000000000, 0.4687500000000000000, 0.4765625000000000000, 0.4843750000000000000, 0.4921875000000000000, 0.5000000000000000000, 0.5078125000000000000, 0.5156250000000000000, 0.5234375000000000000, 0.5312500000000000000, 0.5390625000000000000, 0.5468750000000000000, 0.5546875000000000000, 0.5625000000000000000, 0.5703125000000000000, 0.5781250000000000000, 0.5859375000000000000, 0.5937500000000000000, 0.6015625000000000000, 0.6093750000000000000, 0.6171875000000000000, 0.6250000000000000000, 0.6328125000000000000, 0.6406250000000000000, 0.6484375000000000000, 0.6562500000000000000, 0.6640625000000000000, 0.6718750000000000000, 0.6796875000000000000, 0.6875000000000000000, 0.6953125000000000000, 0.7031250000000000000, 0.7109375000000000000, 0.7187500000000000000, 0.7265625000000000000, 0.7343750000000000000, 0.7421875000000000000, 0.7500000000000000000, 0.7578125000000000000, 0.7656250000000000000, 0.7734375000000000000, 0.7812500000000000000, 0.7890625000000000000, 0.7968750000000000000, 0.8046875000000000000, 0.8125000000000000000, 0.8203125000000000000, 0.8281250000000000000, 0.8359375000000000000, 0.8437500000000000000, 0.8515625000000000000, 0.8593750000000000000, 0.8671875000000000000, 0.8750000000000000000, 0.8828125000000000000, 0.8906250000000000000, 0.8984375000000000000, 0.9062500000000000000, 0.9140625000000000000, 0.9218750000000000000, 0.9296875000000000000, 0.9375000000000000000, 0.9453125000000000000, 0.9531250000000000000, 0.9609375000000000000, 0.9687500000000000000, 0.9765625000000000000, 0.9843750000000000000, 0.9921875000000000000, 1.000000000000000000 ),
 .UNSPECIFIED. ) 
 GEOMETRIC_REPRESENTATION_ITEM ( )  RATIONAL_B_SPLINE_SURFACE ( (
 ( 1.000000000000000000, 0.9238795325112869605, 1.000000000000000000, 0.9238795325112869605, 1.000000000000000000, 0.9238795325112869605, 1.000000000000000000, 0.9238795325112869605, 1.000000000000000000, 0.9238795325112869605, 1.000000000000000000, 0.9238795325112869605, 1.000000000000000000, 0.9238795325112869605, 1.000000000000000000, 0.9238795325112869605, 1.000000000000000000, 0.9238795325112869605, 1.000000000000000000, 0.9238795325112869605, 1.000000000000000000, 0.9238795325112869605, 1.000000000000000000, 0.9238795325112869605, 1.000000000000000000, 0.9238795325112869605, 1.000000000000000000, 0.9238795325112869605, 1.000000000000000000, 0.9238795325112869605, 1.000000000000000000, 0.9238795325112869605, 1.000000000000000000, 0.9238795325112869605, 1.000000000000000000, 0.9238795325112869605, 1.000000000000000000, 0.9238795325112869605, 1.000000000000000000, 0.9238795325112869605, 1.000000000000000000, 0.9238795325112869605, 1.000000000000000000, 0.9238795325112869605, 1.000000000000000000, 0.9238795325112869605, 1.000000000000000000, 0.9238795325112869605, 1.000000000000000000, 0.9238795325112869605, 1.000000000000000000, 0.9238795325112869605, 1.000000000000000000, 0.9238795325112869605, 1.000000000000000000, 0.9238795325112869605, 1.000000000000000000, 0.9238795325112869605, 1.000000000000000000, 0.9238795325112869605, 1.000000000000000000, 0.9238795325112869605, 1.000000000000000000, 0.9238795325112869605, 1.000000000000000000, 0.9238795325112869605, 1.000000000000000000, 0.9238795325112869605, 1.000000000000000000, 0.9238795325112869605, 1.000000000000000000, 0.9238795325112869605, 1.000000000000000000, 0.9238795325112869605, 1.000000000000000000, 0.9238795325112869605, 1.000000000000000000, 0.9238795325112869605, 1.000000000000000000, 0.9238795325112869605, 1.000000000000000000, 0.9238795325112869605, 1.000000000000000000, 0.9238795325112869605, 1.000000000000000000, 0.9238795325112869605, 1.000000000000000000, 0.9238795325112869605, 1.000000000000000000, 0.9238795325112869605, 1.000000000000000000, 0.9238795325112869605, 1.000000000000000000, 0.9238795325112869605, 1.000000000000000000, 0.9238795325112869605, 1.000000000000000000, 0.9238795325112869605, 1.000000000000000000, 0.9238795325112869605, 1.000000000000000000, 0.9238795325112869605, 1.000000000000000000, 0.9238795325112869605, 1.000000000000000000, 0.9238795325112869605, 1.000000000000000000, 0.9238795325112869605, 1.000000000000000000, 0.9238795325112869605, 1.000000000000000000, 0.9238795325112869605, 1.000000000000000000, 0.9238795325112869605, 1.000000000000000000, 0.9238795325112869605, 1.000000000000000000, 0.9238795325112869605, 1.000000000000000000, 0.9238795325112869605, 1.000000000000000000, 0.9238795325112869605, 1.000000000000000000, 0.9238795325112869605, 1.000000000000000000, 0.9238795325112869605, 1.000000000000000000, 0.9238795325112869605, 1.000000000000000000, 0.9238795325112869605, 1.000000000000000000, 0.9238795325112869605, 1.000000000000000000, 0.9238795325112869605, 1.000000000000000000, 0.9238795325112869605, 1.000000000000000000, 0.9238795325112869605, 1.000000000000000000, 0.9238795325112869605, 1.000000000000000000, 0.9238795325112869605, 1.000000000000000000, 0.9238795325112869605, 1.000000000000000000, 0.9238795325112869605, 1.000000000000000000, 0.9238795325112869605, 1.000000000000000000, 0.9238795325112869605, 1.000000000000000000, 0.9238795325112869605, 1.000000000000000000, 0.9238795325112869605, 1.000000000000000000, 0.9238795325112869605, 1.000000000000000000, 0.9238795325112869605, 1.000000000000000000, 0.9238795325112869605, 1.000000000000000000, 0.9238795325112869605, 1.000000000000000000, 0.9238795325112869605, 1.000000000000000000, 0.9238795325112869605, 1.000000000000000000, 0.9238795325112869605, 1.000000000000000000, 0.9238795325112869605, 1.000000000000000000, 0.9238795325112869605, 1.000000000000000000, 0.9238795325112869605, 1.000000000000000000, 0.9238795325112869605, 1.000000000000000000, 0.9238795325112869605, 1.000000000000000000, 0.9238795325112869605, 1.000000000000000000, 0.9238795325112869605, 1.000000000000000000, 0.9238795325112869605, 1.000000000000000000, 0.9238795325112869605, 1.000000000000000000, 0.9238795325112869605, 1.000000000000000000, 0.9238795325112869605, 1.000000000000000000, 0.9238795325112869605, 1.000000000000000000, 0.9238795325112869605, 1.000000000000000000, 0.9238795325112869605, 1.000000000000000000, 0.9238795325112869605, 1.000000000000000000, 0.9238795325112869605, 1.000000000000000000, 0.9238795325112869605, 1.000000000000000000, 0.9238795325112869605, 1.000000000000000000, 0.9238795325112869605, 1.000000000000000000, 0.9238795325112869605, 1.000000000000000000, 0.9238795325112869605, 1.000000000000000000, 0.9238795325112869605, 1.000000000000000000, 0.9238795325112869605, 1.000000000000000000, 0.9238795325112869605, 1.000000000000000000, 0.9238795325112869605, 1.000000000000000000, 0.9238795325112869605, 1.000000000000000000, 0.9238795325112869605, 1.000000000000000000, 0.9238795325112869605, 1.000000000000000000, 0.9238795325112869605, 1.000000000000000000, 0.9238795325112869605, 1.000000000000000000, 0.9238795325112869605, 1.000000000000000000, 0.9238795325112869605, 1.000000000000000000, 0.9238795325112869605, 1.000000000000000000, 0.9238795325112869605, 1.000000000000000000, 0.9238795325112869605, 1.000000000000000000, 0.9238795325112869605, 1.000000000000000000, 0.9238795325112869605, 1.000000000000000000, 0.9238795325112869605, 1.000000000000000000, 0.9238795325112869605, 1.000000000000000000, 0.9238795325112869605, 1.000000000000000000, 0.9238795325112869605, 1.000000000000000000, 0.9238795325112869605, 1.000000000000000000, 0.9238795325112869605, 1.000000000000000000, 0.9238795325112869605, 1.000000000000000000),
 ( 1.000000000000000000, 0.9238795325112869605, 1.000000000000000000, 0.9238795325112869605, 1.000000000000000000, 0.9238795325112869605, 1.000000000000000000, 0.9238795325112869605, 1.000000000000000000, 0.9238795325112869605, 1.000000000000000000, 0.9238795325112869605, 1.000000000000000000, 0.9238795325112869605, 1.000000000000000000, 0.9238795325112869605, 1.000000000000000000, 0.9238795325112869605, 1.000000000000000000, 0.9238795325112869605, 1.000000000000000000, 0.9238795325112869605, 1.000000000000000000, 0.9238795325112869605, 1.000000000000000000, 0.9238795325112869605, 1.000000000000000000, 0.9238795325112869605, 1.000000000000000000, 0.9238795325112869605, 1.000000000000000000, 0.9238795325112869605, 1.000000000000000000, 0.9238795325112869605, 1.000000000000000000, 0.9238795325112869605, 1.000000000000000000, 0.9238795325112869605, 1.000000000000000000, 0.9238795325112869605, 1.000000000000000000, 0.9238795325112869605, 1.000000000000000000, 0.9238795325112869605, 1.000000000000000000, 0.9238795325112869605, 1.000000000000000000, 0.9238795325112869605, 1.000000000000000000, 0.9238795325112869605, 1.000000000000000000, 0.9238795325112869605, 1.000000000000000000, 0.9238795325112869605, 1.000000000000000000, 0.9238795325112869605, 1.000000000000000000, 0.9238795325112869605, 1.000000000000000000, 0.9238795325112869605, 1.000000000000000000, 0.9238795325112869605, 1.000000000000000000, 0.9238795325112869605, 1.000000000000000000, 0.9238795325112869605, 1.000000000000000000, 0.9238795325112869605, 1.000000000000000000, 0.9238795325112869605, 1.000000000000000000, 0.9238795325112869605, 1.000000000000000000, 0.9238795325112869605, 1.000000000000000000, 0.9238795325112869605, 1.000000000000000000, 0.9238795325112869605, 1.000000000000000000, 0.9238795325112869605, 1.000000000000000000, 0.9238795325112869605, 1.000000000000000000, 0.9238795325112869605, 1.000000000000000000, 0.9238795325112869605, 1.000000000000000000, 0.9238795325112869605, 1.000000000000000000, 0.9238795325112869605, 1.000000000000000000, 0.9238795325112869605, 1.000000000000000000, 0.9238795325112869605, 1.000000000000000000, 0.9238795325112869605, 1.000000000000000000, 0.9238795325112869605, 1.000000000000000000, 0.9238795325112869605, 1.000000000000000000, 0.9238795325112869605, 1.000000000000000000, 0.9238795325112869605, 1.000000000000000000, 0.9238795325112869605, 1.000000000000000000, 0.9238795325112869605, 1.000000000000000000, 0.9238795325112869605, 1.000000000000000000, 0.9238795325112869605, 1.000000000000000000, 0.9238795325112869605, 1.000000000000000000, 0.9238795325112869605, 1.000000000000000000, 0.9238795325112869605, 1.000000000000000000, 0.9238795325112869605, 1.000000000000000000, 0.9238795325112869605, 1.000000000000000000, 0.9238795325112869605, 1.000000000000000000, 0.9238795325112869605, 1.000000000000000000, 0.9238795325112869605, 1.000000000000000000, 0.9238795325112869605, 1.000000000000000000, 0.9238795325112869605, 1.000000000000000000, 0.9238795325112869605, 1.000000000000000000, 0.9238795325112869605, 1.000000000000000000, 0.9238795325112869605, 1.000000000000000000, 0.9238795325112869605, 1.000000000000000000, 0.9238795325112869605, 1.000000000000000000, 0.9238795325112869605, 1.000000000000000000, 0.9238795325112869605, 1.000000000000000000, 0.9238795325112869605, 1.000000000000000000, 0.9238795325112869605, 1.000000000000000000, 0.9238795325112869605, 1.000000000000000000, 0.9238795325112869605, 1.000000000000000000, 0.9238795325112869605, 1.000000000000000000, 0.9238795325112869605, 1.000000000000000000, 0.9238795325112869605, 1.000000000000000000, 0.9238795325112869605, 1.000000000000000000, 0.9238795325112869605, 1.000000000000000000, 0.9238795325112869605, 1.000000000000000000, 0.9238795325112869605, 1.000000000000000000, 0.9238795325112869605, 1.000000000000000000, 0.9238795325112869605, 1.000000000000000000, 0.9238795325112869605, 1.000000000000000000, 0.9238795325112869605, 1.000000000000000000, 0.9238795325112869605, 1.000000000000000000, 0.9238795325112869605, 1.000000000000000000, 0.9238795325112869605, 1.000000000000000000, 0.9238795325112869605, 1.000000000000000000, 0.9238795325112869605, 1.000000000000000000, 0.9238795325112869605, 1.000000000000000000, 0.9238795325112869605, 1.000000000000000000, 0.9238795325112869605, 1.000000000000000000, 0.9238795325112869605, 1.000000000000000000, 0.9238795325112869605, 1.000000000000000000, 0.9238795325112869605, 1.000000000000000000, 0.9238795325112869605, 1.000000000000000000, 0.9238795325112869605, 1.000000000000000000, 0.9238795325112869605, 1.000000000000000000, 0.9238795325112869605, 1.000000000000000000, 0.9238795325112869605, 1.000000000000000000, 0.9238795325112869605, 1.000000000000000000, 0.9238795325112869605, 1.000000000000000000, 0.9238795325112869605, 1.000000000000000000, 0.9238795325112869605, 1.000000000000000000, 0.9238795325112869605, 1.000000000000000000, 0.9238795325112869605, 1.000000000000000000, 0.9238795325112869605, 1.000000000000000000, 0.9238795325112869605, 1.000000000000000000, 0.9238795325112869605, 1.000000000000000000, 0.9238795325112869605, 1.000000000000000000, 0.9238795325112869605, 1.000000000000000000, 0.9238795325112869605, 1.000000000000000000, 0.9238795325112869605, 1.000000000000000000, 0.9238795325112869605, 1.000000000000000000, 0.9238795325112869605, 1.000000000000000000, 0.9238795325112869605, 1.000000000000000000, 0.9238795325112869605, 1.000000000000000000, 0.9238795325112869605, 1.000000000000000000, 0.9238795325112869605, 1.000000000000000000, 0.9238795325112869605, 1.000000000000000000, 0.9238795325112869605, 1.000000000000000000, 0.9238795325112869605, 1.000000000000000000, 0.9238795325112869605, 1.000000000000000000, 0.9238795325112869605, 1.000000000000000000) ) ) 
 REPRESENTATION_ITEM ( '' )  SURFACE ( )  );
#8994=EDGE_CURVE ( 'NONE', #22341, #18093, #18842, .T. ) ;
#8997=CARTESIAN_POINT ( 'NONE',  ( 124.0848681442452772, -4.089484607189486809, -7.948022111789456723 ) ) ;
#8999=CARTESIAN_POINT ( 'NONE',  ( 125.9568481442452850, -6.344957434206665248, -7.627207830600338134 ) ) ;
#9001=DIRECTION ( 'NONE',  ( 0.000000000000000000, 0.6004852223388322807, -0.7996358532186280677 ) ) ;
#9002=CARTESIAN_POINT ( 'NONE',  ( 135.3184548109119874, -0.6896191363000483410, -17.70303589939592825 ) ) ;
#9008=CARTESIAN_POINT ( 'NONE',  ( 118.9794681442453026, -0.8288870151387760510, -10.36305467784173118 ) ) ;
#9009=CARTESIAN_POINT ( 'NONE',  ( 125.2761281442453054, -10.63000616557722466, -14.87417383870573495 ) ) ;
#9010=CARTESIAN_POINT ( 'NONE',  ( 126.2252495083089343, -5.683655150050220151, -18.32939578658380952 ) ) ;
#9014=CARTESIAN_POINT ( 'NONE',  ( 117.9016614775786280, -0.1624402480850797581, -16.17319339645315424 ) ) ;
#9019=CARTESIAN_POINT ( 'NONE',  ( 121.0783548109119749, 0.2603800115204892296, -16.42320221600525088 ) ) ;
#9020=CARTESIAN_POINT ( 'NONE',  ( 121.8725281442453223, -6.222761293078241884, -8.102969835052219238 ) ) ;
#9023=CARTESIAN_POINT ( 'NONE',  ( 126.2872529661361654, 0.06646519102223864828, -14.41099760634975269 ) ) ;
#9025=CARTESIAN_POINT ( 'NONE',  ( 121.9292548109119849, -7.894159318335828068, -9.358103419637847864 ) ) ;
#9026=CARTESIAN_POINT ( 'NONE',  ( 120.0572748109119772, -6.222761293078241884, -8.102969835052219238 ) ) ;
#9030=CARTESIAN_POINT ( 'NONE',  ( 126.2184548109119788, -4.863998795839242995, -13.39321520033831447 ) ) ;
#9034=CARTESIAN_POINT ( 'NONE',  ( 151.2860562277021472, -4.863998795839242995, -13.39321520033831447 ) ) ;
#9036=CARTESIAN_POINT ( 'NONE',  ( 119.8870948109119752, -9.261995988541697145, -16.69588392320189030 ) ) ;
#9037=CARTESIAN_POINT ( 'NONE',  ( 120.6245414775786458, -9.988377603198976828, -10.36322818467138340 ) ) ;
#9039=CARTESIAN_POINT ( 'NONE',  ( 115.3489614775786407, -9.261995988541697145, -16.69588392320189030 ) ) ;
#9043=CARTESIAN_POINT ( 'NONE',  ( 122.2128881442453263, -1.834011780172310813, -8.268836392978581529 ) ) ;
#9044=CARTESIAN_POINT ( 'NONE',  ( 121.6456214775786293, -10.63000616557722466, -14.87417383870573495 ) ) ;
#9045=CARTESIAN_POINT ( 'NONE',  ( 126.4106614775786284, -6.222761293078241884, -8.102969835052219238 ) ) ;
#9046=CARTESIAN_POINT ( 'NONE',  ( 111.8886348109120092, -6.222761293078241884, -8.102969835052219238 ) ) ;
#9047=CARTESIAN_POINT ( 'NONE',  ( 114.9518748109119883, -7.643976991954077427, -18.09477374809248928 ) ) ;
#9048=CARTESIAN_POINT ( 'NONE',  ( 124.0281414775786146, -1.834011780172310813, -8.268836392978581529 ) ) ;
#9050=CARTESIAN_POINT ( 'NONE',  ( 120.9081748109119872, -4.153390946401325223, -8.397313243818185668 ) ) ;
#9054=APPLICATION_CONTEXT ( 'automotive_design' ) ;
#9057=CARTESIAN_POINT ( 'NONE',  ( 124.1983214775786166, -8.166667518702819706, -8.995218007635861213 ) ) ;
#9063=CARTESIAN_POINT ( 'NONE',  ( 123.7445081442452874, -7.894159318335828068, -9.358103419637847864 ) ) ;
#9064=CARTESIAN_POINT ( 'NONE',  ( 123.4564593026122878, -1.179503403430468333, -17.05068175419387089 ) ) ;
#9065=CARTESIAN_POINT ( 'NONE',  ( 125.3328548109119964, -0.8288870151387760510, -10.36305467784173118 ) ) ;
#9067=CARTESIAN_POINT ( 'NONE',  ( 125.1626748109119802, -9.988377603198980381, -10.36322818467138518 ) ) ;
#9068=( BOUNDED_CURVE ( )  B_SPLINE_CURVE ( 2, ( #4476, #39133, #31614, #31839, #14295, #28213, #21358, #608, #28431, #18163, #1053, #827, #7900, #14969, #28881, #11554, #15872 ),
 .UNSPECIFIED., .F., .T. ) 
 B_SPLINE_CURVE_WITH_KNOTS ( ( 3, 2, 2, 2, 2, 2, 2, 2, 3 ),
 ( 0.2046282416568590001, 0.2109375000000000000, 0.2187500000000000000, 0.2265625000000000000, 0.2343750000000000000, 0.2421875000000000000, 0.2500000000000000000, 0.2578125000000000000, 0.2641217583431409999 ),
 .UNSPECIFIED. ) 
 CURVE ( )  GEOMETRIC_REPRESENTATION_ITEM ( )  RATIONAL_B_SPLINE_CURVE ( ( 0.9763430640195970289, 0.9385262470928680267, 1.000000000000000000, 0.9238795325112869605, 1.000000000000000000, 0.9238795325112869605, 1.000000000000000000, 0.9238795325112869605, 1.000000000000000000, 0.9238795325112869605, 1.000000000000000000, 0.9238795325112869605, 1.000000000000000000, 0.9238795325112869605, 1.000000000000000000, 0.9385262470928680267, 0.9763430640195970289 ) ) 
 REPRESENTATION_ITEM ( '' )  );
#9069=CARTESIAN_POINT ( 'NONE',  ( 119.4332814775786318, -8.899110576539710493, -16.42337572283490132 ) ) ;
#9070=CARTESIAN_POINT ( 'NONE',  ( 124.9924948109119924, -5.574606645277164318, -18.38911715685844683 ) ) ;
#9072=CARTESIAN_POINT ( 'NONE',  ( 123.9714148109119805, -0.4660016031367893996, -10.09054647747474043 ) ) ;
#9073=CARTESIAN_POINT ( 'NONE',  ( 116.7671281442453335, -1.834011780172310813, -8.268836392978581529 ) ) ;
#9075=CARTESIAN_POINT ( 'NONE',  ( 113.0798948109119948, -8.899110576539710493, -16.42337572283490132 ) ) ;
#9076=CARTESIAN_POINT ( 'NONE',  ( 125.7866681442452688, -8.899110576539710493, -16.42337572283490132 ) ) ;
#9077=CARTESIAN_POINT ( 'NONE',  ( 124.8790414775786246, -0.4660016031367893996, -10.09054647747474043 ) ) ;
#9083=CARTESIAN_POINT ( 'NONE',  ( 117.4478481442453131, -9.565557343593413364, -10.61323700422348004 ) ) ;
#9087=CARTESIAN_POINT ( 'NONE',  ( 123.5743281442453139, -2.084020599724406786, -8.691656652584148546 ) ) ;
#9095=CARTESIAN_POINT ( 'NONE',  ( 118.5256548109119876, -0.4660016031367893996, -10.09054647747474043 ) ) ;
#9096=CARTESIAN_POINT ( 'NONE',  ( 124.9924948109119924, -5.574606645277164318, -18.38911715685844683 ) ) ;
#9097=CARTESIAN_POINT ( 'NONE',  ( 113.7038881442453402, -6.222761293078241884, -8.102969835052219238 ) ) ;
#9099=CARTESIAN_POINT ( 'NONE',  ( 114.9562903192117034, -2.378957183258582742, -17.95140958770220152 ) ) ;
#9100=CARTESIAN_POINT ( 'NONE',  ( 114.1577014775786552, -6.344957434206662583, -7.627207830600332805 ) ) ;
#9102=CARTESIAN_POINT ( 'NONE',  ( 123.8579614775786126, 0.5811942927096110934, -14.16772938898807510 ) ) ;
#9105=CARTESIAN_POINT ( 'NONE',  ( 113.7606148109119886, -1.561330072975668060, -17.79121239304076596 ) ) ;
#9106=CARTESIAN_POINT ( 'NONE',  ( 115.1787814775786387, -0.1624402480850797581, -16.17319339645315424 ) ) ;
#9108=CARTESIAN_POINT ( 'NONE',  ( 112.5126281442453120, -10.30919188438810075, -12.61870101168855918 ) ) ;
#9109=( GEOMETRIC_REPRESENTATION_CONTEXT ( 3 ) GLOBAL_UNCERTAINTY_ASSIGNED_CONTEXT ( ( #35143 ) ) GLOBAL_UNIT_ASSIGNED_CONTEXT ( ( #10523, #20784, #27408 ) ) REPRESENTATION_CONTEXT ( 'NONE', 'WORKASPACE' ) );
#9111=CARTESIAN_POINT ( 'NONE',  ( 121.1918081442452859, 0.9020085738987339008, -11.91225656197089222 ) ) ;
#9115=CARTESIAN_POINT ( 'NONE',  ( 123.7184548109119788, -4.683672500039349984, -14.88233656108870662 ) ) ;
#9117=CARTESIAN_POINT ( 'NONE',  ( 115.9729548109119861, -3.505236298600246325, -18.68346056562440793 ) ) ;
#9121=CARTESIAN_POINT ( 'NONE',  ( 113.4769814775786330, 0.4262465694468514643, -12.03445270309931736 ) ) ;
#9122=CARTESIAN_POINT ( 'NONE',  ( 126.1837548109119496, 0.4262465694468514643, -12.03445270309931736 ) ) ;
#9124=CARTESIAN_POINT ( 'NONE',  ( 112.8529881442453302, -1.561330072975668060, -17.79121239304076596 ) ) ;
#9125=CARTESIAN_POINT ( 'NONE',  ( 116.0296814775786345, -1.833838273342658809, -17.42832698103878286 ) ) ;
#9126=CARTESIAN_POINT ( 'NONE',  ( 124.7655881442452852, 0.5811942927096110934, -14.16772938898807510 ) ) ;
#9127=CARTESIAN_POINT ( 'NONE',  ( 122.2696148109119889, -4.089484607189486809, -7.948022111789456723 ) ) ;
#9129=CARTESIAN_POINT ( 'NONE',  ( 113.9307948109119906, 0.9020085738987339008, -11.91225656197089222 ) ) ;
#9134=CARTESIAN_POINT ( 'NONE',  ( 128.1691939224698729, -3.811125363834908963, -16.04426352910759235 ) ) ;
#9135=CARTESIAN_POINT ( 'NONE',  ( 117.9016614775786280, -9.988377603198976828, -10.36322818467138340 ) ) ;
#9140=CARTESIAN_POINT ( 'NONE',  ( 115.5191414775786569, -6.222761293078241884, -8.102969835052219238 ) ) ;
#9142=CARTESIAN_POINT ( 'NONE',  ( 120.3409081442453044, -0.4660016031367893996, -10.09054647747474043 ) ) ;
#9146=CARTESIAN_POINT ( 'NONE',  ( 120.8514481442453103, -2.084020599724394796, -8.691656652584146769 ) ) ;
#9147=CARTESIAN_POINT ( 'NONE',  ( 122.6099748109119929, -0.8288870151387760510, -10.36305467784173118 ) ) ;
#9148=CARTESIAN_POINT ( 'NONE',  ( 120.8514481442452961, -7.893985811506177619, -18.51759400769804742 ) ) ;
#9149=CARTESIAN_POINT ( 'NONE',  ( 113.9875214775786532, -8.899110576539710493, -16.42337572283490132 ) ) ;
#9150=CARTESIAN_POINT ( 'NONE',  ( 115.2355081442453155, -10.30919188438810075, -12.61870101168855918 ) ) ;
#9153=CARTESIAN_POINT ( 'NONE',  ( 124.8223148109119762, -10.15424416112533912, -14.75197769757731336 ) ) ;
#9154=CARTESIAN_POINT ( 'NONE',  ( 118.2987481442453088, -7.894159318335828068, -9.358103419637847864 ) ) ;
#9160=CARTESIAN_POINT ( 'NONE',  ( 113.5904348109119866, -7.893985811506177619, -18.51759400769804742 ) ) ;
#9161=CARTESIAN_POINT ( 'NONE',  ( 122.1561614775786353, -8.899110576539710493, -16.42337572283490132 ) ) ;
#9164=CARTESIAN_POINT ( 'NONE',  ( 117.8449348109119938, -8.166667518702817929, -8.995218007635861213 ) ) ;
#9166=CARTESIAN_POINT ( 'NONE',  ( 115.1220548109119761, -1.833838273342658809, -17.42832698103878286 ) ) ;
#9169=CARTESIAN_POINT ( 'NONE',  ( 124.4252281442452812, -0.8288870151387760510, -10.36305467784173118 ) ) ;
#9171=CARTESIAN_POINT ( 'NONE',  ( 120.6245414775786458, -0.1624402480850797581, -16.17319339645315424 ) ) ;
#9173=CARTESIAN_POINT ( 'NONE',  ( 117.4478481442453131, 0.2603800115204892296, -16.42320221600525088 ) ) ;
#9176=CARTESIAN_POINT ( 'NONE',  ( 115.0653281442453277, -6.344957434206662583, -7.627207830600332805 ) ) ;
#9177=CARTESIAN_POINT ( 'NONE',  ( 114.1009748109119784, -4.089484607189486809, -7.948022111789456723 ) ) ;
#9178=CARTESIAN_POINT ( 'NONE',  ( 116.2565881442453133, -0.8288870151387760510, -10.36305467784173118 ) ) ;
#9179=CARTESIAN_POINT ( 'NONE',  ( 124.4252281442452812, -0.8288870151387760510, -10.36305467784173118 ) ) ;
#9180=CARTESIAN_POINT ( 'NONE',  ( 113.7606148109119886, -1.561330072975668060, -17.79121239304076596 ) ) ;
#9183=CARTESIAN_POINT ( 'NONE',  ( 124.0281414775786146, -7.643976991954077427, -18.09477374809248928 ) ) ;
#9184=CARTESIAN_POINT ( 'NONE',  ( 122.9503348109119827, 0.5811942927096136469, -14.16772938898805378 ) ) ;
#9191=CARTESIAN_POINT ( 'NONE',  ( 123.0637881442452937, -0.4660016031367893996, -10.09054647747474043 ) ) ;
#9193=CARTESIAN_POINT ( 'NONE',  ( 121.2485348109119769, -0.4660016031367893996, -10.09054647747474043 ) ) ;
#9196=CARTESIAN_POINT ( 'NONE',  ( 121.0216281442452981, -1.561330072975668948, -17.79121239304076951 ) ) ;
#9197=CARTESIAN_POINT ( 'NONE',  ( 120.0572748109119772, -3.383040157471821630, -19.15922257007629170 ) ) ;
#9201=ORIENTED_EDGE ( 'NONE', *, *, #31738, .F. ) ;
#9203=DIRECTION ( 'NONE',  ( 1.000000000000000000, 0.000000000000000000, 0.000000000000000000 ) ) ;
#9204=CARTESIAN_POINT ( 'NONE',  ( 123.1205148109119563, -7.643976991954077427, -18.09477374809248928 ) ) ;
#9208=CARTESIAN_POINT ( 'NONE',  ( 116.9940348109119839, -0.1624402480850797581, -16.17319339645315424 ) ) ;
#9211=CARTESIAN_POINT ( 'NONE',  ( 112.4559014775786778, -0.1624402480850797581, -16.17319339645315424 ) ) ;
#9212=CARTESIAN_POINT ( 'NONE',  ( 125.2194014775786286, -10.30919188438810075, -12.61870101168855918 ) ) ;
#9215=CARTESIAN_POINT ( 'NONE',  ( 123.2339681442453241, -3.505236298600246325, -18.68346056562440793 ) ) ;
#9216=CARTESIAN_POINT ( 'NONE',  ( 116.7671281442453335, -1.834011780172310813, -8.268836392978581529 ) ) ;
#9217=CARTESIAN_POINT ( 'NONE',  ( 121.3619881442452879, -4.089484607189486809, -7.948022111789456723 ) ) ;
#9218=CARTESIAN_POINT ( 'NONE',  ( 122.6667014775786413, -2.084020599724406786, -8.691656652584148546 ) ) ;
#9219=ORIENTED_EDGE ( 'NONE', *, *, #13074, .T. ) ;
#9223=CARTESIAN_POINT ( 'NONE',  ( 124.7655881442452852, 0.5811942927096110934, -14.16772938898807510 ) ) ;
#9224=CARTESIAN_POINT ( 'NONE',  ( 113.8740681442453138, -9.859900752359374465, -12.68260735090039404 ) ) ;
#9225=CARTESIAN_POINT ( 'NONE',  ( 125.3328548109119964, -9.261995988541697145, -16.69588392320189030 ) ) ;
#9228=ORIENTED_EDGE ( 'NONE', *, *, #21674, .F. ) ;
#9229=CARTESIAN_POINT ( 'NONE',  ( 119.0405381477680038, -2.280480477428463715, -18.08254604495226658 ) ) ;
#9233=CARTESIAN_POINT ( 'NONE',  ( 118.5256548109119876, -8.899110576539710493, -16.42337572283490132 ) ) ;
#9234=CARTESIAN_POINT ( 'NONE',  ( 115.0653281442453277, -3.505236298600246325, -18.68346056562440793 ) ) ;
#9235=CARTESIAN_POINT ( 'NONE',  ( 125.7299414775786204, -10.15424416112551143, -14.75197769757842181 ) ) ;
#9237=CARTESIAN_POINT ( 'NONE',  ( 115.6740958961590593, -2.263366209404225504, -18.10533625161308180 ) ) ;
#9238=CARTESIAN_POINT ( 'NONE',  ( 116.6536748109119941, -10.15424416112533912, -14.75197769757731336 ) ) ;
#9239=CARTESIAN_POINT ( 'NONE',  ( 113.6471614775786492, -4.153390946401321671, -8.397313243818183892 ) ) ;
#9243=CARTESIAN_POINT ( 'NONE',  ( 122.2696148109119889, -4.089484607189486809, -7.948022111789456723 ) ) ;
#9244=CARTESIAN_POINT ( 'NONE',  ( 124.4819548109119722, -2.084020599724406786, -8.691656652584148546 ) ) ;
#9247=CARTESIAN_POINT ( 'NONE',  ( 125.9001214775786224, -4.089484607189486809, -7.948022111789456723 ) ) ;
#9250=CARTESIAN_POINT ( 'NONE',  ( 125.1059481442452750, -1.833838273342660141, -17.42832698103878286 ) ) ;
#9252=CARTESIAN_POINT ( 'NONE',  ( 120.3409081442453044, -8.899110576539710493, -16.42337572283490132 ) ) ;
#9255=CARTESIAN_POINT ( 'NONE',  ( 117.0507614775786465, -10.30919188438810252, -12.61870101168856628 ) ) ;
#9257=CARTESIAN_POINT ( 'NONE',  ( 114.0442481442453300, -7.643976991954077427, -18.09477374809248928 ) ) ;
#9261=CARTESIAN_POINT ( 'NONE',  ( 121.1350814775786233, 0.5811942927096110934, -14.16772938898807510 ) ) ;
#9262=CARTESIAN_POINT ( 'NONE',  ( 120.7379948109119709, -10.63000616557722466, -14.87417383870573495 ) ) ;
#9264=CARTESIAN_POINT ( 'NONE',  ( 117.8449348109119938, -8.166667518702817929, -8.995218007635861213 ) ) ;
#9265=CARTESIAN_POINT ( 'NONE',  ( 113.1933481442453058, -4.089484607189486809, -7.948022111789456723 ) ) ;
#9267=CARTESIAN_POINT ( 'NONE',  ( 113.6471614775786492, -4.153390946401321671, -8.397313243818183892 ) ) ;
#9268=CARTESIAN_POINT ( 'NONE',  ( 112.6260814775786514, -0.8288870151387760510, -10.36305467784173118 ) ) ;
#9269=CARTESIAN_POINT ( 'NONE',  ( 120.4543614775786295, -4.089484607189486809, -7.948022111789456723 ) ) ;
#9271=CARTESIAN_POINT ( 'NONE',  ( 124.6521348109119884, -7.894159318335828068, -9.358103419637847864 ) ) ;
#9274=CARTESIAN_POINT ( 'NONE',  ( 112.5126281442453120, 0.1319031606808879209, -14.10382304977623669 ) ) ;
#9276=CARTESIAN_POINT ( 'NONE',  ( 118.6391081442452986, -5.574606645277164318, -18.38911715685844683 ) ) ;
#9277=CARTESIAN_POINT ( 'NONE',  ( 111.3780948109119890, -5.574606645277164318, -18.38911715685844683 ) ) ;
#9279=CARTESIAN_POINT ( 'NONE',  ( 121.0783548109119749, -9.565557343593413364, -10.61323700422348004 ) ) ;
#9285=CARTESIAN_POINT ( 'NONE',  ( 124.5954081442453116, -3.383040157471821630, -19.15922257007629170 ) ) ;
#9287=CARTESIAN_POINT ( 'NONE',  ( 111.8886348109120092, -3.383040157471821630, -19.15922257007629170 ) ) ;
#9295=CARTESIAN_POINT ( 'NONE',  ( 126.1837548109119211, -10.63000616557722466, -14.87417383870573495 ) ) ;
#9296=CARTESIAN_POINT ( 'NONE',  ( 116.8805814775786445, -3.505236298600246325, -18.68346056562440793 ) ) ;
#9299=CARTESIAN_POINT ( 'NONE',  ( 123.9146881442452894, 0.9020085738987339008, -11.91225656197089222 ) ) ;
#9300=CARTESIAN_POINT ( 'NONE',  ( 113.9875214775786532, -0.4660016031367893996, -10.09054647747474043 ) ) ;
#9303=CARTESIAN_POINT ( 'NONE',  ( 124.7088614775786226, -9.565557343593413364, -10.61323700422348004 ) ) ;
#9304=CARTESIAN_POINT ( 'NONE',  ( 125.4463081442452932, -5.638512984488999180, -18.83840828888717311 ) ) ;
#9308=CARTESIAN_POINT ( 'NONE',  ( 116.3133148109120043, -2.084020599724406786, -8.691656652584148546 ) ) ;
#9309=CARTESIAN_POINT ( 'NONE',  ( 117.5045748109119756, -9.859900752359374465, -12.68260735090039404 ) ) ;
#9312=ORIENTED_EDGE ( 'NONE', *, *, #24773, .F. ) ;
#9313=CYLINDRICAL_SURFACE ( 'NONE', #26981, 1.999999999999998890 ) ;
#9314=CARTESIAN_POINT ( 'NONE',  ( 126.4106614775786284, -6.222761293078241884, -8.102969835052219238 ) ) ;
#9321=CARTESIAN_POINT ( 'NONE',  ( 117.7314814775786260, -4.089484607189486809, -7.948022111789456723 ) ) ;
#9322=CARTESIAN_POINT ( 'NONE',  ( 125.8433948109119456, -7.643976991954077427, -18.09477374809248928 ) ) ;
#9323=EDGE_CURVE ( 'NONE', #22022, #13784, #44888, .T. ) ;
#9324=CARTESIAN_POINT ( 'NONE',  ( 115.6325948109119821, -9.565557343593413364, -10.61323700422348004 ) ) ;
#9325=CARTESIAN_POINT ( 'NONE',  ( 116.2050738206745137, -2.348512537728063787, -17.99195118506216318 ) ) ;
#9326=CARTESIAN_POINT ( 'NONE',  ( 124.1983214775786166, -8.166667518702828588, -8.995218007635868318 ) ) ;
#9327=CARTESIAN_POINT ( 'NONE',  ( 114.1009748109119784, -4.089484607189486809, -7.948022111789456723 ) ) ;
#9329=CARTESIAN_POINT ( 'NONE',  ( 123.2339681442453241, -6.344957434206665248, -7.627207830600338134 ) ) ;
#9332=CARTESIAN_POINT ( 'NONE',  ( 114.5547881442453217, -5.638512984488999180, -18.83840828888717311 ) ) ;
#9333=CARTESIAN_POINT ( 'NONE',  ( 115.6893214775786447, -9.859900752359374465, -12.68260735090039404 ) ) ;
#9335=CARTESIAN_POINT ( 'NONE',  ( 113.3068014775786594, -8.166667518702817929, -8.995218007635859436 ) ) ;
#9337=CARTESIAN_POINT ( 'NONE',  ( 123.3474214775786209, -9.988377603198976828, -10.36322818467138340 ) ) ;
#9341=CARTESIAN_POINT ( 'NONE',  ( 115.5758681442453053, -7.894159318335828068, -9.358103419637847864 ) ) ;
#9342=CARTESIAN_POINT ( 'NONE',  ( 123.6270561621488184, -4.437987522111543015, -15.20954377567900373 ) ) ;
#9343=CARTESIAN_POINT ( 'NONE',  ( 114.6115148109119986, -6.222761293078241884, -8.102969835052219238 ) ) ;
#9346=CARTESIAN_POINT ( 'NONE',  ( 115.8027748109119841, -8.899110576539710493, -16.42337572283490132 ) ) ;
#9347=CARTESIAN_POINT ( 'NONE',  ( 114.4980614775786592, -7.893985811506177619, -18.51759400769804742 ) ) ;
#9349=CARTESIAN_POINT ( 'NONE',  ( 126.6942948109119840, -8.899110576539710493, -16.42337572283490132 ) ) ;
#9350=CARTESIAN_POINT ( 'NONE',  ( 114.7249681442453237, -9.565557343593413364, -10.61323700422348004 ) ) ;
#9351=CARTESIAN_POINT ( 'NONE',  ( 124.5386814775786206, -5.638512984488999180, -18.83840828888717311 ) ) ;
#9352=CARTESIAN_POINT ( 'NONE',  ( 122.2128881442453263, -1.834011780172310813, -8.268836392978581529 ) ) ;
#9354=CARTESIAN_POINT ( 'NONE',  ( 112.9664414775786412, 0.5811942927096154232, -14.16772938898807155 ) ) ;
#9361=CARTESIAN_POINT ( 'NONE',  ( 118.2987481442453088, -1.561330072975668504, -17.79121239304076951 ) ) ;
#9364=CARTESIAN_POINT ( 'NONE',  ( 114.3278814775786429, 0.1319031606808879209, -14.10382304977623669 ) ) ;
#9366=CARTESIAN_POINT ( 'NONE',  ( 118.2987481442453088, -1.561330072975668504, -17.79121239304076951 ) ) ;
#9368=DIRECTION ( 'NONE',  ( 1.000000000000000000, 0.000000000000000000, 0.000000000000000000 ) ) ;
#9371=CARTESIAN_POINT ( 'NONE',  ( 121.8725281442453223, -6.222761293078241884, -8.102969835052219238 ) ) ;
#9372=CARTESIAN_POINT ( 'NONE',  ( 121.4754414775786131, -8.166667518702819706, -8.995218007635861213 ) ) ;
#9373=CARTESIAN_POINT ( 'NONE',  ( 113.3068014775786594, -1.833838273342658809, -17.42832698103878286 ) ) ;
#9374=CARTESIAN_POINT ( 'NONE',  ( 114.1577014775786552, -6.344957434206662583, -7.627207830600332805 ) ) ;
#9375=CARTESIAN_POINT ( 'NONE',  ( 118.2005203923315548, -1.063912429576147511, -17.20460841810472985 ) ) ;
#9376=CARTESIAN_POINT ( 'NONE',  ( 125.7866681442452688, -8.899110576539710493, -16.42337572283490132 ) ) ;
#9377=CARTESIAN_POINT ( 'NONE',  ( 119.4900081442453086, -7.643976991954077427, -18.09477374809248928 ) ) ;
#9378=ORIENTED_EDGE ( 'NONE', *, *, #19023, .T. ) ;
#9379=CARTESIAN_POINT ( 'NONE',  ( 119.5467348109119712, -4.089484607189483256, -7.948022111789462052 ) ) ;
#9380=CARTESIAN_POINT ( 'NONE',  ( 113.2500748109119968, -6.344957434206662583, -7.627207830600332805 ) ) ;
#9381=CARTESIAN_POINT ( 'NONE',  ( 122.2696148109119889, -5.574606645277164318, -18.38911715685844683 ) ) ;
#9384=CARTESIAN_POINT ( 'NONE',  ( 117.2776681442452968, -5.638512984488999180, -18.83840828888717311 ) ) ;
#9386=CARTESIAN_POINT ( 'NONE',  ( 117.1074881442453233, 0.4262465694468514643, -12.03445270309931736 ) ) ;
#9389=CARTESIAN_POINT ( 'NONE',  ( 111.8319081442453182, -5.638512984488999180, -18.83840828888717311 ) ) ;
#9390=B_SPLINE_CURVE_WITH_KNOTS ( 'NONE', 3,
 ( #20034, #6117, #33916, #27554, #3151, #37343, #24133, #41466, #13859, #6572, #20710, #30964, #12974, #2687, #6348, #23458, #33690, #41249, #10448, #19802, #41022, #38025, #6801, #20262 ),
 .UNSPECIFIED., .F., .F.,
 ( 4, 2, 2, 1, 1, 1, 2, 2, 2, 1, 1, 1, 2, 2, 4 ),
 ( 0.000000000000000000, 0.2499999999999916178, 0.3749999999999865663, 0.4374999999999830136, 0.4687499999999789058, 0.4843749999999755196, 0.4921874999999747979, 0.4999999999999740208, 0.6249999999999837907, 0.6874999999999900080, 0.7187499999999965583, 0.7343749999999972244, 0.7421874999999965583, 0.7499999999999957812, 1.000000000000000000 ),
 .UNSPECIFIED. ) ;
#9391=CARTESIAN_POINT ( 'NONE',  ( 122.0994348109119443, -10.15424416112533912, -14.75197769757731336 ) ) ;
#9393=ORIENTED_EDGE ( 'NONE', *, *, #21448, .F. ) ;
#9394=CARTESIAN_POINT ( 'NONE',  ( 118.4122014775786340, 0.5811942927096110934, -14.16772938898807510 ) ) ;
#9396=CARTESIAN_POINT ( 'NONE',  ( 120.3976348109119812, -1.834011780172310813, -8.268836392978581529 ) ) ;
#9397=CARTESIAN_POINT ( 'NONE',  ( 113.4769814775786330, -10.63000616557722466, -14.87417383870573495 ) ) ;
#9398=CARTESIAN_POINT ( 'NONE',  ( 120.6245414775786458, -0.1624402480850797581, -16.17319339645315424 ) ) ;
#9400=CARTESIAN_POINT ( 'NONE',  ( 111.8319081442453182, -5.638512984488999180, -18.83840828888717311 ) ) ;
#9401=EDGE_CURVE ( 'NONE', #21122, #28482, #9390, .T. ) ;
#9403=CARTESIAN_POINT ( 'NONE',  ( 124.4252281442452812, -0.8288870151387760510, -10.36305467784173118 ) ) ;
#9404=CARTESIAN_POINT ( 'NONE',  ( 123.5743281442453139, -7.893985811506158079, -18.51759400769805453 ) ) ;
#9409=CARTESIAN_POINT ( 'NONE',  ( 122.6667014775786413, -7.893985811506177619, -18.51759400769804742 ) ) ;
#9410=CARTESIAN_POINT ( 'NONE',  ( 121.9292548109119849, -7.894159318335828068, -9.358103419637847864 ) ) ;
#9412=CARTESIAN_POINT ( 'NONE',  ( 119.8870948109119752, -9.261995988541697145, -16.69588392320189030 ) ) ;
#9413=CARTESIAN_POINT ( 'NONE',  ( 112.9664414775786412, -9.859900752359374465, -12.68260735090039404 ) ) ;
#9414=CARTESIAN_POINT ( 'NONE',  ( 119.7736414775786358, -10.30919188438810075, -12.61870101168855918 ) ) ;
#9415=CARTESIAN_POINT ( 'NONE',  ( 120.1707281442453166, 0.2603800115204892296, -16.42320221600525088 ) ) ;
#9417=CARTESIAN_POINT ( 'NONE',  ( 125.7299414775786346, -10.15424416112533912, -14.75197769757731336 ) ) ;
#9423=CARTESIAN_POINT ( 'NONE',  ( 124.8223148109119762, -10.15424416112533912, -14.75197769757731336 ) ) ;
#9426=CARTESIAN_POINT ( 'NONE',  ( 117.7314814775786260, -5.574606645277164318, -18.38911715685844683 ) ) ;
#9429=CARTESIAN_POINT ( 'NONE',  ( 117.1642148109119859, -0.8288870151387760510, -10.36305467784173118 ) ) ;
#9430=CARTESIAN_POINT ( 'NONE',  ( 123.5743281442453139, -7.893985811506177619, -18.51759400769804742 ) ) ;
#9433=CARTESIAN_POINT ( 'NONE',  ( 121.9292548109119849, -7.894159318335828068, -9.358103419637847864 ) ) ;
#9434=CARTESIAN_POINT ( 'NONE',  ( 117.8449348109119938, -8.166667518702817929, -8.995218007635861213 ) ) ;
#9435=CARTESIAN_POINT ( 'NONE',  ( 124.6521348109119884, -1.561330072975668948, -17.79121239304076951 ) ) ;
#9436=CARTESIAN_POINT ( 'NONE',  ( 122.1561614775786353, -8.899110576539710493, -16.42337572283490132 ) ) ;
#9441=CARTESIAN_POINT ( 'NONE',  ( 124.5386814775786206, -5.638512984488999180, -18.83840828888717311 ) ) ;
#9442=CARTESIAN_POINT ( 'NONE',  ( 115.6325948109119821, -9.565557343593413364, -10.61323700422348004 ) ) ;
#9443=CARTESIAN_POINT ( 'NONE',  ( 125.1626748109119802, -9.988377603198980381, -10.36322818467138518 ) ) ;
#9446=ORIENTED_EDGE ( 'NONE', *, *, #34328, .F. ) ;
#9447=ADVANCED_FACE ( 'NONE', ( #45102 ), #3553, .T. ) ;
#9453=CARTESIAN_POINT ( 'NONE',  ( 121.0783548109119749, -9.565557343593413364, -10.61323700422348004 ) ) ;
#9454=CARTESIAN_POINT ( 'NONE',  ( 115.6893214775786447, -9.859900752359374465, -12.68260735090039404 ) ) ;
#9455=CARTESIAN_POINT ( 'NONE',  ( 125.6732148109119862, -9.859900752359370912, -12.68260735090036562 ) ) ;
#9457=ADVANCED_FACE ( 'NONE', ( #31849 ), #31254, .F. ) ;
#9460=CARTESIAN_POINT ( 'NONE',  ( 120.7947214775786193, -0.8288870151387760510, -10.36305467784173118 ) ) ;
#9461=CARTESIAN_POINT ( 'NONE',  ( 112.6260814775786514, -0.8288870151387760510, -10.36305467784173118 ) ) ;
#9464=CARTESIAN_POINT ( 'NONE',  ( 111.2184548109119788, -8.862178061932382889, -16.39564131203247399 ) ) ;
#9465=DIRECTION ( 'NONE',  ( 1.000000000000000000, 0.000000000000000000, 0.000000000000000000 ) ) ;
#9466=CARTESIAN_POINT ( 'NONE',  ( 122.2128881442453263, -1.834011780172310813, -8.268836392978581529 ) ) ;
#9467=CARTESIAN_POINT ( 'NONE',  ( 112.9664414775786412, 0.5811942927096154232, -14.16772938898807155 ) ) ;
#9471=CARTESIAN_POINT ( 'NONE',  ( 113.4725659692789748, -1.179503403430478770, -17.05068175419387799 ) ) ;
#9473=CARTESIAN_POINT ( 'NONE',  ( 124.1415948109119540, -3.505236298600246325, -18.68346056562440793 ) ) ;
#9474=CARTESIAN_POINT ( 'NONE',  ( 118.7525614775786380, -1.833838273342659253, -17.42832698103878286 ) ) ;
#9479=CARTESIAN_POINT ( 'NONE',  ( 113.5904348109119866, -2.084020599724406786, -8.691656652584148546 ) ) ;
#9482=CARTESIAN_POINT ( 'NONE',  ( 123.2906948109119867, -8.166667518702819706, -8.995218007635861213 ) ) ;
#9483=CARTESIAN_POINT ( 'NONE',  ( 122.3830681442452857, -8.166667518702819706, -8.995218007635861213 ) ) ;
#9485=CARTESIAN_POINT ( 'NONE',  ( 118.4122014775786340, 0.5811942927096110934, -14.16772938898807510 ) ) ;
#9486=CARTESIAN_POINT ( 'NONE',  ( 113.2500748109119968, -6.344957434206662583, -7.627207830600332805 ) ) ;
#9488=CARTESIAN_POINT ( 'NONE',  ( 113.8173414775786512, -9.565557343593413364, -10.61323700422348004 ) ) ;
#9489=CARTESIAN_POINT ( 'NONE',  ( 125.7866681442452688, -0.4660016031367893996, -10.09054647747474043 ) ) ;
#9490=CARTESIAN_POINT ( 'NONE',  ( 121.3619881442452879, -4.089484607189486809, -7.948022111789456723 ) ) ;
#9492=CARTESIAN_POINT ( 'NONE',  ( 114.8384214775786489, 0.9020085738987339008, -11.91225656197089222 ) ) ;
#9494=CARTESIAN_POINT ( 'NONE',  ( 113.6471614775786492, -4.153390946401321671, -8.397313243818183892 ) ) ;
#9496=CARTESIAN_POINT ( 'NONE',  ( 116.0864081442453113, -0.1624402480850797581, -16.17319339645315424 ) ) ;
#9497=CARTESIAN_POINT ( 'NONE',  ( 113.6471614775786492, -4.153390946401321671, -8.397313243818183892 ) ) ;
#9501=CARTESIAN_POINT ( 'NONE',  ( 124.0848681442452772, -5.574606645277164318, -18.38911715685844683 ) ) ;
#9506=CARTESIAN_POINT ( 'NONE',  ( 124.7655881442452852, 0.5811942927096110934, -14.16772938898807510 ) ) ;
#9508=CARTESIAN_POINT ( 'NONE',  ( 111.7184548109119788, -9.261995988541697145, -16.69588392320189030 ) ) ;
#9512=CARTESIAN_POINT ( 'NONE',  ( 123.6071420163423085, -1.087735405160626723, -17.17288456429612964 ) ) ;
#9513=CARTESIAN_POINT ( 'NONE',  ( 137.1322768238038350, -4.609925023091584251, -18.75211014789456598 ) ) ;
#9515=CARTESIAN_POINT ( 'NONE',  ( 124.4252281442452812, -9.261995988541697145, -16.69588392320189030 ) ) ;
#9516=CARTESIAN_POINT ( 'NONE',  ( 120.4543614775786295, -5.574606645277164318, -18.38911715685844683 ) ) ;
#9518=ORIENTED_EDGE ( 'NONE', *, *, #6378, .T. ) ;
#9519=CARTESIAN_POINT ( 'NONE',  ( 122.3263414775786373, -6.344957434206665248, -7.627207830600338134 ) ) ;
#9521=CARTESIAN_POINT ( 'NONE',  ( 120.4543614775786295, -4.089484607189486809, -7.948022111789456723 ) ) ;
#9523=CARTESIAN_POINT ( 'NONE',  ( 113.5337081442453240, -0.8288870151387760510, -10.36305467784173118 ) ) ;
#9524=( BOUNDED_CURVE ( )  B_SPLINE_CURVE ( 2, ( #31328, #14682, #547, #7608, #18329, #995, #6951, #24286, #31553, #35180, #42731, #28596, #35639, #102, #24943, #7159, #42507 ),
 .UNSPECIFIED., .F., .F. ) 
 B_SPLINE_CURVE_WITH_KNOTS ( ( 3, 2, 2, 2, 2, 2, 2, 2, 3 ),
 ( 0.1420046674808919940, 0.1484375000000000000, 0.1562500000000000000, 0.1640625000000000000, 0.1718750000000000000, 0.1796875000000000000, 0.1875000000000000000, 0.1953125000000000000, 0.2017453325190585178 ),
 .UNSPECIFIED. ) 
 CURVE ( )  GEOMETRIC_REPRESENTATION_ITEM ( )  RATIONAL_B_SPLINE_CURVE ( ( 0.9778625265006459788, 0.9373222120152210346, 1.000000000000000000, 0.9238795325112869605, 1.000000000000000000, 0.9238795325112869605, 1.000000000000000000, 0.9238795325112869605, 1.000000000000000000, 0.9238795325112869605, 1.000000000000000000, 0.9238795325112869605, 1.000000000000000000, 0.9238795325112869605, 1.000000000000000000, 0.9373222120157019832, 0.9778625265000240319 ) ) 
 REPRESENTATION_ITEM ( '' )  );
#9525=CARTESIAN_POINT ( 'NONE',  ( 112.0020881442453344, 0.2603800115204892296, -16.42320221600525088 ) ) ;
#9526=CARTESIAN_POINT ( 'NONE',  ( 123.6310548109119765, -5.638512984488999180, -18.83840828888717311 ) ) ;
#9530=CARTESIAN_POINT ( 'NONE',  ( 116.4834948109119779, -7.894159318335828068, -9.358103419637847864 ) ) ;
#9532=CARTESIAN_POINT ( 'NONE',  ( 118.0151148109119816, 0.4262465694468514643, -12.03445270309931736 ) ) ;
#9536=AXIS2_PLACEMENT_3D ( 'NONE', #30681, #6282, #20651 ) ;
#9538=CARTESIAN_POINT ( 'NONE',  ( 112.0020881442453344, 0.2603800115204892296, -16.42320221600525088 ) ) ;
#9544=CARTESIAN_POINT ( 'NONE',  ( 111.5045738707033536, -1.272620149025138092, -16.92668288537504750 ) ) ;
#9546=CARTESIAN_POINT ( 'NONE',  ( 118.9794681442453026, -9.261995988541697145, -16.69588392320189030 ) ) ;
#9547=CARTESIAN_POINT ( 'NONE',  ( 125.9568481442452850, -3.505236298600246325, -18.68346056562440793 ) ) ;
#9548=CARTESIAN_POINT ( 'NONE',  ( 118.0718414775786442, -0.8288870151387760510, -10.36305467784173118 ) ) ;
#9550=CARTESIAN_POINT ( 'NONE',  ( 122.0994348109119443, 0.9020085738987339008, -11.91225656197089222 ) ) ;
#9551=CARTESIAN_POINT ( 'NONE',  ( 113.7038881442453402, -3.383040157471821630, -19.15922257007629170 ) ) ;
#9554=CARTESIAN_POINT ( 'NONE',  ( 125.1059481442452750, -8.166667518702819706, -8.995218007635861213 ) ) ;
#9555=B_SPLINE_CURVE_WITH_KNOTS ( 'NONE', 3,
 ( #22462, #36494, #37159, #30343, #5480, #15987, #19858, #43576, #39929, #40610 ),
 .UNSPECIFIED., .F., .F.,
 ( 4, 3, 3, 4 ),
 ( 0.000000000000000000, 0.0001671877560958114864, 0.0003343755126086594954, 0.0006438490228507209303 ),
 .UNSPECIFIED. ) ;
#9558=CARTESIAN_POINT ( 'NONE',  ( 119.7169148109119874, -9.988377603198976828, -10.36322818467138340 ) ) ;
#9559=CARTESIAN_POINT ( 'NONE',  ( 115.8027748109119841, -8.899110576539710493, -16.42337572283490132 ) ) ;
#9560=CARTESIAN_POINT ( 'NONE',  ( 126.9115046738230319, -4.631886270669566485, -18.73501732256985619 ) ) ;
#9561=CARTESIAN_POINT ( 'NONE',  ( 112.3991748109119868, -8.166667518702817929, -8.995218007635859436 ) ) ;
#9564=CARTESIAN_POINT ( 'NONE',  ( 120.7379948109119709, -10.63000616557722466, -14.87417383870573495 ) ) ;
#9569=CARTESIAN_POINT ( 'NONE',  ( 115.6325948109119821, -9.565557343593413364, -10.61323700422348004 ) ) ;
#9570=CARTESIAN_POINT ( 'NONE',  ( 112.4174607241439361, -2.443475742715324639, -17.86549347949428679 ) ) ;
#9571=CARTESIAN_POINT ( 'NONE',  ( 116.3700414775786527, -4.153390946401321671, -8.397313243818183892 ) ) ;
#9575=CARTESIAN_POINT ( 'NONE',  ( 114.3846081442453197, 0.4262465694468514643, -12.03445270309931736 ) ) ;
#9576=CARTESIAN_POINT ( 'NONE',  ( 116.0864081442453113, -9.988377603198976828, -10.36322818467138340 ) ) ;
#9578=CARTESIAN_POINT ( 'NONE',  ( 112.6828081442453282, -7.893985811506177619, -18.51759400769804742 ) ) ;
#9579=CARTESIAN_POINT ( 'NONE',  ( 117.0507614775786465, 0.1319031606808879209, -14.10382304977623669 ) ) ;
#9580=CARTESIAN_POINT ( 'NONE',  ( 125.1059481442452750, -8.166667518702819706, -8.995218007635861213 ) ) ;
#9581=CARTESIAN_POINT ( 'NONE',  ( 118.1852948109119836, -4.153390946401325223, -8.397313243818185668 ) ) ;
#9583=CARTESIAN_POINT ( 'NONE',  ( 113.4769814775786330, -10.63000616557722466, -14.87417383870573495 ) ) ;
#9589=CARTESIAN_POINT ( 'NONE',  ( 119.6034614775786196, -6.344957434206665248, -7.627207830600338134 ) ) ;
#9591=CARTESIAN_POINT ( 'NONE',  ( 125.7299414775786346, 0.9020085738987339008, -11.91225656197089222 ) ) ;
#9592=CARTESIAN_POINT ( 'NONE',  ( 124.7655881442452852, 0.5811942927096102052, -14.16772938898805556 ) ) ;
#9593=CARTESIAN_POINT ( 'NONE',  ( 115.7460481442453357, -10.15424416112533912, -14.75197769757731336 ) ) ;
#9595=CARTESIAN_POINT ( 'NONE',  ( 123.8012348109119642, 0.2603800115204892296, -16.42320221600525088 ) ) ;
#9600=CARTESIAN_POINT ( 'NONE',  ( 123.6877814775786533, -6.222761293078241884, -8.102969835052219238 ) ) ;
#9601=CARTESIAN_POINT ( 'NONE',  ( 121.5321681442453183, -9.988377603198976828, -10.36322818467138340 ) ) ;
#9603=CARTESIAN_POINT ( 'NONE',  ( 112.5126281442453120, 0.1319031606808879209, -14.10382304977623669 ) ) ;
#9604=CARTESIAN_POINT ( 'NONE',  ( 116.2565881442452991, -9.261995988541697145, -16.69588392320189030 ) ) ;
#9606=CARTESIAN_POINT ( 'NONE',  ( 128.2184548109119930, -1.191816558809784876, -8.648209655763537285 ) ) ;
#9607=CARTESIAN_POINT ( 'NONE',  ( 118.2420214775786320, -6.222761293078241884, -8.102969835052219238 ) ) ;
#9610=CARTESIAN_POINT ( 'NONE',  ( 114.7816948109119863, 0.5811942927096154232, -14.16772938898807155 ) ) ;
#9611=CARTESIAN_POINT ( 'NONE',  ( 121.9859814775786333, -9.565557343593413364, -10.61323700422348004 ) ) ;
#9614=CARTESIAN_POINT ( 'NONE',  ( 137.4945747549916462, -0.6989084441936219694, -10.59149681938009380 ) ) ;
#9615=CARTESIAN_POINT ( 'NONE',  ( 118.5256548109119876, -0.4660016031367893996, -10.09054647747474043 ) ) ;
#9617=CARTESIAN_POINT ( 'NONE',  ( 115.0086014775786509, -5.574606645277164318, -18.38911715685844683 ) ) ;
#9621=CARTESIAN_POINT ( 'NONE',  ( 125.9568481442452850, -3.505236298600246325, -18.68346056562440793 ) ) ;
#9622=CARTESIAN_POINT ( 'NONE',  ( 119.5467348109119712, -5.574606645277164318, -18.38911715685844683 ) ) ;
#9624=CARTESIAN_POINT ( 'NONE',  ( 120.3976348109119812, -1.834011780172310813, -8.268836392978581529 ) ) ;
#9627=CARTESIAN_POINT ( 'NONE',  ( 119.7169148109119874, -9.988377603198976828, -10.36322818467138340 ) ) ;
#9628=CARTESIAN_POINT ( 'NONE',  ( 117.2209414775786485, -7.893985811506177619, -18.51759400769804742 ) ) ;
#9629=CARTESIAN_POINT ( 'NONE',  ( 120.2841814775786276, -10.15424416112533912, -14.75197769757731336 ) ) ;
#9630=CARTESIAN_POINT ( 'NONE',  ( 125.7299414775786346, -10.15424416112533912, -14.75197769757731336 ) ) ;
#9631=CARTESIAN_POINT ( 'NONE',  ( 112.3416152477524008, -1.220279397241704755, -16.99638242193885418 ) ) ;
#9632=B_SPLINE_CURVE_WITH_KNOTS ( 'NONE', 3,
 ( #28526, #36241, #32813, #18705, #14607, #31923, #4785, #18254, #5007, #11195 ),
 .UNSPECIFIED., .F., .F.,
 ( 4, 3, 3, 4 ),
 ( 0.000000000000000000, 1.701546542203775152E-05, 3.403093084406119836E-05, 6.582972837196840747E-05 ),
 .UNSPECIFIED. ) ;
#9634=CARTESIAN_POINT ( 'NONE',  ( 123.1772414775786189, -5.574606645277164318, -18.38911715685844683 ) ) ;
#9640=CARTESIAN_POINT ( 'NONE',  ( 123.4041481442452834, -10.30919188438810075, -12.61870101168855918 ) ) ;
#9641=CARTESIAN_POINT ( 'NONE',  ( 122.8368814775786291, -7.894159318335828068, -9.358103419637847864 ) ) ;
#9643=CARTESIAN_POINT ( 'NONE',  ( 123.9146881442452894, 0.9020085738987339008, -11.91225656197089222 ) ) ;
#9644=CARTESIAN_POINT ( 'NONE',  ( 113.5337081442453240, -0.8288870151387760510, -10.36305467784173118 ) ) ;
#9646=CARTESIAN_POINT ( 'NONE',  ( 119.2063748109119814, -1.561330072975668504, -17.79121239304076951 ) ) ;
#9647=CARTESIAN_POINT ( 'NONE',  ( 122.8936081442453059, 0.2603800115204892296, -16.42320221600525088 ) ) ;
#9649=CARTESIAN_POINT ( 'NONE',  ( 125.5030348109119558, -6.222761293078241884, -8.102969835052219238 ) ) ;
#9651=CARTESIAN_POINT ( 'NONE',  ( 116.0864081442453113, -9.988377603198973276, -10.36322818467138163 ) ) ;
#9655=CARTESIAN_POINT ( 'NONE',  ( 135.3184548109119874, -4.863998795839242995, -13.39321520033831447 ) ) ;
#9657=CARTESIAN_POINT ( 'NONE',  ( 124.5954081442453116, -6.222761293078241884, -8.102969835052219238 ) ) ;
#9660=CARTESIAN_POINT ( 'NONE',  ( 118.8660148109119774, 0.1319031606808879209, -14.10382304977623669 ) ) ;
#9662=CARTESIAN_POINT ( 'NONE',  ( 117.6180281442453150, -8.899110576539710493, -16.42337572283490132 ) ) ;
#9663=CARTESIAN_POINT ( 'NONE',  ( 122.4397948109119767, -9.988377603198976828, -10.36322818467138340 ) ) ;
#9664=ORIENTED_EDGE ( 'NONE', *, *, #36685, .T. ) ;
#9665=CARTESIAN_POINT ( 'NONE',  ( 122.8368814775786291, -7.894159318335828068, -9.358103419637847864 ) ) ;
#9667=CARTESIAN_POINT ( 'NONE',  ( 117.2209414775786485, -7.893985811506177619, -18.51759400769804742 ) ) ;
#9668=CARTESIAN_POINT ( 'NONE',  ( 125.0492214775786266, -6.344957434206665248, -7.627207830600338134 ) ) ;
#9669=CARTESIAN_POINT ( 'NONE',  ( 124.7088614775786226, -9.565557343593413364, -10.61323700422348004 ) ) ;
#9673=CARTESIAN_POINT ( 'NONE',  ( 125.7299414775786346, 0.9020085738987339008, -11.91225656197089222 ) ) ;
#9674=CARTESIAN_POINT ( 'NONE',  ( 114.0442481442453300, -7.643976991954077427, -18.09477374809248928 ) ) ;
#9675=CARTESIAN_POINT ( 'NONE',  ( 125.2194014775786286, -10.30919188438810075, -12.61870101168855918 ) ) ;
#9676=CARTESIAN_POINT ( 'NONE',  ( 114.6874464091100947, -0.9924539043446216624, -17.29976612834909133 ) ) ;
#9684=CARTESIAN_POINT ( 'NONE',  ( 120.0005481442453146, -4.153390946401325223, -8.397313243818185668 ) ) ;
#9685=CARTESIAN_POINT ( 'NONE',  ( 115.8595014775786609, -7.643976991954077427, -18.09477374809248928 ) ) ;
#9686=CARTESIAN_POINT ( 'NONE',  ( 125.1743048082055481, -0.1020945015695004648, -15.74893487844865980 ) ) ;
#9688=DIRECTION ( 'NONE',  ( -0.7071067811865480168, -0.5654279342906962658, -0.4246071727182139655 ) ) ;
#9689=CARTESIAN_POINT ( 'NONE',  ( 121.3619881442452879, -5.574606645277164318, -18.38911715685844683 ) ) ;
#9690=CARTESIAN_POINT ( 'NONE',  ( 113.8173414775786512, -9.565557343593413364, -10.61323700422348004 ) ) ;
#9692=CONICAL_SURFACE ( 'NONE', #39539, 5.999999999999997335, 0.4636476090008060935 ) ;
#9696=CARTESIAN_POINT ( 'NONE',  ( 125.8433948109119456, -1.834011780172310813, -8.268836392978581529 ) ) ;
#9697=B_SPLINE_CURVE_WITH_KNOTS ( 'NONE', 3,
 ( #18004, #1342, #4762, #38740, #4310, #894, #14813, #42408, #11172, #35769, #15256, #35308, #28726, #4080, #43076, #18463, #11845, #3861, #28276, #7509, #42632, #17783, #18231, #24848, #11396, #32353, #42184, #11615, #39198, #4539 ),
 .UNSPECIFIED., .F., .F.,
 ( 4, 2, 2, 1, 2, 2, 2, 1, 1, 2, 2, 2, 1, 1, 1, 2, 2, 4 ),
 ( 0.000000000000000000, 0.03125000000000712624, 0.06250000000001425249, 0.09375000000002137179, 0.1093750000000202061, 0.1250000000000190403, 0.1875000000000160982, 0.2187500000000227318, 0.2343750000000259792, 0.2421875000000274780, 0.2500000000000289768, 0.3750000000000738853, 0.4375000000000856537, 0.4687500000000914269, 0.4843750000000939804, 0.4921875000000951461, 0.5000000000000962563, 1.000000000000000000 ),
 .UNSPECIFIED. ) ;
#9698=CARTESIAN_POINT ( 'NONE',  ( 112.2857214775786474, -4.089484607189486809, -7.948022111789456723 ) ) ;
#9700=CARTESIAN_POINT ( 'NONE',  ( 114.9518748109119883, -1.834011780172310813, -8.268836392978581529 ) ) ;
#9701=CARTESIAN_POINT ( 'NONE',  ( 126.3999550322272540, 0.07939618298893640069, -14.60940398381636562 ) ) ;
#9703=EDGE_CURVE ( 'NONE', #24392, #40611, #28455, .T. ) ;
#9704=CARTESIAN_POINT ( 'NONE',  ( 112.0588148109119828, 0.5811942927096154232, -14.16772938898807155 ) ) ;
#9705=CARTESIAN_POINT ( 'NONE',  ( 121.4754414775786131, -1.833838273342659697, -17.42832698103878286 ) ) ;
#9710=CARTESIAN_POINT ( 'NONE',  ( 113.3635281442453504, -0.1624402480850797581, -16.17319339645315424 ) ) ;
#9714=CARTESIAN_POINT ( 'NONE',  ( 124.3685014775786328, -10.63000616557722466, -14.87417383870573495 ) ) ;
#9715=CARTESIAN_POINT ( 'NONE',  ( 122.2696148109119889, -4.089484607189486809, -7.948022111789456723 ) ) ;
#9716=DIRECTION ( 'NONE',  ( 0.000000000000000000, 0.6004852223388323917, -0.7996358532186279566 ) ) ;
#9717=CARTESIAN_POINT ( 'NONE',  ( 121.3619881442452879, -4.089484607189486809, -7.948022111789456723 ) ) ;
#9718=CARTESIAN_POINT ( 'NONE',  ( 114.1009748109119784, -4.089484607189486809, -7.948022111789456723 ) ) ;
#9719=ORIENTED_EDGE ( 'NONE', *, *, #2425, .T. ) ;
#9720=CARTESIAN_POINT ( 'NONE',  ( 112.6828081442453282, -2.084020599724406786, -8.691656652584148546 ) ) ;
#9722=CARTESIAN_POINT ( 'NONE',  ( 126.1270281442452870, -10.30919188438810075, -12.61870101168855918 ) ) ;
#9723=VECTOR ( 'NONE', #37794, 1000.000000000000000 ) ;
#9724=CARTESIAN_POINT ( 'NONE',  ( 125.5030348109119558, -3.383040157471821630, -19.15922257007629170 ) ) ;
#9725=CARTESIAN_POINT ( 'NONE',  ( 113.5337081442453240, -9.261995988541697145, -16.69588392320189030 ) ) ;
#9726=CARTESIAN_POINT ( 'NONE',  ( 113.5904348109119866, -2.084020599724406786, -8.691656652584148546 ) ) ;
#9729=CARTESIAN_POINT ( 'NONE',  ( 118.4689281442453250, -10.15424416112533912, -14.75197769757731336 ) ) ;
#9730=EDGE_CURVE ( 'NONE', #40512, #30086, #26271, .T. ) ;
#9732=AXIS2_PLACEMENT_3D ( 'NONE', #10237, #6813, #17304 ) ;
#9734=CARTESIAN_POINT ( 'NONE',  ( 122.2128881442453263, -7.643976991954077427, -18.09477374809248928 ) ) ;
#9739=CARTESIAN_POINT ( 'NONE',  ( 126.1837548109119211, -10.63000616557722466, -14.87417383870573495 ) ) ;
#9742=CARTESIAN_POINT ( 'NONE',  ( 112.3424481442453384, -6.344957434206662583, -7.627207830600333693 ) ) ;
#9746=CARTESIAN_POINT ( 'NONE',  ( 117.7314814775786260, -4.089484607189486809, -7.948022111789456723 ) ) ;
#9747=VECTOR ( 'NONE', #26656, 1000.000000000000000 ) ;
#9751=CARTESIAN_POINT ( 'NONE',  ( 126.0703014775786102, -9.988377603198980381, -10.36322818467138518 ) ) ;
#9752=CARTESIAN_POINT ( 'NONE',  ( 122.3830681442452857, -1.833838273342659697, -17.42832698103878286 ) ) ;
#9753=CARTESIAN_POINT ( 'NONE',  ( 125.5597614775786326, -7.894159318335828068, -9.358103419637847864 ) ) ;
#9755=CARTESIAN_POINT ( 'NONE',  ( 121.9859814775786333, 0.2603800115204892296, -16.42320221600525088 ) ) ;
#9756=CARTESIAN_POINT ( 'NONE',  ( 119.5467348109119712, -4.089484607189486809, -7.948022111789456723 ) ) ;
#9758=CARTESIAN_POINT ( 'NONE',  ( 113.7414098793805408, -2.191907684172563986, -18.20049396185734025 ) ) ;
#9759=CARTESIAN_POINT ( 'NONE',  ( 122.4965214775786251, -10.30919188438810075, -12.61870101168855918 ) ) ;
#9765=CARTESIAN_POINT ( 'NONE',  ( 117.4478481442453131, -9.565557343593413364, -10.61323700422348004 ) ) ;
#9766=CARTESIAN_POINT ( 'NONE',  ( 116.2565881442453133, -0.8288870151387760510, -10.36305467784173118 ) ) ;
#9771=CARTESIAN_POINT ( 'NONE',  ( 112.5126281442453120, -10.30919188438810075, -12.61870101168855918 ) ) ;
#9775=ORIENTED_EDGE ( 'NONE', *, *, #28955, .F. ) ;
#9777=CARTESIAN_POINT ( 'NONE',  ( 111.5125327111057345, -1.267766418764825875, -16.93314635290698789 ) ) ;
#9779=CARTESIAN_POINT ( 'NONE',  ( 118.0151148109119816, -10.63000616557722466, -14.87417383870573495 ) ) ;
#9780=CARTESIAN_POINT ( 'NONE',  ( 113.8740681442453138, 0.5811942927096154232, -14.16772938898807155 ) ) ;
#9781=CARTESIAN_POINT ( 'NONE',  ( 117.9016614775786280, -0.1624402480850797581, -16.17319339645315424 ) ) ;
#9783=CARTESIAN_POINT ( 'NONE',  ( 116.0506660444391969, -1.267766418764730840, -16.93314635290706605 ) ) ;
#9784=CARTESIAN_POINT ( 'NONE',  ( 122.6667014775786413, -7.893985811506177619, -18.51759400769804742 ) ) ;
#9785=CARTESIAN_POINT ( 'NONE',  ( 120.0005481442453146, -5.638512984488999180, -18.83840828888717311 ) ) ;
#9790=CARTESIAN_POINT ( 'NONE',  ( 114.3846081442453197, 0.4262465694468514643, -12.03445270309931736 ) ) ;
#9791=CARTESIAN_POINT ( 'NONE',  ( 124.8790414775786246, -8.899110576539426276, -16.42337572283528146 ) ) ;
#9794=CARTESIAN_POINT ( 'NONE',  ( 118.3554748109119998, 0.2603800115204892296, -16.42320221600525088 ) ) ;
#9795=CARTESIAN_POINT ( 'NONE',  ( 126.3063647503470719, -5.222031867898532909, -18.42446631453262285 ) ) ;
#9796=CARTESIAN_POINT ( 'NONE',  ( 113.9307948109119906, 0.9020085738987339008, -11.91225656197089222 ) ) ;
#9798=CARTESIAN_POINT ( 'NONE',  ( 121.4754414775786131, -8.166667518702819706, -8.995218007635861213 ) ) ;
#9801=CARTESIAN_POINT ( 'NONE',  ( 112.3991748109119868, -1.833838273342658809, -17.42832698103878286 ) ) ;
#9802=CARTESIAN_POINT ( 'NONE',  ( 125.1269327111056953, -1.267766418764818770, -16.93314635290698078 ) ) ;
#9804=CARTESIAN_POINT ( 'NONE',  ( 116.0296814775786345, -1.833838273342658809, -17.42832698103878286 ) ) ;
#9806=CARTESIAN_POINT ( 'NONE',  ( 118.9227414775786542, 0.4262465694468514643, -12.03445270309931736 ) ) ;
#9808=LINE ( 'NONE', #23717, #36850 ) ;
#9809=CARTESIAN_POINT ( 'NONE',  ( 114.4413348109119823, -0.8288870151387760510, -10.36305467784173118 ) ) ;
#9810=CARTESIAN_POINT ( 'NONE',  ( 115.2355081442453155, -10.30919188438810075, -12.61870101168855918 ) ) ;
#9812=CARTESIAN_POINT ( 'NONE',  ( 111.9453614775786434, -1.561330072975668060, -17.79121239304076596 ) ) ;
#9813=CARTESIAN_POINT ( 'NONE',  ( 116.4834948109119779, -7.894159318335828068, -9.358103419637847864 ) ) ;
#9814=CARTESIAN_POINT ( 'NONE',  ( 112.6260814775786514, -0.8288870151387760510, -10.36305467784173118 ) ) ;
#9815=CARTESIAN_POINT ( 'NONE',  ( 118.3554748109119998, -9.565557343593413364, -10.61323700422348004 ) ) ;
#9817=CARTESIAN_POINT ( 'NONE',  ( 113.7038881442453402, -3.383040157471821630, -19.15922257007629170 ) ) ;
#9822=CARTESIAN_POINT ( 'NONE',  ( 118.4122014775786340, 0.5811942927096110934, -14.16772938898807510 ) ) ;
#9824=CARTESIAN_POINT ( 'NONE',  ( 124.8223148109119762, 0.9020085738987339008, -11.91225656197089222 ) ) ;
#9826=CARTESIAN_POINT ( 'NONE',  ( 118.7525614775786380, -1.833838273342659253, -17.42832698103878286 ) ) ;
#9829=CARTESIAN_POINT ( 'NONE',  ( 124.5954081442453116, -3.383040157471821630, -19.15922257007629170 ) ) ;
#9834=CARTESIAN_POINT ( 'NONE',  ( 124.3117748109119844, 0.1319031606808879209, -14.10382304977623669 ) ) ;
#9835=CARTESIAN_POINT ( 'NONE',  ( 118.5823814775786360, -1.834011780172310813, -8.268836392978581529 ) ) ;
#9836=CARTESIAN_POINT ( 'NONE',  ( 113.8173414775786512, -9.565557343593413364, -10.61323700422348004 ) ) ;
#9837=CARTESIAN_POINT ( 'NONE',  ( 119.2631014775786298, 0.2603800115204892296, -16.42320221600525088 ) ) ;
#9839=CARTESIAN_POINT ( 'NONE',  ( 126.5254139958947519, -1.171961747752007899, -9.797753127676378071 ) ) ;
#9840=CARTESIAN_POINT ( 'NONE',  ( 124.7088614775786226, -9.565557343593413364, -10.61323700422348004 ) ) ;
#9846=CARTESIAN_POINT ( 'NONE',  ( 117.2209414775786485, -7.893985811506177619, -18.51759400769804742 ) ) ;
#9847=CARTESIAN_POINT ( 'NONE',  ( 120.4543614775786295, -5.574606645277164318, -18.38911715685844683 ) ) ;
#9850=CARTESIAN_POINT ( 'NONE',  ( 135.3184548109119874, -1.191816558809784876, -8.648209655763537285 ) ) ;
#9851=CARTESIAN_POINT ( 'NONE',  ( 117.6747548109119919, -1.834011780172310813, -8.268836392978581529 ) ) ;
#9854=CARTESIAN_POINT ( 'NONE',  ( 117.9016614775786280, -0.1624402480850797581, -16.17319339645315424 ) ) ;
#9857=CARTESIAN_POINT ( 'NONE',  ( 126.3539348109119800, -4.153390946401325223, -8.397313243818185668 ) ) ;
#9858=CARTESIAN_POINT ( 'NONE',  ( 122.9503348109119827, -9.859900752359378018, -12.68260735090039759 ) ) ;
#9861=CARTESIAN_POINT ( 'NONE',  ( 123.5176014775786228, -9.261995988541697145, -16.69588392320189030 ) ) ;
#9864=CARTESIAN_POINT ( 'NONE',  ( 121.7023481442452777, -9.261995988541697145, -16.69588392320189030 ) ) ;
#9865=CARTESIAN_POINT ( 'NONE',  ( 119.7169148109119874, -9.988377603198976828, -10.36322818467138340 ) ) ;
#9866=CARTESIAN_POINT ( 'NONE',  ( 118.2987481442453088, -7.894159318335828068, -9.358103419637847864 ) ) ;
#9867=CARTESIAN_POINT ( 'NONE',  ( 123.9146881442452894, -10.15424416112533912, -14.75197769757731336 ) ) ;
#9868=CARTESIAN_POINT ( 'NONE',  ( 112.6260814775786514, -9.261995988541697145, -16.69588392320189030 ) ) ;
#9870=CARTESIAN_POINT ( 'NONE',  ( 122.6667014775786413, -2.084020599724406786, -8.691656652584148546 ) ) ;
#9871=CARTESIAN_POINT ( 'NONE',  ( 123.1205148109119563, -1.834011780172307704, -8.268836392978586858 ) ) ;
#9872=FACE_OUTER_BOUND ( 'NONE', #10047, .T. ) ;
#9877=CARTESIAN_POINT ( 'NONE',  ( 123.7445081442452874, -1.561330072975668948, -17.79121239304076951 ) ) ;
#9878=CARTESIAN_POINT ( 'NONE',  ( 123.2339681442453241, -3.505236298600246325, -18.68346056562440793 ) ) ;
#9880=CARTESIAN_POINT ( 'NONE',  ( 125.7299414775786346, 0.9020085738987339008, -11.91225656197089222 ) ) ;
#9881=CARTESIAN_POINT ( 'NONE',  ( 113.5904348109119866, -2.084020599724406786, -8.691656652584148546 ) ) ;
#9882=CARTESIAN_POINT ( 'NONE',  ( 121.9292548109119849, -7.894159318335831621, -9.358103419637851417 ) ) ;
#9883=CARTESIAN_POINT ( 'NONE',  ( 118.6958348109119754, -6.344957434206665248, -7.627207830600338134 ) ) ;
#9884=CARTESIAN_POINT ( 'NONE',  ( 121.3052614775786111, -1.834011780172310813, -8.268836392978581529 ) ) ;
#9887=CARTESIAN_POINT ( 'NONE',  ( 126.2404814775786264, -0.8288870151387760510, -10.36305467784173118 ) ) ;
#9892=CARTESIAN_POINT ( 'NONE',  ( 112.5126281442453120, 0.1319031606808879209, -14.10382304977623669 ) ) ;
#9893=CARTESIAN_POINT ( 'NONE',  ( 125.3895814775786448, -2.084020599724406786, -8.691656652584148546 ) ) ;
#9896=CARTESIAN_POINT ( 'NONE',  ( 122.5532481442453019, 0.4262465694468514643, -12.03445270309931736 ) ) ;
#9898=CARTESIAN_POINT ( 'NONE',  ( 116.8805814775786445, -3.505236298600246325, -18.68346056562440793 ) ) ;
#9899=CARTESIAN_POINT ( 'NONE',  ( 121.8725281442453223, -3.383040157471821630, -19.15922257007629170 ) ) ;
#9901=CARTESIAN_POINT ( 'NONE',  ( 121.3052614775786111, -7.643976991954077427, -18.09477374809248928 ) ) ;
#9902=CARTESIAN_POINT ( 'NONE',  ( 118.0151148109119816, -10.63000616557722466, -14.87417383870573495 ) ) ;
#9903=CARTESIAN_POINT ( 'NONE',  ( 124.0848681442452772, -4.089484607189486809, -7.948022111789456723 ) ) ;
#9905=CARTESIAN_POINT ( 'NONE',  ( 123.2906948109119867, -1.833838273342659697, -17.42832698103878286 ) ) ;
#9909=CARTESIAN_POINT ( 'NONE',  ( 122.2696148109119889, -4.089484607189486809, -7.948022111789456723 ) ) ;
#9910=CARTESIAN_POINT ( 'NONE',  ( 115.5191414775786569, -6.222761293078241884, -8.102969835052219238 ) ) ;
#9911=CARTESIAN_POINT ( 'NONE',  ( 112.9097148109120070, -9.565557343593413364, -10.61323700422348004 ) ) ;
#9912=DIRECTION ( 'NONE',  ( 2.478482478837576011E-29, 0.6004852223389939292, -0.7996358532185066093 ) ) ;
#9914=EDGE_LOOP ( 'NONE', ( #30288, #15330, #1190, #2309, #30814 ) ) ;
#9919=CARTESIAN_POINT ( 'NONE',  ( 124.2550481442452792, -0.1624402480850797581, -16.17319339645315424 ) ) ;
#9920=CARTESIAN_POINT ( 'NONE',  ( 114.0442481442453300, -7.643976991954077427, -18.09477374809248928 ) ) ;
#9921=CARTESIAN_POINT ( 'NONE',  ( 127.3665996190938046, -6.875750515655262518, -18.59280027438719429 ) ) ;
#9922=ORIENTED_EDGE ( 'NONE', *, *, #8010, .F. ) ;
#9924=CARTESIAN_POINT ( 'NONE',  ( 114.3278814775786429, 0.1319031606808879209, -14.10382304977623669 ) ) ;
#9926=CARTESIAN_POINT ( 'NONE',  ( 111.5588148109119828, 0.08617673920517221475, -14.09731900820172967 ) ) ;
#9928=CARTESIAN_POINT ( 'NONE',  ( 125.3895814775786448, -7.893985811506177619, -18.51759400769804742 ) ) ;
#9930=CARTESIAN_POINT ( 'NONE',  ( 126.5241148109119393, -9.565557343593413364, -10.61323700422348004 ) ) ;
#9932=CARTESIAN_POINT ( 'NONE',  ( 112.2857214775786474, -4.089484607189486809, -7.948022111789456723 ) ) ;
#9933=CARTESIAN_POINT ( 'NONE',  ( 113.7406697909088393, -1.016270020561755860, -17.26805140881366896 ) ) ;
#9935=CARTESIAN_POINT ( 'NONE',  ( 124.4252281442452812, -0.8288870151387760510, -10.36305467784173118 ) ) ;
#9936=CARTESIAN_POINT ( 'NONE',  ( 124.0281414775786146, -7.643976991954077427, -18.09477374809248928 ) ) ;
#9942=CARTESIAN_POINT ( 'NONE',  ( 113.9307948109119764, -10.15424416112533912, -14.75197769757731336 ) ) ;
#9944=CARTESIAN_POINT ( 'NONE',  ( 111.7184544661070333, -9.250647026409817286, -16.71020059006274039 ) ) ;
#9947=CARTESIAN_POINT ( 'NONE',  ( 120.3409081442453044, -0.4660016031367893996, -10.09054647747474043 ) ) ;
#9948=CARTESIAN_POINT ( 'NONE',  ( 127.7184548109119788, -4.863998795839242995, -13.39321520033831447 ) ) ;
#9949=CARTESIAN_POINT ( 'NONE',  ( 120.0005481442453146, -5.638512984488999180, -18.83840828888717311 ) ) ;
#9952=CARTESIAN_POINT ( 'NONE',  ( 112.5693548109119888, 0.4262465694468514643, -12.03445270309931736 ) ) ;
#9954=CARTESIAN_POINT ( 'NONE',  ( 125.0492214775786266, -6.344957434206665248, -7.627207830600338134 ) ) ;
#9955=CARTESIAN_POINT ( 'NONE',  ( 124.5386814775786206, -5.638512984488999180, -18.83840828888717311 ) ) ;
#9956=CARTESIAN_POINT ( 'NONE',  ( 114.4980614775786592, -7.893985811506177619, -18.51759400769804742 ) ) ;
#9957=CARTESIAN_POINT ( 'NONE',  ( 111.7751814775786556, -2.084020599724406786, -8.691656652584148546 ) ) ;
#9959=CARTESIAN_POINT ( 'NONE',  ( 118.5823814775786360, -7.643976991954077427, -18.09477374809248928 ) ) ;
#9960=B_SPLINE_CURVE_WITH_KNOTS ( 'NONE', 3,
 ( #41133, #26761, #34036, #6465, #12860, #13534, #44775, #30178, #13083, #40902 ),
 .UNSPECIFIED., .F., .F.,
 ( 4, 3, 3, 4 ),
 ( 0.000000000000000000, 0.0001671877548681284921, 0.0003343755096277660228, 0.0006463528481650619413 ),
 .UNSPECIFIED. ) ;
#9961=CARTESIAN_POINT ( 'NONE',  ( 113.2500748109119968, -6.344957434206662583, -7.627207830600332805 ) ) ;
#9962=CARTESIAN_POINT ( 'NONE',  ( 123.2906948109119867, -1.833838273342659697, -17.42832698103878286 ) ) ;
#9965=B_SPLINE_CURVE_WITH_KNOTS ( 'NONE', 3,
 ( #45025, #13783, #37946, #10367, #38163, #6719, #27695, #24275, #34938, #34724 ),
 .UNSPECIFIED., .F., .F.,
 ( 4, 3, 3, 4 ),
 ( 0.000000000000000000, 0.0001671877560958085049, 0.0003343755126086545080, 0.0006438490228505469159 ),
 .UNSPECIFIED. ) ;
#9969=EDGE_CURVE ( 'NONE', #19203, #1246, #35603, .T. ) ;
#9970=CARTESIAN_POINT ( 'NONE',  ( 124.9924948109119924, -4.089484607189486809, -7.948022111789456723 ) ) ;
#9977=CARTESIAN_POINT ( 'NONE',  ( 117.6747548109119919, -1.834011780172310813, -8.268836392978581529 ) ) ;
#9979=CARTESIAN_POINT ( 'NONE',  ( 125.1309504620138284, -2.495269033102075262, -17.79652296963211455 ) ) ;
#9981=CARTESIAN_POINT ( 'NONE',  ( 120.5678148109119832, -1.833838273342659253, -17.42832698103878286 ) ) ;
#9985=CARTESIAN_POINT ( 'NONE',  ( 119.3198281442452924, 0.5811942927096110934, -14.16772938898807510 ) ) ;
#9987=CARTESIAN_POINT ( 'NONE',  ( 115.2922348109119781, 0.4262465694468514643, -12.03445270309931736 ) ) ;
#9990=CARTESIAN_POINT ( 'NONE',  ( 113.0231681442453180, -10.15424416112533912, -14.75197769757731336 ) ) ;
#9994=CARTESIAN_POINT ( 'NONE',  ( 117.9016614775786280, -0.1624402480850797581, -16.17319339645315424 ) ) ;
#9995=CARTESIAN_POINT ( 'NONE',  ( 119.6601881442453106, -1.833838273342659253, -17.42832698103878286 ) ) ;
#10001=CARTESIAN_POINT ( 'NONE',  ( 113.3068014775786594, -8.166667518702817929, -8.995218007635859436 ) ) ;
#10002=CARTESIAN_POINT ( 'NONE',  ( 123.1973327483929097, -2.423081321603731908, -17.89265170041263175 ) ) ;
#10009=CARTESIAN_POINT ( 'NONE',  ( 123.5743281442453139, -7.893985811506177619, -18.51759400769804742 ) ) ;
#10010=CARTESIAN_POINT ( 'NONE',  ( 126.6375681442452930, -10.15424416112533912, -14.75197769757731336 ) ) ;
#10011=CARTESIAN_POINT ( 'NONE',  ( 118.8092881442453290, -0.1624402480850797581, -16.17319339645315424 ) ) ;
#10014=CARTESIAN_POINT ( 'NONE',  ( 122.4397948109119767, -9.988377603198976828, -10.36322818467138340 ) ) ;
#10015=CARTESIAN_POINT ( 'NONE',  ( 116.5969481442453031, 0.5811942927096154232, -14.16772938898807155 ) ) ;
#10019=CARTESIAN_POINT ( 'NONE',  ( 113.3635281442453504, -0.1624402480850797581, -16.17319339645315424 ) ) ;
#10022=CARTESIAN_POINT ( 'NONE',  ( 116.7104014775786425, -0.4660016031367893996, -10.09054647747474043 ) ) ;
#10026=CARTESIAN_POINT ( 'NONE',  ( 116.8238548109119819, -4.089484607189486809, -7.948022111789456723 ) ) ;
#10033=CARTESIAN_POINT ( 'NONE',  ( 115.4056881442453459, -2.084020599724406786, -8.691656652584148546 ) ) ;
#10035=CARTESIAN_POINT ( 'NONE',  ( 118.8660148109119774, 0.1319031606808879209, -14.10382304977623669 ) ) ;
#10037=CARTESIAN_POINT ( 'NONE',  ( 116.2565881442453133, -0.8288870151387760510, -10.36305467784173118 ) ) ;
#10038=ADVANCED_FACE ( 'NONE', ( #26368 ), #12996, .T. ) ;
#10039=CARTESIAN_POINT ( 'NONE',  ( 113.8740681442453138, 0.5811942927096154232, -14.16772938898807155 ) ) ;
#10041=CARTESIAN_POINT ( 'NONE',  ( 115.1787814775786387, -9.988377603198976828, -10.36322818467138340 ) ) ;
#10042=CARTESIAN_POINT ( 'NONE',  ( 112.7962614775786676, -6.222761293078241884, -8.102969835052219238 ) ) ;
#10046=CARTESIAN_POINT ( 'NONE',  ( 117.7314814775786260, -5.574606645277164318, -18.38911715685844683 ) ) ;
#10047=EDGE_LOOP ( 'NONE', ( #34292, #25587, #15430, #22526, #39555 ) ) ;
#10048=CARTESIAN_POINT ( 'NONE',  ( 112.9097148109120070, 0.2603800115204892296, -16.42320221600525088 ) ) ;
#10054=CARTESIAN_POINT ( 'NONE',  ( 117.6180281442453150, -0.4660016031367893996, -10.09054647747474043 ) ) ;
#10056=PLANE ( 'NONE',  #17599 ) ;
#10057=CARTESIAN_POINT ( 'NONE',  ( 119.3198281442452924, -9.859900752359374465, -12.68260735090039404 ) ) ;
#10059=CARTESIAN_POINT ( 'NONE',  ( 122.3830681442452857, -8.166667518702819706, -8.995218007635861213 ) ) ;
#10063=CARTESIAN_POINT ( 'NONE',  ( 112.0020881442453344, 0.2603800115204892296, -16.42320221600525088 ) ) ;
#10064=CARTESIAN_POINT ( 'NONE',  ( 121.1350814775786233, -9.859900752359378018, -12.68260735090039759 ) ) ;
#10065=CARTESIAN_POINT ( 'NONE',  ( 125.1626748109119802, -9.988377603198980381, -10.36322818467138518 ) ) ;
#10067=CARTESIAN_POINT ( 'NONE',  ( 118.5256548109119876, -8.899110576539710493, -16.42337572283490132 ) ) ;
#10069=CARTESIAN_POINT ( 'NONE',  ( 120.1140014775786398, -1.561330072975668504, -17.79121239304076951 ) ) ;
#10071=CARTESIAN_POINT ( 'NONE',  ( 126.5561942423832420, -1.182158702725811805, -9.765297139248401592 ) ) ;
#10072=CARTESIAN_POINT ( 'NONE',  ( 122.2128881442453263, -7.643976991954077427, -18.09477374809248928 ) ) ;
#10073=ORIENTED_EDGE ( 'NONE', *, *, #12505, .F. ) ;
#10075=CARTESIAN_POINT ( 'NONE',  ( 116.9373081442452929, -8.166667518702817929, -8.995218007635861213 ) ) ;
#10076=CARTESIAN_POINT ( 'NONE',  ( 125.5030348109119558, -6.222761293078241884, -8.102969835052219238 ) ) ;
#10080=CARTESIAN_POINT ( 'NONE',  ( 123.5743281442453139, -7.893985811506177619, -18.51759400769804742 ) ) ;
#10082=CARTESIAN_POINT ( 'NONE',  ( 118.6958348109119754, -3.505236298600246325, -18.68346056562440793 ) ) ;
#10085=CARTESIAN_POINT ( 'NONE',  ( 112.2857214775786474, -4.089484607189486809, -7.948022111789456723 ) ) ;
#10086=CARTESIAN_POINT ( 'NONE',  ( 124.7655881442452852, -9.859900752359378018, -12.68260735090039759 ) ) ;
#10090=CARTESIAN_POINT ( 'NONE',  ( 120.6245414775786458, -9.988377603198976828, -10.36322818467138340 ) ) ;
#10094=CARTESIAN_POINT ( 'NONE',  ( 120.0005481442453146, -5.638512984488999180, -18.83840828888717311 ) ) ;
#10095=CARTESIAN_POINT ( 'NONE',  ( 119.4900081442453086, -1.834011780172310813, -8.268836392978581529 ) ) ;
#10096=CARTESIAN_POINT ( 'NONE',  ( 121.2485348109119769, -8.899110576539710493, -16.42337572283490132 ) ) ;
#10097=CARTESIAN_POINT ( 'NONE',  ( 123.5176014775786228, -0.8288870151387760510, -10.36305467784173118 ) ) ;
#10098=CARTESIAN_POINT ( 'NONE',  ( 115.4056881442453459, -7.893985811506177619, -18.51759400769804742 ) ) ;
#10100=CARTESIAN_POINT ( 'NONE',  ( 125.9001214775786224, -5.574606645277164318, -18.38911715685844683 ) ) ;
#10105=CARTESIAN_POINT ( 'NONE',  ( 121.9859814775786333, 0.2603800115204892296, -16.42320221600525088 ) ) ;
#10106=CARTESIAN_POINT ( 'NONE',  ( 123.0070614775786169, -10.15424416112533912, -14.75197769757731336 ) ) ;
#10108=CARTESIAN_POINT ( 'NONE',  ( 124.4819548109119722, -7.893985811506177619, -18.51759400769804742 ) ) ;
#10112=CARTESIAN_POINT ( 'NONE',  ( 123.5743281442453139, -7.893985811506177619, -18.51759400769804742 ) ) ;
#10113=CARTESIAN_POINT ( 'NONE',  ( 122.0994348109119443, 0.9020085738987339008, -11.91225656197089222 ) ) ;
#10115=CARTESIAN_POINT ( 'NONE',  ( 126.4673881442452910, -7.894159318335828068, -9.358103419637847864 ) ) ;
#10121=CARTESIAN_POINT ( 'NONE',  ( 125.3328548109119964, -0.8288870151387760510, -10.36305467784173118 ) ) ;
#10124=CARTESIAN_POINT ( 'NONE',  ( 122.4397948109119767, -0.1624402480850797581, -16.17319339645315424 ) ) ;
#10125=CARTESIAN_POINT ( 'NONE',  ( 116.0864081442453113, -0.1624402480850797581, -16.17319339645315424 ) ) ;
#10126=CARTESIAN_POINT ( 'NONE',  ( 112.0020881442453344, -9.565557343593413364, -10.61323700422348004 ) ) ;
#10128=CARTESIAN_POINT ( 'NONE',  ( 125.3895814775786448, -2.084020599724406786, -8.691656652584148546 ) ) ;
#10129=CARTESIAN_POINT ( 'NONE',  ( 117.0507614775786465, -10.30919188438810075, -12.61870101168855918 ) ) ;
#10130=VECTOR ( 'NONE', #37797, 1000.000000000000000 ) ;
#10132=ORIENTED_EDGE ( 'NONE', *, *, #778, .T. ) ;
#10135=CARTESIAN_POINT ( 'NONE',  ( 115.4624148109119943, -4.153390946401321671, -8.397313243818183892 ) ) ;
#10136=CARTESIAN_POINT ( 'NONE',  ( 114.6115148109119986, -6.222761293078241884, -8.102969835052219238 ) ) ;
#10142=CARTESIAN_POINT ( 'NONE',  ( 121.4187148109119789, -3.505236298600246325, -18.68346056562440793 ) ) ;
#10143=CARTESIAN_POINT ( 'NONE',  ( 114.4413348109119823, -0.8288870151387760510, -10.36305467784173118 ) ) ;
#10146=CARTESIAN_POINT ( 'NONE',  ( 126.8848622761261993, -2.292895460366377591, -18.06601363898300860 ) ) ;
#10152=EDGE_CURVE ( 'NONE', #3839, #41752, #21823, .T. ) ;
#10154=CARTESIAN_POINT ( 'NONE',  ( 124.7088614775786226, -9.565557343593413364, -10.61323700422348004 ) ) ;
#10156=CARTESIAN_POINT ( 'NONE',  ( 113.0231681442453322, 0.9020085738987339008, -11.91225656197089222 ) ) ;
#10158=CARTESIAN_POINT ( 'NONE',  ( 113.5841162859069016, -1.111561923218668646, -17.14115599315433869 ) ) ;
#10160=CARTESIAN_POINT ( 'NONE',  ( 126.0703014775786102, -0.1624402480850797581, -16.17319339645315424 ) ) ;
#10161=CARTESIAN_POINT ( 'NONE',  ( 123.1772414775786189, -5.574606645277164318, -18.38911715685844683 ) ) ;
#10165=DIRECTION ( 'NONE',  ( 1.000000000000000000, 0.000000000000000000, 0.000000000000000000 ) ) ;
#10166=CARTESIAN_POINT ( 'NONE',  ( 113.7606148109119886, -7.894159318335828068, -9.358103419637847864 ) ) ;
#10168=CARTESIAN_POINT ( 'NONE',  ( 128.2184548109119930, -4.863998795839242995, -13.39321520033831447 ) ) ;
#10170=CARTESIAN_POINT ( 'NONE',  ( 126.0135748109119902, -8.166667518702819706, -8.995218007635861213 ) ) ;
#10171=CARTESIAN_POINT ( 'NONE',  ( 124.2550481442452792, -9.988377603198980381, -10.36322818467138518 ) ) ;
#10174=CARTESIAN_POINT ( 'NONE',  ( 119.5467348109119712, -4.089484607189486809, -7.948022111789456723 ) ) ;
#10175=CARTESIAN_POINT ( 'NONE',  ( 117.1642148109119859, -9.261995988541697145, -16.69588392320189030 ) ) ;
#10177=CARTESIAN_POINT ( 'NONE',  ( 111.8319081442453182, -4.153390946401321671, -8.397313243818183892 ) ) ;
#10178=CARTESIAN_POINT ( 'NONE',  ( 124.3685014775786328, -10.63000616557722466, -14.87417383870573495 ) ) ;
#10179=CARTESIAN_POINT ( 'NONE',  ( 113.7606148109119886, -1.561330072975668060, -17.79121239304076596 ) ) ;
#10181=CARTESIAN_POINT ( 'NONE',  ( 115.8027748109119841, -8.899110576539710493, -16.42337572283490132 ) ) ;
#10183=CARTESIAN_POINT ( 'NONE',  ( 117.5613014775786525, -10.15424416112533912, -14.75197769757731336 ) ) ;
#10184=CARTESIAN_POINT ( 'NONE',  ( 116.0864081442453113, -9.988377603198976828, -10.36322818467138340 ) ) ;
#10186=CARTESIAN_POINT ( 'NONE',  ( 121.9292548109119849, -7.894159318335828068, -9.358103419637847864 ) ) ;
#10191=CARTESIAN_POINT ( 'NONE',  ( 124.8223148109119762, 0.9020085738987339008, -11.91225656197089222 ) ) ;
#10193=B_SPLINE_CURVE_WITH_KNOTS ( 'NONE', 3,
 ( #43677, #18829, #26353, #40261, #4914, #19732, #22925, #30224, #43911, #36596 ),
 .UNSPECIFIED., .F., .F.,
 ( 4, 3, 3, 4 ),
 ( 8.673617379884039324E-19, 0.0001671877548681299829, 0.0003343755096277710101, 0.0006463528481650640013 ),
 .UNSPECIFIED. ) ;
#10196=CARTESIAN_POINT ( 'NONE',  ( 112.9664414775786412, -9.859900752359374465, -12.68260735090039404 ) ) ;
#10199=CARTESIAN_POINT ( 'NONE',  ( 117.4478481442453131, 0.2603800115204892296, -16.42320221600525088 ) ) ;
#10203=CARTESIAN_POINT ( 'NONE',  ( 120.6812681442452941, 0.1319031606808879209, -14.10382304977623669 ) ) ;
#10205=CARTESIAN_POINT ( 'NONE',  ( 125.2761281442453054, -10.63000616557722466, -14.87417383870573495 ) ) ;
#10206=CARTESIAN_POINT ( 'NONE',  ( 119.4900081442453086, -1.834011780172310813, -8.268836392978581529 ) ) ;
#10208=CARTESIAN_POINT ( 'NONE',  ( 114.1009748109119784, -5.574606645277164318, -18.38911715685844683 ) ) ;
#10209=CARTESIAN_POINT ( 'NONE',  ( 111.3780948109119890, -5.574606645277164318, -18.38911715685844683 ) ) ;
#10213=CARTESIAN_POINT ( 'NONE',  ( 117.3343948109119737, -6.222761293078241884, -8.102969835052219238 ) ) ;
#10214=CARTESIAN_POINT ( 'NONE',  ( 120.3976348109119812, -7.643976991954077427, -18.09477374809248928 ) ) ;
#10219=CARTESIAN_POINT ( 'NONE',  ( 123.9714148109119805, -8.899110576539726480, -16.42337572283488001 ) ) ;
#10220=CARTESIAN_POINT ( 'NONE',  ( 114.3846081442453197, -10.63000616557722466, -14.87417383870573495 ) ) ;
#10221=CARTESIAN_POINT ( 'NONE',  ( 113.9307948109119906, 0.9020085738987339008, -11.91225656197089222 ) ) ;
#10224=VERTEX_POINT ( 'NONE', #1605 ) ;
#10227=CARTESIAN_POINT ( 'NONE',  ( 122.0427081442452817, 0.5811942927096110934, -14.16772938898807510 ) ) ;
#10229=CARTESIAN_POINT ( 'NONE',  ( 113.6471614775786492, -5.638512984488999180, -18.83840828888717311 ) ) ;
#10230=CARTESIAN_POINT ( 'NONE',  ( 119.8303681442453126, 0.4262465694468514643, -12.03445270309931736 ) ) ;
#10233=CARTESIAN_POINT ( 'NONE',  ( 121.4187148109119789, -6.344957434206665248, -7.627207830600338134 ) ) ;
#10234=CARTESIAN_POINT ( 'NONE',  ( 117.9016614775786280, -9.988377603198976828, -10.36322818467138340 ) ) ;
#10236=CARTESIAN_POINT ( 'NONE',  ( 126.0135748109119902, -8.166667518702819706, -8.995218007635861213 ) ) ;
#10237=CARTESIAN_POINT ( 'NONE',  ( 135.3184548109119874, -4.863998795839242995, -13.39321520033831447 ) ) ;
#10239=CARTESIAN_POINT ( 'NONE',  ( 117.4478481442453131, 0.2603800115204892296, -16.42320221600525088 ) ) ;
#10242=CARTESIAN_POINT ( 'NONE',  ( 115.4056881442453459, -7.893985811506177619, -18.51759400769804742 ) ) ;
#10245=CARTESIAN_POINT ( 'NONE',  ( 125.6164881442453094, 0.2603800115204892296, -16.42320221600525088 ) ) ;
#10248=CARTESIAN_POINT ( 'NONE',  ( 112.2857214775786474, -5.574606645277164318, -18.38911715685844683 ) ) ;
#10250=CARTESIAN_POINT ( 'NONE',  ( 115.6893214775786447, -9.859900752359374465, -12.68260735090039404 ) ) ;
#10252=CARTESIAN_POINT ( 'NONE',  ( 116.5969481442453031, -9.859900752359374465, -12.68260735090039404 ) ) ;
#10255=CARTESIAN_POINT ( 'NONE',  ( 116.9373081442452929, -1.833838273342659253, -17.42832698103878286 ) ) ;
#10257=CARTESIAN_POINT ( 'NONE',  ( 115.6325948109119821, 0.2603800115204892296, -16.42320221600525088 ) ) ;
#10258=CARTESIAN_POINT ( 'NONE',  ( 111.8319081442453182, -4.153390946401321671, -8.397313243818183892 ) ) ;
#10259=CARTESIAN_POINT ( 'NONE',  ( 116.7671281442453335, -7.643976991954077427, -18.09477374809248928 ) ) ;
#10261=CARTESIAN_POINT ( 'NONE',  ( 116.4267681442453153, -3.383040157471821630, -19.15922257007629170 ) ) ;
#10267=CARTESIAN_POINT ( 'NONE',  ( 121.1918081442452859, 0.9020085738987339008, -11.91225656197089222 ) ) ;
#10268=ORIENTED_EDGE ( 'NONE', *, *, #6757, .T. ) ;
#10270=CARTESIAN_POINT ( 'NONE',  ( 116.8238548109119819, -5.574606645277164318, -18.38911715685844683 ) ) ;
#10271=ADVANCED_FACE ( 'NONE', ( #4132 ), #3653, .T. ) ;
#10273=CARTESIAN_POINT ( 'NONE',  ( 121.9859814775786333, 0.2603800115204892296, -16.42320221600525088 ) ) ;
#10276=CARTESIAN_POINT ( 'NONE',  ( 124.4756362859068872, -1.111561923218658210, -17.14115599315433158 ) ) ;
#10279=CARTESIAN_POINT ( 'NONE',  ( 125.5030348109119558, -6.222761293078241884, -8.102969835052219238 ) ) ;
#10280=CARTESIAN_POINT ( 'NONE',  ( 124.3117748109119844, -10.30919188438810075, -12.61870101168855918 ) ) ;
#10282=CARTESIAN_POINT ( 'NONE',  ( 118.1852948109119836, -4.153390946401325223, -8.397313243818185668 ) ) ;
#10284=CARTESIAN_POINT ( 'NONE',  ( 120.6812681442452941, -10.30919188438810075, -12.61870101168855918 ) ) ;
#10286=CARTESIAN_POINT ( 'NONE',  ( 121.2485348109119769, -8.899110576539710493, -16.42337572283490132 ) ) ;
#10290=CARTESIAN_POINT ( 'NONE',  ( 115.4624148109119943, -5.638512984488999180, -18.83840828888717311 ) ) ;
#10291=CARTESIAN_POINT ( 'NONE',  ( 125.6732148109119862, -9.859900752359378018, -12.68260735090039759 ) ) ;
#10297=CARTESIAN_POINT ( 'NONE',  ( 137.1399781294065576, -1.251936845180553481, -9.436198808430885876 ) ) ;
#10300=CARTESIAN_POINT ( 'NONE',  ( 121.7023481442452777, -9.261995988541697145, -16.69588392320189030 ) ) ;
#10302=CARTESIAN_POINT ( 'NONE',  ( 120.0572748109119772, -6.222761293078241884, -8.102969835052219238 ) ) ;
#10303=VERTEX_POINT ( 'NONE', #24730 ) ;
#10305=CARTESIAN_POINT ( 'NONE',  ( 114.5547881442453217, -5.638512984488999180, -18.83840828888717311 ) ) ;
#10306=CARTESIAN_POINT ( 'NONE',  ( 124.8790414775786246, -8.899110576539710493, -16.42337572283490132 ) ) ;
#10309=CARTESIAN_POINT ( 'NONE',  ( 123.5743281442453139, -7.893985811506177619, -18.51759400769804742 ) ) ;
#10312=CARTESIAN_POINT ( 'NONE',  ( 119.6601881442453106, -8.166667518702819706, -8.995218007635861213 ) ) ;
#10313=CARTESIAN_POINT ( 'NONE',  ( 119.3765548109119834, 0.9020085738987339008, -11.91225656197089222 ) ) ;
#10314=CARTESIAN_POINT ( 'NONE',  ( 120.9649014775786355, -6.222761293078241884, -8.102969835052219238 ) ) ;
#10316=CARTESIAN_POINT ( 'NONE',  ( 117.7882081442453170, -6.344957434206665248, -7.627207830600338134 ) ) ;
#10318=CARTESIAN_POINT ( 'NONE',  ( 125.4463081442452932, -4.153390946401325223, -8.397313243818185668 ) ) ;
#10324=DIRECTION ( 'NONE',  ( -1.000000000000000000, 0.000000000000000000, 0.000000000000000000 ) ) ;
#10325=CARTESIAN_POINT ( 'NONE',  ( 113.1366214775786432, -1.834011780172310813, -8.268836392978581529 ) ) ;
#10327=CARTESIAN_POINT ( 'NONE',  ( 124.7088614775786226, 0.2603800115204892296, -16.42320221600525088 ) ) ;
#10330=CARTESIAN_POINT ( 'NONE',  ( 122.3830681442452857, -8.166667518702819706, -8.995218007635861213 ) ) ;
#10331=CARTESIAN_POINT ( 'NONE',  ( 124.2550481442452792, -9.988377603198980381, -10.36322818467138518 ) ) ;
#10333=CARTESIAN_POINT ( 'NONE',  ( 126.1837548109119496, 0.4262465694468514643, -12.03445270309931736 ) ) ;
#10338=CARTESIAN_POINT ( 'NONE',  ( 115.1787814775786387, -0.1624402480850797581, -16.17319339645315424 ) ) ;
#10339=CARTESIAN_POINT ( 'NONE',  ( 113.4202548109119846, -10.30919188438810075, -12.61870101168855918 ) ) ;
#10342=CARTESIAN_POINT ( 'NONE',  ( 121.0216281442452981, -7.894159318335828068, -9.358103419637847864 ) ) ;
#10343=CARTESIAN_POINT ( 'NONE',  ( 116.4834948109119779, -7.894159318335828068, -9.358103419637847864 ) ) ;
#10344=CARTESIAN_POINT ( 'NONE',  ( 126.1270281442452870, -10.30919188438810075, -12.61870101168855918 ) ) ;
#10345=ORIENTED_EDGE ( 'NONE', *, *, #33987, .F. ) ;
#10346=CARTESIAN_POINT ( 'NONE',  ( 124.9924948109119924, -5.574606645277164318, -18.38911715685844683 ) ) ;
#10347=CARTESIAN_POINT ( 'NONE',  ( 125.3328548109119964, -0.8288870151387760510, -10.36305467784173118 ) ) ;
#10348=CARTESIAN_POINT ( 'NONE',  ( 113.8173414775786512, -9.565557343593413364, -10.61323700422348004 ) ) ;
#10351=EDGE_CURVE ( 'NONE', #10826, #32113, #12637, .T. ) ;
#10354=CARTESIAN_POINT ( 'NONE',  ( 119.9438214775786378, -2.084020599724406786, -8.691656652584148546 ) ) ;
#10355=CARTESIAN_POINT ( 'NONE',  ( 113.5337081442453240, -0.8288870151387760510, -10.36305467784173118 ) ) ;
#10365=CARTESIAN_POINT ( 'NONE',  ( 123.2906948109119867, -1.833838273342659697, -17.42832698103878286 ) ) ;
#10366=CARTESIAN_POINT ( 'NONE',  ( 117.6180281442453150, -8.899110576539710493, -16.42337572283490132 ) ) ;
#10367=CARTESIAN_POINT ( 'NONE',  ( 120.0157737256648858, -1.063912429576147511, -17.20460841810472985 ) ) ;
#10370=CARTESIAN_POINT ( 'NONE',  ( 114.8951481442453115, -8.899110576539710493, -16.42337572283490132 ) ) ;
#10373=CARTESIAN_POINT ( 'NONE',  ( 125.9001214775786224, -4.089484607189486809, -7.948022111789456723 ) ) ;
#10374=CARTESIAN_POINT ( 'NONE',  ( 111.8886348109120092, -3.383040157471821630, -19.15922257007629170 ) ) ;
#10376=CARTESIAN_POINT ( 'NONE',  ( 115.1220548109119761, -8.166667518702817929, -8.995218007635861213 ) ) ;
#10379=CARTESIAN_POINT ( 'NONE',  ( 126.5808414775786446, -9.859900752359378018, -12.68260735090039759 ) ) ;
#10380=CARTESIAN_POINT ( 'NONE',  ( 115.6893214775786447, 0.5811942927096154232, -14.16772938898807155 ) ) ;
#10381=CARTESIAN_POINT ( 'NONE',  ( 125.1626748109119802, -0.1624402480850797581, -16.17319339645315424 ) ) ;
#10385=CARTESIAN_POINT ( 'NONE',  ( 117.3719165460472027, -2.191907684172563986, -18.20049396185734025 ) ) ;
#10387=CARTESIAN_POINT ( 'NONE',  ( 117.8449348109119938, -1.833838273342659253, -17.42832698103878286 ) ) ;
#10391=CARTESIAN_POINT ( 'NONE',  ( 126.2404814775786264, -9.261995988541697145, -16.69588392320189030 ) ) ;
#10392=CARTESIAN_POINT ( 'NONE',  ( 111.4915481442453142, -1.833838273342658365, -17.42832698103878286 ) ) ;
#10393=CARTESIAN_POINT ( 'NONE',  ( 120.1140014775786398, -7.894159318335804976, -9.358103419637831877 ) ) ;
#10394=CARTESIAN_POINT ( 'NONE',  ( 119.1496481442453046, -3.383040157471821630, -19.15922257007629170 ) ) ;
#10395=CARTESIAN_POINT ( 'NONE',  ( 114.5547881442453217, -5.638512984488999180, -18.83840828888717311 ) ) ;
#10398=CARTESIAN_POINT ( 'NONE',  ( 115.1787814775786387, -0.1624402480850797581, -16.17319339645315424 ) ) ;
#10399=CARTESIAN_POINT ( 'NONE',  ( 123.8012348109119642, 0.2603800115204892296, -16.42320221600525088 ) ) ;
#10400=CARTESIAN_POINT ( 'NONE',  ( 113.8740681442453138, 0.5811942927096154232, -14.16772938898807155 ) ) ;
#10401=CARTESIAN_POINT ( 'NONE',  ( 115.0086014775786509, -5.574606645277164318, -18.38911715685844683 ) ) ;
#10403=CARTESIAN_POINT ( 'NONE',  ( 120.8514481442452961, -2.084020599724406786, -8.691656652584148546 ) ) ;
#10404=B_SPLINE_CURVE_WITH_KNOTS ( 'NONE', 3,
 ( #41221, #30261, #5854, #19777, #33659, #23661, #2436, #23432, #44187, #9979 ),
 .UNSPECIFIED., .F., .F.,
 ( 4, 3, 3, 4 ),
 ( 5.023252700711280216E-16, 1.701546542442415166E-05, 3.403093084891979967E-05, 6.554879158867139171E-05 ),
 .UNSPECIFIED. ) ;
#10406=CARTESIAN_POINT ( 'NONE',  ( 116.1998614775786507, -10.63000616557722466, -14.87417383870573495 ) ) ;
#10407=EDGE_CURVE ( 'NONE', #39007, #42235, #1138, .T. ) ;
#10413=CARTESIAN_POINT ( 'NONE',  ( 125.6732148109119862, 0.5811942927096110934, -14.16772938898807510 ) ) ;
#10416=CARTESIAN_POINT ( 'NONE',  ( 115.0086014775786509, -4.089484607189486809, -7.948022111789456723 ) ) ;
#10417=CARTESIAN_POINT ( 'NONE',  ( 135.8419766445594234, -10.77193394454819320, -14.12650746913758937 ) ) ;
#10420=CARTESIAN_POINT ( 'NONE',  ( 115.5950730757767531, -0.9924539043446216624, -17.29976612834909133 ) ) ;
#10422=CARTESIAN_POINT ( 'NONE',  ( 119.2631014775786298, 0.2603800115204892296, -16.42320221600525088 ) ) ;
#10424=CARTESIAN_POINT ( 'NONE',  ( 111.5491077074049002, -2.419733177069675722, -17.89711025544712086 ) ) ;
#10426=CARTESIAN_POINT ( 'NONE',  ( 121.3619881442452879, -5.574606645277164318, -18.38911715685844683 ) ) ;
#10429=CARTESIAN_POINT ( 'NONE',  ( 119.9438214775786378, -7.893985811506177619, -18.51759400769804742 ) ) ;
#10431=CARTESIAN_POINT ( 'NONE',  ( 116.0296814775786345, -1.833838273342658809, -17.42832698103878286 ) ) ;
#10433=CARTESIAN_POINT ( 'NONE',  ( 111.3213681442453264, -7.643976991954077427, -18.09477374809248928 ) ) ;
#10436=CARTESIAN_POINT ( 'NONE',  ( 121.4187148109119789, -3.505236298600246325, -18.68346056562440793 ) ) ;
#10438=CARTESIAN_POINT ( 'NONE',  ( 121.9859814775786333, -9.565557343593413364, -10.61323700422348004 ) ) ;
#10444=CARTESIAN_POINT ( 'NONE',  ( 113.2500748109119968, -6.344957434206662583, -7.627207830600332805 ) ) ;
#10445=CARTESIAN_POINT ( 'NONE',  ( 116.0296814775786345, -8.166667518702817929, -8.995218007635861213 ) ) ;
#10448=CARTESIAN_POINT ( 'NONE',  ( 123.5944003412206484, -3.153399869360316909, -14.42216642652626746 ) ) ;
#10450=CARTESIAN_POINT ( 'NONE',  ( 121.0216281442452981, -1.561330072975668948, -17.79121239304076951 ) ) ;
#10451=CARTESIAN_POINT ( 'NONE',  ( 113.3068014775786594, -8.166667518702817929, -8.995218007635859436 ) ) ;
#10452=CARTESIAN_POINT ( 'NONE',  ( 118.2987481442453088, -7.894159318335828068, -9.358103419637847864 ) ) ;
#10455=CARTESIAN_POINT ( 'NONE',  ( 120.8514481442452961, -7.893985811506177619, -18.51759400769804742 ) ) ;
#10456=CARTESIAN_POINT ( 'NONE',  ( 119.2631014775786298, 0.2603800115204892296, -16.42320221600525088 ) ) ;
#10459=CARTESIAN_POINT ( 'NONE',  ( 126.2404814775786264, -9.261995988541697145, -16.69588392320189030 ) ) ;
#10461=ORIENTED_EDGE ( 'NONE', *, *, #6916, .F. ) ;
#10462=( BOUNDED_CURVE ( )  B_SPLINE_CURVE ( 2, ( #29224, #43131, #32408, #32184, #722, #21930, #11901, #8476, #11006, #38800, #7571, #18065, #31956, #14644, #19408, #40163, #2523 ),
 .UNSPECIFIED., .F., .F. ) 
 B_SPLINE_CURVE_WITH_KNOTS ( ( 3, 2, 2, 2, 2, 2, 2, 2, 3 ),
 ( 0.4546282416568590001, 0.4609375000000000000, 0.4687500000000000000, 0.4765625000000000000, 0.4843750000000000000, 0.4921875000000000000, 0.5000000000000000000, 0.5078125000000000000, 0.5141217583431409999 ),
 .UNSPECIFIED. ) 
 CURVE ( )  GEOMETRIC_REPRESENTATION_ITEM ( )  RATIONAL_B_SPLINE_CURVE ( ( 0.9763430640195960297, 0.9385262470928690259, 1.000000000000000000, 0.9238795325112869605, 1.000000000000000000, 0.9238795325112869605, 1.000000000000000000, 0.9238795325112869605, 1.000000000000000000, 0.9238795325112869605, 1.000000000000000000, 0.9238795325112869605, 1.000000000000000000, 0.9238795325112869605, 1.000000000000000000, 0.9385262470928680267, 0.9763430640195970289 ) ) 
 REPRESENTATION_ITEM ( '' )  );
#10463=CARTESIAN_POINT ( 'NONE',  ( 116.2565881442452991, -9.261995988541697145, -16.69588392320189030 ) ) ;
#10464=AXIS2_PLACEMENT_3D ( 'NONE', #30007, #19523, #16333 ) ;
#10466=CARTESIAN_POINT ( 'NONE',  ( 117.0507614775786465, -10.30919188438810075, -12.61870101168855918 ) ) ;
#10471=CARTESIAN_POINT ( 'NONE',  ( 119.8355804873411756, -2.348512537728041583, -17.99195118506215962 ) ) ;
#10474=CARTESIAN_POINT ( 'NONE',  ( 118.3554748109119998, -9.565557343593413364, -10.61323700422348004 ) ) ;
#10476=CARTESIAN_POINT ( 'NONE',  ( 117.7314814775786260, -5.574606645277164318, -18.38911715685844683 ) ) ;
#10479=CARTESIAN_POINT ( 'NONE',  ( 120.1140014775786398, -7.894159318335828068, -9.358103419637847864 ) ) ;
#10480=CARTESIAN_POINT ( 'NONE',  ( 111.7751814775786556, -7.893985811506177619, -18.51759400769804742 ) ) ;
#10481=CARTESIAN_POINT ( 'NONE',  ( 116.3133148109119759, -7.893985811506177619, -18.51759400769804742 ) ) ;
#10482=CARTESIAN_POINT ( 'NONE',  ( 117.5613014775786525, -10.15424416112533912, -14.75197769757731336 ) ) ;
#10483=EDGE_LOOP ( 'NONE', ( #9518, #2009, #24364, #6352, #3416 ) ) ;
#10484=CARTESIAN_POINT ( 'NONE',  ( 116.1998614775786507, -10.63000616557722466, -14.87417383870573495 ) ) ;
#10487=DIRECTION ( 'NONE',  ( 1.000000000000000000, 0.000000000000000000, 0.000000000000000000 ) ) ;
#10489=CARTESIAN_POINT ( 'NONE',  ( 122.6667014775786413, -7.893985811506177619, -18.51759400769804742 ) ) ;
#10491=CARTESIAN_POINT ( 'NONE',  ( 127.9806007748782406, -9.485509010566754995, -9.755774181203904050 ) ) ;
#10492=CARTESIAN_POINT ( 'NONE',  ( 119.0361948109119652, -2.084020599724406786, -8.691656652584148546 ) ) ;
#10493=CARTESIAN_POINT ( 'NONE',  ( 116.0296814775786345, -8.166667518702805495, -8.995218007635852331 ) ) ;
#10494=CARTESIAN_POINT ( 'NONE',  ( 124.3117748109119844, 0.1319031606808835910, -14.10382304977624734 ) ) ;
#10495=CARTESIAN_POINT ( 'NONE',  ( 122.2128881442453263, -1.834011780172310813, -8.268836392978581529 ) ) ;
#10500=CARTESIAN_POINT ( 'NONE',  ( 113.3068014775786594, -8.166667518702817929, -8.995218007635859436 ) ) ;
#10501=CARTESIAN_POINT ( 'NONE',  ( 112.0588148109119828, 0.5811942927096154232, -14.16772938898807155 ) ) ;
#10502=CARTESIAN_POINT ( 'NONE',  ( 121.7590748109119687, -7.893985811506177619, -18.51759400769804742 ) ) ;
#10503=CARTESIAN_POINT ( 'NONE',  ( 117.2776681442452968, -4.153390946401321671, -8.397313243818183892 ) ) ;
#10505=CARTESIAN_POINT ( 'NONE',  ( 119.0361948109119652, -7.893985811506177619, -18.51759400769804742 ) ) ;
#10507=CARTESIAN_POINT ( 'NONE',  ( 121.7023481442452777, -0.8288870151387760510, -10.36305467784173118 ) ) ;
#10510=CARTESIAN_POINT ( 'NONE',  ( 116.6536748109119941, 0.9020085738987339008, -11.91225656197089222 ) ) ;
#10511=CARTESIAN_POINT ( 'NONE',  ( 123.7445081442452874, -7.894159318335828068, -9.358103419637847864 ) ) ;
#10515=CARTESIAN_POINT ( 'NONE',  ( 122.0427081442452817, 0.5811942927096110934, -14.16772938898807510 ) ) ;
#10517=CARTESIAN_POINT ( 'NONE',  ( 118.1852948109119836, -4.153390946401325223, -8.397313243818185668 ) ) ;
#10518=ADVANCED_FACE ( 'NONE', ( #26484 ), #31622, .T. ) ;
#10521=CARTESIAN_POINT ( 'NONE',  ( 114.6682414775786469, -1.561330072975668060, -17.79121239304076596 ) ) ;
#10522=CARTESIAN_POINT ( 'NONE',  ( 124.0281414775786146, -7.643976991954077427, -18.09477374809248928 ) ) ;
#10523=( LENGTH_UNIT ( ) NAMED_UNIT ( * ) SI_UNIT ( .MILLI., .METRE. ) );
#10526=CARTESIAN_POINT ( 'NONE',  ( 122.9503348109119827, 0.5811942927096110934, -14.16772938898807510 ) ) ;
#10528=CARTESIAN_POINT ( 'NONE',  ( 111.2184548109119788, -8.862178061932382889, -16.39564131203247399 ) ) ;
#10529=CARTESIAN_POINT ( 'NONE',  ( 124.2550481442452792, -9.988377603198980381, -10.36322818467138518 ) ) ;
#10530=CARTESIAN_POINT ( 'NONE',  ( 117.3343948109119737, -3.383040157471821630, -19.15922257007629170 ) ) ;
#10531=CARTESIAN_POINT ( 'NONE',  ( 122.0994348109119443, -10.15424416112533912, -14.75197769757731336 ) ) ;
#10532=CARTESIAN_POINT ( 'NONE',  ( 121.5888948109119809, 0.1319031606808879209, -14.10382304977623669 ) ) ;
#10533=CARTESIAN_POINT ( 'NONE',  ( 125.2655881442453278, 0.08617673920530924403, -14.09731900820076334 ) ) ;
#10534=CARTESIAN_POINT ( 'NONE',  ( 115.8027748109119841, -0.4660016031367893996, -10.09054647747474043 ) ) ;
#10539=LINE ( 'NONE', #10986, #13148 ) ;
#10540=CARTESIAN_POINT ( 'NONE',  ( 111.8319081442453182, -5.638512984488999180, -18.83840828888717311 ) ) ;
#10541=( BOUNDED_SURFACE ( )  B_SPLINE_SURFACE ( 1, 2, ( 
 ( #24023, #44544, #19917, #6689, #33802, #20600, #9892, #2574, #34476, #20152, #5760, #37692, #2805, #16731, #30628, #29949, #27215, #23802, #20374, #34261, #3255, #3036, #16957, #30852, #28110, #34906, #42462, #11227, #7339, #34694, #41579, #27885, #28325, #42237, #31733, #24241, #13756, #31069, #38135, #44997, #282, #27665, #24675, #21708, #18062, #6906, #20816, #3482, #17837, #31953, #3696, #21033, #41800, #10338, #7568, #10558, #7123, #35136, #21257, #35595, #11002, #718, #24455, #7799, #17617, #17398, #24902, #14640, #31509, #38795, #35366, #17180, #38562, #4141, #14192, #25134, #503, #21481, #42014, #28557, #39028, #31286, #60, #13973, #38346, #10779, #3918, #14415, #22822, #35819, #18736, #32629, #39709, #28779, #951, #19183, #43355, #12124, #33062, #1836, #18285, #8473, #15765, #18514, #29666, #1395, #39483, #43579, #15310, #39254, #25799, #32845, #32181, #26026, #43128, #22375, #11897, #26247, #8921, #1175, #11671, #11454, #29219, #36272, #1613, #8247, #4815, #22597, #14869, #36047, #42686, #5040, #22154, #40160, #25360, #39932, #8019, #21926, #18954, #15534, #29439, #8692, #36498, #4591, #25580, #5267, #15090, #12349, #4365, #32405, #29001, #42909, #34200, #40613, #2974, #36939, #5484, #16446, #10064, #43811, #16903, #12577, #12802, #40845, #2292, #23516, #13026, #29894, #36714, #30795, #44719, #9371, #13479, #5710, #19404, #30346, #33291, #26481, #27382, #16671, #6173, #40386, #2066, #15990, #9147, #23053, #19861, #19627, #44269, #41304, #37635, #33511, #16220, #30124, #37403, #6408, #23280, #37162, #44038, #26702, #27155, #5939, #33749, #9600, #20094, #2519, #30567, #20316, #26924, #33979, #2747, #44486, #13253, #41077, #9834, #23744, #42181, #42405, #221, #10941, #7069, #31899, #24623, #14359, #27826, #28272, #443, #24844, #28498, #665, #38736, #7506, #38291, #14134, #23966, #10279, #20980, #34853, #28050, #3200, #20540, #21421, #17780, #31673, #35305, #4077, #37852, #41958, #18001, #38076, #14581, #3639, #13915, #6626, #17557, #13700, #10723 ),
 ( #34419, #24184, #17124, #31013, #35077, #44943, #10501, #27608, #41522, #6854, #20761, #17343, #34640, #3426, #38506, #31233, #5, #41737, #24402, #3858, #31452, #7283, #21199, #21645, #18897, #4306, #14810, #22542, #39194, #21871, #1339, #8417, #7960, #8192, #11841, #32572, #22100, #39877, #42629, #1784, #29387, #22323, #29612, #42853, #25073, #38966, #28723, #7735, #4536, #35534, #8642, #25748, #891, #25971, #1116, #36440, #36219, #18460, #5207, #4759, #18228, #32788, #15034, #32122, #11393, #11168, #11612, #25302, #35765, #1559, #19127, #33009, #32350, #43300, #35988, #28945, #15709, #25523, #15253, #39426, #18681, #29159, #4984, #43072, #39654, #15483, #12069, #29839, #41026, #30514, #34151, #2465, #12977, #37347, #44435, #23694, #5884, #20265, #20038, #23229, #12522, #26872, #19353, #37110, #22996, #13203, #9321, #33920, #26647, #6120, #27103, #9779, #37580, #40330, #40562, #36887, #40788, #36662, #16851, #12746, #9095, #2691, #26423, #5657, #6353, #19576, #33241, #16621, #9546, #33455, #16389, #2920, #2235, #43527, #12296, #2014, #19805, #33694, #30289, #16166, #26195, #43757, #40102, #8862, #44216, #30070, #22764, #23461, #5435, #15939, #43982, #3154, #38241, #7231, #41908, #27556, #34805, #21147, #13650, #14307, #394, #34371, #45104, #41688, #10450, #38027, #38460, #17074, #35253, #24575, #24353, #44890, #42132, #14085, #28226, #38685, #23918, #30967, #7020, #37799, #41469, #10892, #10227, #24135, #20931, #28002, #6803, #27776, #31400, #3591, #17501, #24791, #20712, #21370, #3803, #10672, #4030, #17294, #44667, #13429, #34591, #27333, #3374, #41251, #7450, #168, #20492, #30743, #31186, #10009, #35021, #13862, #6574, #17729, #31626, #38911, #28444, #31850, #620, #17951, #25018, #14530, #42356, #11117, #7682, #21596, #35483, #33969, #26692, #33501, #41067, #9824, #5929, #33282, #40148, #26470, #26915, #20306, #33738, #23041, #26238, #2057, #13244, #2737, #6399, #19851, #30334, #9591, #16662, #23734, #23271, #37625, #37392, #40603, #29883, #44260, #36705 ) ),
 .UNSPECIFIED., .F., .F., .T. ) 
 B_SPLINE_SURFACE_WITH_KNOTS ( ( 2, 2 ),
 ( 3, 2, 2, 2, 2, 2, 2, 2, 2, 2, 2, 2, 2, 2, 2, 2, 2, 2, 2, 2, 2, 2, 2, 2, 2, 2, 2, 2, 2, 2, 2, 2, 2, 2, 2, 2, 2, 2, 2, 2, 2, 2, 2, 2, 2, 2, 2, 2, 2, 2, 2, 2, 2, 2, 2, 2, 2, 2, 2, 2, 2, 2, 2, 2, 2, 2, 2, 2, 2, 2, 2, 2, 2, 2, 2, 2, 2, 2, 2, 2, 2, 2, 2, 2, 2, 2, 2, 2, 2, 2, 2, 2, 2, 2, 2, 2, 2, 2, 2, 2, 2, 2, 2, 2, 2, 2, 2, 2, 2, 2, 2, 2, 2, 2, 2, 2, 2, 2, 2, 2, 2, 2, 2, 2, 2, 2, 2, 2, 3 ),
 ( 0.000000000000000000, 1.000000000000000000 ),
 ( 0.000000000000000000, 0.007812500000000000000, 0.01562500000000000000, 0.02343750000000000000, 0.03125000000000000000, 0.03906250000000000000, 0.04687500000000000000, 0.05468750000000000000, 0.06250000000000000000, 0.07031250000000000000, 0.07812500000000000000, 0.08593750000000000000, 0.09375000000000000000, 0.1015625000000000000, 0.1093750000000000000, 0.1171875000000000000, 0.1250000000000000000, 0.1328125000000000000, 0.1406250000000000000, 0.1484375000000000000, 0.1562500000000000000, 0.1640625000000000000, 0.1718750000000000000, 0.1796875000000000000, 0.1875000000000000000, 0.1953125000000000000, 0.2031250000000000000, 0.2109375000000000000, 0.2187500000000000000, 0.2265625000000000000, 0.2343750000000000000, 0.2421875000000000000, 0.2500000000000000000, 0.2578125000000000000, 0.2656250000000000000, 0.2734375000000000000, 0.2812500000000000000, 0.2890625000000000000, 0.2968750000000000000, 0.3046875000000000000, 0.3125000000000000000, 0.3203125000000000000, 0.3281250000000000000, 0.3359375000000000000, 0.3437500000000000000, 0.3515625000000000000, 0.3593750000000000000, 0.3671875000000000000, 0.3750000000000000000, 0.3828125000000000000, 0.3906250000000000000, 0.3984375000000000000, 0.4062500000000000000, 0.4140625000000000000, 0.4218750000000000000, 0.4296875000000000000, 0.4375000000000000000, 0.4453125000000000000, 0.4531250000000000000, 0.4609375000000000000, 0.4687500000000000000, 0.4765625000000000000, 0.4843750000000000000, 0.4921875000000000000, 0.5000000000000000000, 0.5078125000000000000, 0.5156250000000000000, 0.5234375000000000000, 0.5312500000000000000, 0.5390625000000000000, 0.5468750000000000000, 0.5546875000000000000, 0.5625000000000000000, 0.5703125000000000000, 0.5781250000000000000, 0.5859375000000000000, 0.5937500000000000000, 0.6015625000000000000, 0.6093750000000000000, 0.6171875000000000000, 0.6250000000000000000, 0.6328125000000000000, 0.6406250000000000000, 0.6484375000000000000, 0.6562500000000000000, 0.6640625000000000000, 0.6718750000000000000, 0.6796875000000000000, 0.6875000000000000000, 0.6953125000000000000, 0.7031250000000000000, 0.7109375000000000000, 0.7187500000000000000, 0.7265625000000000000, 0.7343750000000000000, 0.7421875000000000000, 0.7500000000000000000, 0.7578125000000000000, 0.7656250000000000000, 0.7734375000000000000, 0.7812500000000000000, 0.7890625000000000000, 0.7968750000000000000, 0.8046875000000000000, 0.8125000000000000000, 0.8203125000000000000, 0.8281250000000000000, 0.8359375000000000000, 0.8437500000000000000, 0.8515625000000000000, 0.8593750000000000000, 0.8671875000000000000, 0.8750000000000000000, 0.8828125000000000000, 0.8906250000000000000, 0.8984375000000000000, 0.9062500000000000000, 0.9140625000000000000, 0.9218750000000000000, 0.9296875000000000000, 0.9375000000000000000, 0.9453125000000000000, 0.9531250000000000000, 0.9609375000000000000, 0.9687500000000000000, 0.9765625000000000000, 0.9843750000000000000, 0.9921875000000000000, 1.000000000000000000 ),
 .UNSPECIFIED. ) 
 GEOMETRIC_REPRESENTATION_ITEM ( )  RATIONAL_B_SPLINE_SURFACE ( (
 ( 1.000000000000000000, 0.9238795325112869605, 1.000000000000000000, 0.9238795325112869605, 1.000000000000000000, 0.9238795325112869605, 1.000000000000000000, 0.9238795325112869605, 1.000000000000000000, 0.9238795325112869605, 1.000000000000000000, 0.9238795325112869605, 1.000000000000000000, 0.9238795325112869605, 1.000000000000000000, 0.9238795325112869605, 1.000000000000000000, 0.9238795325112869605, 1.000000000000000000, 0.9238795325112869605, 1.000000000000000000, 0.9238795325112869605, 1.000000000000000000, 0.9238795325112869605, 1.000000000000000000, 0.9238795325112869605, 1.000000000000000000, 0.9238795325112869605, 1.000000000000000000, 0.9238795325112869605, 1.000000000000000000, 0.9238795325112869605, 1.000000000000000000, 0.9238795325112869605, 1.000000000000000000, 0.9238795325112869605, 1.000000000000000000, 0.9238795325112869605, 1.000000000000000000, 0.9238795325112869605, 1.000000000000000000, 0.9238795325112869605, 1.000000000000000000, 0.9238795325112869605, 1.000000000000000000, 0.9238795325112869605, 1.000000000000000000, 0.9238795325112869605, 1.000000000000000000, 0.9238795325112869605, 1.000000000000000000, 0.9238795325112869605, 1.000000000000000000, 0.9238795325112869605, 1.000000000000000000, 0.9238795325112869605, 1.000000000000000000, 0.9238795325112869605, 1.000000000000000000, 0.9238795325112869605, 1.000000000000000000, 0.9238795325112869605, 1.000000000000000000, 0.9238795325112869605, 1.000000000000000000, 0.9238795325112869605, 1.000000000000000000, 0.9238795325112869605, 1.000000000000000000, 0.9238795325112869605, 1.000000000000000000, 0.9238795325112869605, 1.000000000000000000, 0.9238795325112869605, 1.000000000000000000, 0.9238795325112869605, 1.000000000000000000, 0.9238795325112869605, 1.000000000000000000, 0.9238795325112869605, 1.000000000000000000, 0.9238795325112869605, 1.000000000000000000, 0.9238795325112869605, 1.000000000000000000, 0.9238795325112869605, 1.000000000000000000, 0.9238795325112869605, 1.000000000000000000, 0.9238795325112869605, 1.000000000000000000, 0.9238795325112869605, 1.000000000000000000, 0.9238795325112869605, 1.000000000000000000, 0.9238795325112869605, 1.000000000000000000, 0.9238795325112869605, 1.000000000000000000, 0.9238795325112869605, 1.000000000000000000, 0.9238795325112869605, 1.000000000000000000, 0.9238795325112869605, 1.000000000000000000, 0.9238795325112869605, 1.000000000000000000, 0.9238795325112869605, 1.000000000000000000, 0.9238795325112869605, 1.000000000000000000, 0.9238795325112869605, 1.000000000000000000, 0.9238795325112869605, 1.000000000000000000, 0.9238795325112869605, 1.000000000000000000, 0.9238795325112869605, 1.000000000000000000, 0.9238795325112869605, 1.000000000000000000, 0.9238795325112869605, 1.000000000000000000, 0.9238795325112869605, 1.000000000000000000, 0.9238795325112869605, 1.000000000000000000, 0.9238795325112869605, 1.000000000000000000, 0.9238795325112869605, 1.000000000000000000, 0.9238795325112869605, 1.000000000000000000, 0.9238795325112869605, 1.000000000000000000, 0.9238795325112869605, 1.000000000000000000, 0.9238795325112869605, 1.000000000000000000, 0.9238795325112869605, 1.000000000000000000, 0.9238795325112869605, 1.000000000000000000, 0.9238795325112869605, 1.000000000000000000, 0.9238795325112869605, 1.000000000000000000, 0.9238795325112869605, 1.000000000000000000, 0.9238795325112869605, 1.000000000000000000, 0.9238795325112869605, 1.000000000000000000, 0.9238795325112869605, 1.000000000000000000, 0.9238795325112869605, 1.000000000000000000, 0.9238795325112869605, 1.000000000000000000, 0.9238795325112869605, 1.000000000000000000, 0.9238795325112869605, 1.000000000000000000, 0.9238795325112869605, 1.000000000000000000, 0.9238795325112869605, 1.000000000000000000, 0.9238795325112869605, 1.000000000000000000, 0.9238795325112869605, 1.000000000000000000, 0.9238795325112869605, 1.000000000000000000, 0.9238795325112869605, 1.000000000000000000, 0.9238795325112869605, 1.000000000000000000, 0.9238795325112869605, 1.000000000000000000, 0.9238795325112869605, 1.000000000000000000, 0.9238795325112869605, 1.000000000000000000, 0.9238795325112869605, 1.000000000000000000, 0.9238795325112869605, 1.000000000000000000, 0.9238795325112869605, 1.000000000000000000, 0.9238795325112869605, 1.000000000000000000, 0.9238795325112869605, 1.000000000000000000, 0.9238795325112869605, 1.000000000000000000, 0.9238795325112869605, 1.000000000000000000, 0.9238795325112869605, 1.000000000000000000, 0.9238795325112869605, 1.000000000000000000, 0.9238795325112869605, 1.000000000000000000, 0.9238795325112869605, 1.000000000000000000, 0.9238795325112869605, 1.000000000000000000, 0.9238795325112869605, 1.000000000000000000, 0.9238795325112869605, 1.000000000000000000, 0.9238795325112869605, 1.000000000000000000, 0.9238795325112869605, 1.000000000000000000, 0.9238795325112869605, 1.000000000000000000, 0.9238795325112869605, 1.000000000000000000, 0.9238795325112869605, 1.000000000000000000, 0.9238795325112869605, 1.000000000000000000, 0.9238795325112869605, 1.000000000000000000, 0.9238795325112869605, 1.000000000000000000, 0.9238795325112869605, 1.000000000000000000, 0.9238795325112869605, 1.000000000000000000, 0.9238795325112869605, 1.000000000000000000, 0.9238795325112869605, 1.000000000000000000, 0.9238795325112869605, 1.000000000000000000, 0.9238795325112869605, 1.000000000000000000, 0.9238795325112869605, 1.000000000000000000, 0.9238795325112869605, 1.000000000000000000, 0.9238795325112869605, 1.000000000000000000, 0.9238795325112869605, 1.000000000000000000, 0.9238795325112869605, 1.000000000000000000, 0.9238795325112869605, 1.000000000000000000, 0.9238795325112869605, 1.000000000000000000, 0.9238795325112869605, 1.000000000000000000, 0.9238795325112869605, 1.000000000000000000),
 ( 1.000000000000000000, 0.9238795325112869605, 1.000000000000000000, 0.9238795325112869605, 1.000000000000000000, 0.9238795325112869605, 1.000000000000000000, 0.9238795325112869605, 1.000000000000000000, 0.9238795325112869605, 1.000000000000000000, 0.9238795325112869605, 1.000000000000000000, 0.9238795325112869605, 1.000000000000000000, 0.9238795325112869605, 1.000000000000000000, 0.9238795325112869605, 1.000000000000000000, 0.9238795325112869605, 1.000000000000000000, 0.9238795325112869605, 1.000000000000000000, 0.9238795325112869605, 1.000000000000000000, 0.9238795325112869605, 1.000000000000000000, 0.9238795325112869605, 1.000000000000000000, 0.9238795325112869605, 1.000000000000000000, 0.9238795325112869605, 1.000000000000000000, 0.9238795325112869605, 1.000000000000000000, 0.9238795325112869605, 1.000000000000000000, 0.9238795325112869605, 1.000000000000000000, 0.9238795325112869605, 1.000000000000000000, 0.9238795325112869605, 1.000000000000000000, 0.9238795325112869605, 1.000000000000000000, 0.9238795325112869605, 1.000000000000000000, 0.9238795325112869605, 1.000000000000000000, 0.9238795325112869605, 1.000000000000000000, 0.9238795325112869605, 1.000000000000000000, 0.9238795325112869605, 1.000000000000000000, 0.9238795325112869605, 1.000000000000000000, 0.9238795325112869605, 1.000000000000000000, 0.9238795325112869605, 1.000000000000000000, 0.9238795325112869605, 1.000000000000000000, 0.9238795325112869605, 1.000000000000000000, 0.9238795325112869605, 1.000000000000000000, 0.9238795325112869605, 1.000000000000000000, 0.9238795325112869605, 1.000000000000000000, 0.9238795325112869605, 1.000000000000000000, 0.9238795325112869605, 1.000000000000000000, 0.9238795325112869605, 1.000000000000000000, 0.9238795325112869605, 1.000000000000000000, 0.9238795325112869605, 1.000000000000000000, 0.9238795325112869605, 1.000000000000000000, 0.9238795325112869605, 1.000000000000000000, 0.9238795325112869605, 1.000000000000000000, 0.9238795325112869605, 1.000000000000000000, 0.9238795325112869605, 1.000000000000000000, 0.9238795325112869605, 1.000000000000000000, 0.9238795325112869605, 1.000000000000000000, 0.9238795325112869605, 1.000000000000000000, 0.9238795325112869605, 1.000000000000000000, 0.9238795325112869605, 1.000000000000000000, 0.9238795325112869605, 1.000000000000000000, 0.9238795325112869605, 1.000000000000000000, 0.9238795325112869605, 1.000000000000000000, 0.9238795325112869605, 1.000000000000000000, 0.9238795325112869605, 1.000000000000000000, 0.9238795325112869605, 1.000000000000000000, 0.9238795325112869605, 1.000000000000000000, 0.9238795325112869605, 1.000000000000000000, 0.9238795325112869605, 1.000000000000000000, 0.9238795325112869605, 1.000000000000000000, 0.9238795325112869605, 1.000000000000000000, 0.9238795325112869605, 1.000000000000000000, 0.9238795325112869605, 1.000000000000000000, 0.9238795325112869605, 1.000000000000000000, 0.9238795325112869605, 1.000000000000000000, 0.9238795325112869605, 1.000000000000000000, 0.9238795325112869605, 1.000000000000000000, 0.9238795325112869605, 1.000000000000000000, 0.9238795325112869605, 1.000000000000000000, 0.9238795325112869605, 1.000000000000000000, 0.9238795325112869605, 1.000000000000000000, 0.9238795325112869605, 1.000000000000000000, 0.9238795325112869605, 1.000000000000000000, 0.9238795325112869605, 1.000000000000000000, 0.9238795325112869605, 1.000000000000000000, 0.9238795325112869605, 1.000000000000000000, 0.9238795325112869605, 1.000000000000000000, 0.9238795325112869605, 1.000000000000000000, 0.9238795325112869605, 1.000000000000000000, 0.9238795325112869605, 1.000000000000000000, 0.9238795325112869605, 1.000000000000000000, 0.9238795325112869605, 1.000000000000000000, 0.9238795325112869605, 1.000000000000000000, 0.9238795325112869605, 1.000000000000000000, 0.9238795325112869605, 1.000000000000000000, 0.9238795325112869605, 1.000000000000000000, 0.9238795325112869605, 1.000000000000000000, 0.9238795325112869605, 1.000000000000000000, 0.9238795325112869605, 1.000000000000000000, 0.9238795325112869605, 1.000000000000000000, 0.9238795325112869605, 1.000000000000000000, 0.9238795325112869605, 1.000000000000000000, 0.9238795325112869605, 1.000000000000000000, 0.9238795325112869605, 1.000000000000000000, 0.9238795325112869605, 1.000000000000000000, 0.9238795325112869605, 1.000000000000000000, 0.9238795325112869605, 1.000000000000000000, 0.9238795325112869605, 1.000000000000000000, 0.9238795325112869605, 1.000000000000000000, 0.9238795325112869605, 1.000000000000000000, 0.9238795325112869605, 1.000000000000000000, 0.9238795325112869605, 1.000000000000000000, 0.9238795325112869605, 1.000000000000000000, 0.9238795325112869605, 1.000000000000000000, 0.9238795325112869605, 1.000000000000000000, 0.9238795325112869605, 1.000000000000000000, 0.9238795325112869605, 1.000000000000000000, 0.9238795325112869605, 1.000000000000000000, 0.9238795325112869605, 1.000000000000000000, 0.9238795325112869605, 1.000000000000000000, 0.9238795325112869605, 1.000000000000000000, 0.9238795325112869605, 1.000000000000000000, 0.9238795325112869605, 1.000000000000000000, 0.9238795325112869605, 1.000000000000000000, 0.9238795325112869605, 1.000000000000000000, 0.9238795325112869605, 1.000000000000000000, 0.9238795325112869605, 1.000000000000000000, 0.9238795325112869605, 1.000000000000000000, 0.9238795325112869605, 1.000000000000000000, 0.9238795325112869605, 1.000000000000000000, 0.9238795325112869605, 1.000000000000000000, 0.9238795325112869605, 1.000000000000000000, 0.9238795325112869605, 1.000000000000000000, 0.9238795325112869605, 1.000000000000000000, 0.9238795325112869605, 1.000000000000000000, 0.9238795325112869605, 1.000000000000000000, 0.9238795325112869605, 1.000000000000000000, 0.9238795325112869605, 1.000000000000000000) ) ) 
 REPRESENTATION_ITEM ( '' )  SURFACE ( )  );
#10544=CARTESIAN_POINT ( 'NONE',  ( 124.1415948109119540, -6.344957434206665248, -7.627207830600338134 ) ) ;
#10547=CARTESIAN_POINT ( 'NONE',  ( 123.2339681442453241, -6.344957434206665248, -7.627207830600338134 ) ) ;
#10552=CARTESIAN_POINT ( 'NONE',  ( 112.6828081442453282, -7.893985811506177619, -18.51759400769804742 ) ) ;
#10557=DIRECTION ( 'NONE',  ( -1.000000000000000000, 0.000000000000000000, 0.000000000000000000 ) ) ;
#10558=CARTESIAN_POINT ( 'NONE',  ( 115.2922348109119781, 0.4262465694468514643, -12.03445270309931736 ) ) ;
#10559=CARTESIAN_POINT ( 'NONE',  ( 126.0135748109119902, -1.833838273342660141, -17.42832698103878286 ) ) ;
#10562=CARTESIAN_POINT ( 'NONE',  ( 119.9438214775786378, -2.084020599724406786, -8.691656652584148546 ) ) ;
#10563=PRODUCT_DEFINITION_CONTEXT ( 'detailed design', #9054, 'design' ) ;
#10564=CARTESIAN_POINT ( 'NONE',  ( 118.7525614775786380, -1.833838273342659253, -17.42832698103878286 ) ) ;
#10565=CARTESIAN_POINT ( 'NONE',  ( 112.6260814775786514, -0.8288870151387760510, -10.36305467784173118 ) ) ;
#10568=CARTESIAN_POINT ( 'NONE',  ( 124.0848681442452772, -5.574606645277164318, -18.38911715685844683 ) ) ;
#10570=CARTESIAN_POINT ( 'NONE',  ( 112.8529881442453160, -7.894159318335828068, -9.358103419637847864 ) ) ;
#10576=CARTESIAN_POINT ( 'NONE',  ( 118.3554748109119998, -9.565557343593413364, -10.61323700422348004 ) ) ;
#10577=CARTESIAN_POINT ( 'NONE',  ( 112.0020881442453344, -9.565557343593413364, -10.61323700422348004 ) ) ;
#10581=CARTESIAN_POINT ( 'NONE',  ( 112.1533811237171534, -8.920124835228172344, -16.36603124229645090 ) ) ;
#10586=CARTESIAN_POINT ( 'NONE',  ( 112.7395348109119766, -5.638512984488999180, -18.83840828888717311 ) ) ;
#10587=CARTESIAN_POINT ( 'NONE',  ( 121.5321681442453183, -0.1624402480850797581, -16.17319339645315424 ) ) ;
#10588=CARTESIAN_POINT ( 'NONE',  ( 119.2063748109119814, -7.894159318335828068, -9.358103419637847864 ) ) ;
#10592=CARTESIAN_POINT ( 'NONE',  ( 117.3911214775786505, -7.894159318335828068, -9.358103419637847864 ) ) ;
#10593=CARTESIAN_POINT ( 'NONE',  ( 125.5030348109119558, -6.222761293078241884, -8.102969835052219238 ) ) ;
#10594=CARTESIAN_POINT ( 'NONE',  ( 125.1573330740870489, -1.286148409757067679, -16.90866798357478729 ) ) ;
#10596=CARTESIAN_POINT ( 'NONE',  ( 114.7816948109119863, 0.5811942927096154232, -14.16772938898807155 ) ) ;
#10598=CARTESIAN_POINT ( 'NONE',  ( 113.9875214775786532, -0.4660016031367893996, -10.09054647747474043 ) ) ;
#10601=CARTESIAN_POINT ( 'NONE',  ( 114.0442481442453300, -1.834011780172310813, -8.268836392978581529 ) ) ;
#10602=ADVANCED_FACE ( 'NONE', ( #32245 ), #17643, .T. ) ;
#10603=CARTESIAN_POINT ( 'NONE',  ( 114.6115148109119986, -3.383040157471821630, -19.15922257007629170 ) ) ;
#10604=CARTESIAN_POINT ( 'NONE',  ( 123.1205148109119563, -7.643976991954077427, -18.09477374809248928 ) ) ;
#10607=CARTESIAN_POINT ( 'NONE',  ( 117.2209414775786485, -7.893985811506194494, -18.51759400769804031 ) ) ;
#10609=CARTESIAN_POINT ( 'NONE',  ( 118.3554748109119998, -9.565557343593413364, -10.61323700422348004 ) ) ;
#10614=CARTESIAN_POINT ( 'NONE',  ( 125.5030348109119558, -3.383040157471821630, -19.15922257007629170 ) ) ;
#10617=CARTESIAN_POINT ( 'NONE',  ( 121.8158014775786171, -5.638512984488999180, -18.83840828888717311 ) ) ;
#10618=CARTESIAN_POINT ( 'NONE',  ( 115.4624148109119943, -5.638512984488999180, -18.83840828888717311 ) ) ;
#10621=CARTESIAN_POINT ( 'NONE',  ( 116.3133148109120043, -2.084020599724406786, -8.691656652584148546 ) ) ;
#10622=CARTESIAN_POINT ( 'NONE',  ( 123.2906948109119867, -8.166667518702819706, -8.995218007635861213 ) ) ;
#10623=CARTESIAN_POINT ( 'NONE',  ( 117.6180281442453150, -0.4660016031367893996, -10.09054647747474043 ) ) ;
#10624=CARTESIAN_POINT ( 'NONE',  ( 114.4980614775786734, -2.084020599724406786, -8.691656652584148546 ) ) ;
#10625=EDGE_LOOP ( 'NONE', ( #22534, #22242, #7634, #25651 ) ) ;
#10626=CARTESIAN_POINT ( 'NONE',  ( 121.4754414775786131, -1.833838273342659697, -17.42832698103878286 ) ) ;
#10627=CARTESIAN_POINT ( 'NONE',  ( 117.2209414775786485, -7.893985811506177619, -18.51759400769804742 ) ) ;
#10628=CARTESIAN_POINT ( 'NONE',  ( 137.5120057812997629, 0.07598602772913314041, -14.15343988704196043 ) ) ;
#10633=CARTESIAN_POINT ( 'NONE',  ( 113.4202548109119846, -10.30919188438810075, -12.61870101168855918 ) ) ;
#10635=CARTESIAN_POINT ( 'NONE',  ( 136.5847729262740415, -10.54478413941382620, -13.96952502453041944 ) ) ;
#10636=CARTESIAN_POINT ( 'NONE',  ( 113.1933481442453058, -5.574606645277164318, -18.38911715685844683 ) ) ;
#10639=CARTESIAN_POINT ( 'NONE',  ( 122.8560864091100768, -0.9924539043446216624, -17.29976612834909133 ) ) ;
#10641=CARTESIAN_POINT ( 'NONE',  ( 118.0151148109119816, -10.63000616557722466, -14.87417383870573495 ) ) ;
#10645=CARTESIAN_POINT ( 'NONE',  ( 123.1205148109119563, -7.643976991954077427, -18.09477374809248928 ) ) ;
#10646=CARTESIAN_POINT ( 'NONE',  ( 120.9649014775786355, -6.222761293078241884, -8.102969835052219238 ) ) ;
#10649=CARTESIAN_POINT ( 'NONE',  ( 121.7023481442452777, -9.261995988541697145, -16.69588392320189030 ) ) ;
#10651=CARTESIAN_POINT ( 'NONE',  ( 116.6536748109119941, -10.15424416112533912, -14.75197769757731336 ) ) ;
#10652=CARTESIAN_POINT ( 'NONE',  ( 114.3846081442453197, 0.4262465694468514643, -12.03445270309931736 ) ) ;
#10655=CARTESIAN_POINT ( 'NONE',  ( 119.8870948109119752, -0.8288870151387760510, -10.36305467784173118 ) ) ;
#10656=CARTESIAN_POINT ( 'NONE',  ( 122.0427081442452817, -9.859900752359378018, -12.68260735090039759 ) ) ;
#10659=CYLINDRICAL_SURFACE ( 'NONE', #12897, 5.999999999999997335 ) ;
#10666=CARTESIAN_POINT ( 'NONE',  ( 112.2289948109119848, -1.834011780172310813, -8.268836392978581529 ) ) ;
#10667=CARTESIAN_POINT ( 'NONE',  ( 115.2355081442453155, -10.30919188438810075, -12.61870101168855918 ) ) ;
#10669=CARTESIAN_POINT ( 'NONE',  ( 138.2184548109119930, -10.44474571748257041, -15.59668151425567650 ) ) ;
#10672=CARTESIAN_POINT ( 'NONE',  ( 122.7801548109119665, -3.383040157471821630, -19.15922257007629170 ) ) ;
#10673=CARTESIAN_POINT ( 'NONE',  ( 114.6115148109119986, -3.383040157471821630, -19.15922257007629170 ) ) ;
#10674=CARTESIAN_POINT ( 'NONE',  ( 123.2339681442453241, -3.505236298600246325, -18.68346056562440793 ) ) ;
#10676=CARTESIAN_POINT ( 'NONE',  ( 124.0848681442452772, -4.089484607189486809, -7.948022111789456723 ) ) ;
#10677=CARTESIAN_POINT ( 'NONE',  ( 118.6391081442452986, -4.089484607189486809, -7.948022111789456723 ) ) ;
#10680=CARTESIAN_POINT ( 'NONE',  ( 113.8740681442453138, -9.859900752359374465, -12.68260735090039404 ) ) ;
#10683=CARTESIAN_POINT ( 'NONE',  ( 121.1350814775786233, 0.5811942927096110934, -14.16772938898807510 ) ) ;
#10686=CARTESIAN_POINT ( 'NONE',  ( 116.1431348109119881, -10.30919188438810075, -12.61870101168855918 ) ) ;
#10689=CARTESIAN_POINT ( 'NONE',  ( 125.0492214775786266, -6.344957434206665248, -7.627207830600338134 ) ) ;
#10691=CARTESIAN_POINT ( 'NONE',  ( 115.3489614775786407, -0.8288870151387760510, -10.36305467784173118 ) ) ;
#10693=CARTESIAN_POINT ( 'NONE',  ( 120.9649014775786355, -6.222761293078241884, -8.102969835052219238 ) ) ;
#10694=CARTESIAN_POINT ( 'NONE',  ( 111.2184548109119788, -8.862178061932382889, -16.39564131203247399 ) ) ;
#10695=CARTESIAN_POINT ( 'NONE',  ( 120.2841814775786276, -10.15424416112533912, -14.75197769757731336 ) ) ;
#10698=CARTESIAN_POINT ( 'NONE',  ( 119.2631014775786298, -9.565557343593413364, -10.61323700422348004 ) ) ;
#10699=CARTESIAN_POINT ( 'NONE',  ( 111.8886348109120092, -3.383040157471821630, -19.15922257007629170 ) ) ;
#10700=CARTESIAN_POINT ( 'NONE',  ( 117.1074881442453233, -10.63000616557722466, -14.87417383870573495 ) ) ;
#10701=CARTESIAN_POINT ( 'NONE',  ( 123.4608748109119745, -10.63000616557723355, -14.87417383870568344 ) ) ;
#10702=CARTESIAN_POINT ( 'NONE',  ( 121.8158014775786171, -4.153390946401325223, -8.397313243818185668 ) ) ;
#10704=CARTESIAN_POINT ( 'NONE',  ( 117.9583881442453048, -10.30919188438810075, -12.61870101168855918 ) ) ;
#10706=AXIS2_PLACEMENT_3D ( 'NONE', #2623, #10165, #16784 ) ;
#10711=CARTESIAN_POINT ( 'NONE',  ( 123.8012348109119642, 0.2603800115204892296, -16.42320221600525088 ) ) ;
#10713=CARTESIAN_POINT ( 'NONE',  ( 126.4536383592459146, -8.380280027055789560, -9.674679031694752851 ) ) ;
#10714=CARTESIAN_POINT ( 'NONE',  ( 119.3765548109119834, -10.15424416112533912, -14.75197769757731336 ) ) ;
#10722=CARTESIAN_POINT ( 'NONE',  ( 113.5337081442453240, -9.261995988541697145, -16.69588392320189030 ) ) ;
#10723=CARTESIAN_POINT ( 'NONE',  ( 126.6942948109119840, -8.899110576539710493, -16.42337572283490132 ) ) ;
#10724=CARTESIAN_POINT ( 'NONE',  ( 124.7088614775786226, 0.2603800115204892296, -16.42320221600525088 ) ) ;
#10725=CARTESIAN_POINT ( 'NONE',  ( 115.5191414775786569, -6.222761293078241884, -8.102969835052219238 ) ) ;
#10727=DIRECTION ( 'NONE',  ( 1.000000000000000000, 0.000000000000000000, 0.000000000000000000 ) ) ;
#10728=CARTESIAN_POINT ( 'NONE',  ( 118.6958348109119754, -6.344957434206665248, -7.627207830600338134 ) ) ;
#10730=( BOUNDED_SURFACE ( )  B_SPLINE_SURFACE ( 1, 2, ( 
 ( #20578, #21014, #10760, #37892, #31714, #3677, #38328, #6670, #37672, #483, #24437, #28307, #20356, #34457, #24223, #3236, #14171 ),
 ( #41997, #24657, #38543, #3014, #17162, #13514, #27423, #6887, #44979, #7318, #13737, #27646, #20796, #21463, #25342, #8230, #25783 ) ),
 .UNSPECIFIED., .F., .F., .T. ) 
 B_SPLINE_SURFACE_WITH_KNOTS ( ( 2, 2 ),
 ( 3, 2, 2, 2, 2, 2, 2, 2, 3 ),
 ( 0.000000000000000000, 1.000000000000000000 ),
 ( 0.000000000000000000, 0.1250000000000000000, 0.2500000000000000000, 0.3750000000000000000, 0.5000000000000000000, 0.6250000000000000000, 0.7500000000000000000, 0.8750000000000000000, 1.000000000000000000 ),
 .UNSPECIFIED. ) 
 GEOMETRIC_REPRESENTATION_ITEM ( )  RATIONAL_B_SPLINE_SURFACE ( (
 ( 1.000000000000000000, 0.9238795325112869605, 1.000000000000000000, 0.9238795325112869605, 1.000000000000000000, 0.9238795325112869605, 1.000000000000000000, 0.9238795325112869605, 1.000000000000000000, 0.9238795325112869605, 1.000000000000000000, 0.9238795325112869605, 1.000000000000000000, 0.9238795325112869605, 1.000000000000000000, 0.9238795325112869605, 1.000000000000000000),
 ( 1.000000000000000000, 0.9238795325112869605, 1.000000000000000000, 0.9238795325112869605, 1.000000000000000000, 0.9238795325112869605, 1.000000000000000000, 0.9238795325112869605, 1.000000000000000000, 0.9238795325112869605, 1.000000000000000000, 0.9238795325112869605, 1.000000000000000000, 0.9238795325112869605, 1.000000000000000000, 0.9238795325112869605, 1.000000000000000000) ) ) 
 REPRESENTATION_ITEM ( '' )  SURFACE ( )  );
#10733=CARTESIAN_POINT ( 'NONE',  ( 122.7234281442452755, -4.153390946401325223, -8.397313243818185668 ) ) ;
#10736=CARTESIAN_POINT ( 'NONE',  ( 117.5045748109119756, 0.5811942927096110934, -14.16772938898807510 ) ) ;
#10737=CARTESIAN_POINT ( 'NONE',  ( 124.0281414775786146, -7.643976991954077427, -18.09477374809248928 ) ) ;
#10738=ORIENTED_EDGE ( 'NONE', *, *, #42307, .F. ) ;
#10739=CARTESIAN_POINT ( 'NONE',  ( 121.3096769858783404, -2.378957183258601393, -17.95140958770220152 ) ) ;
#10740=CARTESIAN_POINT ( 'NONE',  ( 124.1415948109119540, -6.344957434206665248, -7.627207830600338134 ) ) ;
#10742=CARTESIAN_POINT ( 'NONE',  ( 118.9794681442453026, -0.8288870151387760510, -10.36305467784173118 ) ) ;
#10745=CARTESIAN_POINT ( 'NONE',  ( 113.5904348109119866, -7.893985811506177619, -18.51759400769804742 ) ) ;
#10746=CARTESIAN_POINT ( 'NONE',  ( 124.8223148109119762, -10.15424416112533912, -14.75197769757731336 ) ) ;
#10747=CARTESIAN_POINT ( 'NONE',  ( 120.6245414775786458, -9.988377603198960841, -10.36322818467135853 ) ) ;
#10750=CARTESIAN_POINT ( 'NONE',  ( 125.6732148109119862, 0.5811942927096110934, -14.16772938898807510 ) ) ;
#10753=CARTESIAN_POINT ( 'NONE',  ( 122.4397948109119767, -9.988377603198976828, -10.36322818467138340 ) ) ;
#10754=CARTESIAN_POINT ( 'NONE',  ( 121.7023481442452777, -9.261995988541697145, -16.69588392320189030 ) ) ;
#10755=CARTESIAN_POINT ( 'NONE',  ( 123.9146881442452894, -10.15424416112533912, -14.75197769757731336 ) ) ;
#10756=CARTESIAN_POINT ( 'NONE',  ( 121.7590748109119687, -2.084020599724406786, -8.691656652584148546 ) ) ;
#10757=CARTESIAN_POINT ( 'NONE',  ( 125.8328548109119964, -8.862178061931794915, -16.39564131203325559 ) ) ;
#10758=CARTESIAN_POINT ( 'NONE',  ( 114.4980614775786592, -7.893985811506177619, -18.51759400769804742 ) ) ;
#10760=CARTESIAN_POINT ( 'NONE',  ( 125.0386814775786490, -5.568102603701690967, -18.34339073538286513 ) ) ;
#10766=CARTESIAN_POINT ( 'NONE',  ( 126.3539348109119800, -4.153390946401325223, -8.397313243818185668 ) ) ;
#10768=CARTESIAN_POINT ( 'NONE',  ( 112.6828081442453282, -2.084020599724406786, -8.691656652584148546 ) ) ;
#10771=CARTESIAN_POINT ( 'NONE',  ( 124.8790414775786246, -0.4660016031367893996, -10.09054647747474043 ) ) ;
#10772=CARTESIAN_POINT ( 'NONE',  ( 124.4819548109119722, -7.893985811506177619, -18.51759400769804742 ) ) ;
#10774=CARTESIAN_POINT ( 'NONE',  ( 113.0231681442453322, 0.9020085738987339008, -11.91225656197089222 ) ) ;
#10779=CARTESIAN_POINT ( 'NONE',  ( 116.9940348109119839, -0.1624402480850797581, -16.17319339645315424 ) ) ;
#10780=CARTESIAN_POINT ( 'NONE',  ( 111.7184548109119788, -9.261995988541697145, -16.69588392320189030 ) ) ;
#10783=CARTESIAN_POINT ( 'NONE',  ( 122.2696148109119889, -5.574606645277164318, -18.38911715685844683 ) ) ;
#10784=CARTESIAN_POINT ( 'NONE',  ( 118.5823814775786360, -7.643976991954077427, -18.09477374809248928 ) ) ;
#10785=CARTESIAN_POINT ( 'NONE',  ( 111.8886348109120092, -6.222761293078241884, -8.102969835052219238 ) ) ;
#10787=CARTESIAN_POINT ( 'NONE',  ( 125.6732148109119862, -9.859900752359378018, -12.68260735090039759 ) ) ;
#10789=CARTESIAN_POINT ( 'NONE',  ( 113.0798948109119948, -8.899110576539710493, -16.42337572283490132 ) ) ;
#10791=CARTESIAN_POINT ( 'NONE',  ( 126.2202699136527286, -8.897422299132054846, -16.34980449512860545 ) ) ;
#10795=CARTESIAN_POINT ( 'NONE',  ( 119.3198281442452924, -9.859900752359374465, -12.68260735090039404 ) ) ;
#10797=CARTESIAN_POINT ( 'NONE',  ( 114.4413348109119823, -0.8288870151387760510, -10.36305467784173118 ) ) ;
#10800=DIRECTION ( 'NONE',  ( 1.000000000000000000, 0.000000000000000000, 0.000000000000000000 ) ) ;
#10806=CARTESIAN_POINT ( 'NONE',  ( 114.3278814775786429, -10.30919188438810075, -12.61870101168855918 ) ) ;
#10807=CARTESIAN_POINT ( 'NONE',  ( 121.5888948109119809, 0.1319031606808879209, -14.10382304977623669 ) ) ;
#10808=CARTESIAN_POINT ( 'NONE',  ( 117.3911214775786505, -7.894159318335828068, -9.358103419637847864 ) ) ;
#10809=DIRECTION ( 'NONE',  ( -1.000000000000000000, 0.000000000000000000, 0.000000000000000000 ) ) ;
#10811=CARTESIAN_POINT ( 'NONE',  ( 117.3343948109119737, -6.222761293078241884, -8.102969835052219238 ) ) ;
#10813=CARTESIAN_POINT ( 'NONE',  ( 125.1493398804576458, -1.281315077902259958, -16.91510428757999307 ) ) ;
#10815=CARTESIAN_POINT ( 'NONE',  ( 114.6115148109119986, -3.383040157471821630, -19.15922257007629170 ) ) ;
#10816=ORIENTED_EDGE ( 'NONE', *, *, #1869, .F. ) ;
#10817=CARTESIAN_POINT ( 'NONE',  ( 116.0864081442453113, -9.988377603198976828, -10.36322818467138340 ) ) ;
#10818=LINE ( 'NONE', #27930, #15245 ) ;
#10820=CARTESIAN_POINT ( 'NONE',  ( 126.0135748109119902, -1.833838273342660141, -17.42832698103878286 ) ) ;
#10821=CARTESIAN_POINT ( 'NONE',  ( 112.3991748109119868, -8.166667518702817929, -8.995218007635859436 ) ) ;
#10822=CARTESIAN_POINT ( 'NONE',  ( 122.9503348109119827, -9.859900752359378018, -12.68260735090039759 ) ) ;
#10825=EDGE_CURVE ( 'NONE', #16862, #15722, #28084, .T. ) ;
#10826=VERTEX_POINT ( 'NONE', #34885 ) ;
#10827=CARTESIAN_POINT ( 'NONE',  ( 120.5102552477523830, -1.220279397241718966, -16.99638242193886484 ) ) ;
#10829=CARTESIAN_POINT ( 'NONE',  ( 117.3343948109119737, -6.222761293078241884, -8.102969835052219238 ) ) ;
#10831=CARTESIAN_POINT ( 'NONE',  ( 122.6603829525735421, -1.111561923218657322, -17.14115599315433158 ) ) ;
#10834=CARTESIAN_POINT ( 'NONE',  ( 111.6050014775786536, 0.1319031606808879209, -14.10382304977623669 ) ) ;
#10835=CARTESIAN_POINT ( 'NONE',  ( 120.1707281442453166, -9.565557343593393824, -10.61323700422344274 ) ) ;
#10837=CARTESIAN_POINT ( 'NONE',  ( 123.4041481442452834, -10.30919188438810075, -12.61870101168855918 ) ) ;
#10838=CARTESIAN_POINT ( 'NONE',  ( 116.0864081442453113, -9.988377603198976828, -10.36322818467138340 ) ) ;
#10841=CARTESIAN_POINT ( 'NONE',  ( 116.5969481442453031, -9.859900752359374465, -12.68260735090039404 ) ) ;
#10843=CARTESIAN_POINT ( 'NONE',  ( 116.3700414775786527, -5.638512984488999180, -18.83840828888717311 ) ) ;
#10844=CARTESIAN_POINT ( 'NONE',  ( 117.7314814775786260, -5.574606645277164318, -18.38911715685844683 ) ) ;
#10846=CARTESIAN_POINT ( 'NONE',  ( 120.1707281442453166, -9.565557343593413364, -10.61323700422348004 ) ) ;
#10847=EDGE_CURVE ( 'NONE', #39689, #15722, #11255, .T. ) ;
#10848=CARTESIAN_POINT ( 'NONE',  ( 115.9162281442453235, -4.089484607189486809, -7.948022111789456723 ) ) ;
#10849=CARTESIAN_POINT ( 'NONE',  ( 136.8358652995586340, 0.6885668881867501590, -12.92874118612615497 ) ) ;
#10855=CARTESIAN_POINT ( 'NONE',  ( 126.8198326591488723, 0.4339650712495903284, -13.22324850598036328 ) ) ;
#10857=CARTESIAN_POINT ( 'NONE',  ( 115.4056881442453459, -7.893985811506177619, -18.51759400769804742 ) ) ;
#10859=CARTESIAN_POINT ( 'NONE',  ( 136.7741008876076023, -10.45032920902457363, -13.88867884707207345 ) ) ;
#10860=CARTESIAN_POINT ( 'NONE',  ( 112.4559014775786778, -0.1624402480850797581, -16.17319339645315424 ) ) ;
#10864=CARTESIAN_POINT ( 'NONE',  ( 112.7395348109119766, -4.153390946401321671, -8.397313243818183892 ) ) ;
#10868=CARTESIAN_POINT ( 'NONE',  ( 114.8951481442453115, -0.4660016031367893996, -10.09054647747474043 ) ) ;
#10870=CARTESIAN_POINT ( 'NONE',  ( 120.0572748109119772, -6.222761293078241884, -8.102969835052219238 ) ) ;
#10872=CARTESIAN_POINT ( 'NONE',  ( 136.9394333025927040, -7.157115554028094628, -8.388523816445465187 ) ) ;
#10873=CARTESIAN_POINT ( 'NONE',  ( 123.4608748109119745, -10.63000616557722466, -14.87417383870573495 ) ) ;
#10875=CARTESIAN_POINT ( 'NONE',  ( 121.1350814775786233, -9.859900752359378018, -12.68260735090039759 ) ) ;
#10876=CARTESIAN_POINT ( 'NONE',  ( 125.9568481442452850, -6.344957434206665248, -7.627207830600338134 ) ) ;
#10879=CARTESIAN_POINT ( 'NONE',  ( 118.9227414775786542, 0.4262465694468514643, -12.03445270309931736 ) ) ;
#10880=CARTESIAN_POINT ( 'NONE',  ( 118.9227414775786542, 0.4262465694468514643, -12.03445270309931736 ) ) ;
#10881=FACE_OUTER_BOUND ( 'NONE', #32444, .T. ) ;
#10886=CARTESIAN_POINT ( 'NONE',  ( 118.2987481442453088, -1.561330072975668504, -17.79121239304076951 ) ) ;
#10887=CARTESIAN_POINT ( 'NONE',  ( 116.1431348109119881, -10.30919188438810075, -12.61870101168855918 ) ) ;
#10891=CARTESIAN_POINT ( 'NONE',  ( 113.1706886996682186, -1.172797794773252189, -17.05961127468924943 ) ) ;
#10892=CARTESIAN_POINT ( 'NONE',  ( 121.9859814775786333, 0.2603800115204892296, -16.42320221600525088 ) ) ;
#10893=CARTESIAN_POINT ( 'NONE',  ( 116.6536748109119941, 0.9020085738987339008, -11.91225656197089222 ) ) ;
#10895=CARTESIAN_POINT ( 'NONE',  ( 121.1918081442452859, -10.15424416112533912, -14.75197769757731336 ) ) ;
#10897=CARTESIAN_POINT ( 'NONE',  ( 111.8886348109120092, -6.222761293078241884, -8.102969835052219238 ) ) ;
#10898=CARTESIAN_POINT ( 'NONE',  ( 123.1205148109119563, -1.834011780172310813, -8.268836392978581529 ) ) ;
#10901=CARTESIAN_POINT ( 'NONE',  ( 116.8805814775786445, -3.505236298600246325, -18.68346056562440793 ) ) ;
#10902=CARTESIAN_POINT ( 'NONE',  ( 111.4665458264767750, -1.295815253274133161, -16.89579513612386563 ) ) ;
#10903=EDGE_LOOP ( 'NONE', ( #21547, #7910, #6055, #20690, #12815 ) ) ;
#10904=CARTESIAN_POINT ( 'NONE',  ( 123.0070614775786169, 0.9020085738987339008, -11.91225656197089222 ) ) ;
#10906=CARTESIAN_POINT ( 'NONE',  ( 117.7882081442453170, -6.344957434206665248, -7.627207830600338134 ) ) ;
#10911=CARTESIAN_POINT ( 'NONE',  ( 115.4056881442453459, -2.084020599724406786, -8.691656652584148546 ) ) ;
#10912=CARTESIAN_POINT ( 'NONE',  ( 126.2184548109105435, -7.866424907533402511, -9.395035934245175469 ) ) ;
#10914=CARTESIAN_POINT ( 'NONE',  ( 121.5888948109119809, 0.1319031606808879209, -14.10382304977623669 ) ) ;
#10916=CARTESIAN_POINT ( 'NONE',  ( 120.8514481442452961, -2.084020599724406786, -8.691656652584148546 ) ) ;
#10919=CARTESIAN_POINT ( 'NONE',  ( 117.7882081442453170, -3.505236298600246325, -18.68346056562440793 ) ) ;
#10921=CARTESIAN_POINT ( 'NONE',  ( 114.9518748109119883, -1.834011780172310813, -8.268836392978581529 ) ) ;
#10923=CARTESIAN_POINT ( 'NONE',  ( 118.8092881442453290, -0.1624402480850797581, -16.17319339645315424 ) ) ;
#10925=CARTESIAN_POINT ( 'NONE',  ( 115.9162281442453235, -4.089484607189486809, -7.948022111789456723 ) ) ;
#10930=CARTESIAN_POINT ( 'NONE',  ( 122.1561614775786353, -0.4660016031367893996, -10.09054647747474043 ) ) ;
#10932=CARTESIAN_POINT ( 'NONE',  ( 126.6211808763552398, -8.557162640264039055, -9.730331182193353357 ) ) ;
#10933=CARTESIAN_POINT ( 'NONE',  ( 121.6456214775786293, 0.4262465694468514643, -12.03445270309931736 ) ) ;
#10939=ORIENTED_EDGE ( 'NONE', *, *, #4208, .T. ) ;
#10940=CARTESIAN_POINT ( 'NONE',  ( 115.9162281442453235, -4.089484607189486809, -7.948022111789456723 ) ) ;
#10941=CARTESIAN_POINT ( 'NONE',  ( 124.5954081442453116, -6.222761293078241884, -8.102969835052219238 ) ) ;
#10942=CARTESIAN_POINT ( 'NONE',  ( 123.3474214775786209, -9.988377603198976828, -10.36322818467138340 ) ) ;
#10943=CARTESIAN_POINT ( 'NONE',  ( 117.1642148109119859, -0.8288870151387760510, -10.36305467784173118 ) ) ;
#10944=CARTESIAN_POINT ( 'NONE',  ( 112.1722681442453222, -8.899110576539710493, -16.42337572283490132 ) ) ;
#10946=CARTESIAN_POINT ( 'NONE',  ( 122.7801548109119665, -3.383040157471821630, -19.15922257007629170 ) ) ;
#10950=CARTESIAN_POINT ( 'NONE',  ( 125.7866681442452688, -8.899110576539710493, -16.42337572283490132 ) ) ;
#10954=CARTESIAN_POINT ( 'NONE',  ( 118.8660148109119774, -10.30919188438810075, -12.61870101168855918 ) ) ;
#10955=CARTESIAN_POINT ( 'NONE',  ( 124.5386814775786206, -4.153390946401325223, -8.397313243818185668 ) ) ;
#10956=ORIENTED_EDGE ( 'NONE', *, *, #7187, .T. ) ;
#10957=CARTESIAN_POINT ( 'NONE',  ( 137.0134976903448774, 0.07479499832984452812, -11.07881363349517301 ) ) ;
#10958=CARTESIAN_POINT ( 'NONE',  ( 122.6667014775786413, -7.893985811506177619, -18.51759400769804742 ) ) ;
#10960=CARTESIAN_POINT ( 'NONE',  ( 120.7947214775786193, -0.8288870151387760510, -10.36305467784173118 ) ) ;
#10963=CARTESIAN_POINT ( 'NONE',  ( 115.5758681442453053, -1.561330072975668060, -17.79121239304076951 ) ) ;
#10967=CARTESIAN_POINT ( 'NONE',  ( 120.8514481442452961, -7.893985811506198047, -18.51759400769803676 ) ) ;
#10968=CARTESIAN_POINT ( 'NONE',  ( 138.2184548109119930, -9.609004340414083245, -9.721032963308941177 ) ) ;
#10969=CARTESIAN_POINT ( 'NONE',  ( 125.1059481442452750, -8.166667518702819706, -8.995218007635861213 ) ) ;
#10972=CARTESIAN_POINT ( 'NONE',  ( 124.0848681442452772, -4.089484607189486809, -7.948022111789456723 ) ) ;
#10973=CARTESIAN_POINT ( 'NONE',  ( 123.7445081442452874, -1.561330072975668948, -17.79121239304076951 ) ) ;
#10974=CARTESIAN_POINT ( 'NONE',  ( 123.6877814775786533, -6.222761293078241884, -8.102969835052219238 ) ) ;
#10975=CARTESIAN_POINT ( 'NONE',  ( 119.7169148109119874, -0.1624402480850797581, -16.17319339645315424 ) ) ;
#10976=CARTESIAN_POINT ( 'NONE',  ( 114.4413348109119823, -9.261995988541697145, -16.69588392320189030 ) ) ;
#10986=CARTESIAN_POINT ( 'NONE',  ( 138.2184548109119930, 1.087851763053662602, -12.63461456455805276 ) ) ;
#10987=CARTESIAN_POINT ( 'NONE',  ( 112.2289948109119848, -1.834011780172310813, -8.268836392978581529 ) ) ;
#10989=CARTESIAN_POINT ( 'NONE',  ( 114.7249681442453237, -9.565557343593413364, -10.61323700422348004 ) ) ;
#10991=CARTESIAN_POINT ( 'NONE',  ( 118.8660148109119774, 0.1319031606808853119, -14.10382304977625800 ) ) ;
#10994=CARTESIAN_POINT ( 'NONE',  ( 124.5386814775786206, -5.638512984488999180, -18.83840828888717311 ) ) ;
#10996=CARTESIAN_POINT ( 'NONE',  ( 117.5045748109119756, 0.5811942927096110934, -14.16772938898807510 ) ) ;
#11001=CIRCLE ( 'NONE', #15386, 3.499999999999998668 ) ;
#11002=CARTESIAN_POINT ( 'NONE',  ( 115.5758681442453053, -7.894159318335828068, -9.358103419637847864 ) ) ;
#11003=CARTESIAN_POINT ( 'NONE',  ( 114.1009748109119784, -4.089484607189486809, -7.948022111789456723 ) ) ;
#11006=CARTESIAN_POINT ( 'NONE',  ( 118.2987481442453088, -7.894159318335806752, -9.358103419637831877 ) ) ;
#11007=CARTESIAN_POINT ( 'NONE',  ( 118.2987481442453088, -7.894159318335828068, -9.358103419637847864 ) ) ;
#11008=CARTESIAN_POINT ( 'NONE',  ( 126.0703014775786102, -9.988377603198980381, -10.36322818467138518 ) ) ;
#11012=CARTESIAN_POINT ( 'NONE',  ( 113.5337081442453240, -0.8288870151387760510, -10.36305467784173118 ) ) ;
#11014=CARTESIAN_POINT ( 'NONE',  ( 126.7702028005465422, -9.551180355136843048, -15.81524199167786193 ) ) ;
#11017=CARTESIAN_POINT ( 'NONE',  ( 124.5954081442453116, -6.222761293078241884, -8.102969835052219238 ) ) ;
#11020=CARTESIAN_POINT ( 'NONE',  ( 119.0929214775786278, -4.153390946401325223, -8.397313243818185668 ) ) ;
#11022=CARTESIAN_POINT ( 'NONE',  ( 115.6893214775786447, -9.859900752359374465, -12.68260735090039404 ) ) ;
#11031=CARTESIAN_POINT ( 'NONE',  ( 112.7395348109119766, -5.638512984488999180, -18.83840828888717311 ) ) ;
#11032=CARTESIAN_POINT ( 'NONE',  ( 117.9016614775786280, -0.1624402480850797581, -16.17319339645315424 ) ) ;
#11035=CARTESIAN_POINT ( 'NONE',  ( 115.1220548109119761, -1.833838273342658809, -17.42832698103878286 ) ) ;
#11038=CARTESIAN_POINT ( 'NONE',  ( 114.6682414775786469, -1.561330072975668060, -17.79121239304076596 ) ) ;
#11040=CARTESIAN_POINT ( 'NONE',  ( 115.6893214775786447, 0.5811942927096154232, -14.16772938898807155 ) ) ;
#11043=CARTESIAN_POINT ( 'NONE',  ( 113.7606148109119886, -1.561330072975668060, -17.79121239304076596 ) ) ;
#11044=CARTESIAN_POINT ( 'NONE',  ( 113.6471614775786492, -5.638512984488999180, -18.83840828888717311 ) ) ;
#11045=CARTESIAN_POINT ( 'NONE',  ( 126.5041214912230032, -10.00604656586921593, -13.30322242015582823 ) ) ;
#11052=CARTESIAN_POINT ( 'NONE',  ( 116.0296814775786345, -1.833838273342658809, -17.42832698103878286 ) ) ;
#11057=CARTESIAN_POINT ( 'NONE',  ( 115.3489614775786407, -0.8288870151387760510, -10.36305467784173118 ) ) ;
#11059=CARTESIAN_POINT ( 'NONE',  ( 125.5030348109119558, -3.383040157471821630, -19.15922257007629170 ) ) ;
#11061=CARTESIAN_POINT ( 'NONE',  ( 116.7104014775786425, -0.4660016031367893996, -10.09054647747474043 ) ) ;
#11063=CARTESIAN_POINT ( 'NONE',  ( 113.3635281442453504, -0.1624402480850797581, -16.17319339645315424 ) ) ;
#11064=CARTESIAN_POINT ( 'NONE',  ( 111.8886348109120092, -3.383040157471821630, -19.15922257007629170 ) ) ;
#11065=CARTESIAN_POINT ( 'NONE',  ( 117.2209414775786485, -7.893985811506177619, -18.51759400769804742 ) ) ;
#11066=CARTESIAN_POINT ( 'NONE',  ( 116.0296814775786345, -1.833838273342658809, -17.42832698103878286 ) ) ;
#11068=CARTESIAN_POINT ( 'NONE',  ( 120.3976348109119812, -7.643976991954077427, -18.09477374809248928 ) ) ;
#11069=CARTESIAN_POINT ( 'NONE',  ( 118.5256548109119876, -0.4660016031367893996, -10.09054647747474043 ) ) ;
#11070=CARTESIAN_POINT ( 'NONE',  ( 136.7439301332540538, 0.3743339856268463883, -15.44589132379487317 ) ) ;
#11073=CARTESIAN_POINT ( 'NONE',  ( 126.8093656611956845, 0.4289529172945278357, -13.23035857857622766 ) ) ;
#11075=B_SPLINE_CURVE_WITH_KNOTS ( 'NONE', 3,
 ( #44096, #41363, #13307, #27441, #37912, #23113, #2345, #37458, #36990, #33568 ),
 .UNSPECIFIED., .F., .F.,
 ( 4, 3, 3, 4 ),
 ( 0.000000000000000000, 0.0001671877548681235048, 0.0003343755096277615233, 0.0006463528481650619413 ),
 .UNSPECIFIED. ) ;
#11077=CARTESIAN_POINT ( 'NONE',  ( 113.3068014775786594, -8.166667518702817929, -8.995218007635859436 ) ) ;
#11079=CARTESIAN_POINT ( 'NONE',  ( 115.0653281442453277, -3.505236298600246325, -18.68346056562440793 ) ) ;
#11084=CARTESIAN_POINT ( 'NONE',  ( 114.2711548109119803, -0.1624402480850797581, -16.17319339645315424 ) ) ;
#11087=CARTESIAN_POINT ( 'NONE',  ( 125.1733191598100916, -1.295815253274133161, -16.89579513612386563 ) ) ;
#11089=CARTESIAN_POINT ( 'NONE',  ( 119.4332814775786318, -0.4660016031367893996, -10.09054647747474043 ) ) ;
#11090=CARTESIAN_POINT ( 'NONE',  ( 125.1626748109119802, -0.1624402480850797581, -16.17319339645315424 ) ) ;
#11091=CARTESIAN_POINT ( 'NONE',  ( 120.6245414775786458, -0.1624402480850797581, -16.17319339645315424 ) ) ;
#11092=CARTESIAN_POINT ( 'NONE',  ( 112.0588148109119828, -9.859900752359374465, -12.68260735090039404 ) ) ;
#11094=CARTESIAN_POINT ( 'NONE',  ( 137.2618751060991258, -7.298444271412085627, -8.736063270064514441 ) ) ;
#11095=CARTESIAN_POINT ( 'NONE',  ( 121.7590748109119687, -7.893985811506177619, -18.51759400769804742 ) ) ;
#11097=CARTESIAN_POINT ( 'NONE',  ( 120.3976348109119812, -7.643976991954077427, -18.09477374809248928 ) ) ;
#11098=CARTESIAN_POINT ( 'NONE',  ( 117.0507614775786465, 0.1319031606808879209, -14.10382304977623669 ) ) ;
#11101=CARTESIAN_POINT ( 'NONE',  ( 118.5823814775786360, -7.643976991954077427, -18.09477374809248928 ) ) ;
#11102=CARTESIAN_POINT ( 'NONE',  ( 125.5597614775786326, -7.894159318335828068, -9.358103419637847864 ) ) ;
#11109=CARTESIAN_POINT ( 'NONE',  ( 117.9016614775786280, -9.988377603198976828, -10.36322818467138340 ) ) ;
#11110=CARTESIAN_POINT ( 'NONE',  ( 114.2144281442453178, -8.166667518702817929, -8.995218007635859436 ) ) ;
#11112=CARTESIAN_POINT ( 'NONE',  ( 111.7751814775786556, -7.893985811506177619, -18.51759400769804742 ) ) ;
#11113=ADVANCED_FACE ( 'NONE', ( #8671 ), #32800, .T. ) ;
#11117=CARTESIAN_POINT ( 'NONE',  ( 124.3685014775786328, -10.63000616557722466, -14.87417383870573495 ) ) ;
#11119=CARTESIAN_POINT ( 'NONE',  ( 117.5045748109119756, 0.5811942927096110934, -14.16772938898807510 ) ) ;
#11120=CARTESIAN_POINT ( 'NONE',  ( 120.6812681442452941, 0.1319031606808879209, -14.10382304977623669 ) ) ;
#11121=CARTESIAN_POINT ( 'NONE',  ( 125.5030348109119558, -3.383040157471821630, -19.15922257007629170 ) ) ;
#11122=CARTESIAN_POINT ( 'NONE',  ( 123.0070614775786169, 0.9020085738987339008, -11.91225656197089222 ) ) ;
#11125=CARTESIAN_POINT ( 'NONE',  ( 116.5402214775786405, -9.565557343593413364, -10.61323700422348004 ) ) ;
#11128=CARTESIAN_POINT ( 'NONE',  ( 120.5110881442453206, -6.344957434206665248, -7.627207830600338134 ) ) ;
#11130=CARTESIAN_POINT ( 'NONE',  ( 117.9016614775786280, -9.988377603198976828, -10.36322818467138340 ) ) ;
#11135=CARTESIAN_POINT ( 'NONE',  ( 114.3846081442453197, 0.4262465694468514643, -12.03445270309931736 ) ) ;
#11137=CARTESIAN_POINT ( 'NONE',  ( 123.8818742721482664, -2.287189184988711155, -18.07361239780447448 ) ) ;
#11138=CARTESIAN_POINT ( 'NONE',  ( 121.6456214775786293, 0.4262465694468514643, -12.03445270309931736 ) ) ;
#11139=CARTESIAN_POINT ( 'NONE',  ( 121.0890424739651507, 0.3208234527006196823, -15.99825685930876595 ) ) ;
#11141=CARTESIAN_POINT ( 'NONE',  ( 121.9859814775786333, -9.565557343593413364, -10.61323700422348004 ) ) ;
#11144=CARTESIAN_POINT ( 'NONE',  ( 119.1496481442453046, -6.222761293078241884, -8.102969835052219238 ) ) ;
#11145=CARTESIAN_POINT ( 'NONE',  ( 114.0442481442453300, -1.834011780172310813, -8.268836392978581529 ) ) ;
#11146=CARTESIAN_POINT ( 'NONE',  ( 119.3765548109119834, 0.9020085738987339008, -11.91225656197089222 ) ) ;
#11147=CARTESIAN_POINT ( 'NONE',  ( 112.6828081442453282, -7.893985811506177619, -18.51759400769804742 ) ) ;
#11149=CARTESIAN_POINT ( 'NONE',  ( 120.9649014775786355, -6.222761293078241884, -8.102969835052219238 ) ) ;
#11151=CARTESIAN_POINT ( 'NONE',  ( 117.4478481442453131, 0.2603800115204892296, -16.42320221600525088 ) ) ;
#11157=CARTESIAN_POINT ( 'NONE',  ( 122.2696148109119889, -4.089484607189486809, -7.948022111789456723 ) ) ;
#11159=CARTESIAN_POINT ( 'NONE',  ( 126.3444272079758406, -8.232969492540654244, -9.613686683291632562 ) ) ;
#11160=CARTESIAN_POINT ( 'NONE',  ( 121.4187148109119789, -3.505236298600246325, -18.68346056562440793 ) ) ;
#11164=CARTESIAN_POINT ( 'NONE',  ( 126.0135748109119902, -8.166667518702819706, -8.995218007635861213 ) ) ;
#11167=CARTESIAN_POINT ( 'NONE',  ( 115.7460481442453357, 0.9020085738987339008, -11.91225656197089222 ) ) ;
#11168=CARTESIAN_POINT ( 'NONE',  ( 115.4056881442453459, -7.893985811506177619, -18.51759400769804742 ) ) ;
#11170=EDGE_CURVE ( 'NONE', #20392, #8490, #10539, .T. ) ;
#11171=CARTESIAN_POINT ( 'NONE',  ( 120.5678148109119832, -1.833838273342659253, -17.42832698103878286 ) ) ;
#11172=CARTESIAN_POINT ( 'NONE',  ( 126.2872529661399597, -3.846216389819564707, -8.462751213476616741 ) ) ;
#11174=CARTESIAN_POINT ( 'NONE',  ( 122.3263414775786373, -6.344957434206665248, -7.627207830600338134 ) ) ;
#11175=CARTESIAN_POINT ( 'NONE',  ( 111.4915481442453142, -1.833838273342658365, -17.42832698103878286 ) ) ;
#11176=ADVANCED_FACE ( 'NONE', ( #14401 ), #20321, .T. ) ;
#11179=CARTESIAN_POINT ( 'NONE',  ( 112.5126281442453120, -10.30919188438810075, -12.61870101168855918 ) ) ;
#11183=CARTESIAN_POINT ( 'NONE',  ( 120.6245414775786458, -9.988377603198976828, -10.36322818467138340 ) ) ;
#11186=CARTESIAN_POINT ( 'NONE',  ( 135.5886503745695677, 0.7166931025281868539, -11.18974842684922066 ) ) ;
#11187=CARTESIAN_POINT ( 'NONE',  ( 125.2761281442453054, -10.63000616557722466, -14.87417383870573495 ) ) ;
#11189=CARTESIAN_POINT ( 'NONE',  ( 123.3474214775786209, -0.1624402480850797581, -16.17319339645315424 ) ) ;
#11192=CARTESIAN_POINT ( 'NONE',  ( 113.8173414775786512, 0.2603800115204892296, -16.42320221600525088 ) ) ;
#11194=CARTESIAN_POINT ( 'NONE',  ( 112.8721930757767495, -0.9924539043446216624, -17.29976612834909133 ) ) ;
#11195=CARTESIAN_POINT ( 'NONE',  ( 111.4705635773848940, -2.467220198592768199, -17.83387418641523325 ) ) ;
#11196=CARTESIAN_POINT ( 'NONE',  ( 125.5030348109119558, -3.383040157471821630, -19.15922257007629170 ) ) ;
#11199=CARTESIAN_POINT ( 'NONE',  ( 124.6521348109119884, -1.561330072975668948, -17.79121239304076951 ) ) ;
#11200=CARTESIAN_POINT ( 'NONE',  ( 123.8579614775786126, 0.5811942927096110934, -14.16772938898807510 ) ) ;
#11201=CARTESIAN_POINT ( 'NONE',  ( 122.6667014775786413, -2.084020599724406786, -8.691656652584148546 ) ) ;
#11202=CARTESIAN_POINT ( 'NONE',  ( 121.8158014775786171, -4.153390946401325223, -8.397313243818185668 ) ) ;
#11203=B_SPLINE_CURVE_WITH_KNOTS ( 'NONE', 3,
 ( #16450, #1839, #26030, #9375, #15768, #1617, #19632, #15538, #37168, #2296 ),
 .UNSPECIFIED., .F., .F.,
 ( 4, 3, 3, 4 ),
 ( 0.000000000000000000, 0.0001671877560958130043, 0.0003343755126086615011, 0.0006438490228505480001 ),
 .UNSPECIFIED. ) ;
#11204=DIRECTION ( 'NONE',  ( 1.000000000000000000, -1.488292102367680609E-29, 1.981883451652704298E-29 ) ) ;
#11205=CARTESIAN_POINT ( 'NONE',  ( 120.5678148109119832, -8.166667518702819706, -8.995218007635861213 ) ) ;
#11208=ORIENTED_EDGE ( 'NONE', *, *, #31399, .T. ) ;
#11213=CARTESIAN_POINT ( 'NONE',  ( 125.9001214775786224, -4.089484607189486809, -7.948022111789456723 ) ) ;
#11214=CARTESIAN_POINT ( 'NONE',  ( 126.1270281442452870, 0.1319031606808879209, -14.10382304977623669 ) ) ;
#11216=CARTESIAN_POINT ( 'NONE',  ( 114.1577014775786552, -3.505236298600246325, -18.68346056562440793 ) ) ;
#11218=CARTESIAN_POINT ( 'NONE',  ( 118.8209181415389111, -0.1020945015694968705, -15.74893487844867757 ) ) ;
#11219=CARTESIAN_POINT ( 'NONE',  ( 125.6732148109119862, 0.5811942927096110934, -14.16772938898807510 ) ) ;
#11220=CARTESIAN_POINT ( 'NONE',  ( 126.1837548109119211, -10.63000616557722466, -14.87417383870573495 ) ) ;
#11222=CARTESIAN_POINT ( 'NONE',  ( 117.1074881442453233, -10.63000616557722466, -14.87417383870573495 ) ) ;
#11227=CARTESIAN_POINT ( 'NONE',  ( 113.7038881442453402, -6.222761293078241884, -8.102969835052219238 ) ) ;
#11228=CARTESIAN_POINT ( 'NONE',  ( 126.6942948109119840, -8.899110576539710493, -16.42337572283490132 ) ) ;
#11230=CARTESIAN_POINT ( 'NONE',  ( 124.0281414775786146, -7.643976991954077427, -18.09477374809248928 ) ) ;
#11231=CARTESIAN_POINT ( 'NONE',  ( 118.5256548109119876, -8.899110576539710493, -16.42337572283490132 ) ) ;
#11232=CARTESIAN_POINT ( 'NONE',  ( 115.8595014775786609, -7.643976991954077427, -18.09477374809248928 ) ) ;
#11235=CARTESIAN_POINT ( 'NONE',  ( 121.5722776481213856, -2.395992375830759524, -17.92872468182853396 ) ) ;
#11236=CARTESIAN_POINT ( 'NONE',  ( 115.9729548109119861, -3.505236298600246325, -18.68346056562440793 ) ) ;
#11237=VERTEX_POINT ( 'NONE', #36259 ) ;
#11245=CARTESIAN_POINT ( 'NONE',  ( 118.6391081442452986, -5.574606645277164318, -18.38911715685844683 ) ) ;
#11246=CARTESIAN_POINT ( 'NONE',  ( 118.9794681442453026, -0.8288870151387760510, -10.36305467784173118 ) ) ;
#11247=CARTESIAN_POINT ( 'NONE',  ( 110.5511732076914200, -2.900984314291613408, -17.25625241347383110 ) ) ;
#11253=CARTESIAN_POINT ( 'NONE',  ( 113.3635281442453504, -9.988377603198976828, -10.36322818467138340 ) ) ;
#11254=CARTESIAN_POINT ( 'NONE',  ( 124.8790414775786246, -8.899110576539710493, -16.42337572283490132 ) ) ;
#11255=( BOUNDED_CURVE ( )  B_SPLINE_CURVE ( 2, ( #27642, #7315, #10533, #24879, #21235, #14616, #41556, #17376, #31488, #38771, #17594, #7541, #10757 ),
 .UNSPECIFIED., .F., .F. ) 
 B_SPLINE_CURVE_WITH_KNOTS ( ( 3, 2, 2, 2, 2, 2, 3 ),
 ( 0.2742732506792325275, 0.3750000000000000000, 0.5000000000000000000, 0.6250000000000000000, 0.7500000000000000000, 0.8750000000000000000, 1.000000000000000222 ),
 .UNSPECIFIED. ) 
 CURVE ( )  GEOMETRIC_REPRESENTATION_ITEM ( )  RATIONAL_B_SPLINE_CURVE ( ( 0.9761776733140340445, 0.9386610620246780279, 1.000000000000000000, 0.9238795325112869605, 1.000000000000000000, 0.9238795325112869605, 1.000000000000000000, 0.9238795325112869605, 1.000000000000000000, 0.9238795325112869605, 1.000000000000000000, 0.9238795325112869605, 1.000000000000000000 ) ) 
 REPRESENTATION_ITEM ( '' )  );
#11256=CARTESIAN_POINT ( 'NONE',  ( 116.4267681442453153, -6.222761293078241884, -8.102969835052219238 ) ) ;
#11258=ORIENTED_EDGE ( 'NONE', *, *, #5890, .F. ) ;
#11259=CARTESIAN_POINT ( 'NONE',  ( 118.0151148109119816, 0.4262465694468514643, -12.03445270309931736 ) ) ;
#11264=CARTESIAN_POINT ( 'NONE',  ( 113.9875214775786532, -0.4660016031367893996, -10.09054647747474043 ) ) ;
#11265=ORIENTED_EDGE ( 'NONE', *, *, #778, .F. ) ;
#11266=CARTESIAN_POINT ( 'NONE',  ( 115.8027748109119841, -0.4660016031367893996, -10.09054647747474043 ) ) ;
#11269=CARTESIAN_POINT ( 'NONE',  ( 118.1285681442453068, -7.893985811506177619, -18.51759400769804742 ) ) ;
#11270=CARTESIAN_POINT ( 'NONE',  ( 113.9875214775786532, -0.4660016031367893996, -10.09054647747474043 ) ) ;
#11272=DIRECTION ( 'NONE',  ( -1.000000000000000000, 0.000000000000000000, 0.000000000000000000 ) ) ;
#11277=CARTESIAN_POINT ( 'NONE',  ( 116.9940348109119839, -0.1624402480850797581, -16.17319339645315424 ) ) ;
#11278=EDGE_CURVE ( 'NONE', #2634, #38747, #3882, .T. ) ;
#11282=CARTESIAN_POINT ( 'NONE',  ( 121.8310270589982309, -1.063912429576147511, -17.20460841810472985 ) ) ;
#11283=CARTESIAN_POINT ( 'NONE',  ( 114.2711548109119803, -0.1624402480850797581, -16.17319339645315424 ) ) ;
#11284=CARTESIAN_POINT ( 'NONE',  ( 120.2274548109119934, -9.859900752359374465, -12.68260735090039404 ) ) ;
#11285=CARTESIAN_POINT ( 'NONE',  ( 123.1205148109119563, -1.834011780172310813, -8.268836392978581529 ) ) ;
#11286=CARTESIAN_POINT ( 'NONE',  ( 120.1140014775786398, -1.561330072975668504, -17.79121239304076951 ) ) ;
#11288=CARTESIAN_POINT ( 'NONE',  ( 113.7606148109119886, -7.894159318335828068, -9.358103419637847864 ) ) ;
#11289=CARTESIAN_POINT ( 'NONE',  ( 112.8529881442453302, -1.561330072975668060, -17.79121239304076596 ) ) ;
#11290=CARTESIAN_POINT ( 'NONE',  ( 118.5823814775786360, -1.834011780172310813, -8.268836392978581529 ) ) ;
#11291=CARTESIAN_POINT ( 'NONE',  ( 118.0718414775786442, -0.8288870151387760510, -10.36305467784173118 ) ) ;
#11293=CARTESIAN_POINT ( 'NONE',  ( 122.7801548109119665, -6.222761293078241884, -8.102969835052219238 ) ) ;
#11294=CARTESIAN_POINT ( 'NONE',  ( 120.6245414775786458, -9.988377603198976828, -10.36322818467138340 ) ) ;
#11295=CARTESIAN_POINT ( 'NONE',  ( 137.0728789364823683, 0.5386892458729081179, -13.08566328863867056 ) ) ;
#11299=CARTESIAN_POINT ( 'NONE',  ( 126.4325107881277575, 0.2402159677550416428, -13.56302502275812039 ) ) ;
#11301=CARTESIAN_POINT ( 'NONE',  ( 116.1998614775786507, -10.63000616557722466, -14.87417383870573495 ) ) ;
#11302=CARTESIAN_POINT ( 'NONE',  ( 135.4522060580572145, -10.81582635000027359, -14.15180293287611413 ) ) ;
#11303=CARTESIAN_POINT ( 'NONE',  ( 114.1577014775786552, -3.505236298600246325, -18.68346056562440793 ) ) ;
#11307=CARTESIAN_POINT ( 'NONE',  ( 115.5084538145250406, -3.807985514183278131, -19.09877912889401941 ) ) ;
#11308=DIRECTION ( 'NONE',  ( 0.000000000000000000, 0.6004852223388323917, -0.7996358532186279566 ) ) ;
#11309=CARTESIAN_POINT ( 'NONE',  ( 126.2184548109119788, -4.863998795839242995, -13.39321520033831447 ) ) ;
#11311=CARTESIAN_POINT ( 'NONE',  ( 119.6034614775786196, -6.344957434206665248, -7.627207830600338134 ) ) ;
#11312=AXIS2_PLACEMENT_3D ( 'NONE', #19957, #19725, #16084 ) ;
#11313=CARTESIAN_POINT ( 'NONE',  ( 120.0005481442453146, -4.153390946401325223, -8.397313243818185668 ) ) ;
#11314=CARTESIAN_POINT ( 'NONE',  ( 126.0703014775786102, -9.988377603198980381, -10.36322818467138518 ) ) ;
#11316=CARTESIAN_POINT ( 'NONE',  ( 136.8611794030174735, -7.138509913861316392, -8.324458807404662153 ) ) ;
#11317=CARTESIAN_POINT ( 'NONE',  ( 123.9146881442452894, 0.9020085738987339008, -11.91225656197089222 ) ) ;
#11319=CARTESIAN_POINT ( 'NONE',  ( 117.6180281442453150, -8.899110576539710493, -16.42337572283490132 ) ) ;
#11320=CARTESIAN_POINT ( 'NONE',  ( 115.2922348109119781, 0.4262465694468514643, -12.03445270309931736 ) ) ;
#11324=CARTESIAN_POINT ( 'NONE',  ( 121.4754414775786131, -1.833838273342659697, -17.42832698103878286 ) ) ;
#11325=CARTESIAN_POINT ( 'NONE',  ( 125.1059481442452750, -1.833838273342660141, -17.42832698103878286 ) ) ;
#11326=CARTESIAN_POINT ( 'NONE',  ( 126.2184548109119788, -5.568102603702699049, -18.34339073538272302 ) ) ;
#11332=CARTESIAN_POINT ( 'NONE',  ( 119.2631014775786298, 0.2603800115204892296, -16.42320221600525088 ) ) ;
#11333=CARTESIAN_POINT ( 'NONE',  ( 118.1852948109119836, -5.638512984488999180, -18.83840828888717311 ) ) ;
#11335=CARTESIAN_POINT ( 'NONE',  ( 114.8384214775786489, 0.9020085738987339008, -11.91225656197089222 ) ) ;
#11339=CARTESIAN_POINT ( 'NONE',  ( 115.6893214775786447, 0.5811942927096154232, -14.16772938898807155 ) ) ;
#11340=CARTESIAN_POINT ( 'NONE',  ( 123.1205148109119563, -7.643976991954077427, -18.09477374809248928 ) ) ;
#11342=CARTESIAN_POINT ( 'NONE',  ( 124.1983214775786166, -8.166667518702819706, -8.995218007635861213 ) ) ;
#11343=CARTESIAN_POINT ( 'NONE',  ( 123.5176014775786228, -9.261995988541697145, -16.69588392320189030 ) ) ;
#11345=CARTESIAN_POINT ( 'NONE',  ( 116.0296814775786345, -1.833838273342658809, -17.42832698103878286 ) ) ;
#11350=B_SPLINE_CURVE_WITH_KNOTS ( 'NONE', 3,
 ( #950, #4364, #281, #39253, #8246, #14868, #38561, #4590, #42908, #28778, #11453, #14414, #21925, #18513, #28109, #8018, #28324, #42236, #11670, #35818, #32404, #24901, #21256, #1174, #14638, #39482, #502, #24674, #31952, #36046 ),
 .UNSPECIFIED., .F., .F.,
 ( 4, 2, 2, 1, 2, 2, 2, 1, 1, 2, 2, 2, 1, 1, 1, 2, 2, 4 ),
 ( 0.000000000000000000, 0.03125000000005303397, 0.06250000000010677570, 0.09375000000016052437, 0.1093750000001824374, 0.1250000000002043643, 0.1875000000002640388, 0.2187500000002932932, 0.2343750000002999823, 0.2421875000003030909, 0.2500000000003061995, 0.3750000000002949307, 0.4375000000002782219, 0.4687500000002805534, 0.4843750000002921552, 0.4921875000002978728, 0.5000000000003035350, 1.000000000000000000 ),
 .UNSPECIFIED. ) ;
#11352=CARTESIAN_POINT ( 'NONE',  ( 118.0151148109119816, -10.63000616557722466, -14.87417383870573495 ) ) ;
#11356=CARTESIAN_POINT ( 'NONE',  ( 127.7425183523502881, -7.050714571525749541, -18.72418924296322729 ) ) ;
#11358=CARTESIAN_POINT ( 'NONE',  ( 117.5045748109119756, -9.859900752359374465, -12.68260735090039404 ) ) ;
#11362=CARTESIAN_POINT ( 'NONE',  ( 119.8303681442453126, 0.4262465694468514643, -12.03445270309931736 ) ) ;
#11367=CARTESIAN_POINT ( 'NONE',  ( 122.1561614775786353, -8.899110576539710493, -16.42337572283490132 ) ) ;
#11369=CARTESIAN_POINT ( 'NONE',  ( 121.4544569107182070, -2.467220198592778413, -17.83387418641524391 ) ) ;
#11370=CARTESIAN_POINT ( 'NONE',  ( 122.3263414775786373, -3.505236298600246325, -18.68346056562440793 ) ) ;
#11371=CARTESIAN_POINT ( 'NONE',  ( 113.9875214775786532, -0.4660016031367893996, -10.09054647747474043 ) ) ;
#11372=CARTESIAN_POINT ( 'NONE',  ( 119.0361948109119652, -7.893985811506177619, -18.51759400769804742 ) ) ;
#11373=CARTESIAN_POINT ( 'NONE',  ( 125.9568481442452850, -3.505236298600246325, -18.68346056562440793 ) ) ;
#11375=CARTESIAN_POINT ( 'NONE',  ( 122.2696148109119889, -5.574606645277164318, -18.38911715685844683 ) ) ;
#11377=CARTESIAN_POINT ( 'NONE',  ( 121.5321681442453183, -9.988377603198976828, -10.36322818467138340 ) ) ;
#11381=CARTESIAN_POINT ( 'NONE',  ( 124.8223148109119762, 0.9020085738987339008, -11.91225656197089222 ) ) ;
#11385=CARTESIAN_POINT ( 'NONE',  ( 120.3409081442453044, -8.899110576539710493, -16.42337572283490132 ) ) ;
#11387=CARTESIAN_POINT ( 'NONE',  ( 111.6722681442453222, -0.8658195297461032114, -10.39078908864415496 ) ) ;
#11392=CARTESIAN_POINT ( 'NONE',  ( 115.2355081442453155, -10.30919188438810075, -12.61870101168855918 ) ) ;
#11393=CARTESIAN_POINT ( 'NONE',  ( 115.3489614775786407, -9.261995988541697145, -16.69588392320189030 ) ) ;
#11395=CARTESIAN_POINT ( 'NONE',  ( 119.8303681442453126, 0.4262465694468514643, -12.03445270309931736 ) ) ;
#11396=CARTESIAN_POINT ( 'NONE',  ( 126.9932531981140755, -3.096686212419476281, -8.303943172126736272 ) ) ;
#11397=CARTESIAN_POINT ( 'NONE',  ( 123.9146881442452894, 0.9020085738987339008, -11.91225656197089222 ) ) ;
#11398=CARTESIAN_POINT ( 'NONE',  ( 111.5482748109120053, -0.1624402480850797581, -16.17319339645315424 ) ) ;
#11403=CARTESIAN_POINT ( 'NONE',  ( 112.6828081442453282, -7.893985811506177619, -18.51759400769804742 ) ) ;
#11408=CARTESIAN_POINT ( 'NONE',  ( 118.9227414775786400, -10.63000616557722466, -14.87417383870573495 ) ) ;
#11411=CARTESIAN_POINT ( 'NONE',  ( 136.8192643132360615, 0.2368078868278960802, -11.12719817101369379 ) ) ;
#11412=CARTESIAN_POINT ( 'NONE',  ( 112.6260814775786514, -0.8288870151387760510, -10.36305467784173118 ) ) ;
#11414=CARTESIAN_POINT ( 'NONE',  ( 122.8936081442453059, -9.565557343593413364, -10.61323700422348004 ) ) ;
#11415=VERTEX_POINT ( 'NONE', #16207 ) ;
#11416=CARTESIAN_POINT ( 'NONE',  ( 116.9940348109119839, -9.988377603198976828, -10.36322818467138340 ) ) ;
#11422=CARTESIAN_POINT ( 'NONE',  ( 135.5837700375882946, -5.617920683068854615, -7.449848511264947959 ) ) ;
#11423=CARTESIAN_POINT ( 'NONE',  ( 124.5386814775786206, -5.638512984488999180, -18.83840828888717311 ) ) ;
#11424=AXIS2_PLACEMENT_3D ( 'NONE', #9655, #9203, #6230 ) ;
#11425=DIRECTION ( 'NONE',  ( 1.000000000000000000, 0.000000000000000000, 0.000000000000000000 ) ) ;
#11427=CARTESIAN_POINT ( 'NONE',  ( 123.9714148109119805, -0.4660016031367893996, -10.09054647747474043 ) ) ;
#11428=CARTESIAN_POINT ( 'NONE',  ( 122.0994348109119443, 0.9020085738987339008, -11.91225656197089222 ) ) ;
#11429=CARTESIAN_POINT ( 'NONE',  ( 122.1561614775786353, -8.899110576539710493, -16.42337572283490132 ) ) ;
#11431=CARTESIAN_POINT ( 'NONE',  ( 122.6099748109119929, -0.8288870151387760510, -10.36305467784173118 ) ) ;
#11432=CARTESIAN_POINT ( 'NONE',  ( 113.7038881442453402, -6.222761293078241884, -8.102969835052219238 ) ) ;
#11433=CARTESIAN_POINT ( 'NONE',  ( 120.3976348109119812, -1.834011780172310813, -8.268836392978581529 ) ) ;
#11440=CARTESIAN_POINT ( 'NONE',  ( 125.4357681442453156, -2.109465145233854422, -8.734689011828928429 ) ) ;
#11441=CARTESIAN_POINT ( 'NONE',  ( 113.5337081442453240, -9.261995988541697145, -16.69588392320189030 ) ) ;
#11443=CARTESIAN_POINT ( 'NONE',  ( 112.1155414775786454, -10.15424416112533912, -14.75197769757731336 ) ) ;
#11445=CARTESIAN_POINT ( 'NONE',  ( 119.3765548109119550, -10.15424416112534622, -14.75197769757730448 ) ) ;
#11449=CARTESIAN_POINT ( 'NONE',  ( 116.5402214775786405, 0.2603800115204892296, -16.42320221600525088 ) ) ;
#11453=CARTESIAN_POINT ( 'NONE',  ( 126.3230600034226967, -7.578048725806381114, -9.131528562227654078 ) ) ;
#11454=CARTESIAN_POINT ( 'NONE',  ( 119.0361948109119652, -2.084020599724406786, -8.691656652584148546 ) ) ;
#11455=CARTESIAN_POINT ( 'NONE',  ( 115.0086014775786509, -4.089484607189486809, -7.948022111789456723 ) ) ;
#11457=CARTESIAN_POINT ( 'NONE',  ( 113.6471614775786492, -5.638512984488999180, -18.83840828888717311 ) ) ;
#11458=CARTESIAN_POINT ( 'NONE',  ( 124.5954081442453116, -6.222761293078241884, -8.102969835052219238 ) ) ;
#11460=CARTESIAN_POINT ( 'NONE',  ( 119.7736414775786358, 0.1319031606808879209, -14.10382304977623669 ) ) ;
#11461=CARTESIAN_POINT ( 'NONE',  ( 115.9729548109119861, -3.505236298600246325, -18.68346056562440793 ) ) ;
#11466=CARTESIAN_POINT ( 'NONE',  ( 119.1496481442453046, -6.222761293078241884, -8.102969835052219238 ) ) ;
#11469=EDGE_CURVE ( 'NONE', #1246, #42627, #578, .T. ) ;
#11470=CARTESIAN_POINT ( 'NONE',  ( 115.8027748109119841, -0.4660016031367893996, -10.09054647747474043 ) ) ;
#11472=CARTESIAN_POINT ( 'NONE',  ( 119.2255797424434149, -0.9924539043446216624, -17.29976612834909133 ) ) ;
#11474=ORIENTED_EDGE ( 'NONE', *, *, #15835, .T. ) ;
#11475=CARTESIAN_POINT ( 'NONE',  ( 121.5321681442453183, -0.1624402480850797581, -16.17319339645315424 ) ) ;
#11476=CARTESIAN_POINT ( 'NONE',  ( 116.0864081442453113, -0.1624402480850797581, -16.17319339645315424 ) ) ;
#11483=CARTESIAN_POINT ( 'NONE',  ( 113.8740681442453138, 0.5811942927096154232, -14.16772938898807155 ) ) ;
#11484=CARTESIAN_POINT ( 'NONE',  ( 111.8886348109120092, -3.383040157471821630, -19.15922257007629170 ) ) ;
#11486=CARTESIAN_POINT ( 'NONE',  ( 119.6601881442453106, -1.833838273342659253, -17.42832698103878286 ) ) ;
#11489=CARTESIAN_POINT ( 'NONE',  ( 120.6812681442452941, 0.1319031606808879209, -14.10382304977623669 ) ) ;
#11493=CARTESIAN_POINT ( 'NONE',  ( 116.7671281442453335, -1.834011780172310813, -8.268836392978581529 ) ) ;
#11495=CARTESIAN_POINT ( 'NONE',  ( 117.7314814775786260, -4.089484607189486809, -7.948022111789456723 ) ) ;
#11498=CARTESIAN_POINT ( 'NONE',  ( 116.5402214775786405, 0.2603800115204892296, -16.42320221600525088 ) ) ;
#11499=CARTESIAN_POINT ( 'NONE',  ( 118.1852948109119836, -5.638512984488999180, -18.83840828888717311 ) ) ;
#11500=AXIS2_PLACEMENT_3D ( 'NONE', #13354, #19726, #27483 ) ;
#11501=CARTESIAN_POINT ( 'NONE',  ( 127.7617783745462816, -10.60212575679465630, -14.01825014569091366 ) ) ;
#11503=CARTESIAN_POINT ( 'NONE',  ( 128.2184548109119930, -1.191816558809784876, -8.648209655763537285 ) ) ;
#11507=CARTESIAN_POINT ( 'NONE',  ( 120.1140014775786398, -7.894159318335828068, -9.358103419637847864 ) ) ;
#11511=CARTESIAN_POINT ( 'NONE',  ( 126.2184548109108704, -4.273267060618931801, -8.426913831475415506 ) ) ;
#11512=CARTESIAN_POINT ( 'NONE',  ( 114.7249681442453237, -9.565557343593413364, -10.61323700422348004 ) ) ;
#11514=CARTESIAN_POINT ( 'NONE',  ( 124.3685014775786328, -10.63000616557722466, -14.87417383870573495 ) ) ;
#11515=CARTESIAN_POINT ( 'NONE',  ( 120.6245414775786458, -9.988377603198976828, -10.36322818467138340 ) ) ;
#11516=ORIENTED_EDGE ( 'NONE', *, *, #37597, .F. ) ;
#11517=CARTESIAN_POINT ( 'NONE',  ( 117.6180281442453150, -8.899110576539710493, -16.42337572283490132 ) ) ;
#11518=CARTESIAN_POINT ( 'NONE',  ( 112.3424481442453384, -6.344957434206662583, -7.627207830600332805 ) ) ;
#11519=CARTESIAN_POINT ( 'NONE',  ( 119.3765548109119834, 0.9020085738987339008, -11.91225656197089222 ) ) ;
#11521=CARTESIAN_POINT ( 'NONE',  ( 121.0783548109119749, -9.565557343593413364, -10.61323700422348004 ) ) ;
#11523=CARTESIAN_POINT ( 'NONE',  ( 125.4463081442452932, -4.153390946401325223, -8.397313243818185668 ) ) ;
#11524=CARTESIAN_POINT ( 'NONE',  ( 119.1496481442453046, -3.383040157471821630, -19.15922257007629170 ) ) ;
#11525=CARTESIAN_POINT ( 'NONE',  ( 137.1351618658244433, 0.2097776830087426103, -15.12324877602753048 ) ) ;
#11530=CARTESIAN_POINT ( 'NONE',  ( 116.9940348109119839, -9.988377603198976828, -10.36322818467138340 ) ) ;
#11533=CARTESIAN_POINT ( 'NONE',  ( 114.7816948109119863, -9.859900752359374465, -12.68260735090039404 ) ) ;
#11534=CARTESIAN_POINT ( 'NONE',  ( 111.7184548109119788, -9.142054238649166109, -15.98131134002176523 ) ) ;
#11541=CARTESIAN_POINT ( 'NONE',  ( 119.5467348109119712, -4.089484607189486809, -7.948022111789456723 ) ) ;
#11542=CARTESIAN_POINT ( 'NONE',  ( 119.8870948109119752, -0.8288870151387760510, -10.36305467784173118 ) ) ;
#11543=CARTESIAN_POINT ( 'NONE',  ( 114.2144281442453178, -1.833838273342658809, -17.42832698103878286 ) ) ;
#11545=CARTESIAN_POINT ( 'NONE',  ( 137.3930029278097891, -7.442204666858849293, -8.961833290247417594 ) ) ;
#11546=CARTESIAN_POINT ( 'NONE',  ( 124.1415948109119540, -6.344957434206665248, -7.627207830600338134 ) ) ;
#11548=CARTESIAN_POINT ( 'NONE',  ( 119.4900081442453086, -7.643976991954077427, -18.09477374809248928 ) ) ;
#11549=CARTESIAN_POINT ( 'NONE',  ( 115.5191414775786569, -6.222761293078241884, -8.102969835052219238 ) ) ;
#11552=CARTESIAN_POINT ( 'NONE',  ( 123.8012348109119642, -9.565557343593413364, -10.61323700422348004 ) ) ;
#11553=CARTESIAN_POINT ( 'NONE',  ( 123.4041481442452834, 0.1319031606808879209, -14.10382304977623669 ) ) ;
#11554=CARTESIAN_POINT ( 'NONE',  ( 115.0536981469516888, -3.929494816604748753, -18.62311481910882449 ) ) ;
#11561=CARTESIAN_POINT ( 'NONE',  ( 117.5613014775786525, 0.9020085738987339008, -11.91225656197089222 ) ) ;
#11562=CARTESIAN_POINT ( 'NONE',  ( 119.5467348109119712, -4.089484607189486809, -7.948022111789456723 ) ) ;
#11564=CARTESIAN_POINT ( 'NONE',  ( 112.0588148109119828, 0.5811942927096154232, -14.16772938898807155 ) ) ;
#11567=CARTESIAN_POINT ( 'NONE',  ( 117.8449348109119938, -8.166667518702817929, -8.995218007635861213 ) ) ;
#11568=CARTESIAN_POINT ( 'NONE',  ( 120.5678148109119832, -1.833838273342659253, -17.42832698103878286 ) ) ;
#11570=CARTESIAN_POINT ( 'NONE',  ( 115.5758681442453053, -7.894159318335828068, -9.358103419637847864 ) ) ;
#11571=CARTESIAN_POINT ( 'NONE',  ( 120.1707281442453166, 0.2603800115204892296, -16.42320221600525088 ) ) ;
#11574=CARTESIAN_POINT ( 'NONE',  ( 115.5191414775786569, -6.222761293078241884, -8.102969835052219238 ) ) ;
#11579=CARTESIAN_POINT ( 'NONE',  ( 121.0783548109119749, 0.2603800115204892296, -16.42320221600525088 ) ) ;
#11584=CARTESIAN_POINT ( 'NONE',  ( 116.9373081442452929, -1.833838273342659253, -17.42832698103878286 ) ) ;
#11586=CARTESIAN_POINT ( 'NONE',  ( 124.0325569858783439, -2.378957183258601393, -17.95140958770220152 ) ) ;
#11587=CARTESIAN_POINT ( 'NONE',  ( 123.6310548109119765, -4.153390946401325223, -8.397313243818185668 ) ) ;
#11589=CARTESIAN_POINT ( 'NONE',  ( 123.2906948109119867, -1.833838273342659697, -17.42832698103878286 ) ) ;
#11591=CARTESIAN_POINT ( 'NONE',  ( 123.8579614775786126, -9.859900752359378018, -12.68260735090039759 ) ) ;
#11592=CARTESIAN_POINT ( 'NONE',  ( 113.0231681442453322, 0.9020085738987339008, -11.91225656197089222 ) ) ;
#11593=CARTESIAN_POINT ( 'NONE',  ( 120.9081748109119872, -5.638512984488999180, -18.83840828888717311 ) ) ;
#11594=CARTESIAN_POINT ( 'NONE',  ( 113.5904348109119866, -7.893985811506177619, -18.51759400769804742 ) ) ;
#11596=CARTESIAN_POINT ( 'NONE',  ( 119.8303681442453126, 0.4262465694468514643, -12.03445270309931736 ) ) ;
#11598=CARTESIAN_POINT ( 'NONE',  ( 122.2128881442453263, -1.834011780172310813, -8.268836392978581529 ) ) ;
#11601=CARTESIAN_POINT ( 'NONE',  ( 112.6828081442453282, -2.084020599724406786, -8.691656652584148546 ) ) ;
#11602=CARTESIAN_POINT ( 'NONE',  ( 138.2010754744741519, -3.429981731480040708, -16.55181326108910866 ) ) ;
#11604=EDGE_LOOP ( 'NONE', ( #4833, #12764, #33845, #15935 ) ) ;
#11606=CARTESIAN_POINT ( 'NONE',  ( 119.8870948109119752, -0.8288870151387760510, -10.36305467784173118 ) ) ;
#11611=VERTEX_POINT ( 'NONE', #31220 ) ;
#11612=CARTESIAN_POINT ( 'NONE',  ( 115.4624148109119943, -5.638512984488999180, -18.83840828888717311 ) ) ;
#11614=CARTESIAN_POINT ( 'NONE',  ( 120.5110881442453206, -3.505236298600246325, -18.68346056562440793 ) ) ;
#11615=CARTESIAN_POINT ( 'NONE',  ( 127.3434826498071288, -2.860650813802300352, -8.201060023076600203 ) ) ;
#11617=CARTESIAN_POINT ( 'NONE',  ( 111.3213681442453264, -7.643976991954077427, -18.09477374809248928 ) ) ;
#11618=DIRECTION ( 'NONE',  ( 1.000000000000000000, 0.000000000000000000, 0.000000000000000000 ) ) ;
#11620=ORIENTED_EDGE ( 'NONE', *, *, #31449, .F. ) ;
#11623=CARTESIAN_POINT ( 'NONE',  ( 121.0783548109119749, 0.2603800115204892296, -16.42320221600525088 ) ) ;
#11626=CARTESIAN_POINT ( 'NONE',  ( 135.3184548109119874, 0.7167481258041168424, -11.18974888642104659 ) ) ;
#11627=CARTESIAN_POINT ( 'NONE',  ( 112.5126281442453120, 0.1319031606808879209, -14.10382304977623669 ) ) ;
#11629=CARTESIAN_POINT ( 'NONE',  ( 121.8158014775786171, -4.153390946401325223, -8.397313243818185668 ) ) ;
#11631=CARTESIAN_POINT ( 'NONE',  ( 118.0718414775786300, -9.261995988541697145, -16.69588392320189030 ) ) ;
#11634=CARTESIAN_POINT ( 'NONE',  ( 120.4543614775786295, -4.089484607189480592, -7.948022111789465605 ) ) ;
#11636=CARTESIAN_POINT ( 'NONE',  ( 125.2761281442453054, -10.63000616557722466, -14.87417383870573495 ) ) ;
#11640=CARTESIAN_POINT ( 'NONE',  ( 123.2184548109119788, -4.863998795839242995, -13.39321520033831447 ) ) ;
#11641=B_SPLINE_CURVE_WITH_KNOTS ( 'NONE', 3,
 ( #24858, #6642, #31024, #24412, #44955, #24197, #28285, #6864, #31244, #17571, #234, #13928, #27837, #31465, #3873, #38751, #18908, #21661, #25985, #8429, #1352, #18694, #36230, #43311, #11853, #42418, #35779, #25536, #38981, #28514, #25315, #39209, #32363, #1129, #25086, #8203, #36001, #4772, #25760, #15492, #28959, #14595, #4995, #12079, #7749, #39889, #35549, #22112, #39666, #4321, #29173, #29399, #8651, #22334, #18014, #35319 ),
 .UNSPECIFIED., .F., .F.,
 ( 4, 2, 2, 2, 2, 2, 2, 1, 2, 2, 2, 2, 2, 2, 2, 2, 2, 2, 2, 2, 2, 1, 2, 2, 2, 2, 2, 2, 4 ),
 ( 0.000000000000000000, 0.06249999999997815636, 0.09374999999997378486, 0.1093749999999781009, 0.1249999999999824307, 0.1875000000000227873, 0.2187500000000374145, 0.2343750000000390799, 0.2421875000000399125, 0.2500000000000407452, 0.3125000000000284772, 0.3437500000000180966, 0.3593750000000173195, 0.3750000000000165978, 0.5000000000000366374, 0.5625000000000461853, 0.5937500000000491829, 0.6093750000000490719, 0.6250000000000488498, 0.6875000000000446310, 0.7187500000000426326, 0.7343750000000419664, 0.7421875000000414113, 0.7500000000000407452, 0.8125000000000156541, 0.8437500000000029976, 0.8593750000000026645, 0.8750000000000022204, 1.000000000000000000 ),
 .UNSPECIFIED. ) ;
#11642=CARTESIAN_POINT ( 'NONE',  ( 125.3895814775786448, -7.893985811506177619, -18.51759400769804742 ) ) ;
#11644=CARTESIAN_POINT ( 'NONE',  ( 113.2500748109119968, -6.344957434206662583, -7.627207830600332805 ) ) ;
#11645=CARTESIAN_POINT ( 'NONE',  ( 123.7637130757767352, -0.9924539043446216624, -17.29976612834909133 ) ) ;
#11646=CARTESIAN_POINT ( 'NONE',  ( 122.0994348109119443, -10.15424416112533912, -14.75197769757731336 ) ) ;
#11647=CARTESIAN_POINT ( 'NONE',  ( 112.3991748109119868, -1.833838273342658809, -17.42832698103878286 ) ) ;
#11648=CARTESIAN_POINT ( 'NONE',  ( 119.2063748109119814, -1.561330072975668504, -17.79121239304076951 ) ) ;
#11656=CARTESIAN_POINT ( 'NONE',  ( 126.4852516627930612, -9.823310243116877061, -12.06768105343453179 ) ) ;
#11657=CARTESIAN_POINT ( 'NONE',  ( 115.6325948109119821, 0.2603800115204892296, -16.42320221600525088 ) ) ;
#11658=ORIENTED_EDGE ( 'NONE', *, *, #18895, .F. ) ;
#11659=CARTESIAN_POINT ( 'NONE',  ( 116.1431348109119881, 0.1319031606808879209, -14.10382304977623669 ) ) ;
#11665=CARTESIAN_POINT ( 'NONE',  ( 116.3133148109119759, -7.893985811506177619, -18.51759400769804742 ) ) ;
#11670=CARTESIAN_POINT ( 'NONE',  ( 126.5621572004118889, -7.381812952428812302, -8.875070251845482261 ) ) ;
#11671=CARTESIAN_POINT ( 'NONE',  ( 118.9794681442453026, -0.8288870151387760510, -10.36305467784173118 ) ) ;
#11672=CARTESIAN_POINT ( 'NONE',  ( 116.5969481442453031, 0.5811942927096154232, -14.16772938898807155 ) ) ;
#11673=CARTESIAN_POINT ( 'NONE',  ( 112.2289948109119848, -1.834011780172310813, -8.268836392978581529 ) ) ;
#11675=CARTESIAN_POINT ( 'NONE',  ( 124.3685014775786328, 0.4262465694468514643, -12.03445270309931736 ) ) ;
#11676=CARTESIAN_POINT ( 'NONE',  ( 122.0994348109119443, -10.15424416112533912, -14.75197769757731336 ) ) ;
#11677=CARTESIAN_POINT ( 'NONE',  ( 115.4056881442453459, -2.084020599724406786, -8.691656652584148546 ) ) ;
#11684=CARTESIAN_POINT ( 'NONE',  ( 117.7882081442453170, -3.505236298600246325, -18.68346056562440793 ) ) ;
#11686=DIRECTION ( 'NONE',  ( 0.000000000000000000, 0.6004852223388321697, -0.7996358532186279566 ) ) ;
#11687=CARTESIAN_POINT ( 'NONE',  ( 116.5402214775786405, 0.2603800115204892296, -16.42320221600525088 ) ) ;
#11690=ORIENTED_EDGE ( 'NONE', *, *, #39358, .T. ) ;
#11691=CARTESIAN_POINT ( 'NONE',  ( 123.4608748109119745, 0.4262465694468514643, -12.03445270309931736 ) ) ;
#11692=CARTESIAN_POINT ( 'NONE',  ( 118.4122014775786340, -9.859900752359374465, -12.68260735090039404 ) ) ;
#11694=CARTESIAN_POINT ( 'NONE',  ( 116.4267681442453153, -6.222761293078227673, -8.102969835052210357 ) ) ;
#11700=CARTESIAN_POINT ( 'NONE',  ( 115.5191414775786569, -3.383040157471821630, -19.15922257007629170 ) ) ;
#11701=CARTESIAN_POINT ( 'NONE',  ( 125.5597614775786326, -7.894159318335828068, -9.358103419637847864 ) ) ;
#11702=CARTESIAN_POINT ( 'NONE',  ( 120.2274548109119934, -9.859900752359378018, -12.68260735090039759 ) ) ;
#11705=CARTESIAN_POINT ( 'NONE',  ( 119.8303681442453126, 0.4262465694468514643, -12.03445270309931736 ) ) ;
#11708=CONICAL_SURFACE ( 'NONE', #1512, 1.499999999999999334, 1.249045772398253540 ) ;
#11711=CARTESIAN_POINT ( 'NONE',  ( 119.7169148109119874, -9.988377603198976828, -10.36322818467138340 ) ) ;
#11714=CARTESIAN_POINT ( 'NONE',  ( 116.7671281442453335, -1.834011780172310813, -8.268836392978581529 ) ) ;
#11715=CARTESIAN_POINT ( 'NONE',  ( 115.3367294832010543, -2.324775150319240868, -18.02356106541842351 ) ) ;
#11717=CARTESIAN_POINT ( 'NONE',  ( 115.5758681442453053, -1.561330072975668060, -17.79121239304076951 ) ) ;
#11718=CARTESIAN_POINT ( 'NONE',  ( 118.6958348109119754, -6.344957434206665248, -7.627207830600338134 ) ) ;
#11719=CARTESIAN_POINT ( 'NONE',  ( 126.3444272079794786, -9.918751065189484351, -13.10290698151034228 ) ) ;
#11725=CARTESIAN_POINT ( 'NONE',  ( 121.8158014775786171, -4.153390946401325223, -8.397313243818185668 ) ) ;
#11728=CARTESIAN_POINT ( 'NONE',  ( 115.7460481442453357, -10.15424416112533912, -14.75197769757731336 ) ) ;
#11730=CARTESIAN_POINT ( 'NONE',  ( 124.7655881442452852, 0.5811942927096110934, -14.16772938898807510 ) ) ;
#11731=B_SPLINE_CURVE_WITH_KNOTS ( 'NONE', 3,
 ( #17097, #17318, #44689, #10694 ),
 .UNSPECIFIED., .F., .F.,
 ( 4, 4 ),
 ( 0.0003857850822298949651, 0.001092701553673899872 ),
 .UNSPECIFIED. ) ;
#11732=CARTESIAN_POINT ( 'NONE',  ( 118.9227414775786400, -10.63000616557722466, -14.87417383870573495 ) ) ;
#11735=CARTESIAN_POINT ( 'NONE',  ( 118.1852948109119836, -4.153390946401325223, -8.397313243818185668 ) ) ;
#11736=CARTESIAN_POINT ( 'NONE',  ( 113.0798948109119948, -0.4660016031367893996, -10.09054647747474043 ) ) ;
#11738=CARTESIAN_POINT ( 'NONE',  ( 120.1707281442453166, 0.2603800115204892296, -16.42320221600525088 ) ) ;
#11739=CARTESIAN_POINT ( 'NONE',  ( 119.8870948109119752, -0.8288870151387760510, -10.36305467784173118 ) ) ;
#11742=CARTESIAN_POINT ( 'NONE',  ( 124.9924948109119924, -5.574606645277164318, -18.38911715685844683 ) ) ;
#11745=CARTESIAN_POINT ( 'NONE',  ( 121.1350814775786233, 0.5811942927096110934, -14.16772938898807510 ) ) ;
#11752=CARTESIAN_POINT ( 'NONE',  ( 116.7104014775786425, -8.899110576539710493, -16.42337572283490132 ) ) ;
#11753=CARTESIAN_POINT ( 'NONE',  ( 124.7655881442452852, 0.5811942927096110934, -14.16772938898807510 ) ) ;
#11755=CARTESIAN_POINT ( 'NONE',  ( 117.8239502440515452, -2.467220198592778413, -17.83387418641524391 ) ) ;
#11757=CARTESIAN_POINT ( 'NONE',  ( 115.3489614775786407, -9.261995988541700697, -16.69588392320188319 ) ) ;
#11761=CARTESIAN_POINT ( 'NONE',  ( 120.9081748109119872, -5.638512984488999180, -18.83840828888717311 ) ) ;
#11762=CARTESIAN_POINT ( 'NONE',  ( 122.6099748109119929, -0.8288870151387760510, -10.36305467784173118 ) ) ;
#11765=CARTESIAN_POINT ( 'NONE',  ( 125.5597614775786326, -1.561330072975669392, -17.79121239304076951 ) ) ;
#11768=CARTESIAN_POINT ( 'NONE',  ( 118.2987481442453088, -7.894159318335828068, -9.358103419637847864 ) ) ;
#11770=CARTESIAN_POINT ( 'NONE',  ( 120.0572748109119772, -6.222761293078241884, -8.102969835052219238 ) ) ;
#11771=CARTESIAN_POINT ( 'NONE',  ( 114.9518748109119883, -7.643976991954077427, -18.09477374809248928 ) ) ;
#11774=CARTESIAN_POINT ( 'NONE',  ( 123.6310548109119765, -4.153390946401325223, -8.397313243818185668 ) ) ;
#11776=CARTESIAN_POINT ( 'NONE',  ( 124.9357681442453014, -7.643976991954077427, -18.09477374809248928 ) ) ;
#11778=DIRECTION ( 'NONE',  ( 1.000000000000000000, 0.000000000000000000, 0.000000000000000000 ) ) ;
#11783=CARTESIAN_POINT ( 'NONE',  ( 120.6812681442452941, -10.30919188438810075, -12.61870101168855918 ) ) ;
#11784=CARTESIAN_POINT ( 'NONE',  ( 119.7169148109119874, -9.988377603198976828, -10.36322818467138340 ) ) ;
#11786=FACE_OUTER_BOUND ( 'NONE', #36950, .T. ) ;
#11787=DIRECTION ( 'NONE',  ( -1.000000000000000000, 0.000000000000000000, 0.000000000000000000 ) ) ;
#11790=CARTESIAN_POINT ( 'NONE',  ( 115.9162281442453235, -4.089484607189486809, -7.948022111789456723 ) ) ;
#11792=CARTESIAN_POINT ( 'NONE',  ( 124.5386814775786206, -4.153390946401325223, -8.397313243818185668 ) ) ;
#11794=CARTESIAN_POINT ( 'NONE',  ( 114.4413348109119823, -0.8288870151387760510, -10.36305467784173118 ) ) ;
#11795=CARTESIAN_POINT ( 'NONE',  ( 122.7801548109119665, -3.383040157471821630, -19.15922257007629170 ) ) ;
#11798=CARTESIAN_POINT ( 'NONE',  ( 118.2420214775786320, -6.222761293078241884, -8.102969835052219238 ) ) ;
#11803=CARTESIAN_POINT ( 'NONE',  ( 120.0005481442453146, -5.638512984488999180, -18.83840828888717311 ) ) ;
#11809=CARTESIAN_POINT ( 'NONE',  ( 119.8303681442453126, 0.4262465694468514643, -12.03445270309931736 ) ) ;
#11812=CARTESIAN_POINT ( 'NONE',  ( 123.3474214775786209, -0.1624402480850797581, -16.17319339645315424 ) ) ;
#11813=CARTESIAN_POINT ( 'NONE',  ( 125.7866681442453256, -8.899110576539104756, -16.42337572283570424 ) ) ;
#11814=CARTESIAN_POINT ( 'NONE',  ( 125.5597614775786326, -7.894159318335828068, -9.358103419637847864 ) ) ;
#11816=CARTESIAN_POINT ( 'NONE',  ( 116.1998614775786507, 0.4262465694468514643, -12.03445270309931736 ) ) ;
#11817=CARTESIAN_POINT ( 'NONE',  ( 122.0994348109119443, -10.15424416112533912, -14.75197769757731336 ) ) ;
#11818=CARTESIAN_POINT ( 'NONE',  ( 114.4980614775786592, -7.893985811506177619, -18.51759400769804742 ) ) ;
#11819=CARTESIAN_POINT ( 'NONE',  ( 119.2631014775786298, 0.2603800115204892296, -16.42320221600525088 ) ) ;
#11820=CARTESIAN_POINT ( 'NONE',  ( 114.7249681442453237, 0.2603800115204892296, -16.42320221600525088 ) ) ;
#11822=CARTESIAN_POINT ( 'NONE',  ( 125.2194014775786286, 0.1319031606808879209, -14.10382304977623669 ) ) ;
#11825=CARTESIAN_POINT ( 'NONE',  ( 119.0361948109119652, -7.893985811506177619, -18.51759400769804742 ) ) ;
#11828=FACE_OUTER_BOUND ( 'NONE', #34630, .T. ) ;
#11829=FACE_OUTER_BOUND ( 'NONE', #28203, .T. ) ;
#11832=CARTESIAN_POINT ( 'NONE',  ( 126.0135748109119902, -8.166667518702819706, -8.995218007635861213 ) ) ;
#11834=CARTESIAN_POINT ( 'NONE',  ( 122.4397948109119767, -0.1624402480850797581, -16.17319339645315424 ) ) ;
#11839=VERTEX_POINT ( 'NONE', #35755 ) ;
#11841=CARTESIAN_POINT ( 'NONE',  ( 113.6471614775786492, -5.638512984488999180, -18.83840828888717311 ) ) ;
#11842=CARTESIAN_POINT ( 'NONE',  ( 126.1837548109119211, -10.63000616557722466, -14.87417383870573495 ) ) ;
#11843=CARTESIAN_POINT ( 'NONE',  ( 119.3765548109119834, -10.15424416112533912, -14.75197769757731336 ) ) ;
#11845=CARTESIAN_POINT ( 'NONE',  ( 126.4852516627927912, -3.538464648936350265, -8.433903753060587150 ) ) ;
#11849=CARTESIAN_POINT ( 'NONE',  ( 125.0492214775786266, -3.505236298600246325, -18.68346056562440793 ) ) ;
#11852=CARTESIAN_POINT ( 'NONE',  ( 121.3619881442452879, -4.089484607189486809, -7.948022111789456723 ) ) ;
#11853=CARTESIAN_POINT ( 'NONE',  ( 137.2865145795265391, -8.514350784173746689, -17.13881612151974210 ) ) ;
#11854=ORIENTED_EDGE ( 'NONE', *, *, #3829, .T. ) ;
#11855=CARTESIAN_POINT ( 'NONE',  ( 115.5758681442453053, -1.561330072975668060, -17.79121239304076951 ) ) ;
#11856=CARTESIAN_POINT ( 'NONE',  ( 111.5482748109120053, -0.1624402480850797581, -16.17319339645315424 ) ) ;
#11859=CARTESIAN_POINT ( 'NONE',  ( 121.7590748109119687, -2.084020599724406786, -8.691656652584148546 ) ) ;
#11862=CARTESIAN_POINT ( 'NONE',  ( 117.5613014775786525, 0.9020085738987339008, -11.91225656197089222 ) ) ;
#11867=CARTESIAN_POINT ( 'NONE',  ( 136.7082020370459077, -5.390462347091045103, -7.772095544634614050 ) ) ;
#11868=CARTESIAN_POINT ( 'NONE',  ( 113.5904348109119866, -2.084020599724406786, -8.691656652584148546 ) ) ;
#11872=CARTESIAN_POINT ( 'NONE',  ( 125.6732148109119862, 0.5811942927096110934, -14.16772938898807510 ) ) ;
#11873=CARTESIAN_POINT ( 'NONE',  ( 113.0231681442453322, 0.9020085738987339008, -11.91225656197089222 ) ) ;
#11875=CARTESIAN_POINT ( 'NONE',  ( 123.9714148109119805, -8.899110576539710493, -16.42337572283490132 ) ) ;
#11876=CARTESIAN_POINT ( 'NONE',  ( 112.2289948109119848, -7.643976991954077427, -18.09477374809248928 ) ) ;
#11877=CARTESIAN_POINT ( 'NONE',  ( 119.2631014775786298, 0.2603800115204892296, -16.42320221600525088 ) ) ;
#11878=ORIENTED_EDGE ( 'NONE', *, *, #2319, .F. ) ;
#11883=CARTESIAN_POINT ( 'NONE',  ( 126.5621572004067872, -9.839173191191122214, -11.97876773276561302 ) ) ;
#11884=CARTESIAN_POINT ( 'NONE',  ( 113.8173414775786512, 0.2603800115204892296, -16.42320221600525088 ) ) ;
#11886=CARTESIAN_POINT ( 'NONE',  ( 116.4267681442453153, -6.222761293078241884, -8.102969835052219238 ) ) ;
#11889=CARTESIAN_POINT ( 'NONE',  ( 111.2647102085435193, -8.897589485953298905, -16.42540022429002633 ) ) ;
#11891=CARTESIAN_POINT ( 'NONE',  ( 112.2857214775786474, -4.089484607189486809, -7.948022111789456723 ) ) ;
#11892=CARTESIAN_POINT ( 'NONE',  ( 120.5678148109119832, -8.166667518702819706, -8.995218007635861213 ) ) ;
#11897=CARTESIAN_POINT ( 'NONE',  ( 118.7525614775786380, -1.833838273342659253, -17.42832698103878286 ) ) ;
#11899=CARTESIAN_POINT ( 'NONE',  ( 117.0507614775786465, -10.30919188438810075, -12.61870101168855918 ) ) ;
#11901=CARTESIAN_POINT ( 'NONE',  ( 118.1852948109119836, -4.153390946401313677, -8.397313243818183892 ) ) ;
#11902=CARTESIAN_POINT ( 'NONE',  ( 124.5954081442453116, -6.222761293078241884, -8.102969835052219238 ) ) ;
#11903=CARTESIAN_POINT ( 'NONE',  ( 116.4267681442453153, -6.222761293078241884, -8.102969835052219238 ) ) ;
#11905=EDGE_CURVE ( 'NONE', #16801, #30998, #5977, .T. ) ;
#11908=CARTESIAN_POINT ( 'NONE',  ( 121.5330010407382133, -2.419733177069661512, -17.89711025544711376 ) ) ;
#11909=CARTESIAN_POINT ( 'NONE',  ( 117.4478481442453131, -9.565557343593413364, -10.61323700422348004 ) ) ;
#11912=CARTESIAN_POINT ( 'NONE',  ( 113.6471614775786492, -5.638512984488999180, -18.83840828888717311 ) ) ;
#11915=CARTESIAN_POINT ( 'NONE',  ( 119.1081470589982274, -1.063912429576147511, -17.20460841810472985 ) ) ;
#11918=CARTESIAN_POINT ( 'NONE',  ( 122.8368814775786291, -7.894159318335828068, -9.358103419637847864 ) ) ;
#11919=CARTESIAN_POINT ( 'NONE',  ( 116.0296814775786345, -1.833838273342658809, -17.42832698103878286 ) ) ;
#11920=( BOUNDED_CURVE ( )  B_SPLINE_CURVE ( 2, ( #43121, #40553, #18507, #14862, #30060, #5033, #35812, #39701, #12737, #32397, #23222, #5876, #42678, #8240, #4808, #32622, #15083 ),
 .UNSPECIFIED., .F., .F. ) 
 B_SPLINE_CURVE_WITH_KNOTS ( ( 3, 2, 2, 2, 2, 2, 2, 2, 3 ),
 ( 0.7671282416568590001, 0.7734375000000000000, 0.7812500000000000000, 0.7890625000000000000, 0.7968750000000000000, 0.8046875000000000000, 0.8125000000000000000, 0.8203125000000000000, 0.8266217583431409999 ),
 .UNSPECIFIED. ) 
 CURVE ( )  GEOMETRIC_REPRESENTATION_ITEM ( )  RATIONAL_B_SPLINE_CURVE ( ( 0.9763430640195950305, 0.9385262470928690259, 1.000000000000000000, 0.9238795325112869605, 1.000000000000000000, 0.9238795325112869605, 1.000000000000000000, 0.9238795325112869605, 1.000000000000000000, 0.9238795325112869605, 1.000000000000000000, 0.9238795325112869605, 1.000000000000000000, 0.9238795325112869605, 1.000000000000000000, 0.9385262470928680267, 0.9763430640195970289 ) ) 
 REPRESENTATION_ITEM ( '' )  );
#11922=CARTESIAN_POINT ( 'NONE',  ( 112.1657300207295549, -8.916287984722918836, -16.39106325734287850 ) ) ;
#11926=CARTESIAN_POINT ( 'NONE',  ( 117.9583881442453048, -10.30919188438810075, -12.61870101168855918 ) ) ;
#11928=CARTESIAN_POINT ( 'NONE',  ( 116.0296814775786345, -8.166667518702817929, -8.995218007635861213 ) ) ;
#11929=CARTESIAN_POINT ( 'NONE',  ( 117.4478481442453131, -9.565557343593413364, -10.61323700422348004 ) ) ;
#11930=CARTESIAN_POINT ( 'NONE',  ( 120.5678148109119832, -1.833838273342659253, -17.42832698103878286 ) ) ;
#11935=CARTESIAN_POINT ( 'NONE',  ( 118.7525614775786380, -1.833838273342659253, -17.42832698103878286 ) ) ;
#11936=CARTESIAN_POINT ( 'NONE',  ( 123.9714148109119805, -8.899110576539710493, -16.42337572283490132 ) ) ;
#11941=CARTESIAN_POINT ( 'NONE',  ( 119.0361948109119652, -7.893985811506177619, -18.51759400769804742 ) ) ;
#11943=CARTESIAN_POINT ( 'NONE',  ( 121.3052614775786111, -1.834011780172310813, -8.268836392978581529 ) ) ;
#11946=CARTESIAN_POINT ( 'NONE',  ( 117.7314814775786260, -4.089484607189486809, -7.948022111789456723 ) ) ;
#11947=CARTESIAN_POINT ( 'NONE',  ( 119.2631014775786298, 0.2603800115204892296, -16.42320221600525088 ) ) ;
#11948=CARTESIAN_POINT ( 'NONE',  ( 125.5030348109119558, -6.222761293078241884, -8.102969835052219238 ) ) ;
#11953=CARTESIAN_POINT ( 'NONE',  ( 119.0929214775786278, -4.153390946401325223, -8.397313243818185668 ) ) ;
#11956=CARTESIAN_POINT ( 'NONE',  ( 112.6828081442453282, -2.084020599724406786, -8.691656652584148546 ) ) ;
#11959=CARTESIAN_POINT ( 'NONE',  ( 112.9097148109120070, -9.565557343593413364, -10.61323700422348004 ) ) ;
#11960=CARTESIAN_POINT ( 'NONE',  ( 120.9649014775786355, -3.383040157471821630, -19.15922257007629170 ) ) ;
#11963=CARTESIAN_POINT ( 'NONE',  ( 118.8092881442453290, -0.1624402480850797581, -16.17319339645315424 ) ) ;
#11964=CARTESIAN_POINT ( 'NONE',  ( 114.1577014775786552, -6.344957434206662583, -7.627207830600332805 ) ) ;
#11965=CARTESIAN_POINT ( 'NONE',  ( 123.0070614775786169, 0.9020085738987339008, -11.91225656197089222 ) ) ;
#11966=CARTESIAN_POINT ( 'NONE',  ( 118.9227414775786542, 0.4262465694468514643, -12.03445270309931736 ) ) ;
#11968=CARTESIAN_POINT ( 'NONE',  ( 116.2678702882355140, -1.135392229370332462, -17.10942237759954665 ) ) ;
#11971=CARTESIAN_POINT ( 'NONE',  ( 119.0361948109119652, -7.893985811506177619, -18.51759400769804742 ) ) ;
#11973=CARTESIAN_POINT ( 'NONE',  ( 121.9292548109119849, -1.561330072975668948, -17.79121239304076951 ) ) ;
#11975=CARTESIAN_POINT ( 'NONE',  ( 118.7708473908105873, -2.443475742715334853, -17.86549347949429389 ) ) ;
#11979=CARTESIAN_POINT ( 'NONE',  ( 137.5082292857753430, -9.854187482169276535, -12.96399892178506263 ) ) ;
#11980=CARTESIAN_POINT ( 'NONE',  ( 115.4624148109119943, -4.153390946401321671, -8.397313243818183892 ) ) ;
#11981=CARTESIAN_POINT ( 'NONE',  ( 124.9924948109119924, -4.089484607189486809, -7.948022111789456723 ) ) ;
#11986=CARTESIAN_POINT ( 'NONE',  ( 116.9373081442452929, -1.833838273342659253, -17.42832698103878286 ) ) ;
#11990=CARTESIAN_POINT ( 'NONE',  ( 120.9649014775786355, -3.383040157471821630, -19.15922257007629170 ) ) ;
#11991=CARTESIAN_POINT ( 'NONE',  ( 121.8158014775786171, -4.153390946401325223, -8.397313243818185668 ) ) ;
#11994=CARTESIAN_POINT ( 'NONE',  ( 125.1059481442452750, -8.166667518702819706, -8.995218007635861213 ) ) ;
#11996=CARTESIAN_POINT ( 'NONE',  ( 122.3263414775786373, -3.505236298600246325, -18.68346056562440793 ) ) ;
#11997=CARTESIAN_POINT ( 'NONE',  ( 121.8158014775786171, -4.153390946401325223, -8.397313243818185668 ) ) ;
#11998=CARTESIAN_POINT ( 'NONE',  ( 116.8238548109119819, -5.574606645277164318, -18.38911715685844683 ) ) ;
#12001=CARTESIAN_POINT ( 'NONE',  ( 123.7445081442452874, -7.894159318335828068, -9.358103419637847864 ) ) ;
#12002=CARTESIAN_POINT ( 'NONE',  ( 123.2339681442453241, -3.505236298600246325, -18.68346056562440793 ) ) ;
#12004=CARTESIAN_POINT ( 'NONE',  ( 112.7962614775786676, -6.222761293078232114, -8.102969835052212133 ) ) ;
#12010=CARTESIAN_POINT ( 'NONE',  ( 122.0994348109119443, 0.9020085738987339008, -11.91225656197089222 ) ) ;
#12011=CARTESIAN_POINT ( 'NONE',  ( 117.5045748109119756, 0.5811942927096110934, -14.16772938898807510 ) ) ;
#12013=CARTESIAN_POINT ( 'NONE',  ( 115.7460481442453357, 0.9020085738987339008, -11.91225656197089222 ) ) ;
#12018=CARTESIAN_POINT ( 'NONE',  ( 118.8092881442453290, -9.988377603198976828, -10.36322818467138340 ) ) ;
#12019=CARTESIAN_POINT ( 'NONE',  ( 112.3424481442453384, -6.344957434206662583, -7.627207830600332805 ) ) ;
#12021=CARTESIAN_POINT ( 'NONE',  ( 113.3068014775786594, -1.833838273342658809, -17.42832698103878286 ) ) ;
#12022=CARTESIAN_POINT ( 'NONE',  ( 111.7184548109119788, -0.8288870151387760510, -10.36305467784173118 ) ) ;
#12025=CARTESIAN_POINT ( 'NONE',  ( 121.7590748109119687, -2.084020599724406786, -8.691656652584148546 ) ) ;
#12031=CARTESIAN_POINT ( 'NONE',  ( 123.0637881442452937, -0.4660016031367893996, -10.09054647747474043 ) ) ;
#12036=CARTESIAN_POINT ( 'NONE',  ( 119.6034614775786196, -3.505236298600246325, -18.68346056562440793 ) ) ;
#12037=CARTESIAN_POINT ( 'NONE',  ( 111.9645664091100912, -0.9924539043446216624, -17.29976612834909133 ) ) ;
#12039=CARTESIAN_POINT ( 'NONE',  ( 124.7655881442452852, -9.859900752359378018, -12.68260735090039759 ) ) ;
#12041=CARTESIAN_POINT ( 'NONE',  ( 123.6310548109119765, -4.153390946401325223, -8.397313243818185668 ) ) ;
#12045=CARTESIAN_POINT ( 'NONE',  ( 118.1852948109119836, -4.153390946401325223, -8.397313243818185668 ) ) ;
#12046=CARTESIAN_POINT ( 'NONE',  ( 124.1983214775786166, -1.833838273342659697, -17.42832698103878286 ) ) ;
#12047=CARTESIAN_POINT ( 'NONE',  ( 119.8303681442453126, -10.63000616557722466, -14.87417383870573495 ) ) ;
#12049=CARTESIAN_POINT ( 'NONE',  ( 117.2209414775786485, -7.893985811506177619, -18.51759400769804742 ) ) ;
#12052=CARTESIAN_POINT ( 'NONE',  ( 125.7299414775786346, -10.15424416112533912, -14.75197769757731336 ) ) ;
#12054=CARTESIAN_POINT ( 'NONE',  ( 120.3976348109119812, -1.834011780172310813, -8.268836392978581529 ) ) ;
#12058=CARTESIAN_POINT ( 'NONE',  ( 113.6471614775786492, -4.153390946401321671, -8.397313243818183892 ) ) ;
#12063=CARTESIAN_POINT ( 'NONE',  ( 111.8319081442453182, -5.638512984488999180, -18.83840828888717311 ) ) ;
#12069=CARTESIAN_POINT ( 'NONE',  ( 116.5969481442453031, 0.5811942927096154232, -14.16772938898807155 ) ) ;
#12071=CARTESIAN_POINT ( 'NONE',  ( 121.5888948109119809, 0.1319031606808879209, -14.10382304977623669 ) ) ;
#12072=CARTESIAN_POINT ( 'NONE',  ( 113.8740681442453138, -9.859900752359374465, -12.68260735090039404 ) ) ;
#12075=CARTESIAN_POINT ( 'NONE',  ( 113.5904348109119866, -7.893985811506177619, -18.51759400769804742 ) ) ;
#12078=CARTESIAN_POINT ( 'NONE',  ( 122.6667014775786413, -7.893985811506177619, -18.51759400769804742 ) ) ;
#12079=CARTESIAN_POINT ( 'NONE',  ( 136.8340972670098097, -9.953648946029552746, -15.66212078552328713 ) ) ;
#12081=CARTESIAN_POINT ( 'NONE',  ( 113.1366214775786432, -1.834011780172310813, -8.268836392978581529 ) ) ;
#12082=CARTESIAN_POINT ( 'NONE',  ( 124.1983214775786166, -8.166667518702819706, -8.995218007635861213 ) ) ;
#12085=CARTESIAN_POINT ( 'NONE',  ( 123.5176014775786228, -0.8288870151387760510, -10.36305467784173118 ) ) ;
#12087=CARTESIAN_POINT ( 'NONE',  ( 119.2063748109119814, -1.561330072975668504, -17.79121239304076951 ) ) ;
#12092=CARTESIAN_POINT ( 'NONE',  ( 136.2267163768036937, -5.541130735199761403, -7.574948583682552083 ) ) ;
#12093=CARTESIAN_POINT ( 'NONE',  ( 113.4202548109119846, 0.1319031606808879209, -14.10382304977623669 ) ) ;
#12098=CARTESIAN_POINT ( 'NONE',  ( 113.5337081442453240, -0.8288870151387760510, -10.36305467784173118 ) ) ;
#12099=CARTESIAN_POINT ( 'NONE',  ( 126.6375681442452930, -10.15424416112533912, -14.75197769757731336 ) ) ;
#12101=CARTESIAN_POINT ( 'NONE',  ( 121.9859814775786333, -9.565557343593413364, -10.61323700422348004 ) ) ;
#12103=CARTESIAN_POINT ( 'NONE',  ( 118.6958348109119754, -6.344957434206665248, -7.627207830600338134 ) ) ;
#12104=CARTESIAN_POINT ( 'NONE',  ( 121.6456214775786293, -10.63000616557722466, -14.87417383870573495 ) ) ;
#12111=CARTESIAN_POINT ( 'NONE',  ( 125.6164881442453094, -9.565557343593953377, -10.61323700422440197 ) ) ;
#12112=CARTESIAN_POINT ( 'NONE',  ( 116.1998614775786507, -10.63000616557722466, -14.87417383870573495 ) ) ;
#12116=CARTESIAN_POINT ( 'NONE',  ( 115.3489614775786407, -0.8288870151387760510, -10.36305467784173118 ) ) ;
#12117=CARTESIAN_POINT ( 'NONE',  ( 112.9097148109120070, 0.2603800115204892296, -16.42320221600525088 ) ) ;
#12119=CARTESIAN_POINT ( 'NONE',  ( 120.1707281442453166, 0.2603800115204892296, -16.42320221600525088 ) ) ;
#12124=CARTESIAN_POINT ( 'NONE',  ( 117.6747548109119919, -7.643976991954077427, -18.09477374809248928 ) ) ;
#12125=CARTESIAN_POINT ( 'NONE',  ( 117.6747548109119919, -1.834011780172310813, -8.268836392978581529 ) ) ;
#12126=CARTESIAN_POINT ( 'NONE',  ( 116.5969481442453031, 0.5811942927096154232, -14.16772938898807155 ) ) ;
#12128=CARTESIAN_POINT ( 'NONE',  ( 123.9146881442452894, -10.15424416112533912, -14.75197769757731336 ) ) ;
#12129=CARTESIAN_POINT ( 'NONE',  ( 115.1220548109119761, -1.833838273342658809, -17.42832698103878286 ) ) ;
#12133=CARTESIAN_POINT ( 'NONE',  ( 113.1366214775786432, -1.834011780172310813, -8.268836392978581529 ) ) ;
#12134=CARTESIAN_POINT ( 'NONE',  ( 117.9016614775786280, -0.1624402480850797581, -16.17319339645315424 ) ) ;
#12137=CARTESIAN_POINT ( 'NONE',  ( 115.0086014775786509, -4.089484607189486809, -7.948022111789456723 ) ) ;
#12139=CARTESIAN_POINT ( 'NONE',  ( 118.8459235400977718, -1.223627541775709426, -16.99192386690442547 ) ) ;
#12143=CARTESIAN_POINT ( 'NONE',  ( 122.3830681442452857, -1.833838273342659697, -17.42832698103878286 ) ) ;
#12144=CARTESIAN_POINT ( 'NONE',  ( 119.8303681442453126, 0.4262465694468514643, -12.03445270309931736 ) ) ;
#12151=CARTESIAN_POINT ( 'NONE',  ( 114.8384214775786489, 0.9020085738987339008, -11.91225656197089222 ) ) ;
#12152=CARTESIAN_POINT ( 'NONE',  ( 114.9518748109119883, -1.834011780172310813, -8.268836392978581529 ) ) ;
#12153=CARTESIAN_POINT ( 'NONE',  ( 117.3911214775786505, -7.894159318335828068, -9.358103419637847864 ) ) ;
#12154=CARTESIAN_POINT ( 'NONE',  ( 119.9438214775786378, -2.084020599724406786, -8.691656652584148546 ) ) ;
#12157=CARTESIAN_POINT ( 'NONE',  ( 118.3554748109119998, -9.565557343593413364, -10.61323700422348004 ) ) ;
#12158=CARTESIAN_POINT ( 'NONE',  ( 124.9924948109119924, -5.574606645277164318, -18.38911715685844683 ) ) ;
#12162=CIRCLE ( 'NONE', #5606, 5.999999999999997335 ) ;
#12163=CARTESIAN_POINT ( 'NONE',  ( 120.1707281442453166, 0.2603800115204892296, -16.42320221600525088 ) ) ;
#12165=CARTESIAN_POINT ( 'NONE',  ( 120.0005481442453146, -5.638512984488999180, -18.83840828888717311 ) ) ;
#12168=CARTESIAN_POINT ( 'NONE',  ( 117.9583881442453048, -10.30919188438810075, -12.61870101168855918 ) ) ;
#12169=CARTESIAN_POINT ( 'NONE',  ( 116.8238548109119819, -4.089484607189486809, -7.948022111789456723 ) ) ;
#12170=CARTESIAN_POINT ( 'NONE',  ( 111.4241771286805260, -2.495269033102075262, -17.79652296963211455 ) ) ;
#12173=ORIENTED_EDGE ( 'NONE', *, *, #9730, .F. ) ;
#12174=DIRECTION ( 'NONE',  ( 0.000000000000000000, 0.6004852223388321697, -0.7996358532186279566 ) ) ;
#12176=CARTESIAN_POINT ( 'NONE',  ( 120.6245414775786458, -0.1624402480850797581, -16.17319339645315424 ) ) ;
#12179=CARTESIAN_POINT ( 'NONE',  ( 118.2987481442453088, -7.894159318335828068, -9.358103419637847864 ) ) ;
#12180=DIRECTION ( 'NONE',  ( 1.000000000000000000, 0.000000000000000000, 0.000000000000000000 ) ) ;
#12182=CARTESIAN_POINT ( 'NONE',  ( 112.7395348109119766, -4.153390946401321671, -8.397313243818183892 ) ) ;
#12183=CARTESIAN_POINT ( 'NONE',  ( 121.0216281442452981, -1.561330072975668948, -17.79121239304076951 ) ) ;
#12186=CARTESIAN_POINT ( 'NONE',  ( 120.2274548109119934, -9.859900752359378018, -12.68260735090039759 ) ) ;
#12187=CARTESIAN_POINT ( 'NONE',  ( 114.7249681442453237, 0.2603800115204892296, -16.42320221600525088 ) ) ;
#12188=CARTESIAN_POINT ( 'NONE',  ( 122.0994348109119443, 0.9020085738987339008, -11.91225656197089222 ) ) ;
#12189=CARTESIAN_POINT ( 'NONE',  ( 119.9438214775786378, -2.084020599724406786, -8.691656652584148546 ) ) ;
#12191=CARTESIAN_POINT ( 'NONE',  ( 116.3852670589982381, -1.063912429576147067, -17.20460841810472985 ) ) ;
#12192=( BOUNDED_CURVE ( )  B_SPLINE_CURVE ( 2, ( #493, #11218, #10991, #42452, #24893, #31944, #42675, #35355, #4131, #18051, #5030, #11445, #8684, #4580, #29885, #25790, #32395 ),
 .UNSPECIFIED., .F., .T. ) 
 B_SPLINE_CURVE_WITH_KNOTS ( ( 3, 2, 2, 2, 2, 2, 2, 2, 3 ),
 ( 0.5171282416568590001, 0.5234375000000000000, 0.5312500000000000000, 0.5390625000000000000, 0.5468750000000000000, 0.5546875000000000000, 0.5625000000000000000, 0.5703125000000000000, 0.5766217583431409999 ),
 .UNSPECIFIED. ) 
 CURVE ( )  GEOMETRIC_REPRESENTATION_ITEM ( )  RATIONAL_B_SPLINE_CURVE ( ( 0.9763430640195970289, 0.9385262470928680267, 1.000000000000000000, 0.9238795325112869605, 1.000000000000000000, 0.9238795325112869605, 1.000000000000000000, 0.9238795325112869605, 1.000000000000000000, 0.9238795325112869605, 1.000000000000000000, 0.9238795325112869605, 1.000000000000000000, 0.9238795325112869605, 1.000000000000000000, 0.9385262470928680267, 0.9763430640195970289 ) ) 
 REPRESENTATION_ITEM ( '' )  );
#12194=CARTESIAN_POINT ( 'NONE',  ( 119.3765548109119834, 0.9020085738987339008, -11.91225656197089222 ) ) ;
#12197=CARTESIAN_POINT ( 'NONE',  ( 121.1918081442452859, 0.9020085738987339008, -11.91225656197089222 ) ) ;
#12198=CARTESIAN_POINT ( 'NONE',  ( 117.3719165460472027, -2.191907684172563986, -18.20049396185734025 ) ) ;
#12200=CARTESIAN_POINT ( 'NONE',  ( 118.8493976481213821, -2.395992375830759524, -17.92872468182853396 ) ) ;
#12203=CARTESIAN_POINT ( 'NONE',  ( 135.3184548109119874, -10.36826876090623450, -11.00511718064541178 ) ) ;
#12204=CARTESIAN_POINT ( 'NONE',  ( 118.4122014775786340, -9.859900752359374465, -12.68260735090039404 ) ) ;
#12205=CARTESIAN_POINT ( 'NONE',  ( 124.7088614775786226, 0.2603800115204892296, -16.42320221600525088 ) ) ;
#12211=CARTESIAN_POINT ( 'NONE',  ( 117.4478481442453131, -9.565557343593413364, -10.61323700422348004 ) ) ;
#12212=CARTESIAN_POINT ( 'NONE',  ( 113.5214761498677376, -2.324775150319240868, -18.02356106541842351 ) ) ;
#12217=CARTESIAN_POINT ( 'NONE',  ( 124.3685014775786328, -10.63000616557722466, -14.87417383870573495 ) ) ;
#12218=CARTESIAN_POINT ( 'NONE',  ( 123.6310548109119765, -4.153390946401325223, -8.397313243818185668 ) ) ;
#12222=CARTESIAN_POINT ( 'NONE',  ( 124.5386814775786206, -4.153390946401325223, -8.397313243818185668 ) ) ;
#12224=CARTESIAN_POINT ( 'NONE',  ( 121.6456214775786293, 0.4262465694468514643, -12.03445270309931736 ) ) ;
#12225=CARTESIAN_POINT ( 'NONE',  ( 121.3619881442452879, -5.574606645277164318, -18.38911715685844683 ) ) ;
#12227=CARTESIAN_POINT ( 'NONE',  ( 120.9234003923315441, -1.063912429576147511, -17.20460841810472985 ) ) ;
#12236=CARTESIAN_POINT ( 'NONE',  ( 121.9859814775786333, 0.2603800115204892296, -16.42320221600525088 ) ) ;
#12237=CARTESIAN_POINT ( 'NONE',  ( 119.2063748109119814, -1.561330072975668504, -17.79121239304076951 ) ) ;
#12239=CARTESIAN_POINT ( 'NONE',  ( 115.6893214775786447, 0.5811942927096154232, -14.16772938898807155 ) ) ;
#12245=CARTESIAN_POINT ( 'NONE',  ( 123.4041481442452834, -10.30919188438810075, -12.61870101168855918 ) ) ;
#12246=CARTESIAN_POINT ( 'NONE',  ( 118.7525614775786380, -8.166667518702819706, -8.995218007635861213 ) ) ;
#12247=CARTESIAN_POINT ( 'NONE',  ( 125.4463081442452932, -4.153390946401325223, -8.397313243818185668 ) ) ;
#12250=CARTESIAN_POINT ( 'NONE',  ( 114.2144281442453178, -1.833838273342658809, -17.42832698103878286 ) ) ;
#12251=CARTESIAN_POINT ( 'NONE',  ( 111.6050014775786536, 0.1319031606808879209, -14.10382304977623669 ) ) ;
#12253=EDGE_CURVE ( 'NONE', #1633, #27848, #6563, .T. ) ;
#12255=CARTESIAN_POINT ( 'NONE',  ( 120.6245414775786458, -0.1624402480850797581, -16.17319339645315424 ) ) ;
#12258=EDGE_LOOP ( 'NONE', ( #41641, #8462, #12937, #3144 ) ) ;
#12260=CARTESIAN_POINT ( 'NONE',  ( 123.0070614775786169, 0.9020085738987339008, -11.91225656197089222 ) ) ;
#12265=CARTESIAN_POINT ( 'NONE',  ( 118.1285681442453068, -2.084020599724406786, -8.691656652584148546 ) ) ;
#12266=CARTESIAN_POINT ( 'NONE',  ( 112.2289948109119848, -1.834011780172310591, -8.268836392978581529 ) ) ;
#12268=CARTESIAN_POINT ( 'NONE',  ( 123.2906948109119867, -1.833838273342659697, -17.42832698103878286 ) ) ;
#12272=CARTESIAN_POINT ( 'NONE',  ( 123.1772414775786189, -4.089484607189486809, -7.948022111789456723 ) ) ;
#12273=( BOUNDED_CURVE ( )  B_SPLINE_CURVE ( 2, ( #22788, #15732, #22563, #29184, #29410, #26216, #18921, #40125, #29634, #1364, #8215, #2259, #5678 ),
 .UNSPECIFIED., .F., .T. ) 
 B_SPLINE_CURVE_WITH_KNOTS ( ( 3, 2, 2, 2, 2, 2, 3 ),
 ( 0.01712824165687044931, 0.02343750000000000000, 0.03125000000000000000, 0.03906250000000000000, 0.04687500000000000000, 0.05468750000000000000, 0.06249487795845730387 ),
 .UNSPECIFIED. ) 
 CURVE ( )  GEOMETRIC_REPRESENTATION_ITEM ( )  RATIONAL_B_SPLINE_CURVE ( ( 0.9763430640194580290, 0.9385262470929809364, 1.000000000000000000, 0.9238795325112869605, 1.000000000000000000, 0.9238795325112869605, 1.000000000000000000, 0.9238795325112869605, 1.000000000000000000, 0.9238795325112869605, 1.000000000000000000, 0.9239294387124680208, 0.9999002530367769870 ) ) 
 REPRESENTATION_ITEM ( '' )  );
#12274=CARTESIAN_POINT ( 'NONE',  ( 118.1285681442453068, -2.084020599724406786, -8.691656652584148546 ) ) ;
#12275=CARTESIAN_POINT ( 'NONE',  ( 122.8936081442453059, -9.565557343593413364, -10.61323700422348004 ) ) ;
#12276=ORIENTED_EDGE ( 'NONE', *, *, #3829, .F. ) ;
#12277=CARTESIAN_POINT ( 'NONE',  ( 121.5888948109119809, -10.30919188438810075, -12.61870101168855918 ) ) ;
#12278=CARTESIAN_POINT ( 'NONE',  ( 116.8238548109119819, -4.089484607189486809, -7.948022111789456723 ) ) ;
#12280=DIRECTION ( 'NONE',  ( -1.000000000000000000, 0.000000000000000000, 0.000000000000000000 ) ) ;
#12281=CARTESIAN_POINT ( 'NONE',  ( 125.9001214775786224, -5.574606645277164318, -18.38911715685844683 ) ) ;
#12282=CARTESIAN_POINT ( 'NONE',  ( 120.9649014775786355, -3.383040157471821630, -19.15922257007629170 ) ) ;
#12286=CARTESIAN_POINT ( 'NONE',  ( 113.4769814775786330, 0.4262465694468514643, -12.03445270309931736 ) ) ;
#12289=CARTESIAN_POINT ( 'NONE',  ( 125.3895814775786448, -2.084020599724406786, -8.691656652584148546 ) ) ;
#12296=CARTESIAN_POINT ( 'NONE',  ( 119.3198281442452924, 0.5811942927096110934, -14.16772938898807510 ) ) ;
#12298=CARTESIAN_POINT ( 'NONE',  ( 123.3474214775786209, -0.1624402480850797581, -16.17319339645315424 ) ) ;
#12299=CARTESIAN_POINT ( 'NONE',  ( 114.9518748109119883, -7.643976991954077427, -18.09477374809248928 ) ) ;
#12300=CARTESIAN_POINT ( 'NONE',  ( 116.1657942554890752, -2.372251574601226043, -17.96033910819752322 ) ) ;
#12302=CARTESIAN_POINT ( 'NONE',  ( 113.3068014775786594, -8.166667518702817929, -8.995218007635859436 ) ) ;
#12306=CARTESIAN_POINT ( 'NONE',  ( 124.4819548109119722, -7.893985811506177619, -18.51759400769804742 ) ) ;
#12310=CARTESIAN_POINT ( 'NONE',  ( 113.1933481442453058, -4.089484607189486809, -7.948022111789456723 ) ) ;
#12311=CARTESIAN_POINT ( 'NONE',  ( 113.5904348109119866, -2.084020599724406786, -8.691656652584148546 ) ) ;
#12313=CARTESIAN_POINT ( 'NONE',  ( 113.7038881442453402, -3.383040157471821630, -19.15922257007629170 ) ) ;
#12315=CARTESIAN_POINT ( 'NONE',  ( 116.3133148109119759, -7.893985811506177619, -18.51759400769804742 ) ) ;
#12318=CARTESIAN_POINT ( 'NONE',  ( 123.6089988258993202, -4.390761125357079742, -15.27237650495351495 ) ) ;
#12319=CARTESIAN_POINT ( 'NONE',  ( 113.1366214775786432, -7.643976991954077427, -18.09477374809248928 ) ) ;
#12322=CARTESIAN_POINT ( 'NONE',  ( 111.3213681442453264, -7.643976991954077427, -18.09477374809248928 ) ) ;
#12323=CARTESIAN_POINT ( 'NONE',  ( 125.5597614775786326, -7.894159318335828068, -9.358103419637847864 ) ) ;
#12326=CARTESIAN_POINT ( 'NONE',  ( 113.4769814775786330, -10.63000616557722466, -14.87417383870573495 ) ) ;
#12327=CARTESIAN_POINT ( 'NONE',  ( 112.4559014775786778, -0.1624402480850797581, -16.17319339645315424 ) ) ;
#12328=CARTESIAN_POINT ( 'NONE',  ( 122.9503348109119827, 0.5811942927096110934, -14.16772938898807510 ) ) ;
#12329=CARTESIAN_POINT ( 'NONE',  ( 122.7801548109119665, -3.383040157471821630, -19.15922257007629170 ) ) ;
#12331=CARTESIAN_POINT ( 'NONE',  ( 127.3669547543382379, -8.461095036548107018, -17.65169866057126313 ) ) ;
#12336=CARTESIAN_POINT ( 'NONE',  ( 115.6893214775786447, 0.5811942927096154232, -14.16772938898807155 ) ) ;
#12342=CARTESIAN_POINT ( 'NONE',  ( 112.6828081442453282, -2.084020599724406786, -8.691656652584148546 ) ) ;
#12344=CARTESIAN_POINT ( 'NONE',  ( 120.9081748109119872, -5.638512984488999180, -18.83840828888717311 ) ) ;
#12347=VERTEX_POINT ( 'NONE', #20370 ) ;
#12349=CARTESIAN_POINT ( 'NONE',  ( 120.5110881442453206, -3.505236298600246325, -18.68346056562440793 ) ) ;
#12350=CARTESIAN_POINT ( 'NONE',  ( 118.5256548109119876, -0.4660016031367893996, -10.09054647747474043 ) ) ;
#12351=CARTESIAN_POINT ( 'NONE',  ( 114.8384214775786489, -10.15424416112533912, -14.75197769757731336 ) ) ;
#12352=CARTESIAN_POINT ( 'NONE',  ( 113.9875214775786532, -0.4660016031367893996, -10.09054647747474043 ) ) ;
#12354=CARTESIAN_POINT ( 'NONE',  ( 123.8579614775786126, -9.859900752359378018, -12.68260735090039759 ) ) ;
#12355=CARTESIAN_POINT ( 'NONE',  ( 120.1140014775786398, -7.894159318335828068, -9.358103419637847864 ) ) ;
#12360=CARTESIAN_POINT ( 'NONE',  ( 112.5693548109119888, -10.63000616557722466, -14.87417383870573495 ) ) ;
#12361=CARTESIAN_POINT ( 'NONE',  ( 121.8725281442453223, -6.222761293078241884, -8.102969835052219238 ) ) ;
#12365=CARTESIAN_POINT ( 'NONE',  ( 113.7606148109119886, -1.561330072975668060, -17.79121239304076596 ) ) ;
#12367=CARTESIAN_POINT ( 'NONE',  ( 116.7104014775786425, -8.899110576539710493, -16.42337572283490132 ) ) ;
#12370=CARTESIAN_POINT ( 'NONE',  ( 122.8936081442453059, -9.565557343593413364, -10.61323700422348004 ) ) ;
#12371=CARTESIAN_POINT ( 'NONE',  ( 120.0005481442453146, -4.153390946401325223, -8.397313243818185668 ) ) ;
#12375=AXIS2_PLACEMENT_3D ( 'NONE', #42185, #21649, #10727 ) ;
#12378=CARTESIAN_POINT ( 'NONE',  ( 119.3765548109119834, 0.9020085738987339008, -11.91225656197089222 ) ) ;
#12381=CARTESIAN_POINT ( 'NONE',  ( 114.7816948109119863, 0.5811942927096154232, -14.16772938898807155 ) ) ;
#12382=CARTESIAN_POINT ( 'NONE',  ( 116.0864081442453113, -9.988377603198976828, -10.36322818467138340 ) ) ;
#12383=CARTESIAN_POINT ( 'NONE',  ( 117.7314814775786260, -5.574606645277164318, -18.38911715685844683 ) ) ;
#12384=CARTESIAN_POINT ( 'NONE',  ( 120.6245414775786458, -0.1624402480850797581, -16.17319339645315424 ) ) ;
#12385=CARTESIAN_POINT ( 'NONE',  ( 113.3068014775786594, -8.166667518702817929, -8.995218007635859436 ) ) ;
#12387=CARTESIAN_POINT ( 'NONE',  ( 119.1496481442453046, -6.222761293078241884, -8.102969835052219238 ) ) ;
#12388=DIRECTION ( 'NONE',  ( 0.000000000000000000, 0.6004852223388321697, -0.7996358532186279566 ) ) ;
#12392=CARTESIAN_POINT ( 'NONE',  ( 118.3554748109119998, 0.2603800115204892296, -16.42320221600525088 ) ) ;
#12393=VERTEX_POINT ( 'NONE', #34257 ) ;
#12394=CARTESIAN_POINT ( 'NONE',  ( 120.6245414775786458, -9.988377603198976828, -10.36322818467138340 ) ) ;
#12397=CARTESIAN_POINT ( 'NONE',  ( 118.5823814775786360, -1.834011780172310813, -8.268836392978581529 ) ) ;
#12398=CARTESIAN_POINT ( 'NONE',  ( 117.2776681442452968, -5.638512984488999180, -18.83840828888717311 ) ) ;
#12404=CARTESIAN_POINT ( 'NONE',  ( 121.4187148109119789, -3.505236298600246325, -18.68346056562440793 ) ) ;
#12408=CARTESIAN_POINT ( 'NONE',  ( 119.2631014775786298, -9.565557343593413364, -10.61323700422348004 ) ) ;
#12411=CARTESIAN_POINT ( 'NONE',  ( 125.7866681442452688, -0.4660016031367893996, -10.09054647747474043 ) ) ;
#12412=CARTESIAN_POINT ( 'NONE',  ( 124.9357681442453014, -1.834011780172310813, -8.268836392978581529 ) ) ;
#12414=CARTESIAN_POINT ( 'NONE',  ( 118.8660148109119774, 0.1319031606808879209, -14.10382304977623669 ) ) ;
#12415=CARTESIAN_POINT ( 'NONE',  ( 114.7816948109119863, 0.5811942927096154232, -14.16772938898807155 ) ) ;
#12416=CARTESIAN_POINT ( 'NONE',  ( 121.4187148109119789, -6.344957434206665248, -7.627207830600338134 ) ) ;
#12418=CARTESIAN_POINT ( 'NONE',  ( 121.8158014775786171, -4.153390946401325223, -8.397313243818185668 ) ) ;
#12420=CARTESIAN_POINT ( 'NONE',  ( 124.0848681442452772, -5.574606645277164318, -18.38911715685844683 ) ) ;
#12421=CARTESIAN_POINT ( 'NONE',  ( 123.5176014775786228, -9.261995988541697145, -16.69588392320189030 ) ) ;
#12424=CARTESIAN_POINT ( 'NONE',  ( 124.7088614775786226, 0.2603800115204892296, -16.42320221600525088 ) ) ;
#12432=CARTESIAN_POINT ( 'NONE',  ( 137.0134976903310644, -9.992782420886062056, -11.53748965989417385 ) ) ;
#12433=CARTESIAN_POINT ( 'NONE',  ( 120.5110881442453206, -3.505236298600246325, -18.68346056562440793 ) ) ;
#12434=CARTESIAN_POINT ( 'NONE',  ( 123.6877814775786533, -3.383040157471821630, -19.15922257007629170 ) ) ;
#12437=CARTESIAN_POINT ( 'NONE',  ( 116.0086969107182142, -2.467220198592777525, -17.83387418641524391 ) ) ;
#12439=CARTESIAN_POINT ( 'NONE',  ( 116.3700414775786527, -4.153390946401321671, -8.397313243818183892 ) ) ;
#12441=CARTESIAN_POINT ( 'NONE',  ( 135.3184548109119874, 1.087851763053662602, -12.63461456455805276 ) ) ;
#12444=CARTESIAN_POINT ( 'NONE',  ( 122.7801548109119665, -3.383040157471821630, -19.15922257007629170 ) ) ;
#12445=CARTESIAN_POINT ( 'NONE',  ( 121.9292548109119849, -7.894159318335828068, -9.358103419637847864 ) ) ;
#12450=CARTESIAN_POINT ( 'NONE',  ( 121.8725281442453223, -6.222761293078241884, -8.102969835052219238 ) ) ;
#12451=CARTESIAN_POINT ( 'NONE',  ( 121.7023481442452777, -0.8288870151387760510, -10.36305467784173118 ) ) ;
#12454=CARTESIAN_POINT ( 'NONE',  ( 116.5509091406318873, 0.3208234527006367798, -15.99825685930877839 ) ) ;
#12461=CARTESIAN_POINT ( 'NONE',  ( 121.8158014775786171, -5.638512984488999180, -18.83840828888717311 ) ) ;
#12462=CARTESIAN_POINT ( 'NONE',  ( 121.2485348109119769, -0.4660016031367893996, -10.09054647747474043 ) ) ;
#12464=( BOUNDED_SURFACE ( )  B_SPLINE_SURFACE ( 1, 2, ( 
 ( #9508, #37310, #40988, #9287, #26838, #16815, #12710, #20230, #26610, #30707, #12941, #16352, #6077, #19999, #33883, #30479, #44400, #13164, #6311, #44630, #13394, #27297, #38874, #34982, #359, #3768, #32033, #3552, #11077, #7195, #10633, #45068, #31365, #14720, #17692, #583, #7644, #42094, #17467, #24980, #802, #31589, #25210, #38641, #27743, #39108, #38427, #4221, #28407, #14270, #6986, #41657, #14492, #38208, #13828, #3992, #17914, #137, #10416, #21105, #24538, #14050, #20898, #24323, #21557, #10857, #31812, #28633, #42540, #3339, #20678, #21334, #28188, #35446, #34772, #24753, #7413, #27966, #35219, #11301, #42316, #34555, #41873, #18137, #17258, #31147, #22851, #19429, #15165, #4450, #13051, #1028, #36961, #11530, #18371, #29070, #33314, #26950, #12830, #19887, #14945, #9173, #35902, #26729, #25436, #37188, #7877, #8950, #23081, #36742, #28855, #35675, #40639, #33774, #40184, #5510, #42768, #32260, #9394, #2544, #2089, #16015, #18589, #16246, #30149, #29921, #4667, #21785, #26505, #39338, #5962, #44064, #23305, #16471, #42982, #12378, #43836, #8105, #1254, #5733, #30374, #40414, #22006, #19652, #32479, #44295, #26276, #12604, #33538, #2316, #30821, #13504, #6435, #9624, #34229, #41765, #13943, #10090, #20567, #23994, #7093, #23770, #31258, #27410, #44744, #20120, #20346, #34878, #37882, #20786, #27855, #17151, #37662, #31, #21003, #6656, #250, #13726, #2775, #14158, #41332, #24425, #3453, #34445, #27182, #16700, #34666, #13276, #34006, #24210, #38103, #3003, #30595, #3225, #31039, #16926, #41103, #44512, #10526, #44969, #6877, #3666, #17586, #23546, #40871, #41549, #27635, #38316, #9861, #10309, #17369, #31479, #37429, #6199, #21896, #28077, #7308, #28748, #32149, #3887, #42432, #38996, #35334, #24647, #32597, #21226, #11423, #31700, #38533, #4104, #7765, #1368, #32376, #39455, #35104, #42652, #10969, #1142, #470, #11636, #41984, #28527, #25330, #11196, #17807, #24871, #10750, #25549, #14384, #25100, #28296, #21673, #689, #7987, #8218, #18706, #35561 ),
 ( #42207, #39222, #919, #38763, #4334, #18255, #18027, #7533, #21451, #31924, #35790, #14608, #14838, #4560, #18486, #15059, #28974, #22124, #42878, #36018, #4786, #19598, #32814, #44009, #15278, #15734, #29864, #29636, #8444, #43098, #33482, #26671, #1808, #12319, #25998, #23019, #36908, #43551, #12093, #29186, #33263, #11868, #12771, #5680, #2261, #16188, #22565, #36469, #22790, #22348, #8663, #43780, #30093, #2035, #25773, #12544, #39902, #40584, #36242, #9343, #23252, #1582, #5235, #33033, #19150, #39679, #26218, #37134, #5910, #40128, #8892, #36684, #19831, #43326, #33718, #5455, #19374, #5008, #15961, #18925, #26451, #40354, #15504, #9117, #29412, #38051, #27798, #30766, #7044, #20515, #9571, #20956, #20288, #31208, #10252, #44690, #33950, #23487, #41496, #20065, #40815, #30991, #44916, #13225, #26895, #34172, #6380, #41712, #16875, #27581, #34614, #23943, #30537, #6829, #10476, #13451, #2489, #34394, #37373, #16418, #2946, #45131, #24160, #27356, #2718, #6144, #20734, #16644, #44459, #13673, #3401, #27125, #41049, #41275, #10035, #9806, #23716, #37606, #17319, #37822, #13890, #24377, #38264, #30313, #44239, #3176, #6600, #12999, #17098, #31875, #640, #24598, #21396, #25498, #28697, #34828, #14108, #35509, #38939, #10695, #4051, #14553, #42156, #31426, #39402, #28024, #18199, #38482, #192, #10916, #28472, #8167, #39170, #1091, #41932, #4281, #17751, #7934, #7256, #18436, #3611, #35276, #32095, #17974, #21171, #17528, #21844, #15007, #42378, #11141, #417, #42602, #11367, #25044, #31647, #35048, #7707, #3831, #32326, #25273, #35739, #4512, #24816, #38708, #21620, #14333, #28247, #865, #28920, #14783, #7476, #42828, #11589, #5627, #43046, #19548, #43725, #39628, #12041, #39851, #32761, #35965, #15456, #22966, #40301, #36410, #1757, #5178, #33426, #4957, #12493, #8616, #25945, #1316, #1534, #22514, #29362, #22296, #29134, #26392, #43502, #5409, #16132, #43951, #4735, #22074, #22735, #19096, #9065, #25722, #32982, #15682, #11814, #29585, #12715, #15912, #18654 ) ),
 .UNSPECIFIED., .F., .F., .T. ) 
 B_SPLINE_SURFACE_WITH_KNOTS ( ( 2, 2 ),
 ( 3, 2, 2, 2, 2, 2, 2, 2, 2, 2, 2, 2, 2, 2, 2, 2, 2, 2, 2, 2, 2, 2, 2, 2, 2, 2, 2, 2, 2, 2, 2, 2, 2, 2, 2, 2, 2, 2, 2, 2, 2, 2, 2, 2, 2, 2, 2, 2, 2, 2, 2, 2, 2, 2, 2, 2, 2, 2, 2, 2, 2, 2, 2, 2, 2, 2, 2, 2, 2, 2, 2, 2, 2, 2, 2, 2, 2, 2, 2, 2, 2, 2, 2, 2, 2, 2, 2, 2, 2, 2, 2, 2, 2, 2, 2, 2, 2, 2, 2, 2, 2, 2, 2, 2, 2, 2, 2, 2, 2, 2, 2, 2, 2, 2, 2, 2, 2, 2, 2, 2, 2, 2, 2, 2, 2, 2, 2, 2, 3 ),
 ( 0.000000000000000000, 1.000000000000000000 ),
 ( 0.000000000000000000, 0.007812500000000000000, 0.01562500000000000000, 0.02343750000000000000, 0.03125000000000000000, 0.03906250000000000000, 0.04687500000000000000, 0.05468750000000000000, 0.06250000000000000000, 0.07031250000000000000, 0.07812500000000000000, 0.08593750000000000000, 0.09375000000000000000, 0.1015625000000000000, 0.1093750000000000000, 0.1171875000000000000, 0.1250000000000000000, 0.1328125000000000000, 0.1406250000000000000, 0.1484375000000000000, 0.1562500000000000000, 0.1640625000000000000, 0.1718750000000000000, 0.1796875000000000000, 0.1875000000000000000, 0.1953125000000000000, 0.2031250000000000000, 0.2109375000000000000, 0.2187500000000000000, 0.2265625000000000000, 0.2343750000000000000, 0.2421875000000000000, 0.2500000000000000000, 0.2578125000000000000, 0.2656250000000000000, 0.2734375000000000000, 0.2812500000000000000, 0.2890625000000000000, 0.2968750000000000000, 0.3046875000000000000, 0.3125000000000000000, 0.3203125000000000000, 0.3281250000000000000, 0.3359375000000000000, 0.3437500000000000000, 0.3515625000000000000, 0.3593750000000000000, 0.3671875000000000000, 0.3750000000000000000, 0.3828125000000000000, 0.3906250000000000000, 0.3984375000000000000, 0.4062500000000000000, 0.4140625000000000000, 0.4218750000000000000, 0.4296875000000000000, 0.4375000000000000000, 0.4453125000000000000, 0.4531250000000000000, 0.4609375000000000000, 0.4687500000000000000, 0.4765625000000000000, 0.4843750000000000000, 0.4921875000000000000, 0.5000000000000000000, 0.5078125000000000000, 0.5156250000000000000, 0.5234375000000000000, 0.5312500000000000000, 0.5390625000000000000, 0.5468750000000000000, 0.5546875000000000000, 0.5625000000000000000, 0.5703125000000000000, 0.5781250000000000000, 0.5859375000000000000, 0.5937500000000000000, 0.6015625000000000000, 0.6093750000000000000, 0.6171875000000000000, 0.6250000000000000000, 0.6328125000000000000, 0.6406250000000000000, 0.6484375000000000000, 0.6562500000000000000, 0.6640625000000000000, 0.6718750000000000000, 0.6796875000000000000, 0.6875000000000000000, 0.6953125000000000000, 0.7031250000000000000, 0.7109375000000000000, 0.7187500000000000000, 0.7265625000000000000, 0.7343750000000000000, 0.7421875000000000000, 0.7500000000000000000, 0.7578125000000000000, 0.7656250000000000000, 0.7734375000000000000, 0.7812500000000000000, 0.7890625000000000000, 0.7968750000000000000, 0.8046875000000000000, 0.8125000000000000000, 0.8203125000000000000, 0.8281250000000000000, 0.8359375000000000000, 0.8437500000000000000, 0.8515625000000000000, 0.8593750000000000000, 0.8671875000000000000, 0.8750000000000000000, 0.8828125000000000000, 0.8906250000000000000, 0.8984375000000000000, 0.9062500000000000000, 0.9140625000000000000, 0.9218750000000000000, 0.9296875000000000000, 0.9375000000000000000, 0.9453125000000000000, 0.9531250000000000000, 0.9609375000000000000, 0.9687500000000000000, 0.9765625000000000000, 0.9843750000000000000, 0.9921875000000000000, 1.000000000000000000 ),
 .UNSPECIFIED. ) 
 GEOMETRIC_REPRESENTATION_ITEM ( )  RATIONAL_B_SPLINE_SURFACE ( (
 ( 1.000000000000000000, 0.9238795325112869605, 1.000000000000000000, 0.9238795325112869605, 1.000000000000000000, 0.9238795325112869605, 1.000000000000000000, 0.9238795325112869605, 1.000000000000000000, 0.9238795325112869605, 1.000000000000000000, 0.9238795325112869605, 1.000000000000000000, 0.9238795325112869605, 1.000000000000000000, 0.9238795325112869605, 1.000000000000000000, 0.9238795325112869605, 1.000000000000000000, 0.9238795325112869605, 1.000000000000000000, 0.9238795325112869605, 1.000000000000000000, 0.9238795325112869605, 1.000000000000000000, 0.9238795325112869605, 1.000000000000000000, 0.9238795325112869605, 1.000000000000000000, 0.9238795325112869605, 1.000000000000000000, 0.9238795325112869605, 1.000000000000000000, 0.9238795325112869605, 1.000000000000000000, 0.9238795325112869605, 1.000000000000000000, 0.9238795325112869605, 1.000000000000000000, 0.9238795325112869605, 1.000000000000000000, 0.9238795325112869605, 1.000000000000000000, 0.9238795325112869605, 1.000000000000000000, 0.9238795325112869605, 1.000000000000000000, 0.9238795325112869605, 1.000000000000000000, 0.9238795325112869605, 1.000000000000000000, 0.9238795325112869605, 1.000000000000000000, 0.9238795325112869605, 1.000000000000000000, 0.9238795325112869605, 1.000000000000000000, 0.9238795325112869605, 1.000000000000000000, 0.9238795325112869605, 1.000000000000000000, 0.9238795325112869605, 1.000000000000000000, 0.9238795325112869605, 1.000000000000000000, 0.9238795325112869605, 1.000000000000000000, 0.9238795325112869605, 1.000000000000000000, 0.9238795325112869605, 1.000000000000000000, 0.9238795325112869605, 1.000000000000000000, 0.9238795325112869605, 1.000000000000000000, 0.9238795325112869605, 1.000000000000000000, 0.9238795325112869605, 1.000000000000000000, 0.9238795325112869605, 1.000000000000000000, 0.9238795325112869605, 1.000000000000000000, 0.9238795325112869605, 1.000000000000000000, 0.9238795325112869605, 1.000000000000000000, 0.9238795325112869605, 1.000000000000000000, 0.9238795325112869605, 1.000000000000000000, 0.9238795325112869605, 1.000000000000000000, 0.9238795325112869605, 1.000000000000000000, 0.9238795325112869605, 1.000000000000000000, 0.9238795325112869605, 1.000000000000000000, 0.9238795325112869605, 1.000000000000000000, 0.9238795325112869605, 1.000000000000000000, 0.9238795325112869605, 1.000000000000000000, 0.9238795325112869605, 1.000000000000000000, 0.9238795325112869605, 1.000000000000000000, 0.9238795325112869605, 1.000000000000000000, 0.9238795325112869605, 1.000000000000000000, 0.9238795325112869605, 1.000000000000000000, 0.9238795325112869605, 1.000000000000000000, 0.9238795325112869605, 1.000000000000000000, 0.9238795325112869605, 1.000000000000000000, 0.9238795325112869605, 1.000000000000000000, 0.9238795325112869605, 1.000000000000000000, 0.9238795325112869605, 1.000000000000000000, 0.9238795325112869605, 1.000000000000000000, 0.9238795325112869605, 1.000000000000000000, 0.9238795325112869605, 1.000000000000000000, 0.9238795325112869605, 1.000000000000000000, 0.9238795325112869605, 1.000000000000000000, 0.9238795325112869605, 1.000000000000000000, 0.9238795325112869605, 1.000000000000000000, 0.9238795325112869605, 1.000000000000000000, 0.9238795325112869605, 1.000000000000000000, 0.9238795325112869605, 1.000000000000000000, 0.9238795325112869605, 1.000000000000000000, 0.9238795325112869605, 1.000000000000000000, 0.9238795325112869605, 1.000000000000000000, 0.9238795325112869605, 1.000000000000000000, 0.9238795325112869605, 1.000000000000000000, 0.9238795325112869605, 1.000000000000000000, 0.9238795325112869605, 1.000000000000000000, 0.9238795325112869605, 1.000000000000000000, 0.9238795325112869605, 1.000000000000000000, 0.9238795325112869605, 1.000000000000000000, 0.9238795325112869605, 1.000000000000000000, 0.9238795325112869605, 1.000000000000000000, 0.9238795325112869605, 1.000000000000000000, 0.9238795325112869605, 1.000000000000000000, 0.9238795325112869605, 1.000000000000000000, 0.9238795325112869605, 1.000000000000000000, 0.9238795325112869605, 1.000000000000000000, 0.9238795325112869605, 1.000000000000000000, 0.9238795325112869605, 1.000000000000000000, 0.9238795325112869605, 1.000000000000000000, 0.9238795325112869605, 1.000000000000000000, 0.9238795325112869605, 1.000000000000000000, 0.9238795325112869605, 1.000000000000000000, 0.9238795325112869605, 1.000000000000000000, 0.9238795325112869605, 1.000000000000000000, 0.9238795325112869605, 1.000000000000000000, 0.9238795325112869605, 1.000000000000000000, 0.9238795325112869605, 1.000000000000000000, 0.9238795325112869605, 1.000000000000000000, 0.9238795325112869605, 1.000000000000000000, 0.9238795325112869605, 1.000000000000000000, 0.9238795325112869605, 1.000000000000000000, 0.9238795325112869605, 1.000000000000000000, 0.9238795325112869605, 1.000000000000000000, 0.9238795325112869605, 1.000000000000000000, 0.9238795325112869605, 1.000000000000000000, 0.9238795325112869605, 1.000000000000000000, 0.9238795325112869605, 1.000000000000000000, 0.9238795325112869605, 1.000000000000000000, 0.9238795325112869605, 1.000000000000000000, 0.9238795325112869605, 1.000000000000000000, 0.9238795325112869605, 1.000000000000000000, 0.9238795325112869605, 1.000000000000000000, 0.9238795325112869605, 1.000000000000000000, 0.9238795325112869605, 1.000000000000000000, 0.9238795325112869605, 1.000000000000000000, 0.9238795325112869605, 1.000000000000000000, 0.9238795325112869605, 1.000000000000000000, 0.9238795325112869605, 1.000000000000000000, 0.9238795325112869605, 1.000000000000000000, 0.9238795325112869605, 1.000000000000000000, 0.9238795325112869605, 1.000000000000000000, 0.9238795325112869605, 1.000000000000000000, 0.9238795325112869605, 1.000000000000000000, 0.9238795325112869605, 1.000000000000000000),
 ( 1.000000000000000000, 0.9238795325112869605, 1.000000000000000000, 0.9238795325112869605, 1.000000000000000000, 0.9238795325112869605, 1.000000000000000000, 0.9238795325112869605, 1.000000000000000000, 0.9238795325112869605, 1.000000000000000000, 0.9238795325112869605, 1.000000000000000000, 0.9238795325112869605, 1.000000000000000000, 0.9238795325112869605, 1.000000000000000000, 0.9238795325112869605, 1.000000000000000000, 0.9238795325112869605, 1.000000000000000000, 0.9238795325112869605, 1.000000000000000000, 0.9238795325112869605, 1.000000000000000000, 0.9238795325112869605, 1.000000000000000000, 0.9238795325112869605, 1.000000000000000000, 0.9238795325112869605, 1.000000000000000000, 0.9238795325112869605, 1.000000000000000000, 0.9238795325112869605, 1.000000000000000000, 0.9238795325112869605, 1.000000000000000000, 0.9238795325112869605, 1.000000000000000000, 0.9238795325112869605, 1.000000000000000000, 0.9238795325112869605, 1.000000000000000000, 0.9238795325112869605, 1.000000000000000000, 0.9238795325112869605, 1.000000000000000000, 0.9238795325112869605, 1.000000000000000000, 0.9238795325112869605, 1.000000000000000000, 0.9238795325112869605, 1.000000000000000000, 0.9238795325112869605, 1.000000000000000000, 0.9238795325112869605, 1.000000000000000000, 0.9238795325112869605, 1.000000000000000000, 0.9238795325112869605, 1.000000000000000000, 0.9238795325112869605, 1.000000000000000000, 0.9238795325112869605, 1.000000000000000000, 0.9238795325112869605, 1.000000000000000000, 0.9238795325112869605, 1.000000000000000000, 0.9238795325112869605, 1.000000000000000000, 0.9238795325112869605, 1.000000000000000000, 0.9238795325112869605, 1.000000000000000000, 0.9238795325112869605, 1.000000000000000000, 0.9238795325112869605, 1.000000000000000000, 0.9238795325112869605, 1.000000000000000000, 0.9238795325112869605, 1.000000000000000000, 0.9238795325112869605, 1.000000000000000000, 0.9238795325112869605, 1.000000000000000000, 0.9238795325112869605, 1.000000000000000000, 0.9238795325112869605, 1.000000000000000000, 0.9238795325112869605, 1.000000000000000000, 0.9238795325112869605, 1.000000000000000000, 0.9238795325112869605, 1.000000000000000000, 0.9238795325112869605, 1.000000000000000000, 0.9238795325112869605, 1.000000000000000000, 0.9238795325112869605, 1.000000000000000000, 0.9238795325112869605, 1.000000000000000000, 0.9238795325112869605, 1.000000000000000000, 0.9238795325112869605, 1.000000000000000000, 0.9238795325112869605, 1.000000000000000000, 0.9238795325112869605, 1.000000000000000000, 0.9238795325112869605, 1.000000000000000000, 0.9238795325112869605, 1.000000000000000000, 0.9238795325112869605, 1.000000000000000000, 0.9238795325112869605, 1.000000000000000000, 0.9238795325112869605, 1.000000000000000000, 0.9238795325112869605, 1.000000000000000000, 0.9238795325112869605, 1.000000000000000000, 0.9238795325112869605, 1.000000000000000000, 0.9238795325112869605, 1.000000000000000000, 0.9238795325112869605, 1.000000000000000000, 0.9238795325112869605, 1.000000000000000000, 0.9238795325112869605, 1.000000000000000000, 0.9238795325112869605, 1.000000000000000000, 0.9238795325112869605, 1.000000000000000000, 0.9238795325112869605, 1.000000000000000000, 0.9238795325112869605, 1.000000000000000000, 0.9238795325112869605, 1.000000000000000000, 0.9238795325112869605, 1.000000000000000000, 0.9238795325112869605, 1.000000000000000000, 0.9238795325112869605, 1.000000000000000000, 0.9238795325112869605, 1.000000000000000000, 0.9238795325112869605, 1.000000000000000000, 0.9238795325112869605, 1.000000000000000000, 0.9238795325112869605, 1.000000000000000000, 0.9238795325112869605, 1.000000000000000000, 0.9238795325112869605, 1.000000000000000000, 0.9238795325112869605, 1.000000000000000000, 0.9238795325112869605, 1.000000000000000000, 0.9238795325112869605, 1.000000000000000000, 0.9238795325112869605, 1.000000000000000000, 0.9238795325112869605, 1.000000000000000000, 0.9238795325112869605, 1.000000000000000000, 0.9238795325112869605, 1.000000000000000000, 0.9238795325112869605, 1.000000000000000000, 0.9238795325112869605, 1.000000000000000000, 0.9238795325112869605, 1.000000000000000000, 0.9238795325112869605, 1.000000000000000000, 0.9238795325112869605, 1.000000000000000000, 0.9238795325112869605, 1.000000000000000000, 0.9238795325112869605, 1.000000000000000000, 0.9238795325112869605, 1.000000000000000000, 0.9238795325112869605, 1.000000000000000000, 0.9238795325112869605, 1.000000000000000000, 0.9238795325112869605, 1.000000000000000000, 0.9238795325112869605, 1.000000000000000000, 0.9238795325112869605, 1.000000000000000000, 0.9238795325112869605, 1.000000000000000000, 0.9238795325112869605, 1.000000000000000000, 0.9238795325112869605, 1.000000000000000000, 0.9238795325112869605, 1.000000000000000000, 0.9238795325112869605, 1.000000000000000000, 0.9238795325112869605, 1.000000000000000000, 0.9238795325112869605, 1.000000000000000000, 0.9238795325112869605, 1.000000000000000000, 0.9238795325112869605, 1.000000000000000000, 0.9238795325112869605, 1.000000000000000000, 0.9238795325112869605, 1.000000000000000000, 0.9238795325112869605, 1.000000000000000000, 0.9238795325112869605, 1.000000000000000000, 0.9238795325112869605, 1.000000000000000000, 0.9238795325112869605, 1.000000000000000000, 0.9238795325112869605, 1.000000000000000000, 0.9238795325112869605, 1.000000000000000000, 0.9238795325112869605, 1.000000000000000000, 0.9238795325112869605, 1.000000000000000000, 0.9238795325112869605, 1.000000000000000000, 0.9238795325112869605, 1.000000000000000000, 0.9238795325112869605, 1.000000000000000000, 0.9238795325112869605, 1.000000000000000000, 0.9238795325112869605, 1.000000000000000000, 0.9238795325112869605, 1.000000000000000000, 0.9238795325112869605, 1.000000000000000000) ) ) 
 REPRESENTATION_ITEM ( '' )  SURFACE ( )  );
#12465=CARTESIAN_POINT ( 'NONE',  ( 115.5758681442453053, -1.561330072975668060, -17.79121239304076951 ) ) ;
#12468=DIRECTION ( 'NONE',  ( 1.000000000000000000, 0.000000000000000000, 0.000000000000000000 ) ) ;
#12469=CARTESIAN_POINT ( 'NONE',  ( 120.9649014775786355, -3.383040157471821630, -19.15922257007629170 ) ) ;
#12470=CARTESIAN_POINT ( 'NONE',  ( 118.6391081442452986, -4.089484607189486809, -7.948022111789456723 ) ) ;
#12471=CARTESIAN_POINT ( 'NONE',  ( 125.6164881442453094, -9.565557343593413364, -10.61323700422348004 ) ) ;
#12472=CARTESIAN_POINT ( 'NONE',  ( 125.9568481442452850, -6.344957434206665248, -7.627207830600338134 ) ) ;
#12473=AXIS2_PLACEMENT_3D ( 'NONE', #32946, #11778, #40033 ) ;
#12474=CARTESIAN_POINT ( 'NONE',  ( 115.4056881442453459, -2.084020599724406786, -8.691656652584148546 ) ) ;
#12475=CARTESIAN_POINT ( 'NONE',  ( 125.2761281442453054, -10.63000616557722466, -14.87417383870573495 ) ) ;
#12478=CARTESIAN_POINT ( 'NONE',  ( 119.3198281442452924, -9.859900752359374465, -12.68260735090039404 ) ) ;
#12484=CARTESIAN_POINT ( 'NONE',  ( 121.7590748109119687, -7.893985811506177619, -18.51759400769804742 ) ) ;
#12488=CARTESIAN_POINT ( 'NONE',  ( 118.2420214775786320, -6.222761293078241884, -8.102969835052219238 ) ) ;
#12491=CARTESIAN_POINT ( 'NONE',  ( 124.7088614775786226, -9.565557343593413364, -10.61323700422348004 ) ) ;
#12492=CARTESIAN_POINT ( 'NONE',  ( 123.5680096192402146, -1.111561923218658210, -17.14115599315433158 ) ) ;
#12493=CARTESIAN_POINT ( 'NONE',  ( 124.3117748109119844, 0.1319031606808879209, -14.10382304977623669 ) ) ;
#12496=CARTESIAN_POINT ( 'NONE',  ( 125.3328548109119964, -9.261995988541697145, -16.69588392320189030 ) ) ;
#12497=CARTESIAN_POINT ( 'NONE',  ( 119.1496481442453046, -6.222761293078241884, -8.102969835052219238 ) ) ;
#12498=CARTESIAN_POINT ( 'NONE',  ( 124.9357681442453014, -7.643976991954077427, -18.09477374809248928 ) ) ;
#12501=CARTESIAN_POINT ( 'NONE',  ( 124.7655881442452852, 0.5811942927096110934, -14.16772938898807510 ) ) ;
#12502=CARTESIAN_POINT ( 'NONE',  ( 115.0653281442453277, -6.344957434206662583, -7.627207830600332805 ) ) ;
#12504=CARTESIAN_POINT ( 'NONE',  ( 112.7395348109119766, -4.153390946401321671, -8.397313243818183892 ) ) ;
#12505=EDGE_CURVE ( 'NONE', #27848, #22341, #20136, .T. ) ;
#12506=CARTESIAN_POINT ( 'NONE',  ( 125.4463081442452932, -4.153390946401325223, -8.397313243818185668 ) ) ;
#12507=CARTESIAN_POINT ( 'NONE',  ( 125.6732148109119862, 0.5811942927096110934, -14.16772938898807510 ) ) ;
#12511=CARTESIAN_POINT ( 'NONE',  ( 112.9664414775786412, -9.859900752359374465, -12.68260735090039404 ) ) ;
#12515=CARTESIAN_POINT ( 'NONE',  ( 123.8012348109119642, -9.565557343593413364, -10.61323700422348004 ) ) ;
#12522=CARTESIAN_POINT ( 'NONE',  ( 117.3911214775786505, -1.561330072975668504, -17.79121239304076951 ) ) ;
#12524=CARTESIAN_POINT ( 'NONE',  ( 124.5386814775786206, -4.153390946401325223, -8.397313243818185668 ) ) ;
#12525=CARTESIAN_POINT ( 'NONE',  ( 113.7606148109119886, -7.894159318335828068, -9.358103419637847864 ) ) ;
#12527=CARTESIAN_POINT ( 'NONE',  ( 114.8838660002551109, -2.334846009198400907, -18.01015021110789149 ) ) ;
#12528=CARTESIAN_POINT ( 'NONE',  ( 114.7249681442453237, 0.2603800115204892296, -16.42320221600525088 ) ) ;
#12530=CIRCLE ( 'NONE', #38735, 5.999999999999997335 ) ;
#12531=CARTESIAN_POINT ( 'NONE',  ( 125.2761281442453054, -10.63000616557722466, -14.87417383870573495 ) ) ;
#12534=CARTESIAN_POINT ( 'NONE',  ( 113.0798948109119948, -0.4660016031367893996, -10.09054647747474043 ) ) ;
#12535=CARTESIAN_POINT ( 'NONE',  ( 115.1220548109119761, -1.833838273342658809, -17.42832698103878286 ) ) ;
#12537=CARTESIAN_POINT ( 'NONE',  ( 125.5597614775786326, -7.894159318335828068, -9.358103419637847864 ) ) ;
#12539=CARTESIAN_POINT ( 'NONE',  ( 120.0005481442453146, -5.638512984488999180, -18.83840828888717311 ) ) ;
#12541=CARTESIAN_POINT ( 'NONE',  ( 115.5950730757767531, -0.9924539043446216624, -17.29976612834909133 ) ) ;
#12543=CARTESIAN_POINT ( 'NONE',  ( 112.6138494832010650, -2.324775150319229766, -18.02356106541842706 ) ) ;
#12544=CARTESIAN_POINT ( 'NONE',  ( 114.3846081442453197, 0.4262465694468514643, -12.03445270309931736 ) ) ;
#12548=CARTESIAN_POINT ( 'NONE',  ( 111.6050014775786536, 0.1319031606808879209, -14.10382304977623669 ) ) ;
#12549=CARTESIAN_POINT ( 'NONE',  ( 113.6471614775786492, -5.638512984488999180, -18.83840828888717311 ) ) ;
#12551=CARTESIAN_POINT ( 'NONE',  ( 113.2500748109119968, -6.344957434206662583, -7.627207830600332805 ) ) ;
#12552=CARTESIAN_POINT ( 'NONE',  ( 114.1009748109119784, -5.574606645277164318, -18.38911715685844683 ) ) ;
#12553=CARTESIAN_POINT ( 'NONE',  ( 124.6521348109119884, -1.561330072975668948, -17.79121239304076951 ) ) ;
#12555=CARTESIAN_POINT ( 'NONE',  ( 123.5176014775786228, -9.261995988541697145, -16.69588392320189030 ) ) ;
#12563=CARTESIAN_POINT ( 'NONE',  ( 120.2274548109119934, 0.5811942927096110934, -14.16772938898807510 ) ) ;
#12564=ORIENTED_EDGE ( 'NONE', *, *, #7187, .F. ) ;
#12569=CARTESIAN_POINT ( 'NONE',  ( 114.8951481442453115, -8.899110576539710493, -16.42337572283490132 ) ) ;
#12572=CARTESIAN_POINT ( 'NONE',  ( 121.3619881442452879, -4.089484607189486809, -7.948022111789456723 ) ) ;
#12576=CARTESIAN_POINT ( 'NONE',  ( 121.4544569107182070, -2.467220198592778413, -17.83387418641524391 ) ) ;
#12577=CARTESIAN_POINT ( 'NONE',  ( 121.3052614775786111, -7.643976991954077427, -18.09477374809248928 ) ) ;
#12578=CARTESIAN_POINT ( 'NONE',  ( 118.0151148109119816, -10.63000616557722466, -14.87417383870573495 ) ) ;
#12580=CARTESIAN_POINT ( 'NONE',  ( 114.7249681442453237, 0.2603800115204892296, -16.42320221600525088 ) ) ;
#12582=CARTESIAN_POINT ( 'NONE',  ( 124.4819548109119722, -2.084020599724406786, -8.691656652584148546 ) ) ;
#12583=CARTESIAN_POINT ( 'NONE',  ( 118.5256548109119876, -8.899110576539710493, -16.42337572283490132 ) ) ;
#12585=B_SPLINE_CURVE_WITH_KNOTS ( 'NONE', 3,
 ( #1933, #36807, #5576, #8337, #15859, #8563, #15404, #33378, #42777, #32932 ),
 .UNSPECIFIED., .F., .F.,
 ( 4, 3, 3, 4 ),
 ( 0.000000000000000000, 0.0001671877548681289800, 0.0003343755096277714980, 0.0006463528481650629171 ),
 .UNSPECIFIED. ) ;
#12588=CARTESIAN_POINT ( 'NONE',  ( 113.9875214775786532, -0.4660016031367893996, -10.09054647747474043 ) ) ;
#12589=CARTESIAN_POINT ( 'NONE',  ( 120.7379948109119709, 0.4262465694468514643, -12.03445270309931736 ) ) ;
#12590=VERTEX_POINT ( 'NONE', #31763 ) ;
#12592=CARTESIAN_POINT ( 'NONE',  ( 118.6391081442452986, -4.089484607189486809, -7.948022111789456723 ) ) ;
#12593=PRODUCT_DEFINITION_FORMATION_WITH_SPECIFIED_SOURCE ( 'ANY', '', #3366, .NOT_KNOWN. ) ;
#12595=CARTESIAN_POINT ( 'NONE',  ( 114.5547881442453217, -4.153390946401321671, -8.397313243818183892 ) ) ;
#12599=CARTESIAN_POINT ( 'NONE',  ( 125.4463081442452932, -4.153390946401325223, -8.397313243818185668 ) ) ;
#12600=CARTESIAN_POINT ( 'NONE',  ( 119.6034614775786196, -3.505236298600246325, -18.68346056562440793 ) ) ;
#12604=CARTESIAN_POINT ( 'NONE',  ( 120.0572748109119772, -3.383040157471821630, -19.15922257007629170 ) ) ;
#12606=CARTESIAN_POINT ( 'NONE',  ( 117.6180281442453150, -0.4660016031367893996, -10.09054647747474043 ) ) ;
#12607=CARTESIAN_POINT ( 'NONE',  ( 114.2711548109119803, -9.988377603198976828, -10.36322818467138340 ) ) ;
#12608=CARTESIAN_POINT ( 'NONE',  ( 114.6682414775786469, -7.894159318335828068, -9.358103419637847864 ) ) ;
#12609=CARTESIAN_POINT ( 'NONE',  ( 125.4463081442452932, -4.153390946401325223, -8.397313243818185668 ) ) ;
#12610=CARTESIAN_POINT ( 'NONE',  ( 113.5337081442453240, -9.261995988541697145, -16.69588392320189030 ) ) ;
#12611=ORIENTED_EDGE ( 'NONE', *, *, #14992, .F. ) ;
#12612=CARTESIAN_POINT ( 'NONE',  ( 122.2696148109119889, -5.574606645277164318, -18.38911715685844683 ) ) ;
#12614=AXIS2_PLACEMENT_3D ( 'NONE', #23741, #34637, #3197 ) ;
#12615=CARTESIAN_POINT ( 'NONE',  ( 113.8588425628257284, -2.263366209404213958, -18.10533625161307114 ) ) ;
#12620=ADVANCED_FACE ( 'NONE', ( #4620 ), #458, .T. ) ;
#12622=EDGE_CURVE ( 'NONE', #18302, #12590, #37083, .T. ) ;
#12623=CARTESIAN_POINT ( 'NONE',  ( 119.5467348109119712, -4.089484607189486809, -7.948022111789456723 ) ) ;
#12624=ORIENTED_EDGE ( 'NONE', *, *, #12622, .F. ) ;
#12625=CARTESIAN_POINT ( 'NONE',  ( 121.7590748109119687, -7.893985811506177619, -18.51759400769804742 ) ) ;
#12626=FACE_OUTER_BOUND ( 'NONE', #17290, .T. ) ;
#12628=CARTESIAN_POINT ( 'NONE',  ( 120.1140014775786398, -1.561330072975668504, -17.79121239304076951 ) ) ;
#12629=CARTESIAN_POINT ( 'NONE',  ( 119.6601881442453106, -8.166667518702819706, -8.995218007635861213 ) ) ;
#12636=CARTESIAN_POINT ( 'NONE',  ( 124.4819548109119722, -2.084020599724406786, -8.691656652584148546 ) ) ;
#12637=B_SPLINE_CURVE_WITH_KNOTS ( 'NONE', 3,
 ( #116, #28165, #17894, #3749, #35424, #35196, #32012, #38855, #7623, #8084, #34961, #42075, #28381, #3972, #4200, #14925, #27943, #775, #21763, #41853, #563, #7395, #1009, #4429, #31791, #42746, #18345, #42294, #11511, #32238 ),
 .UNSPECIFIED., .F., .F.,
 ( 4, 2, 2, 1, 1, 1, 2, 2, 2, 1, 1, 1, 2, 2, 1, 1, 2, 2, 4 ),
 ( 0.000000000000000000, 0.2499999999997726818, 0.3749999999996590505, 0.4374999999996024291, 0.4687499999995737299, 0.4843749999995729527, 0.4921874999995729527, 0.4999999999995730082, 0.6249999999998475664, 0.6874999999999731326, 0.7187500000000250910, 0.7343750000000514033, 0.7421875000000531797, 0.7500000000000549560, 0.8125000000000354161, 0.8437500000000255351, 0.8593750000000209832, 0.8750000000000164313, 1.000000000000000000 ),
 .UNSPECIFIED. ) ;
#12640=CARTESIAN_POINT ( 'NONE',  ( 117.9016614775786280, -0.1624402480850797581, -16.17319339645315424 ) ) ;
#12643=CARTESIAN_POINT ( 'NONE',  ( 111.6050014775786536, 0.1319031606808879209, -14.10382304977623669 ) ) ;
#12644=CARTESIAN_POINT ( 'NONE',  ( 125.1059481442452750, -8.166667518702819706, -8.995218007635861213 ) ) ;
#12645=EDGE_LOOP ( 'NONE', ( #19982, #33835, #14528, #44732, #23764 ) ) ;
#12646=CARTESIAN_POINT ( 'NONE',  ( 122.6099748109119929, -0.8288870151387760510, -10.36305467784173118 ) ) ;
#12647=CARTESIAN_POINT ( 'NONE',  ( 116.7104014775786425, -0.4660016031367893996, -10.09054647747474043 ) ) ;
#12648=CARTESIAN_POINT ( 'NONE',  ( 122.6099748109119929, -9.261995988541697145, -16.69588392320189030 ) ) ;
#12649=CARTESIAN_POINT ( 'NONE',  ( 122.4965214775786251, 0.1319031606808879209, -14.10382304977623669 ) ) ;
#12651=CARTESIAN_POINT ( 'NONE',  ( 123.4660871540078375, -2.348512537728041583, -17.99195118506215962 ) ) ;
#12652=AXIS2_PLACEMENT_3D ( 'NONE', #39477, #1389, #8013 ) ;
#12653=CARTESIAN_POINT ( 'NONE',  ( 122.7234281442452755, -5.638512984488999180, -18.83840828888717311 ) ) ;
#12655=CARTESIAN_POINT ( 'NONE',  ( 124.5386814775786206, -5.638512984488999180, -18.83840828888717311 ) ) ;
#12658=CARTESIAN_POINT ( 'NONE',  ( 119.1138497606643512, -2.236191541394346061, -18.14152338500401029 ) ) ;
#12661=CARTESIAN_POINT ( 'NONE',  ( 118.2987481442453088, -7.894159318335828068, -9.358103419637847864 ) ) ;
#12662=CARTESIAN_POINT ( 'NONE',  ( 111.5482748109120053, -0.1624402480850797581, -16.17319339645315424 ) ) ;
#12663=CARTESIAN_POINT ( 'NONE',  ( 126.6690297232769780, -6.379022919317676177, -18.39419181305856910 ) ) ;
#12664=EDGE_LOOP ( 'NONE', ( #7997, #35155, #30719, #10939 ) ) ;
#12666=CARTESIAN_POINT ( 'NONE',  ( 115.2355081442453155, 0.1319031606808879209, -14.10382304977623669 ) ) ;
#12669=CARTESIAN_POINT ( 'NONE',  ( 111.9453614775786434, -7.894159318335828068, -9.358103419637847864 ) ) ;
#12671=CARTESIAN_POINT ( 'NONE',  ( 123.6877814775786533, -3.383040157471821630, -19.15922257007629170 ) ) ;
#12673=CARTESIAN_POINT ( 'NONE',  ( 124.1415948109119540, -3.505236298600246325, -18.68346056562440793 ) ) ;
#12676=CARTESIAN_POINT ( 'NONE',  ( 125.3328548109119964, -9.261995988541697145, -16.69588392320189030 ) ) ;
#12678=CARTESIAN_POINT ( 'NONE',  ( 126.4106614775786284, -6.222761293078241884, -8.102969835052219238 ) ) ;
#12679=CARTESIAN_POINT ( 'NONE',  ( 119.9438214775786378, -2.084020599724406786, -8.691656652584148546 ) ) ;
#12680=DIRECTION ( 'NONE',  ( 1.000000000000000000, 0.000000000000000000, 0.000000000000000000 ) ) ;
#12684=CARTESIAN_POINT ( 'NONE',  ( 113.1933481442453058, -5.574606645277164318, -18.38911715685844683 ) ) ;
#12688=CARTESIAN_POINT ( 'NONE',  ( 121.0783548109119749, 0.2603800115204892296, -16.42320221600525088 ) ) ;
#12689=CARTESIAN_POINT ( 'NONE',  ( 120.8514481442452961, -7.893985811506177619, -18.51759400769804742 ) ) ;
#12691=CARTESIAN_POINT ( 'NONE',  ( 117.9583881442453048, -10.30919188438810075, -12.61870101168855918 ) ) ;
#12692=FACE_OUTER_BOUND ( 'NONE', #15088, .T. ) ;
#12693=ORIENTED_EDGE ( 'NONE', *, *, #13141, .T. ) ;
#12694=CARTESIAN_POINT ( 'NONE',  ( 114.4413348109119823, -0.8288870151387760510, -10.36305467784173118 ) ) ;
#12695=CARTESIAN_POINT ( 'NONE',  ( 112.6828081442453282, -2.084020599724406786, -8.691656652584148546 ) ) ;
#12696=CARTESIAN_POINT ( 'NONE',  ( 121.9292548109119849, -1.561330072975668948, -17.79121239304076951 ) ) ;
#12697=CARTESIAN_POINT ( 'NONE',  ( 112.3991748109119868, -8.166667518702817929, -8.995218007635859436 ) ) ;
#12698=CARTESIAN_POINT ( 'NONE',  ( 114.1009748109119784, -5.574606645277164318, -18.38911715685844683 ) ) ;
#12699=ORIENTED_EDGE ( 'NONE', *, *, #7752, .T. ) ;
#12700=CARTESIAN_POINT ( 'NONE',  ( 119.0929214775786278, -4.153390946401325223, -8.397313243818185668 ) ) ;
#12701=CARTESIAN_POINT ( 'NONE',  ( 125.9001214775786224, -4.089484607189486809, -7.948022111789456723 ) ) ;
#12703=CARTESIAN_POINT ( 'NONE',  ( 119.5467348109119712, -5.574606645277164318, -18.38911715685844683 ) ) ;
#12708=CARTESIAN_POINT ( 'NONE',  ( 122.4397948109119767, -9.988377603198976828, -10.36322818467138340 ) ) ;
#12710=CARTESIAN_POINT ( 'NONE',  ( 112.0588148109119828, 0.5811942927096154232, -14.16772938898807155 ) ) ;
#12715=CARTESIAN_POINT ( 'NONE',  ( 125.6732148109119862, -9.859900752359378018, -12.68260735090039759 ) ) ;
#12717=CARTESIAN_POINT ( 'NONE',  ( 126.1270281442452870, -10.30919188438810075, -12.61870101168855918 ) ) ;
#12718=CARTESIAN_POINT ( 'NONE',  ( 117.9583881442453048, 0.1319031606808879209, -14.10382304977623669 ) ) ;
#12719=CARTESIAN_POINT ( 'NONE',  ( 125.4463081442452932, -4.153390946401325223, -8.397313243818185668 ) ) ;
#12721=CARTESIAN_POINT ( 'NONE',  ( 122.0427081442452817, 0.5811942927096110934, -14.16772938898807510 ) ) ;
#12722=CARTESIAN_POINT ( 'NONE',  ( 115.5758681442453053, -1.561330072975668060, -17.79121239304076951 ) ) ;
#12724=CARTESIAN_POINT ( 'NONE',  ( 151.2860562277021472, -4.863998795839242995, -13.39321520033831447 ) ) ;
#12725=( BOUNDED_SURFACE ( )  B_SPLINE_SURFACE ( 1, 2, ( 
 ( #1180, #31955, #15093, #29003, #18064, #36274, #42911, #18957, #29221, #11673, #32847, #25801, #18287, #39711, #15537, #25136, #43357, #42689, #25582, #39031, #24904, #39485, #35368, #38799, #22156, #21483, #7570, #4144, #14642, #42465, #36049, #21928, #4817, #954, #11457, #8694, #2295, #29670, #5487, #26251, #12352, #40162, #5942, #9374, #43582, #30349, #19865, #40849, #19407, #2522, #40389, #19186, #8924, #12580, #22826, #39934, #16223, #16675, #30570, #15993, #13029, #33753, #9150, #36717, #2070, #29898, #16449, #1838, #44273, #26485, #23283, #33065, #44041, #43814, #26927, #12805, #23519, #15767, #33294, #23057, #9604, #36943, #37407, #5713, #20097, #22600, #12126, #19631, #33515, #33982, #37167, #6176, #2751, #40617, #30128, #26029, #36500, #5269, #26705, #3862, #20984, #20544, #17563, #41741, #31457, #41962, #23747, #38295, #44947, #17784, #6412, #20319, #44490, #13256, #34857, #6631, #28054, #20765, #13920, #13705, #37638, #27159, #225, #10728, #31017, #41526, #6858, #27612, #34203, #10505, #41308, #41081, #17348, #9837, #2978, #7074, #3644, #34423, #16906, #30798, #7287, #13483, #37856, #27830, #14139, #31237, #44723, #24406, #10069, #24628, #27385, #38510, #21203, #23970, #3204, #17129, #38080, #9, #10284, #24188, #35082, #34644, #3430, #12469, #28504, #15660, #19305, #669, #43695, #43478, #1735, #14586, #31678, #26369, #25306, #36834, #447, #42410, #18232, #4081, #35770, #35541, #32958, #39200, #7966, #9043, #35310, #11174, #28727, #4312, #22942, #21876, #42186, #7511, #22714, #10946, #896, #29561, #1959, #25078, #4540, #5603, #14363, #8811, #19073, #29783, #12245, #21650, #26142, #38970, #28277, #24849, #7739, #40277, #32128, #11397, #18005, #21426, #38741, #14815, #31904, #40044, #42633, #36612, #5388, #33184, #15887, #27049, #37521, #30010, #23867, #44383, #13377, #44161, #6523, #9954, #6058, #24083, #41194, #40733, #37753, #16796, #20439, #17023, #13146, #3096, #34322, #30463, #9489, #30915, #44838, #5829, #12925, #40968, #9722, #23635, #16336 ),
 ( #40508, #13594, #43927, #33867, #30692, #27503, #30239, #6294, #41422, #37977, #10177, #20214, #19526, #34099, #23404, #2867, #2409, #33403, #2178, #26821, #16108, #37288, #44611, #37057, #9268, #12695, #19978, #23179, #27279, #2636, #26595, #19749, #33634, #16568, #14256, #24736, #17240, #11063, #31574, #569, #31348, #31131, #14479, #7180, #11288, #13815, #27726, #6752, #25196, #42300, #14035, #35432, #28173, #21319, #21090, #45055, #34538, #24965, #18124, #38410, #3755, #42081, #34967, #41642, #3978, #3538, #20662, #38625, #3319, #10398, #28389, #38861, #27951, #24308, #38194, #14704, #20880, #122, #35204, #7629, #7401, #6971, #17901, #17453, #4206, #34755, #32019, #21543, #41859, #10621, #24523, #343, #31798, #17677, #10841, #783, #28618, #42528, #22438, #26086, #8090, #5332, #5101, #8537, #21993, #39094, #33130, #32687, #43640, #7864, #35883, #25647, #11517, #43197, #42968, #39766, #1457, #15378, #15829, #42754, #4653, #36110, #11735, #29726, #29282, #4435, #14931, #29505, #18353, #8313, #36331, #8756, #18574, #11963, #12414, #21770, #15601, #25862, #36557, #19016, #29059, #32903, #32466, #35663, #32244, #1242, #19249, #15153, #18798, #25422, #28842, #1015, #39551, #39323, #1679, #22213, #43421, #4881, #12186, #39990, #22661, #1900, #36780, #30637, #6003, #20163, #5772, #5551, #34046, #26772, #30861, #33351, #2124, #26314, #44784, #16743, #33579, #9901, #2583, #40912, #40681, #19469, #8987, #44554, #37702, #12873, #23346, #33813, #9433, #16053, #23584, #23124, #40222, #44333, #22887, #29959, #2814, #13319, #2354, #43874, #12646, #34271, #40453, #19692, #9665, #27224, #13093, #26542, #37468, #37001, #23814, #9215, #6473, #41142, #16286, #30188, #44106, #19926, #26992, #37229, #16514, #20385, #30413, #3044, #16968, #6240, #10568, #31079, #3490, #17406, #21266, #3263, #35148, #13981, #24684, #20610, #290, #31295, #3926, #14204, #24909, #34485, #10346, #24464, #17846, #38356, #31745, #7131, #21489, #10128, #13542, #21042, #17188, #35373, #10787, #38571, #513 ) ),
 .UNSPECIFIED., .F., .F., .T. ) 
 B_SPLINE_SURFACE_WITH_KNOTS ( ( 2, 2 ),
 ( 3, 2, 2, 2, 2, 2, 2, 2, 2, 2, 2, 2, 2, 2, 2, 2, 2, 2, 2, 2, 2, 2, 2, 2, 2, 2, 2, 2, 2, 2, 2, 2, 2, 2, 2, 2, 2, 2, 2, 2, 2, 2, 2, 2, 2, 2, 2, 2, 2, 2, 2, 2, 2, 2, 2, 2, 2, 2, 2, 2, 2, 2, 2, 2, 2, 2, 2, 2, 2, 2, 2, 2, 2, 2, 2, 2, 2, 2, 2, 2, 2, 2, 2, 2, 2, 2, 2, 2, 2, 2, 2, 2, 2, 2, 2, 2, 2, 2, 2, 2, 2, 2, 2, 2, 2, 2, 2, 2, 2, 2, 2, 2, 2, 2, 2, 2, 2, 2, 2, 2, 2, 2, 2, 2, 2, 2, 2, 2, 3 ),
 ( 0.000000000000000000, 1.000000000000000000 ),
 ( 0.000000000000000000, 0.007812500000000000000, 0.01562500000000000000, 0.02343750000000000000, 0.03125000000000000000, 0.03906250000000000000, 0.04687500000000000000, 0.05468750000000000000, 0.06250000000000000000, 0.07031250000000000000, 0.07812500000000000000, 0.08593750000000000000, 0.09375000000000000000, 0.1015625000000000000, 0.1093750000000000000, 0.1171875000000000000, 0.1250000000000000000, 0.1328125000000000000, 0.1406250000000000000, 0.1484375000000000000, 0.1562500000000000000, 0.1640625000000000000, 0.1718750000000000000, 0.1796875000000000000, 0.1875000000000000000, 0.1953125000000000000, 0.2031250000000000000, 0.2109375000000000000, 0.2187500000000000000, 0.2265625000000000000, 0.2343750000000000000, 0.2421875000000000000, 0.2500000000000000000, 0.2578125000000000000, 0.2656250000000000000, 0.2734375000000000000, 0.2812500000000000000, 0.2890625000000000000, 0.2968750000000000000, 0.3046875000000000000, 0.3125000000000000000, 0.3203125000000000000, 0.3281250000000000000, 0.3359375000000000000, 0.3437500000000000000, 0.3515625000000000000, 0.3593750000000000000, 0.3671875000000000000, 0.3750000000000000000, 0.3828125000000000000, 0.3906250000000000000, 0.3984375000000000000, 0.4062500000000000000, 0.4140625000000000000, 0.4218750000000000000, 0.4296875000000000000, 0.4375000000000000000, 0.4453125000000000000, 0.4531250000000000000, 0.4609375000000000000, 0.4687500000000000000, 0.4765625000000000000, 0.4843750000000000000, 0.4921875000000000000, 0.5000000000000000000, 0.5078125000000000000, 0.5156250000000000000, 0.5234375000000000000, 0.5312500000000000000, 0.5390625000000000000, 0.5468750000000000000, 0.5546875000000000000, 0.5625000000000000000, 0.5703125000000000000, 0.5781250000000000000, 0.5859375000000000000, 0.5937500000000000000, 0.6015625000000000000, 0.6093750000000000000, 0.6171875000000000000, 0.6250000000000000000, 0.6328125000000000000, 0.6406250000000000000, 0.6484375000000000000, 0.6562500000000000000, 0.6640625000000000000, 0.6718750000000000000, 0.6796875000000000000, 0.6875000000000000000, 0.6953125000000000000, 0.7031250000000000000, 0.7109375000000000000, 0.7187500000000000000, 0.7265625000000000000, 0.7343750000000000000, 0.7421875000000000000, 0.7500000000000000000, 0.7578125000000000000, 0.7656250000000000000, 0.7734375000000000000, 0.7812500000000000000, 0.7890625000000000000, 0.7968750000000000000, 0.8046875000000000000, 0.8125000000000000000, 0.8203125000000000000, 0.8281250000000000000, 0.8359375000000000000, 0.8437500000000000000, 0.8515625000000000000, 0.8593750000000000000, 0.8671875000000000000, 0.8750000000000000000, 0.8828125000000000000, 0.8906250000000000000, 0.8984375000000000000, 0.9062500000000000000, 0.9140625000000000000, 0.9218750000000000000, 0.9296875000000000000, 0.9375000000000000000, 0.9453125000000000000, 0.9531250000000000000, 0.9609375000000000000, 0.9687500000000000000, 0.9765625000000000000, 0.9843750000000000000, 0.9921875000000000000, 1.000000000000000000 ),
 .UNSPECIFIED. ) 
 GEOMETRIC_REPRESENTATION_ITEM ( )  RATIONAL_B_SPLINE_SURFACE ( (
 ( 1.000000000000000000, 0.9238795325112869605, 1.000000000000000000, 0.9238795325112869605, 1.000000000000000000, 0.9238795325112869605, 1.000000000000000000, 0.9238795325112869605, 1.000000000000000000, 0.9238795325112869605, 1.000000000000000000, 0.9238795325112869605, 1.000000000000000000, 0.9238795325112869605, 1.000000000000000000, 0.9238795325112869605, 1.000000000000000000, 0.9238795325112869605, 1.000000000000000000, 0.9238795325112869605, 1.000000000000000000, 0.9238795325112869605, 1.000000000000000000, 0.9238795325112869605, 1.000000000000000000, 0.9238795325112869605, 1.000000000000000000, 0.9238795325112869605, 1.000000000000000000, 0.9238795325112869605, 1.000000000000000000, 0.9238795325112869605, 1.000000000000000000, 0.9238795325112869605, 1.000000000000000000, 0.9238795325112869605, 1.000000000000000000, 0.9238795325112869605, 1.000000000000000000, 0.9238795325112869605, 1.000000000000000000, 0.9238795325112869605, 1.000000000000000000, 0.9238795325112869605, 1.000000000000000000, 0.9238795325112869605, 1.000000000000000000, 0.9238795325112869605, 1.000000000000000000, 0.9238795325112869605, 1.000000000000000000, 0.9238795325112869605, 1.000000000000000000, 0.9238795325112869605, 1.000000000000000000, 0.9238795325112869605, 1.000000000000000000, 0.9238795325112869605, 1.000000000000000000, 0.9238795325112869605, 1.000000000000000000, 0.9238795325112869605, 1.000000000000000000, 0.9238795325112869605, 1.000000000000000000, 0.9238795325112869605, 1.000000000000000000, 0.9238795325112869605, 1.000000000000000000, 0.9238795325112869605, 1.000000000000000000, 0.9238795325112869605, 1.000000000000000000, 0.9238795325112869605, 1.000000000000000000, 0.9238795325112869605, 1.000000000000000000, 0.9238795325112869605, 1.000000000000000000, 0.9238795325112869605, 1.000000000000000000, 0.9238795325112869605, 1.000000000000000000, 0.9238795325112869605, 1.000000000000000000, 0.9238795325112869605, 1.000000000000000000, 0.9238795325112869605, 1.000000000000000000, 0.9238795325112869605, 1.000000000000000000, 0.9238795325112869605, 1.000000000000000000, 0.9238795325112869605, 1.000000000000000000, 0.9238795325112869605, 1.000000000000000000, 0.9238795325112869605, 1.000000000000000000, 0.9238795325112869605, 1.000000000000000000, 0.9238795325112869605, 1.000000000000000000, 0.9238795325112869605, 1.000000000000000000, 0.9238795325112869605, 1.000000000000000000, 0.9238795325112869605, 1.000000000000000000, 0.9238795325112869605, 1.000000000000000000, 0.9238795325112869605, 1.000000000000000000, 0.9238795325112869605, 1.000000000000000000, 0.9238795325112869605, 1.000000000000000000, 0.9238795325112869605, 1.000000000000000000, 0.9238795325112869605, 1.000000000000000000, 0.9238795325112869605, 1.000000000000000000, 0.9238795325112869605, 1.000000000000000000, 0.9238795325112869605, 1.000000000000000000, 0.9238795325112869605, 1.000000000000000000, 0.9238795325112869605, 1.000000000000000000, 0.9238795325112869605, 1.000000000000000000, 0.9238795325112869605, 1.000000000000000000, 0.9238795325112869605, 1.000000000000000000, 0.9238795325112869605, 1.000000000000000000, 0.9238795325112869605, 1.000000000000000000, 0.9238795325112869605, 1.000000000000000000, 0.9238795325112869605, 1.000000000000000000, 0.9238795325112869605, 1.000000000000000000, 0.9238795325112869605, 1.000000000000000000, 0.9238795325112869605, 1.000000000000000000, 0.9238795325112869605, 1.000000000000000000, 0.9238795325112869605, 1.000000000000000000, 0.9238795325112869605, 1.000000000000000000, 0.9238795325112869605, 1.000000000000000000, 0.9238795325112869605, 1.000000000000000000, 0.9238795325112869605, 1.000000000000000000, 0.9238795325112869605, 1.000000000000000000, 0.9238795325112869605, 1.000000000000000000, 0.9238795325112869605, 1.000000000000000000, 0.9238795325112869605, 1.000000000000000000, 0.9238795325112869605, 1.000000000000000000, 0.9238795325112869605, 1.000000000000000000, 0.9238795325112869605, 1.000000000000000000, 0.9238795325112869605, 1.000000000000000000, 0.9238795325112869605, 1.000000000000000000, 0.9238795325112869605, 1.000000000000000000, 0.9238795325112869605, 1.000000000000000000, 0.9238795325112869605, 1.000000000000000000, 0.9238795325112869605, 1.000000000000000000, 0.9238795325112869605, 1.000000000000000000, 0.9238795325112869605, 1.000000000000000000, 0.9238795325112869605, 1.000000000000000000, 0.9238795325112869605, 1.000000000000000000, 0.9238795325112869605, 1.000000000000000000, 0.9238795325112869605, 1.000000000000000000, 0.9238795325112869605, 1.000000000000000000, 0.9238795325112869605, 1.000000000000000000, 0.9238795325112869605, 1.000000000000000000, 0.9238795325112869605, 1.000000000000000000, 0.9238795325112869605, 1.000000000000000000, 0.9238795325112869605, 1.000000000000000000, 0.9238795325112869605, 1.000000000000000000, 0.9238795325112869605, 1.000000000000000000, 0.9238795325112869605, 1.000000000000000000, 0.9238795325112869605, 1.000000000000000000, 0.9238795325112869605, 1.000000000000000000, 0.9238795325112869605, 1.000000000000000000, 0.9238795325112869605, 1.000000000000000000, 0.9238795325112869605, 1.000000000000000000, 0.9238795325112869605, 1.000000000000000000, 0.9238795325112869605, 1.000000000000000000, 0.9238795325112869605, 1.000000000000000000, 0.9238795325112869605, 1.000000000000000000, 0.9238795325112869605, 1.000000000000000000, 0.9238795325112869605, 1.000000000000000000, 0.9238795325112869605, 1.000000000000000000, 0.9238795325112869605, 1.000000000000000000, 0.9238795325112869605, 1.000000000000000000, 0.9238795325112869605, 1.000000000000000000, 0.9238795325112869605, 1.000000000000000000, 0.9238795325112869605, 1.000000000000000000, 0.9238795325112869605, 1.000000000000000000, 0.9238795325112869605, 1.000000000000000000),
 ( 1.000000000000000000, 0.9238795325112869605, 1.000000000000000000, 0.9238795325112869605, 1.000000000000000000, 0.9238795325112869605, 1.000000000000000000, 0.9238795325112869605, 1.000000000000000000, 0.9238795325112869605, 1.000000000000000000, 0.9238795325112869605, 1.000000000000000000, 0.9238795325112869605, 1.000000000000000000, 0.9238795325112869605, 1.000000000000000000, 0.9238795325112869605, 1.000000000000000000, 0.9238795325112869605, 1.000000000000000000, 0.9238795325112869605, 1.000000000000000000, 0.9238795325112869605, 1.000000000000000000, 0.9238795325112869605, 1.000000000000000000, 0.9238795325112869605, 1.000000000000000000, 0.9238795325112869605, 1.000000000000000000, 0.9238795325112869605, 1.000000000000000000, 0.9238795325112869605, 1.000000000000000000, 0.9238795325112869605, 1.000000000000000000, 0.9238795325112869605, 1.000000000000000000, 0.9238795325112869605, 1.000000000000000000, 0.9238795325112869605, 1.000000000000000000, 0.9238795325112869605, 1.000000000000000000, 0.9238795325112869605, 1.000000000000000000, 0.9238795325112869605, 1.000000000000000000, 0.9238795325112869605, 1.000000000000000000, 0.9238795325112869605, 1.000000000000000000, 0.9238795325112869605, 1.000000000000000000, 0.9238795325112869605, 1.000000000000000000, 0.9238795325112869605, 1.000000000000000000, 0.9238795325112869605, 1.000000000000000000, 0.9238795325112869605, 1.000000000000000000, 0.9238795325112869605, 1.000000000000000000, 0.9238795325112869605, 1.000000000000000000, 0.9238795325112869605, 1.000000000000000000, 0.9238795325112869605, 1.000000000000000000, 0.9238795325112869605, 1.000000000000000000, 0.9238795325112869605, 1.000000000000000000, 0.9238795325112869605, 1.000000000000000000, 0.9238795325112869605, 1.000000000000000000, 0.9238795325112869605, 1.000000000000000000, 0.9238795325112869605, 1.000000000000000000, 0.9238795325112869605, 1.000000000000000000, 0.9238795325112869605, 1.000000000000000000, 0.9238795325112869605, 1.000000000000000000, 0.9238795325112869605, 1.000000000000000000, 0.9238795325112869605, 1.000000000000000000, 0.9238795325112869605, 1.000000000000000000, 0.9238795325112869605, 1.000000000000000000, 0.9238795325112869605, 1.000000000000000000, 0.9238795325112869605, 1.000000000000000000, 0.9238795325112869605, 1.000000000000000000, 0.9238795325112869605, 1.000000000000000000, 0.9238795325112869605, 1.000000000000000000, 0.9238795325112869605, 1.000000000000000000, 0.9238795325112869605, 1.000000000000000000, 0.9238795325112869605, 1.000000000000000000, 0.9238795325112869605, 1.000000000000000000, 0.9238795325112869605, 1.000000000000000000, 0.9238795325112869605, 1.000000000000000000, 0.9238795325112869605, 1.000000000000000000, 0.9238795325112869605, 1.000000000000000000, 0.9238795325112869605, 1.000000000000000000, 0.9238795325112869605, 1.000000000000000000, 0.9238795325112869605, 1.000000000000000000, 0.9238795325112869605, 1.000000000000000000, 0.9238795325112869605, 1.000000000000000000, 0.9238795325112869605, 1.000000000000000000, 0.9238795325112869605, 1.000000000000000000, 0.9238795325112869605, 1.000000000000000000, 0.9238795325112869605, 1.000000000000000000, 0.9238795325112869605, 1.000000000000000000, 0.9238795325112869605, 1.000000000000000000, 0.9238795325112869605, 1.000000000000000000, 0.9238795325112869605, 1.000000000000000000, 0.9238795325112869605, 1.000000000000000000, 0.9238795325112869605, 1.000000000000000000, 0.9238795325112869605, 1.000000000000000000, 0.9238795325112869605, 1.000000000000000000, 0.9238795325112869605, 1.000000000000000000, 0.9238795325112869605, 1.000000000000000000, 0.9238795325112869605, 1.000000000000000000, 0.9238795325112869605, 1.000000000000000000, 0.9238795325112869605, 1.000000000000000000, 0.9238795325112869605, 1.000000000000000000, 0.9238795325112869605, 1.000000000000000000, 0.9238795325112869605, 1.000000000000000000, 0.9238795325112869605, 1.000000000000000000, 0.9238795325112869605, 1.000000000000000000, 0.9238795325112869605, 1.000000000000000000, 0.9238795325112869605, 1.000000000000000000, 0.9238795325112869605, 1.000000000000000000, 0.9238795325112869605, 1.000000000000000000, 0.9238795325112869605, 1.000000000000000000, 0.9238795325112869605, 1.000000000000000000, 0.9238795325112869605, 1.000000000000000000, 0.9238795325112869605, 1.000000000000000000, 0.9238795325112869605, 1.000000000000000000, 0.9238795325112869605, 1.000000000000000000, 0.9238795325112869605, 1.000000000000000000, 0.9238795325112869605, 1.000000000000000000, 0.9238795325112869605, 1.000000000000000000, 0.9238795325112869605, 1.000000000000000000, 0.9238795325112869605, 1.000000000000000000, 0.9238795325112869605, 1.000000000000000000, 0.9238795325112869605, 1.000000000000000000, 0.9238795325112869605, 1.000000000000000000, 0.9238795325112869605, 1.000000000000000000, 0.9238795325112869605, 1.000000000000000000, 0.9238795325112869605, 1.000000000000000000, 0.9238795325112869605, 1.000000000000000000, 0.9238795325112869605, 1.000000000000000000, 0.9238795325112869605, 1.000000000000000000, 0.9238795325112869605, 1.000000000000000000, 0.9238795325112869605, 1.000000000000000000, 0.9238795325112869605, 1.000000000000000000, 0.9238795325112869605, 1.000000000000000000, 0.9238795325112869605, 1.000000000000000000, 0.9238795325112869605, 1.000000000000000000, 0.9238795325112869605, 1.000000000000000000, 0.9238795325112869605, 1.000000000000000000, 0.9238795325112869605, 1.000000000000000000, 0.9238795325112869605, 1.000000000000000000, 0.9238795325112869605, 1.000000000000000000, 0.9238795325112869605, 1.000000000000000000, 0.9238795325112869605, 1.000000000000000000, 0.9238795325112869605, 1.000000000000000000, 0.9238795325112869605, 1.000000000000000000, 0.9238795325112869605, 1.000000000000000000) ) ) 
 REPRESENTATION_ITEM ( '' )  SURFACE ( )  );
#12726=CARTESIAN_POINT ( 'NONE',  ( 123.1205148109119563, -7.643976991954077427, -18.09477374809248928 ) ) ;
#12727=CARTESIAN_POINT ( 'NONE',  ( 124.9924948109119924, -4.089484607189486809, -7.948022111789456723 ) ) ;
#12732=CARTESIAN_POINT ( 'NONE',  ( 117.2209414775786485, -2.084020599724406786, -8.691656652584148546 ) ) ;
#12733=CARTESIAN_POINT ( 'NONE',  ( 115.0653281442453277, -3.505236298600246325, -18.68346056562440793 ) ) ;
#12737=CARTESIAN_POINT ( 'NONE',  ( 122.8368814775786291, -7.894159318335801423, -9.358103419637830100 ) ) ;
#12738=CARTESIAN_POINT ( 'NONE',  ( 126.4673881442452910, -7.894159318335828068, -9.358103419637847864 ) ) ;
#12745=ORIENTED_EDGE ( 'NONE', *, *, #15835, .F. ) ;
#12746=CARTESIAN_POINT ( 'NONE',  ( 118.4689281442453392, 0.9020085738987339008, -11.91225656197089222 ) ) ;
#12747=CARTESIAN_POINT ( 'NONE',  ( 123.5743281442453139, -2.084020599724406786, -8.691656652584148546 ) ) ;
#12748=CARTESIAN_POINT ( 'NONE',  ( 113.8173414775786512, -9.565557343593413364, -10.61323700422348004 ) ) ;
#12752=CARTESIAN_POINT ( 'NONE',  ( 113.2500748109119968, -6.344957434206662583, -7.627207830600332805 ) ) ;
#12754=CARTESIAN_POINT ( 'NONE',  ( 125.0492214775786266, -6.344957434206665248, -7.627207830600338134 ) ) ;
#12756=ORIENTED_EDGE ( 'NONE', *, *, #851, .F. ) ;
#12757=CARTESIAN_POINT ( 'NONE',  ( 114.3846081442453197, -10.63000616557722466, -14.87417383870573495 ) ) ;
#12760=CARTESIAN_POINT ( 'NONE',  ( 115.5758681442453053, -7.894159318335828068, -9.358103419637847864 ) ) ;
#12761=CARTESIAN_POINT ( 'NONE',  ( 127.0264730702704838, -4.566927068118824984, -18.78905399823883826 ) ) ;
#12762=CARTESIAN_POINT ( 'NONE',  ( 111.8319081442453182, -5.638512984488999180, -18.83840828888717311 ) ) ;
#12764=ORIENTED_EDGE ( 'NONE', *, *, #34740, .T. ) ;
#12765=CARTESIAN_POINT ( 'NONE',  ( 123.1772414775786189, -4.089484607189486809, -7.948022111789456723 ) ) ;
#12769=CARTESIAN_POINT ( 'NONE',  ( 137.4282737236246987, -3.645634682062916188, -8.450363672471354448 ) ) ;
#12771=CARTESIAN_POINT ( 'NONE',  ( 113.6471614775786492, -4.153390946401321671, -8.397313243818183892 ) ) ;
#12774=CARTESIAN_POINT ( 'NONE',  ( 115.6893214775786447, -9.859900752359374465, -12.68260735090039404 ) ) ;
#12775=CARTESIAN_POINT ( 'NONE',  ( 115.9729548109119861, -6.344957434206662583, -7.627207830600332805 ) ) ;
#12777=CARTESIAN_POINT ( 'NONE',  ( 113.7038881442453402, -3.383040157471821630, -19.15922257007629170 ) ) ;
#12778=CARTESIAN_POINT ( 'NONE',  ( 114.2144281442453178, -1.833838273342658809, -17.42832698103878286 ) ) ;
#12779=CARTESIAN_POINT ( 'NONE',  ( 123.0070614775786169, 0.9020085738987339008, -11.91225656197089222 ) ) ;
#12780=CARTESIAN_POINT ( 'NONE',  ( 122.6667014775786413, -7.893985811506177619, -18.51759400769804742 ) ) ;
#12782=CARTESIAN_POINT ( 'NONE',  ( 112.3991748109119868, -8.166667518702817929, -8.995218007635859436 ) ) ;
#12788=CARTESIAN_POINT ( 'NONE',  ( 119.7169148109119874, -9.988377603198976828, -10.36322818467138340 ) ) ;
#12791=CARTESIAN_POINT ( 'NONE',  ( 124.6713397424434078, -0.9924539043446091169, -17.29976612834908423 ) ) ;
#12792=CARTESIAN_POINT ( 'NONE',  ( 116.1431348109119881, 0.1319031606808879209, -14.10382304977623669 ) ) ;
#12793=EDGE_CURVE ( 'NONE', #3055, #45059, #29896, .T. ) ;
#12795=CARTESIAN_POINT ( 'NONE',  ( 119.4900081442453086, -1.834011780172310813, -8.268836392978581529 ) ) ;
#12802=CARTESIAN_POINT ( 'NONE',  ( 121.3619881442452879, -5.574606645277164318, -18.38911715685844683 ) ) ;
#12803=CARTESIAN_POINT ( 'NONE',  ( 120.9649014775786355, -3.383040157471821630, -19.15922257007629170 ) ) ;
#12804=CARTESIAN_POINT ( 'NONE',  ( 112.6828081442453282, -2.084020599724406786, -8.691656652584148546 ) ) ;
#12805=CARTESIAN_POINT ( 'NONE',  ( 115.9729548109119861, -6.344957434206662583, -7.627207830600332805 ) ) ;
#12807=CARTESIAN_POINT ( 'NONE',  ( 126.3063647503471998, -1.053199401995885021, -10.08875103278353258 ) ) ;
#12808=CARTESIAN_POINT ( 'NONE',  ( 118.7525614775786380, -1.833838273342659253, -17.42832698103878286 ) ) ;
#12812=CARTESIAN_POINT ( 'NONE',  ( 119.7736414775786358, -10.30919188438809719, -12.61870101168856273 ) ) ;
#12813=CARTESIAN_POINT ( 'NONE',  ( 114.6682414775786469, -1.561330072975668060, -17.79121239304076596 ) ) ;
#12814=CARTESIAN_POINT ( 'NONE',  ( 120.7947214775786193, -0.8288870151387760510, -10.36305467784173118 ) ) ;
#12815=ORIENTED_EDGE ( 'NONE', *, *, #8010, .T. ) ;
#12820=CARTESIAN_POINT ( 'NONE',  ( 117.6180281442453150, -0.4660016031367893996, -10.09054647747474043 ) ) ;
#12822=CARTESIAN_POINT ( 'NONE',  ( 116.1998614775786507, 0.4262465694468514643, -12.03445270309931736 ) ) ;
#12823=ORIENTED_EDGE ( 'NONE', *, *, #42931, .F. ) ;
#12825=CARTESIAN_POINT ( 'NONE',  ( 111.7184548109119788, -9.261995988541697145, -16.69588392320189030 ) ) ;
#12827=CARTESIAN_POINT ( 'NONE',  ( 119.7736414775786358, 0.1319031606808879209, -14.10382304977623669 ) ) ;
#12830=CARTESIAN_POINT ( 'NONE',  ( 117.2776681442452968, -5.638512984488999180, -18.83840828888717311 ) ) ;
#12833=CARTESIAN_POINT ( 'NONE',  ( 120.1707281442453166, 0.2603800115204892296, -16.42320221600525088 ) ) ;
#12834=CARTESIAN_POINT ( 'NONE',  ( 117.0507614775786465, -10.30919188438810075, -12.61870101168855918 ) ) ;
#12835=CARTESIAN_POINT ( 'NONE',  ( 117.1642148109119859, -0.8288870151387760510, -10.36305467784173118 ) ) ;
#12840=CARTESIAN_POINT ( 'NONE',  ( 123.2339681442453241, -3.505236298600246325, -18.68346056562440793 ) ) ;
#12841=CARTESIAN_POINT ( 'NONE',  ( 122.8560864091100626, -0.9924539043446216624, -17.29976612834909133 ) ) ;
#12847=CARTESIAN_POINT ( 'NONE',  ( 123.6877814775786533, -3.383040157471821630, -19.15922257007629170 ) ) ;
#12849=CARTESIAN_POINT ( 'NONE',  ( 120.1707281442453166, 0.2603800115204892296, -16.42320221600525088 ) ) ;
#12852=CARTESIAN_POINT ( 'NONE',  ( 121.3052614775786111, -1.834011780172310813, -8.268836392978581529 ) ) ;
#12853=CARTESIAN_POINT ( 'NONE',  ( 120.3409081442453044, -0.4660016031367893996, -10.09054647747474043 ) ) ;
#12855=CARTESIAN_POINT ( 'NONE',  ( 123.0070614775786169, -10.15424416112533912, -14.75197769757731336 ) ) ;
#12860=CARTESIAN_POINT ( 'NONE',  ( 118.6164486996681973, -1.172797794773247304, -17.05961127468924587 ) ) ;
#12861=CARTESIAN_POINT ( 'NONE',  ( 123.8579614775786126, -9.859900752359378018, -12.68260735090039759 ) ) ;
#12865=CARTESIAN_POINT ( 'NONE',  ( 117.2209414775786485, -2.084020599724406786, -8.691656652584148546 ) ) ;
#12868=CARTESIAN_POINT ( 'NONE',  ( 113.5904348109119866, -2.084020599724406786, -8.691656652584148546 ) ) ;
#12869=CARTESIAN_POINT ( 'NONE',  ( 122.1561614775786353, -0.4660016031367893996, -10.09054647747474043 ) ) ;
#12873=CARTESIAN_POINT ( 'NONE',  ( 121.7590748109119687, -2.084020599724406786, -8.691656652584148546 ) ) ;
#12874=CARTESIAN_POINT ( 'NONE',  ( 115.4624148109119943, -5.638512984488999180, -18.83840828888717311 ) ) ;
#12875=CARTESIAN_POINT ( 'NONE',  ( 123.8579614775786126, 0.5811942927096110934, -14.16772938898807510 ) ) ;
#12876=CARTESIAN_POINT ( 'NONE',  ( 123.9714148109119805, -8.899110576539710493, -16.42337572283490132 ) ) ;
#12879=CARTESIAN_POINT ( 'NONE',  ( 122.2128881442453263, -1.834011780172310813, -8.268836392978581529 ) ) ;
#12880=CARTESIAN_POINT ( 'NONE',  ( 114.4413348109119823, -0.8288870151387760510, -10.36305467784173118 ) ) ;
#12881=CARTESIAN_POINT ( 'NONE',  ( 125.8433948109119456, -1.834011780172310813, -8.268836392978581529 ) ) ;
#12884=DIRECTION ( 'NONE',  ( 1.000000000000000000, 0.000000000000000000, 0.000000000000000000 ) ) ;
#12890=CARTESIAN_POINT ( 'NONE',  ( 117.6180281442453150, -8.899110576539710493, -16.42337572283490132 ) ) ;
#12891=CARTESIAN_POINT ( 'NONE',  ( 113.7606148109119886, -7.894159318335828068, -9.358103419637847864 ) ) ;
#12892=CARTESIAN_POINT ( 'NONE',  ( 126.7960359500334135, -6.485669677952845547, -18.42724950168021181 ) ) ;
#12895=CARTESIAN_POINT ( 'NONE',  ( 116.5969481442453031, -9.859900752359374465, -12.68260735090039404 ) ) ;
#12896=CARTESIAN_POINT ( 'NONE',  ( 112.9664414775786412, -9.859900752359374465, -12.68260735090039404 ) ) ;
#12897=AXIS2_PLACEMENT_3D ( 'NONE', #41896, #2965, #35241 ) ;
#12901=CARTESIAN_POINT ( 'NONE',  ( 121.7023481442452777, -9.261995988541697145, -16.69588392320189030 ) ) ;
#12902=CARTESIAN_POINT ( 'NONE',  ( 126.3539348109119800, -4.153390946401325223, -8.397313243818185668 ) ) ;
#12905=CARTESIAN_POINT ( 'NONE',  ( 127.3434826498001087, 0.3281563814195650464, -15.39656318237291366 ) ) ;
#12907=CARTESIAN_POINT ( 'NONE',  ( 126.6942948109119840, -8.899110576539710493, -16.42337572283490132 ) ) ;
#12909=CARTESIAN_POINT ( 'NONE',  ( 120.5110881442453206, -3.505236298600246325, -18.68346056562440793 ) ) ;
#12914=CARTESIAN_POINT ( 'NONE',  ( 113.4769814775786330, 0.4262465694468514643, -12.03445270309931736 ) ) ;
#12918=CARTESIAN_POINT ( 'NONE',  ( 125.5030348109119558, -3.383040157471821630, -19.15922257007629170 ) ) ;
#12919=CARTESIAN_POINT ( 'NONE',  ( 122.0994348109119443, 0.9020085738987339008, -11.91225656197089222 ) ) ;
#12921=CARTESIAN_POINT ( 'NONE',  ( 118.1852948109119836, -5.638512984488999180, -18.83840828888717311 ) ) ;
#12922=CARTESIAN_POINT ( 'NONE',  ( 112.0588148109119828, 0.5811942927096154232, -14.16772938898807155 ) ) ;
#12924=CARTESIAN_POINT ( 'NONE',  ( 113.8740681442453138, -9.859900752359374465, -12.68260735090039404 ) ) ;
#12925=CARTESIAN_POINT ( 'NONE',  ( 126.0135748109119902, -8.166667518702819706, -8.995218007635861213 ) ) ;
#12926=CARTESIAN_POINT ( 'NONE',  ( 119.7736414775786358, -10.30919188438810075, -12.61870101168855918 ) ) ;
#12927=CARTESIAN_POINT ( 'NONE',  ( 113.6471614775786492, -5.638512984488999180, -18.83840828888717311 ) ) ;
#12928=CARTESIAN_POINT ( 'NONE',  ( 112.9097148109120070, -9.565557343593413364, -10.61323700422348004 ) ) ;
#12930=CARTESIAN_POINT ( 'NONE',  ( 119.4332814775786318, -8.899110576539710493, -16.42337572283490132 ) ) ;
#12931=CARTESIAN_POINT ( 'NONE',  ( 123.6877814775786533, -3.383040157471821630, -19.15922257007629170 ) ) ;
#12934=CARTESIAN_POINT ( 'NONE',  ( 123.5743281442453139, -2.084020599724406786, -8.691656652584148546 ) ) ;
#12936=CYLINDRICAL_SURFACE ( 'NONE', #5387, 1.499999999999999334 ) ;
#12937=ORIENTED_EDGE ( 'NONE', *, *, #17770, .F. ) ;
#12939=CARTESIAN_POINT ( 'NONE',  ( 122.9503348109119827, 0.5811942927096110934, -14.16772938898807510 ) ) ;
#12941=CARTESIAN_POINT ( 'NONE',  ( 112.2857214775786474, -4.089484607189486809, -7.948022111789456723 ) ) ;
#12951=CARTESIAN_POINT ( 'NONE',  ( 119.7169148109119874, -0.1624402480850797581, -16.17319339645315424 ) ) ;
#12954=CARTESIAN_POINT ( 'NONE',  ( 121.3619881442452879, -4.089484607189486809, -7.948022111789456723 ) ) ;
#12955=CARTESIAN_POINT ( 'NONE',  ( 118.8660148109119774, -10.30919188438810075, -12.61870101168855918 ) ) ;
#12957=CARTESIAN_POINT ( 'NONE',  ( 113.3068014775786594, -8.166667518702816153, -8.995218007635859436 ) ) ;
#12958=CARTESIAN_POINT ( 'NONE',  ( 126.4106614775786284, -6.222761293078241884, -8.102969835052219238 ) ) ;
#12959=CARTESIAN_POINT ( 'NONE',  ( 124.9357681442453014, -1.834011780172310813, -8.268836392978581529 ) ) ;
#12963=CARTESIAN_POINT ( 'NONE',  ( 115.2922348109119781, 0.4262465694468514643, -12.03445270309931736 ) ) ;
#12964=CARTESIAN_POINT ( 'NONE',  ( 115.5191414775786569, -6.222761293078241884, -8.102969835052219238 ) ) ;
#12969=CARTESIAN_POINT ( 'NONE',  ( 111.7751814775786556, -7.893985811506177619, -18.51759400769804742 ) ) ;
#12970=CARTESIAN_POINT ( 'NONE',  ( 111.8319081442453182, -5.638512984488999180, -18.83840828888717311 ) ) ;
#12974=CARTESIAN_POINT ( 'NONE',  ( 123.4976477054562594, -2.905774387498770928, -14.75189568944841056 ) ) ;
#12977=CARTESIAN_POINT ( 'NONE',  ( 116.9373081442452929, -8.166667518702817929, -8.995218007635861213 ) ) ;
#12978=CARTESIAN_POINT ( 'NONE',  ( 125.3895814775786448, -2.084020599724406786, -8.691656652584148546 ) ) ;
#12979=CARTESIAN_POINT ( 'NONE',  ( 114.8951481442453115, -8.899110576539710493, -16.42337572283490132 ) ) ;
#12980=DIRECTION ( 'NONE',  ( 0.000000000000000000, 0.6004852223388321697, -0.7996358532186279566 ) ) ;
#12981=CARTESIAN_POINT ( 'NONE',  ( 122.7234281442452755, -5.638512984488999180, -18.83840828888717311 ) ) ;
#12982=CARTESIAN_POINT ( 'NONE',  ( 115.3489614775786407, -9.261995988541697145, -16.69588392320189030 ) ) ;
#12983=B_SPLINE_CURVE_WITH_KNOTS ( 'NONE', 3,
 ( #14936, #28847, #29510, #12191, #21998, #35888, #11968, #36563, #4886, #15159 ),
 .UNSPECIFIED., .F., .F.,
 ( 4, 3, 3, 4 ),
 ( 0.000000000000000000, 0.0001671877560958114864, 0.0003343755126086585196, 0.0006438490228505489759 ),
 .UNSPECIFIED. ) ;
#12985=CARTESIAN_POINT ( 'NONE',  ( 124.1415948109119540, -6.344957434206665248, -7.627207830600338134 ) ) ;
#12987=CARTESIAN_POINT ( 'NONE',  ( 116.1431348109119881, -10.30919188438810075, -12.61870101168855918 ) ) ;
#12988=CARTESIAN_POINT ( 'NONE',  ( 115.7460481442453357, -10.15424416112533912, -14.75197769757731336 ) ) ;
#12989=CARTESIAN_POINT ( 'NONE',  ( 126.5041214912219516, -4.953991576021822496, -18.53526297036774650 ) ) ;
#12990=CARTESIAN_POINT ( 'NONE',  ( 113.5337081442453240, -9.261995988541697145, -16.69588392320189030 ) ) ;
#12992=CARTESIAN_POINT ( 'NONE',  ( 120.2841814775786276, 0.9020085738987339008, -11.91225656197089222 ) ) ;
#12995=DIRECTION ( 'NONE',  ( 1.000000000000000000, 0.000000000000000000, 0.000000000000000000 ) ) ;
#12996=( BOUNDED_SURFACE ( )  B_SPLINE_SURFACE ( 1, 2, ( 
 ( #44382, #20438, #13374, #40732, #44610, #27278, #16335, #9952, #19977, #9720, #44159, #3095, #27048, #23178, #44835, #13145, #40506, #23866, #37056, #30691, #37752, #40966, #30237, #17021, #37287, #13592, #9267, #23634, #2407, #9488, #12924, #26820, #23402, #6522, #2866, #6056, #34321, #30913, #27502, #20213, #12694, #26593, #33865, #2635, #37520, #16567, #33633, #16795, #5827, #19747, #30462, #34098, #20296, #34834, #6389, #23497, #27591, #37383, #16652, #17324, #31214, #16883, #30775, #44700, #17107, #30547, #2956, #38058, #27803, #41504, #6154, #6836, #34181, #38270, #44468, #7051, #45140, #27135, #13461, #27363, #3182, #10259, #20074, #33959, #3619, #28032, #24384, #17539, #41283, #20742, #41718, #23724, #20962, #34621, #2727, #10482, #31432, #13897, #10046, #3407, #199, #41058, #14115, #23950, #30997, #37615, #9581, #44923, #13233, #9815, #34401, #37831, #6608, #20521, #13681, #24166, #4288, #10923, #4743, #31882, #1323, #38488, #32105, #14339, #35285, #24825, #42162, #38716, #35748, #39177, #28253, #15017, #4521, #18663, #28705, #11596, #21852, #3838, #7487, #42385, #21404, #24605, #872, #15234, #41939, #35516, #647, #32556, #31655, #4058, #14562, #28481, #18444, #423, #32333, #11149, #7941, #1100, #28928, #17982, #39411, #42612, #8174, #17758, #25055, #7715, #42835, #38948, #25506, #18207, #10702, #7263, #21180, #21628, #14791, #35057, #22084, #35972, #11375, #25281, #19337, #23211, #16145, #19559, #15693, #33668, #5638, #5190, #2215, #37090, #29143, #36201, #19107, #12726, #33436, #40085, #32993, #30048, #43962, #15464, #22525, #5420, #8846, #33222, #25953, #19786, #25730, #39637, #1997, #1543, #22745, #4968, #40312, #1767, #36647, #18878, #15923, #39860, #26629, #40542, #29595, #9303, #22979, #29820, #36868, #43736, #5864, #2448, #8625, #43056, #11822, #29370, #8401, #43512, #12506, #43281, #22305, #26402, #32769, #12052, #9076, #36421, #12281, #26177, #10820, #17881, #24504, #31112, #24945, #6953, #21524, #12958, #7161, #33900, #10379, #45037, #17222 ),
 ( #549, #16368, #17437, #31555, #31330, #9525, #44196, #35182, #28368, #3519, #14017, #104, #17659, #27709, #42281, #13797, #30271, #34950, #26854, #23441, #24717, #38606, #24288, #38174, #20858, #38388, #37325, #34736, #323, #3959, #3736, #40767, #14236, #41623, #14461, #6096, #11043, #7382, #2670, #27932, #41841, #10601, #28152, #20017, #21073, #38841, #35411, #31778, #7610, #42062, #21299, #36314, #18331, #15583, #15361, #14684, #5084, #26070, #42733, #42951, #8737, #4186, #32224, #35861, #21750, #8294, #8071, #4863, #11717, #25628, #39974, #7844, #997, #1222, #21974, #22196, #32887, #762, #36092, #39750, #28598, #18556, #1439, #28823, #35641, #11498, #29487, #1661, #18781, #39301, #39533, #14912, #18104, #31999, #25403, #43400, #4635, #29042, #4417, #25177, #22645, #32448, #15136, #32671, #29266, #43178, #11946, #25842, #8518, #42509, #12168, #22421, #19000, #11269, #39075, #16035, #15809, #30395, #36983, #41124, #43623, #12397, #36541, #9883, #8970, #20145, #5315, #5752, #5984, #19672, #29710, #19231, #9646, #2797, #23103, #33560, #2337, #37212, #2107, #16724, #33333, #33112, #9414, #1882, #26297, #44317, #13073, #43856, #12628, #26526, #44087, #40204, #29943, #19909, #23568, #23326, #22869, #33794, #40435, #34029, #36762, #30619, #26972, #5531, #9196, #16266, #30170, #2566, #19450, #12852, #44536, #26753, #6221, #13298, #40660, #16495, #37449, #40893, #27206, #34898, #34253, #24667, #494, #17172, #17389, #28317, #23793, #6681, #10330, #41355, #27876, #27657, #24447, #31278, #52, #14407, #27433, #20589, #20807, #41570, #41790, #7330, #20366, #10547, #14181, #3026, #38124, #21025, #3246, #10112, #31061, #35127, #42229, #272, #13965, #34686, #21249, #31501, #44989, #17609, #28099, #24015, #42007, #24233, #38338, #37903, #3909, #7115, #16949, #37684, #3474, #30843, #10771, #44766, #38554, #17827, #3687, #34467, #31723, #13748, #6457, #13525, #6897, #28549, #4357, #25125, #11219, #39020, #4807, #8239, #42453, #29210, #18728, #18946, #42900, #25791, #36038 ) ),
 .UNSPECIFIED., .F., .F., .F. ) 
 B_SPLINE_SURFACE_WITH_KNOTS ( ( 2, 2 ),
 ( 3, 2, 2, 2, 2, 2, 2, 2, 2, 2, 2, 2, 2, 2, 2, 2, 2, 2, 2, 2, 2, 2, 2, 2, 2, 2, 2, 2, 2, 2, 2, 2, 2, 2, 2, 2, 2, 2, 2, 2, 2, 2, 2, 2, 2, 2, 2, 2, 2, 2, 2, 2, 2, 2, 2, 2, 2, 2, 2, 2, 2, 2, 2, 2, 2, 2, 2, 2, 2, 2, 2, 2, 2, 2, 2, 2, 2, 2, 2, 2, 2, 2, 2, 2, 2, 2, 2, 2, 2, 2, 2, 2, 2, 2, 2, 2, 2, 2, 2, 2, 2, 2, 2, 2, 2, 2, 2, 2, 2, 2, 2, 2, 2, 2, 2, 2, 2, 2, 2, 2, 2, 2, 2, 2, 2, 2, 2, 2, 3 ),
 ( 0.000000000000000000, 1.000000000000000000 ),
 ( 0.000000000000000000, 0.007812500000000000000, 0.01562500000000000000, 0.02343750000000000000, 0.03125000000000000000, 0.03906250000000000000, 0.04687500000000000000, 0.05468750000000000000, 0.06250000000000000000, 0.07031250000000000000, 0.07812500000000000000, 0.08593750000000000000, 0.09375000000000000000, 0.1015625000000000000, 0.1093750000000000000, 0.1171875000000000000, 0.1250000000000000000, 0.1328125000000000000, 0.1406250000000000000, 0.1484375000000000000, 0.1562500000000000000, 0.1640625000000000000, 0.1718750000000000000, 0.1796875000000000000, 0.1875000000000000000, 0.1953125000000000000, 0.2031250000000000000, 0.2109375000000000000, 0.2187500000000000000, 0.2265625000000000000, 0.2343750000000000000, 0.2421875000000000000, 0.2500000000000000000, 0.2578125000000000000, 0.2656250000000000000, 0.2734375000000000000, 0.2812500000000000000, 0.2890625000000000000, 0.2968750000000000000, 0.3046875000000000000, 0.3125000000000000000, 0.3203125000000000000, 0.3281250000000000000, 0.3359375000000000000, 0.3437500000000000000, 0.3515625000000000000, 0.3593750000000000000, 0.3671875000000000000, 0.3750000000000000000, 0.3828125000000000000, 0.3906250000000000000, 0.3984375000000000000, 0.4062500000000000000, 0.4140625000000000000, 0.4218750000000000000, 0.4296875000000000000, 0.4375000000000000000, 0.4453125000000000000, 0.4531250000000000000, 0.4609375000000000000, 0.4687500000000000000, 0.4765625000000000000, 0.4843750000000000000, 0.4921875000000000000, 0.5000000000000000000, 0.5078125000000000000, 0.5156250000000000000, 0.5234375000000000000, 0.5312500000000000000, 0.5390625000000000000, 0.5468750000000000000, 0.5546875000000000000, 0.5625000000000000000, 0.5703125000000000000, 0.5781250000000000000, 0.5859375000000000000, 0.5937500000000000000, 0.6015625000000000000, 0.6093750000000000000, 0.6171875000000000000, 0.6250000000000000000, 0.6328125000000000000, 0.6406250000000000000, 0.6484375000000000000, 0.6562500000000000000, 0.6640625000000000000, 0.6718750000000000000, 0.6796875000000000000, 0.6875000000000000000, 0.6953125000000000000, 0.7031250000000000000, 0.7109375000000000000, 0.7187500000000000000, 0.7265625000000000000, 0.7343750000000000000, 0.7421875000000000000, 0.7500000000000000000, 0.7578125000000000000, 0.7656250000000000000, 0.7734375000000000000, 0.7812500000000000000, 0.7890625000000000000, 0.7968750000000000000, 0.8046875000000000000, 0.8125000000000000000, 0.8203125000000000000, 0.8281250000000000000, 0.8359375000000000000, 0.8437500000000000000, 0.8515625000000000000, 0.8593750000000000000, 0.8671875000000000000, 0.8750000000000000000, 0.8828125000000000000, 0.8906250000000000000, 0.8984375000000000000, 0.9062500000000000000, 0.9140625000000000000, 0.9218750000000000000, 0.9296875000000000000, 0.9375000000000000000, 0.9453125000000000000, 0.9531250000000000000, 0.9609375000000000000, 0.9687500000000000000, 0.9765625000000000000, 0.9843750000000000000, 0.9921875000000000000, 1.000000000000000000 ),
 .UNSPECIFIED. ) 
 GEOMETRIC_REPRESENTATION_ITEM ( )  RATIONAL_B_SPLINE_SURFACE ( (
 ( 1.000000000000000000, 0.9238795325112869605, 1.000000000000000000, 0.9238795325112869605, 1.000000000000000000, 0.9238795325112869605, 1.000000000000000000, 0.9238795325112869605, 1.000000000000000000, 0.9238795325112869605, 1.000000000000000000, 0.9238795325112869605, 1.000000000000000000, 0.9238795325112869605, 1.000000000000000000, 0.9238795325112869605, 1.000000000000000000, 0.9238795325112869605, 1.000000000000000000, 0.9238795325112869605, 1.000000000000000000, 0.9238795325112869605, 1.000000000000000000, 0.9238795325112869605, 1.000000000000000000, 0.9238795325112869605, 1.000000000000000000, 0.9238795325112869605, 1.000000000000000000, 0.9238795325112869605, 1.000000000000000000, 0.9238795325112869605, 1.000000000000000000, 0.9238795325112869605, 1.000000000000000000, 0.9238795325112869605, 1.000000000000000000, 0.9238795325112869605, 1.000000000000000000, 0.9238795325112869605, 1.000000000000000000, 0.9238795325112869605, 1.000000000000000000, 0.9238795325112869605, 1.000000000000000000, 0.9238795325112869605, 1.000000000000000000, 0.9238795325112869605, 1.000000000000000000, 0.9238795325112869605, 1.000000000000000000, 0.9238795325112869605, 1.000000000000000000, 0.9238795325112869605, 1.000000000000000000, 0.9238795325112869605, 1.000000000000000000, 0.9238795325112869605, 1.000000000000000000, 0.9238795325112869605, 1.000000000000000000, 0.9238795325112869605, 1.000000000000000000, 0.9238795325112869605, 1.000000000000000000, 0.9238795325112869605, 1.000000000000000000, 0.9238795325112869605, 1.000000000000000000, 0.9238795325112869605, 1.000000000000000000, 0.9238795325112869605, 1.000000000000000000, 0.9238795325112869605, 1.000000000000000000, 0.9238795325112869605, 1.000000000000000000, 0.9238795325112869605, 1.000000000000000000, 0.9238795325112869605, 1.000000000000000000, 0.9238795325112869605, 1.000000000000000000, 0.9238795325112869605, 1.000000000000000000, 0.9238795325112869605, 1.000000000000000000, 0.9238795325112869605, 1.000000000000000000, 0.9238795325112869605, 1.000000000000000000, 0.9238795325112869605, 1.000000000000000000, 0.9238795325112869605, 1.000000000000000000, 0.9238795325112869605, 1.000000000000000000, 0.9238795325112869605, 1.000000000000000000, 0.9238795325112869605, 1.000000000000000000, 0.9238795325112869605, 1.000000000000000000, 0.9238795325112869605, 1.000000000000000000, 0.9238795325112869605, 1.000000000000000000, 0.9238795325112869605, 1.000000000000000000, 0.9238795325112869605, 1.000000000000000000, 0.9238795325112869605, 1.000000000000000000, 0.9238795325112869605, 1.000000000000000000, 0.9238795325112869605, 1.000000000000000000, 0.9238795325112869605, 1.000000000000000000, 0.9238795325112869605, 1.000000000000000000, 0.9238795325112869605, 1.000000000000000000, 0.9238795325112869605, 1.000000000000000000, 0.9238795325112869605, 1.000000000000000000, 0.9238795325112869605, 1.000000000000000000, 0.9238795325112869605, 1.000000000000000000, 0.9238795325112869605, 1.000000000000000000, 0.9238795325112869605, 1.000000000000000000, 0.9238795325112869605, 1.000000000000000000, 0.9238795325112869605, 1.000000000000000000, 0.9238795325112869605, 1.000000000000000000, 0.9238795325112869605, 1.000000000000000000, 0.9238795325112869605, 1.000000000000000000, 0.9238795325112869605, 1.000000000000000000, 0.9238795325112869605, 1.000000000000000000, 0.9238795325112869605, 1.000000000000000000, 0.9238795325112869605, 1.000000000000000000, 0.9238795325112869605, 1.000000000000000000, 0.9238795325112869605, 1.000000000000000000, 0.9238795325112869605, 1.000000000000000000, 0.9238795325112869605, 1.000000000000000000, 0.9238795325112869605, 1.000000000000000000, 0.9238795325112869605, 1.000000000000000000, 0.9238795325112869605, 1.000000000000000000, 0.9238795325112869605, 1.000000000000000000, 0.9238795325112869605, 1.000000000000000000, 0.9238795325112869605, 1.000000000000000000, 0.9238795325112869605, 1.000000000000000000, 0.9238795325112869605, 1.000000000000000000, 0.9238795325112869605, 1.000000000000000000, 0.9238795325112869605, 1.000000000000000000, 0.9238795325112869605, 1.000000000000000000, 0.9238795325112869605, 1.000000000000000000, 0.9238795325112869605, 1.000000000000000000, 0.9238795325112869605, 1.000000000000000000, 0.9238795325112869605, 1.000000000000000000, 0.9238795325112869605, 1.000000000000000000, 0.9238795325112869605, 1.000000000000000000, 0.9238795325112869605, 1.000000000000000000, 0.9238795325112869605, 1.000000000000000000, 0.9238795325112869605, 1.000000000000000000, 0.9238795325112869605, 1.000000000000000000, 0.9238795325112869605, 1.000000000000000000, 0.9238795325112869605, 1.000000000000000000, 0.9238795325112869605, 1.000000000000000000, 0.9238795325112869605, 1.000000000000000000, 0.9238795325112869605, 1.000000000000000000, 0.9238795325112869605, 1.000000000000000000, 0.9238795325112869605, 1.000000000000000000, 0.9238795325112869605, 1.000000000000000000, 0.9238795325112869605, 1.000000000000000000, 0.9238795325112869605, 1.000000000000000000, 0.9238795325112869605, 1.000000000000000000, 0.9238795325112869605, 1.000000000000000000, 0.9238795325112869605, 1.000000000000000000, 0.9238795325112869605, 1.000000000000000000, 0.9238795325112869605, 1.000000000000000000, 0.9238795325112869605, 1.000000000000000000, 0.9238795325112869605, 1.000000000000000000, 0.9238795325112869605, 1.000000000000000000, 0.9238795325112869605, 1.000000000000000000, 0.9238795325112869605, 1.000000000000000000, 0.9238795325112869605, 1.000000000000000000, 0.9238795325112869605, 1.000000000000000000, 0.9238795325112869605, 1.000000000000000000, 0.9238795325112869605, 1.000000000000000000, 0.9238795325112869605, 1.000000000000000000, 0.9238795325112869605, 1.000000000000000000, 0.9238795325112869605, 1.000000000000000000),
 ( 1.000000000000000000, 0.9238795325112869605, 1.000000000000000000, 0.9238795325112869605, 1.000000000000000000, 0.9238795325112869605, 1.000000000000000000, 0.9238795325112869605, 1.000000000000000000, 0.9238795325112869605, 1.000000000000000000, 0.9238795325112869605, 1.000000000000000000, 0.9238795325112869605, 1.000000000000000000, 0.9238795325112869605, 1.000000000000000000, 0.9238795325112869605, 1.000000000000000000, 0.9238795325112869605, 1.000000000000000000, 0.9238795325112869605, 1.000000000000000000, 0.9238795325112869605, 1.000000000000000000, 0.9238795325112869605, 1.000000000000000000, 0.9238795325112869605, 1.000000000000000000, 0.9238795325112869605, 1.000000000000000000, 0.9238795325112869605, 1.000000000000000000, 0.9238795325112869605, 1.000000000000000000, 0.9238795325112869605, 1.000000000000000000, 0.9238795325112869605, 1.000000000000000000, 0.9238795325112869605, 1.000000000000000000, 0.9238795325112869605, 1.000000000000000000, 0.9238795325112869605, 1.000000000000000000, 0.9238795325112869605, 1.000000000000000000, 0.9238795325112869605, 1.000000000000000000, 0.9238795325112869605, 1.000000000000000000, 0.9238795325112869605, 1.000000000000000000, 0.9238795325112869605, 1.000000000000000000, 0.9238795325112869605, 1.000000000000000000, 0.9238795325112869605, 1.000000000000000000, 0.9238795325112869605, 1.000000000000000000, 0.9238795325112869605, 1.000000000000000000, 0.9238795325112869605, 1.000000000000000000, 0.9238795325112869605, 1.000000000000000000, 0.9238795325112869605, 1.000000000000000000, 0.9238795325112869605, 1.000000000000000000, 0.9238795325112869605, 1.000000000000000000, 0.9238795325112869605, 1.000000000000000000, 0.9238795325112869605, 1.000000000000000000, 0.9238795325112869605, 1.000000000000000000, 0.9238795325112869605, 1.000000000000000000, 0.9238795325112869605, 1.000000000000000000, 0.9238795325112869605, 1.000000000000000000, 0.9238795325112869605, 1.000000000000000000, 0.9238795325112869605, 1.000000000000000000, 0.9238795325112869605, 1.000000000000000000, 0.9238795325112869605, 1.000000000000000000, 0.9238795325112869605, 1.000000000000000000, 0.9238795325112869605, 1.000000000000000000, 0.9238795325112869605, 1.000000000000000000, 0.9238795325112869605, 1.000000000000000000, 0.9238795325112869605, 1.000000000000000000, 0.9238795325112869605, 1.000000000000000000, 0.9238795325112869605, 1.000000000000000000, 0.9238795325112869605, 1.000000000000000000, 0.9238795325112869605, 1.000000000000000000, 0.9238795325112869605, 1.000000000000000000, 0.9238795325112869605, 1.000000000000000000, 0.9238795325112869605, 1.000000000000000000, 0.9238795325112869605, 1.000000000000000000, 0.9238795325112869605, 1.000000000000000000, 0.9238795325112869605, 1.000000000000000000, 0.9238795325112869605, 1.000000000000000000, 0.9238795325112869605, 1.000000000000000000, 0.9238795325112869605, 1.000000000000000000, 0.9238795325112869605, 1.000000000000000000, 0.9238795325112869605, 1.000000000000000000, 0.9238795325112869605, 1.000000000000000000, 0.9238795325112869605, 1.000000000000000000, 0.9238795325112869605, 1.000000000000000000, 0.9238795325112869605, 1.000000000000000000, 0.9238795325112869605, 1.000000000000000000, 0.9238795325112869605, 1.000000000000000000, 0.9238795325112869605, 1.000000000000000000, 0.9238795325112869605, 1.000000000000000000, 0.9238795325112869605, 1.000000000000000000, 0.9238795325112869605, 1.000000000000000000, 0.9238795325112869605, 1.000000000000000000, 0.9238795325112869605, 1.000000000000000000, 0.9238795325112869605, 1.000000000000000000, 0.9238795325112869605, 1.000000000000000000, 0.9238795325112869605, 1.000000000000000000, 0.9238795325112869605, 1.000000000000000000, 0.9238795325112869605, 1.000000000000000000, 0.9238795325112869605, 1.000000000000000000, 0.9238795325112869605, 1.000000000000000000, 0.9238795325112869605, 1.000000000000000000, 0.9238795325112869605, 1.000000000000000000, 0.9238795325112869605, 1.000000000000000000, 0.9238795325112869605, 1.000000000000000000, 0.9238795325112869605, 1.000000000000000000, 0.9238795325112869605, 1.000000000000000000, 0.9238795325112869605, 1.000000000000000000, 0.9238795325112869605, 1.000000000000000000, 0.9238795325112869605, 1.000000000000000000, 0.9238795325112869605, 1.000000000000000000, 0.9238795325112869605, 1.000000000000000000, 0.9238795325112869605, 1.000000000000000000, 0.9238795325112869605, 1.000000000000000000, 0.9238795325112869605, 1.000000000000000000, 0.9238795325112869605, 1.000000000000000000, 0.9238795325112869605, 1.000000000000000000, 0.9238795325112869605, 1.000000000000000000, 0.9238795325112869605, 1.000000000000000000, 0.9238795325112869605, 1.000000000000000000, 0.9238795325112869605, 1.000000000000000000, 0.9238795325112869605, 1.000000000000000000, 0.9238795325112869605, 1.000000000000000000, 0.9238795325112869605, 1.000000000000000000, 0.9238795325112869605, 1.000000000000000000, 0.9238795325112869605, 1.000000000000000000, 0.9238795325112869605, 1.000000000000000000, 0.9238795325112869605, 1.000000000000000000, 0.9238795325112869605, 1.000000000000000000, 0.9238795325112869605, 1.000000000000000000, 0.9238795325112869605, 1.000000000000000000, 0.9238795325112869605, 1.000000000000000000, 0.9238795325112869605, 1.000000000000000000, 0.9238795325112869605, 1.000000000000000000, 0.9238795325112869605, 1.000000000000000000, 0.9238795325112869605, 1.000000000000000000, 0.9238795325112869605, 1.000000000000000000, 0.9238795325112869605, 1.000000000000000000, 0.9238795325112869605, 1.000000000000000000, 0.9238795325112869605, 1.000000000000000000, 0.9238795325112869605, 1.000000000000000000, 0.9238795325112869605, 1.000000000000000000, 0.9238795325112869605, 1.000000000000000000, 0.9238795325112869605, 1.000000000000000000) ) ) 
 REPRESENTATION_ITEM ( '' )  SURFACE ( )  );
#12997=CARTESIAN_POINT ( 'NONE',  ( 115.3489614775786407, -0.8288870151387760510, -10.36305467784173118 ) ) ;
#12998=CARTESIAN_POINT ( 'NONE',  ( 137.2618751060971647, -3.292307989136469271, -8.378698585220082151 ) ) ;
#12999=CARTESIAN_POINT ( 'NONE',  ( 119.6034614775786196, -3.505236298600246325, -18.68346056562440793 ) ) ;
#13001=CARTESIAN_POINT ( 'NONE',  ( 116.6536748109119941, -10.15424416112533912, -14.75197769757731336 ) ) ;
#13002=CARTESIAN_POINT ( 'NONE',  ( 115.5758681442453053, -1.561330072975668060, -17.79121239304076951 ) ) ;
#13004=CARTESIAN_POINT ( 'NONE',  ( 111.7184548109119788, -9.261995988541697145, -16.69588392320189030 ) ) ;
#13005=CARTESIAN_POINT ( 'NONE',  ( 116.5969481442453031, -9.859900752359374465, -12.68260735090039404 ) ) ;
#13006=CARTESIAN_POINT ( 'NONE',  ( 123.8579614775786126, 0.5811942927096110934, -14.16772938898807510 ) ) ;
#13007=CARTESIAN_POINT ( 'NONE',  ( 123.2906948109119867, -8.166667518702819706, -8.995218007635861213 ) ) ;
#13008=ORIENTED_EDGE ( 'NONE', *, *, #4404, .F. ) ;
#13009=CARTESIAN_POINT ( 'NONE',  ( 114.6682414775786469, -1.561330072975668060, -17.79121239304076596 ) ) ;
#13013=CARTESIAN_POINT ( 'NONE',  ( 128.0388906786927805, -4.056017420846984578, -15.71820436844875424 ) ) ;
#13014=CARTESIAN_POINT ( 'NONE',  ( 117.0507614775786465, -10.30919188438810075, -12.61870101168855918 ) ) ;
#13017=DIRECTION ( 'NONE',  ( 1.000000000000000000, 0.000000000000000000, 0.000000000000000000 ) ) ;
#13018=CARTESIAN_POINT ( 'NONE',  ( 113.1366214775786432, -7.643976991954077427, -18.09477374809248928 ) ) ;
#13021=CARTESIAN_POINT ( 'NONE',  ( 122.9503348109119827, 0.5811942927096110934, -14.16772938898807510 ) ) ;
#13026=CARTESIAN_POINT ( 'NONE',  ( 121.5888948109119809, 0.1319031606808879209, -14.10382304977623669 ) ) ;
#13027=CARTESIAN_POINT ( 'NONE',  ( 120.0005481442453146, -5.638512984488999180, -18.83840828888717311 ) ) ;
#13028=CARTESIAN_POINT ( 'NONE',  ( 115.1220548109119761, -1.833838273342658809, -17.42832698103878286 ) ) ;
#13029=CARTESIAN_POINT ( 'NONE',  ( 115.1220548109119761, -8.166667518702817929, -8.995218007635861213 ) ) ;
#13032=CARTESIAN_POINT ( 'NONE',  ( 118.6958348109119754, -3.505236298600246325, -18.68346056562440793 ) ) ;
#13035=CARTESIAN_POINT ( 'NONE',  ( 111.8319081442453182, -5.638512984488999180, -18.83840828888717311 ) ) ;
#13036=CARTESIAN_POINT ( 'NONE',  ( 120.6812681442452941, 0.1319031606808879209, -14.10382304977623669 ) ) ;
#13037=EDGE_LOOP ( 'NONE', ( #42852, #912, #42498, #27704, #25597 ) ) ;
#13039=CARTESIAN_POINT ( 'NONE',  ( 119.6034614775786196, -6.344957434206665248, -7.627207830600338134 ) ) ;
#13041=CARTESIAN_POINT ( 'NONE',  ( 117.1642148109119859, -0.8288870151387760510, -10.36305467784173118 ) ) ;
#13045=CARTESIAN_POINT ( 'NONE',  ( 124.0848681442452772, -5.574606645277164318, -18.38911715685844683 ) ) ;
#13046=CARTESIAN_POINT ( 'NONE',  ( 120.5110881442453206, -3.505236298600246325, -18.68346056562440793 ) ) ;
#13051=CARTESIAN_POINT ( 'NONE',  ( 116.8238548109119819, -4.089484607189486809, -7.948022111789456723 ) ) ;
#13053=CARTESIAN_POINT ( 'NONE',  ( 119.8870948109119752, -9.261995988541697145, -16.69588392320189030 ) ) ;
#13054=CARTESIAN_POINT ( 'NONE',  ( 120.2841814775786276, 0.9020085738987339008, -11.91225656197089222 ) ) ;
#13055=CARTESIAN_POINT ( 'NONE',  ( 119.3765548109119834, -10.15424416112533912, -14.75197769757731336 ) ) ;
#13056=CARTESIAN_POINT ( 'NONE',  ( 125.6164881442453094, -9.565557343593413364, -10.61323700422348004 ) ) ;
#13057=CARTESIAN_POINT ( 'NONE',  ( 111.9453614775786434, -1.561330072975668060, -17.79121239304076596 ) ) ;
#13059=CARTESIAN_POINT ( 'NONE',  ( 122.7234281442452755, -4.153390946401325223, -8.397313243818185668 ) ) ;
#13066=CARTESIAN_POINT ( 'NONE',  ( 123.4608748109119745, -10.63000616557722466, -14.87417383870573495 ) ) ;
#13067=CARTESIAN_POINT ( 'NONE',  ( 121.5888948109119809, 0.1319031606808879209, -14.10382304977623669 ) ) ;
#13070=CARTESIAN_POINT ( 'NONE',  ( 125.4463081442452932, -5.638512984488999180, -18.83840828888717311 ) ) ;
#13071=CARTESIAN_POINT ( 'NONE',  ( 113.9875214775786532, -8.899110576539710493, -16.42337572283490132 ) ) ;
#13073=CARTESIAN_POINT ( 'NONE',  ( 120.0005481442453146, -5.638512984488999180, -18.83840828888717311 ) ) ;
#13074=EDGE_CURVE ( 'NONE', #6181, #35601, #5111, .T. ) ;
#13076=CARTESIAN_POINT ( 'NONE',  ( 120.4543614775786295, -4.089484607189486809, -7.948022111789456723 ) ) ;
#13078=CARTESIAN_POINT ( 'NONE',  ( 124.8790414775786246, -8.899110576539710493, -16.42337572283490132 ) ) ;
#13079=CARTESIAN_POINT ( 'NONE',  ( 115.6893214775786447, 0.5811942927096102052, -14.16772938898808221 ) ) ;
#13082=LINE ( 'NONE', #3481, #33952 ) ;
#13083=CARTESIAN_POINT ( 'NONE',  ( 118.3912731944929391, -1.036737761566197014, -17.24079555149560861 ) ) ;
#13084=CARTESIAN_POINT ( 'NONE',  ( 124.1415948109119540, -3.505236298600246325, -18.68346056562440793 ) ) ;
#13088=CARTESIAN_POINT ( 'NONE',  ( 118.9794681442453026, -0.8288870151387760510, -10.36305467784173118 ) ) ;
#13090=CARTESIAN_POINT ( 'NONE',  ( 116.9373081442452929, -1.833838273342659253, -17.42832698103878286 ) ) ;
#13091=CARTESIAN_POINT ( 'NONE',  ( 123.6877814775786533, -3.383040157471821630, -19.15922257007629170 ) ) ;
#13093=CARTESIAN_POINT ( 'NONE',  ( 122.9503348109119827, -9.859900752359378018, -12.68260735090039759 ) ) ;
#13094=CARTESIAN_POINT ( 'NONE',  ( 119.1496481442453046, -3.383040157471821630, -19.15922257007629170 ) ) ;
#13095=CARTESIAN_POINT ( 'NONE',  ( 124.4252281442452812, -9.261995988541697145, -16.69588392320189030 ) ) ;
#13096=CARTESIAN_POINT ( 'NONE',  ( 124.5954081442453116, -6.222761293078241884, -8.102969835052219238 ) ) ;
#13097=ORIENTED_EDGE ( 'NONE', *, *, #21801, .F. ) ;
#13099=CARTESIAN_POINT ( 'NONE',  ( 125.4463081442452932, -5.638512984488999180, -18.83840828888717311 ) ) ;
#13100=CARTESIAN_POINT ( 'NONE',  ( 114.6682414775786469, -7.894159318335828068, -9.358103419637847864 ) ) ;
#13101=CARTESIAN_POINT ( 'NONE',  ( 123.4041481442452834, -10.30919188438810075, -12.61870101168855918 ) ) ;
#13109=CARTESIAN_POINT ( 'NONE',  ( 119.3765548109119834, -10.15424416112533912, -14.75197769757731336 ) ) ;
#13110=CARTESIAN_POINT ( 'NONE',  ( 114.3278814775786429, 0.1319031606808879209, -14.10382304977623669 ) ) ;
#13111=CARTESIAN_POINT ( 'NONE',  ( 126.4599182912884743, -0.4449873272706824645, -10.80585118086940533 ) ) ;
#13114=CARTESIAN_POINT ( 'NONE',  ( 121.3052614775786111, -7.643976991954077427, -18.09477374809248928 ) ) ;
#13118=CARTESIAN_POINT ( 'NONE',  ( 111.6722681442453222, -0.8658195297461032114, -10.39078908864415496 ) ) ;
#13120=CARTESIAN_POINT ( 'NONE',  ( 123.9146881442452894, 0.9020085738987339008, -11.91225656197089222 ) ) ;
#13121=CARTESIAN_POINT ( 'NONE',  ( 113.1366214775786432, -1.834011780172310813, -8.268836392978581529 ) ) ;
#13124=CARTESIAN_POINT ( 'NONE',  ( 114.1577014775786552, -6.344957434206662583, -7.627207830600332805 ) ) ;
#13125=CARTESIAN_POINT ( 'NONE',  ( 113.7798197424434363, -0.9924539043446216624, -17.29976612834909133 ) ) ;
#13128=CARTESIAN_POINT ( 'NONE',  ( 124.7088614775786226, -9.565557343593413364, -10.61323700422348004 ) ) ;
#13129=CARTESIAN_POINT ( 'NONE',  ( 121.0783548109119749, -9.565557343593413364, -10.61323700422348004 ) ) ;
#13134=CARTESIAN_POINT ( 'NONE',  ( 113.0798948109119948, -8.899110576539710493, -16.42337572283490132 ) ) ;
#13136=CARTESIAN_POINT ( 'NONE',  ( 111.7184548109119788, -9.261995988541697145, -16.69588392320189030 ) ) ;
#13138=CARTESIAN_POINT ( 'NONE',  ( 123.1205148109119563, -1.834011780172310813, -8.268836392978581529 ) ) ;
#13139=CARTESIAN_POINT ( 'NONE',  ( 120.5678148109119832, -8.166667518702819706, -8.995218007635861213 ) ) ;
#13141=EDGE_CURVE ( 'NONE', #21889, #26433, #31659, .T. ) ;
#13142=CARTESIAN_POINT ( 'NONE',  ( 122.0427081442452817, 0.5811942927096110934, -14.16772938898807510 ) ) ;
#13143=CARTESIAN_POINT ( 'NONE',  ( 113.0231681442453322, 0.9020085738987339008, -11.91225656197089222 ) ) ;
#13145=CARTESIAN_POINT ( 'NONE',  ( 113.0231681442453180, -10.15424416112533912, -14.75197769757731336 ) ) ;
#13146=CARTESIAN_POINT ( 'NONE',  ( 125.5597614775786326, -1.561330072975669392, -17.79121239304076951 ) ) ;
#13147=CARTESIAN_POINT ( 'NONE',  ( 125.1626748109119802, -9.988377603198980381, -10.36322818467138518 ) ) ;
#13148=VECTOR ( 'NONE', #10324, 1000.000000000000000 ) ;
#13149=CARTESIAN_POINT ( 'NONE',  ( 115.8027748109119841, -0.4660016031367893996, -10.09054647747474043 ) ) ;
#13150=CARTESIAN_POINT ( 'NONE',  ( 112.0020881442453344, -9.565557343593413364, -10.61323700422348004 ) ) ;
#13152=CARTESIAN_POINT ( 'NONE',  ( 117.2209414775786485, -2.084020599724406786, -8.691656652584148546 ) ) ;
#13153=CARTESIAN_POINT ( 'NONE',  ( 112.9097148109120070, 0.2603800115204892296, -16.42320221600525088 ) ) ;
#13156=CARTESIAN_POINT ( 'NONE',  ( 121.9859814775786333, -9.565557343593413364, -10.61323700422348004 ) ) ;
#13161=CARTESIAN_POINT ( 'NONE',  ( 114.5308753496756680, -1.087735405160637603, -17.17288456429614030 ) ) ;
#13164=CARTESIAN_POINT ( 'NONE',  ( 112.6828081442453282, -7.893985811506177619, -18.51759400769804742 ) ) ;
#13170=CARTESIAN_POINT ( 'NONE',  ( 119.0929214775786278, -5.638512984488999180, -18.83840828888717311 ) ) ;
#13171=CARTESIAN_POINT ( 'NONE',  ( 137.4565547821518976, -5.984952545581320393, -18.32735042449561291 ) ) ;
#13175=CARTESIAN_POINT ( 'NONE',  ( 119.6601881442453106, -1.833838273342659253, -17.42832698103878286 ) ) ;
#13176=CARTESIAN_POINT ( 'NONE',  ( 125.6164881442453094, -9.565557343593413364, -10.61323700422348004 ) ) ;
#13178=CARTESIAN_POINT ( 'NONE',  ( 121.3052614775786111, -1.834011780172310813, -8.268836392978581529 ) ) ;
#13179=CARTESIAN_POINT ( 'NONE',  ( 120.2274548109119934, 0.5811942927096110934, -14.16772938898807510 ) ) ;
#13180=CARTESIAN_POINT ( 'NONE',  ( 126.1837548109119211, -10.63000616557722466, -14.87417383870573495 ) ) ;
#13181=CARTESIAN_POINT ( 'NONE',  ( 112.4559014775786778, -0.1624402480850797581, -16.17319339645315424 ) ) ;
#13182=CARTESIAN_POINT ( 'NONE',  ( 125.3895814775786448, -7.893985811506177619, -18.51759400769804742 ) ) ;
#13186=CARTESIAN_POINT ( 'NONE',  ( 117.6747548109119919, -7.643976991954077427, -18.09477374809248928 ) ) ;
#13188=CARTESIAN_POINT ( 'NONE',  ( 117.3911214775786505, -7.894159318335828068, -9.358103419637847864 ) ) ;
#13195=CARTESIAN_POINT ( 'NONE',  ( 115.2355081442453155, -10.30919188438810075, -12.61870101168855918 ) ) ;
#13201=CARTESIAN_POINT ( 'NONE',  ( 111.4812862606558923, -1.286823604262816279, -16.90776886114078437 ) ) ;
#13203=CARTESIAN_POINT ( 'NONE',  ( 117.6747548109119919, -1.834011780172310813, -8.268836392978581529 ) ) ;
#13204=CARTESIAN_POINT ( 'NONE',  ( 112.9664414775786412, 0.5811942927096154232, -14.16772938898807155 ) ) ;
#13205=CARTESIAN_POINT ( 'NONE',  ( 119.9438214775786378, -2.084020599724406786, -8.691656652584148546 ) ) ;
#13209=CARTESIAN_POINT ( 'NONE',  ( 123.1772414775786189, -4.089484607189486809, -7.948022111789456723 ) ) ;
#13210=CARTESIAN_POINT ( 'NONE',  ( 119.4900081442453086, -1.834011780172310813, -8.268836392978581529 ) ) ;
#13212=CARTESIAN_POINT ( 'NONE',  ( 113.9875214775786532, -8.899110576539710493, -16.42337572283490132 ) ) ;
#13215=CARTESIAN_POINT ( 'NONE',  ( 118.7525614775786380, -8.166667518702819706, -8.995218007635861213 ) ) ;
#13216=CARTESIAN_POINT ( 'NONE',  ( 126.4536383592362370, -5.007014633634890188, -18.50900364442074064 ) ) ;
#13217=CARTESIAN_POINT ( 'NONE',  ( 115.4624148109119943, -5.638512984488999180, -18.83840828888717311 ) ) ;
#13219=CARTESIAN_POINT ( 'NONE',  ( 122.2128881442453263, -1.834011780172310813, -8.268836392978581529 ) ) ;
#13221=CARTESIAN_POINT ( 'NONE',  ( 113.7606148109119886, -7.894159318335828068, -9.358103419637847864 ) ) ;
#13223=CARTESIAN_POINT ( 'NONE',  ( 117.8449348109119938, -1.833838273342659253, -17.42832698103878286 ) ) ;
#13224=CARTESIAN_POINT ( 'NONE',  ( 123.3190498203445031, -3.658217111620186035, -16.24788372853176099 ) ) ;
#13225=CARTESIAN_POINT ( 'NONE',  ( 117.1074881442453233, 0.4262465694468514643, -12.03445270309931736 ) ) ;
#13227=CARTESIAN_POINT ( 'NONE',  ( 114.8951481442453115, -8.899110576539710493, -16.42337572283490132 ) ) ;
#13228=CARTESIAN_POINT ( 'NONE',  ( 114.6115148109119986, -3.383040157471821630, -19.15922257007629170 ) ) ;
#13230=CARTESIAN_POINT ( 'NONE',  ( 113.3068014775786594, -8.166667518702817929, -8.995218007635859436 ) ) ;
#13231=CARTESIAN_POINT ( 'NONE',  ( 115.5758681442453053, -7.894159318335828068, -9.358103419637847864 ) ) ;
#13232=CARTESIAN_POINT ( 'NONE',  ( 123.4608748109119745, -10.63000616557722466, -14.87417383870573495 ) ) ;
#13233=CARTESIAN_POINT ( 'NONE',  ( 118.2987481442453088, -7.894159318335828068, -9.358103419637847864 ) ) ;
#13235=CARTESIAN_POINT ( 'NONE',  ( 112.6828081442453282, -7.893985811506177619, -18.51759400769804742 ) ) ;
#13242=CARTESIAN_POINT ( 'NONE',  ( 117.7314814775786260, -4.089484607189486809, -7.948022111789456723 ) ) ;
#13244=CARTESIAN_POINT ( 'NONE',  ( 125.4463081442452932, -5.638512984488999180, -18.83840828888717311 ) ) ;
#13246=CARTESIAN_POINT ( 'NONE',  ( 119.4332814775786318, -8.899110576539710493, -16.42337572283490132 ) ) ;
#13248=CARTESIAN_POINT ( 'NONE',  ( 122.0427081442452817, 0.5811942927096110934, -14.16772938898807510 ) ) ;
#13252=CARTESIAN_POINT ( 'NONE',  ( 112.6260814775786514, -9.261995988541697145, -16.69588392320189030 ) ) ;
#13253=CARTESIAN_POINT ( 'NONE',  ( 124.1983214775786166, -1.833838273342659697, -17.42832698103878286 ) ) ;
#13254=CARTESIAN_POINT ( 'NONE',  ( 120.2841814775786276, 0.9020085738987339008, -11.91225656197089222 ) ) ;
#13255=CARTESIAN_POINT ( 'NONE',  ( 113.3635281442453504, -0.1624402480850797581, -16.17319339645315424 ) ) ;
#13256=CARTESIAN_POINT ( 'NONE',  ( 118.1285681442453068, -7.893985811506177619, -18.51759400769804742 ) ) ;
#13257=CARTESIAN_POINT ( 'NONE',  ( 127.0264730702703417, -1.258626024824194056, -9.367719562983635839 ) ) ;
#13258=CARTESIAN_POINT ( 'NONE',  ( 119.0361948109119652, -2.084020599724406786, -8.691656652584148546 ) ) ;
#13261=CARTESIAN_POINT ( 'NONE',  ( 116.0296814775786345, -8.166667518702817929, -8.995218007635861213 ) ) ;
#13262=CARTESIAN_POINT ( 'NONE',  ( 120.0572748109119772, -6.222761293078241884, -8.102969835052219238 ) ) ;
#13265=CARTESIAN_POINT ( 'NONE',  ( 136.6675107540917793, -1.259382374902307422, -9.019811723025741301 ) ) ;
#13266=CARTESIAN_POINT ( 'NONE',  ( 118.4689281442453392, 0.9020085738987339008, -11.91225656197089222 ) ) ;
#13268=CARTESIAN_POINT ( 'NONE',  ( 115.2922348109119781, 0.4262465694468514643, -12.03445270309931736 ) ) ;
#13272=CARTESIAN_POINT ( 'NONE',  ( 124.3117748109119844, 0.1319031606808879209, -14.10382304977623669 ) ) ;
#13276=CARTESIAN_POINT ( 'NONE',  ( 122.3263414775786373, -6.344957434206665248, -7.627207830600338134 ) ) ;
#13280=CARTESIAN_POINT ( 'NONE',  ( 121.5321681442453183, -9.988377603198976828, -10.36322818467138340 ) ) ;
#13281=CARTESIAN_POINT ( 'NONE',  ( 120.2274548109119934, 0.5811942927096110934, -14.16772938898807510 ) ) ;
#13282=CARTESIAN_POINT ( 'NONE',  ( 118.9794681442453026, -0.8288870151387760510, -10.36305467784173118 ) ) ;
#13286=CARTESIAN_POINT ( 'NONE',  ( 125.1059481442452750, -1.833838273342660141, -17.42832698103878286 ) ) ;
#13287=CARTESIAN_POINT ( 'NONE',  ( 122.2469553663348449, -1.172797794773259072, -17.05961127468926719 ) ) ;
#13292=CARTESIAN_POINT ( 'NONE',  ( 123.5743281442453139, -7.893985811506177619, -18.51759400769804742 ) ) ;
#13293=CARTESIAN_POINT ( 'NONE',  ( 122.6667014775786413, -2.084020599724406786, -8.691656652584148546 ) ) ;
#13295=CARTESIAN_POINT ( 'NONE',  ( 125.1626748109119802, -9.988377603198980381, -10.36322818467138518 ) ) ;
#13296=CARTESIAN_POINT ( 'NONE',  ( 114.2144281442453178, -1.833838273342658809, -17.42832698103878286 ) ) ;
#13297=CARTESIAN_POINT ( 'NONE',  ( 121.6456214775786435, 0.4262465694468626776, -12.03445270309935111 ) ) ;
#13298=CARTESIAN_POINT ( 'NONE',  ( 121.5321681442453183, -9.988377603198976828, -10.36322818467138340 ) ) ;
#13299=CARTESIAN_POINT ( 'NONE',  ( 119.6034614775786196, -6.344957434206665248, -7.627207830600338134 ) ) ;
#13301=CARTESIAN_POINT ( 'NONE',  ( 126.3539348109119800, -4.153390946401325223, -8.397313243818185668 ) ) ;
#13307=CARTESIAN_POINT ( 'NONE',  ( 114.2719877074049037, -2.419733177069680607, -17.89711025544712442 ) ) ;
#13309=CARTESIAN_POINT ( 'NONE',  ( 122.1561614775786353, -8.899110576539710493, -16.42337572283490132 ) ) ;
#13312=CARTESIAN_POINT ( 'NONE',  ( 120.6812681442452941, 0.1319031606808879209, -14.10382304977623669 ) ) ;
#13314=CARTESIAN_POINT ( 'NONE',  ( 115.1220548109119761, -1.833838273342658809, -17.42832698103878286 ) ) ;
#13315=CARTESIAN_POINT ( 'NONE',  ( 123.2906948109119867, -8.166667518702819706, -8.995218007635861213 ) ) ;
#13319=CARTESIAN_POINT ( 'NONE',  ( 122.4397948109119767, -0.1624402480850797581, -16.17319339645315424 ) ) ;
#13321=CARTESIAN_POINT ( 'NONE',  ( 117.9016614775786280, -9.988377603198976828, -10.36322818467138340 ) ) ;
#13322=CARTESIAN_POINT ( 'NONE',  ( 125.6164881442453094, 0.2603800115204892296, -16.42320221600525088 ) ) ;
#13323=CARTESIAN_POINT ( 'NONE',  ( 124.8223148109119762, -10.15424416112533912, -14.75197769757731336 ) ) ;
#13325=CARTESIAN_POINT ( 'NONE',  ( 123.5786714811013240, -2.280480477428469488, -18.08254604495227014 ) ) ;
#13326=CARTESIAN_POINT ( 'NONE',  ( 124.1983214775786166, -8.166667518702819706, -8.995218007635861213 ) ) ;
#13327=CARTESIAN_POINT ( 'NONE',  ( 115.5758681442453053, -7.894159318335828068, -9.358103419637847864 ) ) ;
#13328=CARTESIAN_POINT ( 'NONE',  ( 124.4819548109119722, -7.893985811506177619, -18.51759400769804742 ) ) ;
#13332=ADVANCED_FACE ( 'NONE', ( #11828 ), #22750, .F. ) ;
#13340=CARTESIAN_POINT ( 'NONE',  ( 123.9714148109119805, -8.899110576539710493, -16.42337572283490132 ) ) ;
#13341=CARTESIAN_POINT ( 'NONE',  ( 112.8529881442453160, -7.894159318335828068, -9.358103419637847864 ) ) ;
#13342=CARTESIAN_POINT ( 'NONE',  ( 127.7429221095975009, 0.4602738061672586589, -11.18760673166210218 ) ) ;
#13348=CARTESIAN_POINT ( 'NONE',  ( 111.2751814775786556, -7.618532446445550832, -18.05174138884716228 ) ) ;
#13350=CARTESIAN_POINT ( 'NONE',  ( 126.0703014775786102, -9.988377603198980381, -10.36322818467138518 ) ) ;
#13351=CARTESIAN_POINT ( 'NONE',  ( 125.6732148109119862, -9.859900752359378018, -12.68260735090039759 ) ) ;
#13353=CARTESIAN_POINT ( 'NONE',  ( 112.6828081442453282, -7.893985811506177619, -18.51759400769804742 ) ) ;
#13354=CARTESIAN_POINT ( 'NONE',  ( 126.2184548109119788, -4.863998795839242995, -13.39321520033831447 ) ) ;
#13356=CARTESIAN_POINT ( 'NONE',  ( 125.2761281442453054, 0.4262465694468514643, -12.03445270309931736 ) ) ;
#13357=CARTESIAN_POINT ( 'NONE',  ( 123.2906948109119867, -1.833838273342659697, -17.42832698103878286 ) ) ;
#13363=CARTESIAN_POINT ( 'NONE',  ( 113.1366214775786432, -7.643976991954077427, -18.09477374809248928 ) ) ;
#13365=DIRECTION ( 'NONE',  ( 1.000000000000000000, 0.000000000000000000, 0.000000000000000000 ) ) ;
#13367=CARTESIAN_POINT ( 'NONE',  ( 125.7299414775786346, 0.9020085738987339008, -11.91225656197089222 ) ) ;
#13368=CARTESIAN_POINT ( 'NONE',  ( 122.4965214775786251, -10.30919188438810075, -12.61870101168855918 ) ) ;
#13371=CARTESIAN_POINT ( 'NONE',  ( 118.5256548109119876, -0.4660016031367893996, -10.09054647747474043 ) ) ;
#13372=CARTESIAN_POINT ( 'NONE',  ( 112.7962614775786676, -3.383040157471821630, -19.15922257007629170 ) ) ;
#13374=CARTESIAN_POINT ( 'NONE',  ( 112.2857214775786474, -5.574606645277164318, -18.38911715685844683 ) ) ;
#13377=CARTESIAN_POINT ( 'NONE',  ( 124.8790414775786246, -0.4660016031367893996, -10.09054647747474043 ) ) ;
#13379=CARTESIAN_POINT ( 'NONE',  ( 122.6099748109119929, -9.261995988541697145, -16.69588392320189030 ) ) ;
#13380=CARTESIAN_POINT ( 'NONE',  ( 116.0296814775786345, -8.166667518702817929, -8.995218007635861213 ) ) ;
#13381=CARTESIAN_POINT ( 'NONE',  ( 111.2646414775786496, -8.899110576539710493, -16.42337572283490132 ) ) ;
#13383=CARTESIAN_POINT ( 'NONE',  ( 117.4478481442453131, -9.565557343593413364, -10.61323700422348004 ) ) ;
#13384=CARTESIAN_POINT ( 'NONE',  ( 113.1366214775786432, -1.834011780172310813, -8.268836392978581529 ) ) ;
#13386=CARTESIAN_POINT ( 'NONE',  ( 123.0637881442452937, -8.899110576539710493, -16.42337572283490132 ) ) ;
#13394=CARTESIAN_POINT ( 'NONE',  ( 112.8529881442453302, -1.561330072975668060, -17.79121239304076596 ) ) ;
#13400=CARTESIAN_POINT ( 'NONE',  ( 118.6958348109119754, -6.344957434206665248, -7.627207830600338134 ) ) ;
#13404=CARTESIAN_POINT ( 'NONE',  ( 119.9438214775786378, -2.084020599724406786, -8.691656652584148546 ) ) ;
#13406=CARTESIAN_POINT ( 'NONE',  ( 125.7299414775786346, 0.9020085738987339008, -11.91225656197089222 ) ) ;
#13407=CARTESIAN_POINT ( 'NONE',  ( 118.8092881442453290, -9.988377603198976828, -10.36322818467138340 ) ) ;
#13408=CARTESIAN_POINT ( 'NONE',  ( 114.2144281442453178, -1.833838273342658809, -17.42832698103878286 ) ) ;
#13409=CARTESIAN_POINT ( 'NONE',  ( 125.5030348109119558, -3.383040157471821630, -19.15922257007629170 ) ) ;
#13414=CARTESIAN_POINT ( 'NONE',  ( 117.0507614775786465, 0.1319031606808879209, -14.10382304977623669 ) ) ;
#13415=CARTESIAN_POINT ( 'NONE',  ( 119.0361948109119652, -2.084020599724406786, -8.691656652584148546 ) ) ;
#13421=CARTESIAN_POINT ( 'NONE',  ( 114.8384214775786489, 0.9020085738987339008, -11.91225656197089222 ) ) ;
#13429=CARTESIAN_POINT ( 'NONE',  ( 123.0070614775786169, 0.9020085738987339008, -11.91225656197089222 ) ) ;
#13430=CARTESIAN_POINT ( 'NONE',  ( 114.6682414775786469, -1.561330072975668060, -17.79121239304076596 ) ) ;
#13431=CARTESIAN_POINT ( 'NONE',  ( 120.1140014775786398, -7.894159318335828068, -9.358103419637847864 ) ) ;
#13433=CARTESIAN_POINT ( 'NONE',  ( 120.5110881442453206, -6.344957434206665248, -7.627207830600338134 ) ) ;
#13434=CARTESIAN_POINT ( 'NONE',  ( 118.4122014775786340, 0.5811942927096110934, -14.16772938898807510 ) ) ;
#13437=CARTESIAN_POINT ( 'NONE',  ( 113.6471614775786492, -4.153390946401321671, -8.397313243818183892 ) ) ;
#13438=CARTESIAN_POINT ( 'NONE',  ( 135.3184548109119874, -1.191816558809784876, -8.648209655763537285 ) ) ;
#13440=CARTESIAN_POINT ( 'NONE',  ( 117.2776681442452968, -5.638512984488999180, -18.83840828888717311 ) ) ;
#13442=CARTESIAN_POINT ( 'NONE',  ( 115.5191414775786569, -3.383040157471821630, -19.15922257007629170 ) ) ;
#13444=CARTESIAN_POINT ( 'NONE',  ( 121.9859814775786333, 0.2603800115204892296, -16.42320221600525088 ) ) ;
#13449=CARTESIAN_POINT ( 'NONE',  ( 115.0653281442453277, -3.505236298600246325, -18.68346056562440793 ) ) ;
#13451=CARTESIAN_POINT ( 'NONE',  ( 117.7882081442453170, -3.505236298600246325, -18.68346056562440793 ) ) ;
#13454=CARTESIAN_POINT ( 'NONE',  ( 116.3133148109120043, -2.084020599724406786, -8.691656652584148546 ) ) ;
#13455=CARTESIAN_POINT ( 'NONE',  ( 114.2144281442453178, -8.166667518702817929, -8.995218007635859436 ) ) ;
#13457=CARTESIAN_POINT ( 'NONE',  ( 117.0507614775786465, -10.30919188438810075, -12.61870101168855918 ) ) ;
#13458=CARTESIAN_POINT ( 'NONE',  ( 113.8173414775786512, -9.565557343593413364, -10.61323700422348004 ) ) ;
#13459=CARTESIAN_POINT ( 'NONE',  ( 111.5482748109120053, -0.1624402480850797581, -16.17319339645315424 ) ) ;
#13461=CARTESIAN_POINT ( 'NONE',  ( 116.5969481442453031, -9.859900752359374465, -12.68260735090039404 ) ) ;
#13463=CARTESIAN_POINT ( 'NONE',  ( 112.6260814775786514, -9.261995988541697145, -16.69588392320189030 ) ) ;
#13466=CARTESIAN_POINT ( 'NONE',  ( 110.5511756189168011, -1.701529060415639671, -16.35552654288092356 ) ) ;
#13468=CARTESIAN_POINT ( 'NONE',  ( 117.8449348109119938, -8.166667518702817929, -8.995218007635861213 ) ) ;
#13471=CARTESIAN_POINT ( 'NONE',  ( 125.2194014775786286, -10.30919188438809542, -12.61870101168851832 ) ) ;
#13472=CARTESIAN_POINT ( 'NONE',  ( 119.6601881442453106, -1.833838273342659253, -17.42832698103878286 ) ) ;
#13474=CARTESIAN_POINT ( 'NONE',  ( 125.2194014775786286, -10.30919188438810075, -12.61870101168855918 ) ) ;
#13478=CARTESIAN_POINT ( 'NONE',  ( 113.0231681442453322, 0.9020085738987339008, -11.91225656197089222 ) ) ;
#13479=CARTESIAN_POINT ( 'NONE',  ( 121.9292548109119849, -7.894159318335828068, -9.358103419637847864 ) ) ;
#13480=CARTESIAN_POINT ( 'NONE',  ( 123.0637881442452937, -0.4660016031367893996, -10.09054647747474043 ) ) ;
#13481=CARTESIAN_POINT ( 'NONE',  ( 115.2922348109119781, 0.4262465694468514643, -12.03445270309931736 ) ) ;
#13483=CARTESIAN_POINT ( 'NONE',  ( 119.7169148109119874, -9.988377603198976828, -10.36322818467138340 ) ) ;
#13485=CARTESIAN_POINT ( 'NONE',  ( 127.2313854076961519, -1.266593818456560827, -9.224256396174785877 ) ) ;
#13486=CARTESIAN_POINT ( 'NONE',  ( 121.4754414775786131, -1.833838273342659697, -17.42832698103878286 ) ) ;
#13489=CARTESIAN_POINT ( 'NONE',  ( 117.1642148109119859, -9.261995988541697145, -16.69588392320189030 ) ) ;
#13490=CARTESIAN_POINT ( 'NONE',  ( 125.3328548109119964, -0.8288870151387760510, -10.36305467784173118 ) ) ;
#13494=CARTESIAN_POINT ( 'NONE',  ( 117.5045748109119756, 0.5811942927096110934, -14.16772938898807510 ) ) ;
#13496=CARTESIAN_POINT ( 'NONE',  ( 119.0929214775786278, -4.153390946401325223, -8.397313243818185668 ) ) ;
#13499=CARTESIAN_POINT ( 'NONE',  ( 111.8886348109120092, -3.383040157471821630, -19.15922257007629170 ) ) ;
#13501=CARTESIAN_POINT ( 'NONE',  ( 123.3474214775786209, -0.1624402480850797581, -16.17319339645315424 ) ) ;
#13504=CARTESIAN_POINT ( 'NONE',  ( 120.2841814775786276, 0.9020085738987339008, -11.91225656197089222 ) ) ;
#13507=CARTESIAN_POINT ( 'NONE',  ( 118.5256548109119876, -0.4660016031367893996, -10.09054647747474043 ) ) ;
#13508=CARTESIAN_POINT ( 'NONE',  ( 117.3911214775786505, -1.561330072975668504, -17.79121239304076951 ) ) ;
#13509=CARTESIAN_POINT ( 'NONE',  ( 118.8092881442453290, -0.1624402480850797581, -16.17319339645315424 ) ) ;
#13510=CARTESIAN_POINT ( 'NONE',  ( 125.5597614775786326, -7.894159318335828068, -9.358103419637847864 ) ) ;
#13511=CARTESIAN_POINT ( 'NONE',  ( 117.6747548109119919, -1.834011780172310813, -8.268836392978581529 ) ) ;
#13513=CARTESIAN_POINT ( 'NONE',  ( 121.9859814775786333, -9.565557343593413364, -10.61323700422348004 ) ) ;
#13514=CARTESIAN_POINT ( 'NONE',  ( 125.1626748109119802, -0.1624402480845399399, -16.17319339645223053 ) ) ;
#13518=CARTESIAN_POINT ( 'NONE',  ( 120.6812681442452941, -10.30919188438810075, -12.61870101168855918 ) ) ;
#13519=CARTESIAN_POINT ( 'NONE',  ( 122.7801548109119665, -6.222761293078241884, -8.102969835052219238 ) ) ;
#13521=CARTESIAN_POINT ( 'NONE',  ( 123.8012348109119642, 0.2603800115204892296, -16.42320221600525088 ) ) ;
#13523=CARTESIAN_POINT ( 'NONE',  ( 112.2289948109119848, -7.643976991954077427, -18.09477374809248928 ) ) ;
#13525=CARTESIAN_POINT ( 'NONE',  ( 125.3895814775786448, -7.893985811506177619, -18.51759400769804742 ) ) ;
#13526=CARTESIAN_POINT ( 'NONE',  ( 121.1918081442452859, 0.9020085738987339008, -11.91225656197089222 ) ) ;
#13529=CARTESIAN_POINT ( 'NONE',  ( 113.3068014775786594, -8.166667518702817929, -8.995218007635859436 ) ) ;
#13534=CARTESIAN_POINT ( 'NONE',  ( 118.5771691344827587, -1.149058757900091265, -17.09122335155388939 ) ) ;
#13535=CARTESIAN_POINT ( 'NONE',  ( 124.3685014775786328, 0.4262465694468514643, -12.03445270309931736 ) ) ;
#13538=CARTESIAN_POINT ( 'NONE',  ( 123.1205148109119563, -7.643976991954077427, -18.09477374809248928 ) ) ;
#13539=CARTESIAN_POINT ( 'NONE',  ( 114.8951481442453115, -8.899110576539710493, -16.42337572283490132 ) ) ;
#13540=CARTESIAN_POINT ( 'NONE',  ( 113.1933481442453058, -5.574606645277164318, -18.38911715685844683 ) ) ;
#13542=CARTESIAN_POINT ( 'NONE',  ( 125.4463081442452932, -4.153390946401325223, -8.397313243818185668 ) ) ;
#13543=CARTESIAN_POINT ( 'NONE',  ( 117.1642148109119859, -9.261995988541697145, -16.69588392320189030 ) ) ;
#13548=CARTESIAN_POINT ( 'NONE',  ( 116.5969481442453031, -9.859900752359374465, -12.68260735090039404 ) ) ;
#13549=CARTESIAN_POINT ( 'NONE',  ( 113.6471614775786492, -4.153390946401321671, -8.397313243818183892 ) ) ;
#13550=CARTESIAN_POINT ( 'NONE',  ( 115.1220548109119761, -8.166667518702807271, -8.995218007635852331 ) ) ;
#13553=EDGE_LOOP ( 'NONE', ( #44609, #21513, #16228, #5740, #13913 ) ) ;
#13557=VECTOR ( 'NONE', #31459, 1000.000000000000000 ) ;
#13558=CARTESIAN_POINT ( 'NONE',  ( 118.0596094832010579, -2.324775150319241757, -18.02356106541842706 ) ) ;
#13559=CARTESIAN_POINT ( 'NONE',  ( 124.8223148109119762, -10.15424416112533912, -14.75197769757731336 ) ) ;
#13560=CARTESIAN_POINT ( 'NONE',  ( 113.9875214775786532, -8.899110576539710493, -16.42337572283490132 ) ) ;
#13561=CARTESIAN_POINT ( 'NONE',  ( 126.3183919423436805, -5.950396648433367019, -18.32522280981617513 ) ) ;
#13564=CARTESIAN_POINT ( 'NONE',  ( 112.2289948109119848, -7.643976991954077427, -18.09477374809248928 ) ) ;
#13568=CARTESIAN_POINT ( 'NONE',  ( 125.2761281442453054, -10.63000616557722466, -14.87417383870573495 ) ) ;
#13570=CARTESIAN_POINT ( 'NONE',  ( 125.3328548109119964, -0.8288870151387760510, -10.36305467784173118 ) ) ;
#13572=CARTESIAN_POINT ( 'NONE',  ( 112.4559014775786494, -9.988377603198976828, -10.36322818467138340 ) ) ;
#13575=CARTESIAN_POINT ( 'NONE',  ( 125.7299414775786346, -10.15424416112533912, -14.75197769757731336 ) ) ;
#13576=CARTESIAN_POINT ( 'NONE',  ( 123.4041481442452834, 0.1319031606808879209, -14.10382304977623669 ) ) ;
#13581=CARTESIAN_POINT ( 'NONE',  ( 112.3308181469516995, -3.929494816604734098, -18.62311481910882804 ) ) ;
#13582=CARTESIAN_POINT ( 'NONE',  ( 112.6828081442453282, -2.084020599724406786, -8.691656652584148546 ) ) ;
#13584=CARTESIAN_POINT ( 'NONE',  ( 117.7882081442453170, -6.344957434206651037, -7.627207830600339911 ) ) ;
#13587=CARTESIAN_POINT ( 'NONE',  ( 111.9453614775786434, -7.894159318335828068, -9.358103419637847864 ) ) ;
#13589=CARTESIAN_POINT ( 'NONE',  ( 121.0783548109119749, 0.2603800115204892296, -16.42320221600525088 ) ) ;
#13590=CARTESIAN_POINT ( 'NONE',  ( 116.6536748109119941, 0.9020085738987339008, -11.91225656197089222 ) ) ;
#13591=ORIENTED_EDGE ( 'NONE', *, *, #5573, .F. ) ;
#13592=CARTESIAN_POINT ( 'NONE',  ( 113.5904348109119866, -2.084020599724406786, -8.691656652584148546 ) ) ;
#13594=CARTESIAN_POINT ( 'NONE',  ( 111.3213681442453264, -7.643976991954077427, -18.09477374809248928 ) ) ;
#13595=CARTESIAN_POINT ( 'NONE',  ( 122.6667014775786413, -7.893985811506177619, -18.51759400769804742 ) ) ;
#13596=CARTESIAN_POINT ( 'NONE',  ( 115.0653281442453277, -6.344957434206662583, -7.627207830600332805 ) ) ;
#13597=CARTESIAN_POINT ( 'NONE',  ( 115.2355081442453155, 0.1319031606808879209, -14.10382304977623669 ) ) ;
#13599=CARTESIAN_POINT ( 'NONE',  ( 115.9162281442453093, -5.574606645277164318, -18.38911715685844683 ) ) ;
#13600=CARTESIAN_POINT ( 'NONE',  ( 117.5613014775786525, 0.9020085738987339008, -11.91225656197089222 ) ) ;
#13601=CARTESIAN_POINT ( 'NONE',  ( 123.6877814775786533, -6.222761293078241884, -8.102969835052219238 ) ) ;
#13611=CARTESIAN_POINT ( 'NONE',  ( 112.5126281442453120, -10.30919188438810075, -12.61870101168855918 ) ) ;
#13612=CARTESIAN_POINT ( 'NONE',  ( 112.8529881442453302, -7.894159318335828068, -9.358103419637847864 ) ) ;
#13616=CARTESIAN_POINT ( 'NONE',  ( 119.6601881442453106, -8.166667518702819706, -8.995218007635861213 ) ) ;
#13617=CARTESIAN_POINT ( 'NONE',  ( 137.3216041022093066, -6.332459753521784585, -18.38014592818993620 ) ) ;
#13621=CARTESIAN_POINT ( 'NONE',  ( 121.9292548109119849, -7.894159318335828068, -9.358103419637847864 ) ) ;
#13623=CARTESIAN_POINT ( 'NONE',  ( 125.4463081442452932, -5.638512984488999180, -18.83840828888717311 ) ) ;
#13624=CARTESIAN_POINT ( 'NONE',  ( 120.0005481442453146, -5.638512984488999180, -18.83840828888717311 ) ) ;
#13625=CARTESIAN_POINT ( 'NONE',  ( 125.7866681442452688, -0.4660016031367893996, -10.09054647747474043 ) ) ;
#13626=CARTESIAN_POINT ( 'NONE',  ( 114.3278814775786429, 0.1319031606808879209, -14.10382304977623669 ) ) ;
#13628=CARTESIAN_POINT ( 'NONE',  ( 112.3991748109119868, -1.833838273342658809, -17.42832698103878286 ) ) ;
#13632=CARTESIAN_POINT ( 'NONE',  ( 116.0864081442453113, -0.1624402480850797581, -16.17319339645315424 ) ) ;
#13633=CARTESIAN_POINT ( 'NONE',  ( 120.4543614775786295, -5.574606645277164318, -18.38911715685844683 ) ) ;
#13640=CARTESIAN_POINT ( 'NONE',  ( 113.3635281442453504, -9.988377603198976828, -10.36322818467138340 ) ) ;
#13641=CARTESIAN_POINT ( 'NONE',  ( 115.4624148109119943, -5.638512984488999180, -18.83840828888717311 ) ) ;
#13649=EDGE_LOOP ( 'NONE', ( #13814, #28515, #13097, #18301, #21573 ) ) ;
#13650=CARTESIAN_POINT ( 'NONE',  ( 120.6812681442452941, -10.30919188438810075, -12.61870101168855918 ) ) ;
#13651=CARTESIAN_POINT ( 'NONE',  ( 113.7038881442453402, -3.383040157471821630, -19.15922257007629170 ) ) ;
#13652=CARTESIAN_POINT ( 'NONE',  ( 119.3765548109119834, -10.15424416112533912, -14.75197769757731336 ) ) ;
#13654=CARTESIAN_POINT ( 'NONE',  ( 120.1707281442453166, 0.2603800115204892296, -16.42320221600525088 ) ) ;
#13655=CARTESIAN_POINT ( 'NONE',  ( 116.4267681442453153, -3.383040157471821630, -19.15922257007629170 ) ) ;
#13657=CARTESIAN_POINT ( 'NONE',  ( 111.7751814775786556, -2.084020599724406786, -8.691656652584148546 ) ) ;
#13659=ORIENTED_EDGE ( 'NONE', *, *, #34764, .T. ) ;
#13660=( BOUNDED_CURVE ( )  B_SPLINE_CURVE ( 2, ( #32726, #19514, #1281, #1499, #15420, #29325, #43239, #12004, #34087, #44824, #23391, #19737, #20427, #40721, #12684, #16785, #26582 ),
 .UNSPECIFIED., .F., .T. ) 
 B_SPLINE_CURVE_WITH_KNOTS ( ( 3, 2, 2, 2, 2, 2, 2, 2, 3 ),
 ( 0.07962824165685890299, 0.08593750000000000000, 0.09375000000000000000, 0.1015625000000000000, 0.1093750000000000000, 0.1171875000000000000, 0.1250000000000000000, 0.1328125000000000000, 0.1391217583431412219 ),
 .UNSPECIFIED. ) 
 CURVE ( )  GEOMETRIC_REPRESENTATION_ITEM ( )  RATIONAL_B_SPLINE_CURVE ( ( 0.9763430640195970289, 0.9385262470928680267, 1.000000000000000000, 0.9238795325112869605, 1.000000000000000000, 0.9238795325112869605, 1.000000000000000000, 0.9238795325112869605, 1.000000000000000000, 0.9238795325112869605, 1.000000000000000000, 0.9238795325112869605, 1.000000000000000000, 0.9238795325112869605, 1.000000000000000000, 0.9385262470928680267, 0.9763430640195970289 ) ) 
 REPRESENTATION_ITEM ( '' )  );
#13661=CARTESIAN_POINT ( 'NONE',  ( 118.5256548109119876, -0.4660016031367893996, -10.09054647747474043 ) ) ;
#13663=CARTESIAN_POINT ( 'NONE',  ( 114.9518748109119883, -1.834011780172310813, -8.268836392978581529 ) ) ;
#13666=CARTESIAN_POINT ( 'NONE',  ( 124.2550481442452792, -9.988377603198980381, -10.36322818467138518 ) ) ;
#13669=CARTESIAN_POINT ( 'NONE',  ( 112.1722681442453222, -8.899110576539710493, -16.42337572283490132 ) ) ;
#13671=CARTESIAN_POINT ( 'NONE',  ( 117.3911214775786505, -7.894159318335828068, -9.358103419637847864 ) ) ;
#13673=CARTESIAN_POINT ( 'NONE',  ( 118.5823814775786360, -7.643976991954077427, -18.09477374809248928 ) ) ;
#13676=CARTESIAN_POINT ( 'NONE',  ( 114.1577014775786552, -3.505236298600246325, -18.68346056562440793 ) ) ;
#13678=CARTESIAN_POINT ( 'NONE',  ( 114.7249681442453237, 0.2603800115204892296, -16.42320221600525088 ) ) ;
#13679=CARTESIAN_POINT ( 'NONE',  ( 126.1837548109119211, -10.63000616557722466, -14.87417383870573495 ) ) ;
#13681=CARTESIAN_POINT ( 'NONE',  ( 118.6391081442452986, -5.574606645277164318, -18.38911715685844683 ) ) ;
#13683=CARTESIAN_POINT ( 'NONE',  ( 118.0718414775786300, -9.261995988541697145, -16.69588392320189030 ) ) ;
#13689=CARTESIAN_POINT ( 'NONE',  ( 122.4397948109119767, -9.988377603198976828, -10.36322818467138340 ) ) ;
#13692=CARTESIAN_POINT ( 'NONE',  ( 119.8303681442453126, 0.4262465694468514643, -12.03445270309931736 ) ) ;
#13695=CARTESIAN_POINT ( 'NONE',  ( 124.0848681442452772, -4.089484607189486809, -7.948022111789456723 ) ) ;
#13699=CARTESIAN_POINT ( 'NONE',  ( 112.0588148109119828, 0.5811942927096154232, -14.16772938898807155 ) ) ;
#13700=CARTESIAN_POINT ( 'NONE',  ( 126.6375681442452930, -10.15424416112533912, -14.75197769757731336 ) ) ;
#13701=CARTESIAN_POINT ( 'NONE',  ( 123.9714148109119805, -0.4660016031367893996, -10.09054647747474043 ) ) ;
#13703=CARTESIAN_POINT ( 'NONE',  ( 117.5613014775786525, -10.15424416112533912, -14.75197769757731336 ) ) ;
#13705=CARTESIAN_POINT ( 'NONE',  ( 118.4689281442453392, 0.9020085738987339008, -11.91225656197089222 ) ) ;
#13708=CARTESIAN_POINT ( 'NONE',  ( 123.0637881442452937, -8.899110576539710493, -16.42337572283490132 ) ) ;
#13710=LINE ( 'NONE', #3434, #24910 ) ;
#13711=CARTESIAN_POINT ( 'NONE',  ( 115.9729548109119861, -6.344957434206662583, -7.627207830600332805 ) ) ;
#13712=CARTESIAN_POINT ( 'NONE',  ( 125.4463081442452932, -4.153390946401325223, -8.397313243818185668 ) ) ;
#13716=CARTESIAN_POINT ( 'NONE',  ( 121.1918081442452859, 0.9020085738987339008, -11.91225656197089222 ) ) ;
#13718=CARTESIAN_POINT ( 'NONE',  ( 118.8092881442453290, -0.1624402480850797581, -16.17319339645315424 ) ) ;
#13721=CARTESIAN_POINT ( 'NONE',  ( 112.7395348109119766, -5.638512984488999180, -18.83840828888717311 ) ) ;
#13722=CARTESIAN_POINT ( 'NONE',  ( 123.4041481442452834, 0.1319031606808879209, -14.10382304977623669 ) ) ;
#13726=CARTESIAN_POINT ( 'NONE',  ( 121.7590748109119687, -7.893985811506177619, -18.51759400769804742 ) ) ;
#13729=CARTESIAN_POINT ( 'NONE',  ( 118.8660148109119774, -10.30919188438810075, -12.61870101168855918 ) ) ;
#13730=CARTESIAN_POINT ( 'NONE',  ( 119.3198281442452924, 0.5811942927096110934, -14.16772938898807510 ) ) ;
#13731=CARTESIAN_POINT ( 'NONE',  ( 120.0005481442453146, -4.153390946401325223, -8.397313243818185668 ) ) ;
#13733=CARTESIAN_POINT ( 'NONE',  ( 114.6115148109119986, -3.383040157471821630, -19.15922257007629170 ) ) ;
#13736=CARTESIAN_POINT ( 'NONE',  ( 126.1270281442452870, 0.1319031606808879209, -14.10382304977623669 ) ) ;
#13737=CARTESIAN_POINT ( 'NONE',  ( 125.4463081442453500, -4.153390946402302220, -8.397313243818043560 ) ) ;
#13741=CARTESIAN_POINT ( 'NONE',  ( 122.3263414775786373, -6.344957434206665248, -7.627207830600338134 ) ) ;
#13742=CARTESIAN_POINT ( 'NONE',  ( 126.5808414775786446, -9.859900752359378018, -12.68260735090039759 ) ) ;
#13743=( BOUNDED_CURVE ( )  B_SPLINE_CURVE ( 2, ( #12037, #1311, #43497, #15223, #22510, #12266, #22731, #9742, #40526, #5848, #13611, #33652, #30255, #20679, #40990, #44181, #44401 ),
 .UNSPECIFIED., .F., .T. ) 
 B_SPLINE_CURVE_WITH_KNOTS ( ( 3, 2, 2, 2, 2, 2, 2, 2, 3 ),
 ( 0.01700466748089215011, 0.02343750000000000000, 0.03125000000000000000, 0.03906250000000000000, 0.04687500000000000000, 0.05468750000000000000, 0.06250000000000000000, 0.07031250000000000000, 0.07674533251905850395 ),
 .UNSPECIFIED. ) 
 CURVE ( )  GEOMETRIC_REPRESENTATION_ITEM ( )  RATIONAL_B_SPLINE_CURVE ( ( 0.9778625265006459788, 0.9373222120152210346, 1.000000000000000000, 0.9238795325112869605, 1.000000000000000000, 0.9238795325112869605, 1.000000000000000000, 0.9238795325112869605, 1.000000000000000000, 0.9238795325112869605, 1.000000000000000000, 0.9238795325112869605, 1.000000000000000000, 0.9238795325112869605, 1.000000000000000000, 0.9373222120157009840, 0.9778625265000240319 ) ) 
 REPRESENTATION_ITEM ( '' )  );
#13745=CARTESIAN_POINT ( 'NONE',  ( 126.0703014775786102, -9.988377603198980381, -10.36322818467138518 ) ) ;
#13748=CARTESIAN_POINT ( 'NONE',  ( 125.2761281442453054, -10.63000616557722466, -14.87417383870573495 ) ) ;
#13749=CARTESIAN_POINT ( 'NONE',  ( 125.6164881442453094, 0.2603800115204892296, -16.42320221600525088 ) ) ;
#13751=CARTESIAN_POINT ( 'NONE',  ( 125.9001214775786224, -5.574606645277164318, -18.38911715685844683 ) ) ;
#13752=CARTESIAN_POINT ( 'NONE',  ( 111.8862721015961483, -1.040089454026968951, -17.23633227186634187 ) ) ;
#13756=CARTESIAN_POINT ( 'NONE',  ( 114.2144281442453178, -1.833838273342658809, -17.42832698103878286 ) ) ;
#13757=CARTESIAN_POINT ( 'NONE',  ( 113.3635281442453504, -9.988377603198976828, -10.36322818467138340 ) ) ;
#13761=CARTESIAN_POINT ( 'NONE',  ( 123.3474214775786209, -0.1624402480850797581, -16.17319339645315424 ) ) ;
#13762=CARTESIAN_POINT ( 'NONE',  ( 115.0653281442453277, -3.505236298600246325, -18.68346056562440793 ) ) ;
#13763=CARTESIAN_POINT ( 'NONE',  ( 112.3424481442453384, -3.505236298600246325, -18.68346056562440793 ) ) ;
#13766=CARTESIAN_POINT ( 'NONE',  ( 119.7736414775786358, -10.30919188438810075, -12.61870101168855918 ) ) ;
#13768=CARTESIAN_POINT ( 'NONE',  ( 112.5693548109119888, 0.4262465694468514643, -12.03445270309931736 ) ) ;
#13771=ORIENTED_EDGE ( 'NONE', *, *, #16530, .T. ) ;
#13772=CARTESIAN_POINT ( 'NONE',  ( 118.1852948109119836, -4.153390946401325223, -8.397313243818185668 ) ) ;
#13773=CARTESIAN_POINT ( 'NONE',  ( 115.5191414775786569, -6.222761293078241884, -8.102969835052219238 ) ) ;
#13774=CARTESIAN_POINT ( 'NONE',  ( 151.2860562277021472, -4.863998795839242995, -13.39321520033831447 ) ) ;
#13780=CARTESIAN_POINT ( 'NONE',  ( 117.8239502440515452, -2.467220198592778413, -17.83387418641524391 ) ) ;
#13781=CARTESIAN_POINT ( 'NONE',  ( 121.6456214775786293, 0.4262465694468514643, -12.03445270309931736 ) ) ;
#13782=CARTESIAN_POINT ( 'NONE',  ( 117.6747548109119919, -7.643976991954077427, -18.09477374809248928 ) ) ;
#13783=CARTESIAN_POINT ( 'NONE',  ( 120.0940564575754905, -1.016270020561755860, -17.26805140881366896 ) ) ;
#13784=VERTEX_POINT ( 'NONE', #11503 ) ;
#13785=DIRECTION ( 'NONE',  ( -1.000000000000000000, 0.000000000000000000, 0.000000000000000000 ) ) ;
#13786=CARTESIAN_POINT ( 'NONE',  ( 117.5045748109119756, -9.859900752359374465, -12.68260735090039404 ) ) ;
#13791=CARTESIAN_POINT ( 'NONE',  ( 125.8433948109119456, -7.643976991954077427, -18.09477374809248928 ) ) ;
#13793=CARTESIAN_POINT ( 'NONE',  ( 113.5337081442453240, -9.261995988541697145, -16.69588392320189030 ) ) ;
#13794=AXIS2_PLACEMENT_3D ( 'NONE', #20364, #36981, #44085 ) ;
#13797=CARTESIAN_POINT ( 'NONE',  ( 112.5693548109119888, -10.63000616557722466, -14.87417383870573495 ) ) ;
#13798=CARTESIAN_POINT ( 'NONE',  ( 115.5191414775786569, -3.383040157471821630, -19.15922257007629170 ) ) ;
#13799=CARTESIAN_POINT ( 'NONE',  ( 122.6667014775786413, -2.084020599724406786, -8.691656652584148546 ) ) ;
#13804=CARTESIAN_POINT ( 'NONE',  ( 116.8238548109119819, -5.574606645277164318, -18.38911715685844683 ) ) ;
#13809=CARTESIAN_POINT ( 'NONE',  ( 124.8223148109119762, 0.9020085738987339008, -11.91225656197089222 ) ) ;
#13810=CARTESIAN_POINT ( 'NONE',  ( 112.4559014775786778, -0.1624402480850797581, -16.17319339645315424 ) ) ;
#13811=LINE ( 'NONE', #16791, #2221 ) ;
#13812=CARTESIAN_POINT ( 'NONE',  ( 118.7525614775786380, -8.166667518702819706, -8.995218007635861213 ) ) ;
#13813=CARTESIAN_POINT ( 'NONE',  ( 117.2209414775786485, -7.893985811506177619, -18.51759400769804742 ) ) ;
#13814=ORIENTED_EDGE ( 'NONE', *, *, #45007, .T. ) ;
#13815=CARTESIAN_POINT ( 'NONE',  ( 113.8173414775786512, -9.565557343593413364, -10.61323700422348004 ) ) ;
#13816=CARTESIAN_POINT ( 'NONE',  ( 125.2761281442453054, -10.63000616557722466, -14.87417383870573495 ) ) ;
#13817=CARTESIAN_POINT ( 'NONE',  ( 112.4559014775786494, -9.988377603198976828, -10.36322818467138340 ) ) ;
#13818=CARTESIAN_POINT ( 'NONE',  ( 114.8951481442453115, -8.899110576539710493, -16.42337572283490132 ) ) ;
#13820=CARTESIAN_POINT ( 'NONE',  ( 120.6245414775786458, -0.1624402480850797581, -16.17319339645315424 ) ) ;
#13821=CARTESIAN_POINT ( 'NONE',  ( 115.9729548109119861, -6.344957434206662583, -7.627207830600332805 ) ) ;
#13828=CARTESIAN_POINT ( 'NONE',  ( 114.7816948109119863, 0.5811942927096154232, -14.16772938898807155 ) ) ;
#13829=CARTESIAN_POINT ( 'NONE',  ( 135.5837700375960821, -10.80736548491261750, -14.14713708756795540 ) ) ;
#13832=CARTESIAN_POINT ( 'NONE',  ( 115.4776403923315655, -1.063912429576147511, -17.20460841810472985 ) ) ;
#13834=CARTESIAN_POINT ( 'NONE',  ( 119.4900081442453086, -1.834011780172310813, -8.268836392978581529 ) ) ;
#13835=CARTESIAN_POINT ( 'NONE',  ( 137.0130966147668232, -6.718222664625504770, -18.52177234174325804 ) ) ;
#13838=CARTESIAN_POINT ( 'NONE',  ( 120.6245414775786458, -0.1624402480850797581, -16.17319339645315424 ) ) ;
#13840=CARTESIAN_POINT ( 'NONE',  ( 124.9357681442453014, -1.834011780172310813, -8.268836392978581529 ) ) ;
#13841=CARTESIAN_POINT ( 'NONE',  ( 120.1707281442453166, 0.2603800115204892296, -16.42320221600525088 ) ) ;
#13842=CARTESIAN_POINT ( 'NONE',  ( 126.0703014775786102, -9.988377603198980381, -10.36322818467138518 ) ) ;
#13843=CARTESIAN_POINT ( 'NONE',  ( 116.8805814775786445, -3.505236298600246325, -18.68346056562440793 ) ) ;
#13844=CARTESIAN_POINT ( 'NONE',  ( 112.2289948109119848, -7.643976991954077427, -18.09477374809248928 ) ) ;
#13848=CARTESIAN_POINT ( 'NONE',  ( 119.4332814775786318, -8.899110576539710493, -16.42337572283490132 ) ) ;
#13849=CARTESIAN_POINT ( 'NONE',  ( 121.8725281442453223, -6.222761293078241884, -8.102969835052219238 ) ) ;
#13855=CARTESIAN_POINT ( 'NONE',  ( 113.0798948109119948, -0.4660016031367893996, -10.09054647747474043 ) ) ;
#13856=CARTESIAN_POINT ( 'NONE',  ( 114.4980614775786592, -7.893985811506177619, -18.51759400769804742 ) ) ;
#13859=CARTESIAN_POINT ( 'NONE',  ( 123.4666292975675219, -2.827606292292531798, -14.85598063601935870 ) ) ;
#13860=EDGE_CURVE ( 'NONE', #25860, #2299, #8054, .T. ) ;
#13862=CARTESIAN_POINT ( 'NONE',  ( 123.6877814775786533, -3.383040157471821630, -19.15922257007629170 ) ) ;
#13863=CIRCLE ( 'NONE', #29150, 5.999999999999997335 ) ;
#13864=CARTESIAN_POINT ( 'NONE',  ( 126.4673881442452910, -7.894159318335828068, -9.358103419637847864 ) ) ;
#13865=CARTESIAN_POINT ( 'NONE',  ( 119.0361948109119652, -2.084020599724406786, -8.691656652584148546 ) ) ;
#13868=CARTESIAN_POINT ( 'NONE',  ( 120.3976348109119812, -1.834011780172310813, -8.268836392978581529 ) ) ;
#13869=CARTESIAN_POINT ( 'NONE',  ( 118.9227414775786400, -10.63000616557722466, -14.87417383870573495 ) ) ;
#13872=CARTESIAN_POINT ( 'NONE',  ( 111.3780948109119890, -5.574606645277164318, -18.38911715685844683 ) ) ;
#13875=CARTESIAN_POINT ( 'NONE',  ( 118.8660148109119774, -10.30919188438810075, -12.61870101168855918 ) ) ;
#13877=CARTESIAN_POINT ( 'NONE',  ( 114.2144281442453178, -8.166667518702817929, -8.995218007635859436 ) ) ;
#13878=ORIENTED_EDGE ( 'NONE', *, *, #39558, .F. ) ;
#13882=CARTESIAN_POINT ( 'NONE',  ( 119.8748628165343888, -2.324775150319219108, -18.02356106541841996 ) ) ;
#13886=CARTESIAN_POINT ( 'NONE',  ( 119.6034614775786196, -3.505236298600246325, -18.68346056562440793 ) ) ;
#13888=EDGE_CURVE ( 'NONE', #8490, #12590, #21165, .T. ) ;
#13889=CARTESIAN_POINT ( 'NONE',  ( 120.2513676054816045, -2.287189184988711155, -18.07361239780447448 ) ) ;
#13890=CARTESIAN_POINT ( 'NONE',  ( 119.2063748109119814, -7.894159318335828068, -9.358103419637847864 ) ) ;
#13893=CARTESIAN_POINT ( 'NONE',  ( 118.6958348109119754, -3.505236298600246325, -18.68346056562440793 ) ) ;
#13896=CARTESIAN_POINT ( 'NONE',  ( 115.2922348109119781, -10.63000616557722466, -14.87417383870573495 ) ) ;
#13897=CARTESIAN_POINT ( 'NONE',  ( 117.6747548109119919, -7.643976991954077427, -18.09477374809248928 ) ) ;
#13899=CARTESIAN_POINT ( 'NONE',  ( 118.5823814775786360, -1.834011780172310813, -8.268836392978581529 ) ) ;
#13901=CARTESIAN_POINT ( 'NONE',  ( 115.5758681442453053, -7.894159318335810305, -9.358103419637833653 ) ) ;
#13903=CARTESIAN_POINT ( 'NONE',  ( 123.7445081442452874, -1.561330072975668948, -17.79121239304076951 ) ) ;
#13905=CARTESIAN_POINT ( 'NONE',  ( 127.7617783745704259, -9.363433729589941024, -9.777713163270945529 ) ) ;
#13906=CARTESIAN_POINT ( 'NONE',  ( 117.1642148109119859, -0.8288870151387760510, -10.36305467784173118 ) ) ;
#13909=CARTESIAN_POINT ( 'NONE',  ( 123.6877814775786533, -3.383040157471821630, -19.15922257007629170 ) ) ;
#13913=ORIENTED_EDGE ( 'NONE', *, *, #1869, .T. ) ;
#13915=CARTESIAN_POINT ( 'NONE',  ( 126.4673881442452910, -7.894159318335828068, -9.358103419637847864 ) ) ;
#13916=CARTESIAN_POINT ( 'NONE',  ( 122.4965214775786251, -10.30919188438810075, -12.61870101168855918 ) ) ;
#13918=CARTESIAN_POINT ( 'NONE',  ( 115.3489614775786407, -0.8288870151387760510, -10.36305467784173118 ) ) ;
#13920=CARTESIAN_POINT ( 'NONE',  ( 118.4122014775786340, 0.5811942927096110934, -14.16772938898807510 ) ) ;
#13923=CARTESIAN_POINT ( 'NONE',  ( 123.5176014775786228, -0.8288870151387760510, -10.36305467784173118 ) ) ;
#13927=CARTESIAN_POINT ( 'NONE',  ( 117.7882081442453170, -6.344957434206665248, -7.627207830600338134 ) ) ;
#13928=CARTESIAN_POINT ( 'NONE',  ( 136.5278073585050720, -8.477255842839500843, -17.84929476442550822 ) ) ;
#13932=CARTESIAN_POINT ( 'NONE',  ( 137.2528433483991250, -1.225607619245683511, -9.593372870557891119 ) ) ;
#13933=CARTESIAN_POINT ( 'NONE',  ( 121.8158014775786171, -5.638512984488999180, -18.83840828888717311 ) ) ;
#13935=CARTESIAN_POINT ( 'NONE',  ( 120.3976348109119812, -7.643976991954077427, -18.09477374809248928 ) ) ;
#13938=CARTESIAN_POINT ( 'NONE',  ( 114.3278814775786429, -10.30919188438810075, -12.61870101168855918 ) ) ;
#13939=CARTESIAN_POINT ( 'NONE',  ( 123.2906948109119867, -1.833838273342659697, -17.42832698103878286 ) ) ;
#13943=CARTESIAN_POINT ( 'NONE',  ( 120.5678148109119832, -8.166667518702819706, -8.995218007635861213 ) ) ;
#13946=CARTESIAN_POINT ( 'NONE',  ( 123.3474214775786209, -9.988377603198976828, -10.36322818467138340 ) ) ;
#13947=CARTESIAN_POINT ( 'NONE',  ( 120.5678148109119832, -8.166667518702819706, -8.995218007635861213 ) ) ;
#13948=CARTESIAN_POINT ( 'NONE',  ( 118.9227414775786542, 0.4262465694468514643, -12.03445270309931736 ) ) ;
#13950=CARTESIAN_POINT ( 'NONE',  ( 121.4754414775786131, -1.833838273342659697, -17.42832698103878286 ) ) ;
#13952=CARTESIAN_POINT ( 'NONE',  ( 114.5547881442453217, -5.638512984488999180, -18.83840828888717311 ) ) ;
#13960=CARTESIAN_POINT ( 'NONE',  ( 125.6164881442453094, -9.565557343593413364, -10.61323700422348004 ) ) ;
#13962=CARTESIAN_POINT ( 'NONE',  ( 123.1772414775786189, -4.089484607189486809, -7.948022111789456723 ) ) ;
#13964=CARTESIAN_POINT ( 'NONE',  ( 123.3116793777725064, -1.267766418764731728, -16.93314635290706605 ) ) ;
#13965=CARTESIAN_POINT ( 'NONE',  ( 123.8579614775786126, 0.5811942927096110934, -14.16772938898807510 ) ) ;
#13966=CARTESIAN_POINT ( 'NONE',  ( 124.9924948109119924, -4.089484607189486809, -7.948022111789456723 ) ) ;
#13968=CARTESIAN_POINT ( 'NONE',  ( 111.8886348109120092, -3.383040157471821630, -19.15922257007629170 ) ) ;
#13973=CARTESIAN_POINT ( 'NONE',  ( 116.8805814775786445, -3.505236298600246325, -18.68346056562440793 ) ) ;
#13974=CARTESIAN_POINT ( 'NONE',  ( 112.8529881442453302, -1.561330072975668060, -17.79121239304076596 ) ) ;
#13977=CARTESIAN_POINT ( 'NONE',  ( 121.5321681442453183, -0.1624402480850797581, -16.17319339645315424 ) ) ;
#13978=CARTESIAN_POINT ( 'NONE',  ( 119.0361948109119652, -2.084020599724406786, -8.691656652584148546 ) ) ;
#13979=CARTESIAN_POINT ( 'NONE',  ( 112.2857214775786474, -5.574606645277164318, -18.38911715685844683 ) ) ;
#13981=CARTESIAN_POINT ( 'NONE',  ( 124.4819548109119722, -2.084020599724406786, -8.691656652584148546 ) ) ;
#13983=CARTESIAN_POINT ( 'NONE',  ( 112.6828081442453282, -2.084020599724406786, -8.691656652584148546 ) ) ;
#13984=ORIENTED_EDGE ( 'NONE', *, *, #38175, .F. ) ;
#13990=CARTESIAN_POINT ( 'NONE',  ( 119.2063748109119814, -7.894159318335828068, -9.358103419637847864 ) ) ;
#13991=CARTESIAN_POINT ( 'NONE',  ( 113.5904348109119866, -2.084020599724406786, -8.691656652584148546 ) ) ;
#13992=FACE_OUTER_BOUND ( 'NONE', #14099, .T. ) ;
#14001=CARTESIAN_POINT ( 'NONE',  ( 121.4754414775786131, -1.833838273342659697, -17.42832698103878286 ) ) ;
#14002=CARTESIAN_POINT ( 'NONE',  ( 119.0929214775786278, -4.153390946401325223, -8.397313243818185668 ) ) ;
#14006=CARTESIAN_POINT ( 'NONE',  ( 115.6325948109119821, -9.565557343593413364, -10.61323700422348004 ) ) ;
#14008=CARTESIAN_POINT ( 'NONE',  ( 125.1626748109119802, -0.1624402480850797581, -16.17319339645315424 ) ) ;
#14011=CARTESIAN_POINT ( 'NONE',  ( 126.0135748109119902, -8.166667518702819706, -8.995218007635861213 ) ) ;
#14012=CARTESIAN_POINT ( 'NONE',  ( 115.7460481442453357, 0.9020085738987339008, -11.91225656197089222 ) ) ;
#14014=CARTESIAN_POINT ( 'NONE',  ( 112.7395348109119766, -5.638512984488999180, -18.83840828888717311 ) ) ;
#14017=CARTESIAN_POINT ( 'NONE',  ( 112.2857214775786474, -4.089484607189486809, -7.948022111789456723 ) ) ;
#14018=CARTESIAN_POINT ( 'NONE',  ( 112.1722681442453222, -0.4660016031367893996, -10.09054647747474043 ) ) ;
#14019=CARTESIAN_POINT ( 'NONE',  ( 124.5954081442453116, -6.222761293078241884, -8.102969835052219238 ) ) ;
#14025=CARTESIAN_POINT ( 'NONE',  ( 118.0151148109119816, 0.4262465694468514643, -12.03445270309931736 ) ) ;
#14030=CARTESIAN_POINT ( 'NONE',  ( 124.0848681442452772, -4.089484607189486809, -7.948022111789456723 ) ) ;
#14031=CARTESIAN_POINT ( 'NONE',  ( 120.5468302440515203, -2.467220198592777969, -17.83387418641524391 ) ) ;
#14032=CARTESIAN_POINT ( 'NONE',  ( 121.7590748109119687, -7.893985811506177619, -18.51759400769804742 ) ) ;
#14033=CARTESIAN_POINT ( 'NONE',  ( 115.1220548109119761, -8.166667518702817929, -8.995218007635861213 ) ) ;
#14035=CARTESIAN_POINT ( 'NONE',  ( 114.1009748109119784, -5.574606645277164318, -18.38911715685844683 ) ) ;
#14036=CARTESIAN_POINT ( 'NONE',  ( 124.1983214775786166, -8.166667518702819706, -8.995218007635861213 ) ) ;
#14037=CARTESIAN_POINT ( 'NONE',  ( 119.6601881442453106, -8.166667518702819706, -8.995218007635861213 ) ) ;
#14038=CARTESIAN_POINT ( 'NONE',  ( 115.3489614775786407, -0.8288870151387760510, -10.36305467784173118 ) ) ;
#14040=CARTESIAN_POINT ( 'NONE',  ( 122.0994348109119443, -10.15424416112533912, -14.75197769757731336 ) ) ;
#14042=CARTESIAN_POINT ( 'NONE',  ( 117.0507614775786465, -10.30919188438810075, -12.61870101168855918 ) ) ;
#14043=CARTESIAN_POINT ( 'NONE',  ( 137.5015123043530991, 0.1307850961568663151, -13.82943359837360298 ) ) ;
#14045=( GEOMETRIC_REPRESENTATION_CONTEXT ( 3 ) GLOBAL_UNCERTAINTY_ASSIGNED_CONTEXT ( ( #42019 ) ) GLOBAL_UNIT_ASSIGNED_CONTEXT ( ( #14534, #41472, #41691 ) ) REPRESENTATION_CONTEXT ( 'NONE', 'WORKASPACE' ) );
#14050=CARTESIAN_POINT ( 'NONE',  ( 115.1787814775786387, -9.988377603198976828, -10.36322818467138340 ) ) ;
#14053=CARTESIAN_POINT ( 'NONE',  ( 112.5126281442453120, 0.1319031606808879209, -14.10382304977623669 ) ) ;
#14057=CARTESIAN_POINT ( 'NONE',  ( 117.1642148109119859, -9.261995988541697145, -16.69588392320189030 ) ) ;
#14060=CARTESIAN_POINT ( 'NONE',  ( 118.8092881442453290, -9.988377603198960841, -10.36322818467135853 ) ) ;
#14061=CARTESIAN_POINT ( 'NONE',  ( 138.2184548109119930, -5.044325091639137781, -11.90409383958792411 ) ) ;
#14063=CARTESIAN_POINT ( 'NONE',  ( 125.6164881442453094, 0.2603800115204892296, -16.42320221600525088 ) ) ;
#14064=CARTESIAN_POINT ( 'NONE',  ( 123.0637881442452937, -0.4660016031367893996, -10.09054647747474043 ) ) ;
#14066=CARTESIAN_POINT ( 'NONE',  ( 115.4624148109119943, -4.153390946401321671, -8.397313243818183892 ) ) ;
#14068=CARTESIAN_POINT ( 'NONE',  ( 113.0798948109119948, -8.899110576539710493, -16.42337572283490132 ) ) ;
#14071=CARTESIAN_POINT ( 'NONE',  ( 120.3976348109119812, -7.643976991954077427, -18.09477374809248928 ) ) ;
#14073=CARTESIAN_POINT ( 'NONE',  ( 119.3765548109119834, -10.15424416112533912, -14.75197769757731336 ) ) ;
#14078=CARTESIAN_POINT ( 'NONE',  ( 112.3991748109119868, -8.166667518702817929, -8.995218007635859436 ) ) ;
#14079=CARTESIAN_POINT ( 'NONE',  ( 114.8951481442453115, -0.4660016031367893996, -10.09054647747474043 ) ) ;
#14085=CARTESIAN_POINT ( 'NONE',  ( 121.5321681442453183, -9.988377603198976828, -10.36322818467138340 ) ) ;
#14086=CARTESIAN_POINT ( 'NONE',  ( 112.6828081442453282, -7.893985811506177619, -18.51759400769804742 ) ) ;
#14087=CARTESIAN_POINT ( 'NONE',  ( 119.2631014775786298, -9.565557343593413364, -10.61323700422348004 ) ) ;
#14088=CARTESIAN_POINT ( 'NONE',  ( 125.6164881442453094, 0.2603800115204892296, -16.42320221600525088 ) ) ;
#14089=CARTESIAN_POINT ( 'NONE',  ( 116.9373081442452929, -8.166667518702817929, -8.995218007635861213 ) ) ;
#14091=CARTESIAN_POINT ( 'NONE',  ( 112.1722681442453222, -8.899110576539710493, -16.42337572283490132 ) ) ;
#14094=CARTESIAN_POINT ( 'NONE',  ( 121.2485348109119769, -0.4660016031367893996, -10.09054647747474043 ) ) ;
#14096=VECTOR ( 'NONE', #11787, 1000.000000000000000 ) ;
#14098=CARTESIAN_POINT ( 'NONE',  ( 117.1642148109119859, -9.261995988541697145, -16.69588392320189030 ) ) ;
#14099=EDGE_LOOP ( 'NONE', ( #16617, #38695, #17604, #35364, #34348 ) ) ;
#14102=CARTESIAN_POINT ( 'NONE',  ( 126.1270281442452870, -10.30919188438810075, -12.61870101168855918 ) ) ;
#14104=CARTESIAN_POINT ( 'NONE',  ( 112.6828081442453282, -2.084020599724406786, -8.691656652584148546 ) ) ;
#14106=CARTESIAN_POINT ( 'NONE',  ( 119.2631014775786298, -9.565557343593413364, -10.61323700422348004 ) ) ;
#14108=CARTESIAN_POINT ( 'NONE',  ( 120.1140014775786398, -7.894159318335828068, -9.358103419637847864 ) ) ;
#14111=CARTESIAN_POINT ( 'NONE',  ( 117.8449348109119938, -1.833838273342659253, -17.42832698103878286 ) ) ;
#14112=CARTESIAN_POINT ( 'NONE',  ( 111.7184548109119788, -9.261995988541697145, -16.69588392320189030 ) ) ;
#14113=CARTESIAN_POINT ( 'NONE',  ( 115.1220548109119761, -8.166667518702817929, -8.995218007635861213 ) ) ;
#14114=CARTESIAN_POINT ( 'NONE',  ( 123.0070614775786311, 0.9020085738987273505, -11.91225656197088512 ) ) ;
#14115=CARTESIAN_POINT ( 'NONE',  ( 117.9583881442453048, 0.1319031606808879209, -14.10382304977623669 ) ) ;
#14117=CARTESIAN_POINT ( 'NONE',  ( 117.3343948109119737, -3.383040157471821630, -19.15922257007629170 ) ) ;
#14122=CARTESIAN_POINT ( 'NONE',  ( 121.8725281442453223, -3.383040157471821630, -19.15922257007629170 ) ) ;
#14124=CARTESIAN_POINT ( 'NONE',  ( 118.2795432127138611, -2.191907684172563986, -18.20049396185734025 ) ) ;
#14125=CARTESIAN_POINT ( 'NONE',  ( 117.9583881442453048, 0.1319031606808879209, -14.10382304977623669 ) ) ;
#14133=CARTESIAN_POINT ( 'NONE',  ( 114.4413348109119823, -9.261995988541697145, -16.69588392320189030 ) ) ;
#14134=CARTESIAN_POINT ( 'NONE',  ( 125.3895814775786448, -2.084020599724406786, -8.691656652584148546 ) ) ;
#14135=CARTESIAN_POINT ( 'NONE',  ( 124.6521348109119884, -1.561330072975668948, -17.79121239304076951 ) ) ;
#14136=CARTESIAN_POINT ( 'NONE',  ( 115.8595014775786609, -7.643976991954077427, -18.09477374809248928 ) ) ;
#14139=CARTESIAN_POINT ( 'NONE',  ( 119.8870948109119752, -9.261995988541697145, -16.69588392320189030 ) ) ;
#14142=CARTESIAN_POINT ( 'NONE',  ( 124.5954081442453116, -6.222761293078241884, -8.102969835052219238 ) ) ;
#14146=CARTESIAN_POINT ( 'NONE',  ( 117.4478481442453131, 0.2603800115204892296, -16.42320221600525088 ) ) ;
#14147=CARTESIAN_POINT ( 'NONE',  ( 123.1772414775786189, -5.574606645277164318, -18.38911715685844683 ) ) ;
#14149=CARTESIAN_POINT ( 'NONE',  ( 136.7741008876067781, -1.264212383164096121, -9.092737378789559344 ) ) ;
#14150=CARTESIAN_POINT ( 'NONE',  ( 124.0848681442452772, -4.089484607189486809, -7.948022111789456723 ) ) ;
#14152=CARTESIAN_POINT ( 'NONE',  ( 121.4754414775786131, -1.833838273342659697, -17.42832698103878286 ) ) ;
#14154=ORIENTED_EDGE ( 'NONE', *, *, #37928, .T. ) ;
#14155=CARTESIAN_POINT ( 'NONE',  ( 113.3635281442453504, -9.988377603198976828, -10.36322818467138340 ) ) ;
#14156=CARTESIAN_POINT ( 'NONE',  ( 124.6521348109119884, -7.894159318335828068, -9.358103419637847864 ) ) ;
#14158=CARTESIAN_POINT ( 'NONE',  ( 121.8725281442453223, -3.383040157471821630, -19.15922257007629170 ) ) ;
#14162=CARTESIAN_POINT ( 'NONE',  ( 123.1772414775786189, -4.089484607189486809, -7.948022111789456723 ) ) ;
#14163=CARTESIAN_POINT ( 'NONE',  ( 120.9081748109119872, -5.638512984488999180, -18.83840828888717311 ) ) ;
#14164=CARTESIAN_POINT ( 'NONE',  ( 125.0492214775786266, -3.505236298600246325, -18.68346056562440793 ) ) ;
#14165=CARTESIAN_POINT ( 'NONE',  ( 119.5467348109119712, -5.574606645277164318, -18.38911715685844683 ) ) ;
#14167=CARTESIAN_POINT ( 'NONE',  ( 114.2711548109119803, -9.988377603198976828, -10.36322818467138340 ) ) ;
#14171=CARTESIAN_POINT ( 'NONE',  ( 125.8328548109119964, -8.862178061931794915, -16.39564131203325559 ) ) ;
#14175=CARTESIAN_POINT ( 'NONE',  ( 125.3790414775786388, -0.8658195297466895202, -10.39078908864337514 ) ) ;
#14176=CARTESIAN_POINT ( 'NONE',  ( 125.3328548109119964, -0.8288870151387760510, -10.36305467784173118 ) ) ;
#14178=CARTESIAN_POINT ( 'NONE',  ( 113.5337081442453240, -0.8288870151387760510, -10.36305467784173118 ) ) ;
#14181=CARTESIAN_POINT ( 'NONE',  ( 123.2906948109119867, -8.166667518702819706, -8.995218007635861213 ) ) ;
#14182=( BOUNDED_CURVE ( )  B_SPLINE_CURVE ( 2, ( #21563, #1259, #18376, #21338, #35450, #4225, #18144, #32264, #1032, #8333, #42988, #35223, #28860, #42772, #8111, #3997, #11755 ),
 .UNSPECIFIED., .F., .T. ) 
 B_SPLINE_CURVE_WITH_KNOTS ( ( 3, 2, 2, 2, 2, 2, 2, 2, 3 ),
 ( 0.3921282416568590001, 0.3984375000000000000, 0.4062500000000000000, 0.4140625000000000000, 0.4218750000000000000, 0.4296875000000000000, 0.4375000000000000000, 0.4453125000000000000, 0.4516217583431409999 ),
 .UNSPECIFIED. ) 
 CURVE ( )  GEOMETRIC_REPRESENTATION_ITEM ( )  RATIONAL_B_SPLINE_CURVE ( ( 0.9763430640195970289, 0.9385262470928680267, 1.000000000000000000, 0.9238795325112869605, 1.000000000000000000, 0.9238795325112869605, 1.000000000000000000, 0.9238795325112869605, 1.000000000000000000, 0.9238795325112869605, 1.000000000000000000, 0.9238795325112869605, 1.000000000000000000, 0.9238795325112869605, 1.000000000000000000, 0.9385262470928680267, 0.9763430640195970289 ) ) 
 REPRESENTATION_ITEM ( '' )  );
#14183=CARTESIAN_POINT ( 'NONE',  ( 124.9357681442453014, -1.834011780172310813, -8.268836392978581529 ) ) ;
#14185=CARTESIAN_POINT ( 'NONE',  ( 113.7606148109119886, -1.561330072975668060, -17.79121239304076596 ) ) ;
#14192=CARTESIAN_POINT ( 'NONE',  ( 116.3700414775786527, -4.153390946401321671, -8.397313243818183892 ) ) ;
#14193=CARTESIAN_POINT ( 'NONE',  ( 113.7606148109119886, -1.561330072975668060, -17.79121239304076596 ) ) ;
#14197=CARTESIAN_POINT ( 'NONE',  ( 120.5110881442453206, -3.505236298600246325, -18.68346056562440793 ) ) ;
#14198=CARTESIAN_POINT ( 'NONE',  ( 120.9649014775786355, -6.222761293078241884, -8.102969835052219238 ) ) ;
#14199=CARTESIAN_POINT ( 'NONE',  ( 113.9307948109119764, -10.15424416112533912, -14.75197769757731336 ) ) ;
#14200=EDGE_LOOP ( 'NONE', ( #5758, #37036, #6814, #30785 ) ) ;
#14204=CARTESIAN_POINT ( 'NONE',  ( 124.8223148109119762, -10.15424416112533912, -14.75197769757731336 ) ) ;
#14206=CARTESIAN_POINT ( 'NONE',  ( 114.4980614775786734, -2.084020599724406786, -8.691656652584148546 ) ) ;
#14212=CARTESIAN_POINT ( 'NONE',  ( 119.8303681442453126, 0.4262465694468514643, -12.03445270309931736 ) ) ;
#14213=CARTESIAN_POINT ( 'NONE',  ( 114.3278814775786429, 0.1319031606808879209, -14.10382304977623669 ) ) ;
#14217=CARTESIAN_POINT ( 'NONE',  ( 121.3000491344827481, -1.149058757900107697, -17.09122335155391781 ) ) ;
#14222=CARTESIAN_POINT ( 'NONE',  ( 113.3068014775786594, -8.166667518702817929, -8.995218007635859436 ) ) ;
#14223=CARTESIAN_POINT ( 'NONE',  ( 122.8936081442453059, -9.565557343593413364, -10.61323700422348004 ) ) ;
#14224=CARTESIAN_POINT ( 'NONE',  ( 116.9940348109119839, -0.1624402480850797581, -16.17319339645315424 ) ) ;
#14228=CARTESIAN_POINT ( 'NONE',  ( 116.6536748109119941, -10.15424416112533912, -14.75197769757731336 ) ) ;
#14230=CARTESIAN_POINT ( 'NONE',  ( 116.9190222310133578, -1.244021962887374544, -16.96476564598603076 ) ) ;
#14231=CARTESIAN_POINT ( 'NONE',  ( 113.7038881442453402, -3.383040157471821630, -19.15922257007629170 ) ) ;
#14233=CARTESIAN_POINT ( 'NONE',  ( 116.2565881442452991, -9.261995988541697145, -16.69588392320189030 ) ) ;
#14236=CARTESIAN_POINT ( 'NONE',  ( 113.5337081442453240, -9.261995988541697145, -16.69588392320189030 ) ) ;
#14237=CARTESIAN_POINT ( 'NONE',  ( 112.7395348109119766, -5.638512984488999180, -18.83840828888717311 ) ) ;
#14238=CARTESIAN_POINT ( 'NONE',  ( 121.9859814775786333, -9.565557343593413364, -10.61323700422348004 ) ) ;
#14245=CARTESIAN_POINT ( 'NONE',  ( 114.8951481442453115, -8.899110576539710493, -16.42337572283490132 ) ) ;
#14250=CARTESIAN_POINT ( 'NONE',  ( 125.6164881442453094, 0.2603800115204892296, -16.42320221600525088 ) ) ;
#14252=CARTESIAN_POINT ( 'NONE',  ( 123.6877814775786533, -3.383040157471821630, -19.15922257007629170 ) ) ;
#14253=CARTESIAN_POINT ( 'NONE',  ( 115.6893214775786447, 0.5811942927096154232, -14.16772938898807155 ) ) ;
#14254=VERTEX_POINT ( 'NONE', #18809 ) ;
#14256=CARTESIAN_POINT ( 'NONE',  ( 113.1933481442453058, -5.574606645277164318, -18.38911715685844683 ) ) ;
#14257=CARTESIAN_POINT ( 'NONE',  ( 113.2500748109119968, -6.344957434206662583, -7.627207830600332805 ) ) ;
#14258=CARTESIAN_POINT ( 'NONE',  ( 118.0151148109119816, -10.63000616557722466, -14.87417383870573495 ) ) ;
#14259=CARTESIAN_POINT ( 'NONE',  ( 117.6180281442453150, -8.899110576539710493, -16.42337572283490132 ) ) ;
#14262=CARTESIAN_POINT ( 'NONE',  ( 120.7947214775786193, -0.8288870151387760510, -10.36305467784173118 ) ) ;
#14263=CARTESIAN_POINT ( 'NONE',  ( 117.6747548109119919, -1.834011780172310813, -8.268836392978581529 ) ) ;
#14265=CARTESIAN_POINT ( 'NONE',  ( 136.9920288091157943, 0.2741831093159626254, -15.27028804600930556 ) ) ;
#14268=CARTESIAN_POINT ( 'NONE',  ( 126.8594690244564731, 0.4528996404656494557, -13.19682093318863814 ) ) ;
#14270=CARTESIAN_POINT ( 'NONE',  ( 114.4980614775786592, -7.893985811506177619, -18.51759400769804742 ) ) ;
#14276=CARTESIAN_POINT ( 'NONE',  ( 113.9875214775786532, -8.899110576539710493, -16.42337572283490132 ) ) ;
#14280=CARTESIAN_POINT ( 'NONE',  ( 118.5256548109119876, -0.4660016031367711919, -10.09054647747476352 ) ) ;
#14281=CARTESIAN_POINT ( 'NONE',  ( 114.4413348109119823, -9.261995988541697145, -16.69588392320189030 ) ) ;
#14283=CARTESIAN_POINT ( 'NONE',  ( 117.4478481442453131, -9.565557343593413364, -10.61323700422348004 ) ) ;
#14286=CARTESIAN_POINT ( 'NONE',  ( 122.4397948109119767, -9.988377603198976828, -10.36322818467138340 ) ) ;
#14288=CARTESIAN_POINT ( 'NONE',  ( 116.2565881442453133, -0.8288870151387760510, -10.36305467784173118 ) ) ;
#14290=CARTESIAN_POINT ( 'NONE',  ( 112.8529881442453160, -7.894159318335828068, -9.358103419637847864 ) ) ;
#14293=CARTESIAN_POINT ( 'NONE',  ( 119.2063748109119814, -7.894159318335828068, -9.358103419637847864 ) ) ;
#14294=CARTESIAN_POINT ( 'NONE',  ( 120.2274548109119934, -9.859900752359378018, -12.68260735090039759 ) ) ;
#14295=CARTESIAN_POINT ( 'NONE',  ( 114.4413348109119823, -0.8288870151387681684, -10.36305467784174184 ) ) ;
#14301=CARTESIAN_POINT ( 'NONE',  ( 115.8595014775786609, -1.834011780172310813, -8.268836392978581529 ) ) ;
#14302=CARTESIAN_POINT ( 'NONE',  ( 114.4413348109119823, -9.261995988541697145, -16.69588392320189030 ) ) ;
#14304=CARTESIAN_POINT ( 'NONE',  ( 114.1009748109119784, -4.089484607189486809, -7.948022111789456723 ) ) ;
#14307=CARTESIAN_POINT ( 'NONE',  ( 120.7379948109119709, -10.63000616557722466, -14.87417383870573495 ) ) ;
#14308=CARTESIAN_POINT ( 'NONE',  ( 116.5969481442453031, 0.5811942927096154232, -14.16772938898807155 ) ) ;
#14310=CARTESIAN_POINT ( 'NONE',  ( 121.5321681442453183, -0.1624402480850797581, -16.17319339645315424 ) ) ;
#14313=CARTESIAN_POINT ( 'NONE',  ( 125.5597614775786326, -1.561330072975669392, -17.79121239304076951 ) ) ;
#14314=CARTESIAN_POINT ( 'NONE',  ( 122.9503348109119827, 0.5811942927096110934, -14.16772938898807510 ) ) ;
#14317=CARTESIAN_POINT ( 'NONE',  ( 115.1220548109119761, -1.833838273342658809, -17.42832698103878286 ) ) ;
#14320=CARTESIAN_POINT ( 'NONE',  ( 122.3830681442452857, -8.166667518702819706, -8.995218007635861213 ) ) ;
#14323=CARTESIAN_POINT ( 'NONE',  ( 118.6958348109119754, -6.344957434206665248, -7.627207830600338134 ) ) ;
#14326=CARTESIAN_POINT ( 'NONE',  ( 124.3685014775786328, -10.63000616557722466, -14.87417383870573495 ) ) ;
#14329=CARTESIAN_POINT ( 'NONE',  ( 115.2922348109119781, 0.4262465694468514643, -12.03445270309931736 ) ) ;
#14330=CARTESIAN_POINT ( 'NONE',  ( 120.5887993777725029, -1.267766418764730840, -16.93314635290706605 ) ) ;
#14331=CARTESIAN_POINT ( 'NONE',  ( 121.3619881442452879, -5.574606645277164318, -18.38911715685844683 ) ) ;
#14332=CARTESIAN_POINT ( 'NONE',  ( 120.3296260002550895, -2.334846009198419559, -18.01015021110789505 ) ) ;
#14333=CARTESIAN_POINT ( 'NONE',  ( 122.8936081442453059, -9.565557343593413364, -10.61323700422348004 ) ) ;
#14335=CARTESIAN_POINT ( 'NONE',  ( 119.0361948109119652, -2.084020599724406786, -8.691656652584148546 ) ) ;
#14337=CARTESIAN_POINT ( 'NONE',  ( 116.0864081442453113, -9.988377603198976828, -10.36322818467138340 ) ) ;
#14339=CARTESIAN_POINT ( 'NONE',  ( 119.1496481442453046, -6.222761293078241884, -8.102969835052219238 ) ) ;
#14341=CARTESIAN_POINT ( 'NONE',  ( 118.2420214775786320, -3.383040157471821630, -19.15922257007629170 ) ) ;
#14347=CARTESIAN_POINT ( 'NONE',  ( 123.8579614775786126, 0.5811942927096110934, -14.16772938898807510 ) ) ;
#14349=CARTESIAN_POINT ( 'NONE',  ( 126.5125895482207312, -8.445584708276319574, -9.696654088380508796 ) ) ;
#14350=CARTESIAN_POINT ( 'NONE',  ( 120.5678148109119832, -1.833838273342659253, -17.42832698103878286 ) ) ;
#14351=CARTESIAN_POINT ( 'NONE',  ( 115.6432824739652148, 0.3208234527006404435, -15.99825685930877661 ) ) ;
#14358=CARTESIAN_POINT ( 'NONE',  ( 113.7038881442453402, -3.383040157471821630, -19.15922257007629170 ) ) ;
#14359=CARTESIAN_POINT ( 'NONE',  ( 124.8223148109119762, -10.15424416112533912, -14.75197769757731336 ) ) ;
#14360=CARTESIAN_POINT ( 'NONE',  ( 122.0427081442452817, 0.5811942927096110934, -14.16772938898807510 ) ) ;
#14361=CARTESIAN_POINT ( 'NONE',  ( 117.0507614775786465, 0.1319031606808879209, -14.10382304977623669 ) ) ;
#14363=CARTESIAN_POINT ( 'NONE',  ( 123.1772414775786189, -4.089484607189486809, -7.948022111789456723 ) ) ;
#14364=CARTESIAN_POINT ( 'NONE',  ( 111.7289948109120132, -2.109465145232937378, -8.734689011829464889 ) ) ;
#14367=CARTESIAN_POINT ( 'NONE',  ( 124.9924948109119924, -5.574606645277164318, -18.38911715685844683 ) ) ;
#14371=CARTESIAN_POINT ( 'NONE',  ( 120.2274548109119934, 0.5811942927096110934, -14.16772938898807510 ) ) ;
#14372=CARTESIAN_POINT ( 'NONE',  ( 123.5743281442453139, -2.084020599724406786, -8.691656652584148546 ) ) ;
#14374=CARTESIAN_POINT ( 'NONE',  ( 137.0596819398274135, 0.02950868989288273417, -11.06250843582902732 ) ) ;
#14375=CARTESIAN_POINT ( 'NONE',  ( 120.6812681442452941, -10.30919188438810075, -12.61870101168855918 ) ) ;
#14377=CARTESIAN_POINT ( 'NONE',  ( 118.4689281442453392, -10.15424416112533912, -14.75197769757731336 ) ) ;
#14379=CARTESIAN_POINT ( 'NONE',  ( 114.8384214775786489, 0.9020085738987339008, -11.91225656197089222 ) ) ;
#14384=CARTESIAN_POINT ( 'NONE',  ( 125.7866681442452688, -0.4660016031367893996, -10.09054647747474043 ) ) ;
#14385=FACE_OUTER_BOUND ( 'NONE', #24266, .T. ) ;
#14387=CARTESIAN_POINT ( 'NONE',  ( 125.1059481442452750, -8.166667518702819706, -8.995218007635861213 ) ) ;
#14388=CARTESIAN_POINT ( 'NONE',  ( 122.8936081442453059, 0.2603800115204892296, -16.42320221600525088 ) ) ;
#14389=CARTESIAN_POINT ( 'NONE',  ( 121.5888948109119809, 0.1319031606808879209, -14.10382304977623669 ) ) ;
#14390=CARTESIAN_POINT ( 'NONE',  ( 120.4543614775786295, -5.574606645277164318, -18.38911715685844683 ) ) ;
#14392=CARTESIAN_POINT ( 'NONE',  ( 116.7104014775786425, -0.4660016031367893996, -10.09054647747474043 ) ) ;
#14395=CARTESIAN_POINT ( 'NONE',  ( 122.6710448144346657, -2.280480477428469488, -18.08254604495227014 ) ) ;
#14401=FACE_OUTER_BOUND ( 'NONE', #22973, .T. ) ;
#14402=CARTESIAN_POINT ( 'NONE',  ( 126.5241148109119393, -9.565557343593413364, -10.61323700422348004 ) ) ;
#14404=CARTESIAN_POINT ( 'NONE',  ( 113.3635281442453504, -0.1624402480850797581, -16.17319339645315424 ) ) ;
#14406=CARTESIAN_POINT ( 'NONE',  ( 122.3620835773848654, -2.467220198592777969, -17.83387418641524391 ) ) ;
#14407=CARTESIAN_POINT ( 'NONE',  ( 122.7801548109119665, -3.383040157471821630, -19.15922257007629170 ) ) ;
#14408=CARTESIAN_POINT ( 'NONE',  ( 123.2906948109119867, -8.166667518702819706, -8.995218007635861213 ) ) ;
#14410=CARTESIAN_POINT ( 'NONE',  ( 117.0507614775786465, -10.30919188438810075, -12.61870101168855918 ) ) ;
#14414=CARTESIAN_POINT ( 'NONE',  ( 126.3509913982132105, -7.545821528410036727, -9.094723512232105733 ) ) ;
#14415=CARTESIAN_POINT ( 'NONE',  ( 117.1074881442453233, 0.4262465694468514643, -12.03445270309931736 ) ) ;
#14416=CARTESIAN_POINT ( 'NONE',  ( 111.7751814775786556, -7.893985811506177619, -18.51759400769804742 ) ) ;
#14420=CARTESIAN_POINT ( 'NONE',  ( 118.4122014775786340, -9.859900752359374465, -12.68260735090039404 ) ) ;
#14421=CARTESIAN_POINT ( 'NONE',  ( 112.5126281442453120, 0.1319031606808879209, -14.10382304977623669 ) ) ;
#14425=CARTESIAN_POINT ( 'NONE',  ( 125.6164881442453094, -9.565557343593413364, -10.61323700422348004 ) ) ;
#14426=CARTESIAN_POINT ( 'NONE',  ( 114.3846081442453197, 0.4262465694468514643, -12.03445270309931736 ) ) ;
#14427=ORIENTED_EDGE ( 'NONE', *, *, #33918, .F. ) ;
#14428=CARTESIAN_POINT ( 'NONE',  ( 126.2940345447972277, -9.080993302305092385, -16.14937674896652098 ) ) ;
#14430=CARTESIAN_POINT ( 'NONE',  ( 112.8529881442453302, -1.561330072975668060, -17.79121239304076596 ) ) ;
#14433=CARTESIAN_POINT ( 'NONE',  ( 125.0492214775786266, -3.505236298600246325, -18.68346056562440793 ) ) ;
#14435=CARTESIAN_POINT ( 'NONE',  ( 116.8805814775786445, -3.505236298600246325, -18.68346056562440793 ) ) ;
#14437=CARTESIAN_POINT ( 'NONE',  ( 112.6828081442453282, -2.084020599724406786, -8.691656652584148546 ) ) ;
#14444=CARTESIAN_POINT ( 'NONE',  ( 112.9664414775786412, 0.5811942927096154232, -14.16772938898807155 ) ) ;
#14445=EDGE_CURVE ( 'NONE', #40322, #32536, #39664, .T. ) ;
#14446=CARTESIAN_POINT ( 'NONE',  ( 125.3328548109119964, -0.8288870151387760510, -10.36305467784173118 ) ) ;
#14448=CARTESIAN_POINT ( 'NONE',  ( 118.9794681442453026, -0.8288870151387760510, -10.36305467784173118 ) ) ;
#14449=FACE_OUTER_BOUND ( 'NONE', #24712, .T. ) ;
#14452=CARTESIAN_POINT ( 'NONE',  ( 116.1431348109119881, 0.1319031606808879209, -14.10382304977623669 ) ) ;
#14456=CARTESIAN_POINT ( 'NONE',  ( 113.3635281442453504, -9.988377603198976828, -10.36322818467138340 ) ) ;
#14458=CARTESIAN_POINT ( 'NONE',  ( 118.8092881442453290, -9.988377603198976828, -10.36322818467138340 ) ) ;
#14461=CARTESIAN_POINT ( 'NONE',  ( 113.6471614775786492, -5.638512984488999180, -18.83840828888717311 ) ) ;
#14462=CARTESIAN_POINT ( 'NONE',  ( 115.0086014775786509, -4.089484607189486809, -7.948022111789456723 ) ) ;
#14466=ORIENTED_EDGE ( 'NONE', *, *, #28469, .F. ) ;
#14467=CARTESIAN_POINT ( 'NONE',  ( 112.0827276054816366, -2.287189184988692947, -18.07361239780447448 ) ) ;
#14469=CARTESIAN_POINT ( 'NONE',  ( 117.5613014775786525, -10.15424416112533912, -14.75197769757731336 ) ) ;
#14471=CARTESIAN_POINT ( 'NONE',  ( 122.4040527111058339, -1.267766418764731728, -16.93314635290706605 ) ) ;
#14474=CARTESIAN_POINT ( 'NONE',  ( 125.0492214775786266, -6.344957434206665248, -7.627207830600338134 ) ) ;
#14475=CARTESIAN_POINT ( 'NONE',  ( 120.2841814775786276, -10.15424416112534622, -14.75197769757730448 ) ) ;
#14476=CARTESIAN_POINT ( 'NONE',  ( 125.5597614775786326, -1.561330072975669392, -17.79121239304076951 ) ) ;
#14477=CARTESIAN_POINT ( 'NONE',  ( 114.8951481442453115, -0.4660016031367893996, -10.09054647747474043 ) ) ;
#14478=ORIENTED_EDGE ( 'NONE', *, *, #19256, .F. ) ;
#14479=CARTESIAN_POINT ( 'NONE',  ( 113.6471614775786492, -4.153390946401321671, -8.397313243818183892 ) ) ;
#14481=CARTESIAN_POINT ( 'NONE',  ( 116.2565881442452991, -9.261995988541697145, -16.69588392320189030 ) ) ;
#14482=CARTESIAN_POINT ( 'NONE',  ( 114.6682414775786469, -7.894159318335828068, -9.358103419637847864 ) ) ;
#14484=CARTESIAN_POINT ( 'NONE',  ( 121.8158014775786171, -4.153390946401325223, -8.397313243818185668 ) ) ;
#14486=CARTESIAN_POINT ( 'NONE',  ( 115.0653281442453277, -6.344957434206662583, -7.627207830600332805 ) ) ;
#14487=CARTESIAN_POINT ( 'NONE',  ( 137.2645862585842451, 0.3856499210305354142, -13.29373647331895114 ) ) ;
#14489=CARTESIAN_POINT ( 'NONE',  ( 114.4526169549021830, -1.135392229370321582, -17.10942237759953954 ) ) ;
#14490=CARTESIAN_POINT ( 'NONE',  ( 127.1470196510598782, 0.5883225706286522305, -13.03016238292672213 ) ) ;
#14492=CARTESIAN_POINT ( 'NONE',  ( 114.6682414775786469, -1.561330072975668060, -17.79121239304076596 ) ) ;
#14495=CARTESIAN_POINT ( 'NONE',  ( 115.2355081442453155, 0.1319031606808879209, -14.10382304977623669 ) ) ;
#14500=CARTESIAN_POINT ( 'NONE',  ( 113.1366214775786432, -7.643976991954077427, -18.09477374809248928 ) ) ;
#14503=CARTESIAN_POINT ( 'NONE',  ( 118.6958348109119754, -6.344957434206651037, -7.627207830600339911 ) ) ;
#14504=CARTESIAN_POINT ( 'NONE',  ( 118.8092881442453290, -9.988377603198976828, -10.36322818467138340 ) ) ;
#14505=CARTESIAN_POINT ( 'NONE',  ( 124.7088614775786226, -9.565557343593413364, -10.61323700422348004 ) ) ;
#14506=CARTESIAN_POINT ( 'NONE',  ( 118.6391081442452986, -5.574606645277164318, -18.38911715685844683 ) ) ;
#14507=CARTESIAN_POINT ( 'NONE',  ( 125.6164881442453094, 0.2603800115204892296, -16.42320221600525088 ) ) ;
#14509=CARTESIAN_POINT ( 'NONE',  ( 137.2865145795256865, -8.609599717022557996, -9.742863212004273521 ) ) ;
#14511=CARTESIAN_POINT ( 'NONE',  ( 121.2485348109119769, -0.4660016031367893996, -10.09054647747474043 ) ) ;
#14513=CARTESIAN_POINT ( 'NONE',  ( 118.4122014775786340, -9.859900752359374465, -12.68260735090039404 ) ) ;
#14514=CARTESIAN_POINT ( 'NONE',  ( 126.1837548109119211, -10.63000616557722466, -14.87417383870573495 ) ) ;
#14517=CARTESIAN_POINT ( 'NONE',  ( 119.7169148109119874, -0.1624402480850797581, -16.17319339645315424 ) ) ;
#14518=CARTESIAN_POINT ( 'NONE',  ( 124.0848681442452772, -5.574606645277164318, -18.38911715685844683 ) ) ;
#14523=CARTESIAN_POINT ( 'NONE',  ( 122.4040527111058339, -1.267766418764731728, -16.93314635290706605 ) ) ;
#14524=CARTESIAN_POINT ( 'NONE',  ( 115.7460481442453357, 0.9020085738987339008, -11.91225656197089222 ) ) ;
#14525=CARTESIAN_POINT ( 'NONE',  ( 113.6471614775786492, -5.638512984488999180, -18.83840828888717311 ) ) ;
#14527=CARTESIAN_POINT ( 'NONE',  ( 111.9453614775786434, -1.561330072975668060, -17.79121239304076596 ) ) ;
#14528=ORIENTED_EDGE ( 'NONE', *, *, #23091, .F. ) ;
#14529=CARTESIAN_POINT ( 'NONE',  ( 113.1314091344827659, -1.149058757900096595, -17.09122335155389649 ) ) ;
#14530=CARTESIAN_POINT ( 'NONE',  ( 124.2550481442452792, -9.988377603198980381, -10.36322818467138518 ) ) ;
#14531=CARTESIAN_POINT ( 'NONE',  ( 117.1074881442453233, -10.63000616557722466, -14.87417383870573495 ) ) ;
#14533=CARTESIAN_POINT ( 'NONE',  ( 123.0070614775786169, -10.15424416112533912, -14.75197769757731336 ) ) ;
#14534=( LENGTH_UNIT ( ) NAMED_UNIT ( * ) SI_UNIT ( .MILLI., .METRE. ) );
#14535=CARTESIAN_POINT ( 'NONE',  ( 112.1722681442453222, -8.899110576539710493, -16.42337572283490132 ) ) ;
#14536=CARTESIAN_POINT ( 'NONE',  ( 120.9649014775786355, -3.383040157471821630, -19.15922257007629170 ) ) ;
#14538=CARTESIAN_POINT ( 'NONE',  ( 115.8027748109119841, -8.899110576539710493, -16.42337572283490132 ) ) ;
#14541=CARTESIAN_POINT ( 'NONE',  ( 123.1772414775786189, -4.089484607189486809, -7.948022111789456723 ) ) ;
#14544=CARTESIAN_POINT ( 'NONE',  ( 118.5256548109119876, -0.4660016031367893996, -10.09054647747474043 ) ) ;
#14548=CARTESIAN_POINT ( 'NONE',  ( 122.4965214775786251, -10.30919188438810075, -12.61870101168855918 ) ) ;
#14549=CARTESIAN_POINT ( 'NONE',  ( 115.6893214775786447, -9.859900752359374465, -12.68260735090039404 ) ) ;
#14551=CARTESIAN_POINT ( 'NONE',  ( 121.2485348109119769, -8.899110576539710493, -16.42337572283490132 ) ) ;
#14553=CARTESIAN_POINT ( 'NONE',  ( 120.3976348109119812, -7.643976991954077427, -18.09477374809248928 ) ) ;
#14557=CARTESIAN_POINT ( 'NONE',  ( 118.2420214775786320, -6.222761293078241884, -8.102969835052219238 ) ) ;
#14558=CARTESIAN_POINT ( 'NONE',  ( 113.1366214775786432, -1.834011780172310813, -8.268836392978581529 ) ) ;
#14559=CARTESIAN_POINT ( 'NONE',  ( 118.5823814775786360, -1.834011780172310813, -8.268836392978581529 ) ) ;
#14560=CARTESIAN_POINT ( 'NONE',  ( 125.3328548109119964, -0.8288870151387760510, -10.36305467784173118 ) ) ;
#14561=CARTESIAN_POINT ( 'NONE',  ( 128.2184548109119930, -7.067465109756605912, -7.812468278694988832 ) ) ;
#14562=CARTESIAN_POINT ( 'NONE',  ( 120.6812681442452941, 0.1319031606808879209, -14.10382304977623669 ) ) ;
#14564=CARTESIAN_POINT ( 'NONE',  ( 117.8449348109119938, -8.166667518702817929, -8.995218007635861213 ) ) ;
#14569=CARTESIAN_POINT ( 'NONE',  ( 127.8631586617352838, -4.391174868859571312, -15.27166827963823614 ) ) ;
#14570=CARTESIAN_POINT ( 'NONE',  ( 122.6099748109119929, -9.261995988541697145, -16.69588392320189030 ) ) ;
#14573=CARTESIAN_POINT ( 'NONE',  ( 128.2184548109119930, -9.609004340414083245, -9.721032963308941177 ) ) ;
#14574=CARTESIAN_POINT ( 'NONE',  ( 121.7590748109119687, -2.084020599724406786, -8.691656652584148546 ) ) ;
#14577=CARTESIAN_POINT ( 'NONE',  ( 111.5588148109119828, 0.08617673920517221475, -14.09731900820172967 ) ) ;
#14580=CARTESIAN_POINT ( 'NONE',  ( 113.5904348109119866, -7.893985811506177619, -18.51759400769804742 ) ) ;
#14581=CARTESIAN_POINT ( 'NONE',  ( 126.3539348109119800, -4.153390946401325223, -8.397313243818185668 ) ) ;
#14583=CARTESIAN_POINT ( 'NONE',  ( 120.6812681442452941, 0.1319031606808879209, -14.10382304977623669 ) ) ;
#14586=CARTESIAN_POINT ( 'NONE',  ( 121.4187148109119789, -6.344957434206665248, -7.627207830600338134 ) ) ;
#14587=FACE_OUTER_BOUND ( 'NONE', #9914, .T. ) ;
#14590=CARTESIAN_POINT ( 'NONE',  ( 112.3991748109119868, -8.166667518702817929, -8.995218007635859436 ) ) ;
#14594=CARTESIAN_POINT ( 'NONE',  ( 119.6034614775786196, -6.344957434206665248, -7.627207830600338134 ) ) ;
#14595=CARTESIAN_POINT ( 'NONE',  ( 136.9012041053437088, -9.901132554421634424, -15.67648283907295159 ) ) ;
#14597=CARTESIAN_POINT ( 'NONE',  ( 112.0020881442453344, 0.2603800115204892296, -16.42320221600525088 ) ) ;
#14598=CARTESIAN_POINT ( 'NONE',  ( 121.4187148109119789, -6.344957434206665248, -7.627207830600338134 ) ) ;
#14600=CARTESIAN_POINT ( 'NONE',  ( 122.0427081442452817, -9.859900752359378018, -12.68260735090039759 ) ) ;
#14603=CARTESIAN_POINT ( 'NONE',  ( 114.4413348109119823, -9.261995988541697145, -16.69588392320189030 ) ) ;
#14604=CARTESIAN_POINT ( 'NONE',  ( 110.2184548109119788, -4.863998795839242995, -13.39321520033831447 ) ) ;
#14607=CARTESIAN_POINT ( 'NONE',  ( 111.4401632144035403, -2.485602189585009114, -17.80939581708303621 ) ) ;
#14608=CARTESIAN_POINT ( 'NONE',  ( 111.8886348109120092, -6.222761293078241884, -8.102969835052219238 ) ) ;
#14612=CARTESIAN_POINT ( 'NONE',  ( 123.0637881442452937, -0.4660016031367893996, -10.09054647747474043 ) ) ;
#14613=CARTESIAN_POINT ( 'NONE',  ( 120.9649014775786355, -3.383040157471821630, -19.15922257007629170 ) ) ;
#14614=CARTESIAN_POINT ( 'NONE',  ( 122.7801548109119665, -6.222761293078241884, -8.102969835052219238 ) ) ;
#14615=CARTESIAN_POINT ( 'NONE',  ( 119.0929214775786278, -4.153390946401325223, -8.397313243818185668 ) ) ;
#14616=CARTESIAN_POINT ( 'NONE',  ( 125.4357681442453440, -2.109465145233854422, -8.734689011828928429 ) ) ;
#14617=CARTESIAN_POINT ( 'NONE',  ( 118.7525614775786380, -8.166667518702819706, -8.995218007635861213 ) ) ;
#14625=CARTESIAN_POINT ( 'NONE',  ( 125.0492214775786266, -6.344957434206665248, -7.627207830600338134 ) ) ;
#14626=CARTESIAN_POINT ( 'NONE',  ( 125.0492214775786266, -3.505236298600246325, -18.68346056562440793 ) ) ;
#14628=CARTESIAN_POINT ( 'NONE',  ( 112.5693548109119888, 0.4262465694468514643, -12.03445270309931736 ) ) ;
#14632=CARTESIAN_POINT ( 'NONE',  ( 125.5030348109119558, -3.383040157471821630, -19.15922257007629170 ) ) ;
#14634=CARTESIAN_POINT ( 'NONE',  ( 114.4413348109119823, -9.261995988541697145, -16.69588392320189030 ) ) ;
#14638=CARTESIAN_POINT ( 'NONE',  ( 126.9932531981167756, -7.212978846078887507, -8.544877725673300617 ) ) ;
#14640=CARTESIAN_POINT ( 'NONE',  ( 115.9729548109119861, -3.505236298600246325, -18.68346056562440793 ) ) ;
#14641=CARTESIAN_POINT ( 'NONE',  ( 113.1366214775786432, -1.834011780172310813, -8.268836392978581529 ) ) ;
#14642=CARTESIAN_POINT ( 'NONE',  ( 113.3068014775786594, -8.166667518702817929, -8.995218007635859436 ) ) ;
#14644=CARTESIAN_POINT ( 'NONE',  ( 118.5823814775786502, -7.643976991954101408, -18.09477374809246797 ) ) ;
#14646=CARTESIAN_POINT ( 'NONE',  ( 120.1140014775786398, -7.894159318335828068, -9.358103419637847864 ) ) ;
#14647=CARTESIAN_POINT ( 'NONE',  ( 115.2922348109119781, 0.4262465694468514643, -12.03445270309931736 ) ) ;
#14651=CARTESIAN_POINT ( 'NONE',  ( 112.9664414775786412, -9.859900752359374465, -12.68260735090039404 ) ) ;
#14654=CARTESIAN_POINT ( 'NONE',  ( 123.9714148109119805, -8.899110576539726480, -16.42337572283488001 ) ) ;
#14656=CARTESIAN_POINT ( 'NONE',  ( 112.4559014775786778, -0.1624402480850797581, -16.17319339645315424 ) ) ;
#14660=CARTESIAN_POINT ( 'NONE',  ( 118.5256548109119876, -8.899110576539710493, -16.42337572283490132 ) ) ;
#14661=CARTESIAN_POINT ( 'NONE',  ( 118.7525614775786380, -1.833838273342659253, -17.42832698103878286 ) ) ;
#14669=CARTESIAN_POINT ( 'NONE',  ( 112.5126281442453120, -10.30919188438810075, -12.61870101168855918 ) ) ;
#14671=CARTESIAN_POINT ( 'NONE',  ( 125.0492214775786266, -3.505236298600246325, -18.68346056562440793 ) ) ;
#14672=CARTESIAN_POINT ( 'NONE',  ( 118.0151148109119816, 0.4262465694468514643, -12.03445270309931736 ) ) ;
#14675=CARTESIAN_POINT ( 'NONE',  ( 117.9583881442453048, 0.1319031606808879209, -14.10382304977623669 ) ) ;
#14677=CARTESIAN_POINT ( 'NONE',  ( 125.1653261673649524, -1.290981801452376843, -16.90223159988300594 ) ) ;
#14679=CARTESIAN_POINT ( 'NONE',  ( 116.4267681442453153, -3.383040157471821630, -19.15922257007629170 ) ) ;
#14681=CARTESIAN_POINT ( 'NONE',  ( 118.9227414775786400, -10.63000616557722466, -14.87417383870573495 ) ) ;
#14682=CARTESIAN_POINT ( 'NONE',  ( 113.8280291406318838, 0.3208234527006404435, -15.99825685930877661 ) ) ;
#14684=CARTESIAN_POINT ( 'NONE',  ( 114.8384214775786489, 0.9020085738987339008, -11.91225656197089222 ) ) ;
#14685=CARTESIAN_POINT ( 'NONE',  ( 112.6828081442453282, -7.893985811506177619, -18.51759400769804742 ) ) ;
#14690=ORIENTED_EDGE ( 'NONE', *, *, #31421, .F. ) ;
#14694=CARTESIAN_POINT ( 'NONE',  ( 114.9518748109119883, -7.643976991954077427, -18.09477374809248928 ) ) ;
#14699=CARTESIAN_POINT ( 'NONE',  ( 114.4980614775786734, -2.084020599724406786, -8.691656652584148546 ) ) ;
#14700=CARTESIAN_POINT ( 'NONE',  ( 136.2937225531903778, 0.9357610074967241953, -12.72675860691893490 ) ) ;
#14701=CARTESIAN_POINT ( 'NONE',  ( 123.6310548109119765, -5.638512984488999180, -18.83840828888717311 ) ) ;
#14702=CARTESIAN_POINT ( 'NONE',  ( 120.9081748109119872, -5.638512984488999180, -18.83840828888717311 ) ) ;
#14704=CARTESIAN_POINT ( 'NONE',  ( 115.5191414775786569, -6.222761293078241884, -8.102969835052219238 ) ) ;
#14707=CARTESIAN_POINT ( 'NONE',  ( 117.7882081442453170, -6.344957434206665248, -7.627207830600338134 ) ) ;
#14708=CARTESIAN_POINT ( 'NONE',  ( 120.0005481442453146, -4.153390946401325223, -8.397313243818185668 ) ) ;
#14711=CARTESIAN_POINT ( 'NONE',  ( 122.2128881442453263, -7.643976991954077427, -18.09477374809248928 ) ) ;
#14714=CARTESIAN_POINT ( 'NONE',  ( 119.9438214775786378, -7.893985811506177619, -18.51759400769804742 ) ) ;
#14720=CARTESIAN_POINT ( 'NONE',  ( 113.5904348109119866, -7.893985811506177619, -18.51759400769804742 ) ) ;
#14722=CARTESIAN_POINT ( 'NONE',  ( 116.9373081442452929, -1.833838273342659253, -17.42832698103878286 ) ) ;
#14724=DIRECTION ( 'NONE',  ( 1.000000000000000000, 0.000000000000000000, 0.000000000000000000 ) ) ;
#14726=CARTESIAN_POINT ( 'NONE',  ( 113.3635281442453504, -0.1624402480850797581, -16.17319339645315424 ) ) ;
#14732=CARTESIAN_POINT ( 'NONE',  ( 119.8870948109119752, -9.261995988541697145, -16.69588392320189030 ) ) ;
#14733=CARTESIAN_POINT ( 'NONE',  ( 119.3198281442452924, -9.859900752359374465, -12.68260735090039404 ) ) ;
#14734=CARTESIAN_POINT ( 'NONE',  ( 111.2646414775786496, -8.899110576539710493, -16.42337572283490132 ) ) ;
#14736=CARTESIAN_POINT ( 'NONE',  ( 136.9012041053403834, -7.147266434572221883, -8.356081441750150773 ) ) ;
#14737=CARTESIAN_POINT ( 'NONE',  ( 124.1983214775786166, -8.166667518702819706, -8.995218007635861213 ) ) ;
#14739=CARTESIAN_POINT ( 'NONE',  ( 120.7379948109119709, 0.4262465694468514643, -12.03445270309931736 ) ) ;
#14741=CARTESIAN_POINT ( 'NONE',  ( 117.8449348109119938, -1.833838273342659253, -17.42832698103878286 ) ) ;
#14745=CARTESIAN_POINT ( 'NONE',  ( 120.1707281442453166, -9.565557343593413364, -10.61323700422348004 ) ) ;
#14746=CARTESIAN_POINT ( 'NONE',  ( 123.6877814775786533, -6.222761293078241884, -8.102969835052219238 ) ) ;
#14752=CARTESIAN_POINT ( 'NONE',  ( 117.6747548109119919, -1.834011780172310813, -8.268836392978581529 ) ) ;
#14753=CARTESIAN_POINT ( 'NONE',  ( 119.3198281442452924, 0.5811942927096110934, -14.16772938898807510 ) ) ;
#14755=CARTESIAN_POINT ( 'NONE',  ( 113.5904348109119866, -7.893985811506177619, -18.51759400769804742 ) ) ;
#14757=CARTESIAN_POINT ( 'NONE',  ( 113.2885155643466817, -1.244021962887382315, -16.96476564598603787 ) ) ;
#14758=CARTESIAN_POINT ( 'NONE',  ( 116.3700414775786527, -5.638512984488999180, -18.83840828888717311 ) ) ;
#14759=CARTESIAN_POINT ( 'NONE',  ( 120.9649014775786355, -6.222761293078241884, -8.102969835052219238 ) ) ;
#14762=CARTESIAN_POINT ( 'NONE',  ( 125.9001214775786224, -4.089484607189486809, -7.948022111789456723 ) ) ;
#14763=CARTESIAN_POINT ( 'NONE',  ( 121.5321681442453183, -9.988377603198976828, -10.36322818467138340 ) ) ;
#14766=MECHANICAL_DESIGN_GEOMETRIC_PRESENTATION_REPRESENTATION('',(#35147),#43897);
#14768=CARTESIAN_POINT ( 'NONE',  ( 115.5758681442453053, -7.894159318335828068, -9.358103419637847864 ) ) ;
#14772=CARTESIAN_POINT ( 'NONE',  ( 120.5678148109119832, -8.166667518702819706, -8.995218007635861213 ) ) ;
#14776=CARTESIAN_POINT ( 'NONE',  ( 121.9484597424434043, -0.9924539043446216624, -17.29976612834909133 ) ) ;
#14777=CARTESIAN_POINT ( 'NONE',  ( 117.4478481442453131, -9.565557343593413364, -10.61323700422348004 ) ) ;
#14779=CARTESIAN_POINT ( 'NONE',  ( 124.1049594150595823, -2.423081321603731908, -17.89265170041263175 ) ) ;
#14780=CARTESIAN_POINT ( 'NONE',  ( 119.9438214775786378, -2.084020599724406786, -8.691656652584148546 ) ) ;
#14783=CARTESIAN_POINT ( 'NONE',  ( 123.1205148109119563, -7.643976991954077427, -18.09477374809248928 ) ) ;
#14786=CARTESIAN_POINT ( 'NONE',  ( 119.8303681442453126, 0.4262465694468514643, -12.03445270309931736 ) ) ;
#14787=CARTESIAN_POINT ( 'NONE',  ( 114.8951481442453115, -0.4660016031367893996, -10.09054647747474043 ) ) ;
#14788=CARTESIAN_POINT ( 'NONE',  ( 119.8870948109119752, -9.261995988541697145, -16.69588392320189030 ) ) ;
#14789=CARTESIAN_POINT ( 'NONE',  ( 126.6942948109119840, -8.899110576539710493, -16.42337572283490132 ) ) ;
#14791=CARTESIAN_POINT ( 'NONE',  ( 122.0427081442452817, -9.859900752359378018, -12.68260735090039759 ) ) ;
#14793=CARTESIAN_POINT ( 'NONE',  ( 119.2631014775786298, 0.2603800115204892296, -16.42320221600525088 ) ) ;
#14799=CARTESIAN_POINT ( 'NONE',  ( 125.9568481442452850, -6.344957434206665248, -7.627207830600338134 ) ) ;
#14802=CARTESIAN_POINT ( 'NONE',  ( 123.3474214775786209, -0.1624402480850797581, -16.17319339645315424 ) ) ;
#14809=CARTESIAN_POINT ( 'NONE',  ( 114.5547881442453217, -5.638512984488999180, -18.83840828888717311 ) ) ;
#14810=CARTESIAN_POINT ( 'NONE',  ( 113.1933481442453058, -4.089484607189486809, -7.948022111789456723 ) ) ;
#14811=CARTESIAN_POINT ( 'NONE',  ( 125.6732148109119862, 0.5811942927096110934, -14.16772938898807510 ) ) ;
#14812=CARTESIAN_POINT ( 'NONE',  ( 119.3198281442452924, -9.859900752359374465, -12.68260735090039404 ) ) ;
#14813=CARTESIAN_POINT ( 'NONE',  ( 126.2597653975865200, -3.915316323808516685, -8.462872152827413785 ) ) ;
#14815=CARTESIAN_POINT ( 'NONE',  ( 124.1415948109119540, -6.344957434206665248, -7.627207830600338134 ) ) ;
#14816=CARTESIAN_POINT ( 'NONE',  ( 123.5743281442453139, -2.084020599724360601, -8.691656652584175191 ) ) ;
#14819=CARTESIAN_POINT ( 'NONE',  ( 112.5693548109119888, -10.63000616557722466, -14.87417383870573495 ) ) ;
#14823=ADVANCED_FACE ( 'NONE', ( #43130 ), #12725, .T. ) ;
#14824=CARTESIAN_POINT ( 'NONE',  ( 121.1350814775786233, 0.5811942927096110934, -14.16772938898807510 ) ) ;
#14829=CARTESIAN_POINT ( 'NONE',  ( 124.5386814775786206, -5.638512984488999180, -18.83840828888717311 ) ) ;
#14830=CARTESIAN_POINT ( 'NONE',  ( 127.7617783745703974, -4.238963850480659268, -19.13134216130518794 ) ) ;
#14831=CARTESIAN_POINT ( 'NONE',  ( 122.7234281442452755, -4.153390946401325223, -8.397313243818185668 ) ) ;
#14833=ORIENTED_EDGE ( 'NONE', *, *, #31713, .F. ) ;
#14834=CARTESIAN_POINT ( 'NONE',  ( 116.9373081442452929, -8.166667518702817929, -8.995218007635861213 ) ) ;
#14836=CARTESIAN_POINT ( 'NONE',  ( 120.5110881442453064, -6.344957434206645708, -7.627207830600334582 ) ) ;
#14837=CARTESIAN_POINT ( 'NONE',  ( 136.7741008876058402, -5.359462442573635244, -7.806884787152266192 ) ) ;
#14838=CARTESIAN_POINT ( 'NONE',  ( 111.9453614775786434, -7.894159318335828068, -9.358103419637847864 ) ) ;
#14841=CARTESIAN_POINT ( 'NONE',  ( 122.0427081442452817, 0.5811942927096110934, -14.16772938898807510 ) ) ;
#14842=CARTESIAN_POINT ( 'NONE',  ( 124.1415948109119540, -6.344957434206665248, -7.627207830600338134 ) ) ;
#14843=CARTESIAN_POINT ( 'NONE',  ( 122.7234281442452755, -4.153390946401325223, -8.397313243818185668 ) ) ;
#14845=CARTESIAN_POINT ( 'NONE',  ( 124.6521348109119884, -7.894159318335828068, -9.358103419637847864 ) ) ;
#14847=CARTESIAN_POINT ( 'NONE',  ( 121.3619881442452879, -4.089484607189486809, -7.948022111789456723 ) ) ;
#14856=CARTESIAN_POINT ( 'NONE',  ( 116.8805814775786445, -6.344957434206662583, -7.627207830600332805 ) ) ;
#14858=CARTESIAN_POINT ( 'NONE',  ( 111.9453614775786434, -7.894159318335828068, -9.358103419637847864 ) ) ;
#14862=CARTESIAN_POINT ( 'NONE',  ( 122.5532481442453019, 0.4262465694468476896, -12.03445270309931381 ) ) ;
#14864=CARTESIAN_POINT ( 'NONE',  ( 116.0296814775786345, -8.166667518702817929, -8.995218007635861213 ) ) ;
#14868=CARTESIAN_POINT ( 'NONE',  ( 126.2471382750679822, -7.710119271726137313, -9.264776471331988006 ) ) ;
#14869=CARTESIAN_POINT ( 'NONE',  ( 119.4332814775786318, -8.899110576539710493, -16.42337572283490132 ) ) ;
#14870=CARTESIAN_POINT ( 'NONE',  ( 117.1074881442453233, -10.63000616557722466, -14.87417383870573495 ) ) ;
#14872=CARTESIAN_POINT ( 'NONE',  ( 125.3895814775786448, -2.084020599724406786, -8.691656652584148546 ) ) ;
#14873=CARTESIAN_POINT ( 'NONE',  ( 118.9794681442453026, -0.8288870151387760510, -10.36305467784173118 ) ) ;
#14874=CARTESIAN_POINT ( 'NONE',  ( 115.2355081442453155, 0.1319031606808879209, -14.10382304977623669 ) ) ;
#14879=CARTESIAN_POINT ( 'NONE',  ( 116.5969481442453031, -9.859900752359374465, -12.68260735090039404 ) ) ;
#14882=CARTESIAN_POINT ( 'NONE',  ( 114.4980614775786592, -7.893985811506177619, -18.51759400769804742 ) ) ;
#14885=CARTESIAN_POINT ( 'NONE',  ( 114.2711548109119803, -0.1624402480850797581, -16.17319339645315424 ) ) ;
#14886=ORIENTED_EDGE ( 'NONE', *, *, #27820, .F. ) ;
#14887=EDGE_LOOP ( 'NONE', ( #20491, #23827, #27687, #34249 ) ) ;
#14888=CARTESIAN_POINT ( 'NONE',  ( 123.0070614775786169, -10.15424416112533912, -14.75197769757731336 ) ) ;
#14889=CARTESIAN_POINT ( 'NONE',  ( 116.3133148109120043, -2.084020599724406786, -8.691656652584148546 ) ) ;
#14892=ORIENTED_EDGE ( 'NONE', *, *, #31399, .F. ) ;
#14898=CARTESIAN_POINT ( 'NONE',  ( 112.9097148109120070, 0.2603800115204892296, -16.42320221600525088 ) ) ;
#14899=CARTESIAN_POINT ( 'NONE',  ( 122.7234281442452755, -4.153390946401325223, -8.397313243818185668 ) ) ;
#14902=CARTESIAN_POINT ( 'NONE',  ( 121.0783548109119749, -9.565557343593413364, -10.61323700422348004 ) ) ;
#14907=CARTESIAN_POINT ( 'NONE',  ( 114.5547881442453217, -5.638512984488999180, -18.83840828888717311 ) ) ;
#14908=ORIENTED_EDGE ( 'NONE', *, *, #40368, .T. ) ;
#14909=CARTESIAN_POINT ( 'NONE',  ( 119.0361948109119652, -7.893985811506177619, -18.51759400769804742 ) ) ;
#14912=CARTESIAN_POINT ( 'NONE',  ( 116.8805814775786445, -6.344957434206662583, -7.627207830600332805 ) ) ;
#14913=CARTESIAN_POINT ( 'NONE',  ( 117.9583881442453048, -10.30919188438810075, -12.61870101168855918 ) ) ;
#14921=CARTESIAN_POINT ( 'NONE',  ( 120.3409081442453044, -8.899110576539710493, -16.42337572283490132 ) ) ;
#14922=DIRECTION ( 'NONE',  ( -0.7071067811865480168, 0.5654279342907823080, 0.4246071727180995570 ) ) ;
#14925=CARTESIAN_POINT ( 'NONE',  ( 126.6211808763662248, -4.885409866343571217, -8.191703873976955208 ) ) ;
#14926=CARTESIAN_POINT ( 'NONE',  ( 113.7038881442453402, -6.222761293078241884, -8.102969835052219238 ) ) ;
#14928=CARTESIAN_POINT ( 'NONE',  ( 124.0848681442452772, -4.089484607189486809, -7.948022111789456723 ) ) ;
#14929=CARTESIAN_POINT ( 'NONE',  ( 120.3976348109119812, -1.834011780172310813, -8.268836392978581529 ) ) ;
#14931=CARTESIAN_POINT ( 'NONE',  ( 118.4122014775786340, -9.859900752359374465, -12.68260735090039404 ) ) ;
#14932=CARTESIAN_POINT ( 'NONE',  ( 126.1837548109119211, -10.63000616557722466, -14.87417383870573495 ) ) ;
#14933=CARTESIAN_POINT ( 'NONE',  ( 116.5402214775786405, 0.2603800115204892296, -16.42320221600525088 ) ) ;
#14934=CARTESIAN_POINT ( 'NONE',  ( 120.2841814775786276, -10.15424416112533912, -14.75197769757731336 ) ) ;
#14936=CARTESIAN_POINT ( 'NONE',  ( 116.5026997424434114, -0.9924539043446216624, -17.29976612834909133 ) ) ;
#14938=CARTESIAN_POINT ( 'NONE',  ( 118.7525614775786380, -8.166667518702819706, -8.995218007635861213 ) ) ;
#14939=CARTESIAN_POINT ( 'NONE',  ( 135.3184548109119874, -4.863998795839242995, -13.39321520033831447 ) ) ;
#14945=CARTESIAN_POINT ( 'NONE',  ( 117.3911214775786505, -1.561330072975668504, -17.79121239304076951 ) ) ;
#14947=CARTESIAN_POINT ( 'NONE',  ( 117.3911214775786505, -7.894159318335828068, -9.358103419637847864 ) ) ;
#14948=CARTESIAN_POINT ( 'NONE',  ( 112.1234697116520920, -8.918491192341182483, -16.31914947962552631 ) ) ;
#14951=CARTESIAN_POINT ( 'NONE',  ( 113.3068014775786594, -1.833838273342658809, -17.42832698103878286 ) ) ;
#14952=DIRECTION ( 'NONE',  ( 1.000000000000000000, 0.000000000000000000, 0.000000000000000000 ) ) ;
#14955=CARTESIAN_POINT ( 'NONE',  ( 117.5045748109119756, 0.5811942927096110934, -14.16772938898807510 ) ) ;
#14956=CARTESIAN_POINT ( 'NONE',  ( 117.3911214775786505, -7.894159318335828068, -9.358103419637847864 ) ) ;
#14957=CARTESIAN_POINT ( 'NONE',  ( 111.9453614775786434, -7.894159318335828068, -9.358103419637847864 ) ) ;
#14960=CARTESIAN_POINT ( 'NONE',  ( 121.9292548109119849, -1.561330072975668948, -17.79121239304076951 ) ) ;
#14962=CARTESIAN_POINT ( 'NONE',  ( 119.5467348109119712, -5.574606645277164318, -18.38911715685844683 ) ) ;
#14963=CARTESIAN_POINT ( 'NONE',  ( 115.6893214775786447, -9.859900752359374465, -12.68260735090039404 ) ) ;
#14967=CARTESIAN_POINT ( 'NONE',  ( 123.3474214775786209, -0.1624402480850797581, -16.17319339645315424 ) ) ;
#14968=CARTESIAN_POINT ( 'NONE',  ( 122.5532481442453019, 0.4262465694468514643, -12.03445270309931736 ) ) ;
#14969=CARTESIAN_POINT ( 'NONE',  ( 114.9518748109119883, -7.643976991954099631, -18.09477374809247152 ) ) ;
#14975=CARTESIAN_POINT ( 'NONE',  ( 116.3700414775786527, -5.638512984488999180, -18.83840828888717311 ) ) ;
#14976=CARTESIAN_POINT ( 'NONE',  ( 118.9794681442453026, -9.261995988541697145, -16.69588392320189030 ) ) ;
#14978=CARTESIAN_POINT ( 'NONE',  ( 112.1155414775786454, 0.9020085738987339008, -11.91225656197089222 ) ) ;
#14980=CARTESIAN_POINT ( 'NONE',  ( 117.1754969549021723, -1.135392229370316031, -17.10942237759952533 ) ) ;
#14982=CARTESIAN_POINT ( 'NONE',  ( 116.9373081442452929, -8.166667518702817929, -8.995218007635861213 ) ) ;
#14983=CARTESIAN_POINT ( 'NONE',  ( 122.4965214775786251, 0.1319031606808879209, -14.10382304977623669 ) ) ;
#14984=CARTESIAN_POINT ( 'NONE',  ( 124.2550481442452792, -9.988377603198980381, -10.36322818467138518 ) ) ;
#14985=CARTESIAN_POINT ( 'NONE',  ( 121.3052614775786111, -1.834011780172310813, -8.268836392978581529 ) ) ;
#14988=CARTESIAN_POINT ( 'NONE',  ( 117.9583881442453048, 0.1319031606808879209, -14.10382304977623669 ) ) ;
#14992=EDGE_CURVE ( 'NONE', #40981, #29459, #15112, .T. ) ;
#14995=CARTESIAN_POINT ( 'NONE',  ( 120.4543614775786295, -4.089484607189486809, -7.948022111789456723 ) ) ;
#14996=EDGE_LOOP ( 'NONE', ( #888, #3637, #10956, #43405 ) ) ;
#15000=CARTESIAN_POINT ( 'NONE',  ( 115.8027748109119841, -8.899110576539710493, -16.42337572283490132 ) ) ;
#15003=CARTESIAN_POINT ( 'NONE',  ( 123.4608748109119745, 0.4262465694468514643, -12.03445270309931736 ) ) ;
#15004=CARTESIAN_POINT ( 'NONE',  ( 121.7023481442452777, -9.261995988541729119, -16.69588392320184767 ) ) ;
#15005=AXIS2_PLACEMENT_3D ( 'NONE', #33945, #5294, #29690 ) ;
#15007=CARTESIAN_POINT ( 'NONE',  ( 121.8725281442453223, -6.222761293078241884, -8.102969835052219238 ) ) ;
#15009=CARTESIAN_POINT ( 'NONE',  ( 124.2550481442452792, -0.1624402480850797581, -16.17319339645315424 ) ) ;
#15011=CARTESIAN_POINT ( 'NONE',  ( 112.7395348109119766, -5.638512984488999180, -18.83840828888717311 ) ) ;
#15012=CARTESIAN_POINT ( 'NONE',  ( 117.8449348109119938, -8.166667518702817929, -8.995218007635861213 ) ) ;
#15013=CARTESIAN_POINT ( 'NONE',  ( 126.0703014775786102, -0.1624402480850797581, -16.17319339645315424 ) ) ;
#15017=CARTESIAN_POINT ( 'NONE',  ( 119.6034614775786196, -3.505236298600246325, -18.68346056562440793 ) ) ;
#15019=CARTESIAN_POINT ( 'NONE',  ( 118.8660148109119774, -10.30919188438810075, -12.61870101168855918 ) ) ;
#15027=CARTESIAN_POINT ( 'NONE',  ( 121.7023481442452919, -0.8288870151387760510, -10.36305467784173118 ) ) ;
#15028=LINE ( 'NONE', #4531, #25004 ) ;
#15030=CARTESIAN_POINT ( 'NONE',  ( 125.5030348109119558, -3.383040157471821630, -19.15922257007629170 ) ) ;
#15034=CARTESIAN_POINT ( 'NONE',  ( 115.2355081442453155, -10.30919188438810075, -12.61870101168855918 ) ) ;
#15036=CARTESIAN_POINT ( 'NONE',  ( 120.1140014775786398, -7.894159318335828068, -9.358103419637847864 ) ) ;
#15037=CARTESIAN_POINT ( 'NONE',  ( 112.5693548109119888, 0.4262465694468514643, -12.03445270309931736 ) ) ;
#15046=CARTESIAN_POINT ( 'NONE',  ( 121.3052614775786111, -1.834011780172310813, -8.268836392978581529 ) ) ;
#15050=CARTESIAN_POINT ( 'NONE',  ( 121.2372526669217478, -2.334846009198419559, -18.01015021110789505 ) ) ;
#15051=CARTESIAN_POINT ( 'NONE',  ( 112.3424481442453384, -3.505236298600246325, -18.68346056562440793 ) ) ;
#15052=CARTESIAN_POINT ( 'NONE',  ( 127.0298367773230126, -4.565043486894647451, -18.79063384679673376 ) ) ;
#15054=CARTESIAN_POINT ( 'NONE',  ( 124.1983214775786166, -1.833838273342659697, -17.42832698103878286 ) ) ;
#15056=CARTESIAN_POINT ( 'NONE',  ( 118.2420214775786320, -3.383040157471821630, -19.15922257007629170 ) ) ;
#15058=LINE ( 'NONE', #42431, #19275 ) ;
#15059=CARTESIAN_POINT ( 'NONE',  ( 112.1155414775786454, -10.15424416112533912, -14.75197769757731336 ) ) ;
#15063=CARTESIAN_POINT ( 'NONE',  ( 112.6260814775786514, -0.8288870151387760510, -10.36305467784173118 ) ) ;
#15064=CARTESIAN_POINT ( 'NONE',  ( 126.3539348109119800, -4.153390946401325223, -8.397313243818185668 ) ) ;
#15066=CARTESIAN_POINT ( 'NONE',  ( 124.8790414775786246, -8.899110576539710493, -16.42337572283490132 ) ) ;
#15068=CARTESIAN_POINT ( 'NONE',  ( 120.6245414775786458, -9.988377603198976828, -10.36322818467138340 ) ) ;
#15071=CARTESIAN_POINT ( 'NONE',  ( 126.9115046738447887, -8.477094959678533215, -17.33456804528672635 ) ) ;
#15075=CARTESIAN_POINT ( 'NONE',  ( 125.3895814775786590, -2.084020599725330491, -8.691656652583604981 ) ) ;
#15076=CARTESIAN_POINT ( 'NONE',  ( 114.1577014775786552, -6.344957434206662583, -7.627207830600332805 ) ) ;
#15078=CARTESIAN_POINT ( 'NONE',  ( 112.9664414775786412, -9.859900752359374465, -12.68260735090039404 ) ) ;
#15082=CARTESIAN_POINT ( 'NONE',  ( 112.5693548109119888, 0.4262465694468514643, -12.03445270309931736 ) ) ;
#15083=CARTESIAN_POINT ( 'NONE',  ( 123.2697102440515238, -2.467220198592778413, -17.83387418641524391 ) ) ;
#15085=CARTESIAN_POINT ( 'NONE',  ( 115.1220548109119761, -8.166667518702817929, -8.995218007635861213 ) ) ;
#15088=EDGE_LOOP ( 'NONE', ( #5221, #11208, #30982, #7103 ) ) ;
#15090=CARTESIAN_POINT ( 'NONE',  ( 120.4543614775786295, -5.574606645277164318, -18.38911715685844683 ) ) ;
#15091=CARTESIAN_POINT ( 'NONE',  ( 116.8238548109119819, -4.089484607189486809, -7.948022111789456723 ) ) ;
#15093=CARTESIAN_POINT ( 'NONE',  ( 111.8319081442453182, -5.638512984488999180, -18.83840828888717311 ) ) ;
#15094=CARTESIAN_POINT ( 'NONE',  ( 125.3328548109119964, -0.8288870151387760510, -10.36305467784173118 ) ) ;
#15096=CARTESIAN_POINT ( 'NONE',  ( 123.5743281442453139, -2.084020599724406786, -8.691656652584148546 ) ) ;
#15097=CARTESIAN_POINT ( 'NONE',  ( 115.0086014775786509, -5.574606645277164318, -18.38911715685844683 ) ) ;
#15101=CARTESIAN_POINT ( 'NONE',  ( 118.1852948109119836, -4.153390946401325223, -8.397313243818185668 ) ) ;
#15102=VERTEX_POINT ( 'NONE', #20988 ) ;
#15104=CARTESIAN_POINT ( 'NONE',  ( 113.4769814775786330, -10.63000616557722466, -14.87417383870573495 ) ) ;
#15105=CIRCLE ( 'NONE', #20937, 1.499999999999999334 ) ;
#15107=CARTESIAN_POINT ( 'NONE',  ( 118.7735460444391862, -1.267766418764730840, -16.93314635290706605 ) ) ;
#15110=CARTESIAN_POINT ( 'NONE',  ( 122.4397948109119767, -0.1624402480850797581, -16.17319339645315424 ) ) ;
#15111=CARTESIAN_POINT ( 'NONE',  ( 116.7104014775786425, -8.899110576539710493, -16.42337572283490132 ) ) ;
#15112=( BOUNDED_CURVE ( )  B_SPLINE_CURVE ( 2, ( #33299, #19636, #44048, #37412, #30133, #20103, #9379, #33520, #2300, #16230, #12812, #23288, #37172, #26932, #33988, #2528, #3649 ),
 .UNSPECIFIED., .F., .T. ) 
 B_SPLINE_CURVE_WITH_KNOTS ( ( 3, 2, 2, 2, 2, 2, 2, 2, 3 ),
 ( 0.5170046674808920217, 0.5234375000000000000, 0.5312500000000000000, 0.5390625000000000000, 0.5468750000000000000, 0.5546875000000000000, 0.5625000000000000000, 0.5703125000000000000, 0.5767453325190590174 ),
 .UNSPECIFIED. ) 
 CURVE ( )  GEOMETRIC_REPRESENTATION_ITEM ( )  RATIONAL_B_SPLINE_CURVE ( ( 0.9778625265006459788, 0.9373222120152210346, 1.000000000000000000, 0.9238795325112869605, 1.000000000000000000, 0.9238795325112869605, 1.000000000000000000, 0.9238795325112869605, 1.000000000000000000, 0.9238795325112869605, 1.000000000000000000, 0.9238795325112869605, 1.000000000000000000, 0.9238795325112869605, 1.000000000000000000, 0.9373222120157009840, 0.9778625265000250311 ) ) 
 REPRESENTATION_ITEM ( '' )  );
#15121=CARTESIAN_POINT ( 'NONE',  ( 114.2144281442453178, -8.166667518702817929, -8.995218007635859436 ) ) ;
#15122=CARTESIAN_POINT ( 'NONE',  ( 125.2194014775786286, 0.1319031606808879209, -14.10382304977623669 ) ) ;
#15123=CARTESIAN_POINT ( 'NONE',  ( 121.1350814775786233, -9.859900752359378018, -12.68260735090039759 ) ) ;
#15126=CARTESIAN_POINT ( 'NONE',  ( 119.5467348109119712, -5.574606645277164318, -18.38911715685844683 ) ) ;
#15131=CARTESIAN_POINT ( 'NONE',  ( 119.4900081442453086, -1.834011780172310813, -8.268836392978581529 ) ) ;
#15133=CARTESIAN_POINT ( 'NONE',  ( 115.5758681442453053, -1.561330072975668060, -17.79121239304076951 ) ) ;
#15134=CARTESIAN_POINT ( 'NONE',  ( 115.4100314811013561, -2.280480477428491248, -18.08254604495227724 ) ) ;
#15136=CARTESIAN_POINT ( 'NONE',  ( 117.5045748109119756, 0.5811942927096110934, -14.16772938898807510 ) ) ;
#15137=CARTESIAN_POINT ( 'NONE',  ( 116.3133148109119759, -7.893985811506177619, -18.51759400769804742 ) ) ;
#15138=CARTESIAN_POINT ( 'NONE',  ( 126.2184548109108135, -9.830300164702144627, -12.80248346511802104 ) ) ;
#15142=CARTESIAN_POINT ( 'NONE',  ( 112.1218600025837304, -2.311015703046748193, -18.04188382666269064 ) ) ;
#15144=CARTESIAN_POINT ( 'NONE',  ( 119.3765548109119834, -10.15424416112533912, -14.75197769757731336 ) ) ;
#15147=CARTESIAN_POINT ( 'NONE',  ( 112.7962614775786676, -6.222761293078241884, -8.102969835052219238 ) ) ;
#15148=CARTESIAN_POINT ( 'NONE',  ( 115.0086014775786509, -5.574606645277164318, -18.38911715685844683 ) ) ;
#15150=CARTESIAN_POINT ( 'NONE',  ( 124.1983214775786166, -8.166667518702819706, -8.995218007635861213 ) ) ;
#15151=CARTESIAN_POINT ( 'NONE',  ( 121.1918081442452859, 0.9020085738987339008, -11.91225656197089222 ) ) ;
#15153=CARTESIAN_POINT ( 'NONE',  ( 119.6034614775786196, -3.505236298600246325, -18.68346056562440793 ) ) ;
#15154=CARTESIAN_POINT ( 'NONE',  ( 126.2404814775786264, -9.261995988541697145, -16.69588392320189030 ) ) ;
#15155=CARTESIAN_POINT ( 'NONE',  ( 122.2128881442453263, -1.834011780172310813, -8.268836392978581529 ) ) ;
#15157=CARTESIAN_POINT ( 'NONE',  ( 119.6034614775786196, -3.505236298600246325, -18.68346056562440793 ) ) ;
#15159=CARTESIAN_POINT ( 'NONE',  ( 116.0506660444391969, -1.267766418764730840, -16.93314635290706605 ) ) ;
#15160=CARTESIAN_POINT ( 'NONE',  ( 121.5888948109119809, -10.30919188438810075, -12.61870101168855918 ) ) ;
#15161=CARTESIAN_POINT ( 'NONE',  ( 116.9163235773848726, -2.467220198592778413, -17.83387418641524391 ) ) ;
#15163=CARTESIAN_POINT ( 'NONE',  ( 126.4144288373559846, 0.2303623831909507591, -13.58551579586932156 ) ) ;
#15165=CARTESIAN_POINT ( 'NONE',  ( 116.7104014775786425, -0.4660016031367893996, -10.09054647747474043 ) ) ;
#15167=CARTESIAN_POINT ( 'NONE',  ( 117.1642148109119859, -0.8288870151387760510, -10.36305467784173118 ) ) ;
#15168=CARTESIAN_POINT ( 'NONE',  ( 124.8790414775786246, -0.4660016031367893996, -10.09054647747474043 ) ) ;
#15169=CARTESIAN_POINT ( 'NONE',  ( 126.2184548109105435, -0.8658195297460520301, -10.39078908864422246 ) ) ;
#15172=CARTESIAN_POINT ( 'NONE',  ( 112.8529881442453302, -7.894159318335828068, -9.358103419637847864 ) ) ;
#15176=CARTESIAN_POINT ( 'NONE',  ( 118.1852948109119836, -5.638512984488999180, -18.83840828888717311 ) ) ;
#15180=CARTESIAN_POINT ( 'NONE',  ( 122.7801548109119665, -6.222761293078241884, -8.102969835052219238 ) ) ;
#15183=CARTESIAN_POINT ( 'NONE',  ( 126.2184548109119788, 0.08617673920515746266, -14.09731900820182915 ) ) ;
#15185=CARTESIAN_POINT ( 'NONE',  ( 120.6245414775786458, -0.1624402480850797581, -16.17319339645315424 ) ) ;
#15186=CARTESIAN_POINT ( 'NONE',  ( 120.5110881442453206, -3.505236298600246325, -18.68346056562440793 ) ) ;
#15187=CARTESIAN_POINT ( 'NONE',  ( 115.6325948109119821, -9.565557343593413364, -10.61323700422348004 ) ) ;
#15190=CARTESIAN_POINT ( 'NONE',  ( 122.9503348109119827, -9.859900752359378018, -12.68260735090039759 ) ) ;
#15191=CARTESIAN_POINT ( 'NONE',  ( 124.4819548109119722, -2.084020599724406786, -8.691656652584148546 ) ) ;
#15193=FACE_OUTER_BOUND ( 'NONE', #8017, .T. ) ;
#15199=CARTESIAN_POINT ( 'NONE',  ( 117.3911214775786505, -1.561330072975668504, -17.79121239304076951 ) ) ;
#15200=CARTESIAN_POINT ( 'NONE',  ( 118.6391081442452986, -4.089484607189486809, -7.948022111789456723 ) ) ;
#15206=CARTESIAN_POINT ( 'NONE',  ( 118.1852948109119836, -5.638512984488999180, -18.83840828888717311 ) ) ;
#15207=CARTESIAN_POINT ( 'NONE',  ( 122.6099748109119929, -0.8288870151387760510, -10.36305467784173118 ) ) ;
#15209=CARTESIAN_POINT ( 'NONE',  ( 115.1220548109119761, -1.833838273342658809, -17.42832698103878286 ) ) ;
#15210=CARTESIAN_POINT ( 'NONE',  ( 120.0572748109119772, -3.383040157471821630, -19.15922257007629170 ) ) ;
#15212=CARTESIAN_POINT ( 'NONE',  ( 114.8384214775786489, -10.15424416112533912, -14.75197769757731336 ) ) ;
#15217=CARTESIAN_POINT ( 'NONE',  ( 117.8449348109119938, -8.166667518702817929, -8.995218007635861213 ) ) ;
#15222=CARTESIAN_POINT ( 'NONE',  ( 114.1577014775786552, -3.505236298600246325, -18.68346056562440793 ) ) ;
#15223=CARTESIAN_POINT ( 'NONE',  ( 112.1155414775786596, 0.9020085738987339008, -11.91225656197089222 ) ) ;
#15225=CARTESIAN_POINT ( 'NONE',  ( 123.6877814775786533, -6.222761293078241884, -8.102969835052219238 ) ) ;
#15229=CARTESIAN_POINT ( 'NONE',  ( 124.5954081442453116, -6.222761293078241884, -8.102969835052219238 ) ) ;
#15230=CARTESIAN_POINT ( 'NONE',  ( 113.4769814775786330, -10.63000616557722466, -14.87417383870573495 ) ) ;
#15231=CARTESIAN_POINT ( 'NONE',  ( 118.1285681442453068, -7.893985811506177619, -18.51759400769804742 ) ) ;
#15232=CARTESIAN_POINT ( 'NONE',  ( 112.9097148109120070, 0.2603800115204892296, -16.42320221600525088 ) ) ;
#15234=CARTESIAN_POINT ( 'NONE',  ( 120.2841814775786276, -10.15424416112533912, -14.75197769757731336 ) ) ;
#15236=CARTESIAN_POINT ( 'NONE',  ( 120.0005481442453146, -5.638512984488999180, -18.83840828888717311 ) ) ;
#15241=CARTESIAN_POINT ( 'NONE',  ( 113.9307948109119764, -10.15424416112533912, -14.75197769757731336 ) ) ;
#15245=VECTOR ( 'NONE', #41839, 1000.000000000000000 ) ;
#15246=CARTESIAN_POINT ( 'NONE',  ( 121.9292548109119849, -7.894159318335828068, -9.358103419637847864 ) ) ;
#15253=CARTESIAN_POINT ( 'NONE',  ( 116.1431348109119881, -10.30919188438810075, -12.61870101168855918 ) ) ;
#15255=CARTESIAN_POINT ( 'NONE',  ( 119.2631014775786298, -9.565557343593413364, -10.61323700422348004 ) ) ;
#15256=CARTESIAN_POINT ( 'NONE',  ( 126.3230600034167850, -3.769654384711456085, -8.460624569279659113 ) ) ;
#15261=DIRECTION ( 'NONE',  ( -1.000000000000000000, 0.000000000000000000, 0.000000000000000000 ) ) ;
#15262=CARTESIAN_POINT ( 'NONE',  ( 119.0929214775786278, -5.638512984488999180, -18.83840828888717311 ) ) ;
#15264=EDGE_CURVE ( 'NONE', #42627, #21157, #13710, .T. ) ;
#15265=CARTESIAN_POINT ( 'NONE',  ( 114.9518748109119883, -1.834011780172310813, -8.268836392978581529 ) ) ;
#15268=CARTESIAN_POINT ( 'NONE',  ( 125.5597614775786326, -1.561330072975669392, -17.79121239304076951 ) ) ;
#15270=CARTESIAN_POINT ( 'NONE',  ( 124.8223148109119762, -10.15424416112533912, -14.75197769757731336 ) ) ;
#15272=CARTESIAN_POINT ( 'NONE',  ( 116.7104014775786425, -0.4660016031367893996, -10.09054647747474043 ) ) ;
#15277=CARTESIAN_POINT ( 'NONE',  ( 136.0320772899192718, -5.573080998308148182, -7.524869074880469633 ) ) ;
#15278=CARTESIAN_POINT ( 'NONE',  ( 112.6260814775786514, -0.8288870151387760510, -10.36305467784173118 ) ) ;
#15282=CARTESIAN_POINT ( 'NONE',  ( 112.3991748109119868, -1.833838273342658809, -17.42832698103878286 ) ) ;
#15284=CARTESIAN_POINT ( 'NONE',  ( 125.9001214775786224, -5.574606645277164318, -18.38911715685844683 ) ) ;
#15286=CARTESIAN_POINT ( 'NONE',  ( 124.2550481442452792, -0.1624402480850797581, -16.17319339645315424 ) ) ;
#15288=CARTESIAN_POINT ( 'NONE',  ( 120.1707281442453166, 0.2603800115204892296, -16.42320221600525088 ) ) ;
#15290=CARTESIAN_POINT ( 'NONE',  ( 126.8137406968053114, -8.488853573463353896, -17.25709863353327833 ) ) ;
#15295=CARTESIAN_POINT ( 'NONE',  ( 125.6059481442453318, -7.866424907534184996, -9.395035934245763443 ) ) ;
#15296=CARTESIAN_POINT ( 'NONE',  ( 116.0296814775786345, -8.166667518702817929, -8.995218007635861213 ) ) ;
#15298=CARTESIAN_POINT ( 'NONE',  ( 116.8805814775786445, -3.505236298600246325, -18.68346056562440793 ) ) ;
#15301=CARTESIAN_POINT ( 'NONE',  ( 111.2646643879000834, -8.898622535612265239, -16.42406377531225914 ) ) ;
#15304=CARTESIAN_POINT ( 'NONE',  ( 117.3911214775786505, -1.561330072975668504, -17.79121239304076951 ) ) ;
#15310=CARTESIAN_POINT ( 'NONE',  ( 118.2987481442453088, -7.894159318335828068, -9.358103419637847864 ) ) ;
#15311=CARTESIAN_POINT ( 'NONE',  ( 115.8595014775786609, -1.834011780172310813, -8.268836392978581529 ) ) ;
#15314=CARTESIAN_POINT ( 'NONE',  ( 123.4041481442452834, 0.1319031606808879209, -14.10382304977623669 ) ) ;
#15315=CARTESIAN_POINT ( 'NONE',  ( 125.1059481442452750, -1.833838273342660141, -17.42832698103878286 ) ) ;
#15316=CARTESIAN_POINT ( 'NONE',  ( 116.7104014775786425, -8.899110576539710493, -16.42337572283490132 ) ) ;
#15321=CARTESIAN_POINT ( 'NONE',  ( 117.5045748109119756, -9.859900752359374465, -12.68260735090039404 ) ) ;
#15326=CARTESIAN_POINT ( 'NONE',  ( 114.6115148109119986, -3.383040157471821630, -19.15922257007629170 ) ) ;
#15328=CARTESIAN_POINT ( 'NONE',  ( 113.9307948109119764, -10.15424416112533912, -14.75197769757731336 ) ) ;
#15330=ORIENTED_EDGE ( 'NONE', *, *, #12505, .T. ) ;
#15331=CARTESIAN_POINT ( 'NONE',  ( 121.9292548109119849, -7.894159318335828068, -9.358103419637847864 ) ) ;
#15332=CARTESIAN_POINT ( 'NONE',  ( 117.4478481442453131, -9.565557343593413364, -10.61323700422348004 ) ) ;
#15335=CARTESIAN_POINT ( 'NONE',  ( 116.3700414775786527, -4.153390946401313677, -8.397313243818183892 ) ) ;
#15337=DIRECTION ( 'NONE',  ( 1.000000000000000000, 0.000000000000000000, 0.000000000000000000 ) ) ;
#15341=CARTESIAN_POINT ( 'NONE',  ( 117.2209414775786485, -7.893985811506177619, -18.51759400769804742 ) ) ;
#15342=CARTESIAN_POINT ( 'NONE',  ( 125.6164881442453094, -9.565557343593413364, -10.61323700422348004 ) ) ;
#15343=CARTESIAN_POINT ( 'NONE',  ( 114.7816948109119863, -9.859900752359374465, -12.68260735090039404 ) ) ;
#15344=CARTESIAN_POINT ( 'NONE',  ( 122.9503348109119827, -9.859900752359378018, -12.68260735090039759 ) ) ;
#15345=CARTESIAN_POINT ( 'NONE',  ( 112.4201593777725208, -1.267766418764741276, -16.93314635290707315 ) ) ;
#15347=CARTESIAN_POINT ( 'NONE',  ( 119.3198281442452924, -9.859900752359374465, -12.68260735090039404 ) ) ;
#15349=CARTESIAN_POINT ( 'NONE',  ( 124.1983214775786166, -1.833838273342659697, -17.42832698103878286 ) ) ;
#15355=CARTESIAN_POINT ( 'NONE',  ( 117.7882081442453170, -6.344957434206665248, -7.627207830600338134 ) ) ;
#15358=CARTESIAN_POINT ( 'NONE',  ( 120.0572748109119772, -3.383040157471821630, -19.15922257007629170 ) ) ;
#15361=CARTESIAN_POINT ( 'NONE',  ( 114.7816948109119863, 0.5811942927096154232, -14.16772938898807155 ) ) ;
#15362=CARTESIAN_POINT ( 'NONE',  ( 119.2063748109119814, -1.561330072975668504, -17.79121239304076951 ) ) ;
#15366=ORIENTED_EDGE ( 'NONE', *, *, #797, .F. ) ;
#15369=CARTESIAN_POINT ( 'NONE',  ( 122.0994348109119443, -10.15424416112533912, -14.75197769757731336 ) ) ;
#15372=CARTESIAN_POINT ( 'NONE',  ( 113.6471614775786492, -4.153390946401321671, -8.397313243818183892 ) ) ;
#15374=CARTESIAN_POINT ( 'NONE',  ( 126.1837548109119211, -10.63000616557722466, -14.87417383870573495 ) ) ;
#15375=CARTESIAN_POINT ( 'NONE',  ( 119.9438214775786378, -7.893985811506177619, -18.51759400769804742 ) ) ;
#15378=CARTESIAN_POINT ( 'NONE',  ( 117.9016614775786280, -0.1624402480850797581, -16.17319339645315424 ) ) ;
#15379=CARTESIAN_POINT ( 'NONE',  ( 116.3133148109119759, -7.893985811506177619, -18.51759400769804742 ) ) ;
#15381=CARTESIAN_POINT ( 'NONE',  ( 122.8368814775786291, -1.561330072975668948, -17.79121239304076951 ) ) ;
#15382=CARTESIAN_POINT ( 'NONE',  ( 119.2631014775786298, -9.565557343593413364, -10.61323700422348004 ) ) ;
#15384=CARTESIAN_POINT ( 'NONE',  ( 123.6877814775786533, -6.222761293078241884, -8.102969835052219238 ) ) ;
#15386=AXIS2_PLACEMENT_3D ( 'NONE', #28838, #12180, #8751 ) ;
#15387=CARTESIAN_POINT ( 'NONE',  ( 120.7379948109119709, -10.63000616557722466, -14.87417383870573495 ) ) ;
#15389=CARTESIAN_POINT ( 'NONE',  ( 121.6456214775786293, -10.63000616557722466, -14.87417383870573495 ) ) ;
#15392=CARTESIAN_POINT ( 'NONE',  ( 127.8688423620682215, -3.182392322772966242, -14.38315457524332075 ) ) ;
#15395=CARTESIAN_POINT ( 'NONE',  ( 136.1673833308564099, -10.27421185173757934, -11.10761155373447373 ) ) ;
#15396=CARTESIAN_POINT ( 'NONE',  ( 114.2711548109119803, -0.1624402480850797581, -16.17319339645315424 ) ) ;
#15397=CARTESIAN_POINT ( 'NONE',  ( 112.0588148109119828, -9.859900752359374465, -12.68260735090039404 ) ) ;
#15401=CARTESIAN_POINT ( 'NONE',  ( 114.9518748109119883, -7.643976991954077427, -18.09477374809248928 ) ) ;
#15404=CARTESIAN_POINT ( 'NONE',  ( 123.9836468052895526, -1.125321370491285444, -17.12283323191017814 ) ) ;
#15406=CARTESIAN_POINT ( 'NONE',  ( 120.2274548109119934, 0.5811942927096110934, -14.16772938898807510 ) ) ;
#15407=CARTESIAN_POINT ( 'NONE',  ( 121.5888948109119809, 0.1319031606808879209, -14.10382304977623669 ) ) ;
#15409=CARTESIAN_POINT ( 'NONE',  ( 137.1399781294005891, -8.821015187752031750, -9.781153249680350825 ) ) ;
#15412=CARTESIAN_POINT ( 'NONE',  ( 119.6601881442453106, -1.833838273342659253, -17.42832698103878286 ) ) ;
#15413=CARTESIAN_POINT ( 'NONE',  ( 121.0216281442452981, -7.894159318335828068, -9.358103419637847864 ) ) ;
#15414=CARTESIAN_POINT ( 'NONE',  ( 115.0086014775786509, -5.574606645277164318, -18.38911715685844683 ) ) ;
#15415=CARTESIAN_POINT ( 'NONE',  ( 120.6611768734311028, -1.223627541775709426, -16.99192386690442547 ) ) ;
#15417=CARTESIAN_POINT ( 'NONE',  ( 124.6521348109119884, -7.894159318335828068, -9.358103419637847864 ) ) ;
#15418=CARTESIAN_POINT ( 'NONE',  ( 122.2696148109119889, -5.574606645277164318, -18.38911715685844683 ) ) ;
#15420=CARTESIAN_POINT ( 'NONE',  ( 112.6260814775786514, -0.8288870151387699448, -10.36305467784174006 ) ) ;
#15425=CARTESIAN_POINT ( 'NONE',  ( 121.8725281442453223, -3.383040157471821630, -19.15922257007629170 ) ) ;
#15426=CARTESIAN_POINT ( 'NONE',  ( 117.3343948109119737, -3.383040157471821630, -19.15922257007629170 ) ) ;
#15428=CARTESIAN_POINT ( 'NONE',  ( 116.5969481442453031, 0.5811942927096154232, -14.16772938898807155 ) ) ;
#15430=ORIENTED_EDGE ( 'NONE', *, *, #44279, .T. ) ;
#15432=CARTESIAN_POINT ( 'NONE',  ( 118.4122014775786340, 0.5811942927096110934, -14.16772938898807510 ) ) ;
#15433=CARTESIAN_POINT ( 'NONE',  ( 112.1722681442453222, -0.4660016031367893996, -10.09054647747474043 ) ) ;
#15435=CARTESIAN_POINT ( 'NONE',  ( 113.3635281442453504, -0.1624402480850797581, -16.17319339645315424 ) ) ;
#15436=CARTESIAN_POINT ( 'NONE',  ( 125.5597614775786326, -1.561330072975669392, -17.79121239304076951 ) ) ;
#15440=CARTESIAN_POINT ( 'NONE',  ( 120.0572748109119772, -6.222761293078241884, -8.102969835052219238 ) ) ;
#15445=CARTESIAN_POINT ( 'NONE',  ( 123.4608748109119745, -10.63000616557722466, -14.87417383870573495 ) ) ;
#15448=AXIS2_PLACEMENT_3D ( 'NONE', #30383, #20131, #2327 ) ;
#15451=CARTESIAN_POINT ( 'NONE',  ( 118.6391081442452986, -5.574606645277164318, -18.38911715685844683 ) ) ;
#15454=CARTESIAN_POINT ( 'NONE',  ( 121.9859814775786333, -9.565557343593413364, -10.61323700422348004 ) ) ;
#15456=CARTESIAN_POINT ( 'NONE',  ( 123.8579614775786126, -9.859900752359378018, -12.68260735090039759 ) ) ;
#15459=CARTESIAN_POINT ( 'NONE',  ( 117.1642148109119859, -0.8288870151387760510, -10.36305467784173118 ) ) ;
#15460=CARTESIAN_POINT ( 'NONE',  ( 123.1205148109119563, -7.643976991954077427, -18.09477374809248928 ) ) ;
#15461=CARTESIAN_POINT ( 'NONE',  ( 118.9227414775786400, -10.63000616557722466, -14.87417383870573495 ) ) ;
#15462=CARTESIAN_POINT ( 'NONE',  ( 116.8805814775786445, -6.344957434206662583, -7.627207830600332805 ) ) ;
#15464=CARTESIAN_POINT ( 'NONE',  ( 123.4608748109119745, 0.4262465694468514643, -12.03445270309931736 ) ) ;
#15466=CARTESIAN_POINT ( 'NONE',  ( 120.1140014775786398, -1.561330072975668504, -17.79121239304076951 ) ) ;
#15472=CARTESIAN_POINT ( 'NONE',  ( 137.6352241515737376, -2.583465948169414883, -17.67907559073337964 ) ) ;
#15473=CARTESIAN_POINT ( 'NONE',  ( 125.8433948109119456, -1.834011780172310813, -8.268836392978581529 ) ) ;
#15475=CARTESIAN_POINT ( 'NONE',  ( 124.4252281442452812, -0.8288870151387760510, -10.36305467784173118 ) ) ;
#15483=CARTESIAN_POINT ( 'NONE',  ( 116.5402214775786405, 0.2603800115204892296, -16.42320221600525088 ) ) ;
#15485=CARTESIAN_POINT ( 'NONE',  ( 121.4754414775786131, -1.833838273342659697, -17.42832698103878286 ) ) ;
#15486=CARTESIAN_POINT ( 'NONE',  ( 115.9729548109119861, -3.505236298600246325, -18.68346056562440793 ) ) ;
#15489=CARTESIAN_POINT ( 'NONE',  ( 113.4202548109119846, -10.30919188438810075, -12.61870101168855918 ) ) ;
#15491=CARTESIAN_POINT ( 'NONE',  ( 124.4252281442452812, -9.261995988541697145, -16.69588392320189030 ) ) ;
#15492=CARTESIAN_POINT ( 'NONE',  ( 137.0134976903428310, -9.802792590006783158, -15.70761676718206523 ) ) ;
#15493=VERTEX_POINT ( 'NONE', #14654 ) ;
#15494=CARTESIAN_POINT ( 'NONE',  ( 115.0086014775786509, -4.089484607189486809, -7.948022111789456723 ) ) ;
#15495=CARTESIAN_POINT ( 'NONE',  ( 124.4819548109119722, -7.893985811506177619, -18.51759400769804742 ) ) ;
#15497=CARTESIAN_POINT ( 'NONE',  ( 125.0492214775786266, -3.505236298600246325, -18.68346056562440793 ) ) ;
#15499=CARTESIAN_POINT ( 'NONE',  ( 118.8660148109119774, -10.30919188438810075, -12.61870101168855918 ) ) ;
#15504=CARTESIAN_POINT ( 'NONE',  ( 115.9162281442453093, -5.574606645277164318, -18.38911715685844683 ) ) ;
#15508=CARTESIAN_POINT ( 'NONE',  ( 113.7038881442453402, -6.222761293078241884, -8.102969835052219238 ) ) ;
#15509=CARTESIAN_POINT ( 'NONE',  ( 113.1366214775786432, -1.834011780172310813, -8.268836392978581529 ) ) ;
#15511=CARTESIAN_POINT ( 'NONE',  ( 124.9924948109119924, -5.574606645277164318, -18.38911715685844683 ) ) ;
#15513=CARTESIAN_POINT ( 'NONE',  ( 120.4543614775786295, -4.089484607189486809, -7.948022111789456723 ) ) ;
#15514=CARTESIAN_POINT ( 'NONE',  ( 120.8514481442452961, -7.893985811506177619, -18.51759400769804742 ) ) ;
#15515=ORIENTED_EDGE ( 'NONE', *, *, #4208, .F. ) ;
#15516=CARTESIAN_POINT ( 'NONE',  ( 117.8659193777725278, -1.267766418764730840, -16.93314635290706605 ) ) ;
#15520=CARTESIAN_POINT ( 'NONE',  ( 125.7299414775786488, -10.15424416112507799, -14.75197769757834543 ) ) ;
#15521=CARTESIAN_POINT ( 'NONE',  ( 113.4769814775786330, -10.63000616557722466, -14.87417383870573495 ) ) ;
#15527=CARTESIAN_POINT ( 'NONE',  ( 112.7962614775786676, -3.383040157471821630, -19.15922257007629170 ) ) ;
#15528=CARTESIAN_POINT ( 'NONE',  ( 121.4187148109119789, -6.344957434206665248, -7.627207830600338134 ) ) ;
#15532=ORIENTED_EDGE ( 'NONE', *, *, #10152, .T. ) ;
#15533=CARTESIAN_POINT ( 'NONE',  ( 121.4070848136183400, -3.929494816604741203, -18.62311481910882804 ) ) ;
#15534=CARTESIAN_POINT ( 'NONE',  ( 120.0572748109119772, -6.222761293078241884, -8.102969835052219238 ) ) ;
#15536=CARTESIAN_POINT ( 'NONE',  ( 117.8449348109119938, -8.166667518702817929, -8.995218007635861213 ) ) ;
#15537=CARTESIAN_POINT ( 'NONE',  ( 112.5126281442453120, -10.30919188438810075, -12.61870101168855918 ) ) ;
#15538=CARTESIAN_POINT ( 'NONE',  ( 118.0106993026122950, -1.179503403430468333, -17.05068175419387089 ) ) ;
#15539=CARTESIAN_POINT ( 'NONE',  ( 122.3263414775786373, -3.505236298600246325, -18.68346056562440793 ) ) ;
#15540=CARTESIAN_POINT ( 'NONE',  ( 115.5758681442453053, -7.894159318335828068, -9.358103419637847864 ) ) ;
#15545=CARTESIAN_POINT ( 'NONE',  ( 117.6180281442453150, -8.899110576539710493, -16.42337572283490132 ) ) ;
#15548=CARTESIAN_POINT ( 'NONE',  ( 114.7249681442453237, 0.2603800115204892296, -16.42320221600525088 ) ) ;
#15550=CARTESIAN_POINT ( 'NONE',  ( 113.1933481442453058, -5.574606645277164318, -18.38911715685844683 ) ) ;
#15551=ADVANCED_FACE ( 'NONE', ( #33874 ), #32542, .T. ) ;
#15552=ORIENTED_EDGE ( 'NONE', *, *, #17958, .T. ) ;
#15554=CARTESIAN_POINT ( 'NONE',  ( 122.7801548109119665, -6.222761293078241884, -8.102969835052219238 ) ) ;
#15555=CARTESIAN_POINT ( 'NONE',  ( 116.8238548109119819, -5.574606645277164318, -18.38911715685844683 ) ) ;
#15556=EDGE_CURVE ( 'NONE', #30023, #29206, #31602, .T. ) ;
#15564=CARTESIAN_POINT ( 'NONE',  ( 118.0718414775786300, -9.261995988541697145, -16.69588392320189030 ) ) ;
#15565=CARTESIAN_POINT ( 'NONE',  ( 113.8173414775786512, 0.2603800115204892296, -16.42320221600525088 ) ) ;
#15566=CARTESIAN_POINT ( 'NONE',  ( 116.3700414775786527, -4.153390946401321671, -8.397313243818183892 ) ) ;
#15567=CARTESIAN_POINT ( 'NONE',  ( 122.7801548109119665, -6.222761293078241884, -8.102969835052219238 ) ) ;
#15569=ORIENTED_EDGE ( 'NONE', *, *, #37000, .T. ) ;
#15570=CARTESIAN_POINT ( 'NONE',  ( 119.4900081442453086, -7.643976991954077427, -18.09477374809248928 ) ) ;
#15571=ADVANCED_FACE ( 'NONE', ( #24991 ), #28201, .F. ) ;
#15572=CARTESIAN_POINT ( 'NONE',  ( 124.5386814775786206, -4.153390946401325223, -8.397313243818185668 ) ) ;
#15575=CARTESIAN_POINT ( 'NONE',  ( 114.1175919737025737, -1.196538596002799215, -17.02799684832027083 ) ) ;
#15577=CARTESIAN_POINT ( 'NONE',  ( 118.5823814775786360, -1.834011780172310813, -8.268836392978581529 ) ) ;
#15580=CARTESIAN_POINT ( 'NONE',  ( 119.2631014775786298, 0.2603800115204892296, -16.42320221600525088 ) ) ;
#15583=CARTESIAN_POINT ( 'NONE',  ( 114.7249681442453237, 0.2603800115204892296, -16.42320221600525088 ) ) ;
#15586=CARTESIAN_POINT ( 'NONE',  ( 119.3765548109119834, 0.9020085738987339008, -11.91225656197089222 ) ) ;
#15592=CARTESIAN_POINT ( 'NONE',  ( 119.6601881442453106, -1.833838273342659253, -17.42832698103878286 ) ) ;
#15595=CARTESIAN_POINT ( 'NONE',  ( 112.7962614775786676, -6.222761293078241884, -8.102969835052219238 ) ) ;
#15598=CARTESIAN_POINT ( 'NONE',  ( 113.5337081442453240, -0.8288870151387760510, -10.36305467784173118 ) ) ;
#15599=CARTESIAN_POINT ( 'NONE',  ( 118.8092881442453290, -9.988377603198976828, -10.36322818467138340 ) ) ;
#15601=CARTESIAN_POINT ( 'NONE',  ( 118.9794681442453026, -0.8288870151387760510, -10.36305467784173118 ) ) ;
#15602=CARTESIAN_POINT ( 'NONE',  ( 116.0296814775786345, -8.166667518702817929, -8.995218007635861213 ) ) ;
#15603=CARTESIAN_POINT ( 'NONE',  ( 123.1772414775786189, -4.089484607189486809, -7.948022111789456723 ) ) ;
#15604=CARTESIAN_POINT ( 'NONE',  ( 120.0572748109119772, -6.222761293078241884, -8.102969835052219238 ) ) ;
#15606=CARTESIAN_POINT ( 'NONE',  ( 125.6732148109119862, -9.859900752359378018, -12.68260735090039759 ) ) ;
#15607=CARTESIAN_POINT ( 'NONE',  ( 120.0005481442453146, -5.638512984488999180, -18.83840828888717311 ) ) ;
#15609=CARTESIAN_POINT ( 'NONE',  ( 122.4965214775786251, -10.30919188438810075, -12.61870101168855918 ) ) ;
#15615=B_SPLINE_CURVE_WITH_KNOTS ( 'NONE', 3,
 ( #6991, #40993, #23657, #3343, #6773, #37543, #20683, #17262, #20234, #10639 ),
 .UNSPECIFIED., .F., .F.,
 ( 4, 3, 3, 4 ),
 ( 0.000000000000000000, 0.0001671877548681325037, 0.0003343755096277755095, 0.0006463528481650619413 ),
 .UNSPECIFIED. ) ;
#15617=CARTESIAN_POINT ( 'NONE',  ( 136.9012041053371149, -10.04030426489261707, -11.44593779250850574 ) ) ;
#15618=CARTESIAN_POINT ( 'NONE',  ( 119.6601881442453106, -1.833838273342659253, -17.42832698103878286 ) ) ;
#15619=CARTESIAN_POINT ( 'NONE',  ( 124.3117748109119844, -10.30919188438810075, -12.61870101168855918 ) ) ;
#15625=CARTESIAN_POINT ( 'NONE',  ( 114.5547881442453217, -4.153390946401321671, -8.397313243818183892 ) ) ;
#15627=CARTESIAN_POINT ( 'NONE',  ( 113.3250873908105945, -2.443475742715324639, -17.86549347949428679 ) ) ;
#15632=CARTESIAN_POINT ( 'NONE',  ( 124.4252281442452812, -9.261995988541697145, -16.69588392320189030 ) ) ;
#15633=CARTESIAN_POINT ( 'NONE',  ( 121.3052614775786111, -7.643976991954077427, -18.09477374809248928 ) ) ;
#15634=ORIENTED_EDGE ( 'NONE', *, *, #42304, .T. ) ;
#15638=CARTESIAN_POINT ( 'NONE',  ( 124.4252281442452812, -0.8288870151387760510, -10.36305467784173118 ) ) ;
#15639=CARTESIAN_POINT ( 'NONE',  ( 122.3263414775786373, -3.505236298600246325, -18.68346056562440793 ) ) ;
#15640=CARTESIAN_POINT ( 'NONE',  ( 119.2063748109119814, -7.894159318335828068, -9.358103419637847864 ) ) ;
#15649=CARTESIAN_POINT ( 'NONE',  ( 121.0216281442452981, -1.561330072975668948, -17.79121239304076951 ) ) ;
#15650=CARTESIAN_POINT ( 'NONE',  ( 118.3554748109119998, 0.2603800115204892296, -16.42320221600525088 ) ) ;
#15654=( BOUNDED_CURVE ( )  B_SPLINE_CURVE ( 2, ( #14776, #18428, #32320, #31870, #7039, #635, #411, #28691, #34823, #3606, #14548, #17522, #31419, #7251, #21166, #28466, #35042 ),
 .UNSPECIFIED., .F., .T. ) 
 B_SPLINE_CURVE_WITH_KNOTS ( ( 3, 2, 2, 2, 2, 2, 2, 2, 3 ),
 ( 0.7045046674808920217, 0.7109375000000000000, 0.7187500000000000000, 0.7265625000000000000, 0.7343750000000000000, 0.7421875000000000000, 0.7500000000000000000, 0.7578125000000000000, 0.7642453325190590174 ),
 .UNSPECIFIED. ) 
 CURVE ( )  GEOMETRIC_REPRESENTATION_ITEM ( )  RATIONAL_B_SPLINE_CURVE ( ( 0.9778625265006459788, 0.9373222120152210346, 1.000000000000000000, 0.9238795325112869605, 1.000000000000000000, 0.9238795325112869605, 1.000000000000000000, 0.9238795325112869605, 1.000000000000000000, 0.9238795325112869605, 1.000000000000000000, 0.9238795325112869605, 1.000000000000000000, 0.9238795325112869605, 1.000000000000000000, 0.9373222120157009840, 0.9778625265000250311 ) ) 
 REPRESENTATION_ITEM ( '' )  );
#15655=CARTESIAN_POINT ( 'NONE',  ( 117.7882081442453170, -6.344957434206665248, -7.627207830600338134 ) ) ;
#15656=CARTESIAN_POINT ( 'NONE',  ( 111.4705635773848940, -2.467220198592768199, -17.83387418641523325 ) ) ;
#15660=CARTESIAN_POINT ( 'NONE',  ( 121.0783548109119749, 0.2603800115204892296, -16.42320221600525088 ) ) ;
#15661=CARTESIAN_POINT ( 'NONE',  ( 121.0783548109119749, 0.2603800115204892296, -16.42320221600525088 ) ) ;
#15662=CARTESIAN_POINT ( 'NONE',  ( 126.4673881442452910, -7.894159318335828068, -9.358103419637847864 ) ) ;
#15663=CARTESIAN_POINT ( 'NONE',  ( 114.1009748109119784, -5.574606645277164318, -18.38911715685844683 ) ) ;
#15664=CARTESIAN_POINT ( 'NONE',  ( 111.4915481442453142, -1.833838273342658365, -17.42832698103878286 ) ) ;
#15665=CIRCLE ( 'NONE', #19311, 4.999999999999998224 ) ;
#15667=CARTESIAN_POINT ( 'NONE',  ( 120.7947214775786193, -0.8288870151387760510, -10.36305467784173118 ) ) ;
#15669=CARTESIAN_POINT ( 'NONE',  ( 124.1773369107181821, -2.467220198592779301, -17.83387418641524391 ) ) ;
#15672=CARTESIAN_POINT ( 'NONE',  ( 121.9859814775786333, 0.2603800115204892296, -16.42320221600525088 ) ) ;
#15676=CARTESIAN_POINT ( 'NONE',  ( 118.9227414775786542, 0.4262465694468514643, -12.03445270309931736 ) ) ;
#15679=CARTESIAN_POINT ( 'NONE',  ( 125.2761281442453054, 0.4262465694468514643, -12.03445270309931736 ) ) ;
#15682=CARTESIAN_POINT ( 'NONE',  ( 125.5030348109119558, -6.222761293078241884, -8.102969835052219238 ) ) ;
#15685=CARTESIAN_POINT ( 'NONE',  ( 122.1561614775786353, -0.4660016031367893996, -10.09054647747474043 ) ) ;
#15686=CARTESIAN_POINT ( 'NONE',  ( 117.2776681442452968, -4.153390946401325223, -8.397313243818185668 ) ) ;
#15687=CARTESIAN_POINT ( 'NONE',  ( 121.8725281442453223, -6.222761293078241884, -8.102969835052219238 ) ) ;
#15689=CARTESIAN_POINT ( 'NONE',  ( 124.3685014775786328, -10.63000616557722466, -14.87417383870573495 ) ) ;
#15690=CARTESIAN_POINT ( 'NONE',  ( 116.3700414775786527, -5.638512984488999180, -18.83840828888717311 ) ) ;
#15692=CARTESIAN_POINT ( 'NONE',  ( 113.8740681442453138, -9.859900752359374465, -12.68260735090039404 ) ) ;
#15693=CARTESIAN_POINT ( 'NONE',  ( 122.6099748109119929, -0.8288870151387760510, -10.36305467784173118 ) ) ;
#15694=CARTESIAN_POINT ( 'NONE',  ( 120.6245414775786458, -9.988377603198976828, -10.36322818467138340 ) ) ;
#15701=CARTESIAN_POINT ( 'NONE',  ( 125.7299414775786346, 0.9020085738987339008, -11.91225656197089222 ) ) ;
#15703=CARTESIAN_POINT ( 'NONE',  ( 111.8886348109120092, -3.383040157471821630, -19.15922257007629170 ) ) ;
#15706=CARTESIAN_POINT ( 'NONE',  ( 111.7857214775786474, -4.159894987975828684, -8.443039665293898821 ) ) ;
#15709=CARTESIAN_POINT ( 'NONE',  ( 116.0296814775786345, -8.166667518702817929, -8.995218007635861213 ) ) ;
#15710=CARTESIAN_POINT ( 'NONE',  ( 112.8721930757767495, -0.9924539043446216624, -17.29976612834909133 ) ) ;
#15711=CARTESIAN_POINT ( 'NONE',  ( 124.3685014775786328, 0.4262465694468514643, -12.03445270309931736 ) ) ;
#15712=CARTESIAN_POINT ( 'NONE',  ( 116.1431348109119881, 0.1319031606808879209, -14.10382304977623669 ) ) ;
#15714=CARTESIAN_POINT ( 'NONE',  ( 116.0479673908105980, -2.443475742715333965, -17.86549347949429389 ) ) ;
#15715=CARTESIAN_POINT ( 'NONE',  ( 123.9146881442452894, 0.9020085738987452251, -11.91225656197092597 ) ) ;
#15716=CARTESIAN_POINT ( 'NONE',  ( 116.0296814775786345, -8.166667518702817929, -8.995218007635861213 ) ) ;
#15717=B_SPLINE_CURVE_WITH_KNOTS ( 'NONE', 3,
 ( #30627, #37457, #7122, #21032, #30851, #23801, #37691, #6464, #37910, #20373 ),
 .UNSPECIFIED., .F., .F.,
 ( 4, 3, 3, 4 ),
 ( 0.000000000000000000, 0.0001671877560959399915, 0.0003343755126089165055, 0.0006438490228512240001 ),
 .UNSPECIFIED. ) ;
#15720=CARTESIAN_POINT ( 'NONE',  ( 125.3895814775786448, -7.893985811506177619, -18.51759400769804742 ) ) ;
#15722=VERTEX_POINT ( 'NONE', #33784 ) ;
#15723=CARTESIAN_POINT ( 'NONE',  ( 114.1009748109119784, -4.089484607189486809, -7.948022111789456723 ) ) ;
#15724=CARTESIAN_POINT ( 'NONE',  ( 113.1366214775786432, -7.643976991954077427, -18.09477374809248928 ) ) ;
#15727=CARTESIAN_POINT ( 'NONE',  ( 113.1366214775786432, -1.834011780172310813, -8.268836392978581529 ) ) ;
#15729=CARTESIAN_POINT ( 'NONE',  ( 118.6391081442452986, -4.089484607189486809, -7.948022111789456723 ) ) ;
#15732=CARTESIAN_POINT ( 'NONE',  ( 111.5599048082056868, -0.1020945015690391533, -15.74893487844545703 ) ) ;
#15733=CARTESIAN_POINT ( 'NONE',  ( 136.9394333025907713, -2.946625990313646248, -8.232885575275636469 ) ) ;
#15734=CARTESIAN_POINT ( 'NONE',  ( 112.6828081442453282, -2.084020599724406786, -8.691656652584148546 ) ) ;
#15738=CARTESIAN_POINT ( 'NONE',  ( 113.0231681442453180, -10.15424416112533912, -14.75197769757731336 ) ) ;
#15739=CARTESIAN_POINT ( 'NONE',  ( 126.4106614775786284, -6.222761293078241884, -8.102969835052219238 ) ) ;
#15741=CARTESIAN_POINT ( 'NONE',  ( 123.1205148109119563, -7.643976991954077427, -18.09477374809248928 ) ) ;
#15743=CARTESIAN_POINT ( 'NONE',  ( 124.4252281442452812, -9.261995988541697145, -16.69588392320189030 ) ) ;
#15744=CARTESIAN_POINT ( 'NONE',  ( 122.0994348109119443, 0.9020085738987339008, -11.91225656197089222 ) ) ;
#15746=CARTESIAN_POINT ( 'NONE',  ( 127.0298367773232400, -8.469156795426192375, -17.42115985237845521 ) ) ;
#15748=CIRCLE ( 'NONE', #41259, 4.999999999999998224 ) ;
#15752=CARTESIAN_POINT ( 'NONE',  ( 125.6732148109119862, -9.859900752359514797, -12.68260735090137459 ) ) ;
#15753=CARTESIAN_POINT ( 'NONE',  ( 115.2922348109119781, -10.63000616557722466, -14.87417383870573495 ) ) ;
#15758=CARTESIAN_POINT ( 'NONE',  ( 113.4202548109119846, 0.1319031606808879209, -14.10382304977623669 ) ) ;
#15759=CARTESIAN_POINT ( 'NONE',  ( 113.0294866692503888, -2.311015703046748193, -18.04188382666269064 ) ) ;
#15760=CARTESIAN_POINT ( 'NONE',  ( 120.8514481442452961, -7.893985811506177619, -18.51759400769804742 ) ) ;
#15765=CARTESIAN_POINT ( 'NONE',  ( 117.9583881442453048, 0.1319031606808879209, -14.10382304977623669 ) ) ;
#15766=CARTESIAN_POINT ( 'NONE',  ( 116.3700414775786527, -5.638512984488999180, -18.83840828888717311 ) ) ;
#15767=CARTESIAN_POINT ( 'NONE',  ( 116.0864081442453113, -9.988377603198976828, -10.36322818467138340 ) ) ;
#15768=CARTESIAN_POINT ( 'NONE',  ( 118.1613820163423298, -1.087735405160632718, -17.17288456429612253 ) ) ;
#15769=CARTESIAN_POINT ( 'NONE',  ( 123.2906948109119867, -1.833838273342659697, -17.42832698103878286 ) ) ;
#15770=CARTESIAN_POINT ( 'NONE',  ( 120.5110881442453206, -3.505236298600246325, -18.68346056562440793 ) ) ;
#15771=VERTEX_POINT ( 'NONE', #2554 ) ;
#15774=CARTESIAN_POINT ( 'NONE',  ( 112.2289948109119848, -1.834011780172310813, -8.268836392978581529 ) ) ;
#15775=CARTESIAN_POINT ( 'NONE',  ( 122.6099748109119929, -0.8288870151387760510, -10.36305467784173118 ) ) ;
#15778=CARTESIAN_POINT ( 'NONE',  ( 115.4056881442453459, -7.893985811506177619, -18.51759400769804742 ) ) ;
#15780=CARTESIAN_POINT ( 'NONE',  ( 115.5758681442453053, -7.894159318335828068, -9.358103419637847864 ) ) ;
#15784=CARTESIAN_POINT ( 'NONE',  ( 123.4041481442452834, 0.1319031606808879209, -14.10382304977623669 ) ) ;
#15785=CARTESIAN_POINT ( 'NONE',  ( 121.4187148109119789, -3.505236298600246325, -18.68346056562440793 ) ) ;
#15792=CARTESIAN_POINT ( 'NONE',  ( 115.5758681442453053, -1.561330072975668060, -17.79121239304076951 ) ) ;
#15793=CARTESIAN_POINT ( 'NONE',  ( 115.8595014775786609, -1.834011780172310813, -8.268836392978581529 ) ) ;
#15794=CARTESIAN_POINT ( 'NONE',  ( 116.4834948109119779, -7.894159318335828068, -9.358103419637847864 ) ) ;
#15795=CARTESIAN_POINT ( 'NONE',  ( 120.2841814775786276, -10.15424416112533912, -14.75197769757731336 ) ) ;
#15796=CARTESIAN_POINT ( 'NONE',  ( 113.1366214775786432, -1.834011780172310813, -8.268836392978581529 ) ) ;
#15798=CARTESIAN_POINT ( 'NONE',  ( 119.9438214775786378, -2.084020599724406786, -8.691656652584148546 ) ) ;
#15804=CARTESIAN_POINT ( 'NONE',  ( 119.3765548109119834, 0.9020085738987339008, -11.91225656197089222 ) ) ;
#15806=CARTESIAN_POINT ( 'NONE',  ( 119.3765548109119834, 0.9020085738987339008, -11.91225656197089222 ) ) ;
#15809=CARTESIAN_POINT ( 'NONE',  ( 118.2987481442453088, -1.561330072975668504, -17.79121239304076951 ) ) ;
#15810=CARTESIAN_POINT ( 'NONE',  ( 116.9373081442452929, -8.166667518702817929, -8.995218007635861213 ) ) ;
#15815=ORIENTED_EDGE ( 'NONE', *, *, #43145, .T. ) ;
#15818=CARTESIAN_POINT ( 'NONE',  ( 118.6958348109119754, -3.505236298600246325, -18.68346056562440793 ) ) ;
#15821=CARTESIAN_POINT ( 'NONE',  ( 118.5256548109119876, -8.899110576539710493, -16.42337572283490132 ) ) ;
#15824=CARTESIAN_POINT ( 'NONE',  ( 112.5126281442453120, 0.1319031606808879209, -14.10382304977623669 ) ) ;
#15825=CARTESIAN_POINT ( 'NONE',  ( 124.5386814775786206, -5.638512984488999180, -18.83840828888717311 ) ) ;
#15828=ADVANCED_FACE ( 'NONE', ( #9872 ), #40211, .T. ) ;
#15829=CARTESIAN_POINT ( 'NONE',  ( 117.9583881442453048, 0.1319031606808879209, -14.10382304977623669 ) ) ;
#15830=CARTESIAN_POINT ( 'NONE',  ( 114.4413348109119823, -9.261995988541697145, -16.69588392320189030 ) ) ;
#15831=CARTESIAN_POINT ( 'NONE',  ( 119.8303681442453126, -10.63000616557722466, -14.87417383870573495 ) ) ;
#15832=CARTESIAN_POINT ( 'NONE',  ( 124.0281414775786146, -7.643976991954077427, -18.09477374809248928 ) ) ;
#15834=CARTESIAN_POINT ( 'NONE',  ( 125.5597614775786326, -7.894159318335828068, -9.358103419637847864 ) ) ;
#15835=EDGE_CURVE ( 'NONE', #14254, #40113, #6395, .T. ) ;
#15836=CARTESIAN_POINT ( 'NONE',  ( 122.9503348109119827, 0.5811942927096110934, -14.16772938898807510 ) ) ;
#15837=CARTESIAN_POINT ( 'NONE',  ( 112.3424481442453384, -3.505236298600246325, -18.68346056562440793 ) ) ;
#15839=CARTESIAN_POINT ( 'NONE',  ( 111.2646414775786496, -8.899110576539710493, -16.42337572283490132 ) ) ;
#15841=CARTESIAN_POINT ( 'NONE',  ( 117.4893492294923902, -2.263366209404196638, -18.10533625161307114 ) ) ;
#15845=CARTESIAN_POINT ( 'NONE',  ( 138.2004992774602954, -2.227975765267806274, -15.65448404533372972 ) ) ;
#15848=CARTESIAN_POINT ( 'NONE',  ( 137.4443952029584750, -9.944843709095133377, -13.20533582317771248 ) ) ;
#15849=CARTESIAN_POINT ( 'NONE',  ( 118.5823814775786360, -7.643976991954077427, -18.09477374809248928 ) ) ;
#15850=CARTESIAN_POINT ( 'NONE',  ( 124.0848681442452772, -4.089484607189486809, -7.948022111789456723 ) ) ;
#15856=CARTESIAN_POINT ( 'NONE',  ( 114.6682414775786469, -7.894159318335828068, -9.358103419637847864 ) ) ;
#15857=CARTESIAN_POINT ( 'NONE',  ( 113.3643610407382454, -2.419733177069680607, -17.89711025544712442 ) ) ;
#15859=CARTESIAN_POINT ( 'NONE',  ( 124.0622086996681901, -1.172797794773259072, -17.05961127468926719 ) ) ;
#15861=CARTESIAN_POINT ( 'NONE',  ( 122.0994348109119443, 0.9020085738987339008, -11.91225656197089222 ) ) ;
#15862=CARTESIAN_POINT ( 'NONE',  ( 122.2128881442453263, -7.643976991954077427, -18.09477374809248928 ) ) ;
#15865=CARTESIAN_POINT ( 'NONE',  ( 126.2597653975789598, 0.06634425167100366227, -14.34189767235250912 ) ) ;
#15867=CARTESIAN_POINT ( 'NONE',  ( 121.7590748109119687, -2.084020599724406786, -8.691656652584148546 ) ) ;
#15868=CARTESIAN_POINT ( 'NONE',  ( 121.2485348109119769, -8.899110576539710493, -16.42337572283490132 ) ) ;
#15872=CARTESIAN_POINT ( 'NONE',  ( 115.1010702440515558, -2.467220198592777525, -17.83387418641524391 ) ) ;
#15878=CARTESIAN_POINT ( 'NONE',  ( 121.3052614775786111, -1.834011780172310813, -8.268836392978581529 ) ) ;
#15879=CARTESIAN_POINT ( 'NONE',  ( 123.8579614775786126, 0.5811942927096110934, -14.16772938898807510 ) ) ;
#15881=CARTESIAN_POINT ( 'NONE',  ( 116.4834948109119779, -1.561330072975668504, -17.79121239304076951 ) ) ;
#15887=CARTESIAN_POINT ( 'NONE',  ( 124.5386814775786206, -5.638512984488999180, -18.83840828888717311 ) ) ;
#15888=CARTESIAN_POINT ( 'NONE',  ( 119.5467348109119712, -4.089484607189486809, -7.948022111789456723 ) ) ;
#15889=CARTESIAN_POINT ( 'NONE',  ( 125.8433948109119456, -7.643976991954077427, -18.09477374809248928 ) ) ;
#15892=CARTESIAN_POINT ( 'NONE',  ( 113.5337081442453240, -0.8288870151387760510, -10.36305467784173118 ) ) ;
#15893=CARTESIAN_POINT ( 'NONE',  ( 126.0135748109119902, -8.166667518702819706, -8.995218007635861213 ) ) ;
#15895=CARTESIAN_POINT ( 'NONE',  ( 119.1496481442453046, -6.222761293078241884, -8.102969835052219238 ) ) ;
#15901=CARTESIAN_POINT ( 'NONE',  ( 122.2128881442453263, -1.834011780172310813, -8.268836392978581529 ) ) ;
#15906=CARTESIAN_POINT ( 'NONE',  ( 119.1496481442453046, -6.222761293078241884, -8.102969835052219238 ) ) ;
#15910=CARTESIAN_POINT ( 'NONE',  ( 121.7023481442452777, -0.8288870151387760510, -10.36305467784173118 ) ) ;
#15912=CARTESIAN_POINT ( 'NONE',  ( 125.7299414775786346, -10.15424416112533912, -14.75197769757731336 ) ) ;
#15914=CARTESIAN_POINT ( 'NONE',  ( 125.0492214775786266, -6.344957434206665248, -7.627207830600338134 ) ) ;
#15915=CARTESIAN_POINT ( 'NONE',  ( 117.5045748109119756, -9.859900752359374465, -12.68260735090039404 ) ) ;
#15916=CARTESIAN_POINT ( 'NONE',  ( 122.1561614775786353, -8.899110576539710493, -16.42337572283490132 ) ) ;
#15918=CARTESIAN_POINT ( 'NONE',  ( 121.7023481442452777, -9.261995988541697145, -16.69588392320189030 ) ) ;
#15919=CARTESIAN_POINT ( 'NONE',  ( 115.8595014775786609, -1.834011780172310813, -8.268836392978581529 ) ) ;
#15921=CARTESIAN_POINT ( 'NONE',  ( 112.5693548109119888, 0.4262465694468514643, -12.03445270309931736 ) ) ;
#15923=CARTESIAN_POINT ( 'NONE',  ( 124.4252281442452812, -0.8288870151387760510, -10.36305467784173118 ) ) ;
#15924=CARTESIAN_POINT ( 'NONE',  ( 125.7299414775786346, 0.9020085738987339008, -11.91225656197089222 ) ) ;
#15927=DIRECTION ( 'NONE',  ( -1.000000000000000000, 0.000000000000000000, 0.000000000000000000 ) ) ;
#15928=CARTESIAN_POINT ( 'NONE',  ( 112.1722681442453222, -8.899110576539710493, -16.42337572283490132 ) ) ;
#15932=CARTESIAN_POINT ( 'NONE',  ( 126.0703014775786102, -0.1624402480850797581, -16.17319339645315424 ) ) ;
#15935=ORIENTED_EDGE ( 'NONE', *, *, #7278, .T. ) ;
#15939=CARTESIAN_POINT ( 'NONE',  ( 120.1707281442453166, 0.2603800115204892296, -16.42320221600525088 ) ) ;
#15940=CARTESIAN_POINT ( 'NONE',  ( 122.7234281442452755, -4.153390946401325223, -8.397313243818185668 ) ) ;
#15941=CARTESIAN_POINT ( 'NONE',  ( 116.4834948109119779, -7.894159318335828068, -9.358103419637847864 ) ) ;
#15943=CARTESIAN_POINT ( 'NONE',  ( 128.2184548109119930, -2.475900776146301219, -7.888945235271306977 ) ) ;
#15944=CARTESIAN_POINT ( 'NONE',  ( 115.2922348109119781, -10.63000616557722466, -14.87417383870573495 ) ) ;
#15947=CARTESIAN_POINT ( 'NONE',  ( 123.4041481442452834, -10.30919188438810075, -12.61870101168855918 ) ) ;
#15950=CARTESIAN_POINT ( 'NONE',  ( 113.2500748109119968, -6.344957434206662583, -7.627207830600332805 ) ) ;
#15951=CARTESIAN_POINT ( 'NONE',  ( 113.3068014775786594, -1.833838273342658809, -17.42832698103878286 ) ) ;
#15953=CARTESIAN_POINT ( 'NONE',  ( 112.1722681442453222, -0.4660016031367893996, -10.09054647747474043 ) ) ;
#15955=CARTESIAN_POINT ( 'NONE',  ( 121.3052614775786111, -1.834011780172310813, -8.268836392978581529 ) ) ;
#15960=CARTESIAN_POINT ( 'NONE',  ( 137.1886586612182271, -3.190032180672805140, -8.343492096882645370 ) ) ;
#15961=CARTESIAN_POINT ( 'NONE',  ( 115.6893214775786447, -9.859900752359374465, -12.68260735090039404 ) ) ;
#15964=CARTESIAN_POINT ( 'NONE',  ( 126.1270281442452870, -10.30919188438810075, -12.61870101168855918 ) ) ;
#15965=CARTESIAN_POINT ( 'NONE',  ( 113.5337081442453240, -9.261995988541697145, -16.69588392320189030 ) ) ;
#15968=CARTESIAN_POINT ( 'NONE',  ( 111.8886348109120092, -3.383040157471821630, -19.15922257007629170 ) ) ;
#15969=CARTESIAN_POINT ( 'NONE',  ( 115.4056881442453459, -2.084020599724406786, -8.691656652584148546 ) ) ;
#15970=CARTESIAN_POINT ( 'NONE',  ( 123.5743281442453139, -7.893985811506177619, -18.51759400769804742 ) ) ;
#15971=CARTESIAN_POINT ( 'NONE',  ( 122.8936081442453059, 0.2603800115204892296, -16.42320221600525088 ) ) ;
#15973=CARTESIAN_POINT ( 'NONE',  ( 112.0588148109119828, 0.5811942927096154232, -14.16772938898807155 ) ) ;
#15978=CARTESIAN_POINT ( 'NONE',  ( 120.0572748109119772, -3.383040157471821630, -19.15922257007629170 ) ) ;
#15983=CARTESIAN_POINT ( 'NONE',  ( 114.8384214775786489, -10.15424416112533912, -14.75197769757731336 ) ) ;
#15985=CARTESIAN_POINT ( 'NONE',  ( 119.9438214775786378, -7.893985811506177619, -18.51759400769804742 ) ) ;
#15987=CARTESIAN_POINT ( 'NONE',  ( 119.3828733359170400, -2.311015703046761072, -18.04188382666269774 ) ) ;
#15989=CARTESIAN_POINT ( 'NONE',  ( 120.6361714748722420, -0.1020945015695078478, -15.74893487844866691 ) ) ;
#15990=CARTESIAN_POINT ( 'NONE',  ( 122.5532481442453019, 0.4262465694468514643, -12.03445270309931736 ) ) ;
#15991=CARTESIAN_POINT ( 'NONE',  ( 120.6245414775786458, -9.988377603198976828, -10.36322818467138340 ) ) ;
#15992=CARTESIAN_POINT ( 'NONE',  ( 112.3991748109119868, -1.833838273342658809, -17.42832698103878286 ) ) ;
#15993=CARTESIAN_POINT ( 'NONE',  ( 115.0653281442453277, -6.344957434206662583, -7.627207830600332805 ) ) ;
#15994=CARTESIAN_POINT ( 'NONE',  ( 135.5197384689382432, -7.252067445482663466, -18.89745628190793525 ) ) ;
#15995=CARTESIAN_POINT ( 'NONE',  ( 122.4397948109119767, -0.1624402480850797581, -16.17319339645315424 ) ) ;
#15996=CARTESIAN_POINT ( 'NONE',  ( 121.1918081442452859, -10.15424416112533912, -14.75197769757731336 ) ) ;
#16000=CARTESIAN_POINT ( 'NONE',  ( 112.7962614775786676, -3.383040157471821630, -19.15922257007629170 ) ) ;
#16001=CARTESIAN_POINT ( 'NONE',  ( 121.0783548109119749, -9.565557343593413364, -10.61323700422348004 ) ) ;
#16004=CARTESIAN_POINT ( 'NONE',  ( 117.1642148109119859, -9.261995988541697145, -16.69588392320189030 ) ) ;
#16006=CARTESIAN_POINT ( 'NONE',  ( 118.0151148109119816, 0.4262465694468514643, -12.03445270309931736 ) ) ;
#16009=CARTESIAN_POINT ( 'NONE',  ( 124.6521348109119884, -7.894159318335828068, -9.358103419637847864 ) ) ;
#16010=ADVANCED_FACE ( 'NONE', ( #24005 ), #10730, .T. ) ;
#16011=CARTESIAN_POINT ( 'NONE',  ( 122.3830681442452857, -1.833838273342659697, -17.42832698103878286 ) ) ;
#16015=CARTESIAN_POINT ( 'NONE',  ( 118.5823814775786360, -1.834011780172310813, -8.268836392978581529 ) ) ;
#16017=CARTESIAN_POINT ( 'NONE',  ( 115.0086014775786509, -4.089484607189486809, -7.948022111789456723 ) ) ;
#16018=CARTESIAN_POINT ( 'NONE',  ( 116.6536748109119941, 0.9020085738987339008, -11.91225656197089222 ) ) ;
#16019=CARTESIAN_POINT ( 'NONE',  ( 115.7460481442453357, -10.15424416112533912, -14.75197769757731336 ) ) ;
#16020=CARTESIAN_POINT ( 'NONE',  ( 123.1772414775786189, -5.574606645277164318, -18.38911715685844683 ) ) ;
#16021=CARTESIAN_POINT ( 'NONE',  ( 112.9664414775786412, 0.5811942927096154232, -14.16772938898807155 ) ) ;
#16023=CARTESIAN_POINT ( 'NONE',  ( 121.7023481442452919, -0.8288870151387760510, -10.36305467784173118 ) ) ;
#16024=DIRECTION ( 'NONE',  ( 1.000000000000000000, 0.000000000000000000, 0.000000000000000000 ) ) ;
#16030=CARTESIAN_POINT ( 'NONE',  ( 118.8092881442453290, -9.988377603198976828, -10.36322818467138340 ) ) ;
#16032=CARTESIAN_POINT ( 'NONE',  ( 119.8303681442453126, -10.63000616557722466, -14.87417383870573495 ) ) ;
#16035=CARTESIAN_POINT ( 'NONE',  ( 118.2420214775786320, -3.383040157471821630, -19.15922257007629170 ) ) ;
#16036=CARTESIAN_POINT ( 'NONE',  ( 121.4754414775786131, -8.166667518702819706, -8.995218007635861213 ) ) ;
#16040=DIRECTION ( 'NONE',  ( 1.000000000000000000, 0.000000000000000000, 0.000000000000000000 ) ) ;
#16043=CARTESIAN_POINT ( 'NONE',  ( 125.6732148109119862, -9.859900752359378018, -12.68260735090039759 ) ) ;
#16047=CARTESIAN_POINT ( 'NONE',  ( 119.3765548109119834, -10.15424416112533912, -14.75197769757731336 ) ) ;
#16050=CARTESIAN_POINT ( 'NONE',  ( 111.4348214775786801, -3.505236298600246325, -18.68346056562440793 ) ) ;
#16051=CARTESIAN_POINT ( 'NONE',  ( 125.0492214775786266, -6.344957434206665248, -7.627207830600338134 ) ) ;
#16053=CARTESIAN_POINT ( 'NONE',  ( 121.9859814775786333, -9.565557343593413364, -10.61323700422348004 ) ) ;
#16054=CARTESIAN_POINT ( 'NONE',  ( 115.5191414775786569, -3.383040157471821630, -19.15922257007629170 ) ) ;
#16055=CARTESIAN_POINT ( 'NONE',  ( 121.8158014775786171, -5.638512984488999180, -18.83840828888717311 ) ) ;
#16057=CARTESIAN_POINT ( 'NONE',  ( 124.8790414775786246, -8.899110576539710493, -16.42337572283490132 ) ) ;
#16060=CARTESIAN_POINT ( 'NONE',  ( 122.6099748109119929, -9.261995988541697145, -16.69588392320189030 ) ) ;
#16062=FACE_OUTER_BOUND ( 'NONE', #20106, .T. ) ;
#16063=CARTESIAN_POINT ( 'NONE',  ( 111.7184548109119788, -0.8288870151387760510, -10.36305467784173118 ) ) ;
#16066=CARTESIAN_POINT ( 'NONE',  ( 118.7315769107182177, -2.467220198592778413, -17.83387418641524391 ) ) ;
#16071=CARTESIAN_POINT ( 'NONE',  ( 119.8303681442453126, 0.4262465694468514643, -12.03445270309931736 ) ) ;
#16072=CARTESIAN_POINT ( 'NONE',  ( 111.4348214775786801, -3.505236298600246325, -18.68346056562440793 ) ) ;
#16073=CARTESIAN_POINT ( 'NONE',  ( 125.1269327111056953, -1.267766418764818770, -16.93314635290698078 ) ) ;
#16076=CARTESIAN_POINT ( 'NONE',  ( 118.0151148109119816, 0.4262465694468514643, -12.03445270309931736 ) ) ;
#16077=CARTESIAN_POINT ( 'NONE',  ( 113.0231681442453180, -10.15424416112533912, -14.75197769757731336 ) ) ;
#16081=CARTESIAN_POINT ( 'NONE',  ( 123.5176014775786228, -9.261995988541697145, -16.69588392320189030 ) ) ;
#16082=CARTESIAN_POINT ( 'NONE',  ( 124.0281414775786146, -7.643976991954077427, -18.09477374809248928 ) ) ;
#16084=DIRECTION ( 'NONE',  ( 0.000000000000000000, 0.6004852223388321697, -0.7996358532186279566 ) ) ;
#16087=CARTESIAN_POINT ( 'NONE',  ( 120.9649014775786355, -6.222761293078241884, -8.102969835052219238 ) ) ;
#16088=CARTESIAN_POINT ( 'NONE',  ( 118.1852948109119836, -4.153390946401325223, -8.397313243818185668 ) ) ;
#16093=AXIS2_PLACEMENT_3D ( 'NONE', #39642, #15927, #22530 ) ;
#16096=B_SPLINE_CURVE_WITH_KNOTS ( 'NONE', 3,
 ( #41519, #31230, #44716, #20977, #44940, #10276, #30792, #41301, #30564, #34850 ),
 .UNSPECIFIED., .F., .F.,
 ( 4, 3, 3, 4 ),
 ( 8.673617379884039324E-19, 0.0001671877560958089928, 0.0003343755126086570017, 0.0006438490228505489759 ),
 .UNSPECIFIED. ) ;
#16100=CARTESIAN_POINT ( 'NONE',  ( 120.9081748109119872, -5.638512984488999180, -18.83840828888717311 ) ) ;
#16101=CARTESIAN_POINT ( 'NONE',  ( 123.2906948109119867, -8.166667518702819706, -8.995218007635861213 ) ) ;
#16103=CARTESIAN_POINT ( 'NONE',  ( 117.2209414775786485, -7.893985811506177619, -18.51759400769804742 ) ) ;
#16106=ORIENTED_EDGE ( 'NONE', *, *, #4499, .T. ) ;
#16108=CARTESIAN_POINT ( 'NONE',  ( 112.3991748109119868, -1.833838273342658809, -17.42832698103878286 ) ) ;
#16110=CARTESIAN_POINT ( 'NONE',  ( 120.9081748109119872, -5.638512984488999180, -18.83840828888717311 ) ) ;
#16111=CARTESIAN_POINT ( 'NONE',  ( 112.1155414775786454, 0.9020085738987339008, -11.91225656197089222 ) ) ;
#16112=CARTESIAN_POINT ( 'NONE',  ( 114.1577014775786552, -3.505236298600246325, -18.68346056562440793 ) ) ;
#16113=EDGE_LOOP ( 'NONE', ( #36253, #9446, #9201, #12564, #34732, #18755, #16636, #14427, #41885, #29446, #34768, #34851, #36758 ) ) ;
#16115=CARTESIAN_POINT ( 'NONE',  ( 112.5693548109119888, 0.4262465694468514643, -12.03445270309931736 ) ) ;
#16116=CARTESIAN_POINT ( 'NONE',  ( 124.8790414775786246, -0.4660016031367893996, -10.09054647747474043 ) ) ;
#16118=CARTESIAN_POINT ( 'NONE',  ( 118.5823814775786360, -7.643976991954077427, -18.09477374809248928 ) ) ;
#16120=CARTESIAN_POINT ( 'NONE',  ( 124.4862981477679824, -2.280480477428469488, -18.08254604495227014 ) ) ;
#16123=CARTESIAN_POINT ( 'NONE',  ( 123.9146881442452894, 0.9020085738987339008, -11.91225656197089222 ) ) ;
#16125=DIRECTION ( 'NONE',  ( -1.000000000000000000, 0.000000000000000000, 0.000000000000000000 ) ) ;
#16126=CARTESIAN_POINT ( 'NONE',  ( 123.2697102440515238, -2.467220198592778413, -17.83387418641524391 ) ) ;
#16131=LINE ( 'NONE', #40756, #355 ) ;
#16132=CARTESIAN_POINT ( 'NONE',  ( 124.9924948109119924, -5.574606645277164318, -18.38911715685844683 ) ) ;
#16137=CARTESIAN_POINT ( 'NONE',  ( 117.7882081442453170, -3.505236298600246325, -18.68346056562440793 ) ) ;
#16140=CARTESIAN_POINT ( 'NONE',  ( 121.4187148109119789, -6.344957434206665248, -7.627207830600338134 ) ) ;
#16141=CARTESIAN_POINT ( 'NONE',  ( 116.0296814775786345, -8.166667518702817929, -8.995218007635861213 ) ) ;
#16144=DIRECTION ( 'NONE',  ( 0.000000000000000000, -0.6004852223388321697, 0.7996358532186280677 ) ) ;
#16145=CARTESIAN_POINT ( 'NONE',  ( 122.4965214775786251, 0.1319031606808879209, -14.10382304977623669 ) ) ;
#16146=CARTESIAN_POINT ( 'NONE',  ( 122.8936081442453059, 0.2603800115204892296, -16.42320221600525088 ) ) ;
#16150=CARTESIAN_POINT ( 'NONE',  ( 114.3846081442453197, 0.4262465694468514643, -12.03445270309931736 ) ) ;
#16151=CARTESIAN_POINT ( 'NONE',  ( 116.3133148109120043, -2.084020599724406786, -8.691656652584148546 ) ) ;
#16157=CARTESIAN_POINT ( 'NONE',  ( 126.0135748109119902, -1.833838273342660141, -17.42832698103878286 ) ) ;
#16162=EDGE_LOOP ( 'NONE', ( #32988, #929, #20522, #34000 ) ) ;
#16164=CARTESIAN_POINT ( 'NONE',  ( 111.4665458264767750, -1.295815253274133161, -16.89579513612386563 ) ) ;
#16165=ORIENTED_EDGE ( 'NONE', *, *, #18214, .T. ) ;
#16166=CARTESIAN_POINT ( 'NONE',  ( 119.6034614775786196, -6.344957434206665248, -7.627207830600338134 ) ) ;
#16168=CARTESIAN_POINT ( 'NONE',  ( 122.8936081442453059, -9.565557343593413364, -10.61323700422348004 ) ) ;
#16169=CARTESIAN_POINT ( 'NONE',  ( 113.1933481442453058, -5.574606645277164318, -18.38911715685844683 ) ) ;
#16170=CARTESIAN_POINT ( 'NONE',  ( 116.0872410407382347, -2.419733177069680607, -17.89711025544712442 ) ) ;
#16172=CARTESIAN_POINT ( 'NONE',  ( 116.3700414775786527, -5.638512984488999180, -18.83840828888717311 ) ) ;
#16175=CARTESIAN_POINT ( 'NONE',  ( 124.8223148109119762, 0.9020085738987339008, -11.91225656197089222 ) ) ;
#16178=CARTESIAN_POINT ( 'NONE',  ( 115.8027748109119841, -0.4660016031367893996, -10.09054647747474043 ) ) ;
#16179=CARTESIAN_POINT ( 'NONE',  ( 115.4056881442453459, -2.084020599724406786, -8.691656652584148546 ) ) ;
#16181=CARTESIAN_POINT ( 'NONE',  ( 125.5030348109119558, -6.222761293078241884, -8.102969835052219238 ) ) ;
#16182=ORIENTED_EDGE ( 'NONE', *, *, #28917, .T. ) ;
#16183=CARTESIAN_POINT ( 'NONE',  ( 123.0637881442452937, -0.4660016031367893996, -10.09054647747474043 ) ) ;
#16187=CARTESIAN_POINT ( 'NONE',  ( 137.0134976903340203, -3.008273255399957158, -8.264431575293873067 ) ) ;
#16188=CARTESIAN_POINT ( 'NONE',  ( 113.8173414775786512, -9.565557343593413364, -10.61323700422348004 ) ) ;
#16192=CARTESIAN_POINT ( 'NONE',  ( 114.9518748109119883, -7.643976991954077427, -18.09477374809248928 ) ) ;
#16193=CARTESIAN_POINT ( 'NONE',  ( 114.1009748109119784, -4.089484607189486809, -7.948022111789456723 ) ) ;
#16195=CARTESIAN_POINT ( 'NONE',  ( 113.8740681442453138, 0.5811942927096154232, -14.16772938898807155 ) ) ;
#16196=CARTESIAN_POINT ( 'NONE',  ( 116.7671281442453335, -7.643976991954077427, -18.09477374809248928 ) ) ;
#16197=CARTESIAN_POINT ( 'NONE',  ( 123.3474214775786209, -9.988377603198976828, -10.36322818467138340 ) ) ;
#16200=CARTESIAN_POINT ( 'NONE',  ( 120.1140014775786398, -1.561330072975668504, -17.79121239304076951 ) ) ;
#16202=CARTESIAN_POINT ( 'NONE',  ( 112.5693548109119888, -10.63000616557722466, -14.87417383870573495 ) ) ;
#16207=CARTESIAN_POINT ( 'NONE',  ( 127.7425183523502881, -7.050714571525749541, -18.72418924296322729 ) ) ;
#16208=CARTESIAN_POINT ( 'NONE',  ( 120.1140014775786398, -1.561330072975668504, -17.79121239304076951 ) ) ;
#16209=ORIENTED_EDGE ( 'NONE', *, *, #32304, .T. ) ;
#16213=CARTESIAN_POINT ( 'NONE',  ( 116.0296814775786345, -1.833838273342658809, -17.42832698103878286 ) ) ;
#16215=CARTESIAN_POINT ( 'NONE',  ( 118.1852948109119836, -5.638512984488999180, -18.83840828888717311 ) ) ;
#16219=CARTESIAN_POINT ( 'NONE',  ( 121.2485348109119769, -8.899110576539744244, -16.42337572283485514 ) ) ;
#16220=CARTESIAN_POINT ( 'NONE',  ( 123.0637881442452937, -8.899110576539710493, -16.42337572283490132 ) ) ;
#16221=CARTESIAN_POINT ( 'NONE',  ( 120.5678148109119832, -8.166667518702819706, -8.995218007635861213 ) ) ;
#16222=CARTESIAN_POINT ( 'NONE',  ( 112.5693548109119888, 0.4262465694468514643, -12.03445270309931736 ) ) ;
#16223=CARTESIAN_POINT ( 'NONE',  ( 114.8951481442453115, -0.4660016031367893996, -10.09054647747474043 ) ) ;
#16224=CARTESIAN_POINT ( 'NONE',  ( 119.1871698793805194, -2.191907684172563986, -18.20049396185734025 ) ) ;
#16226=CARTESIAN_POINT ( 'NONE',  ( 126.2184548109108135, -0.9345830046690825066, -10.29922024082877030 ) ) ;
#16227=CARTESIAN_POINT ( 'NONE',  ( 120.3409081442453044, -8.899110576539710493, -16.42337572283490132 ) ) ;
#16228=ORIENTED_EDGE ( 'NONE', *, *, #27906, .F. ) ;
#16230=CARTESIAN_POINT ( 'NONE',  ( 119.7169148109119874, -9.988377603198960841, -10.36322818467135853 ) ) ;
#16232=CARTESIAN_POINT ( 'NONE',  ( 114.1577014775786552, -6.344957434206662583, -7.627207830600332805 ) ) ;
#16233=CARTESIAN_POINT ( 'NONE',  ( 121.5321681442453183, -0.1624402480850797581, -16.17319339645315424 ) ) ;
#16236=CARTESIAN_POINT ( 'NONE',  ( 116.9940348109119839, -9.988377603198976828, -10.36322818467138340 ) ) ;
#16238=CARTESIAN_POINT ( 'NONE',  ( 115.3489614775786407, -0.8288870151387760510, -10.36305467784173118 ) ) ;
#16242=CARTESIAN_POINT ( 'NONE',  ( 126.5808414775786446, -9.859900752359378018, -12.68260735090039759 ) ) ;
#16243=CARTESIAN_POINT ( 'NONE',  ( 121.6456214775786293, 0.4262465694468514643, -12.03445270309931736 ) ) ;
#16246=CARTESIAN_POINT ( 'NONE',  ( 118.6958348109119754, -6.344957434206665248, -7.627207830600338134 ) ) ;
#16248=CARTESIAN_POINT ( 'NONE',  ( 114.4980614775786592, -7.893985811506177619, -18.51759400769804742 ) ) ;
#16249=CARTESIAN_POINT ( 'NONE',  ( 116.9940348109119839, -9.988377603198976828, -10.36322818467138340 ) ) ;
#16250=CARTESIAN_POINT ( 'NONE',  ( 116.7104014775786425, -8.899110576539710493, -16.42337572283490132 ) ) ;
#16252=CARTESIAN_POINT ( 'NONE',  ( 114.0442481442453300, -1.834011780172310813, -8.268836392978581529 ) ) ;
#16253=ORIENTED_EDGE ( 'NONE', *, *, #24211, .T. ) ;
#16254=CARTESIAN_POINT ( 'NONE',  ( 123.4608748109119745, 0.4262465694468514643, -12.03445270309931736 ) ) ;
#16262=CARTESIAN_POINT ( 'NONE',  ( 122.3830681442452857, -8.166667518702819706, -8.995218007635861213 ) ) ;
#16264=CARTESIAN_POINT ( 'NONE',  ( 119.2063748109119814, -1.561330072975668504, -17.79121239304076951 ) ) ;
#16266=CARTESIAN_POINT ( 'NONE',  ( 121.0783548109119749, 0.2603800115204892296, -16.42320221600525088 ) ) ;
#16267=CARTESIAN_POINT ( 'NONE',  ( 122.2696148109119889, -4.089484607189486809, -7.948022111789456723 ) ) ;
#16269=CARTESIAN_POINT ( 'NONE',  ( 125.3895814775786448, -2.084020599724406786, -8.691656652584148546 ) ) ;
#16270=CARTESIAN_POINT ( 'NONE',  ( 115.8027748109119841, -0.4660016031367859024, -10.09054647747474398 ) ) ;
#16276=CARTESIAN_POINT ( 'NONE',  ( 124.5386814775786206, -4.153390946401325223, -8.397313243818185668 ) ) ;
#16280=CARTESIAN_POINT ( 'NONE',  ( 117.1074881442453233, 0.4262465694468514643, -12.03445270309931736 ) ) ;
#16283=CARTESIAN_POINT ( 'NONE',  ( 126.0135748109119902, -8.166667518702819706, -8.995218007635861213 ) ) ;
#16284=CARTESIAN_POINT ( 'NONE',  ( 123.7445081442452874, -1.561330072975668948, -17.79121239304076951 ) ) ;
#16286=CARTESIAN_POINT ( 'NONE',  ( 123.4041481442452834, 0.1319031606808879209, -14.10382304977623669 ) ) ;
#16287=CARTESIAN_POINT ( 'NONE',  ( 113.7606148109119886, -1.561330072975668060, -17.79121239304076596 ) ) ;
#16288=CARTESIAN_POINT ( 'NONE',  ( 124.4819548109119722, -7.893985811506177619, -18.51759400769804742 ) ) ;
#16289=CARTESIAN_POINT ( 'NONE',  ( 124.4819548109119722, -2.084020599724406786, -8.691656652584148546 ) ) ;
#16291=CARTESIAN_POINT ( 'NONE',  ( 123.5053694832010365, -2.324775150319219108, -18.02356106541841996 ) ) ;
#16293=CARTESIAN_POINT ( 'NONE',  ( 123.0637881442452937, -0.4660016031367893996, -10.09054647747474043 ) ) ;
#16295=CARTESIAN_POINT ( 'NONE',  ( 113.9307948109119764, -10.15424416112533912, -14.75197769757731336 ) ) ;
#16296=CARTESIAN_POINT ( 'NONE',  ( 124.7655881442452852, 0.5811942927096110934, -14.16772938898807510 ) ) ;
#16300=CARTESIAN_POINT ( 'NONE',  ( 136.6129451145462212, -0.8699563032188813994, -17.46288999909464934 ) ) ;
#16303=CARTESIAN_POINT ( 'NONE',  ( 120.8514481442452961, -2.084020599724406786, -8.691656652584148546 ) ) ;
#16304=CARTESIAN_POINT ( 'NONE',  ( 112.2857214775786474, -5.574606645277164318, -18.38911715685844683 ) ) ;
#16305=CARTESIAN_POINT ( 'NONE',  ( 126.4603288065483042, -6.163241521340323992, -18.34700366797996196 ) ) ;
#16308=CARTESIAN_POINT ( 'NONE',  ( 115.9162281442453235, -5.574606645277164318, -18.38911715685844683 ) ) ;
#16311=CARTESIAN_POINT ( 'NONE',  ( 111.6050014775786536, 0.1319031606808879209, -14.10382304977623669 ) ) ;
#16313=CARTESIAN_POINT ( 'NONE',  ( 124.3117748109119844, -10.30919188438810075, -12.61870101168855918 ) ) ;
#16314=CARTESIAN_POINT ( 'NONE',  ( 112.6260814775786514, -9.261995988541697145, -16.69588392320189030 ) ) ;
#16317=CARTESIAN_POINT ( 'NONE',  ( 126.9932531981160224, 0.2252732323729688124, -15.16052778375922117 ) ) ;
#16319=CARTESIAN_POINT ( 'NONE',  ( 124.8223148109119762, -10.15424416112533912, -14.75197769757731336 ) ) ;
#16320=CARTESIAN_POINT ( 'NONE',  ( 120.2841814775786276, -10.15424416112533912, -14.75197769757731336 ) ) ;
#16326=FACE_OUTER_BOUND ( 'NONE', #25816, .T. ) ;
#16329=CARTESIAN_POINT ( 'NONE',  ( 120.3976348109119812, -1.834011780172310813, -8.268836392978581529 ) ) ;
#16330=CARTESIAN_POINT ( 'NONE',  ( 122.7801548109119665, -3.383040157471821630, -19.15922257007629170 ) ) ;
#16331=DIRECTION ( 'NONE',  ( -1.000000000000000000, 0.000000000000000000, 0.000000000000000000 ) ) ;
#16332=CARTESIAN_POINT ( 'NONE',  ( 116.3133148109119759, -7.893985811506177619, -18.51759400769804742 ) ) ;
#16333=DIRECTION ( 'NONE',  ( 0.000000000000000000, -0.6004852223388327248, 0.7996358532186277346 ) ) ;
#16335=CARTESIAN_POINT ( 'NONE',  ( 112.5126281442453120, 0.1319031606808879209, -14.10382304977623669 ) ) ;
#16336=CARTESIAN_POINT ( 'NONE',  ( 126.2404814775786264, -9.261995988541697145, -16.69588392320189030 ) ) ;
#16337=CARTESIAN_POINT ( 'NONE',  ( 119.3198281442452924, 0.5811942927096110934, -14.16772938898807510 ) ) ;
#16338=CARTESIAN_POINT ( 'NONE',  ( 112.8529881442453302, -1.561330072975668060, -17.79121239304076596 ) ) ;
#16339=CARTESIAN_POINT ( 'NONE',  ( 126.1270281442452870, -10.30919188438810075, -12.61870101168855918 ) ) ;
#16341=CARTESIAN_POINT ( 'NONE',  ( 119.2063748109119814, -7.894159318335828068, -9.358103419637847864 ) ) ;
#16342=CARTESIAN_POINT ( 'NONE',  ( 111.4348214775786801, -3.505236298600246325, -18.68346056562440793 ) ) ;
#16344=CARTESIAN_POINT ( 'NONE',  ( 121.3619881442452879, -5.574606645277164318, -18.38911715685844683 ) ) ;
#16346=CARTESIAN_POINT ( 'NONE',  ( 124.6329298793804981, -2.191907684172563986, -18.20049396185734025 ) ) ;
#16350=CARTESIAN_POINT ( 'NONE',  ( 122.0994348109119443, 0.9020085738987339008, -11.91225656197089222 ) ) ;
#16352=CARTESIAN_POINT ( 'NONE',  ( 112.3424481442453384, -6.344957434206662583, -7.627207830600332805 ) ) ;
#16358=CARTESIAN_POINT ( 'NONE',  ( 137.1968316989235461, -4.676744372166964148, -18.70090856814179503 ) ) ;
#16361=CARTESIAN_POINT ( 'NONE',  ( 123.0070614775786169, -10.15424416112533912, -14.75197769757731336 ) ) ;
#16364=CARTESIAN_POINT ( 'NONE',  ( 124.4819548109119722, -7.893985811506177619, -18.51759400769804742 ) ) ;
#16365=CARTESIAN_POINT ( 'NONE',  ( 116.3133148109119759, -7.893985811506177619, -18.51759400769804742 ) ) ;
#16367=CARTESIAN_POINT ( 'NONE',  ( 113.0231681442453180, -10.15424416112533912, -14.75197769757731336 ) ) ;
#16368=CARTESIAN_POINT ( 'NONE',  ( 111.7751814775786556, -7.893985811506177619, -18.51759400769804742 ) ) ;
#16369=CARTESIAN_POINT ( 'NONE',  ( 125.1059481442452750, -8.166667518702819706, -8.995218007635861213 ) ) ;
#16374=CARTESIAN_POINT ( 'NONE',  ( 116.5402214775786405, -9.565557343593413364, -10.61323700422348004 ) ) ;
#16375=CARTESIAN_POINT ( 'NONE',  ( 115.8595014775786609, -7.643976991954077427, -18.09477374809248928 ) ) ;
#16376=CARTESIAN_POINT ( 'NONE',  ( 137.1126581146637307, -2.246346642084271927, -18.12800035012696398 ) ) ;
#16380=CARTESIAN_POINT ( 'NONE',  ( 124.7655881442452852, -9.859900752359378018, -12.68260735090039759 ) ) ;
#16389=CARTESIAN_POINT ( 'NONE',  ( 119.0929214775786278, -5.638512984488999180, -18.83840828888717311 ) ) ;
#16390=CARTESIAN_POINT ( 'NONE',  ( 124.7088614775786226, -9.565557343593413364, -10.61323700422348004 ) ) ;
#16391=CARTESIAN_POINT ( 'NONE',  ( 115.1787814775786387, -0.1624402480850797581, -16.17319339645315424 ) ) ;
#16394=CARTESIAN_POINT ( 'NONE',  ( 122.5532481442453019, -10.63000616557722466, -14.87417383870573495 ) ) ;
#16396=CARTESIAN_POINT ( 'NONE',  ( 115.0086014775786509, -4.089484607189486809, -7.948022111789456723 ) ) ;
#16399=CARTESIAN_POINT ( 'NONE',  ( 124.7088614775786226, 0.2603800115204892296, -16.42320221600525088 ) ) ;
#16402=CARTESIAN_POINT ( 'NONE',  ( 116.4267681442453153, -3.383040157471821630, -19.15922257007629170 ) ) ;
#16403=CARTESIAN_POINT ( 'NONE',  ( 112.9664414775786412, -9.859900752359374465, -12.68260735090039404 ) ) ;
#16405=CARTESIAN_POINT ( 'NONE',  ( 126.6375681442452930, -10.15424416112533912, -14.75197769757731336 ) ) ;
#16408=CARTESIAN_POINT ( 'NONE',  ( 123.5176014775786228, -9.261995988541697145, -16.69588392320189030 ) ) ;
#16412=CARTESIAN_POINT ( 'NONE',  ( 128.2184548109119930, -4.863998795839242995, -13.39321520033831447 ) ) ;
#16413=CARTESIAN_POINT ( 'NONE',  ( 114.7249681442453237, -9.565557343593413364, -10.61323700422348004 ) ) ;
#16416=CARTESIAN_POINT ( 'NONE',  ( 112.3781902440515665, -2.467220198592768199, -17.83387418641523325 ) ) ;
#16418=CARTESIAN_POINT ( 'NONE',  ( 118.0151148109119816, 0.4262465694468514643, -12.03445270309931736 ) ) ;
#16421=CARTESIAN_POINT ( 'NONE',  ( 116.0296814775786345, -1.833838273342658809, -17.42832698103878286 ) ) ;
#16422=CARTESIAN_POINT ( 'NONE',  ( 114.2711548109119803, -9.988377603198976828, -10.36322818467138340 ) ) ;
#16424=CARTESIAN_POINT ( 'NONE',  ( 126.1270281442452870, 0.1319031606808879209, -14.10382304977623669 ) ) ;
#16425=CARTESIAN_POINT ( 'NONE',  ( 115.7460481442453357, -10.15424416112533912, -14.75197769757731336 ) ) ;
#16426=CARTESIAN_POINT ( 'NONE',  ( 121.5321681442453183, -9.988377603198976828, -10.36322818467138340 ) ) ;
#16427=CARTESIAN_POINT ( 'NONE',  ( 122.6099748109119929, -9.261995988541697145, -16.69588392320189030 ) ) ;
#16429=CARTESIAN_POINT ( 'NONE',  ( 114.1577014775786552, -6.344957434206662583, -7.627207830600332805 ) ) ;
#16434=CARTESIAN_POINT ( 'NONE',  ( 118.6391081442452986, -4.089484607189486809, -7.948022111789456723 ) ) ;
#16437=CARTESIAN_POINT ( 'NONE',  ( 138.2184548109119930, -6.243778871467079661, -12.80482167309617125 ) ) ;
#16438=CARTESIAN_POINT ( 'NONE',  ( 112.9097148109120070, -9.565557343593413364, -10.61323700422348004 ) ) ;
#16440=CARTESIAN_POINT ( 'NONE',  ( 119.8303681442453126, -10.63000616557722466, -14.87417383870573495 ) ) ;
#16446=CARTESIAN_POINT ( 'NONE',  ( 121.0783548109119749, -9.565557343593413364, -10.61323700422348004 ) ) ;
#16447=CARTESIAN_POINT ( 'NONE',  ( 121.3619881442452879, -4.089484607189486809, -7.948022111789456723 ) ) ;
#16448=CARTESIAN_POINT ( 'NONE',  ( 113.0798948109119948, -8.899110576539710493, -16.42337572283490132 ) ) ;
#16449=CARTESIAN_POINT ( 'NONE',  ( 115.4624148109119943, -5.638512984488999180, -18.83840828888717311 ) ) ;
#16450=CARTESIAN_POINT ( 'NONE',  ( 118.3179530757767566, -0.9924539043446216624, -17.29976612834909133 ) ) ;
#16451=CARTESIAN_POINT ( 'NONE',  ( 126.3444272079795354, -1.084470278792948328, -10.02424450363365338 ) ) ;
#16452=CARTESIAN_POINT ( 'NONE',  ( 119.5467348109119712, -5.574606645277164318, -18.38911715685844683 ) ) ;
#16456=CARTESIAN_POINT ( 'NONE',  ( 114.7249681442453237, 0.2603800115204892296, -16.42320221600525088 ) ) ;
#16457=CARTESIAN_POINT ( 'NONE',  ( 120.8514481442452961, -2.084020599724406786, -8.691656652584148546 ) ) ;
#16460=CARTESIAN_POINT ( 'NONE',  ( 119.2063748109119814, -1.561330072975668504, -17.79121239304076951 ) ) ;
#16462=CARTESIAN_POINT ( 'NONE',  ( 115.6325948109119821, -9.565557343593413364, -10.61323700422348004 ) ) ;
#16465=CARTESIAN_POINT ( 'NONE',  ( 124.7088614775786226, -9.565557343593413364, -10.61323700422348004 ) ) ;
#16467=CARTESIAN_POINT ( 'NONE',  ( 120.2274548109119934, -9.859900752359378018, -12.68260735090039759 ) ) ;
#16471=CARTESIAN_POINT ( 'NONE',  ( 119.2631014775786298, 0.2603800115204892296, -16.42320221600525088 ) ) ;
#16473=CARTESIAN_POINT ( 'NONE',  ( 118.2987481442453088, -1.561330072975668504, -17.79121239304076951 ) ) ;
#16474=CARTESIAN_POINT ( 'NONE',  ( 116.3133148109119759, -7.893985811506177619, -18.51759400769804742 ) ) ;
#16475=CARTESIAN_POINT ( 'NONE',  ( 119.2631014775786298, -9.565557343593413364, -10.61323700422348004 ) ) ;
#16476=EDGE_CURVE ( 'NONE', #19714, #40981, #10193, .T. ) ;
#16478=CARTESIAN_POINT ( 'NONE',  ( 125.2194014775786286, 0.1319031606808879209, -14.10382304977623669 ) ) ;
#16479=CARTESIAN_POINT ( 'NONE',  ( 112.3424481442453384, -6.344957434206662583, -7.627207830600332805 ) ) ;
#16482=CARTESIAN_POINT ( 'NONE',  ( 121.7590748109119687, -2.084020599724406786, -8.691656652584148546 ) ) ;
#16483=LINE ( 'NONE', #24604, #24919 ) ;
#16489=CARTESIAN_POINT ( 'NONE',  ( 122.8936081442453059, 0.2603800115204892296, -16.42320221600525088 ) ) ;
#16490=CARTESIAN_POINT ( 'NONE',  ( 123.0637881442452937, -8.899110576539710493, -16.42337572283490132 ) ) ;
#16492=CARTESIAN_POINT ( 'NONE',  ( 125.2194014775786286, -10.30919188438810075, -12.61870101168855918 ) ) ;
#16495=CARTESIAN_POINT ( 'NONE',  ( 121.6456214775786293, -10.63000616557722466, -14.87417383870573495 ) ) ;
#16496=CARTESIAN_POINT ( 'NONE',  ( 122.6667014775786413, -7.893985811506177619, -18.51759400769804742 ) ) ;
#16497=CARTESIAN_POINT ( 'NONE',  ( 110.2184548109119788, -1.904930392188239452, -16.08466725871020842 ) ) ;
#16498=CARTESIAN_POINT ( 'NONE',  ( 122.7801548109119665, -6.222761293078241884, -8.102969835052219238 ) ) ;
#16504=CARTESIAN_POINT ( 'NONE',  ( 123.7445081442452874, -7.894159318335828068, -9.358103419637847864 ) ) ;
#16505=AXIS2_PLACEMENT_3D ( 'NONE', #24240, #34260, #44774 ) ;
#16508=CARTESIAN_POINT ( 'NONE',  ( 118.4122014775786340, -9.859900752359374465, -12.68260735090039404 ) ) ;
#16510=CARTESIAN_POINT ( 'NONE',  ( 117.4478481442453131, -9.565557343593413364, -10.61323700422348004 ) ) ;
#16511=CARTESIAN_POINT ( 'NONE',  ( 122.2696148109119889, -4.089484607189486809, -7.948022111789456723 ) ) ;
#16514=CARTESIAN_POINT ( 'NONE',  ( 123.7445081442452874, -7.894159318335828068, -9.358103419637847864 ) ) ;
#16515=CARTESIAN_POINT ( 'NONE',  ( 118.8660148109119774, -10.30919188438810075, -12.61870101168855918 ) ) ;
#16516=CARTESIAN_POINT ( 'NONE',  ( 124.1415948109119540, -6.344957434206665248, -7.627207830600338134 ) ) ;
#16517=CARTESIAN_POINT ( 'NONE',  ( 124.9924948109119924, -5.574606645277164318, -18.38911715685844683 ) ) ;
#16519=CARTESIAN_POINT ( 'NONE',  ( 123.3875309814547023, -2.395992375830759524, -17.92872468182853396 ) ) ;
#16520=EDGE_CURVE ( 'NONE', #45059, #12393, #31473, .T. ) ;
#16522=CARTESIAN_POINT ( 'NONE',  ( 125.3328548109119964, -9.261995988541697145, -16.69588392320189030 ) ) ;
#16523=CARTESIAN_POINT ( 'NONE',  ( 114.9518748109119883, -7.643976991954077427, -18.09477374809248928 ) ) ;
#16524=CARTESIAN_POINT ( 'NONE',  ( 111.9453614775786434, -7.894159318335828068, -9.358103419637847864 ) ) ;
#16530=EDGE_CURVE ( 'NONE', #1359, #37342, #28680, .T. ) ;
#16533=CARTESIAN_POINT ( 'NONE',  ( 118.9227414775786542, 0.4262465694468514643, -12.03445270309931736 ) ) ;
#16534=CARTESIAN_POINT ( 'NONE',  ( 112.3991748109119868, -1.833838273342658809, -17.42832698103878286 ) ) ;
#16535=CARTESIAN_POINT ( 'NONE',  ( 125.3895814775786448, -2.084020599724410339, -8.691656652584146769 ) ) ;
#16538=CARTESIAN_POINT ( 'NONE',  ( 120.5110881442453206, -3.505236298600246325, -18.68346056562440793 ) ) ;
#16539=CARTESIAN_POINT ( 'NONE',  ( 113.9875214775786532, -8.899110576539710493, -16.42337572283490132 ) ) ;
#16544=CARTESIAN_POINT ( 'NONE',  ( 123.3474214775786209, -9.988377603198976828, -10.36322818467138340 ) ) ;
#16545=CARTESIAN_POINT ( 'NONE',  ( 113.0231681442453322, 0.9020085738987339008, -11.91225656197089222 ) ) ;
#16550=CARTESIAN_POINT ( 'NONE',  ( 111.9453614775786434, -1.561330072975668060, -17.79121239304076596 ) ) ;
#16552=CARTESIAN_POINT ( 'NONE',  ( 120.0005481442453146, -4.153390946401325223, -8.397313243818185668 ) ) ;
#16555=CARTESIAN_POINT ( 'NONE',  ( 117.1074881442453233, -10.63000616557722111, -14.87417383870573850 ) ) ;
#16557=CARTESIAN_POINT ( 'NONE',  ( 112.9097148109120070, -9.565557343593413364, -10.61323700422348004 ) ) ;
#16559=CARTESIAN_POINT ( 'NONE',  ( 117.8449348109119938, -8.166667518702803719, -8.995218007635848778 ) ) ;
#16561=CARTESIAN_POINT ( 'NONE',  ( 124.1415948109119540, -6.344957434206665248, -7.627207830600338134 ) ) ;
#16562=CARTESIAN_POINT ( 'NONE',  ( 121.5321681442453183, -9.988377603198976828, -10.36322818467138340 ) ) ;
#16564=CARTESIAN_POINT ( 'NONE',  ( 121.1918081442452859, 0.9020085738987339008, -11.91225656197089222 ) ) ;
#16565=CARTESIAN_POINT ( 'NONE',  ( 112.1722681442453222, -0.4660016031367893996, -10.09054647747474043 ) ) ;
#16567=CARTESIAN_POINT ( 'NONE',  ( 114.7249681442453237, -9.565557343593413364, -10.61323700422348004 ) ) ;
#16568=CARTESIAN_POINT ( 'NONE',  ( 113.1366214775786432, -7.643976991954077427, -18.09477374809248928 ) ) ;
#16569=CARTESIAN_POINT ( 'NONE',  ( 123.6877814775786533, -3.383040157471821630, -19.15922257007629170 ) ) ;
#16570=CARTESIAN_POINT ( 'NONE',  ( 115.8595014775786609, -1.834011780172310813, -8.268836392978581529 ) ) ;
#16572=CARTESIAN_POINT ( 'NONE',  ( 113.8740681442453138, -9.859900752359374465, -12.68260735090039404 ) ) ;
#16574=CARTESIAN_POINT ( 'NONE',  ( 115.9729548109119861, -3.505236298600246325, -18.68346056562440793 ) ) ;
#16575=CARTESIAN_POINT ( 'NONE',  ( 111.8319081442453182, -5.638512984488999180, -18.83840828888717311 ) ) ;
#16577=CARTESIAN_POINT ( 'NONE',  ( 123.8012348109119642, -9.565557343593413364, -10.61323700422348004 ) ) ;
#16582=CARTESIAN_POINT ( 'NONE',  ( 126.0703014775786102, -9.988377603198980381, -10.36322818467138518 ) ) ;
#16588=( BOUNDED_CURVE ( )  B_SPLINE_CURVE ( 2, ( #10219, #2681, #23452, #40779, #16612 ),
 .UNSPECIFIED., .F., .T. ) 
 B_SPLINE_CURVE_WITH_KNOTS ( ( 3, 2, 3 ),
 ( 0.8125000000000000000, 0.8203125000000000000, 0.8266217583431409999 ),
 .UNSPECIFIED. ) 
 CURVE ( )  GEOMETRIC_REPRESENTATION_ITEM ( )  RATIONAL_B_SPLINE_CURVE ( ( 1.000000000000000000, 0.9238795325112859613, 1.000000000000000000, 0.9385262470928680267, 0.9763430640195970289 ) ) 
 REPRESENTATION_ITEM ( '' )  );
#16591=CARTESIAN_POINT ( 'NONE',  ( 116.5402214775786405, 0.2603800115204892296, -16.42320221600525088 ) ) ;
#16592=CARTESIAN_POINT ( 'NONE',  ( 135.8991650439206467, -4.137162889731972548, -19.29038791749874804 ) ) ;
#16596=CARTESIAN_POINT ( 'NONE',  ( 119.8870948109119752, -0.8288870151387760510, -10.36305467784173118 ) ) ;
#16599=CARTESIAN_POINT ( 'NONE',  ( 123.5743281442453139, -7.893985811506177619, -18.51759400769804742 ) ) ;
#16600=CARTESIAN_POINT ( 'NONE',  ( 120.0572748109119772, -3.383040157471821630, -19.15922257007629170 ) ) ;
#16601=CARTESIAN_POINT ( 'NONE',  ( 125.9001214775786224, -4.089484607189486809, -7.948022111789456723 ) ) ;
#16602=CARTESIAN_POINT ( 'NONE',  ( 112.3991748109119868, -1.833838273342658809, -17.42832698103878286 ) ) ;
#16603=CARTESIAN_POINT ( 'NONE',  ( 122.8368814775786291, -1.561330072975668948, -17.79121239304076951 ) ) ;
#16607=CARTESIAN_POINT ( 'NONE',  ( 115.3489614775786407, -0.8288870151387760510, -10.36305467784173118 ) ) ;
#16608=CARTESIAN_POINT ( 'NONE',  ( 117.8449348109119938, -1.833838273342659253, -17.42832698103878286 ) ) ;
#16612=CARTESIAN_POINT ( 'NONE',  ( 124.1773369107181821, -2.467220198592779301, -17.83387418641524391 ) ) ;
#16613=CARTESIAN_POINT ( 'NONE',  ( 113.8740681442453138, 0.5811942927096154232, -14.16772938898807155 ) ) ;
#16617=ORIENTED_EDGE ( 'NONE', *, *, #17538, .F. ) ;
#16621=CARTESIAN_POINT ( 'NONE',  ( 118.9227414775786400, -10.63000616557722466, -14.87417383870573495 ) ) ;
#16622=CARTESIAN_POINT ( 'NONE',  ( 124.3117748109119844, 0.1319031606808879209, -14.10382304977623669 ) ) ;
#16623=CARTESIAN_POINT ( 'NONE',  ( 119.6034614775786196, -3.505236298600246325, -18.68346056562440793 ) ) ;
#16625=CARTESIAN_POINT ( 'NONE',  ( 123.0070614775786169, 0.9020085738987339008, -11.91225656197089222 ) ) ;
#16626=CARTESIAN_POINT ( 'NONE',  ( 119.7169148109119874, -9.988377603198976828, -10.36322818467138340 ) ) ;
#16629=CARTESIAN_POINT ( 'NONE',  ( 112.9097148109120070, -9.565557343593413364, -10.61323700422348004 ) ) ;
#16630=LINE ( 'NONE', #19816, #9747 ) ;
#16632=CARTESIAN_POINT ( 'NONE',  ( 116.9940348109119839, -9.988377603198976828, -10.36322818467138340 ) ) ;
#16633=CARTESIAN_POINT ( 'NONE',  ( 114.4980614775786734, -2.084020599724406786, -8.691656652584148546 ) ) ;
#16635=CARTESIAN_POINT ( 'NONE',  ( 125.8433948109119456, -7.643976991954077427, -18.09477374809248928 ) ) ;
#16636=ORIENTED_EDGE ( 'NONE', *, *, #39615, .F. ) ;
#16637=CARTESIAN_POINT ( 'NONE',  ( 121.0783548109119749, 0.2603800115204892296, -16.42320221600525088 ) ) ;
#16639=FACE_OUTER_BOUND ( 'NONE', #19246, .T. ) ;
#16640=CARTESIAN_POINT ( 'NONE',  ( 125.0483885810856890, -1.220279397241718966, -16.99638242193886484 ) ) ;
#16642=CARTESIAN_POINT ( 'NONE',  ( 114.4980614775786734, -2.084020599724406786, -8.691656652584148546 ) ) ;
#16643=CARTESIAN_POINT ( 'NONE',  ( 136.2632467228237374, -2.605123477878678706, -8.005467003093405864 ) ) ;
#16644=CARTESIAN_POINT ( 'NONE',  ( 118.4689281442453250, -10.15424416112533912, -14.75197769757731336 ) ) ;
#16646=CARTESIAN_POINT ( 'NONE',  ( 115.0653281442453277, -3.505236298600246325, -18.68346056562440793 ) ) ;
#16647=CARTESIAN_POINT ( 'NONE',  ( 117.3911214775786505, -1.561330072975668504, -17.79121239304076951 ) ) ;
#16649=CARTESIAN_POINT ( 'NONE',  ( 112.0020881442453344, 0.2603800115204892296, -16.42320221600525088 ) ) ;
#16650=CARTESIAN_POINT ( 'NONE',  ( 114.7816948109119863, -9.859900752359374465, -12.68260735090039404 ) ) ;
#16651=CARTESIAN_POINT ( 'NONE',  ( 123.9146881442452894, 0.9020085738987339008, -11.91225656197089222 ) ) ;
#16652=CARTESIAN_POINT ( 'NONE',  ( 115.4624148109119943, -4.153390946401321671, -8.397313243818183892 ) ) ;
#16654=CARTESIAN_POINT ( 'NONE',  ( 112.7395348109119766, -5.638512984488999180, -18.83840828888717311 ) ) ;
#16660=CARTESIAN_POINT ( 'NONE',  ( 120.5678148109119832, -8.166667518702819706, -8.995218007635861213 ) ) ;
#16662=CARTESIAN_POINT ( 'NONE',  ( 125.7866681442452688, -0.4660016031367893996, -10.09054647747474043 ) ) ;
#16664=CARTESIAN_POINT ( 'NONE',  ( 115.1220548109119761, -1.833838273342658809, -17.42832698103878286 ) ) ;
#16665=CARTESIAN_POINT ( 'NONE',  ( 124.4252281442452812, -0.8288870151387603968, -10.36305467784175072 ) ) ;
#16666=CARTESIAN_POINT ( 'NONE',  ( 124.7655881442452852, 0.5811942927096110934, -14.16772938898807510 ) ) ;
#16670=CARTESIAN_POINT ( 'NONE',  ( 112.3991748109119868, -8.166667518702817929, -8.995218007635859436 ) ) ;
#16671=CARTESIAN_POINT ( 'NONE',  ( 122.3263414775786373, -3.505236298600246325, -18.68346056562440793 ) ) ;
#16672=CARTESIAN_POINT ( 'NONE',  ( 119.7169148109119874, -9.988377603198976828, -10.36322818467138340 ) ) ;
#16673=CARTESIAN_POINT ( 'NONE',  ( 114.0442481442453300, -7.643976991954077427, -18.09477374809248928 ) ) ;
#16674=( BOUNDED_CURVE ( )  B_SPLINE_CURVE ( 2, ( #9676, #6710, #21051, #16979, #27236, #20397, #34928, #44792, #13550, #20619, #34496, #42775, #11757, #18595, #4227, #11307, #8335 ),
 .UNSPECIFIED., .F., .T. ) 
 B_SPLINE_CURVE_WITH_KNOTS ( ( 3, 2, 2, 2, 2, 2, 2, 2, 3 ),
 ( 0.2045046674808919940, 0.2109375000000000000, 0.2187500000000000000, 0.2265625000000000000, 0.2343750000000000000, 0.2421875000000000000, 0.2500000000000000000, 0.2578125000000000000, 0.2642453325190585178 ),
 .UNSPECIFIED. ) 
 CURVE ( )  GEOMETRIC_REPRESENTATION_ITEM ( )  RATIONAL_B_SPLINE_CURVE ( ( 0.9778625265006459788, 0.9373222120152210346, 1.000000000000000000, 0.9238795325112869605, 1.000000000000000000, 0.9238795325112869605, 1.000000000000000000, 0.9238795325112869605, 1.000000000000000000, 0.9238795325112869605, 1.000000000000000000, 0.9238795325112869605, 1.000000000000000000, 0.9238795325112869605, 1.000000000000000000, 0.9373222120157009840, 0.9778625265000250311 ) ) 
 REPRESENTATION_ITEM ( '' )  );
#16675=CARTESIAN_POINT ( 'NONE',  ( 114.9518748109119883, -1.834011780172310813, -8.268836392978581529 ) ) ;
#16678=CARTESIAN_POINT ( 'NONE',  ( 127.7617783745703974, -1.248496758771796999, -8.893780266587674177 ) ) ;
#16679=CARTESIAN_POINT ( 'NONE',  ( 120.0005481442453146, -4.153390946401325223, -8.397313243818185668 ) ) ;
#16684=CARTESIAN_POINT ( 'NONE',  ( 112.4559014775786494, -9.988377603198976828, -10.36322818467138340 ) ) ;
#16685=CARTESIAN_POINT ( 'NONE',  ( 123.0070614775786169, -10.15424416112533912, -14.75197769757731336 ) ) ;
#16688=CARTESIAN_POINT ( 'NONE',  ( 136.5847729262691246, -1.254589541683206688, -8.968780776681423816 ) ) ;
#16690=CARTESIAN_POINT ( 'NONE',  ( 118.0151148109119816, -10.63000616557722466, -14.87417383870573495 ) ) ;
#16692=CARTESIAN_POINT ( 'NONE',  ( 117.9583881442453048, 0.1319031606808879209, -14.10382304977623669 ) ) ;
#16695=CARTESIAN_POINT ( 'NONE',  ( 126.1837548109119496, 0.4262465694468514643, -12.03445270309931736 ) ) ;
#16697=CARTESIAN_POINT ( 'NONE',  ( 124.9924948109119924, -5.574606645277164318, -18.38911715685844683 ) ) ;
#16700=CARTESIAN_POINT ( 'NONE',  ( 122.2128881442453263, -1.834011780172310813, -8.268836392978581529 ) ) ;
#16702=CYLINDRICAL_SURFACE ( 'NONE', #34265, 1.999999999999998890 ) ;
#16704=CARTESIAN_POINT ( 'NONE',  ( 120.5110881442453206, -6.344957434206665248, -7.627207830600338134 ) ) ;
#16705=CARTESIAN_POINT ( 'NONE',  ( 119.5467348109119712, -4.089484607189486809, -7.948022111789456723 ) ) ;
#16706=CARTESIAN_POINT ( 'NONE',  ( 120.3976348109119812, -7.643976991954077427, -18.09477374809248928 ) ) ;
#16707=CARTESIAN_POINT ( 'NONE',  ( 125.7866681442452688, -8.899110576539710493, -16.42337572283490132 ) ) ;
#16708=CARTESIAN_POINT ( 'NONE',  ( 112.2289948109119848, -1.834011780172310813, -8.268836392978581529 ) ) ;
#16711=CARTESIAN_POINT ( 'NONE',  ( 123.9146881442452894, -10.15424416112533912, -14.75197769757731336 ) ) ;
#16712=CARTESIAN_POINT ( 'NONE',  ( 122.2862319737025416, -1.196538596002817867, -17.02799684832028504 ) ) ;
#16718=CARTESIAN_POINT ( 'NONE',  ( 122.0994348109119443, 0.9020085738987339008, -11.91225656197089222 ) ) ;
#16719=CARTESIAN_POINT ( 'NONE',  ( 121.6456214775786293, 0.4262465694468514643, -12.03445270309931736 ) ) ;
#16721=CARTESIAN_POINT ( 'NONE',  ( 125.5597614775786326, -1.561330072975669392, -17.79121239304076951 ) ) ;
#16723=CARTESIAN_POINT ( 'NONE',  ( 121.7590748109119687, -2.084020599724363265, -8.691656652584173415 ) ) ;
#16724=CARTESIAN_POINT ( 'NONE',  ( 119.6034614775786196, -6.344957434206665248, -7.627207830600338134 ) ) ;
#16725=CARTESIAN_POINT ( 'NONE',  ( 122.7801548109119665, -3.383040157471821630, -19.15922257007629170 ) ) ;
#16727=CARTESIAN_POINT ( 'NONE',  ( 112.3424481442453384, -6.344957434206662583, -7.627207830600332805 ) ) ;
#16731=CARTESIAN_POINT ( 'NONE',  ( 112.9097148109120070, -9.565557343593413364, -10.61323700422348004 ) ) ;
#16732=CARTESIAN_POINT ( 'NONE',  ( 124.9924948109119924, -5.574606645277164318, -18.38911715685844683 ) ) ;
#16736=CARTESIAN_POINT ( 'NONE',  ( 117.9583881442453048, 0.1319031606808879209, -14.10382304977623669 ) ) ;
#16739=CARTESIAN_POINT ( 'NONE',  ( 114.4413348109119823, -0.8288870151387760510, -10.36305467784173118 ) ) ;
#16740=CARTESIAN_POINT ( 'NONE',  ( 124.0281414775786146, -1.834011780172310813, -8.268836392978581529 ) ) ;
#16743=CARTESIAN_POINT ( 'NONE',  ( 121.1918081442452859, -10.15424416112533912, -14.75197769757731336 ) ) ;
#16744=CARTESIAN_POINT ( 'NONE',  ( 117.3911214775786505, -1.561330072975668504, -17.79121239304076951 ) ) ;
#16745=CARTESIAN_POINT ( 'NONE',  ( 125.5597614775786326, -1.561330072975669392, -17.79121239304076951 ) ) ;
#16746=CARTESIAN_POINT ( 'NONE',  ( 125.2194014775786286, 0.1319031606808879209, -14.10382304977623669 ) ) ;
#16749=CARTESIAN_POINT ( 'NONE',  ( 122.3830681442452857, -8.166667518702819706, -8.995218007635861213 ) ) ;
#16750=CARTESIAN_POINT ( 'NONE',  ( 116.4834948109119779, -7.894159318335828068, -9.358103419637847864 ) ) ;
#16751=CARTESIAN_POINT ( 'NONE',  ( 125.4463081442452932, -5.638512984488999180, -18.83840828888717311 ) ) ;
#16752=CARTESIAN_POINT ( 'NONE',  ( 117.6791703192116927, -2.378957183258571639, -17.95140958770219086 ) ) ;
#16760=CARTESIAN_POINT ( 'NONE',  ( 123.6310548109119765, -4.153390946401325223, -8.397313243818185668 ) ) ;
#16761=CARTESIAN_POINT ( 'NONE',  ( 114.1009748109119784, -5.574606645277164318, -18.38911715685844683 ) ) ;
#16762=CARTESIAN_POINT ( 'NONE',  ( 126.5621572003788344, -0.3458538473703972604, -10.87540104374022576 ) ) ;
#16765=CARTESIAN_POINT ( 'NONE',  ( 119.2063748109119814, -7.894159318335828068, -9.358103419637847864 ) ) ;
#16766=CARTESIAN_POINT ( 'NONE',  ( 114.2144281442453178, -1.833838273342658809, -17.42832698103878286 ) ) ;
#16769=CARTESIAN_POINT ( 'NONE',  ( 111.7289948109120132, -2.109465145232937378, -8.734689011829464889 ) ) ;
#16771=CARTESIAN_POINT ( 'NONE',  ( 124.7655881442452852, 0.5811942927096110934, -14.16772938898807510 ) ) ;
#16772=CARTESIAN_POINT ( 'NONE',  ( 112.6828081442453282, -7.893985811506177619, -18.51759400769804742 ) ) ;
#16775=CARTESIAN_POINT ( 'NONE',  ( 113.9307948109119906, 0.9020085738987339008, -11.91225656197089222 ) ) ;
#16780=CARTESIAN_POINT ( 'NONE',  ( 124.7655881442452852, -9.859900752359378018, -12.68260735090039759 ) ) ;
#16781=CARTESIAN_POINT ( 'NONE',  ( 122.4397948109119767, -0.1624402480850797581, -16.17319339645315424 ) ) ;
#16784=DIRECTION ( 'NONE',  ( 0.000000000000000000, 0.6004852223388321697, -0.7996358532186279566 ) ) ;
#16785=CARTESIAN_POINT ( 'NONE',  ( 113.2384448136183721, -3.929494816604734098, -18.62311481910882804 ) ) ;
#16787=CARTESIAN_POINT ( 'NONE',  ( 117.6747548109119776, -1.834011780172314143, -8.268836392978577976 ) ) ;
#16789=CARTESIAN_POINT ( 'NONE',  ( 123.0070614775786169, 0.9020085738987339008, -11.91225656197089222 ) ) ;
#16790=CARTESIAN_POINT ( 'NONE',  ( 123.5743281442453139, -7.893985811506177619, -18.51759400769804742 ) ) ;
#16791=CARTESIAN_POINT ( 'NONE',  ( 151.2860562277021472, -3.410847707154505137, -16.57729307524250828 ) ) ;
#16792=CARTESIAN_POINT ( 'NONE',  ( 119.3198281442452924, 0.5811942927096110934, -14.16772938898807510 ) ) ;
#16795=CARTESIAN_POINT ( 'NONE',  ( 114.8384214775786489, -10.15424416112533912, -14.75197769757731336 ) ) ;
#16796=CARTESIAN_POINT ( 'NONE',  ( 125.3895814775786448, -7.893985811506177619, -18.51759400769804742 ) ) ;
#16797=CARTESIAN_POINT ( 'NONE',  ( 122.0994348109119443, 0.9020085738987339008, -11.91225656197089222 ) ) ;
#16799=CARTESIAN_POINT ( 'NONE',  ( 114.3278814775786429, -10.30919188438810075, -12.61870101168855918 ) ) ;
#16800=CARTESIAN_POINT ( 'NONE',  ( 111.3780948109119890, -5.574606645277164318, -18.38911715685844683 ) ) ;
#16801=VERTEX_POINT ( 'NONE', #27264 ) ;
#16803=CARTESIAN_POINT ( 'NONE',  ( 116.3700414775786527, -4.153390946401321671, -8.397313243818183892 ) ) ;
#16804=CARTESIAN_POINT ( 'NONE',  ( 113.0231681442453322, 0.9020085738987339008, -11.91225656197089222 ) ) ;
#16807=CARTESIAN_POINT ( 'NONE',  ( 122.3263414775786373, -3.505236298600246325, -18.68346056562440793 ) ) ;
#16813=CARTESIAN_POINT ( 'NONE',  ( 111.2184548109119788, -2.495269033102075262, -17.79652296963211455 ) ) ;
#16815=CARTESIAN_POINT ( 'NONE',  ( 112.0020881442453344, 0.2603800115204892296, -16.42320221600525088 ) ) ;
#16819=CARTESIAN_POINT ( 'NONE',  ( 115.1430393777725385, -1.267766418764730840, -16.93314635290706605 ) ) ;
#16820=CARTESIAN_POINT ( 'NONE',  ( 118.4122014775786340, 0.5811942927096110934, -14.16772938898807510 ) ) ;
#16821=CARTESIAN_POINT ( 'NONE',  ( 136.6694018951665157, -6.970064029879566192, -18.66362485201299748 ) ) ;
#16824=CARTESIAN_POINT ( 'NONE',  ( 124.4819548109119722, -7.893985811506177619, -18.51759400769804742 ) ) ;
#16825=CARTESIAN_POINT ( 'NONE',  ( 122.1561614775786353, -8.899110576539710493, -16.42337572283490132 ) ) ;
#16827=CARTESIAN_POINT ( 'NONE',  ( 125.6732148109119862, 0.5811942927096110934, -14.16772938898807510 ) ) ;
#16828=CARTESIAN_POINT ( 'NONE',  ( 119.0929214775786278, -5.638512984488999180, -18.83840828888717311 ) ) ;
#16830=CARTESIAN_POINT ( 'NONE',  ( 116.4267681442453153, -6.222761293078241884, -8.102969835052219238 ) ) ;
#16831=CARTESIAN_POINT ( 'NONE',  ( 122.6667014775786413, -7.893985811506177619, -18.51759400769804742 ) ) ;
#16835=CARTESIAN_POINT ( 'NONE',  ( 116.1998614775786507, 0.4262465694468514643, -12.03445270309931736 ) ) ;
#16837=CARTESIAN_POINT ( 'NONE',  ( 117.3343948109119737, -6.222761293078241884, -8.102969835052219238 ) ) ;
#16843=CARTESIAN_POINT ( 'NONE',  ( 113.0231681442453322, 0.9020085738987339008, -11.91225656197089222 ) ) ;
#16844=CARTESIAN_POINT ( 'NONE',  ( 122.9742476054816080, -2.287189184988711155, -18.07361239780447448 ) ) ;
#16851=CARTESIAN_POINT ( 'NONE',  ( 118.4122014775786340, 0.5811942927096110934, -14.16772938898807510 ) ) ;
#16852=CARTESIAN_POINT ( 'NONE',  ( 113.5337081442453240, -9.261995988541697145, -16.69588392320189030 ) ) ;
#16854=CARTESIAN_POINT ( 'NONE',  ( 120.0005481442453146, -4.153390946401325223, -8.397313243818185668 ) ) ;
#16856=CARTESIAN_POINT ( 'NONE',  ( 121.0216281442452981, -1.561330072975668948, -17.79121239304076951 ) ) ;
#16857=CARTESIAN_POINT ( 'NONE',  ( 117.5045748109119756, 0.5811942927096110934, -14.16772938898807510 ) ) ;
#16860=CARTESIAN_POINT ( 'NONE',  ( 112.7962614775786676, -6.222761293078241884, -8.102969835052219238 ) ) ;
#16862=VERTEX_POINT ( 'NONE', #6737 ) ;
#16863=( BOUNDED_SURFACE ( )  B_SPLINE_SURFACE ( 1, 2, ( 
 ( #4094, #25318, #39212, #7977, #31914, #14597, #21885, #18696, #28517, #35781, #28961, #24638, #38520, #7298, #23241, #8431, #32801, #22777, #22337, #18910, #26658, #43313, #25987, #5444, #12534, #12081, #12310, #15950, #36674, #26207, #43995, #1573, #5896, #33469, #26435, #1796, #9105, #36232, #19819, #39892, #40572, #33022, #15723, #19364, #4997, #30081, #5223, #12757, #40342, #8653, #9332, #8878, #29853, #33705, #2249, #23007, #37122, #15265, #15494, #29175, #29401, #33253, #36899, #22554, #43087, #19139, #5670, #19587, #11855, #25762, #39668, #36454, #16178, #29625, #43540, #40114, #2025, #43768, #12987, #33934, #10463, #41037, #2477, #16402, #20050, #27345, #27568, #41482, #10022, #24365, #24148, #41264, #17086, #16632, #30526, #2934, #27113, #34602, #13440, #38040, #30755, #10239, #31197, #17307, #16864, #20276, #23474, #2703, #44903, #40802, #20943, #44677, #37360, #23931, #37811, #6586, #3387, #9794, #6131, #6815, #13661, #44448, #20504, #20723, #13215, #45117, #13875, #23704, #34383, #3164, #30978, #37593, #6366, #27785, #41699, #34162, #38251, #7031, #30300, #44227, #26883, #9558, #28013, #7245, #42367, #41918, #38469, #1690, #17739, #405, #25028, #32696, #31636, #31862, #35496, #11128, #629, #19027, #21158, #26095, #8546, #1465, #8765, #35263, #38923, #35033, #10683, #12197, #14094, #25872, #31412, #24585, #7693, #4268, #18187, #15389, #178, #21608, #29292, #43206, #11973, #39776, #3816, #22447, #17962, #36339, #4041, #5110, #14320, #32912, #15609, #29516, #28236, #34817, #43430, #40000, #3600, #42143, #17513, #10904, #24804, #38696, #14541, #7462, #21380, #28458, #13101, #37477, #37012, #30422, #23134, #6251, #40463, #26551, #33360, #33823, #44342, #43648, #6012, #40690, #26782, #41150, #2593, #23593, #29969, #13328, #12655, #20172, #22671, #12424, #16296, #27003, #40921, #36567, #44115, #19702, #5343, #9443, #9675, #34056, #9225, #2822, #16751, #30647, #27235, #44565, #19260, #33139, #5781, #12881, #1911, #8999, #33590, #2365, #23355, #40232, #22895 ),
 ( #15839, #29737, #36790, #30196, #26325, #5560, #19480, #2133, #16063, #37241, #19936, #43884, #16524, #10577, #31305, #20831, #38582, #41381, #525, #28128, #21050, #28344, #41598, #3714, #3052, #14437, #27905, #3497, #31755, #9911, #6709, #17196, #16978, #34713, #78, #38365, #34927, #27684, #24475, #20618, #10355, #13991, #13549, #30869, #23824, #34279, #300, #6481, #44791, #41820, #7139, #17634, #31530, #20395, #14213, #42037, #10797, #24693, #7360, #10136, #21275, #38152, #35157, #24263, #3937, #34495, #17857, #17414, #37711, #3271, #27460, #24041, #37933, #31088, #45015, #13773, #6926, #4164, #11022, #25381, #25818, #29020, #32425, #32646, #11919, #11476, #4837, #42707, #39727, #14889, #973, #7821, #8267, #18757, #18081, #25601, #15111, #1198, #15555, #22172, #43150, #4390, #32865, #32200, #8494, #42257, #31975, #35839, #1414, #15332, #24922, #18534, #39278, #38817, #42930, #29242, #22397, #28800, #36292, #5060, #18976, #1635, #7586, #21500, #35387, #8042, #11692, #738, #28577, #21948, #4612, #39506, #14661, #42484, #25154, #36067, #11246, #39050, #21729, #35616, #18305, #26945, #43599, #40868, #43833, #19425, #9622, #12600, #19206, #5729, #12827, #12144, #5959, #23075, #12371, #26272, #29918, #8945, #16467, #40411, #19884, #26502, #37185, #13046, #44292, #9171, #2086, #5291, #1856, #26725, #22618, #2772, #36958, #33085, #19648, #33535, #2313, #30371, #22846, #15785, #33771, #40634, #40179, #16243, #2540, #36738, #23544, #37426, #29687, #30145, #44060, #9391, #5504, #33311, #23301, #6196, #16011, #20116, #34002, #29461, #43375, #26047, #39951, #36518, #8713, #24208, #9858, #20342, #28073, #44741, #27407, #6874, #13939, #13501, #13722, #17366, #38100, #27630, #248, #2998, #7305, #34874, #27852, #35100, #3221, #10522, #23767, #21223, #41328, #41981, #34442, #17148, #20783, #6431, #31475, #6653, #14156, #41762, #10086, #10746, #10306, #31255, #16697, #3662, #24423, #24645, #38529, #34225, #30590, #16923, #34662, #38313, #30818, #44509, #20563, #7090, #21000 ) ),
 .UNSPECIFIED., .F., .F., .T. ) 
 B_SPLINE_SURFACE_WITH_KNOTS ( ( 2, 2 ),
 ( 3, 2, 2, 2, 2, 2, 2, 2, 2, 2, 2, 2, 2, 2, 2, 2, 2, 2, 2, 2, 2, 2, 2, 2, 2, 2, 2, 2, 2, 2, 2, 2, 2, 2, 2, 2, 2, 2, 2, 2, 2, 2, 2, 2, 2, 2, 2, 2, 2, 2, 2, 2, 2, 2, 2, 2, 2, 2, 2, 2, 2, 2, 2, 2, 2, 2, 2, 2, 2, 2, 2, 2, 2, 2, 2, 2, 2, 2, 2, 2, 2, 2, 2, 2, 2, 2, 2, 2, 2, 2, 2, 2, 2, 2, 2, 2, 2, 2, 2, 2, 2, 2, 2, 2, 2, 2, 2, 2, 2, 2, 2, 2, 2, 2, 2, 2, 2, 2, 2, 2, 2, 2, 2, 2, 2, 2, 2, 2, 3 ),
 ( 0.000000000000000000, 1.000000000000000000 ),
 ( 0.000000000000000000, 0.007812500000000000000, 0.01562500000000000000, 0.02343750000000000000, 0.03125000000000000000, 0.03906250000000000000, 0.04687500000000000000, 0.05468750000000000000, 0.06250000000000000000, 0.07031250000000000000, 0.07812500000000000000, 0.08593750000000000000, 0.09375000000000000000, 0.1015625000000000000, 0.1093750000000000000, 0.1171875000000000000, 0.1250000000000000000, 0.1328125000000000000, 0.1406250000000000000, 0.1484375000000000000, 0.1562500000000000000, 0.1640625000000000000, 0.1718750000000000000, 0.1796875000000000000, 0.1875000000000000000, 0.1953125000000000000, 0.2031250000000000000, 0.2109375000000000000, 0.2187500000000000000, 0.2265625000000000000, 0.2343750000000000000, 0.2421875000000000000, 0.2500000000000000000, 0.2578125000000000000, 0.2656250000000000000, 0.2734375000000000000, 0.2812500000000000000, 0.2890625000000000000, 0.2968750000000000000, 0.3046875000000000000, 0.3125000000000000000, 0.3203125000000000000, 0.3281250000000000000, 0.3359375000000000000, 0.3437500000000000000, 0.3515625000000000000, 0.3593750000000000000, 0.3671875000000000000, 0.3750000000000000000, 0.3828125000000000000, 0.3906250000000000000, 0.3984375000000000000, 0.4062500000000000000, 0.4140625000000000000, 0.4218750000000000000, 0.4296875000000000000, 0.4375000000000000000, 0.4453125000000000000, 0.4531250000000000000, 0.4609375000000000000, 0.4687500000000000000, 0.4765625000000000000, 0.4843750000000000000, 0.4921875000000000000, 0.5000000000000000000, 0.5078125000000000000, 0.5156250000000000000, 0.5234375000000000000, 0.5312500000000000000, 0.5390625000000000000, 0.5468750000000000000, 0.5546875000000000000, 0.5625000000000000000, 0.5703125000000000000, 0.5781250000000000000, 0.5859375000000000000, 0.5937500000000000000, 0.6015625000000000000, 0.6093750000000000000, 0.6171875000000000000, 0.6250000000000000000, 0.6328125000000000000, 0.6406250000000000000, 0.6484375000000000000, 0.6562500000000000000, 0.6640625000000000000, 0.6718750000000000000, 0.6796875000000000000, 0.6875000000000000000, 0.6953125000000000000, 0.7031250000000000000, 0.7109375000000000000, 0.7187500000000000000, 0.7265625000000000000, 0.7343750000000000000, 0.7421875000000000000, 0.7500000000000000000, 0.7578125000000000000, 0.7656250000000000000, 0.7734375000000000000, 0.7812500000000000000, 0.7890625000000000000, 0.7968750000000000000, 0.8046875000000000000, 0.8125000000000000000, 0.8203125000000000000, 0.8281250000000000000, 0.8359375000000000000, 0.8437500000000000000, 0.8515625000000000000, 0.8593750000000000000, 0.8671875000000000000, 0.8750000000000000000, 0.8828125000000000000, 0.8906250000000000000, 0.8984375000000000000, 0.9062500000000000000, 0.9140625000000000000, 0.9218750000000000000, 0.9296875000000000000, 0.9375000000000000000, 0.9453125000000000000, 0.9531250000000000000, 0.9609375000000000000, 0.9687500000000000000, 0.9765625000000000000, 0.9843750000000000000, 0.9921875000000000000, 1.000000000000000000 ),
 .UNSPECIFIED. ) 
 GEOMETRIC_REPRESENTATION_ITEM ( )  RATIONAL_B_SPLINE_SURFACE ( (
 ( 1.000000000000000000, 0.9238795325112869605, 1.000000000000000000, 0.9238795325112869605, 1.000000000000000000, 0.9238795325112869605, 1.000000000000000000, 0.9238795325112869605, 1.000000000000000000, 0.9238795325112869605, 1.000000000000000000, 0.9238795325112869605, 1.000000000000000000, 0.9238795325112869605, 1.000000000000000000, 0.9238795325112869605, 1.000000000000000000, 0.9238795325112869605, 1.000000000000000000, 0.9238795325112869605, 1.000000000000000000, 0.9238795325112869605, 1.000000000000000000, 0.9238795325112869605, 1.000000000000000000, 0.9238795325112869605, 1.000000000000000000, 0.9238795325112869605, 1.000000000000000000, 0.9238795325112869605, 1.000000000000000000, 0.9238795325112869605, 1.000000000000000000, 0.9238795325112869605, 1.000000000000000000, 0.9238795325112869605, 1.000000000000000000, 0.9238795325112869605, 1.000000000000000000, 0.9238795325112869605, 1.000000000000000000, 0.9238795325112869605, 1.000000000000000000, 0.9238795325112869605, 1.000000000000000000, 0.9238795325112869605, 1.000000000000000000, 0.9238795325112869605, 1.000000000000000000, 0.9238795325112869605, 1.000000000000000000, 0.9238795325112869605, 1.000000000000000000, 0.9238795325112869605, 1.000000000000000000, 0.9238795325112869605, 1.000000000000000000, 0.9238795325112869605, 1.000000000000000000, 0.9238795325112869605, 1.000000000000000000, 0.9238795325112869605, 1.000000000000000000, 0.9238795325112869605, 1.000000000000000000, 0.9238795325112869605, 1.000000000000000000, 0.9238795325112869605, 1.000000000000000000, 0.9238795325112869605, 1.000000000000000000, 0.9238795325112869605, 1.000000000000000000, 0.9238795325112869605, 1.000000000000000000, 0.9238795325112869605, 1.000000000000000000, 0.9238795325112869605, 1.000000000000000000, 0.9238795325112869605, 1.000000000000000000, 0.9238795325112869605, 1.000000000000000000, 0.9238795325112869605, 1.000000000000000000, 0.9238795325112869605, 1.000000000000000000, 0.9238795325112869605, 1.000000000000000000, 0.9238795325112869605, 1.000000000000000000, 0.9238795325112869605, 1.000000000000000000, 0.9238795325112869605, 1.000000000000000000, 0.9238795325112869605, 1.000000000000000000, 0.9238795325112869605, 1.000000000000000000, 0.9238795325112869605, 1.000000000000000000, 0.9238795325112869605, 1.000000000000000000, 0.9238795325112869605, 1.000000000000000000, 0.9238795325112869605, 1.000000000000000000, 0.9238795325112869605, 1.000000000000000000, 0.9238795325112869605, 1.000000000000000000, 0.9238795325112869605, 1.000000000000000000, 0.9238795325112869605, 1.000000000000000000, 0.9238795325112869605, 1.000000000000000000, 0.9238795325112869605, 1.000000000000000000, 0.9238795325112869605, 1.000000000000000000, 0.9238795325112869605, 1.000000000000000000, 0.9238795325112869605, 1.000000000000000000, 0.9238795325112869605, 1.000000000000000000, 0.9238795325112869605, 1.000000000000000000, 0.9238795325112869605, 1.000000000000000000, 0.9238795325112869605, 1.000000000000000000, 0.9238795325112869605, 1.000000000000000000, 0.9238795325112869605, 1.000000000000000000, 0.9238795325112869605, 1.000000000000000000, 0.9238795325112869605, 1.000000000000000000, 0.9238795325112869605, 1.000000000000000000, 0.9238795325112869605, 1.000000000000000000, 0.9238795325112869605, 1.000000000000000000, 0.9238795325112869605, 1.000000000000000000, 0.9238795325112869605, 1.000000000000000000, 0.9238795325112869605, 1.000000000000000000, 0.9238795325112869605, 1.000000000000000000, 0.9238795325112869605, 1.000000000000000000, 0.9238795325112869605, 1.000000000000000000, 0.9238795325112869605, 1.000000000000000000, 0.9238795325112869605, 1.000000000000000000, 0.9238795325112869605, 1.000000000000000000, 0.9238795325112869605, 1.000000000000000000, 0.9238795325112869605, 1.000000000000000000, 0.9238795325112869605, 1.000000000000000000, 0.9238795325112869605, 1.000000000000000000, 0.9238795325112869605, 1.000000000000000000, 0.9238795325112869605, 1.000000000000000000, 0.9238795325112869605, 1.000000000000000000, 0.9238795325112869605, 1.000000000000000000, 0.9238795325112869605, 1.000000000000000000, 0.9238795325112869605, 1.000000000000000000, 0.9238795325112869605, 1.000000000000000000, 0.9238795325112869605, 1.000000000000000000, 0.9238795325112869605, 1.000000000000000000, 0.9238795325112869605, 1.000000000000000000, 0.9238795325112869605, 1.000000000000000000, 0.9238795325112869605, 1.000000000000000000, 0.9238795325112869605, 1.000000000000000000, 0.9238795325112869605, 1.000000000000000000, 0.9238795325112869605, 1.000000000000000000, 0.9238795325112869605, 1.000000000000000000, 0.9238795325112869605, 1.000000000000000000, 0.9238795325112869605, 1.000000000000000000, 0.9238795325112869605, 1.000000000000000000, 0.9238795325112869605, 1.000000000000000000, 0.9238795325112869605, 1.000000000000000000, 0.9238795325112869605, 1.000000000000000000, 0.9238795325112869605, 1.000000000000000000, 0.9238795325112869605, 1.000000000000000000, 0.9238795325112869605, 1.000000000000000000, 0.9238795325112869605, 1.000000000000000000, 0.9238795325112869605, 1.000000000000000000, 0.9238795325112869605, 1.000000000000000000, 0.9238795325112869605, 1.000000000000000000, 0.9238795325112869605, 1.000000000000000000, 0.9238795325112869605, 1.000000000000000000, 0.9238795325112869605, 1.000000000000000000, 0.9238795325112869605, 1.000000000000000000, 0.9238795325112869605, 1.000000000000000000, 0.9238795325112869605, 1.000000000000000000, 0.9238795325112869605, 1.000000000000000000, 0.9238795325112869605, 1.000000000000000000, 0.9238795325112869605, 1.000000000000000000, 0.9238795325112869605, 1.000000000000000000, 0.9238795325112869605, 1.000000000000000000, 0.9238795325112869605, 1.000000000000000000, 0.9238795325112869605, 1.000000000000000000),
 ( 1.000000000000000000, 0.9238795325112869605, 1.000000000000000000, 0.9238795325112869605, 1.000000000000000000, 0.9238795325112869605, 1.000000000000000000, 0.9238795325112869605, 1.000000000000000000, 0.9238795325112869605, 1.000000000000000000, 0.9238795325112869605, 1.000000000000000000, 0.9238795325112869605, 1.000000000000000000, 0.9238795325112869605, 1.000000000000000000, 0.9238795325112869605, 1.000000000000000000, 0.9238795325112869605, 1.000000000000000000, 0.9238795325112869605, 1.000000000000000000, 0.9238795325112869605, 1.000000000000000000, 0.9238795325112869605, 1.000000000000000000, 0.9238795325112869605, 1.000000000000000000, 0.9238795325112869605, 1.000000000000000000, 0.9238795325112869605, 1.000000000000000000, 0.9238795325112869605, 1.000000000000000000, 0.9238795325112869605, 1.000000000000000000, 0.9238795325112869605, 1.000000000000000000, 0.9238795325112869605, 1.000000000000000000, 0.9238795325112869605, 1.000000000000000000, 0.9238795325112869605, 1.000000000000000000, 0.9238795325112869605, 1.000000000000000000, 0.9238795325112869605, 1.000000000000000000, 0.9238795325112869605, 1.000000000000000000, 0.9238795325112869605, 1.000000000000000000, 0.9238795325112869605, 1.000000000000000000, 0.9238795325112869605, 1.000000000000000000, 0.9238795325112869605, 1.000000000000000000, 0.9238795325112869605, 1.000000000000000000, 0.9238795325112869605, 1.000000000000000000, 0.9238795325112869605, 1.000000000000000000, 0.9238795325112869605, 1.000000000000000000, 0.9238795325112869605, 1.000000000000000000, 0.9238795325112869605, 1.000000000000000000, 0.9238795325112869605, 1.000000000000000000, 0.9238795325112869605, 1.000000000000000000, 0.9238795325112869605, 1.000000000000000000, 0.9238795325112869605, 1.000000000000000000, 0.9238795325112869605, 1.000000000000000000, 0.9238795325112869605, 1.000000000000000000, 0.9238795325112869605, 1.000000000000000000, 0.9238795325112869605, 1.000000000000000000, 0.9238795325112869605, 1.000000000000000000, 0.9238795325112869605, 1.000000000000000000, 0.9238795325112869605, 1.000000000000000000, 0.9238795325112869605, 1.000000000000000000, 0.9238795325112869605, 1.000000000000000000, 0.9238795325112869605, 1.000000000000000000, 0.9238795325112869605, 1.000000000000000000, 0.9238795325112869605, 1.000000000000000000, 0.9238795325112869605, 1.000000000000000000, 0.9238795325112869605, 1.000000000000000000, 0.9238795325112869605, 1.000000000000000000, 0.9238795325112869605, 1.000000000000000000, 0.9238795325112869605, 1.000000000000000000, 0.9238795325112869605, 1.000000000000000000, 0.9238795325112869605, 1.000000000000000000, 0.9238795325112869605, 1.000000000000000000, 0.9238795325112869605, 1.000000000000000000, 0.9238795325112869605, 1.000000000000000000, 0.9238795325112869605, 1.000000000000000000, 0.9238795325112869605, 1.000000000000000000, 0.9238795325112869605, 1.000000000000000000, 0.9238795325112869605, 1.000000000000000000, 0.9238795325112869605, 1.000000000000000000, 0.9238795325112869605, 1.000000000000000000, 0.9238795325112869605, 1.000000000000000000, 0.9238795325112869605, 1.000000000000000000, 0.9238795325112869605, 1.000000000000000000, 0.9238795325112869605, 1.000000000000000000, 0.9238795325112869605, 1.000000000000000000, 0.9238795325112869605, 1.000000000000000000, 0.9238795325112869605, 1.000000000000000000, 0.9238795325112869605, 1.000000000000000000, 0.9238795325112869605, 1.000000000000000000, 0.9238795325112869605, 1.000000000000000000, 0.9238795325112869605, 1.000000000000000000, 0.9238795325112869605, 1.000000000000000000, 0.9238795325112869605, 1.000000000000000000, 0.9238795325112869605, 1.000000000000000000, 0.9238795325112869605, 1.000000000000000000, 0.9238795325112869605, 1.000000000000000000, 0.9238795325112869605, 1.000000000000000000, 0.9238795325112869605, 1.000000000000000000, 0.9238795325112869605, 1.000000000000000000, 0.9238795325112869605, 1.000000000000000000, 0.9238795325112869605, 1.000000000000000000, 0.9238795325112869605, 1.000000000000000000, 0.9238795325112869605, 1.000000000000000000, 0.9238795325112869605, 1.000000000000000000, 0.9238795325112869605, 1.000000000000000000, 0.9238795325112869605, 1.000000000000000000, 0.9238795325112869605, 1.000000000000000000, 0.9238795325112869605, 1.000000000000000000, 0.9238795325112869605, 1.000000000000000000, 0.9238795325112869605, 1.000000000000000000, 0.9238795325112869605, 1.000000000000000000, 0.9238795325112869605, 1.000000000000000000, 0.9238795325112869605, 1.000000000000000000, 0.9238795325112869605, 1.000000000000000000, 0.9238795325112869605, 1.000000000000000000, 0.9238795325112869605, 1.000000000000000000, 0.9238795325112869605, 1.000000000000000000, 0.9238795325112869605, 1.000000000000000000, 0.9238795325112869605, 1.000000000000000000, 0.9238795325112869605, 1.000000000000000000, 0.9238795325112869605, 1.000000000000000000, 0.9238795325112869605, 1.000000000000000000, 0.9238795325112869605, 1.000000000000000000, 0.9238795325112869605, 1.000000000000000000, 0.9238795325112869605, 1.000000000000000000, 0.9238795325112869605, 1.000000000000000000, 0.9238795325112869605, 1.000000000000000000, 0.9238795325112869605, 1.000000000000000000, 0.9238795325112869605, 1.000000000000000000, 0.9238795325112869605, 1.000000000000000000, 0.9238795325112869605, 1.000000000000000000, 0.9238795325112869605, 1.000000000000000000, 0.9238795325112869605, 1.000000000000000000, 0.9238795325112869605, 1.000000000000000000, 0.9238795325112869605, 1.000000000000000000, 0.9238795325112869605, 1.000000000000000000, 0.9238795325112869605, 1.000000000000000000, 0.9238795325112869605, 1.000000000000000000, 0.9238795325112869605, 1.000000000000000000, 0.9238795325112869605, 1.000000000000000000, 0.9238795325112869605, 1.000000000000000000) ) ) 
 REPRESENTATION_ITEM ( '' )  SURFACE ( )  );
#16864=CARTESIAN_POINT ( 'NONE',  ( 117.6180281442453150, -0.4660016031367893996, -10.09054647747474043 ) ) ;
#16866=CARTESIAN_POINT ( 'NONE',  ( 114.1577014775786552, -6.344957434206662583, -7.627207830600332805 ) ) ;
#16869=CARTESIAN_POINT ( 'NONE',  ( 121.0216281442452981, -1.561330072975668948, -17.79121239304076951 ) ) ;
#16871=CARTESIAN_POINT ( 'NONE',  ( 113.3635281442453504, -0.1624402480850797581, -16.17319339645315424 ) ) ;
#16872=CARTESIAN_POINT ( 'NONE',  ( 124.8912734719562110, -1.125321370491286332, -17.12283323191017814 ) ) ;
#16873=CARTESIAN_POINT ( 'NONE',  ( 115.1787814775786387, -0.1624402480850797581, -16.17319339645315424 ) ) ;
#16875=CARTESIAN_POINT ( 'NONE',  ( 117.3911214775786505, -7.894159318335828068, -9.358103419637847864 ) ) ;
#16877=CARTESIAN_POINT ( 'NONE',  ( 117.3911214775786505, -7.894159318335828068, -9.358103419637847864 ) ) ;
#16878=CARTESIAN_POINT ( 'NONE',  ( 115.5191414775786569, -3.383040157471821630, -19.15922257007629170 ) ) ;
#16880=CARTESIAN_POINT ( 'NONE',  ( 115.2355081442453155, -10.30919188438810075, -12.61870101168855918 ) ) ;
#16881=CARTESIAN_POINT ( 'NONE',  ( 113.9875214775786532, -8.899110576539710493, -16.42337572283490132 ) ) ;
#16882=CARTESIAN_POINT ( 'NONE',  ( 126.2404814775786264, -9.261995988541697145, -16.69588392320189030 ) ) ;
#16883=CARTESIAN_POINT ( 'NONE',  ( 115.6325948109119821, -9.565557343593413364, -10.61323700422348004 ) ) ;
#16885=CARTESIAN_POINT ( 'NONE',  ( 112.2857214775786474, -4.089484607189486809, -7.948022111789456723 ) ) ;
#16891=CARTESIAN_POINT ( 'NONE',  ( 117.7882081442453170, -6.344957434206665248, -7.627207830600338134 ) ) ;
#16893=DIRECTION ( 'NONE',  ( 1.000000000000000000, 0.000000000000000000, 0.000000000000000000 ) ) ;
#16894=CARTESIAN_POINT ( 'NONE',  ( 135.3184548109119874, -4.863998795839242995, -13.39321520033831447 ) ) ;
#16895=CARTESIAN_POINT ( 'NONE',  ( 118.2987481442453088, -7.894159318335828068, -9.358103419637847864 ) ) ;
#16897=CARTESIAN_POINT ( 'NONE',  ( 125.0492214775786266, -6.344957434206665248, -7.627207830600338134 ) ) ;
#16901=CARTESIAN_POINT ( 'NONE',  ( 112.9097148109120070, 0.2603800115204892296, -16.42320221600525088 ) ) ;
#16903=CARTESIAN_POINT ( 'NONE',  ( 121.2485348109119769, -8.899110576539710493, -16.42337572283490132 ) ) ;
#16904=CARTESIAN_POINT ( 'NONE',  ( 118.3554748109119998, 0.2603800115204892296, -16.42320221600525088 ) ) ;
#16905=CARTESIAN_POINT ( 'NONE',  ( 116.4834948109119779, -7.894159318335828068, -9.358103419637847864 ) ) ;
#16906=CARTESIAN_POINT ( 'NONE',  ( 119.5467348109119712, -4.089484607189486809, -7.948022111789456723 ) ) ;
#16909=CARTESIAN_POINT ( 'NONE',  ( 124.3685014775786328, 0.4262465694468514643, -12.03445270309931736 ) ) ;
#16912=CARTESIAN_POINT ( 'NONE',  ( 118.6391081442452986, -4.089484607189486809, -7.948022111789456723 ) ) ;
#16913=CARTESIAN_POINT ( 'NONE',  ( 125.2194014775786286, 0.1319031606808879209, -14.10382304977623669 ) ) ;
#16917=CARTESIAN_POINT ( 'NONE',  ( 119.0361948109119652, -7.893985811506177619, -18.51759400769804742 ) ) ;
#16919=CARTESIAN_POINT ( 'NONE',  ( 118.7525614775786380, -1.833838273342659253, -17.42832698103878286 ) ) ;
#16922=CARTESIAN_POINT ( 'NONE',  ( 126.1270281442452870, 0.1319031606808879209, -14.10382304977623669 ) ) ;
#16923=CARTESIAN_POINT ( 'NONE',  ( 125.3895814775786448, -2.084020599724406786, -8.691656652584148546 ) ) ;
#16926=CARTESIAN_POINT ( 'NONE',  ( 122.7801548109119665, -3.383040157471821630, -19.15922257007629170 ) ) ;
#16929=CARTESIAN_POINT ( 'NONE',  ( 118.6391081442452986, -4.089484607189486809, -7.948022111789456723 ) ) ;
#16930=CARTESIAN_POINT ( 'NONE',  ( 118.9227414775786400, -10.63000616557722466, -14.87417383870573495 ) ) ;
#16931=CARTESIAN_POINT ( 'NONE',  ( 118.4689281442453392, -10.15424416112533912, -14.75197769757731336 ) ) ;
#16932=CARTESIAN_POINT ( 'NONE',  ( 125.1059481442452750, -1.833838273342660141, -17.42832698103878286 ) ) ;
#16933=CARTESIAN_POINT ( 'NONE',  ( 117.5045748109119756, 0.5811942927096110934, -14.16772938898807510 ) ) ;
#16936=CARTESIAN_POINT ( 'NONE',  ( 125.2194014775786286, 0.1319031606808879209, -14.10382304977623669 ) ) ;
#16941=CARTESIAN_POINT ( 'NONE',  ( 121.0216281442452981, -1.561330072975668948, -17.79121239304076951 ) ) ;
#16942=CARTESIAN_POINT ( 'NONE',  ( 123.4608748109119745, 0.4262465694468514643, -12.03445270309931736 ) ) ;
#16943=( BOUNDED_SURFACE ( )  B_SPLINE_SURFACE ( 1, 2, ( 
 ( #23515, #41076, #34418, #44485, #31012, #10063, #13699, #2973, #20093, #27607, #20315, #31232, #16670, #30345, #44718, #37402, #13252, #17342, #41521, #24183, #27154, #16901, #30794, #13478, #6853, #20760, #4, #27824, #10500, #32121, #31451, #220, #10722, #14580, #889, #14358, #28271, #21198, #17556, #21644, #3857, #31672, #31898, #18000, #21870, #25072, #25301, #35304, #14133, #35533, #14809, #28497, #664, #38505, #4305, #18227, #7068, #4076, #7282, #35075, #42628, #28722, #11392, #42180, #39193, #7959, #42403, #28049, #20979, #34852, #3638, #11167, #38965, #41957, #10940, #7734, #24622, #17779, #442, #24843, #38734, #7505, #21420, #17474, #31371, #16591, #37772, #27973, #7201, #23658, #17045, #6545, #143, #30938, #17265, #30713, #14057, #45074, #24329, #41441, #20685, #10199, #24546, #21114, #44635, #9977, #9746, #27525, #37999, #2659, #27749, #10641, #24106, #40994, #6993, #41879, #3345, #6775, #16820, #38215, #20905, #30484, #34562, #13400, #27302, #38433, #34778, #3561, #20461, #44405, #13170, #31154, #37544, #10422, #27072, #6318, #44861, #13834, #20235, #34122, #13616, #41665, #2891, #41217, #23888, #34343, #3121, #2927, #26877, #13654, #34156, #30294, #44671, #13868, #34377, #13433, #44220, #40795, #3380, #23466, #20043, #10455, #30748, #33925, #16856, #37805, #27336, #41257, #20716, #37352, #27779, #10233, #3158, #37116, #23698, #2696, #41030, #17299, #34596, #30520, #2469, #31191, #6580, #9550, #6809, #27108, #45110, #17079, #30971, #10014, #44895, #16394, #27560, #9784, #12981, #6124, #5888, #37585, #33699, #16625, #41475, #44442, #13209, #6357, #24140, #23923, #20270, #41692, #19810, #20496, #38032, #3594, #35025, #35487, #28898, #42359, #31630, #34808, #10676, #21825, #11342, #14984, #28450, #38915, #18180, #25253, #4491, #31854, #1072, #842, #4033, #38463, #7686, #172, #17955, #3808, #18413, #42809, #21600, #4261, #17506, #24358, #38689, #11121, #14313, #14088, #38245, #39150, #17732, #28005, #14762, #7454, #28677, #24578, #7024, #7236, #7915 ),
 ( #21152, #20934, #32075, #32305, #21373, #28229, #42136, #31404, #41913, #398, #35256, #10897, #35719, #623, #42579, #24797, #14535, #25021, #33190, #5160, #29565, #19077, #33408, #16115, #8369, #18850, #18634, #36389, #1740, #40048, #43701, #32742, #1516, #1965, #43256, #22052, #12021, #15435, #2185, #35945, #15892, #8148, #25924, #29789, #43483, #29114, #32963, #39830, #32522, #29342, #15663, #22275, #12250, #26146, #8816, #8596, #11794, #22717, #22494, #22947, #25701, #25477, #36616, #30015, #1297, #9047, #5391, #19309, #15209, #4714, #39383, #43026, #39608, #12474, #36169, #26373, #11570, #40283, #4935, #36840, #5608, #19532, #13599, #16574, #2642, #9496, #23184, #34329, #37295, #33872, #16803, #2873, #17246, #23873, #6758, #20219, #37062, #3101, #27509, #44617, #30468, #44388, #24089, #3325, #19757, #13152, #27055, #41427, #40973, #13383, #26828, #10183, #41200, #20445, #37527, #30698, #6300, #20668, #43934, #40739, #6064, #5835, #23640, #34105, #27285, #30921, #19983, #9729, #17029, #9959, #9276, #37758, #6528, #34543, #33639, #44844, #40513, #37983, #12700, #26600, #16341, #2415, #30244, #44166, #12930, #23411, #41865, #17906, #7406, #21324, #348, #31354, #35211, #34973, #42533, #129, #45060, #10846, #4441, #38199, #28623, #11068, #575, #6976, #27733, #13820, #20885, #41648, #14262, #10403, #38631, #35668, #32024, #34762, #3543, #17458, #31804, #789, #3761, #17683, #10626, #24314, #21548, #24529, #21095, #3983, #14484, #31136, #24970, #39099, #28394, #14040, #35437, #14711, #42305, #38866, #27957, #7635, #4214, #38416, #18130, #7186, #31581, #11293, #25202, #7869, #28178, #21777, #42086, #24742, #39329, #26092, #40228, #1905, #32693, #39771, #36786, #4658, #1462, #15384, #8542, #29289, #8992, #18579, #22892, #1685, #12420, #43202, #32250, #25868, #18359, #19257, #25427, #8096, #32471, #19022, #33135, #36115, #22219, #29064, #42759, #8761, #11742, #8318, #36336, #22444, #1020, #43426, #26320, #5106, #11523, #22667, #15834, #32909, #15606, #1247, #39996 ) ),
 .UNSPECIFIED., .F., .F., .T. ) 
 B_SPLINE_SURFACE_WITH_KNOTS ( ( 2, 2 ),
 ( 3, 2, 2, 2, 2, 2, 2, 2, 2, 2, 2, 2, 2, 2, 2, 2, 2, 2, 2, 2, 2, 2, 2, 2, 2, 2, 2, 2, 2, 2, 2, 2, 2, 2, 2, 2, 2, 2, 2, 2, 2, 2, 2, 2, 2, 2, 2, 2, 2, 2, 2, 2, 2, 2, 2, 2, 2, 2, 2, 2, 2, 2, 2, 2, 2, 2, 2, 2, 2, 2, 2, 2, 2, 2, 2, 2, 2, 2, 2, 2, 2, 2, 2, 2, 2, 2, 2, 2, 2, 2, 2, 2, 2, 2, 2, 2, 2, 2, 2, 2, 2, 2, 2, 2, 2, 2, 2, 2, 2, 2, 2, 2, 2, 2, 2, 2, 2, 2, 2, 2, 2, 2, 2, 2, 2, 2, 2, 2, 3 ),
 ( 0.000000000000000000, 1.000000000000000000 ),
 ( 0.000000000000000000, 0.007812500000000000000, 0.01562500000000000000, 0.02343750000000000000, 0.03125000000000000000, 0.03906250000000000000, 0.04687500000000000000, 0.05468750000000000000, 0.06250000000000000000, 0.07031250000000000000, 0.07812500000000000000, 0.08593750000000000000, 0.09375000000000000000, 0.1015625000000000000, 0.1093750000000000000, 0.1171875000000000000, 0.1250000000000000000, 0.1328125000000000000, 0.1406250000000000000, 0.1484375000000000000, 0.1562500000000000000, 0.1640625000000000000, 0.1718750000000000000, 0.1796875000000000000, 0.1875000000000000000, 0.1953125000000000000, 0.2031250000000000000, 0.2109375000000000000, 0.2187500000000000000, 0.2265625000000000000, 0.2343750000000000000, 0.2421875000000000000, 0.2500000000000000000, 0.2578125000000000000, 0.2656250000000000000, 0.2734375000000000000, 0.2812500000000000000, 0.2890625000000000000, 0.2968750000000000000, 0.3046875000000000000, 0.3125000000000000000, 0.3203125000000000000, 0.3281250000000000000, 0.3359375000000000000, 0.3437500000000000000, 0.3515625000000000000, 0.3593750000000000000, 0.3671875000000000000, 0.3750000000000000000, 0.3828125000000000000, 0.3906250000000000000, 0.3984375000000000000, 0.4062500000000000000, 0.4140625000000000000, 0.4218750000000000000, 0.4296875000000000000, 0.4375000000000000000, 0.4453125000000000000, 0.4531250000000000000, 0.4609375000000000000, 0.4687500000000000000, 0.4765625000000000000, 0.4843750000000000000, 0.4921875000000000000, 0.5000000000000000000, 0.5078125000000000000, 0.5156250000000000000, 0.5234375000000000000, 0.5312500000000000000, 0.5390625000000000000, 0.5468750000000000000, 0.5546875000000000000, 0.5625000000000000000, 0.5703125000000000000, 0.5781250000000000000, 0.5859375000000000000, 0.5937500000000000000, 0.6015625000000000000, 0.6093750000000000000, 0.6171875000000000000, 0.6250000000000000000, 0.6328125000000000000, 0.6406250000000000000, 0.6484375000000000000, 0.6562500000000000000, 0.6640625000000000000, 0.6718750000000000000, 0.6796875000000000000, 0.6875000000000000000, 0.6953125000000000000, 0.7031250000000000000, 0.7109375000000000000, 0.7187500000000000000, 0.7265625000000000000, 0.7343750000000000000, 0.7421875000000000000, 0.7500000000000000000, 0.7578125000000000000, 0.7656250000000000000, 0.7734375000000000000, 0.7812500000000000000, 0.7890625000000000000, 0.7968750000000000000, 0.8046875000000000000, 0.8125000000000000000, 0.8203125000000000000, 0.8281250000000000000, 0.8359375000000000000, 0.8437500000000000000, 0.8515625000000000000, 0.8593750000000000000, 0.8671875000000000000, 0.8750000000000000000, 0.8828125000000000000, 0.8906250000000000000, 0.8984375000000000000, 0.9062500000000000000, 0.9140625000000000000, 0.9218750000000000000, 0.9296875000000000000, 0.9375000000000000000, 0.9453125000000000000, 0.9531250000000000000, 0.9609375000000000000, 0.9687500000000000000, 0.9765625000000000000, 0.9843750000000000000, 0.9921875000000000000, 1.000000000000000000 ),
 .UNSPECIFIED. ) 
 GEOMETRIC_REPRESENTATION_ITEM ( )  RATIONAL_B_SPLINE_SURFACE ( (
 ( 1.000000000000000000, 0.9238795325112869605, 1.000000000000000000, 0.9238795325112869605, 1.000000000000000000, 0.9238795325112869605, 1.000000000000000000, 0.9238795325112869605, 1.000000000000000000, 0.9238795325112869605, 1.000000000000000000, 0.9238795325112869605, 1.000000000000000000, 0.9238795325112869605, 1.000000000000000000, 0.9238795325112869605, 1.000000000000000000, 0.9238795325112869605, 1.000000000000000000, 0.9238795325112869605, 1.000000000000000000, 0.9238795325112869605, 1.000000000000000000, 0.9238795325112869605, 1.000000000000000000, 0.9238795325112869605, 1.000000000000000000, 0.9238795325112869605, 1.000000000000000000, 0.9238795325112869605, 1.000000000000000000, 0.9238795325112869605, 1.000000000000000000, 0.9238795325112869605, 1.000000000000000000, 0.9238795325112869605, 1.000000000000000000, 0.9238795325112869605, 1.000000000000000000, 0.9238795325112869605, 1.000000000000000000, 0.9238795325112869605, 1.000000000000000000, 0.9238795325112869605, 1.000000000000000000, 0.9238795325112869605, 1.000000000000000000, 0.9238795325112869605, 1.000000000000000000, 0.9238795325112869605, 1.000000000000000000, 0.9238795325112869605, 1.000000000000000000, 0.9238795325112869605, 1.000000000000000000, 0.9238795325112869605, 1.000000000000000000, 0.9238795325112869605, 1.000000000000000000, 0.9238795325112869605, 1.000000000000000000, 0.9238795325112869605, 1.000000000000000000, 0.9238795325112869605, 1.000000000000000000, 0.9238795325112869605, 1.000000000000000000, 0.9238795325112869605, 1.000000000000000000, 0.9238795325112869605, 1.000000000000000000, 0.9238795325112869605, 1.000000000000000000, 0.9238795325112869605, 1.000000000000000000, 0.9238795325112869605, 1.000000000000000000, 0.9238795325112869605, 1.000000000000000000, 0.9238795325112869605, 1.000000000000000000, 0.9238795325112869605, 1.000000000000000000, 0.9238795325112869605, 1.000000000000000000, 0.9238795325112869605, 1.000000000000000000, 0.9238795325112869605, 1.000000000000000000, 0.9238795325112869605, 1.000000000000000000, 0.9238795325112869605, 1.000000000000000000, 0.9238795325112869605, 1.000000000000000000, 0.9238795325112869605, 1.000000000000000000, 0.9238795325112869605, 1.000000000000000000, 0.9238795325112869605, 1.000000000000000000, 0.9238795325112869605, 1.000000000000000000, 0.9238795325112869605, 1.000000000000000000, 0.9238795325112869605, 1.000000000000000000, 0.9238795325112869605, 1.000000000000000000, 0.9238795325112869605, 1.000000000000000000, 0.9238795325112869605, 1.000000000000000000, 0.9238795325112869605, 1.000000000000000000, 0.9238795325112869605, 1.000000000000000000, 0.9238795325112869605, 1.000000000000000000, 0.9238795325112869605, 1.000000000000000000, 0.9238795325112869605, 1.000000000000000000, 0.9238795325112869605, 1.000000000000000000, 0.9238795325112869605, 1.000000000000000000, 0.9238795325112869605, 1.000000000000000000, 0.9238795325112869605, 1.000000000000000000, 0.9238795325112869605, 1.000000000000000000, 0.9238795325112869605, 1.000000000000000000, 0.9238795325112869605, 1.000000000000000000, 0.9238795325112869605, 1.000000000000000000, 0.9238795325112869605, 1.000000000000000000, 0.9238795325112869605, 1.000000000000000000, 0.9238795325112869605, 1.000000000000000000, 0.9238795325112869605, 1.000000000000000000, 0.9238795325112869605, 1.000000000000000000, 0.9238795325112869605, 1.000000000000000000, 0.9238795325112869605, 1.000000000000000000, 0.9238795325112869605, 1.000000000000000000, 0.9238795325112869605, 1.000000000000000000, 0.9238795325112869605, 1.000000000000000000, 0.9238795325112869605, 1.000000000000000000, 0.9238795325112869605, 1.000000000000000000, 0.9238795325112869605, 1.000000000000000000, 0.9238795325112869605, 1.000000000000000000, 0.9238795325112869605, 1.000000000000000000, 0.9238795325112869605, 1.000000000000000000, 0.9238795325112869605, 1.000000000000000000, 0.9238795325112869605, 1.000000000000000000, 0.9238795325112869605, 1.000000000000000000, 0.9238795325112869605, 1.000000000000000000, 0.9238795325112869605, 1.000000000000000000, 0.9238795325112869605, 1.000000000000000000, 0.9238795325112869605, 1.000000000000000000, 0.9238795325112869605, 1.000000000000000000, 0.9238795325112869605, 1.000000000000000000, 0.9238795325112869605, 1.000000000000000000, 0.9238795325112869605, 1.000000000000000000, 0.9238795325112869605, 1.000000000000000000, 0.9238795325112869605, 1.000000000000000000, 0.9238795325112869605, 1.000000000000000000, 0.9238795325112869605, 1.000000000000000000, 0.9238795325112869605, 1.000000000000000000, 0.9238795325112869605, 1.000000000000000000, 0.9238795325112869605, 1.000000000000000000, 0.9238795325112869605, 1.000000000000000000, 0.9238795325112869605, 1.000000000000000000, 0.9238795325112869605, 1.000000000000000000, 0.9238795325112869605, 1.000000000000000000, 0.9238795325112869605, 1.000000000000000000, 0.9238795325112869605, 1.000000000000000000, 0.9238795325112869605, 1.000000000000000000, 0.9238795325112869605, 1.000000000000000000, 0.9238795325112869605, 1.000000000000000000, 0.9238795325112869605, 1.000000000000000000, 0.9238795325112869605, 1.000000000000000000, 0.9238795325112869605, 1.000000000000000000, 0.9238795325112869605, 1.000000000000000000, 0.9238795325112869605, 1.000000000000000000, 0.9238795325112869605, 1.000000000000000000, 0.9238795325112869605, 1.000000000000000000, 0.9238795325112869605, 1.000000000000000000, 0.9238795325112869605, 1.000000000000000000, 0.9238795325112869605, 1.000000000000000000, 0.9238795325112869605, 1.000000000000000000, 0.9238795325112869605, 1.000000000000000000, 0.9238795325112869605, 1.000000000000000000, 0.9238795325112869605, 1.000000000000000000, 0.9238795325112869605, 1.000000000000000000, 0.9238795325112869605, 1.000000000000000000),
 ( 1.000000000000000000, 0.9238795325112869605, 1.000000000000000000, 0.9238795325112869605, 1.000000000000000000, 0.9238795325112869605, 1.000000000000000000, 0.9238795325112869605, 1.000000000000000000, 0.9238795325112869605, 1.000000000000000000, 0.9238795325112869605, 1.000000000000000000, 0.9238795325112869605, 1.000000000000000000, 0.9238795325112869605, 1.000000000000000000, 0.9238795325112869605, 1.000000000000000000, 0.9238795325112869605, 1.000000000000000000, 0.9238795325112869605, 1.000000000000000000, 0.9238795325112869605, 1.000000000000000000, 0.9238795325112869605, 1.000000000000000000, 0.9238795325112869605, 1.000000000000000000, 0.9238795325112869605, 1.000000000000000000, 0.9238795325112869605, 1.000000000000000000, 0.9238795325112869605, 1.000000000000000000, 0.9238795325112869605, 1.000000000000000000, 0.9238795325112869605, 1.000000000000000000, 0.9238795325112869605, 1.000000000000000000, 0.9238795325112869605, 1.000000000000000000, 0.9238795325112869605, 1.000000000000000000, 0.9238795325112869605, 1.000000000000000000, 0.9238795325112869605, 1.000000000000000000, 0.9238795325112869605, 1.000000000000000000, 0.9238795325112869605, 1.000000000000000000, 0.9238795325112869605, 1.000000000000000000, 0.9238795325112869605, 1.000000000000000000, 0.9238795325112869605, 1.000000000000000000, 0.9238795325112869605, 1.000000000000000000, 0.9238795325112869605, 1.000000000000000000, 0.9238795325112869605, 1.000000000000000000, 0.9238795325112869605, 1.000000000000000000, 0.9238795325112869605, 1.000000000000000000, 0.9238795325112869605, 1.000000000000000000, 0.9238795325112869605, 1.000000000000000000, 0.9238795325112869605, 1.000000000000000000, 0.9238795325112869605, 1.000000000000000000, 0.9238795325112869605, 1.000000000000000000, 0.9238795325112869605, 1.000000000000000000, 0.9238795325112869605, 1.000000000000000000, 0.9238795325112869605, 1.000000000000000000, 0.9238795325112869605, 1.000000000000000000, 0.9238795325112869605, 1.000000000000000000, 0.9238795325112869605, 1.000000000000000000, 0.9238795325112869605, 1.000000000000000000, 0.9238795325112869605, 1.000000000000000000, 0.9238795325112869605, 1.000000000000000000, 0.9238795325112869605, 1.000000000000000000, 0.9238795325112869605, 1.000000000000000000, 0.9238795325112869605, 1.000000000000000000, 0.9238795325112869605, 1.000000000000000000, 0.9238795325112869605, 1.000000000000000000, 0.9238795325112869605, 1.000000000000000000, 0.9238795325112869605, 1.000000000000000000, 0.9238795325112869605, 1.000000000000000000, 0.9238795325112869605, 1.000000000000000000, 0.9238795325112869605, 1.000000000000000000, 0.9238795325112869605, 1.000000000000000000, 0.9238795325112869605, 1.000000000000000000, 0.9238795325112869605, 1.000000000000000000, 0.9238795325112869605, 1.000000000000000000, 0.9238795325112869605, 1.000000000000000000, 0.9238795325112869605, 1.000000000000000000, 0.9238795325112869605, 1.000000000000000000, 0.9238795325112869605, 1.000000000000000000, 0.9238795325112869605, 1.000000000000000000, 0.9238795325112869605, 1.000000000000000000, 0.9238795325112869605, 1.000000000000000000, 0.9238795325112869605, 1.000000000000000000, 0.9238795325112869605, 1.000000000000000000, 0.9238795325112869605, 1.000000000000000000, 0.9238795325112869605, 1.000000000000000000, 0.9238795325112869605, 1.000000000000000000, 0.9238795325112869605, 1.000000000000000000, 0.9238795325112869605, 1.000000000000000000, 0.9238795325112869605, 1.000000000000000000, 0.9238795325112869605, 1.000000000000000000, 0.9238795325112869605, 1.000000000000000000, 0.9238795325112869605, 1.000000000000000000, 0.9238795325112869605, 1.000000000000000000, 0.9238795325112869605, 1.000000000000000000, 0.9238795325112869605, 1.000000000000000000, 0.9238795325112869605, 1.000000000000000000, 0.9238795325112869605, 1.000000000000000000, 0.9238795325112869605, 1.000000000000000000, 0.9238795325112869605, 1.000000000000000000, 0.9238795325112869605, 1.000000000000000000, 0.9238795325112869605, 1.000000000000000000, 0.9238795325112869605, 1.000000000000000000, 0.9238795325112869605, 1.000000000000000000, 0.9238795325112869605, 1.000000000000000000, 0.9238795325112869605, 1.000000000000000000, 0.9238795325112869605, 1.000000000000000000, 0.9238795325112869605, 1.000000000000000000, 0.9238795325112869605, 1.000000000000000000, 0.9238795325112869605, 1.000000000000000000, 0.9238795325112869605, 1.000000000000000000, 0.9238795325112869605, 1.000000000000000000, 0.9238795325112869605, 1.000000000000000000, 0.9238795325112869605, 1.000000000000000000, 0.9238795325112869605, 1.000000000000000000, 0.9238795325112869605, 1.000000000000000000, 0.9238795325112869605, 1.000000000000000000, 0.9238795325112869605, 1.000000000000000000, 0.9238795325112869605, 1.000000000000000000, 0.9238795325112869605, 1.000000000000000000, 0.9238795325112869605, 1.000000000000000000, 0.9238795325112869605, 1.000000000000000000, 0.9238795325112869605, 1.000000000000000000, 0.9238795325112869605, 1.000000000000000000, 0.9238795325112869605, 1.000000000000000000, 0.9238795325112869605, 1.000000000000000000, 0.9238795325112869605, 1.000000000000000000, 0.9238795325112869605, 1.000000000000000000, 0.9238795325112869605, 1.000000000000000000, 0.9238795325112869605, 1.000000000000000000, 0.9238795325112869605, 1.000000000000000000, 0.9238795325112869605, 1.000000000000000000, 0.9238795325112869605, 1.000000000000000000, 0.9238795325112869605, 1.000000000000000000, 0.9238795325112869605, 1.000000000000000000, 0.9238795325112869605, 1.000000000000000000, 0.9238795325112869605, 1.000000000000000000, 0.9238795325112869605, 1.000000000000000000, 0.9238795325112869605, 1.000000000000000000, 0.9238795325112869605, 1.000000000000000000, 0.9238795325112869605, 1.000000000000000000) ) ) 
 REPRESENTATION_ITEM ( '' )  SURFACE ( )  );
#16945=CARTESIAN_POINT ( 'NONE',  ( 123.0070614775786169, 0.9020085738987339008, -11.91225656197089222 ) ) ;
#16947=CARTESIAN_POINT ( 'NONE',  ( 112.7962614775786676, -6.222761293078241884, -8.102969835052219238 ) ) ;
#16949=CARTESIAN_POINT ( 'NONE',  ( 124.6521348109119884, -1.561330072975668948, -17.79121239304076951 ) ) ;
#16950=CARTESIAN_POINT ( 'NONE',  ( 120.2274548109119934, 0.5811942927096110934, -14.16772938898807510 ) ) ;
#16952=CARTESIAN_POINT ( 'NONE',  ( 111.7751814775786556, -7.893985811506177619, -18.51759400769804742 ) ) ;
#16957=CARTESIAN_POINT ( 'NONE',  ( 113.4202548109119846, 0.1319031606808879209, -14.10382304977623669 ) ) ;
#16959=CARTESIAN_POINT ( 'NONE',  ( 123.5743281442453139, -2.084020599724406786, -8.691656652584148546 ) ) ;
#16962=CARTESIAN_POINT ( 'NONE',  ( 121.1350814775786233, -9.859900752359378018, -12.68260735090039759 ) ) ;
#16963=CARTESIAN_POINT ( 'NONE',  ( 114.6682414775786469, -7.894159318335828068, -9.358103419637847864 ) ) ;
#16964=CARTESIAN_POINT ( 'NONE',  ( 112.5693548109119888, 0.4262465694468514643, -12.03445270309931736 ) ) ;
#16968=CARTESIAN_POINT ( 'NONE',  ( 123.9714148109119805, -8.899110576539710493, -16.42337572283490132 ) ) ;
#16970=CARTESIAN_POINT ( 'NONE',  ( 119.2631014775786298, 0.2603800115204892296, -16.42320221600525088 ) ) ;
#16977=CARTESIAN_POINT ( 'NONE',  ( 114.8384214775786489, -10.15424416112533912, -14.75197769757731336 ) ) ;
#16978=CARTESIAN_POINT ( 'NONE',  ( 113.0798948109119948, -8.899110576539710493, -16.42337572283490132 ) ) ;
#16979=CARTESIAN_POINT ( 'NONE',  ( 114.8384214775786489, 0.9020085738987311252, -11.91225656197088867 ) ) ;
#16989=CARTESIAN_POINT ( 'NONE',  ( 124.4252281442452812, -0.8288870151387760510, -10.36305467784173118 ) ) ;
#16990=CARTESIAN_POINT ( 'NONE',  ( 112.9664414775786412, -9.859900752359374465, -12.68260735090039404 ) ) ;
#16998=CARTESIAN_POINT ( 'NONE',  ( 111.7184548109119788, -0.8288870151387760510, -10.36305467784173118 ) ) ;
#17001=CARTESIAN_POINT ( 'NONE',  ( 112.0588148109119828, 0.5811942927096154232, -14.16772938898807155 ) ) ;
#17003=CARTESIAN_POINT ( 'NONE',  ( 114.8951481442453115, -0.4660016031367893996, -10.09054647747474043 ) ) ;
#17004=CARTESIAN_POINT ( 'NONE',  ( 126.4262034846959324, 0.08385758931630681035, -14.64587210211922930 ) ) ;
#17006=CARTESIAN_POINT ( 'NONE',  ( 125.5597614775786326, -7.894159318335828068, -9.358103419637847864 ) ) ;
#17007=CARTESIAN_POINT ( 'NONE',  ( 123.0070614775786169, -10.15424416112533912, -14.75197769757731336 ) ) ;
#17011=CARTESIAN_POINT ( 'NONE',  ( 112.1722681442453222, -8.899110576539710493, -16.42337572283490132 ) ) ;
#17015=CARTESIAN_POINT ( 'NONE',  ( 125.3895814775786448, -7.893985811506177619, -18.51759400769804742 ) ) ;
#17016=CARTESIAN_POINT ( 'NONE',  ( 125.1059481442452750, -8.166667518702819706, -8.995218007635861213 ) ) ;
#17018=CARTESIAN_POINT ( 'NONE',  ( 119.8870948109119752, -9.261995988541697145, -16.69588392320189030 ) ) ;
#17019=CARTESIAN_POINT ( 'NONE',  ( 111.8319081442453182, -5.638512984488999180, -18.83840828888717311 ) ) ;
#17021=CARTESIAN_POINT ( 'NONE',  ( 113.4769814775786330, 0.4262465694468514643, -12.03445270309931736 ) ) ;
#17023=CARTESIAN_POINT ( 'NONE',  ( 125.5030348109119558, -3.383040157471821630, -19.15922257007629170 ) ) ;
#17025=CARTESIAN_POINT ( 'NONE',  ( 123.4608748109119745, -10.63000616557722466, -14.87417383870573495 ) ) ;
#17026=CARTESIAN_POINT ( 'NONE',  ( 115.4624148109119943, -5.638512984488999180, -18.83840828888717311 ) ) ;
#17027=CARTESIAN_POINT ( 'NONE',  ( 115.5758681442453053, -7.894159318335828068, -9.358103419637847864 ) ) ;
#17029=CARTESIAN_POINT ( 'NONE',  ( 118.5256548109119876, -8.899110576539710493, -16.42337572283490132 ) ) ;
#17030=CARTESIAN_POINT ( 'NONE',  ( 112.3991748109119868, -8.166667518702817929, -8.995218007635859436 ) ) ;
#17032=CARTESIAN_POINT ( 'NONE',  ( 125.2761281442453054, 0.4262465694468514643, -12.03445270309931736 ) ) ;
#17037=CARTESIAN_POINT ( 'NONE',  ( 125.1059481442452750, -8.166667518702819706, -8.995218007635861213 ) ) ;
#17045=CARTESIAN_POINT ( 'NONE',  ( 116.8238548109119819, -4.089484607189486809, -7.948022111789456723 ) ) ;
#17049=CARTESIAN_POINT ( 'NONE',  ( 121.2485348109119769, -8.899110576539710493, -16.42337572283490132 ) ) ;
#17053=CARTESIAN_POINT ( 'NONE',  ( 119.0361948109119652, -7.893985811506177619, -18.51759400769804742 ) ) ;
#17055=CARTESIAN_POINT ( 'NONE',  ( 114.4980614775786734, -2.084020599724406786, -8.691656652584148546 ) ) ;
#17056=CARTESIAN_POINT ( 'NONE',  ( 113.3068014775786594, -1.833838273342658809, -17.42832698103878286 ) ) ;
#17060=CARTESIAN_POINT ( 'NONE',  ( 118.2987481442453088, -7.894159318335828068, -9.358103419637847864 ) ) ;
#17061=CARTESIAN_POINT ( 'NONE',  ( 120.0572748109119772, -6.222761293078241884, -8.102969835052219238 ) ) ;
#17067=CARTESIAN_POINT ( 'NONE',  ( 113.7038881442453402, -3.383040157471821630, -19.15922257007629170 ) ) ;
#17068=CARTESIAN_POINT ( 'NONE',  ( 114.8384214775786489, 0.9020085738987339008, -11.91225656197089222 ) ) ;
#17074=CARTESIAN_POINT ( 'NONE',  ( 121.1918081442452859, 0.9020085738987339008, -11.91225656197089222 ) ) ;
#17075=CARTESIAN_POINT ( 'NONE',  ( 113.2500748109119968, -6.344957434206662583, -7.627207830600332805 ) ) ;
#17076=CARTESIAN_POINT ( 'NONE',  ( 118.4122014775786340, -9.859900752359374465, -12.68260735090039404 ) ) ;
#17077=SHAPE_REPRESENTATION_RELATIONSHIP ( 'NONE' , 'NONE' ,  #21588, #24824 ) ;
#17079=CARTESIAN_POINT ( 'NONE',  ( 122.3263414775786373, -6.344957434206665248, -7.627207830600338134 ) ) ;
#17080=CARTESIAN_POINT ( 'NONE',  ( 116.5402214775786405, 0.2603800115204892296, -16.42320221600525088 ) ) ;
#17083=CARTESIAN_POINT ( 'NONE',  ( 111.3213681442453264, -7.643976991954077427, -18.09477374809248928 ) ) ;
#17086=CARTESIAN_POINT ( 'NONE',  ( 116.9373081442452929, -8.166667518702817929, -8.995218007635861213 ) ) ;
#17087=EDGE_CURVE ( 'NONE', #41059, #38747, #7385, .T. ) ;
#17089=CARTESIAN_POINT ( 'NONE',  ( 115.2922348109119781, -10.63000616557722466, -14.87417383870573495 ) ) ;
#17092=CARTESIAN_POINT ( 'NONE',  ( 126.2404814775786264, -9.261995988541697145, -16.69588392320189030 ) ) ;
#17093=LINE ( 'NONE', #34167, #1200 ) ;
#17096=CARTESIAN_POINT ( 'NONE',  ( 117.1642148109119859, -0.8288870151387760510, -10.36305467784173118 ) ) ;
#17097=CARTESIAN_POINT ( 'NONE',  ( 111.7184548109119788, -9.142054238649166109, -15.98131134002176523 ) ) ;
#17098=CARTESIAN_POINT ( 'NONE',  ( 119.6601881442453106, -1.833838273342659253, -17.42832698103878286 ) ) ;
#17101=CARTESIAN_POINT ( 'NONE',  ( 114.8384214775786489, -10.15424416112533912, -14.75197769757731336 ) ) ;
#17103=CARTESIAN_POINT ( 'NONE',  ( 114.3278814775786429, -10.30919188438810075, -12.61870101168855918 ) ) ;
#17105=CARTESIAN_POINT ( 'NONE',  ( 113.7038881442453402, -6.222761293078241884, -8.102969835052219238 ) ) ;
#17107=CARTESIAN_POINT ( 'NONE',  ( 115.8027748109119841, -8.899110576539710493, -16.42337572283490132 ) ) ;
#17109=CARTESIAN_POINT ( 'NONE',  ( 115.5191414775786569, -3.383040157471821630, -19.15922257007629170 ) ) ;
#17114=CARTESIAN_POINT ( 'NONE',  ( 123.6877814775786533, -3.383040157471821630, -19.15922257007629170 ) ) ;
#17117=CARTESIAN_POINT ( 'NONE',  ( 117.4478481442453131, -9.565557343593413364, -10.61323700422348004 ) ) ;
#17119=CARTESIAN_POINT ( 'NONE',  ( 123.3474214775786209, -9.988377603198976828, -10.36322818467138340 ) ) ;
#17124=CARTESIAN_POINT ( 'NONE',  ( 111.8319081442453182, -5.638512984488999180, -18.83840828888717311 ) ) ;
#17125=CARTESIAN_POINT ( 'NONE',  ( 122.2696148109119889, -4.089484607189486809, -7.948022111789456723 ) ) ;
#17127=CARTESIAN_POINT ( 'NONE',  ( 115.4056881442453459, -2.084020599724406786, -8.691656652584148546 ) ) ;
#17129=CARTESIAN_POINT ( 'NONE',  ( 120.5110881442453206, -6.344957434206665248, -7.627207830600338134 ) ) ;
#17132=CARTESIAN_POINT ( 'NONE',  ( 124.1415948109119540, -3.505236298600246325, -18.68346056562440793 ) ) ;
#17136=CARTESIAN_POINT ( 'NONE',  ( 116.2565881442452991, -9.261995988541697145, -16.69588392320189030 ) ) ;
#17137=CARTESIAN_POINT ( 'NONE',  ( 125.7866681442452688, -8.899110576539710493, -16.42337572283490132 ) ) ;
#17138=VERTEX_POINT ( 'NONE', #18784 ) ;
#17141=CARTESIAN_POINT ( 'NONE',  ( 122.1561614775786353, -0.4660016031367893996, -10.09054647747474043 ) ) ;
#17144=CARTESIAN_POINT ( 'NONE',  ( 120.0005481442453146, -4.153390946401325223, -8.397313243818185668 ) ) ;
#17147=CARTESIAN_POINT ( 'NONE',  ( 115.8027748109119841, -0.4660016031367893996, -10.09054647747474043 ) ) ;
#17148=CARTESIAN_POINT ( 'NONE',  ( 124.3685014775786328, 0.4262465694468514643, -12.03445270309931736 ) ) ;
#17150=DIRECTION ( 'NONE',  ( 0.000000000000000000, 0.6004852223388321697, -0.7996358532186279566 ) ) ;
#17151=CARTESIAN_POINT ( 'NONE',  ( 121.4187148109119789, -6.344957434206665248, -7.627207830600338134 ) ) ;
#17154=CARTESIAN_POINT ( 'NONE',  ( 117.3719165460472027, -2.191907684172563986, -18.20049396185734025 ) ) ;
#17155=CARTESIAN_POINT ( 'NONE',  ( 119.8303681442453126, -10.63000616557722466, -14.87417383870573495 ) ) ;
#17156=CARTESIAN_POINT ( 'NONE',  ( 117.1074881442453233, -10.63000616557722466, -14.87417383870573495 ) ) ;
#17157=CARTESIAN_POINT ( 'NONE',  ( 121.4187148109119789, -3.505236298600246325, -18.68346056562440793 ) ) ;
#17159=CARTESIAN_POINT ( 'NONE',  ( 117.2776681442452968, -5.638512984488999180, -18.83840828888717311 ) ) ;
#17161=CARTESIAN_POINT ( 'NONE',  ( 125.5030348109119558, -6.222761293078241884, -8.102969835052219238 ) ) ;
#17162=CARTESIAN_POINT ( 'NONE',  ( 125.1059481442453034, -1.833838273341870773, -17.42832698103818956 ) ) ;
#17166=CARTESIAN_POINT ( 'NONE',  ( 122.2128881442453263, -1.834011780172310813, -8.268836392978581529 ) ) ;
#17167=CARTESIAN_POINT ( 'NONE',  ( 123.5743281442453139, -2.084020599724406786, -8.691656652584148546 ) ) ;
#17169=CARTESIAN_POINT ( 'NONE',  ( 125.6164881442453094, 0.2603800115204892296, -16.42320221600525088 ) ) ;
#17172=CARTESIAN_POINT ( 'NONE',  ( 122.0994348109119443, 0.9020085738987339008, -11.91225656197089222 ) ) ;
#17175=CARTESIAN_POINT ( 'NONE',  ( 112.4559014775786494, -9.988377603198976828, -10.36322818467138340 ) ) ;
#17180=CARTESIAN_POINT ( 'NONE',  ( 116.1998614775786507, 0.4262465694468514643, -12.03445270309931736 ) ) ;
#17181=CARTESIAN_POINT ( 'NONE',  ( 112.6828081442453282, -7.893985811506177619, -18.51759400769804742 ) ) ;
#17184=CARTESIAN_POINT ( 'NONE',  ( 121.4187148109119789, -3.505236298600246325, -18.68346056562440793 ) ) ;
#17185=CARTESIAN_POINT ( 'NONE',  ( 115.3489614775786407, -0.8288870151387760510, -10.36305467784173118 ) ) ;
#17186=CARTESIAN_POINT ( 'NONE',  ( 111.6617281442453304, 0.4262465694468514643, -12.03445270309931736 ) ) ;
#17188=CARTESIAN_POINT ( 'NONE',  ( 125.5597614775786326, -7.894159318335828068, -9.358103419637847864 ) ) ;
#17189=CARTESIAN_POINT ( 'NONE',  ( 119.5467348109119712, -4.089484607189486809, -7.948022111789456723 ) ) ;
#17191=CARTESIAN_POINT ( 'NONE',  ( 113.1933481442453058, -5.574606645277164318, -18.38911715685844683 ) ) ;
#17194=ORIENTED_EDGE ( 'NONE', *, *, #844, .F. ) ;
#17195=CARTESIAN_POINT ( 'NONE',  ( 116.7671281442453335, -7.643976991954077427, -18.09477374809248928 ) ) ;
#17196=CARTESIAN_POINT ( 'NONE',  ( 113.0231681442453180, -10.15424416112533912, -14.75197769757731336 ) ) ;
#17197=PLANE ( 'NONE',  #24592 ) ;
#17200=VERTEX_POINT ( 'NONE', #36766 ) ;
#17205=CARTESIAN_POINT ( 'NONE',  ( 123.5176014775786228, -0.8288870151387760510, -10.36305467784173118 ) ) ;
#17206=CARTESIAN_POINT ( 'NONE',  ( 114.7249681442453237, -9.565557343593413364, -10.61323700422348004 ) ) ;
#17207=CARTESIAN_POINT ( 'NONE',  ( 114.1009748109119784, -5.574606645277172312, -18.38911715685844683 ) ) ;
#17208=ORIENTED_EDGE ( 'NONE', *, *, #28469, .T. ) ;
#17210=CARTESIAN_POINT ( 'NONE',  ( 116.9940348109119839, -0.1624402480850797581, -16.17319339645315424 ) ) ;
#17213=CARTESIAN_POINT ( 'NONE',  ( 112.0693548109120030, -10.10582367741923093, -14.73954123521778925 ) ) ;
#17215=CARTESIAN_POINT ( 'NONE',  ( 116.8404719737025630, -1.196538596002799215, -17.02799684832027083 ) ) ;
#17216=CIRCLE ( 'NONE', #23023, 5.999999999999997335 ) ;
#17217=CARTESIAN_POINT ( 'NONE',  ( 125.7866681442452688, -8.899110576539710493, -16.42337572283490132 ) ) ;
#17219=CARTESIAN_POINT ( 'NONE',  ( 112.0020881442453344, 0.2603800115204892296, -16.42320221600525088 ) ) ;
#17222=CARTESIAN_POINT ( 'NONE',  ( 126.6942948109119840, -8.899110576539710493, -16.42337572283490132 ) ) ;
#17223=CARTESIAN_POINT ( 'NONE',  ( 124.0848681442452772, -5.574606645277164318, -18.38911715685844683 ) ) ;
#17224=CARTESIAN_POINT ( 'NONE',  ( 124.9924948109119924, -5.574606645277164318, -18.38911715685844683 ) ) ;
#17228=CARTESIAN_POINT ( 'NONE',  ( 120.4317020330015140, -1.172797794773259072, -17.05961127468926719 ) ) ;
#17230=CARTESIAN_POINT ( 'NONE',  ( 112.2289948109119848, -7.643976991954077427, -18.09477374809248928 ) ) ;
#17233=CARTESIAN_POINT ( 'NONE',  ( 124.5954081442453116, -3.383040157471821630, -19.15922257007629170 ) ) ;
#17234=CARTESIAN_POINT ( 'NONE',  ( 111.7751814775786556, -2.084020599724406786, -8.691656652584148546 ) ) ;
#17236=CARTESIAN_POINT ( 'NONE',  ( 118.8092881442453290, -9.988377603198976828, -10.36322818467138340 ) ) ;
#17237=CARTESIAN_POINT ( 'NONE',  ( 115.2355081442453155, -10.30919188438810075, -12.61870101168855918 ) ) ;
#17239=AXIS2_PLACEMENT_3D ( 'NONE', #3864, #11618, #8197 ) ;
#17240=CARTESIAN_POINT ( 'NONE',  ( 113.3068014775786594, -1.833838273342658809, -17.42832698103878286 ) ) ;
#17241=CARTESIAN_POINT ( 'NONE',  ( 123.9714148109119805, -0.4660016031367893996, -10.09054647747474043 ) ) ;
#17242=CARTESIAN_POINT ( 'NONE',  ( 113.8173414775786512, 0.2603800115204892296, -16.42320221600525088 ) ) ;
#17243=CARTESIAN_POINT ( 'NONE',  ( 116.3133148109120043, -2.084020599724406786, -8.691656652584148546 ) ) ;
#17244=ORIENTED_EDGE ( 'NONE', *, *, #31713, .T. ) ;
#17246=CARTESIAN_POINT ( 'NONE',  ( 116.4834948109119779, -7.894159318335828068, -9.358103419637847864 ) ) ;
#17249=CARTESIAN_POINT ( 'NONE',  ( 117.3343948109119737, -3.383040157471821630, -19.15922257007629170 ) ) ;
#17250=CARTESIAN_POINT ( 'NONE',  ( 124.5386814775786206, -4.153390946401325223, -8.397313243818185668 ) ) ;
#17258=CARTESIAN_POINT ( 'NONE',  ( 116.4834948109119779, -1.561330072975668504, -17.79121239304076951 ) ) ;
#17260=CARTESIAN_POINT ( 'NONE',  ( 113.5337081442453240, -0.8288870151387760510, -10.36305467784173118 ) ) ;
#17262=CARTESIAN_POINT ( 'NONE',  ( 123.0027181407225783, -1.081026697600530051, -17.18181821144403898 ) ) ;
#17265=CARTESIAN_POINT ( 'NONE',  ( 117.0507614775786465, -10.30919188438810075, -12.61870101168855918 ) ) ;
#17266=CARTESIAN_POINT ( 'NONE',  ( 136.0599924006030790, -4.157849207606297171, -19.25660148625498991 ) ) ;
#17269=CARTESIAN_POINT ( 'NONE',  ( 120.0572748109119772, -6.222761293078241884, -8.102969835052219238 ) ) ;
#17271=CARTESIAN_POINT ( 'NONE',  ( 135.7778351054754182, -9.571724809176972215, -9.731156920816491862 ) ) ;
#17272=CARTESIAN_POINT ( 'NONE',  ( 120.1140014775786398, -1.561330072975668504, -17.79121239304076951 ) ) ;
#17274=CARTESIAN_POINT ( 'NONE',  ( 114.6115148109119986, -6.222761293078241884, -8.102969835052219238 ) ) ;
#17275=CARTESIAN_POINT ( 'NONE',  ( 113.4769814775786330, 0.4262465694468514643, -12.03445270309931736 ) ) ;
#17280=CARTESIAN_POINT ( 'NONE',  ( 120.4543614775786295, -5.574606645277164318, -18.38911715685844683 ) ) ;
#17281=CARTESIAN_POINT ( 'NONE',  ( 120.2841814775786276, -10.15424416112533912, -14.75197769757731336 ) ) ;
#17287=CARTESIAN_POINT ( 'NONE',  ( 115.1787814775786387, -9.988377603198976828, -10.36322818467138340 ) ) ;
#17288=CARTESIAN_POINT ( 'NONE',  ( 115.6325948109119821, 0.2603800115204892296, -16.42320221600525088 ) ) ;
#17290=EDGE_LOOP ( 'NONE', ( #5229, #25537, #4577, #43153 ) ) ;
#17294=CARTESIAN_POINT ( 'NONE',  ( 122.8936081442453059, 0.2603800115204892296, -16.42320221600525088 ) ) ;
#17295=CARTESIAN_POINT ( 'NONE',  ( 113.1933481442453058, -4.089484607189486809, -7.948022111789456723 ) ) ;
#17296=CARTESIAN_POINT ( 'NONE',  ( 118.2420214775786320, -6.222761293078241884, -8.102969835052219238 ) ) ;
#17299=CARTESIAN_POINT ( 'NONE',  ( 121.7590748109119687, -7.893985811506177619, -18.51759400769804742 ) ) ;
#17300=CARTESIAN_POINT ( 'NONE',  ( 116.9940348109119839, -9.988377603198976828, -10.36322818467138340 ) ) ;
#17303=CARTESIAN_POINT ( 'NONE',  ( 112.5126281442453120, 0.1319031606808879209, -14.10382304977623669 ) ) ;
#17304=DIRECTION ( 'NONE',  ( 0.000000000000000000, 0.6004852223388321697, -0.7996358532186279566 ) ) ;
#17305=ORIENTED_EDGE ( 'NONE', *, *, #8321, .T. ) ;
#17307=CARTESIAN_POINT ( 'NONE',  ( 117.5613014775786525, 0.9020085738987339008, -11.91225656197089222 ) ) ;
#17309=CARTESIAN_POINT ( 'NONE',  ( 115.1220548109119761, -8.166667518702817929, -8.995218007635861213 ) ) ;
#17312=CARTESIAN_POINT ( 'NONE',  ( 126.1837548109119211, -10.63000616557722466, -14.87417383870573495 ) ) ;
#17317=CARTESIAN_POINT ( 'NONE',  ( 115.9729548109119861, -3.505236298600246325, -18.68346056562440793 ) ) ;
#17318=CARTESIAN_POINT ( 'NONE',  ( 111.5519368157052611, -9.055753378951116872, -16.12396441109182632 ) ) ;
#17319=CARTESIAN_POINT ( 'NONE',  ( 119.0929214775786278, -4.153390946401325223, -8.397313243818185668 ) ) ;
#17321=CARTESIAN_POINT ( 'NONE',  ( 120.6245414775786458, -0.1624402480850797581, -16.17319339645315424 ) ) ;
#17323=CARTESIAN_POINT ( 'NONE',  ( 117.2776681442452968, -5.638512984488999180, -18.83840828888717311 ) ) ;
#17324=CARTESIAN_POINT ( 'NONE',  ( 115.5191414775786569, -6.222761293078241884, -8.102969835052219238 ) ) ;
#17326=CARTESIAN_POINT ( 'NONE',  ( 118.3554748109119998, 0.2603800115204892296, -16.42320221600525088 ) ) ;
#17331=CARTESIAN_POINT ( 'NONE',  ( 122.5532481442453019, -10.63000616557722466, -14.87417383870573495 ) ) ;
#17333=CARTESIAN_POINT ( 'NONE',  ( 118.5867969858783511, -2.378957183258571639, -17.95140958770219086 ) ) ;
#17334=CARTESIAN_POINT ( 'NONE',  ( 118.8092881442453290, -0.1624402480850797581, -16.17319339645315424 ) ) ;
#17336=CARTESIAN_POINT ( 'NONE',  ( 124.6521348109119884, -7.894159318335843167, -9.358103419637860299 ) ) ;
#17338=CARTESIAN_POINT ( 'NONE',  ( 122.5532481442453019, -10.63000616557722466, -14.87417383870573495 ) ) ;
#17342=CARTESIAN_POINT ( 'NONE',  ( 112.6828081442453282, -7.893985811506177619, -18.51759400769804742 ) ) ;
#17343=CARTESIAN_POINT ( 'NONE',  ( 112.3424481442453384, -6.344957434206662583, -7.627207830600332805 ) ) ;
#17344=CARTESIAN_POINT ( 'NONE',  ( 122.1561614775786353, -0.4660016031367893996, -10.09054647747474043 ) ) ;
#17346=CARTESIAN_POINT ( 'NONE',  ( 115.7460481442453357, -10.15424416112533912, -14.75197769757731336 ) ) ;
#17348=CARTESIAN_POINT ( 'NONE',  ( 119.2063748109119814, -1.561330072975668504, -17.79121239304076951 ) ) ;
#17349=CARTESIAN_POINT ( 'NONE',  ( 127.7184548109119788, -3.484218720211406772, -13.98160872758045947 ) ) ;
#17350=CARTESIAN_POINT ( 'NONE',  ( 122.3263414775786373, -3.505236298600246325, -18.68346056562440793 ) ) ;
#17354=CARTESIAN_POINT ( 'NONE',  ( 117.0507614775786465, -10.30919188438810075, -12.61870101168855918 ) ) ;
#17356=CARTESIAN_POINT ( 'NONE',  ( 123.6877814775786533, -6.222761293078241884, -8.102969835052219238 ) ) ;
#17357=ORIENTED_EDGE ( 'NONE', *, *, #29592, .F. ) ;
#17360=CARTESIAN_POINT ( 'NONE',  ( 123.8579614775786126, 0.5811942927096110934, -14.16772938898807510 ) ) ;
#17362=CARTESIAN_POINT ( 'NONE',  ( 118.3554748109119998, -9.565557343593413364, -10.61323700422348004 ) ) ;
#17365=CARTESIAN_POINT ( 'NONE',  ( 113.4202548109119846, -10.30919188438810075, -12.61870101168855918 ) ) ;
#17366=CARTESIAN_POINT ( 'NONE',  ( 123.4608748109119745, 0.4262465694468514643, -12.03445270309931736 ) ) ;
#17369=CARTESIAN_POINT ( 'NONE',  ( 123.6310548109119765, -5.638512984488999180, -18.83840828888717311 ) ) ;
#17373=CARTESIAN_POINT ( 'NONE',  ( 122.3263414775786373, -6.344957434206665248, -7.627207830600338134 ) ) ;
#17374=CARTESIAN_POINT ( 'NONE',  ( 118.6391081442452986, -4.089484607189486809, -7.948022111789456723 ) ) ;
#17375=CARTESIAN_POINT ( 'NONE',  ( 121.4754414775786131, -1.833838273342659697, -17.42832698103878286 ) ) ;
#17376=CARTESIAN_POINT ( 'NONE',  ( 125.5492214775786550, -6.210324830719740064, -8.151390318758597431 ) ) ;
#17377=CARTESIAN_POINT ( 'NONE',  ( 115.0653281442453277, -6.344957434206662583, -7.627207830600332805 ) ) ;
#17378=ORIENTED_EDGE ( 'NONE', *, *, #39291, .F. ) ;
#17383=CARTESIAN_POINT ( 'NONE',  ( 124.7655881442452852, 0.5811942927096110934, -14.16772938898807510 ) ) ;
#17384=CARTESIAN_POINT ( 'NONE',  ( 125.2761281442453054, 0.4262465694468514643, -12.03445270309931736 ) ) ;
#17386=CARTESIAN_POINT ( 'NONE',  ( 123.9714148109119805, -0.4660016031367893996, -10.09054647747474043 ) ) ;
#17389=CARTESIAN_POINT ( 'NONE',  ( 122.1561614775786353, -0.4660016031367893996, -10.09054647747474043 ) ) ;
#17390=( BOUNDED_SURFACE ( )  B_SPLINE_SURFACE ( 1, 2, ( 
 ( #15928, #5643, #29377, #8631, #22311, #5425, #19342, #43288, #39644, #11601, #43517, #39416, #32775, #22090, #12511, #19564, #4974, #18884, #5196, #4748, #1549, #26182, #29825, #12286, #35977, #40090, #12058, #26407, #18668, #40318, #33227, #15241, #25959, #22531, #36427, #32561, #1328, #43062, #33441, #16150, #2220, #22751, #42841, #19114, #25737, #32999, #1773, #2002, #40547, #30953, #6790, #23446, #23676, #34578, #30054, #12963, #16607, #2452, #34137, #33905, #30728, #37565, #6334, #20699, #33675, #26859, #27089, #2675, #2906, #13632, #26634, #16835, #20476, #9308, #44420, #27318, #9530, #16374, #37332, #41455, #3361, #6559, #20251, #27543, #44651, #20023, #13414, #40772, #43968, #12732, #6103, #10213, #30500, #9765, #30276, #5869, #23216, #13186, #44201, #41234, #41010, #9994, #23903, #37786, #34357, #37095, #24121, #3137, #17060, #44876, #38015, #19792, #41678, #11101, #3788, #34793, #21355, #21130, #17938, #10879, #24776, #39131, #20918, #156, #14293, #35005, #35239, #824, #13848, #4016, #7667, #27763, #31612, #14517, #41894, #3576, #10655, #28656, #35698, #38897, #38667, #14745, #31837, #7218, #7435, #14071, #17280, #45092, #24561, #42562, #38447, #42119, #17488, #38227, #31171, #17713, #31385, #606, #382, #28429, #28211, #42342, #25003, #10436, #11324, #21582, #35469, #4244, #18161, #32057, #24343, #25234, #7898, #21805, #7009, #27989, #4474, #23571, #22032, #33797, #18394, #4916, #19675, #18831, #42791, #32286, #23329, #16498, #36148, #1495, #15190, #12855, #26756, #32723, #1278, #1051, #22477, #14967, #39589, #28879, #5987, #30398, #11774, #25682, #12001, #11552, #43005, #33563, #37215, #36371, #25460, #2340, #29094, #2569, #39363, #44320, #40665, #35926, #8350, #22254, #15417, #8130, #4693, #18613, #13078, #32504, #19912, #5142, #29322, #43235, #26976, #25904, #40896, #16269, #39810, #9649, #8576, #30173, #44091, #9417, #37452, #20369, #13751, #34256, #28105, #34032, #2801, #10333, #9887, #31064, #13301, #3477, #10115, #44992, #44539, #27660, #3031 ),
 ( #54, #16952, #31281, #13968, #23797, #27879, #24018, #41573, #6460, #17612, #24236, #16727, #42010, #17175, #30624, #41793, #27209, #10552, #38341, #38129, #30846, #275, #27436, #10774, #41127, #6900, #37687, #44769, #13529, #41358, #37906, #24450, #34689, #6684, #7118, #21028, #14185, #20811, #34901, #17393, #20594, #34470, #3249, #3690, #20148, #31504, #6225, #29213, #14634, #38790, #21702, #24670, #42232, #28552, #42456, #32399, #7333, #28996, #35590, #32176, #15085, #35814, #7562, #22149, #25354, #36041, #31727, #21476, #4360, #1170, #18280, #42903, #945, #32624, #21252, #38557, #14864, #7794, #35130, #28773, #21921, #11665, #8014, #42681, #4810, #11449, #39248, #498, #43123, #25574, #713, #39478, #18731, #3912, #14410, #11222, #8242, #1390, #4585, #25128, #15304, #17830, #10996, #18057, #18509, #28320, #24897, #35360, #39023, #4135, #31948, #19399, #22592, #26697, #16215, #43574, #9366, #5705, #22816, #23275, #19622, #36492, #33506, #2286, #43349, #30118, #29661, #33286, #26021, #37157, #5478, #22371, #2514, #36709, #8468, #44033, #36267, #12795, #40608, #2061, #39927, #19856, #1830, #16440, #5035, #15985, #29434, #5261, #8687, #12119, #19176, #5933, #9142, #33057, #33743, #30340, #11892, #43805, #25794, #36934, #18949, #15760, #12344, #26242, #39703, #29889, #32839, #1607, #40154, #8916, #12572, #15528, #26476, #40380, #23048, #6848, #26919, #3421, #41299, #6621, #34635, #10273, #13248, #41732, #44938, #10495, #6168, #41071, #10059, #20756, #23962, #17338, #37846, #7064, #40840, #44264, #20534, #27376, #13021, #34414, #41517, #31228, #27603, #3195, #24397, #17119, #31008, #20088, #3634, #45148, #20310, #13909, #38285, #9595, #33974, #34195, #27819, #20975, #13695, #2969, #34848, #17552, #30562, #37630, #24179, #38071, #23511, #9829, #37397, #2741, #16666, #44481, #27150, #23739, #6403, #16897, #30790, #44713, #13474, #25520, #31446, #38501, #21416, #15030, #21867, #42400, #35300, #7956, #18457, #17773, #24839, #7729, #11164, #21641, #28267, #22097, #28045 ) ),
 .UNSPECIFIED., .F., .F., .T. ) 
 B_SPLINE_SURFACE_WITH_KNOTS ( ( 2, 2 ),
 ( 3, 2, 2, 2, 2, 2, 2, 2, 2, 2, 2, 2, 2, 2, 2, 2, 2, 2, 2, 2, 2, 2, 2, 2, 2, 2, 2, 2, 2, 2, 2, 2, 2, 2, 2, 2, 2, 2, 2, 2, 2, 2, 2, 2, 2, 2, 2, 2, 2, 2, 2, 2, 2, 2, 2, 2, 2, 2, 2, 2, 2, 2, 2, 2, 2, 2, 2, 2, 2, 2, 2, 2, 2, 2, 2, 2, 2, 2, 2, 2, 2, 2, 2, 2, 2, 2, 2, 2, 2, 2, 2, 2, 2, 2, 2, 2, 2, 2, 2, 2, 2, 2, 2, 2, 2, 2, 2, 2, 2, 2, 2, 2, 2, 2, 2, 2, 2, 2, 2, 2, 2, 2, 2, 2, 2, 2, 2, 2, 3 ),
 ( 0.000000000000000000, 1.000000000000000000 ),
 ( 0.000000000000000000, 0.007812500000000000000, 0.01562500000000000000, 0.02343750000000000000, 0.03125000000000000000, 0.03906250000000000000, 0.04687500000000000000, 0.05468750000000000000, 0.06250000000000000000, 0.07031250000000000000, 0.07812500000000000000, 0.08593750000000000000, 0.09375000000000000000, 0.1015625000000000000, 0.1093750000000000000, 0.1171875000000000000, 0.1250000000000000000, 0.1328125000000000000, 0.1406250000000000000, 0.1484375000000000000, 0.1562500000000000000, 0.1640625000000000000, 0.1718750000000000000, 0.1796875000000000000, 0.1875000000000000000, 0.1953125000000000000, 0.2031250000000000000, 0.2109375000000000000, 0.2187500000000000000, 0.2265625000000000000, 0.2343750000000000000, 0.2421875000000000000, 0.2500000000000000000, 0.2578125000000000000, 0.2656250000000000000, 0.2734375000000000000, 0.2812500000000000000, 0.2890625000000000000, 0.2968750000000000000, 0.3046875000000000000, 0.3125000000000000000, 0.3203125000000000000, 0.3281250000000000000, 0.3359375000000000000, 0.3437500000000000000, 0.3515625000000000000, 0.3593750000000000000, 0.3671875000000000000, 0.3750000000000000000, 0.3828125000000000000, 0.3906250000000000000, 0.3984375000000000000, 0.4062500000000000000, 0.4140625000000000000, 0.4218750000000000000, 0.4296875000000000000, 0.4375000000000000000, 0.4453125000000000000, 0.4531250000000000000, 0.4609375000000000000, 0.4687500000000000000, 0.4765625000000000000, 0.4843750000000000000, 0.4921875000000000000, 0.5000000000000000000, 0.5078125000000000000, 0.5156250000000000000, 0.5234375000000000000, 0.5312500000000000000, 0.5390625000000000000, 0.5468750000000000000, 0.5546875000000000000, 0.5625000000000000000, 0.5703125000000000000, 0.5781250000000000000, 0.5859375000000000000, 0.5937500000000000000, 0.6015625000000000000, 0.6093750000000000000, 0.6171875000000000000, 0.6250000000000000000, 0.6328125000000000000, 0.6406250000000000000, 0.6484375000000000000, 0.6562500000000000000, 0.6640625000000000000, 0.6718750000000000000, 0.6796875000000000000, 0.6875000000000000000, 0.6953125000000000000, 0.7031250000000000000, 0.7109375000000000000, 0.7187500000000000000, 0.7265625000000000000, 0.7343750000000000000, 0.7421875000000000000, 0.7500000000000000000, 0.7578125000000000000, 0.7656250000000000000, 0.7734375000000000000, 0.7812500000000000000, 0.7890625000000000000, 0.7968750000000000000, 0.8046875000000000000, 0.8125000000000000000, 0.8203125000000000000, 0.8281250000000000000, 0.8359375000000000000, 0.8437500000000000000, 0.8515625000000000000, 0.8593750000000000000, 0.8671875000000000000, 0.8750000000000000000, 0.8828125000000000000, 0.8906250000000000000, 0.8984375000000000000, 0.9062500000000000000, 0.9140625000000000000, 0.9218750000000000000, 0.9296875000000000000, 0.9375000000000000000, 0.9453125000000000000, 0.9531250000000000000, 0.9609375000000000000, 0.9687500000000000000, 0.9765625000000000000, 0.9843750000000000000, 0.9921875000000000000, 1.000000000000000000 ),
 .UNSPECIFIED. ) 
 GEOMETRIC_REPRESENTATION_ITEM ( )  RATIONAL_B_SPLINE_SURFACE ( (
 ( 1.000000000000000000, 0.9238795325112869605, 1.000000000000000000, 0.9238795325112869605, 1.000000000000000000, 0.9238795325112869605, 1.000000000000000000, 0.9238795325112869605, 1.000000000000000000, 0.9238795325112869605, 1.000000000000000000, 0.9238795325112869605, 1.000000000000000000, 0.9238795325112869605, 1.000000000000000000, 0.9238795325112869605, 1.000000000000000000, 0.9238795325112869605, 1.000000000000000000, 0.9238795325112869605, 1.000000000000000000, 0.9238795325112869605, 1.000000000000000000, 0.9238795325112869605, 1.000000000000000000, 0.9238795325112869605, 1.000000000000000000, 0.9238795325112869605, 1.000000000000000000, 0.9238795325112869605, 1.000000000000000000, 0.9238795325112869605, 1.000000000000000000, 0.9238795325112869605, 1.000000000000000000, 0.9238795325112869605, 1.000000000000000000, 0.9238795325112869605, 1.000000000000000000, 0.9238795325112869605, 1.000000000000000000, 0.9238795325112869605, 1.000000000000000000, 0.9238795325112869605, 1.000000000000000000, 0.9238795325112869605, 1.000000000000000000, 0.9238795325112869605, 1.000000000000000000, 0.9238795325112869605, 1.000000000000000000, 0.9238795325112869605, 1.000000000000000000, 0.9238795325112869605, 1.000000000000000000, 0.9238795325112869605, 1.000000000000000000, 0.9238795325112869605, 1.000000000000000000, 0.9238795325112869605, 1.000000000000000000, 0.9238795325112869605, 1.000000000000000000, 0.9238795325112869605, 1.000000000000000000, 0.9238795325112869605, 1.000000000000000000, 0.9238795325112869605, 1.000000000000000000, 0.9238795325112869605, 1.000000000000000000, 0.9238795325112869605, 1.000000000000000000, 0.9238795325112869605, 1.000000000000000000, 0.9238795325112869605, 1.000000000000000000, 0.9238795325112869605, 1.000000000000000000, 0.9238795325112869605, 1.000000000000000000, 0.9238795325112869605, 1.000000000000000000, 0.9238795325112869605, 1.000000000000000000, 0.9238795325112869605, 1.000000000000000000, 0.9238795325112869605, 1.000000000000000000, 0.9238795325112869605, 1.000000000000000000, 0.9238795325112869605, 1.000000000000000000, 0.9238795325112869605, 1.000000000000000000, 0.9238795325112869605, 1.000000000000000000, 0.9238795325112869605, 1.000000000000000000, 0.9238795325112869605, 1.000000000000000000, 0.9238795325112869605, 1.000000000000000000, 0.9238795325112869605, 1.000000000000000000, 0.9238795325112869605, 1.000000000000000000, 0.9238795325112869605, 1.000000000000000000, 0.9238795325112869605, 1.000000000000000000, 0.9238795325112869605, 1.000000000000000000, 0.9238795325112869605, 1.000000000000000000, 0.9238795325112869605, 1.000000000000000000, 0.9238795325112869605, 1.000000000000000000, 0.9238795325112869605, 1.000000000000000000, 0.9238795325112869605, 1.000000000000000000, 0.9238795325112869605, 1.000000000000000000, 0.9238795325112869605, 1.000000000000000000, 0.9238795325112869605, 1.000000000000000000, 0.9238795325112869605, 1.000000000000000000, 0.9238795325112869605, 1.000000000000000000, 0.9238795325112869605, 1.000000000000000000, 0.9238795325112869605, 1.000000000000000000, 0.9238795325112869605, 1.000000000000000000, 0.9238795325112869605, 1.000000000000000000, 0.9238795325112869605, 1.000000000000000000, 0.9238795325112869605, 1.000000000000000000, 0.9238795325112869605, 1.000000000000000000, 0.9238795325112869605, 1.000000000000000000, 0.9238795325112869605, 1.000000000000000000, 0.9238795325112869605, 1.000000000000000000, 0.9238795325112869605, 1.000000000000000000, 0.9238795325112869605, 1.000000000000000000, 0.9238795325112869605, 1.000000000000000000, 0.9238795325112869605, 1.000000000000000000, 0.9238795325112869605, 1.000000000000000000, 0.9238795325112869605, 1.000000000000000000, 0.9238795325112869605, 1.000000000000000000, 0.9238795325112869605, 1.000000000000000000, 0.9238795325112869605, 1.000000000000000000, 0.9238795325112869605, 1.000000000000000000, 0.9238795325112869605, 1.000000000000000000, 0.9238795325112869605, 1.000000000000000000, 0.9238795325112869605, 1.000000000000000000, 0.9238795325112869605, 1.000000000000000000, 0.9238795325112869605, 1.000000000000000000, 0.9238795325112869605, 1.000000000000000000, 0.9238795325112869605, 1.000000000000000000, 0.9238795325112869605, 1.000000000000000000, 0.9238795325112869605, 1.000000000000000000, 0.9238795325112869605, 1.000000000000000000, 0.9238795325112869605, 1.000000000000000000, 0.9238795325112869605, 1.000000000000000000, 0.9238795325112869605, 1.000000000000000000, 0.9238795325112869605, 1.000000000000000000, 0.9238795325112869605, 1.000000000000000000, 0.9238795325112869605, 1.000000000000000000, 0.9238795325112869605, 1.000000000000000000, 0.9238795325112869605, 1.000000000000000000, 0.9238795325112869605, 1.000000000000000000, 0.9238795325112869605, 1.000000000000000000, 0.9238795325112869605, 1.000000000000000000, 0.9238795325112869605, 1.000000000000000000, 0.9238795325112869605, 1.000000000000000000, 0.9238795325112869605, 1.000000000000000000, 0.9238795325112869605, 1.000000000000000000, 0.9238795325112869605, 1.000000000000000000, 0.9238795325112869605, 1.000000000000000000, 0.9238795325112869605, 1.000000000000000000, 0.9238795325112869605, 1.000000000000000000, 0.9238795325112869605, 1.000000000000000000, 0.9238795325112869605, 1.000000000000000000, 0.9238795325112869605, 1.000000000000000000, 0.9238795325112869605, 1.000000000000000000, 0.9238795325112869605, 1.000000000000000000, 0.9238795325112869605, 1.000000000000000000, 0.9238795325112869605, 1.000000000000000000, 0.9238795325112869605, 1.000000000000000000, 0.9238795325112869605, 1.000000000000000000, 0.9238795325112869605, 1.000000000000000000, 0.9238795325112869605, 1.000000000000000000, 0.9238795325112869605, 1.000000000000000000, 0.9238795325112869605, 1.000000000000000000),
 ( 1.000000000000000000, 0.9238795325112869605, 1.000000000000000000, 0.9238795325112869605, 1.000000000000000000, 0.9238795325112869605, 1.000000000000000000, 0.9238795325112869605, 1.000000000000000000, 0.9238795325112869605, 1.000000000000000000, 0.9238795325112869605, 1.000000000000000000, 0.9238795325112869605, 1.000000000000000000, 0.9238795325112869605, 1.000000000000000000, 0.9238795325112869605, 1.000000000000000000, 0.9238795325112869605, 1.000000000000000000, 0.9238795325112869605, 1.000000000000000000, 0.9238795325112869605, 1.000000000000000000, 0.9238795325112869605, 1.000000000000000000, 0.9238795325112869605, 1.000000000000000000, 0.9238795325112869605, 1.000000000000000000, 0.9238795325112869605, 1.000000000000000000, 0.9238795325112869605, 1.000000000000000000, 0.9238795325112869605, 1.000000000000000000, 0.9238795325112869605, 1.000000000000000000, 0.9238795325112869605, 1.000000000000000000, 0.9238795325112869605, 1.000000000000000000, 0.9238795325112869605, 1.000000000000000000, 0.9238795325112869605, 1.000000000000000000, 0.9238795325112869605, 1.000000000000000000, 0.9238795325112869605, 1.000000000000000000, 0.9238795325112869605, 1.000000000000000000, 0.9238795325112869605, 1.000000000000000000, 0.9238795325112869605, 1.000000000000000000, 0.9238795325112869605, 1.000000000000000000, 0.9238795325112869605, 1.000000000000000000, 0.9238795325112869605, 1.000000000000000000, 0.9238795325112869605, 1.000000000000000000, 0.9238795325112869605, 1.000000000000000000, 0.9238795325112869605, 1.000000000000000000, 0.9238795325112869605, 1.000000000000000000, 0.9238795325112869605, 1.000000000000000000, 0.9238795325112869605, 1.000000000000000000, 0.9238795325112869605, 1.000000000000000000, 0.9238795325112869605, 1.000000000000000000, 0.9238795325112869605, 1.000000000000000000, 0.9238795325112869605, 1.000000000000000000, 0.9238795325112869605, 1.000000000000000000, 0.9238795325112869605, 1.000000000000000000, 0.9238795325112869605, 1.000000000000000000, 0.9238795325112869605, 1.000000000000000000, 0.9238795325112869605, 1.000000000000000000, 0.9238795325112869605, 1.000000000000000000, 0.9238795325112869605, 1.000000000000000000, 0.9238795325112869605, 1.000000000000000000, 0.9238795325112869605, 1.000000000000000000, 0.9238795325112869605, 1.000000000000000000, 0.9238795325112869605, 1.000000000000000000, 0.9238795325112869605, 1.000000000000000000, 0.9238795325112869605, 1.000000000000000000, 0.9238795325112869605, 1.000000000000000000, 0.9238795325112869605, 1.000000000000000000, 0.9238795325112869605, 1.000000000000000000, 0.9238795325112869605, 1.000000000000000000, 0.9238795325112869605, 1.000000000000000000, 0.9238795325112869605, 1.000000000000000000, 0.9238795325112869605, 1.000000000000000000, 0.9238795325112869605, 1.000000000000000000, 0.9238795325112869605, 1.000000000000000000, 0.9238795325112869605, 1.000000000000000000, 0.9238795325112869605, 1.000000000000000000, 0.9238795325112869605, 1.000000000000000000, 0.9238795325112869605, 1.000000000000000000, 0.9238795325112869605, 1.000000000000000000, 0.9238795325112869605, 1.000000000000000000, 0.9238795325112869605, 1.000000000000000000, 0.9238795325112869605, 1.000000000000000000, 0.9238795325112869605, 1.000000000000000000, 0.9238795325112869605, 1.000000000000000000, 0.9238795325112869605, 1.000000000000000000, 0.9238795325112869605, 1.000000000000000000, 0.9238795325112869605, 1.000000000000000000, 0.9238795325112869605, 1.000000000000000000, 0.9238795325112869605, 1.000000000000000000, 0.9238795325112869605, 1.000000000000000000, 0.9238795325112869605, 1.000000000000000000, 0.9238795325112869605, 1.000000000000000000, 0.9238795325112869605, 1.000000000000000000, 0.9238795325112869605, 1.000000000000000000, 0.9238795325112869605, 1.000000000000000000, 0.9238795325112869605, 1.000000000000000000, 0.9238795325112869605, 1.000000000000000000, 0.9238795325112869605, 1.000000000000000000, 0.9238795325112869605, 1.000000000000000000, 0.9238795325112869605, 1.000000000000000000, 0.9238795325112869605, 1.000000000000000000, 0.9238795325112869605, 1.000000000000000000, 0.9238795325112869605, 1.000000000000000000, 0.9238795325112869605, 1.000000000000000000, 0.9238795325112869605, 1.000000000000000000, 0.9238795325112869605, 1.000000000000000000, 0.9238795325112869605, 1.000000000000000000, 0.9238795325112869605, 1.000000000000000000, 0.9238795325112869605, 1.000000000000000000, 0.9238795325112869605, 1.000000000000000000, 0.9238795325112869605, 1.000000000000000000, 0.9238795325112869605, 1.000000000000000000, 0.9238795325112869605, 1.000000000000000000, 0.9238795325112869605, 1.000000000000000000, 0.9238795325112869605, 1.000000000000000000, 0.9238795325112869605, 1.000000000000000000, 0.9238795325112869605, 1.000000000000000000, 0.9238795325112869605, 1.000000000000000000, 0.9238795325112869605, 1.000000000000000000, 0.9238795325112869605, 1.000000000000000000, 0.9238795325112869605, 1.000000000000000000, 0.9238795325112869605, 1.000000000000000000, 0.9238795325112869605, 1.000000000000000000, 0.9238795325112869605, 1.000000000000000000, 0.9238795325112869605, 1.000000000000000000, 0.9238795325112869605, 1.000000000000000000, 0.9238795325112869605, 1.000000000000000000, 0.9238795325112869605, 1.000000000000000000, 0.9238795325112869605, 1.000000000000000000, 0.9238795325112869605, 1.000000000000000000, 0.9238795325112869605, 1.000000000000000000, 0.9238795325112869605, 1.000000000000000000, 0.9238795325112869605, 1.000000000000000000, 0.9238795325112869605, 1.000000000000000000, 0.9238795325112869605, 1.000000000000000000, 0.9238795325112869605, 1.000000000000000000, 0.9238795325112869605, 1.000000000000000000, 0.9238795325112869605, 1.000000000000000000, 0.9238795325112869605, 1.000000000000000000) ) ) 
 REPRESENTATION_ITEM ( '' )  SURFACE ( )  );
#17391=CARTESIAN_POINT ( 'NONE',  ( 125.6732148109119862, 0.5811942927096110934, -14.16772938898807510 ) ) ;
#17393=CARTESIAN_POINT ( 'NONE',  ( 113.9307948109119906, 0.9020085738987339008, -11.91225656197089222 ) ) ;
#17396=ORIENTED_EDGE ( 'NONE', *, *, #40117, .F. ) ;
#17397=CARTESIAN_POINT ( 'NONE',  ( 138.2184548109119930, -4.105398160058917334, -19.34506575923121474 ) ) ;
#17398=CARTESIAN_POINT ( 'NONE',  ( 115.8595014775786609, -7.643976991954077427, -18.09477374809248928 ) ) ;
#17399=CARTESIAN_POINT ( 'NONE',  ( 113.9875214775786532, -0.4660016031367893996, -10.09054647747474043 ) ) ;
#17402=CARTESIAN_POINT ( 'NONE',  ( 120.7379948109119709, 0.4262465694468514643, -12.03445270309931736 ) ) ;
#17403=CARTESIAN_POINT ( 'NONE',  ( 117.0507614775786465, 0.1319031606808879209, -14.10382304977623669 ) ) ;
#17404=CARTESIAN_POINT ( 'NONE',  ( 111.3780948109119890, -5.574606645277164318, -18.38911715685844683 ) ) ;
#17405=ORIENTED_EDGE ( 'NONE', *, *, #37021, .F. ) ;
#17406=CARTESIAN_POINT ( 'NONE',  ( 124.2550481442452792, -0.1624402480850797581, -16.17319339645315424 ) ) ;
#17409=CARTESIAN_POINT ( 'NONE',  ( 115.8595014775786609, -7.643976991954077427, -18.09477374809248928 ) ) ;
#17410=ORIENTED_EDGE ( 'NONE', *, *, #20874, .T. ) ;
#17411=CARTESIAN_POINT ( 'NONE',  ( 126.2184548109119788, 0.08617673920515746266, -14.09731900820182915 ) ) ;
#17413=CARTESIAN_POINT ( 'NONE',  ( 120.2274548109119934, -9.859900752359374465, -12.68260735090039404 ) ) ;
#17414=CARTESIAN_POINT ( 'NONE',  ( 115.0653281442453277, -3.505236298600246325, -18.68346056562440793 ) ) ;
#17415=CARTESIAN_POINT ( 'NONE',  ( 117.5676200025837090, -2.311015703046737535, -18.04188382666267998 ) ) ;
#17422=CARTESIAN_POINT ( 'NONE',  ( 124.5386814775786206, -4.153390946401325223, -8.397313243818185668 ) ) ;
#17423=CARTESIAN_POINT ( 'NONE',  ( 118.8660148109119774, 0.1319031606808879209, -14.10382304977623669 ) ) ;
#17424=CARTESIAN_POINT ( 'NONE',  ( 113.8740681442453138, -9.859900752359374465, -12.68260735090037983 ) ) ;
#17427=CARTESIAN_POINT ( 'NONE',  ( 116.7671281442453335, -7.643976991954077427, -18.09477374809248928 ) ) ;
#17430=CARTESIAN_POINT ( 'NONE',  ( 116.7619158011494136, -1.149058757900091265, -17.09122335155388939 ) ) ;
#17431=CARTESIAN_POINT ( 'NONE',  ( 114.4413348109119823, -9.261995988541697145, -16.69588392320189030 ) ) ;
#17433=CARTESIAN_POINT ( 'NONE',  ( 115.4056881442453459, -7.893985811506177619, -18.51759400769804742 ) ) ;
#17437=CARTESIAN_POINT ( 'NONE',  ( 111.8319081442453182, -5.638512984488999180, -18.83840828888717311 ) ) ;
#17438=CARTESIAN_POINT ( 'NONE',  ( 112.9097148109120070, 0.2603800115204892296, -16.42320221600525088 ) ) ;
#17439=CARTESIAN_POINT ( 'NONE',  ( 124.6521348109119884, -7.894159318335828068, -9.358103419637847864 ) ) ;
#17444=CARTESIAN_POINT ( 'NONE',  ( 117.6747548109119919, -7.643976991954077427, -18.09477374809248928 ) ) ;
#17447=CARTESIAN_POINT ( 'NONE',  ( 125.2761281442453054, -10.63000616557722466, -14.87417383870573495 ) ) ;
#17448=CARTESIAN_POINT ( 'NONE',  ( 123.9714148109119805, -0.4660016031367893996, -10.09054647747474043 ) ) ;
#17449=CARTESIAN_POINT ( 'NONE',  ( 120.4543614775786295, -5.574606645277196293, -18.38911715685844683 ) ) ;
#17450=CARTESIAN_POINT ( 'NONE',  ( 120.9081748109119872, -5.638512984488999180, -18.83840828888717311 ) ) ;
#17451=CARTESIAN_POINT ( 'NONE',  ( 115.4056881442453459, -7.893985811506177619, -18.51759400769804742 ) ) ;
#17453=CARTESIAN_POINT ( 'NONE',  ( 115.9729548109119861, -3.505236298600246325, -18.68346056562440793 ) ) ;
#17454=CARTESIAN_POINT ( 'NONE',  ( 124.4252281442452812, -9.261995988541697145, -16.69588392320189030 ) ) ;
#17455=CARTESIAN_POINT ( 'NONE',  ( 119.6034614775786196, -6.344957434206665248, -7.627207830600338134 ) ) ;
#17456=CARTESIAN_POINT ( 'NONE',  ( 114.8384214775786489, -10.15424416112533912, -14.75197769757731336 ) ) ;
#17458=CARTESIAN_POINT ( 'NONE',  ( 121.1918081442452859, -10.15424416112533912, -14.75197769757731336 ) ) ;
#17459=CARTESIAN_POINT ( 'NONE',  ( 115.5758681442453053, -1.561330072975668060, -17.79121239304076951 ) ) ;
#17460=CARTESIAN_POINT ( 'NONE',  ( 136.6626210033597886, 0.7813541710858115108, -12.84505551963111891 ) ) ;
#17467=CARTESIAN_POINT ( 'NONE',  ( 113.8740681442453138, 0.5811942927096154232, -14.16772938898807155 ) ) ;
#17474=CARTESIAN_POINT ( 'NONE',  ( 116.4267681442453153, -3.383040157471821630, -19.15922257007629170 ) ) ;
#17478=CARTESIAN_POINT ( 'NONE',  ( 138.2184548109119930, 0.7334521766912248664, -9.189818643966587430 ) ) ;
#17481=CARTESIAN_POINT ( 'NONE',  ( 121.4754414775786131, -8.166667518702819706, -8.995218007635861213 ) ) ;
#17483=CARTESIAN_POINT ( 'NONE',  ( 116.5969481442453031, -9.859900752359374465, -12.68260735090039404 ) ) ;
#17484=EDGE_CURVE ( 'NONE', #41948, #1558, #33741, .T. ) ;
#17485=CARTESIAN_POINT ( 'NONE',  ( 113.8173414775786512, -9.565557343593413364, -10.61323700422348004 ) ) ;
#17488=CARTESIAN_POINT ( 'NONE',  ( 120.7947214775786193, -0.8288870151387760510, -10.36305467784173118 ) ) ;
#17489=CARTESIAN_POINT ( 'NONE',  ( 120.6812681442452941, 0.1319031606808879209, -14.10382304977623669 ) ) ;
#17494=CARTESIAN_POINT ( 'NONE',  ( 113.4769814775786330, -10.63000616557722466, -14.87417383870573495 ) ) ;
#17495=CARTESIAN_POINT ( 'NONE',  ( 116.0864081442453113, -9.988377603198976828, -10.36322818467138340 ) ) ;
#17498=B_SPLINE_CURVE_WITH_KNOTS ( 'NONE', 3,
 ( #24539, #11302, #13829, #35447, #10417, #24324, #21335, #35220, #42317, #42095, #17693, #34773, #10635, #4222, #41874, #18140, #10859, #38428, #7196, #28634, #42541, #34983, #25211, #28189, #31591, #1920, #15848, #11979, #39340, #1029, #32481, #32921, #26331, #39783, #29073, #32261, #8106, #19267, #8773, #12432, #25881, #15617, #22677, #29743, #29299, #43656, #43439, #1473, #35903, #36347, #42769, #15395, #1255, #36575, #32702, #12203 ),
 .UNSPECIFIED., .F., .F.,
 ( 4, 2, 2, 2, 2, 2, 2, 1, 2, 2, 2, 2, 2, 2, 2, 2, 2, 2, 2, 2, 2, 1, 2, 2, 2, 2, 2, 2, 4 ),
 ( 0.000000000000000000, 0.06249999999995559108, 0.09374999999993996469, 0.1093749999999387573, 0.1249999999999375500, 0.1874999999999329425, 0.2187499999999246436, 0.2343749999999204803, 0.2421874999999237832, 0.2499999999999271139, 0.3124999999999338307, 0.3437499999999332756, 0.3593749999999370504, 0.3749999999999408251, 0.4999999999999611422, 0.5624999999999709122, 0.5937499999999757971, 0.6093749999999760192, 0.6249999999999762412, 0.6874999999999791278, 0.7187499999999805711, 0.7343749999999812372, 0.7421874999999814593, 0.7499999999999816813, 0.8124999999999922284, 0.8437499999999976685, 0.8593750000000004441, 0.8750000000000032196, 1.000000000000000000 ),
 .UNSPECIFIED. ) ;
#17501=CARTESIAN_POINT ( 'NONE',  ( 122.4965214775786251, -10.30919188438810075, -12.61870101168855918 ) ) ;
#17503=CARTESIAN_POINT ( 'NONE',  ( 114.4980614775786592, -7.893985811506177619, -18.51759400769804742 ) ) ;
#17504=CARTESIAN_POINT ( 'NONE',  ( 117.9583881442453048, 0.1319031606808879209, -14.10382304977623669 ) ) ;
#17506=CARTESIAN_POINT ( 'NONE',  ( 125.3328548109119964, -9.261995988541697145, -16.69588392320189030 ) ) ;
#17507=CARTESIAN_POINT ( 'NONE',  ( 118.0151148109119816, -10.63000616557722466, -14.87417383870573495 ) ) ;
#17510=CARTESIAN_POINT ( 'NONE',  ( 113.1933481442453058, -5.574606645277164318, -18.38911715685844683 ) ) ;
#17513=CARTESIAN_POINT ( 'NONE',  ( 122.9503348109119827, 0.5811942927096110934, -14.16772938898807510 ) ) ;
#17517=CARTESIAN_POINT ( 'NONE',  ( 115.7460481442453357, 0.9020085738987339008, -11.91225656197089222 ) ) ;
#17520=CARTESIAN_POINT ( 'NONE',  ( 123.7445081442452874, -1.561330072975668948, -17.79121239304076951 ) ) ;
#17522=CARTESIAN_POINT ( 'NONE',  ( 122.5532481442453019, -10.63000616557722999, -14.87417383870572962 ) ) ;
#17523=CARTESIAN_POINT ( 'NONE',  ( 112.3424481442453384, -3.505236298600246325, -18.68346056562440793 ) ) ;
#17525=CARTESIAN_POINT ( 'NONE',  ( 120.5678148109119832, -1.833838273342659253, -17.42832698103878286 ) ) ;
#17528=CARTESIAN_POINT ( 'NONE',  ( 121.7590748109119687, -2.084020599724406786, -8.691656652584148546 ) ) ;
#17531=CARTESIAN_POINT ( 'NONE',  ( 120.1707281442453166, -9.565557343593413364, -10.61323700422348004 ) ) ;
#17535=CARTESIAN_POINT ( 'NONE',  ( 117.4478481442453131, 0.2603800115204892296, -16.42320221600525088 ) ) ;
#17536=CARTESIAN_POINT ( 'NONE',  ( 122.0950914740559199, -1.081026697600536046, -17.18181821144402832 ) ) ;
#17538=EDGE_CURVE ( 'NONE', #16862, #2299, #15028, .T. ) ;
#17539=CARTESIAN_POINT ( 'NONE',  ( 117.1074881442453233, 0.4262465694468514643, -12.03445270309931736 ) ) ;
#17541=CARTESIAN_POINT ( 'NONE',  ( 115.2355081442453155, -10.30919188438810075, -12.61870101168855918 ) ) ;
#17545=CARTESIAN_POINT ( 'NONE',  ( 127.9707505455493219, -4.185443562423379227, -15.54568186907484950 ) ) ;
#17546=CARTESIAN_POINT ( 'NONE',  ( 121.9292548109119849, -1.561330072975668948, -17.79121239304076951 ) ) ;
#17548=CARTESIAN_POINT ( 'NONE',  ( 126.9115046738297536, -8.805351640776619249, -9.780119036498003737 ) ) ;
#17549=CARTESIAN_POINT ( 'NONE',  ( 117.3343948109119737, -6.222761293078241884, -8.102969835052219238 ) ) ;
#17550=CARTESIAN_POINT ( 'NONE',  ( 116.4642898793805443, -2.191907684172563986, -18.20049396185734025 ) ) ;
#17552=CARTESIAN_POINT ( 'NONE',  ( 124.2550481442452792, -9.988377603198980381, -10.36322818467138518 ) ) ;
#17556=CARTESIAN_POINT ( 'NONE',  ( 113.8740681442453138, 0.5811942927096154232, -14.16772938898807155 ) ) ;
#17557=CARTESIAN_POINT ( 'NONE',  ( 126.5808414775786446, -9.859900752359378018, -12.68260735090039759 ) ) ;
#17558=CARTESIAN_POINT ( 'NONE',  ( 123.1205148109119563, -1.834011780172310813, -8.268836392978581529 ) ) ;
#17560=CARTESIAN_POINT ( 'NONE',  ( 118.8660148109119774, 0.1319031606808879209, -14.10382304977623669 ) ) ;
#17563=CARTESIAN_POINT ( 'NONE',  ( 117.5045748109119756, 0.5811942927096110934, -14.16772938898807510 ) ) ;
#17566=CARTESIAN_POINT ( 'NONE',  ( 124.5386814775786206, -4.153390946401325223, -8.397313243818185668 ) ) ;
#17570=CARTESIAN_POINT ( 'NONE',  ( 118.5823814775786360, -1.834011780172310813, -8.268836392978581529 ) ) ;
#17571=CARTESIAN_POINT ( 'NONE',  ( 136.2267163768046032, -8.499329989147907938, -17.98615556580662656 ) ) ;
#17575=CARTESIAN_POINT ( 'NONE',  ( 137.5082292857839548, -1.031900795168988250, -10.16812068200164454 ) ) ;
#17576=CARTESIAN_POINT ( 'NONE',  ( 123.6877814775786533, -3.383040157471821630, -19.15922257007629170 ) ) ;
#17578=CARTESIAN_POINT ( 'NONE',  ( 121.3052614775786111, -7.643976991954077427, -18.09477374809248928 ) ) ;
#17581=CARTESIAN_POINT ( 'NONE',  ( 112.6828081442453282, -7.893985811506177619, -18.51759400769804742 ) ) ;
#17583=CARTESIAN_POINT ( 'NONE',  ( 120.6812681442452941, -10.30919188438810075, -12.61870101168855918 ) ) ;
#17586=CARTESIAN_POINT ( 'NONE',  ( 123.1772414775786189, -4.089484607189486809, -7.948022111789456723 ) ) ;
#17590=CARTESIAN_POINT ( 'NONE',  ( 124.3685014775786328, -10.63000616557722466, -14.87417383870573495 ) ) ;
#17591=CARTESIAN_POINT ( 'NONE',  ( 120.3976348109119812, -1.834011780172310813, -8.268836392978581529 ) ) ;
#17592=CARTESIAN_POINT ( 'NONE',  ( 124.8790414775786246, -8.899110576539710493, -16.42337572283490132 ) ) ;
#17593=CARTESIAN_POINT ( 'NONE',  ( 119.8303681442453126, 0.4262465694468514643, -12.03445270309931736 ) ) ;
#17594=CARTESIAN_POINT ( 'NONE',  ( 125.7194014775786286, -9.814174330883794539, -12.68911139247586739 ) ) ;
#17595=CARTESIAN_POINT ( 'NONE',  ( 114.7249681442453237, 0.2603800115204892296, -16.42320221600525088 ) ) ;
#17599=AXIS2_PLACEMENT_3D ( 'NONE', #16437, #30335, #6165 ) ;
#17602=CARTESIAN_POINT ( 'NONE',  ( 126.1270281442452870, -10.30919188438810075, -12.61870101168855918 ) ) ;
#17603=CARTESIAN_POINT ( 'NONE',  ( 126.2404814775786264, -0.8288870151387760510, -10.36305467784173118 ) ) ;
#17604=ORIENTED_EDGE ( 'NONE', *, *, #19256, .T. ) ;
#17605=CARTESIAN_POINT ( 'NONE',  ( 114.3278814775786429, 0.1319031606808879209, -14.10382304977623669 ) ) ;
#17609=CARTESIAN_POINT ( 'NONE',  ( 124.1415948109119540, -6.344957434206665248, -7.627207830600338134 ) ) ;
#17610=CARTESIAN_POINT ( 'NONE',  ( 123.1205148109119563, -1.834011780172310813, -8.268836392978581529 ) ) ;
#17612=CARTESIAN_POINT ( 'NONE',  ( 112.2289948109119848, -1.834011780172310813, -8.268836392978581529 ) ) ;
#17616=CARTESIAN_POINT ( 'NONE',  ( 121.4964260444391755, -1.267766418764731728, -16.93314635290706605 ) ) ;
#17617=CARTESIAN_POINT ( 'NONE',  ( 115.8027748109119841, -8.899110576539710493, -16.42337572283490132 ) ) ;
#17618=CARTESIAN_POINT ( 'NONE',  ( 114.1577014775786552, -6.344957434206662583, -7.627207830600332805 ) ) ;
#17621=CARTESIAN_POINT ( 'NONE',  ( 122.3263414775786373, -3.505236298600246325, -18.68346056562440793 ) ) ;
#17622=CARTESIAN_POINT ( 'NONE',  ( 120.2274548109119934, -9.859900752359378018, -12.68260735090039759 ) ) ;
#17623=CARTESIAN_POINT ( 'NONE',  ( 125.6164881442453094, 0.2603800115204892296, -16.42320221600525088 ) ) ;
#17627=CARTESIAN_POINT ( 'NONE',  ( 112.9097148109120070, -9.565557343593413364, -10.61323700422348004 ) ) ;
#17633=CARTESIAN_POINT ( 'NONE',  ( 117.0507614775786465, 0.1319031606808879209, -14.10382304977623669 ) ) ;
#17634=CARTESIAN_POINT ( 'NONE',  ( 114.1577014775786552, -3.505236298600246325, -18.68346056562440793 ) ) ;
#17637=ORIENTED_EDGE ( 'NONE', *, *, #30147, .T. ) ;
#17641=CARTESIAN_POINT ( 'NONE',  ( 113.7038881442453402, -3.383040157471821630, -19.15922257007629170 ) ) ;
#17642=CARTESIAN_POINT ( 'NONE',  ( 122.3830681442452857, -1.833838273342659697, -17.42832698103878286 ) ) ;
#17643=( BOUNDED_SURFACE ( )  B_SPLINE_SURFACE ( 1, 2, ( 
 ( #28843, #28390, #7181, #11064, #29060, #24966, #38862, #42755, #21994, #7865, #17678, #11518, #35433, #4654, #4207, #32467, #1243, #784, #28619, #42529, #11289, #21771, #21091, #31576, #11736, #25648, #344, #14257, #25197, #22888, #26543, #8538, #5773, #5552, #4882, #40454, #16287, #32905, #33131, #44107, #39552, #22439, #26087, #11964, #43641, #43422, #40224, #1901, #15830, #30189, #43198, #36332, #36559, #12187, #12415, #23125, #36111, #26315, #29960, #18799, #8757, #36781, #19017, #25863, #1680, #19693, #12874, #16054, #29727, #37002, #8988, #29506, #19470, #5102, #8314, #22214, #15602, #33580, #39991, #19250, #39767, #15379, #32688, #22662, #5333, #33352, #2125, #43876, #12647, #9216, #2356, #1458, #29284, #41143, #10129, #27225, #13543, #9667, #37230, #44785, #16744, #27675, #19927, #33814, #26773, #40682, #44334, #3264, #9434, #13321, #30862, #9902, #2584, #6005, #20612, #45006, #44555, #6474, #31080, #34272, #2815, #20386, #23585, #23347, #30414, #23815, #16515, #37703, #27451, #30638, #6241, #13094, #3045, #16970, #34486, #41374, #24033, #37924, #17189, #6701, #40913, #26993, #13766, #37469, #41590, #20164, #34047, #1594, #16200, #22800, #26906, #29421, #43335, #22358, #40826, #39912, #5919, #36252, #36695, #36919, #5464, #15514, #5019, #40594, #33729, #8902, #19384, #33273, #23031, #33043, #2500, #19162, #18936, #40364, #32823, #12104, #30103, #44019, #29646, #26008, #8674, #30323, #36478, #15744, #5689, #9352, #9127, #22577, #19608, #1817, #19841, #5245, #16427, #12780, #43560, #12329, #40138, #15971, #33492, #26229, #2047, #44250, #29874, #37145, #13007, #43790, #2270, #23262, #12555, #26461, #26682, #12434, #36799, #32923, #22906, #29745, #5120, #29301, #15850, #26333, #25662, #32704, #15619, #19036, #29525, #36126, #29976, #35905, #4670, #12205, #11753, #1699, #15168, #5353, #11981, #43441, #1257, #26103, #4895, #9009, #43658, #25883, #5567, #33148, #40010, #1475, #42986, #8775, #39785, #22679, #36577, #19269, #18812, #22009, #19489, #1922, #40240 ),
 ( #39567, #33371, #2141, #16072, #43893, #12662, #39342, #29075, #8331, #8554, #22230, #18592, #8108, #32483, #15397, #43214, #22455, #36349, #16304, #44126, #16534, #30431, #34290, #30205, #3063, #27015, #37720, #33598, #13341, #44350, #16990, #27245, #37945, #2374, #23368, #37487, #30881, #23602, #44801, #20181, #34506, #23143, #26560, #6261, #12891, #3284, #23834, #6491, #13560, #9920, #16761, #20629, #27470, #41390, #13110, #31099, #10143, #2602, #24052, #20405, #6718, #17206, #34066, #45024, #40473, #2832, #40932, #9234, #37023, #26789, #19945, #30658, #44576, #41159, #37249, #5793, #19712, #40698, #9454, #6022, #33833, #9685, #24931, #31541, #21283, #20844, #35169, #24488, #28586, #18092, #310, #11256, #7596, #24703, #25164, #21511, #38376, #35398, #4174, #90, #31985, #14224, #3946, #27918, #39062, #7370, #24274, #4402, #10808, #748, #17868, #21738, #10366, #13782, #38593, #34723, #35627, #11032, #38828, #14672, #42267, #31765, #7832, #42496, #18319, #28139, #32210, #27694, #34937, #41611, #38162, #6938, #3506, #537, #17423, #31315, #14448, #3724, #14002, #41828, #10588, #7148, #28354, #21059, #17644, #42048, #36747, #42719, #11486, #18986, #18543, #39735, #21960, #12154, #18768, #8504, #8055, #22408, #11702, #15795, #5300, #32657, #43609, #39961, #11930, #12384, #8723, #25613, #22629, #36528, #32435, #19216, #1425, #36301, #15123, #26282, #5069, #25391, #5515, #25828, #39287, #33096, #35848, #1866, #29697, #32874, #29030, #8957, #36078, #19435, #4622, #1644, #1209, #39516, #42940, #8280, #22182, #40190, #43386, #4850, #22856, #984, #14899, #15567, #28810, #26057, #15344, #29253, #43162, #29471, #16020, #23551, #37888, #6664, #26955, #23310, #10097, #23086, #5738, #37195, #5968, #41109, #36967, #9867, #33779, #44518, #40420, #20126, #19892, #23776, #34013, #44751, #9179, #30154, #44301, #37668, #27189, #2549, #33320, #19657, #33544, #2094, #29928, #2323, #16932, #43842, #16478, #2782, #30379, #26512, #12609, #6444, #13510, #13056, #40877, #9630, #16707 ) ),
 .UNSPECIFIED., .F., .F., .F. ) 
 B_SPLINE_SURFACE_WITH_KNOTS ( ( 2, 2 ),
 ( 3, 2, 2, 2, 2, 2, 2, 2, 2, 2, 2, 2, 2, 2, 2, 2, 2, 2, 2, 2, 2, 2, 2, 2, 2, 2, 2, 2, 2, 2, 2, 2, 2, 2, 2, 2, 2, 2, 2, 2, 2, 2, 2, 2, 2, 2, 2, 2, 2, 2, 2, 2, 2, 2, 2, 2, 2, 2, 2, 2, 2, 2, 2, 2, 2, 2, 2, 2, 2, 2, 2, 2, 2, 2, 2, 2, 2, 2, 2, 2, 2, 2, 2, 2, 2, 2, 2, 2, 2, 2, 2, 2, 2, 2, 2, 2, 2, 2, 2, 2, 2, 2, 2, 2, 2, 2, 2, 2, 2, 2, 2, 2, 2, 2, 2, 2, 2, 2, 2, 2, 2, 2, 2, 2, 2, 2, 2, 2, 3 ),
 ( 0.000000000000000000, 1.000000000000000000 ),
 ( 0.000000000000000000, 0.007812500000000000000, 0.01562500000000000000, 0.02343750000000000000, 0.03125000000000000000, 0.03906250000000000000, 0.04687500000000000000, 0.05468750000000000000, 0.06250000000000000000, 0.07031250000000000000, 0.07812500000000000000, 0.08593750000000000000, 0.09375000000000000000, 0.1015625000000000000, 0.1093750000000000000, 0.1171875000000000000, 0.1250000000000000000, 0.1328125000000000000, 0.1406250000000000000, 0.1484375000000000000, 0.1562500000000000000, 0.1640625000000000000, 0.1718750000000000000, 0.1796875000000000000, 0.1875000000000000000, 0.1953125000000000000, 0.2031250000000000000, 0.2109375000000000000, 0.2187500000000000000, 0.2265625000000000000, 0.2343750000000000000, 0.2421875000000000000, 0.2500000000000000000, 0.2578125000000000000, 0.2656250000000000000, 0.2734375000000000000, 0.2812500000000000000, 0.2890625000000000000, 0.2968750000000000000, 0.3046875000000000000, 0.3125000000000000000, 0.3203125000000000000, 0.3281250000000000000, 0.3359375000000000000, 0.3437500000000000000, 0.3515625000000000000, 0.3593750000000000000, 0.3671875000000000000, 0.3750000000000000000, 0.3828125000000000000, 0.3906250000000000000, 0.3984375000000000000, 0.4062500000000000000, 0.4140625000000000000, 0.4218750000000000000, 0.4296875000000000000, 0.4375000000000000000, 0.4453125000000000000, 0.4531250000000000000, 0.4609375000000000000, 0.4687500000000000000, 0.4765625000000000000, 0.4843750000000000000, 0.4921875000000000000, 0.5000000000000000000, 0.5078125000000000000, 0.5156250000000000000, 0.5234375000000000000, 0.5312500000000000000, 0.5390625000000000000, 0.5468750000000000000, 0.5546875000000000000, 0.5625000000000000000, 0.5703125000000000000, 0.5781250000000000000, 0.5859375000000000000, 0.5937500000000000000, 0.6015625000000000000, 0.6093750000000000000, 0.6171875000000000000, 0.6250000000000000000, 0.6328125000000000000, 0.6406250000000000000, 0.6484375000000000000, 0.6562500000000000000, 0.6640625000000000000, 0.6718750000000000000, 0.6796875000000000000, 0.6875000000000000000, 0.6953125000000000000, 0.7031250000000000000, 0.7109375000000000000, 0.7187500000000000000, 0.7265625000000000000, 0.7343750000000000000, 0.7421875000000000000, 0.7500000000000000000, 0.7578125000000000000, 0.7656250000000000000, 0.7734375000000000000, 0.7812500000000000000, 0.7890625000000000000, 0.7968750000000000000, 0.8046875000000000000, 0.8125000000000000000, 0.8203125000000000000, 0.8281250000000000000, 0.8359375000000000000, 0.8437500000000000000, 0.8515625000000000000, 0.8593750000000000000, 0.8671875000000000000, 0.8750000000000000000, 0.8828125000000000000, 0.8906250000000000000, 0.8984375000000000000, 0.9062500000000000000, 0.9140625000000000000, 0.9218750000000000000, 0.9296875000000000000, 0.9375000000000000000, 0.9453125000000000000, 0.9531250000000000000, 0.9609375000000000000, 0.9687500000000000000, 0.9765625000000000000, 0.9843750000000000000, 0.9921875000000000000, 1.000000000000000000 ),
 .UNSPECIFIED. ) 
 GEOMETRIC_REPRESENTATION_ITEM ( )  RATIONAL_B_SPLINE_SURFACE ( (
 ( 1.000000000000000000, 0.9238795325112869605, 1.000000000000000000, 0.9238795325112869605, 1.000000000000000000, 0.9238795325112869605, 1.000000000000000000, 0.9238795325112869605, 1.000000000000000000, 0.9238795325112869605, 1.000000000000000000, 0.9238795325112869605, 1.000000000000000000, 0.9238795325112869605, 1.000000000000000000, 0.9238795325112869605, 1.000000000000000000, 0.9238795325112869605, 1.000000000000000000, 0.9238795325112869605, 1.000000000000000000, 0.9238795325112869605, 1.000000000000000000, 0.9238795325112869605, 1.000000000000000000, 0.9238795325112869605, 1.000000000000000000, 0.9238795325112869605, 1.000000000000000000, 0.9238795325112869605, 1.000000000000000000, 0.9238795325112869605, 1.000000000000000000, 0.9238795325112869605, 1.000000000000000000, 0.9238795325112869605, 1.000000000000000000, 0.9238795325112869605, 1.000000000000000000, 0.9238795325112869605, 1.000000000000000000, 0.9238795325112869605, 1.000000000000000000, 0.9238795325112869605, 1.000000000000000000, 0.9238795325112869605, 1.000000000000000000, 0.9238795325112869605, 1.000000000000000000, 0.9238795325112869605, 1.000000000000000000, 0.9238795325112869605, 1.000000000000000000, 0.9238795325112869605, 1.000000000000000000, 0.9238795325112869605, 1.000000000000000000, 0.9238795325112869605, 1.000000000000000000, 0.9238795325112869605, 1.000000000000000000, 0.9238795325112869605, 1.000000000000000000, 0.9238795325112869605, 1.000000000000000000, 0.9238795325112869605, 1.000000000000000000, 0.9238795325112869605, 1.000000000000000000, 0.9238795325112869605, 1.000000000000000000, 0.9238795325112869605, 1.000000000000000000, 0.9238795325112869605, 1.000000000000000000, 0.9238795325112869605, 1.000000000000000000, 0.9238795325112869605, 1.000000000000000000, 0.9238795325112869605, 1.000000000000000000, 0.9238795325112869605, 1.000000000000000000, 0.9238795325112869605, 1.000000000000000000, 0.9238795325112869605, 1.000000000000000000, 0.9238795325112869605, 1.000000000000000000, 0.9238795325112869605, 1.000000000000000000, 0.9238795325112869605, 1.000000000000000000, 0.9238795325112869605, 1.000000000000000000, 0.9238795325112869605, 1.000000000000000000, 0.9238795325112869605, 1.000000000000000000, 0.9238795325112869605, 1.000000000000000000, 0.9238795325112869605, 1.000000000000000000, 0.9238795325112869605, 1.000000000000000000, 0.9238795325112869605, 1.000000000000000000, 0.9238795325112869605, 1.000000000000000000, 0.9238795325112869605, 1.000000000000000000, 0.9238795325112869605, 1.000000000000000000, 0.9238795325112869605, 1.000000000000000000, 0.9238795325112869605, 1.000000000000000000, 0.9238795325112869605, 1.000000000000000000, 0.9238795325112869605, 1.000000000000000000, 0.9238795325112869605, 1.000000000000000000, 0.9238795325112869605, 1.000000000000000000, 0.9238795325112869605, 1.000000000000000000, 0.9238795325112869605, 1.000000000000000000, 0.9238795325112869605, 1.000000000000000000, 0.9238795325112869605, 1.000000000000000000, 0.9238795325112869605, 1.000000000000000000, 0.9238795325112869605, 1.000000000000000000, 0.9238795325112869605, 1.000000000000000000, 0.9238795325112869605, 1.000000000000000000, 0.9238795325112869605, 1.000000000000000000, 0.9238795325112869605, 1.000000000000000000, 0.9238795325112869605, 1.000000000000000000, 0.9238795325112869605, 1.000000000000000000, 0.9238795325112869605, 1.000000000000000000, 0.9238795325112869605, 1.000000000000000000, 0.9238795325112869605, 1.000000000000000000, 0.9238795325112869605, 1.000000000000000000, 0.9238795325112869605, 1.000000000000000000, 0.9238795325112869605, 1.000000000000000000, 0.9238795325112869605, 1.000000000000000000, 0.9238795325112869605, 1.000000000000000000, 0.9238795325112869605, 1.000000000000000000, 0.9238795325112869605, 1.000000000000000000, 0.9238795325112869605, 1.000000000000000000, 0.9238795325112869605, 1.000000000000000000, 0.9238795325112869605, 1.000000000000000000, 0.9238795325112869605, 1.000000000000000000, 0.9238795325112869605, 1.000000000000000000, 0.9238795325112869605, 1.000000000000000000, 0.9238795325112869605, 1.000000000000000000, 0.9238795325112869605, 1.000000000000000000, 0.9238795325112869605, 1.000000000000000000, 0.9238795325112869605, 1.000000000000000000, 0.9238795325112869605, 1.000000000000000000, 0.9238795325112869605, 1.000000000000000000, 0.9238795325112869605, 1.000000000000000000, 0.9238795325112869605, 1.000000000000000000, 0.9238795325112869605, 1.000000000000000000, 0.9238795325112869605, 1.000000000000000000, 0.9238795325112869605, 1.000000000000000000, 0.9238795325112869605, 1.000000000000000000, 0.9238795325112869605, 1.000000000000000000, 0.9238795325112869605, 1.000000000000000000, 0.9238795325112869605, 1.000000000000000000, 0.9238795325112869605, 1.000000000000000000, 0.9238795325112869605, 1.000000000000000000, 0.9238795325112869605, 1.000000000000000000, 0.9238795325112869605, 1.000000000000000000, 0.9238795325112869605, 1.000000000000000000, 0.9238795325112869605, 1.000000000000000000, 0.9238795325112869605, 1.000000000000000000, 0.9238795325112869605, 1.000000000000000000, 0.9238795325112869605, 1.000000000000000000, 0.9238795325112869605, 1.000000000000000000, 0.9238795325112869605, 1.000000000000000000, 0.9238795325112869605, 1.000000000000000000, 0.9238795325112869605, 1.000000000000000000, 0.9238795325112869605, 1.000000000000000000, 0.9238795325112869605, 1.000000000000000000, 0.9238795325112869605, 1.000000000000000000, 0.9238795325112869605, 1.000000000000000000, 0.9238795325112869605, 1.000000000000000000, 0.9238795325112869605, 1.000000000000000000, 0.9238795325112869605, 1.000000000000000000, 0.9238795325112869605, 1.000000000000000000, 0.9238795325112869605, 1.000000000000000000, 0.9238795325112869605, 1.000000000000000000),
 ( 1.000000000000000000, 0.9238795325112869605, 1.000000000000000000, 0.9238795325112869605, 1.000000000000000000, 0.9238795325112869605, 1.000000000000000000, 0.9238795325112869605, 1.000000000000000000, 0.9238795325112869605, 1.000000000000000000, 0.9238795325112869605, 1.000000000000000000, 0.9238795325112869605, 1.000000000000000000, 0.9238795325112869605, 1.000000000000000000, 0.9238795325112869605, 1.000000000000000000, 0.9238795325112869605, 1.000000000000000000, 0.9238795325112869605, 1.000000000000000000, 0.9238795325112869605, 1.000000000000000000, 0.9238795325112869605, 1.000000000000000000, 0.9238795325112869605, 1.000000000000000000, 0.9238795325112869605, 1.000000000000000000, 0.9238795325112869605, 1.000000000000000000, 0.9238795325112869605, 1.000000000000000000, 0.9238795325112869605, 1.000000000000000000, 0.9238795325112869605, 1.000000000000000000, 0.9238795325112869605, 1.000000000000000000, 0.9238795325112869605, 1.000000000000000000, 0.9238795325112869605, 1.000000000000000000, 0.9238795325112869605, 1.000000000000000000, 0.9238795325112869605, 1.000000000000000000, 0.9238795325112869605, 1.000000000000000000, 0.9238795325112869605, 1.000000000000000000, 0.9238795325112869605, 1.000000000000000000, 0.9238795325112869605, 1.000000000000000000, 0.9238795325112869605, 1.000000000000000000, 0.9238795325112869605, 1.000000000000000000, 0.9238795325112869605, 1.000000000000000000, 0.9238795325112869605, 1.000000000000000000, 0.9238795325112869605, 1.000000000000000000, 0.9238795325112869605, 1.000000000000000000, 0.9238795325112869605, 1.000000000000000000, 0.9238795325112869605, 1.000000000000000000, 0.9238795325112869605, 1.000000000000000000, 0.9238795325112869605, 1.000000000000000000, 0.9238795325112869605, 1.000000000000000000, 0.9238795325112869605, 1.000000000000000000, 0.9238795325112869605, 1.000000000000000000, 0.9238795325112869605, 1.000000000000000000, 0.9238795325112869605, 1.000000000000000000, 0.9238795325112869605, 1.000000000000000000, 0.9238795325112869605, 1.000000000000000000, 0.9238795325112869605, 1.000000000000000000, 0.9238795325112869605, 1.000000000000000000, 0.9238795325112869605, 1.000000000000000000, 0.9238795325112869605, 1.000000000000000000, 0.9238795325112869605, 1.000000000000000000, 0.9238795325112869605, 1.000000000000000000, 0.9238795325112869605, 1.000000000000000000, 0.9238795325112869605, 1.000000000000000000, 0.9238795325112869605, 1.000000000000000000, 0.9238795325112869605, 1.000000000000000000, 0.9238795325112869605, 1.000000000000000000, 0.9238795325112869605, 1.000000000000000000, 0.9238795325112869605, 1.000000000000000000, 0.9238795325112869605, 1.000000000000000000, 0.9238795325112869605, 1.000000000000000000, 0.9238795325112869605, 1.000000000000000000, 0.9238795325112869605, 1.000000000000000000, 0.9238795325112869605, 1.000000000000000000, 0.9238795325112869605, 1.000000000000000000, 0.9238795325112869605, 1.000000000000000000, 0.9238795325112869605, 1.000000000000000000, 0.9238795325112869605, 1.000000000000000000, 0.9238795325112869605, 1.000000000000000000, 0.9238795325112869605, 1.000000000000000000, 0.9238795325112869605, 1.000000000000000000, 0.9238795325112869605, 1.000000000000000000, 0.9238795325112869605, 1.000000000000000000, 0.9238795325112869605, 1.000000000000000000, 0.9238795325112869605, 1.000000000000000000, 0.9238795325112869605, 1.000000000000000000, 0.9238795325112869605, 1.000000000000000000, 0.9238795325112869605, 1.000000000000000000, 0.9238795325112869605, 1.000000000000000000, 0.9238795325112869605, 1.000000000000000000, 0.9238795325112869605, 1.000000000000000000, 0.9238795325112869605, 1.000000000000000000, 0.9238795325112869605, 1.000000000000000000, 0.9238795325112869605, 1.000000000000000000, 0.9238795325112869605, 1.000000000000000000, 0.9238795325112869605, 1.000000000000000000, 0.9238795325112869605, 1.000000000000000000, 0.9238795325112869605, 1.000000000000000000, 0.9238795325112869605, 1.000000000000000000, 0.9238795325112869605, 1.000000000000000000, 0.9238795325112869605, 1.000000000000000000, 0.9238795325112869605, 1.000000000000000000, 0.9238795325112869605, 1.000000000000000000, 0.9238795325112869605, 1.000000000000000000, 0.9238795325112869605, 1.000000000000000000, 0.9238795325112869605, 1.000000000000000000, 0.9238795325112869605, 1.000000000000000000, 0.9238795325112869605, 1.000000000000000000, 0.9238795325112869605, 1.000000000000000000, 0.9238795325112869605, 1.000000000000000000, 0.9238795325112869605, 1.000000000000000000, 0.9238795325112869605, 1.000000000000000000, 0.9238795325112869605, 1.000000000000000000, 0.9238795325112869605, 1.000000000000000000, 0.9238795325112869605, 1.000000000000000000, 0.9238795325112869605, 1.000000000000000000, 0.9238795325112869605, 1.000000000000000000, 0.9238795325112869605, 1.000000000000000000, 0.9238795325112869605, 1.000000000000000000, 0.9238795325112869605, 1.000000000000000000, 0.9238795325112869605, 1.000000000000000000, 0.9238795325112869605, 1.000000000000000000, 0.9238795325112869605, 1.000000000000000000, 0.9238795325112869605, 1.000000000000000000, 0.9238795325112869605, 1.000000000000000000, 0.9238795325112869605, 1.000000000000000000, 0.9238795325112869605, 1.000000000000000000, 0.9238795325112869605, 1.000000000000000000, 0.9238795325112869605, 1.000000000000000000, 0.9238795325112869605, 1.000000000000000000, 0.9238795325112869605, 1.000000000000000000, 0.9238795325112869605, 1.000000000000000000, 0.9238795325112869605, 1.000000000000000000, 0.9238795325112869605, 1.000000000000000000, 0.9238795325112869605, 1.000000000000000000, 0.9238795325112869605, 1.000000000000000000, 0.9238795325112869605, 1.000000000000000000, 0.9238795325112869605, 1.000000000000000000, 0.9238795325112869605, 1.000000000000000000) ) ) 
 REPRESENTATION_ITEM ( '' )  SURFACE ( )  );
#17644=CARTESIAN_POINT ( 'NONE',  ( 119.4332814775786318, -8.899110576539710493, -16.42337572283490132 ) ) ;
#17647=CARTESIAN_POINT ( 'NONE',  ( 116.4834948109119779, -7.894159318335828068, -9.358103419637847864 ) ) ;
#17649=CARTESIAN_POINT ( 'NONE',  ( 125.1059481442452750, -1.833838273342660141, -17.42832698103878286 ) ) ;
#17654=CARTESIAN_POINT ( 'NONE',  ( 114.3278814775786429, -10.30919188438810075, -12.61870101168855918 ) ) ;
#17656=CARTESIAN_POINT ( 'NONE',  ( 116.1431348109119881, -10.30919188438810075, -12.61870101168855918 ) ) ;
#17659=CARTESIAN_POINT ( 'NONE',  ( 112.3991748109119868, -8.166667518702817929, -8.995218007635859436 ) ) ;
#17660=CARTESIAN_POINT ( 'NONE',  ( 112.7962614775786676, -3.383040157471821630, -19.15922257007629170 ) ) ;
#17661=CARTESIAN_POINT ( 'NONE',  ( 122.7801548109119665, -6.222761293078241884, -8.102969835052219238 ) ) ;
#17667=CARTESIAN_POINT ( 'NONE',  ( 117.0507614775786465, 0.1319031606808879209, -14.10382304977623669 ) ) ;
#17671=CARTESIAN_POINT ( 'NONE',  ( 121.9484597424434043, -0.9924539043446216624, -17.29976612834909133 ) ) ;
#17672=CARTESIAN_POINT ( 'NONE',  ( 111.3780948109119890, -5.574606645277164318, -18.38911715685844683 ) ) ;
#17674=CARTESIAN_POINT ( 'NONE',  ( 124.8790414775786246, -0.4660016031367893996, -10.09054647747474043 ) ) ;
#17675=CARTESIAN_POINT ( 'NONE',  ( 115.1787814775786387, -9.988377603198976828, -10.36322818467138340 ) ) ;
#17677=CARTESIAN_POINT ( 'NONE',  ( 116.5402214775786405, -9.565557343593413364, -10.61323700422348004 ) ) ;
#17678=CARTESIAN_POINT ( 'NONE',  ( 112.2857214775786474, -4.089484607189486809, -7.948022111789456723 ) ) ;
#17679=CARTESIAN_POINT ( 'NONE',  ( 116.7104014775786425, -0.4660016031367893996, -10.09054647747474043 ) ) ;
#17681=CARTESIAN_POINT ( 'NONE',  ( 115.0653281442453277, -3.505236298600246325, -18.68346056562440793 ) ) ;
#17683=CARTESIAN_POINT ( 'NONE',  ( 121.4187148109119789, -3.505236298600246325, -18.68346056562440793 ) ) ;
#17685=CARTESIAN_POINT ( 'NONE',  ( 115.4056881442453459, -7.893985811506177619, -18.51759400769804742 ) ) ;
#17692=CARTESIAN_POINT ( 'NONE',  ( 113.6471614775786492, -5.638512984488999180, -18.83840828888717311 ) ) ;
#17693=CARTESIAN_POINT ( 'NONE',  ( 136.3514896076009109, -10.64081954711834044, -14.04243400364072869 ) ) ;
#17694=CARTESIAN_POINT ( 'NONE',  ( 113.8740681442453138, -9.859900752359374465, -12.68260735090039404 ) ) ;
#17698=CARTESIAN_POINT ( 'NONE',  ( 113.7038881442453402, -6.222761293078241884, -8.102969835052219238 ) ) ;
#17701=CARTESIAN_POINT ( 'NONE',  ( 116.0296814775786345, -8.166667518702817929, -8.995218007635861213 ) ) ;
#17702=CARTESIAN_POINT ( 'NONE',  ( 125.2194014775786286, 0.1319031606808879209, -14.10382304977623669 ) ) ;
#17703=CARTESIAN_POINT ( 'NONE',  ( 119.8303681442453126, 0.4262465694468514643, -12.03445270309931736 ) ) ;
#17705=CARTESIAN_POINT ( 'NONE',  ( 136.5847729262498262, -9.288433219509910188, -9.783805946180876845 ) ) ;
#17706=CARTESIAN_POINT ( 'NONE',  ( 122.2128881442453263, -1.834011780172310813, -8.268836392978581529 ) ) ;
#17708=CARTESIAN_POINT ( 'NONE',  ( 115.3489614775786407, -0.8288870151387760510, -10.36305467784173118 ) ) ;
#17710=CARTESIAN_POINT ( 'NONE',  ( 126.2404814775786264, -9.261995988541697145, -16.69588392320189030 ) ) ;
#17713=CARTESIAN_POINT ( 'NONE',  ( 120.9649014775786355, -6.222761293078241884, -8.102969835052219238 ) ) ;
#17715=CARTESIAN_POINT ( 'NONE',  ( 121.4187148109119789, -3.505236298600246325, -18.68346056562440793 ) ) ;
#17721=CARTESIAN_POINT ( 'NONE',  ( 118.6958348109119754, -6.344957434206665248, -7.627207830600338134 ) ) ;
#17722=CARTESIAN_POINT ( 'NONE',  ( 115.3489614775786407, -9.261995988541697145, -16.69588392320189030 ) ) ;
#17729=CARTESIAN_POINT ( 'NONE',  ( 123.8012348109119642, 0.2603800115204892296, -16.42320221600525088 ) ) ;
#17730=CARTESIAN_POINT ( 'NONE',  ( 112.9097148109120070, 0.2603800115204892296, -16.42320221600525088 ) ) ;
#17731=CARTESIAN_POINT ( 'NONE',  ( 122.7801548109119665, -6.222761293078241884, -8.102969835052219238 ) ) ;
#17732=CARTESIAN_POINT ( 'NONE',  ( 125.7866681442452688, -0.4660016031367893996, -10.09054647747474043 ) ) ;
#17733=CARTESIAN_POINT ( 'NONE',  ( 121.0216281442452981, -1.561330072975668948, -17.79121239304076951 ) ) ;
#17735=CARTESIAN_POINT ( 'NONE',  ( 116.4834948109119779, -7.894159318335828068, -9.358103419637847864 ) ) ;
#17736=CARTESIAN_POINT ( 'NONE',  ( 126.2184548109119788, -2.495269033102075262, -17.79652296963211455 ) ) ;
#17738=B_SPLINE_CURVE_WITH_KNOTS ( 'NONE', 3,
 ( #1829, #37573, #36491, #22370, #16844, #20030, #27326, #43348, #10002, #43573 ),
 .UNSPECIFIED., .F., .F.,
 ( 4, 3, 3, 4 ),
 ( 0.000000000000000000, 0.0001671877560958140072, 0.0003343755126086610133, 0.0006438490228507209303 ),
 .UNSPECIFIED. ) ;
#17739=CARTESIAN_POINT ( 'NONE',  ( 120.1140014775786398, -1.561330072975668504, -17.79121239304076951 ) ) ;
#17742=CARTESIAN_POINT ( 'NONE',  ( 115.1787814775786387, -9.988377603198976828, -10.36322818467138340 ) ) ;
#17745=CARTESIAN_POINT ( 'NONE',  ( 125.3895814775786448, -7.893985811506177619, -18.51759400769804742 ) ) ;
#17747=CARTESIAN_POINT ( 'NONE',  ( 116.4267681442453153, -6.222761293078241884, -8.102969835052219238 ) ) ;
#17749=CARTESIAN_POINT ( 'NONE',  ( 121.3052614775786111, -7.643976991954077427, -18.09477374809248928 ) ) ;
#17751=CARTESIAN_POINT ( 'NONE',  ( 121.2485348109119769, -8.899110576539710493, -16.42337572283490132 ) ) ;
#17754=CARTESIAN_POINT ( 'NONE',  ( 118.4122014775786340, -9.859900752359374465, -12.68260735090039404 ) ) ;
#17756=CARTESIAN_POINT ( 'NONE',  ( 115.5758681442453053, -1.561330072975668060, -17.79121239304076951 ) ) ;
#17758=CARTESIAN_POINT ( 'NONE',  ( 121.4187148109119789, -3.505236298600246325, -18.68346056562440793 ) ) ;
#17760=CARTESIAN_POINT ( 'NONE',  ( 117.6747548109119919, -1.834011780172310813, -8.268836392978581529 ) ) ;
#17766=CARTESIAN_POINT ( 'NONE',  ( 123.0637881442452937, -0.4660016031367893996, -10.09054647747474043 ) ) ;
#17768=CARTESIAN_POINT ( 'NONE',  ( 126.5010429760479695, -8.432961773280235107, -9.692480226144548183 ) ) ;
#17769=CARTESIAN_POINT ( 'NONE',  ( 123.0637881442452937, -8.899110576539710493, -16.42337572283490132 ) ) ;
#17770=EDGE_CURVE ( 'NONE', #22820, #23145, #27999, .T. ) ;
#17773=CARTESIAN_POINT ( 'NONE',  ( 125.8433948109119456, -1.834011780172310813, -8.268836392978581529 ) ) ;
#17779=CARTESIAN_POINT ( 'NONE',  ( 116.0864081442453113, -9.988377603198976828, -10.36322818467138340 ) ) ;
#17780=CARTESIAN_POINT ( 'NONE',  ( 125.9001214775786224, -5.574606645277164318, -18.38911715685844683 ) ) ;
#17781=CARTESIAN_POINT ( 'NONE',  ( 124.9357681442453014, -1.834011780172310813, -8.268836392978581529 ) ) ;
#17782=CARTESIAN_POINT ( 'NONE',  ( 115.8027748109119841, -8.899110576539710493, -16.42337572283490132 ) ) ;
#17783=CARTESIAN_POINT ( 'NONE',  ( 126.8396850857575515, -3.206737104985623699, -8.347647502750785264 ) ) ;
#17784=CARTESIAN_POINT ( 'NONE',  ( 117.9016614775786280, -9.988377603198976828, -10.36322818467138340 ) ) ;
#17785=CARTESIAN_POINT ( 'NONE',  ( 111.6722681442453222, -0.8658195297461032114, -10.39078908864415496 ) ) ;
#17788=CARTESIAN_POINT ( 'NONE',  ( 122.8368814775786291, -7.894159318335828068, -9.358103419637847864 ) ) ;
#17791=CARTESIAN_POINT ( 'NONE',  ( 121.4754414775786131, -8.166667518702819706, -8.995218007635861213 ) ) ;
#17792=CARTESIAN_POINT ( 'NONE',  ( 124.1415948109119540, -3.505236298600246325, -18.68346056562440793 ) ) ;
#17795=CARTESIAN_POINT ( 'NONE',  ( 121.1198558961590521, -2.263366209404226392, -18.10533625161308180 ) ) ;
#17798=CARTESIAN_POINT ( 'NONE',  ( 121.8725281442453223, -3.383040157471821630, -19.15922257007629170 ) ) ;
#17800=CARTESIAN_POINT ( 'NONE',  ( 119.0361948109119652, -2.084020599724406786, -8.691656652584148546 ) ) ;
#17801=CIRCLE ( 'NONE', #35252, 5.999999999999997335 ) ;
#17803=CARTESIAN_POINT ( 'NONE',  ( 112.9097148109120070, 0.2603800115204892296, -16.42320221600525088 ) ) ;
#17805=CARTESIAN_POINT ( 'NONE',  ( 112.4201593777725208, -1.267766418764741276, -16.93314635290707315 ) ) ;
#17806=LINE ( 'NONE', #10968, #38917 ) ;
#17807=CARTESIAN_POINT ( 'NONE',  ( 125.5597614775786326, -1.561330072975669392, -17.79121239304076951 ) ) ;
#17810=CARTESIAN_POINT ( 'NONE',  ( 124.3117748109119844, -10.30919188438810075, -12.61870101168855918 ) ) ;
#17811=CARTESIAN_POINT ( 'NONE',  ( 121.3619881442452879, -4.089484607189486809, -7.948022111789456723 ) ) ;
#17812=CARTESIAN_POINT ( 'NONE',  ( 123.2906948109119867, -1.833838273342659697, -17.42832698103878286 ) ) ;
#17813=CARTESIAN_POINT ( 'NONE',  ( 120.9649014775786355, -6.222761293078241884, -8.102969835052219238 ) ) ;
#17815=CARTESIAN_POINT ( 'NONE',  ( 115.1787814775786387, -9.988377603198976828, -10.36322818467138340 ) ) ;
#17822=CARTESIAN_POINT ( 'NONE',  ( 112.5126281442453120, -10.30919188438810075, -12.61870101168855918 ) ) ;
#17824=CARTESIAN_POINT ( 'NONE',  ( 114.8384214775786489, -10.15424416112533912, -14.75197769757731336 ) ) ;
#17826=CARTESIAN_POINT ( 'NONE',  ( 121.9859814775786333, -9.565557343593409811, -10.61323700422347649 ) ) ;
#17827=CARTESIAN_POINT ( 'NONE',  ( 125.0492214775786266, -6.344957434206665248, -7.627207830600338134 ) ) ;
#17828=CARTESIAN_POINT ( 'NONE',  ( 124.3685014775786328, -10.63000616557722466, -14.87417383870573495 ) ) ;
#17830=CARTESIAN_POINT ( 'NONE',  ( 117.4478481442453131, 0.2603800115204892296, -16.42320221600525088 ) ) ;
#17837=CARTESIAN_POINT ( 'NONE',  ( 114.8951481442453115, -8.899110576539710493, -16.42337572283490132 ) ) ;
#17838=CARTESIAN_POINT ( 'NONE',  ( 126.4106614775786284, -6.222761293078241884, -8.102969835052219238 ) ) ;
#17841=CARTESIAN_POINT ( 'NONE',  ( 124.0848681442452772, -5.574606645277164318, -18.38911715685844683 ) ) ;
#17843=CARTESIAN_POINT ( 'NONE',  ( 121.0783548109119749, -9.565557343593413364, -10.61323700422348004 ) ) ;
#17844=CARTESIAN_POINT ( 'NONE',  ( 112.0588148109119828, -9.859900752359374465, -12.68260735090039404 ) ) ;
#17846=CARTESIAN_POINT ( 'NONE',  ( 125.1059481442452750, -1.833838273342660141, -17.42832698103878286 ) ) ;
#17848=CARTESIAN_POINT ( 'NONE',  ( 112.5126281442453120, 0.1319031606808879209, -14.10382304977623669 ) ) ;
#17850=CARTESIAN_POINT ( 'NONE',  ( 126.4599182912924675, -9.283010264413503521, -15.98057921980140783 ) ) ;
#17852=CARTESIAN_POINT ( 'NONE',  ( 112.7962614775786676, -3.383040157471821630, -19.15922257007629170 ) ) ;
#17856=CARTESIAN_POINT ( 'NONE',  ( 117.4478481442453131, -9.565557343593413364, -10.61323700422348004 ) ) ;
#17857=CARTESIAN_POINT ( 'NONE',  ( 115.0086014775786509, -5.574606645277164318, -18.38911715685844683 ) ) ;
#17858=ADVANCED_FACE ( 'NONE', ( #11786 ), #40153, .T. ) ;
#17860=CARTESIAN_POINT ( 'NONE',  ( 116.0506660444391969, -1.267766418764730840, -16.93314635290706605 ) ) ;
#17862=CARTESIAN_POINT ( 'NONE',  ( 121.3786053070358832, -1.196538596002817867, -17.02799684832028504 ) ) ;
#17867=CARTESIAN_POINT ( 'NONE',  ( 111.7184548109119788, -9.261995988541697145, -16.69588392320189030 ) ) ;
#17868=CARTESIAN_POINT ( 'NONE',  ( 117.5045748109119756, -9.859900752359374465, -12.68260735090039404 ) ) ;
#17872=CARTESIAN_POINT ( 'NONE',  ( 117.1074881442453233, 0.4262465694468514643, -12.03445270309931736 ) ) ;
#17873=DIRECTION ( 'NONE',  ( 0.000000000000000000, 0.6004852223388327248, -0.7996358532186277346 ) ) ;
#17874=CARTESIAN_POINT ( 'NONE',  ( 114.1934435773848833, -2.467220198592768199, -17.83387418641523325 ) ) ;
#17876=CARTESIAN_POINT ( 'NONE',  ( 115.8595014775786609, -1.834011780172310813, -8.268836392978581529 ) ) ;
#17878=CARTESIAN_POINT ( 'NONE',  ( 118.5823814775786360, -1.834011780172310813, -8.268836392978581529 ) ) ;
#17881=CARTESIAN_POINT ( 'NONE',  ( 126.0703014775786102, -0.1624402480850797581, -16.17319339645315424 ) ) ;
#17882=CARTESIAN_POINT ( 'NONE',  ( 114.2144281442453178, -8.166667518702817929, -8.995218007635859436 ) ) ;
#17883=CARTESIAN_POINT ( 'NONE',  ( 126.8137406967851319, -10.15933636723070599, -13.56223398357370158 ) ) ;
#17889=CARTESIAN_POINT ( 'NONE',  ( 115.0086014775786509, -5.574606645277164318, -18.38911715685844683 ) ) ;
#17894=CARTESIAN_POINT ( 'NONE',  ( 127.7617783745857452, -5.489033741201595262, -7.655088239364113534 ) ) ;
#17895=CARTESIAN_POINT ( 'NONE',  ( 125.9001214775786224, -4.089484607189486809, -7.948022111789456723 ) ) ;
#17896=CARTESIAN_POINT ( 'NONE',  ( 120.3409081442453044, -8.899110576539722928, -16.42337572283488356 ) ) ;
#17897=CARTESIAN_POINT ( 'NONE',  ( 125.4463081442452932, -5.638512984488999180, -18.83840828888717311 ) ) ;
#17898=CARTESIAN_POINT ( 'NONE',  ( 115.9729548109119861, -6.344957434206662583, -7.627207830600332805 ) ) ;
#17901=CARTESIAN_POINT ( 'NONE',  ( 115.9162281442453093, -5.574606645277164318, -18.38911715685844683 ) ) ;
#17903=CARTESIAN_POINT ( 'NONE',  ( 116.1998614775786507, -10.63000616557722466, -14.87417383870573495 ) ) ;
#17904=CARTESIAN_POINT ( 'NONE',  ( 116.2565881442453133, -0.8288870151387760510, -10.36305467784173118 ) ) ;
#17906=CARTESIAN_POINT ( 'NONE',  ( 119.6034614775786196, -3.505236298600246325, -18.68346056562440793 ) ) ;
#17907=CARTESIAN_POINT ( 'NONE',  ( 118.1852948109119836, -5.638512984488999180, -18.83840828888717311 ) ) ;
#17909=CARTESIAN_POINT ( 'NONE',  ( 135.5366836739015071, 0.6402420525674652474, -15.78128361289120640 ) ) ;
#17914=CARTESIAN_POINT ( 'NONE',  ( 114.8951481442453115, -0.4660016031367893996, -10.09054647747474043 ) ) ;
#17917=CARTESIAN_POINT ( 'NONE',  ( 115.1220548109119761, -1.833838273342658809, -17.42832698103878286 ) ) ;
#17919=FACE_OUTER_BOUND ( 'NONE', #29483, .T. ) ;
#17921=CARTESIAN_POINT ( 'NONE',  ( 112.2857214775786474, -5.574606645277164318, -18.38911715685844683 ) ) ;
#17923=DIRECTION ( 'NONE',  ( 0.000000000000000000, 0.6004852223388321697, -0.7996358532186279566 ) ) ;
#17925=CARTESIAN_POINT ( 'NONE',  ( 119.2063748109119814, -1.561330072975668504, -17.79121239304076951 ) ) ;
#17926=CARTESIAN_POINT ( 'NONE',  ( 124.1415948109119540, -3.505236298600246325, -18.68346056562440793 ) ) ;
#17927=CARTESIAN_POINT ( 'NONE',  ( 120.1707281442453166, -9.565557343593413364, -10.61323700422348004 ) ) ;
#17928=CARTESIAN_POINT ( 'NONE',  ( 111.8886348109120092, -6.222761293078241884, -8.102969835052219238 ) ) ;
#17930=CARTESIAN_POINT ( 'NONE',  ( 136.1332990479124589, -7.072588780063932212, -7.940136130744186893 ) ) ;
#17931=CARTESIAN_POINT ( 'NONE',  ( 124.6521348109119884, -1.561330072975668948, -17.79121239304076951 ) ) ;
#17933=CARTESIAN_POINT ( 'NONE',  ( 119.8303681442453126, 0.4262465694468514643, -12.03445270309931736 ) ) ;
#17935=CARTESIAN_POINT ( 'NONE',  ( 126.1270281442452870, -10.30919188438810075, -12.61870101168855918 ) ) ;
#17938=CARTESIAN_POINT ( 'NONE',  ( 118.8660148109119774, 0.1319031606808879209, -14.10382304977623669 ) ) ;
#17939=CARTESIAN_POINT ( 'NONE',  ( 119.1496481442453046, -6.222761293078241884, -8.102969835052219238 ) ) ;
#17945=CARTESIAN_POINT ( 'NONE',  ( 118.8092881442453290, -9.988377603198976828, -10.36322818467138340 ) ) ;
#17946=CARTESIAN_POINT ( 'NONE',  ( 113.0798948109119948, -0.4660016031367893996, -10.09054647747474043 ) ) ;
#17948=CARTESIAN_POINT ( 'NONE',  ( 112.6260814775786514, -9.261995988541697145, -16.69588392320189030 ) ) ;
#17951=CARTESIAN_POINT ( 'NONE',  ( 124.1415948109119540, -6.344957434206665248, -7.627207830600338134 ) ) ;
#17952=CARTESIAN_POINT ( 'NONE',  ( 115.2355081442453155, -10.30919188438810075, -12.61870101168855918 ) ) ;
#17953=CARTESIAN_POINT ( 'NONE',  ( 120.9081748109119872, -4.153390946401325223, -8.397313243818185668 ) ) ;
#17955=CARTESIAN_POINT ( 'NONE',  ( 124.9924948109119924, -4.089484607189486809, -7.948022111789456723 ) ) ;
#17956=CARTESIAN_POINT ( 'NONE',  ( 123.1772414775786189, -4.089484607189486809, -7.948022111789456723 ) ) ;
#17958=EDGE_CURVE ( 'NONE', #13784, #34606, #26473, .T. ) ;
#17959=CARTESIAN_POINT ( 'NONE',  ( 116.3133148109120043, -2.084020599724406786, -8.691656652584148546 ) ) ;
#17962=CARTESIAN_POINT ( 'NONE',  ( 122.1561614775786353, -0.4660016031367893996, -10.09054647747474043 ) ) ;
#17965=CARTESIAN_POINT ( 'NONE',  ( 120.5110881442453206, -6.344957434206665248, -7.627207830600338134 ) ) ;
#17968=CARTESIAN_POINT ( 'NONE',  ( 124.4252281442452812, -9.261995988541697145, -16.69588392320189030 ) ) ;
#17970=CARTESIAN_POINT ( 'NONE',  ( 116.3700414775786527, -4.153390946401321671, -8.397313243818183892 ) ) ;
#17972=CARTESIAN_POINT ( 'NONE',  ( 121.0216281442452981, -7.894159318335828068, -9.358103419637847864 ) ) ;
#17974=CARTESIAN_POINT ( 'NONE',  ( 121.6456214775786293, 0.4262465694468514643, -12.03445270309931736 ) ) ;
#17976=VECTOR ( 'NONE', #410, 1000.000000000000000 ) ;
#17977=CARTESIAN_POINT ( 'NONE',  ( 119.5467348109119712, -5.574606645277164318, -18.38911715685844683 ) ) ;
#17978=CARTESIAN_POINT ( 'NONE',  ( 112.6828081442453282, -7.893985811506177619, -18.51759400769804742 ) ) ;
#17979=CARTESIAN_POINT ( 'NONE',  ( 118.2987481442453088, -1.561330072975668504, -17.79121239304076951 ) ) ;
#17980=CARTESIAN_POINT ( 'NONE',  ( 112.1155414775786454, 0.9020085738987339008, -11.91225656197089222 ) ) ;
#17982=CARTESIAN_POINT ( 'NONE',  ( 121.1918081442452859, -10.15424416112533912, -14.75197769757731336 ) ) ;
#17984=CARTESIAN_POINT ( 'NONE',  ( 115.0653281442453277, -6.344957434206662583, -7.627207830600332805 ) ) ;
#17987=CARTESIAN_POINT ( 'NONE',  ( 115.3489614775786407, -0.8288870151387673912, -10.36305467784174184 ) ) ;
#17990=CARTESIAN_POINT ( 'NONE',  ( 120.9081748109119872, -5.638512984488999180, -18.83840828888717311 ) ) ;
#17992=CARTESIAN_POINT ( 'NONE',  ( 126.4162218615764743, -8.334346880300483207, -9.657250028486881632 ) ) ;
#17993=CARTESIAN_POINT ( 'NONE',  ( 122.3830681442452857, -1.833838273342659697, -17.42832698103878286 ) ) ;
#17999=VERTEX_POINT ( 'NONE', #37169 ) ;
#18000=CARTESIAN_POINT ( 'NONE',  ( 114.1577014775786552, -6.344957434206662583, -7.627207830600332805 ) ) ;
#18001=CARTESIAN_POINT ( 'NONE',  ( 126.2404814775786264, -0.8288870151387760510, -10.36305467784173118 ) ) ;
#18002=CARTESIAN_POINT ( 'NONE',  ( 122.4397948109119767, -9.988377603198976828, -10.36322818467138340 ) ) ;
#18003=CARTESIAN_POINT ( 'NONE',  ( 121.9859814775786333, -9.565557343593413364, -10.61323700422348004 ) ) ;
#18004=CARTESIAN_POINT ( 'NONE',  ( 126.2184548109105435, -4.159894987975746972, -8.443039665293909479 ) ) ;
#18005=CARTESIAN_POINT ( 'NONE',  ( 123.9714148109119805, -0.4660016031367893996, -10.09054647747474043 ) ) ;
#18009=CARTESIAN_POINT ( 'NONE',  ( 112.2857214775786474, -4.089484607189486809, -7.948022111789456723 ) ) ;
#18010=ORIENTED_EDGE ( 'NONE', *, *, #10152, .F. ) ;
#18013=CARTESIAN_POINT ( 'NONE',  ( 119.3765548109119834, 0.9020085738987339008, -11.91225656197089222 ) ) ;
#18014=CARTESIAN_POINT ( 'NONE',  ( 135.5886503745704488, -10.44469069420684804, -15.59668197382750598 ) ) ;
#18016=CARTESIAN_POINT ( 'NONE',  ( 121.0024232127138504, -2.191907684172563986, -18.20049396185734025 ) ) ;
#18017=CARTESIAN_POINT ( 'NONE',  ( 123.1772414775786189, -4.089484607189486809, -7.948022111789456723 ) ) ;
#18019=CARTESIAN_POINT ( 'NONE',  ( 121.7023481442452919, -0.8288870151387760510, -10.36305467784173118 ) ) ;
#18021=CARTESIAN_POINT ( 'NONE',  ( 114.2711548109119803, -9.988377603198976828, -10.36322818467138340 ) ) ;
#18025=DIRECTION ( 'NONE',  ( -1.000000000000000000, 0.000000000000000000, 0.000000000000000000 ) ) ;
#18027=CARTESIAN_POINT ( 'NONE',  ( 111.6050014775786536, 0.1319031606808879209, -14.10382304977623669 ) ) ;
#18030=CARTESIAN_POINT ( 'NONE',  ( 122.9503348109119827, 0.5811942927096110934, -14.16772938898807510 ) ) ;
#18031=CARTESIAN_POINT ( 'NONE',  ( 122.3263414775786373, -6.344957434206665248, -7.627207830600338134 ) ) ;
#18032=CARTESIAN_POINT ( 'NONE',  ( 124.1983214775786166, -1.833838273342659697, -17.42832698103878286 ) ) ;
#18033=CARTESIAN_POINT ( 'NONE',  ( 119.3765548109119834, -10.15424416112533912, -14.75197769757731336 ) ) ;
#18034=( BOUNDED_SURFACE ( )  B_SPLINE_SURFACE ( 1, 2, ( 
 ( #29736, #18582, #39775, #15837, #36566, #18805, #1910, #36338, #42976, #19026, #43647, #1464, #32475, #2132, #43883, #32911, #39332, #22000, #30420, #37932, #26780, #40462, #6250, #45013, #33589, #24040, #6480, #41149, #2364, #23132, #9224, #16295, #37010, #9674, #5780, #34054, #31087, #27458, #30195, #44114, #12880, #27234, #41380, #44341, #13100, #37239, #19701, #16977, #19935, #16523, #44564, #30645, #26550, #20394, #34494, #2821, #40689, #30868, #10135, #9910, #13327, #9442, #3051, #44790, #23354, #6011, #33821, #6708, #34278, #23823, #2592, #27002, #40920, #23592, #37476, #20171, #16750, #37709, #13548, #20617, #3270, #17195, #77, #14435, #28575, #31529, #17633, #24474, #38151, #4163, #7138, #3713, #31754, #17856, #32199, #38816, #21727, #35156, #6925, #18079, #42483, #28343, #524, #27904, #35386, #31974, #13772, #3936, #41819, #10576, #25153, #737, #14660, #299, #11245, #39049, #42256, #34711, #21499, #35615, #7820, #28127, #11020, #27683, #13990, #42036, #10795, #24921, #24692, #4389, #38364, #18304, #7585, #41597, #38581, #14212, #7359, #10354, #24261, #3496, #21274, #20830, #17413, #31304, #21049, #34926, #29686, #43373, #22617, #39726, #18975, #8492, #22845, #5503, #42929, #8266, #8041, #25817, #36291, #29460, #33084, #22171, #36065, #36517, #32645, #11475, #1413, #4835, #36737, #25379, #5290, #42706, #15331, #19205, #32863, #18532, #22396, #29241, #21947, #18756, #12143, #15110, #39277, #1634, #5059, #43149, #1197, #15554, #11918, #12370, #29019, #14888, #26045, #32424, #39950, #8712, #35838, #1855, #15784, #11691, #4611, #43597, #26270, #40178, #25600, #8944, #19424, #971, #39505, #28799, #13045, #6652, #40409, #30817, #13272, #2771, #9169, #29917, #2085, #23074, #16009, #16465, #43832, #40867, #37877, #34224, #36957, #5728, #19647, #34001, #2997, #5957, #37184, #44059, #12599, #23765, #26724, #23300, #6195, #37425, #33310, #27178, #41327, #9621, #26501, #37656, #16922, #16695, #20114, #2312, #9857, #6430, #33533, #23541, #16242, #30144, #44740 ),
 ( #12825, #40633, #9389, #13499, #27405, #19883, #2539, #44291, #26944, #33770, #10085, #23988, #30369, #30589, #44508, #41098, #20340, #17581, #13721, #28072, #42428, #17803, #41980, #27628, #24207, #31919, #6873, #3447, #38989, #14155, #17365, #31474, #21222, #10745, #247, #4099, #20782, #11192, #38758, #31696, #20562, #7089, #31253, #24422, #684, #18021, #13938, #31033, #14603, #35099, #10305, #35330, #10521, #28522, #464, #14379, #41543, #34441, #34872, #7304, #38312, #38099, #25095, #21445, #25, #34661, #42201, #3661, #10963, #27851, #3220, #41760, #17147, #44965, #20998, #24644, #38526, #3881, #28292, #24867, #7529, #12315, #1137, #18700, #42648, #29407, #4781, #913, #15272, #29630, #5003, #29181, #14834, #11416, #19144, #39218, #35786, #26212, #1360, #4555, #32591, #8437, #43093, #11862, #36460, #7982, #43545, #25992, #18916, #7760, #39450, #18482, #11631, #33028, #5230, #15056, #18250, #1802, #22342, #25325, #22559, #42874, #15729, #32808, #1578, #25768, #15499, #32145, #43319, #25544, #28744, #21668, #12087, #28967, #36237, #21891, #39897, #32371, #8212, #22119, #8658, #39673, #36011, #35556, #4328, #30307, #12539, #19369, #5675, #6137, #44684, #12992, #2255, #5449, #26443, #37600, #27118, #30759, #44232, #9564, #33940, #41042, #20281, #2483, #16869, #16637, #19824, #9111, #23479, #15955, #33712, #19593, #9798, #5902, #30531, #2030, #36903, #20058, #23013, #44452, #34166, #13444, #37366, #2710, #6370, #13219, #29858, #23709, #30088, #2938, #40121, #8884, #26888, #22785, #33258, #36679, #44001, #43774, #40349, #33474, #16183, #40807, #12765, #26664, #40577, #9337, #23246, #37127, #16408, #45124, #7469, #21387, #17520, #44909, #6591, #38045, #38474, #31867, #184, #34608, #37816, #13666, #24809, #14326, #17968, #31418, #41924, #21163, #28240, #35269, #34822, #4046, #3821, #7038, #41487, #10689, #3170, #20948, #6822, #42149, #38257, #17745, #34387, #24154, #7250, #10245, #31641, #634, #27350, #24591, #35041, #20509, #41269, #41704, #14102, #17312, #17092 ) ),
 .UNSPECIFIED., .F., .F., .T. ) 
 B_SPLINE_SURFACE_WITH_KNOTS ( ( 2, 2 ),
 ( 3, 2, 2, 2, 2, 2, 2, 2, 2, 2, 2, 2, 2, 2, 2, 2, 2, 2, 2, 2, 2, 2, 2, 2, 2, 2, 2, 2, 2, 2, 2, 2, 2, 2, 2, 2, 2, 2, 2, 2, 2, 2, 2, 2, 2, 2, 2, 2, 2, 2, 2, 2, 2, 2, 2, 2, 2, 2, 2, 2, 2, 2, 2, 2, 2, 2, 2, 2, 2, 2, 2, 2, 2, 2, 2, 2, 2, 2, 2, 2, 2, 2, 2, 2, 2, 2, 2, 2, 2, 2, 2, 2, 2, 2, 2, 2, 2, 2, 2, 2, 2, 2, 2, 2, 2, 2, 2, 2, 2, 2, 2, 2, 2, 2, 2, 2, 2, 2, 2, 2, 2, 2, 2, 2, 2, 2, 2, 2, 3 ),
 ( 0.000000000000000000, 1.000000000000000000 ),
 ( 0.000000000000000000, 0.007812500000000000000, 0.01562500000000000000, 0.02343750000000000000, 0.03125000000000000000, 0.03906250000000000000, 0.04687500000000000000, 0.05468750000000000000, 0.06250000000000000000, 0.07031250000000000000, 0.07812500000000000000, 0.08593750000000000000, 0.09375000000000000000, 0.1015625000000000000, 0.1093750000000000000, 0.1171875000000000000, 0.1250000000000000000, 0.1328125000000000000, 0.1406250000000000000, 0.1484375000000000000, 0.1562500000000000000, 0.1640625000000000000, 0.1718750000000000000, 0.1796875000000000000, 0.1875000000000000000, 0.1953125000000000000, 0.2031250000000000000, 0.2109375000000000000, 0.2187500000000000000, 0.2265625000000000000, 0.2343750000000000000, 0.2421875000000000000, 0.2500000000000000000, 0.2578125000000000000, 0.2656250000000000000, 0.2734375000000000000, 0.2812500000000000000, 0.2890625000000000000, 0.2968750000000000000, 0.3046875000000000000, 0.3125000000000000000, 0.3203125000000000000, 0.3281250000000000000, 0.3359375000000000000, 0.3437500000000000000, 0.3515625000000000000, 0.3593750000000000000, 0.3671875000000000000, 0.3750000000000000000, 0.3828125000000000000, 0.3906250000000000000, 0.3984375000000000000, 0.4062500000000000000, 0.4140625000000000000, 0.4218750000000000000, 0.4296875000000000000, 0.4375000000000000000, 0.4453125000000000000, 0.4531250000000000000, 0.4609375000000000000, 0.4687500000000000000, 0.4765625000000000000, 0.4843750000000000000, 0.4921875000000000000, 0.5000000000000000000, 0.5078125000000000000, 0.5156250000000000000, 0.5234375000000000000, 0.5312500000000000000, 0.5390625000000000000, 0.5468750000000000000, 0.5546875000000000000, 0.5625000000000000000, 0.5703125000000000000, 0.5781250000000000000, 0.5859375000000000000, 0.5937500000000000000, 0.6015625000000000000, 0.6093750000000000000, 0.6171875000000000000, 0.6250000000000000000, 0.6328125000000000000, 0.6406250000000000000, 0.6484375000000000000, 0.6562500000000000000, 0.6640625000000000000, 0.6718750000000000000, 0.6796875000000000000, 0.6875000000000000000, 0.6953125000000000000, 0.7031250000000000000, 0.7109375000000000000, 0.7187500000000000000, 0.7265625000000000000, 0.7343750000000000000, 0.7421875000000000000, 0.7500000000000000000, 0.7578125000000000000, 0.7656250000000000000, 0.7734375000000000000, 0.7812500000000000000, 0.7890625000000000000, 0.7968750000000000000, 0.8046875000000000000, 0.8125000000000000000, 0.8203125000000000000, 0.8281250000000000000, 0.8359375000000000000, 0.8437500000000000000, 0.8515625000000000000, 0.8593750000000000000, 0.8671875000000000000, 0.8750000000000000000, 0.8828125000000000000, 0.8906250000000000000, 0.8984375000000000000, 0.9062500000000000000, 0.9140625000000000000, 0.9218750000000000000, 0.9296875000000000000, 0.9375000000000000000, 0.9453125000000000000, 0.9531250000000000000, 0.9609375000000000000, 0.9687500000000000000, 0.9765625000000000000, 0.9843750000000000000, 0.9921875000000000000, 1.000000000000000000 ),
 .UNSPECIFIED. ) 
 GEOMETRIC_REPRESENTATION_ITEM ( )  RATIONAL_B_SPLINE_SURFACE ( (
 ( 1.000000000000000000, 0.9238795325112869605, 1.000000000000000000, 0.9238795325112869605, 1.000000000000000000, 0.9238795325112869605, 1.000000000000000000, 0.9238795325112869605, 1.000000000000000000, 0.9238795325112869605, 1.000000000000000000, 0.9238795325112869605, 1.000000000000000000, 0.9238795325112869605, 1.000000000000000000, 0.9238795325112869605, 1.000000000000000000, 0.9238795325112869605, 1.000000000000000000, 0.9238795325112869605, 1.000000000000000000, 0.9238795325112869605, 1.000000000000000000, 0.9238795325112869605, 1.000000000000000000, 0.9238795325112869605, 1.000000000000000000, 0.9238795325112869605, 1.000000000000000000, 0.9238795325112869605, 1.000000000000000000, 0.9238795325112869605, 1.000000000000000000, 0.9238795325112869605, 1.000000000000000000, 0.9238795325112869605, 1.000000000000000000, 0.9238795325112869605, 1.000000000000000000, 0.9238795325112869605, 1.000000000000000000, 0.9238795325112869605, 1.000000000000000000, 0.9238795325112869605, 1.000000000000000000, 0.9238795325112869605, 1.000000000000000000, 0.9238795325112869605, 1.000000000000000000, 0.9238795325112869605, 1.000000000000000000, 0.9238795325112869605, 1.000000000000000000, 0.9238795325112869605, 1.000000000000000000, 0.9238795325112869605, 1.000000000000000000, 0.9238795325112869605, 1.000000000000000000, 0.9238795325112869605, 1.000000000000000000, 0.9238795325112869605, 1.000000000000000000, 0.9238795325112869605, 1.000000000000000000, 0.9238795325112869605, 1.000000000000000000, 0.9238795325112869605, 1.000000000000000000, 0.9238795325112869605, 1.000000000000000000, 0.9238795325112869605, 1.000000000000000000, 0.9238795325112869605, 1.000000000000000000, 0.9238795325112869605, 1.000000000000000000, 0.9238795325112869605, 1.000000000000000000, 0.9238795325112869605, 1.000000000000000000, 0.9238795325112869605, 1.000000000000000000, 0.9238795325112869605, 1.000000000000000000, 0.9238795325112869605, 1.000000000000000000, 0.9238795325112869605, 1.000000000000000000, 0.9238795325112869605, 1.000000000000000000, 0.9238795325112869605, 1.000000000000000000, 0.9238795325112869605, 1.000000000000000000, 0.9238795325112869605, 1.000000000000000000, 0.9238795325112869605, 1.000000000000000000, 0.9238795325112869605, 1.000000000000000000, 0.9238795325112869605, 1.000000000000000000, 0.9238795325112869605, 1.000000000000000000, 0.9238795325112869605, 1.000000000000000000, 0.9238795325112869605, 1.000000000000000000, 0.9238795325112869605, 1.000000000000000000, 0.9238795325112869605, 1.000000000000000000, 0.9238795325112869605, 1.000000000000000000, 0.9238795325112869605, 1.000000000000000000, 0.9238795325112869605, 1.000000000000000000, 0.9238795325112869605, 1.000000000000000000, 0.9238795325112869605, 1.000000000000000000, 0.9238795325112869605, 1.000000000000000000, 0.9238795325112869605, 1.000000000000000000, 0.9238795325112869605, 1.000000000000000000, 0.9238795325112869605, 1.000000000000000000, 0.9238795325112869605, 1.000000000000000000, 0.9238795325112869605, 1.000000000000000000, 0.9238795325112869605, 1.000000000000000000, 0.9238795325112869605, 1.000000000000000000, 0.9238795325112869605, 1.000000000000000000, 0.9238795325112869605, 1.000000000000000000, 0.9238795325112869605, 1.000000000000000000, 0.9238795325112869605, 1.000000000000000000, 0.9238795325112869605, 1.000000000000000000, 0.9238795325112869605, 1.000000000000000000, 0.9238795325112869605, 1.000000000000000000, 0.9238795325112869605, 1.000000000000000000, 0.9238795325112869605, 1.000000000000000000, 0.9238795325112869605, 1.000000000000000000, 0.9238795325112869605, 1.000000000000000000, 0.9238795325112869605, 1.000000000000000000, 0.9238795325112869605, 1.000000000000000000, 0.9238795325112869605, 1.000000000000000000, 0.9238795325112869605, 1.000000000000000000, 0.9238795325112869605, 1.000000000000000000, 0.9238795325112869605, 1.000000000000000000, 0.9238795325112869605, 1.000000000000000000, 0.9238795325112869605, 1.000000000000000000, 0.9238795325112869605, 1.000000000000000000, 0.9238795325112869605, 1.000000000000000000, 0.9238795325112869605, 1.000000000000000000, 0.9238795325112869605, 1.000000000000000000, 0.9238795325112869605, 1.000000000000000000, 0.9238795325112869605, 1.000000000000000000, 0.9238795325112869605, 1.000000000000000000, 0.9238795325112869605, 1.000000000000000000, 0.9238795325112869605, 1.000000000000000000, 0.9238795325112869605, 1.000000000000000000, 0.9238795325112869605, 1.000000000000000000, 0.9238795325112869605, 1.000000000000000000, 0.9238795325112869605, 1.000000000000000000, 0.9238795325112869605, 1.000000000000000000, 0.9238795325112869605, 1.000000000000000000, 0.9238795325112869605, 1.000000000000000000, 0.9238795325112869605, 1.000000000000000000, 0.9238795325112869605, 1.000000000000000000, 0.9238795325112869605, 1.000000000000000000, 0.9238795325112869605, 1.000000000000000000, 0.9238795325112869605, 1.000000000000000000, 0.9238795325112869605, 1.000000000000000000, 0.9238795325112869605, 1.000000000000000000, 0.9238795325112869605, 1.000000000000000000, 0.9238795325112869605, 1.000000000000000000, 0.9238795325112869605, 1.000000000000000000, 0.9238795325112869605, 1.000000000000000000, 0.9238795325112869605, 1.000000000000000000, 0.9238795325112869605, 1.000000000000000000, 0.9238795325112869605, 1.000000000000000000, 0.9238795325112869605, 1.000000000000000000, 0.9238795325112869605, 1.000000000000000000, 0.9238795325112869605, 1.000000000000000000, 0.9238795325112869605, 1.000000000000000000, 0.9238795325112869605, 1.000000000000000000, 0.9238795325112869605, 1.000000000000000000, 0.9238795325112869605, 1.000000000000000000, 0.9238795325112869605, 1.000000000000000000, 0.9238795325112869605, 1.000000000000000000, 0.9238795325112869605, 1.000000000000000000),
 ( 1.000000000000000000, 0.9238795325112869605, 1.000000000000000000, 0.9238795325112869605, 1.000000000000000000, 0.9238795325112869605, 1.000000000000000000, 0.9238795325112869605, 1.000000000000000000, 0.9238795325112869605, 1.000000000000000000, 0.9238795325112869605, 1.000000000000000000, 0.9238795325112869605, 1.000000000000000000, 0.9238795325112869605, 1.000000000000000000, 0.9238795325112869605, 1.000000000000000000, 0.9238795325112869605, 1.000000000000000000, 0.9238795325112869605, 1.000000000000000000, 0.9238795325112869605, 1.000000000000000000, 0.9238795325112869605, 1.000000000000000000, 0.9238795325112869605, 1.000000000000000000, 0.9238795325112869605, 1.000000000000000000, 0.9238795325112869605, 1.000000000000000000, 0.9238795325112869605, 1.000000000000000000, 0.9238795325112869605, 1.000000000000000000, 0.9238795325112869605, 1.000000000000000000, 0.9238795325112869605, 1.000000000000000000, 0.9238795325112869605, 1.000000000000000000, 0.9238795325112869605, 1.000000000000000000, 0.9238795325112869605, 1.000000000000000000, 0.9238795325112869605, 1.000000000000000000, 0.9238795325112869605, 1.000000000000000000, 0.9238795325112869605, 1.000000000000000000, 0.9238795325112869605, 1.000000000000000000, 0.9238795325112869605, 1.000000000000000000, 0.9238795325112869605, 1.000000000000000000, 0.9238795325112869605, 1.000000000000000000, 0.9238795325112869605, 1.000000000000000000, 0.9238795325112869605, 1.000000000000000000, 0.9238795325112869605, 1.000000000000000000, 0.9238795325112869605, 1.000000000000000000, 0.9238795325112869605, 1.000000000000000000, 0.9238795325112869605, 1.000000000000000000, 0.9238795325112869605, 1.000000000000000000, 0.9238795325112869605, 1.000000000000000000, 0.9238795325112869605, 1.000000000000000000, 0.9238795325112869605, 1.000000000000000000, 0.9238795325112869605, 1.000000000000000000, 0.9238795325112869605, 1.000000000000000000, 0.9238795325112869605, 1.000000000000000000, 0.9238795325112869605, 1.000000000000000000, 0.9238795325112869605, 1.000000000000000000, 0.9238795325112869605, 1.000000000000000000, 0.9238795325112869605, 1.000000000000000000, 0.9238795325112869605, 1.000000000000000000, 0.9238795325112869605, 1.000000000000000000, 0.9238795325112869605, 1.000000000000000000, 0.9238795325112869605, 1.000000000000000000, 0.9238795325112869605, 1.000000000000000000, 0.9238795325112869605, 1.000000000000000000, 0.9238795325112869605, 1.000000000000000000, 0.9238795325112869605, 1.000000000000000000, 0.9238795325112869605, 1.000000000000000000, 0.9238795325112869605, 1.000000000000000000, 0.9238795325112869605, 1.000000000000000000, 0.9238795325112869605, 1.000000000000000000, 0.9238795325112869605, 1.000000000000000000, 0.9238795325112869605, 1.000000000000000000, 0.9238795325112869605, 1.000000000000000000, 0.9238795325112869605, 1.000000000000000000, 0.9238795325112869605, 1.000000000000000000, 0.9238795325112869605, 1.000000000000000000, 0.9238795325112869605, 1.000000000000000000, 0.9238795325112869605, 1.000000000000000000, 0.9238795325112869605, 1.000000000000000000, 0.9238795325112869605, 1.000000000000000000, 0.9238795325112869605, 1.000000000000000000, 0.9238795325112869605, 1.000000000000000000, 0.9238795325112869605, 1.000000000000000000, 0.9238795325112869605, 1.000000000000000000, 0.9238795325112869605, 1.000000000000000000, 0.9238795325112869605, 1.000000000000000000, 0.9238795325112869605, 1.000000000000000000, 0.9238795325112869605, 1.000000000000000000, 0.9238795325112869605, 1.000000000000000000, 0.9238795325112869605, 1.000000000000000000, 0.9238795325112869605, 1.000000000000000000, 0.9238795325112869605, 1.000000000000000000, 0.9238795325112869605, 1.000000000000000000, 0.9238795325112869605, 1.000000000000000000, 0.9238795325112869605, 1.000000000000000000, 0.9238795325112869605, 1.000000000000000000, 0.9238795325112869605, 1.000000000000000000, 0.9238795325112869605, 1.000000000000000000, 0.9238795325112869605, 1.000000000000000000, 0.9238795325112869605, 1.000000000000000000, 0.9238795325112869605, 1.000000000000000000, 0.9238795325112869605, 1.000000000000000000, 0.9238795325112869605, 1.000000000000000000, 0.9238795325112869605, 1.000000000000000000, 0.9238795325112869605, 1.000000000000000000, 0.9238795325112869605, 1.000000000000000000, 0.9238795325112869605, 1.000000000000000000, 0.9238795325112869605, 1.000000000000000000, 0.9238795325112869605, 1.000000000000000000, 0.9238795325112869605, 1.000000000000000000, 0.9238795325112869605, 1.000000000000000000, 0.9238795325112869605, 1.000000000000000000, 0.9238795325112869605, 1.000000000000000000, 0.9238795325112869605, 1.000000000000000000, 0.9238795325112869605, 1.000000000000000000, 0.9238795325112869605, 1.000000000000000000, 0.9238795325112869605, 1.000000000000000000, 0.9238795325112869605, 1.000000000000000000, 0.9238795325112869605, 1.000000000000000000, 0.9238795325112869605, 1.000000000000000000, 0.9238795325112869605, 1.000000000000000000, 0.9238795325112869605, 1.000000000000000000, 0.9238795325112869605, 1.000000000000000000, 0.9238795325112869605, 1.000000000000000000, 0.9238795325112869605, 1.000000000000000000, 0.9238795325112869605, 1.000000000000000000, 0.9238795325112869605, 1.000000000000000000, 0.9238795325112869605, 1.000000000000000000, 0.9238795325112869605, 1.000000000000000000, 0.9238795325112869605, 1.000000000000000000, 0.9238795325112869605, 1.000000000000000000, 0.9238795325112869605, 1.000000000000000000, 0.9238795325112869605, 1.000000000000000000, 0.9238795325112869605, 1.000000000000000000, 0.9238795325112869605, 1.000000000000000000, 0.9238795325112869605, 1.000000000000000000, 0.9238795325112869605, 1.000000000000000000, 0.9238795325112869605, 1.000000000000000000, 0.9238795325112869605, 1.000000000000000000) ) ) 
 REPRESENTATION_ITEM ( '' )  SURFACE ( )  );
#18036=CARTESIAN_POINT ( 'NONE',  ( 118.9794681442453026, -9.261995988541697145, -16.69588392320189030 ) ) ;
#18045=CARTESIAN_POINT ( 'NONE',  ( 124.2550481442452792, -9.988377603198980381, -10.36322818467138518 ) ) ;
#18046=CARTESIAN_POINT ( 'NONE',  ( 112.8529881442453302, -1.561330072975668060, -17.79121239304076596 ) ) ;
#18049=CARTESIAN_POINT ( 'NONE',  ( 113.7606148109119886, -7.894159318335828068, -9.358103419637847864 ) ) ;
#18051=CARTESIAN_POINT ( 'NONE',  ( 119.2631014775786440, -9.565557343593393824, -10.61323700422344274 ) ) ;
#18052=CARTESIAN_POINT ( 'NONE',  ( 112.1722681442453222, -8.899110576539710493, -16.42337572283490132 ) ) ;
#18055=CARTESIAN_POINT ( 'NONE',  ( 124.7088614775786226, 0.2603800115204892296, -16.42320221600525088 ) ) ;
#18057=CARTESIAN_POINT ( 'NONE',  ( 117.5613014775786525, 0.9020085738987339008, -11.91225656197089222 ) ) ;
#18062=CARTESIAN_POINT ( 'NONE',  ( 114.6682414775786469, -7.894159318335828068, -9.358103419637847864 ) ) ;
#18063=CARTESIAN_POINT ( 'NONE',  ( 112.2289948109119848, -1.834011780172310813, -8.268836392978581529 ) ) ;
#18064=CARTESIAN_POINT ( 'NONE',  ( 111.9453614775786434, -1.561330072975668060, -17.79121239304076596 ) ) ;
#18065=CARTESIAN_POINT ( 'NONE',  ( 118.4689281442453250, -10.15424416112534622, -14.75197769757730448 ) ) ;
#18066=CARTESIAN_POINT ( 'NONE',  ( 121.4187148109119789, -3.505236298600246325, -18.68346056562440793 ) ) ;
#18067=CARTESIAN_POINT ( 'NONE',  ( 117.1074881442453233, 0.4262465694468514643, -12.03445270309931736 ) ) ;
#18071=CARTESIAN_POINT ( 'NONE',  ( 114.6115148109119986, -6.222761293078241884, -8.102969835052219238 ) ) ;
#18076=CARTESIAN_POINT ( 'NONE',  ( 124.4819548109119722, -2.084020599724406786, -8.691656652584148546 ) ) ;
#18079=CARTESIAN_POINT ( 'NONE',  ( 117.7882081442453170, -3.505236298600246325, -18.68346056562440793 ) ) ;
#18081=CARTESIAN_POINT ( 'NONE',  ( 116.5969481442453031, -9.859900752359374465, -12.68260735090039404 ) ) ;
#18090=CARTESIAN_POINT ( 'NONE',  ( 112.3991748109119868, -8.166667518702817929, -8.995218007635859436 ) ) ;
#18091=CARTESIAN_POINT ( 'NONE',  ( 112.1722681442453222, -0.4660016031367893996, -10.09054647747474043 ) ) ;
#18092=CARTESIAN_POINT ( 'NONE',  ( 116.3133148109120043, -2.084020599724406786, -8.691656652584148546 ) ) ;
#18093=VERTEX_POINT ( 'NONE', #25113 ) ;
#18094=CARTESIAN_POINT ( 'NONE',  ( 117.8449348109119938, -1.833838273342659253, -17.42832698103878286 ) ) ;
#18096=CARTESIAN_POINT ( 'NONE',  ( 126.2184548109119788, -4.863998795839242995, -13.39321520033831447 ) ) ;
#18098=CARTESIAN_POINT ( 'NONE',  ( 115.4624148109119943, -5.638512984488999180, -18.83840828888717311 ) ) ;
#18100=EDGE_CURVE ( 'NONE', #2538, #39913, #6365, .T. ) ;
#18101=CARTESIAN_POINT ( 'NONE',  ( 118.4122014775786340, 0.5811942927096110934, -14.16772938898807510 ) ) ;
#18104=CARTESIAN_POINT ( 'NONE',  ( 116.9373081442452929, -8.166667518702817929, -8.995218007635861213 ) ) ;
#18107=CARTESIAN_POINT ( 'NONE',  ( 115.3489614775786407, -9.261995988541697145, -16.69588392320189030 ) ) ;
#18108=CARTESIAN_POINT ( 'NONE',  ( 126.2184548109105435, -9.814174330883648878, -12.68911139247483710 ) ) ;
#18114=CARTESIAN_POINT ( 'NONE',  ( 116.5969481442453031, -9.859900752359374465, -12.68260735090039404 ) ) ;
#18119=CARTESIAN_POINT ( 'NONE',  ( 114.8951481442453115, -8.899110576539710493, -16.42337572283490132 ) ) ;
#18120=CARTESIAN_POINT ( 'NONE',  ( 120.3976348109119812, -7.643976991954104960, -18.09477374809246442 ) ) ;
#18121=CARTESIAN_POINT ( 'NONE',  ( 122.9503348109119827, 0.5811942927096110934, -14.16772938898807510 ) ) ;
#18122=CARTESIAN_POINT ( 'NONE',  ( 114.4980614775786592, -7.893985811506177619, -18.51759400769804742 ) ) ;
#18124=CARTESIAN_POINT ( 'NONE',  ( 114.5547881442453217, -4.153390946401321671, -8.397313243818183892 ) ) ;
#18126=CARTESIAN_POINT ( 'NONE',  ( 117.9583881442453048, -10.30919188438810075, -12.61870101168855918 ) ) ;
#18128=CARTESIAN_POINT ( 'NONE',  ( 119.1496481442453046, -6.222761293078241884, -8.102969835052219238 ) ) ;
#18130=CARTESIAN_POINT ( 'NONE',  ( 122.6099748109119929, -0.8288870151387760510, -10.36305467784173118 ) ) ;
#18131=CARTESIAN_POINT ( 'NONE',  ( 115.5191414775786569, -3.383040157471821630, -19.15922257007629170 ) ) ;
#18132=CARTESIAN_POINT ( 'NONE',  ( 137.3645353335808750, 0.1036370839169628438, -14.77667914328649879 ) ) ;
#18135=CARTESIAN_POINT ( 'NONE',  ( 126.2807669870676648, 0.1502658026859126084, -13.80526545341719036 ) ) ;
#18137=CARTESIAN_POINT ( 'NONE',  ( 116.4267681442453153, -3.383040157471821630, -19.15922257007629170 ) ) ;
#18140=CARTESIAN_POINT ( 'NONE',  ( 136.7478768735761321, -10.46432003856224568, -13.90125341227964917 ) ) ;
#18141=CARTESIAN_POINT ( 'NONE',  ( 116.3133148109120043, -2.084020599724406786, -8.691656652584148546 ) ) ;
#18144=CARTESIAN_POINT ( 'NONE',  ( 117.2776681442452968, -4.153390946401313677, -8.397313243818183892 ) ) ;
#18146=FACE_OUTER_BOUND ( 'NONE', #13553, .T. ) ;
#18150=CARTESIAN_POINT ( 'NONE',  ( 117.7314814775786260, -4.089484607189486809, -7.948022111789456723 ) ) ;
#18151=CARTESIAN_POINT ( 'NONE',  ( 117.6747548109119919, -7.643976991954077427, -18.09477374809248928 ) ) ;
#18152=CARTESIAN_POINT ( 'NONE',  ( 125.3328548109119964, -9.261995988541697145, -16.69588392320189030 ) ) ;
#18155=CARTESIAN_POINT ( 'NONE',  ( 123.3474214775786209, -9.988377603198976828, -10.36322818467138340 ) ) ;
#18157=CARTESIAN_POINT ( 'NONE',  ( 119.1496481442453046, -6.222761293078241884, -8.102969835052219238 ) ) ;
#18158=CARTESIAN_POINT ( 'NONE',  ( 117.6747548109119919, -7.643976991954077427, -18.09477374809248928 ) ) ;
#18161=CARTESIAN_POINT ( 'NONE',  ( 121.7023481442452919, -0.8288870151387760510, -10.36305467784173118 ) ) ;
#18162=CARTESIAN_POINT ( 'NONE',  ( 122.4965214775786251, 0.1319031606808879209, -14.10382304977623669 ) ) ;
#18163=CARTESIAN_POINT ( 'NONE',  ( 114.7249681442453237, -9.565557343593411588, -10.61323700422346583 ) ) ;
#18168=CARTESIAN_POINT ( 'NONE',  ( 117.0507614775786465, -10.30919188438810075, -12.61870101168855918 ) ) ;
#18169=CARTESIAN_POINT ( 'NONE',  ( 117.7882081442453170, -6.344957434206665248, -7.627207830600338134 ) ) ;
#18172=CARTESIAN_POINT ( 'NONE',  ( 113.1933481442453058, -4.089484607189486809, -7.948022111789456723 ) ) ;
#18175=CARTESIAN_POINT ( 'NONE',  ( 117.7882081442453170, -6.344957434206665248, -7.627207830600338134 ) ) ;
#18177=CARTESIAN_POINT ( 'NONE',  ( 122.2128881442453263, -7.643976991954077427, -18.09477374809248928 ) ) ;
#18180=CARTESIAN_POINT ( 'NONE',  ( 124.4252281442452812, -9.261995988541697145, -16.69588392320189030 ) ) ;
#18181=CARTESIAN_POINT ( 'NONE',  ( 122.3263414775786373, -6.344957434206665248, -7.627207830600338134 ) ) ;
#18183=CARTESIAN_POINT ( 'NONE',  ( 114.6115148109119986, -6.222761293078241884, -8.102969835052219238 ) ) ;
#18187=CARTESIAN_POINT ( 'NONE',  ( 121.5888948109119809, -10.30919188438810075, -12.61870101168855918 ) ) ;
#18189=CARTESIAN_POINT ( 'NONE',  ( 120.3409081442453044, -0.4660016031367893996, -10.09054647747474043 ) ) ;
#18191=CARTESIAN_POINT ( 'NONE',  ( 125.5597614775786326, -7.894159318335828068, -9.358103419637847864 ) ) ;
#18193=CARTESIAN_POINT ( 'NONE',  ( 119.7177477074048966, -2.419733177069661512, -17.89711025544711376 ) ) ;
#18194=CARTESIAN_POINT ( 'NONE',  ( 114.4413348109119823, -0.8288870151387760510, -10.36305467784173118 ) ) ;
#18197=CARTESIAN_POINT ( 'NONE',  ( 118.0718414775786442, -0.8288870151387760510, -10.36305467784173118 ) ) ;
#18199=CARTESIAN_POINT ( 'NONE',  ( 120.6812681442452941, 0.1319031606808879209, -14.10382304977623669 ) ) ;
#18202=CARTESIAN_POINT ( 'NONE',  ( 119.0929214775786278, -4.153390946401325223, -8.397313243818185668 ) ) ;
#18203=CARTESIAN_POINT ( 'NONE',  ( 114.7816948109119863, 0.5811942927096154232, -14.16772938898807155 ) ) ;
#18204=CARTESIAN_POINT ( 'NONE',  ( 120.3409081442453044, -0.4660016031367893996, -10.09054647747474043 ) ) ;
#18205=CARTESIAN_POINT ( 'NONE',  ( 113.6471614775786492, -5.638512984488999180, -18.83840828888717311 ) ) ;
#18207=CARTESIAN_POINT ( 'NONE',  ( 121.7590748109119687, -2.084020599724406786, -8.691656652584148546 ) ) ;
#18208=ORIENTED_EDGE ( 'NONE', *, *, #40630, .T. ) ;
#18209=CARTESIAN_POINT ( 'NONE',  ( 121.5888948109119809, -10.30919188438810075, -12.61870101168855918 ) ) ;
#18214=EDGE_CURVE ( 'NONE', #21938, #40512, #35659, .T. ) ;
#18216=CARTESIAN_POINT ( 'NONE',  ( 126.2404814775786264, -9.261995988541697145, -16.69588392320189030 ) ) ;
#18220=CARTESIAN_POINT ( 'NONE',  ( 123.1205148109119563, -7.643976991954077427, -18.09477374809248928 ) ) ;
#18227=CARTESIAN_POINT ( 'NONE',  ( 114.8384214775786489, 0.9020085738987339008, -11.91225656197089222 ) ) ;
#18228=CARTESIAN_POINT ( 'NONE',  ( 115.1220548109119761, -8.166667518702817929, -8.995218007635861213 ) ) ;
#18230=CARTESIAN_POINT ( 'NONE',  ( 121.5321681442453183, -0.1624402480850797581, -16.17319339645315424 ) ) ;
#18231=CARTESIAN_POINT ( 'NONE',  ( 126.9276200068654674, -3.142429669179889196, -8.322895171908893275 ) ) ;
#18232=CARTESIAN_POINT ( 'NONE',  ( 121.8158014775786171, -5.638512984488999180, -18.83840828888717311 ) ) ;
#18233=CARTESIAN_POINT ( 'NONE',  ( 112.0020881442453344, -9.565557343593413364, -10.61323700422348004 ) ) ;
#18236=CARTESIAN_POINT ( 'NONE',  ( 111.9453614775786434, -1.561330072975668060, -17.79121239304076596 ) ) ;
#18239=AXIS2_PLACEMENT_3D ( 'NONE', #21966, #18548, #17873 ) ;
#18241=CARTESIAN_POINT ( 'NONE',  ( 120.9649014775786355, -3.383040157471821630, -19.15922257007629170 ) ) ;
#18244=CARTESIAN_POINT ( 'NONE',  ( 121.3820794150595930, -2.423081321603731908, -17.89265170041263175 ) ) ;
#18245=CARTESIAN_POINT ( 'NONE',  ( 112.1722681442453222, -8.899110576539710493, -16.42337572283490132 ) ) ;
#18247=CARTESIAN_POINT ( 'NONE',  ( 124.6521348109119884, -7.894159318335828068, -9.358103419637847864 ) ) ;
#18250=CARTESIAN_POINT ( 'NONE',  ( 118.2987481442453088, -1.561330072975668504, -17.79121239304076951 ) ) ;
#18254=CARTESIAN_POINT ( 'NONE',  ( 111.4556253487318997, -2.476252568991189396, -17.82184623478305596 ) ) ;
#18255=CARTESIAN_POINT ( 'NONE',  ( 111.5482748109120053, -0.1624402480850797581, -16.17319339645315424 ) ) ;
#18258=CARTESIAN_POINT ( 'NONE',  ( 125.2194014775786286, -10.30919188438810075, -12.61870101168855918 ) ) ;
#18259=CARTESIAN_POINT ( 'NONE',  ( 123.9146881442452894, 0.9020085738987339008, -11.91225656197089222 ) ) ;
#18260=CARTESIAN_POINT ( 'NONE',  ( 122.2128881442453263, -7.643976991954077427, -18.09477374809248928 ) ) ;
#18262=CARTESIAN_POINT ( 'NONE',  ( 123.6877814775786533, -6.222761293078241884, -8.102969835052219238 ) ) ;
#18263=CARTESIAN_POINT ( 'NONE',  ( 112.5126281442453120, 0.1319031606808879209, -14.10382304977623669 ) ) ;
#18264=CARTESIAN_POINT ( 'NONE',  ( 118.4689281442453392, 0.9020085738987339008, -11.91225656197089222 ) ) ;
#18271=CARTESIAN_POINT ( 'NONE',  ( 125.4463081442452932, -5.638512984488999180, -18.83840828888717311 ) ) ;
#18272=CARTESIAN_POINT ( 'NONE',  ( 116.5402214775786405, 0.2603800115204892296, -16.42320221600525088 ) ) ;
#18274=CARTESIAN_POINT ( 'NONE',  ( 113.1366214775786432, -7.643976991954077427, -18.09477374809248928 ) ) ;
#18280=CARTESIAN_POINT ( 'NONE',  ( 115.6893214775786447, 0.5811942927096154232, -14.16772938898807155 ) ) ;
#18285=CARTESIAN_POINT ( 'NONE',  ( 117.8449348109119938, -1.833838273342659253, -17.42832698103878286 ) ) ;
#18286=CARTESIAN_POINT ( 'NONE',  ( 115.4056881442453459, -7.893985811506177619, -18.51759400769804742 ) ) ;
#18287=CARTESIAN_POINT ( 'NONE',  ( 112.3991748109119868, -8.166667518702817929, -8.995218007635859436 ) ) ;
#18288=VECTOR ( 'NONE', #14922, 1000.000000000000114 ) ;
#18289=CARTESIAN_POINT ( 'NONE',  ( 125.6164881442453094, -9.565557343593413364, -10.61323700422348004 ) ) ;
#18290=CARTESIAN_POINT ( 'NONE',  ( 121.5321681442453183, -0.1624402480850797581, -16.17319339645315424 ) ) ;
#18291=CARTESIAN_POINT ( 'NONE',  ( 117.3343948109119737, -6.222761293078241884, -8.102969835052219238 ) ) ;
#18295=CARTESIAN_POINT ( 'NONE',  ( 119.0929214775786278, -4.153390946401325223, -8.397313243818185668 ) ) ;
#18298=CARTESIAN_POINT ( 'NONE',  ( 113.8173414775786512, 0.2603800115204892296, -16.42320221600525088 ) ) ;
#18300=CARTESIAN_POINT ( 'NONE',  ( 113.8740681442453138, -9.859900752359374465, -12.68260735090039404 ) ) ;
#18301=ORIENTED_EDGE ( 'NONE', *, *, #13860, .F. ) ;
#18302=VERTEX_POINT ( 'NONE', #8676 ) ;
#18304=CARTESIAN_POINT ( 'NONE',  ( 119.6034614775786196, -3.505236298600246325, -18.68346056562440793 ) ) ;
#18305=CARTESIAN_POINT ( 'NONE',  ( 119.2063748109119814, -7.894159318335828068, -9.358103419637847864 ) ) ;
#18306=( BOUNDED_SURFACE ( )  B_SPLINE_SURFACE ( 1, 2, ( 
 ( #13669, #44686, #10248, #17523, #9801, #34390, #37602, #186, #3395, #14104, #41927, #30533, #23711, #27577, #44455, #27120, #37368, #20283, #2941, #24156, #20060, #16871, #20511, #38047, #33942, #3172, #2713, #30761, #13221, #23936, #37818, #6594, #42374, #4507, #3823, #15222, #38704, #22068, #28467, #11135, #18194, #412, #25493, #636, #8162, #35733, #4048, #39397, #4276, #25268, #29129, #28913, #18429, #35959, #18648, #14329, #10691, #10911, #28692, #32321, #42151, #4730, #14549, #1086, #15000, #38476, #24594, #32540, #7252, #35043, #21389, #21839, #21167, #42596, #17970, #17747, #24812, #1310, #31871, #31643, #28243, #7471, #35504, #42823, #11584, #32088, #35271, #25038, #859, #39165, #38930, #7701, #21615, #14777, #11358, #7929, #8829, #22509, #40064, #33205, #5404, #39846, #25938, #22291, #4951, #12265, #8385, #12488, #8610, #36185, #32976, #5173, #1752, #19320, #15451, #18864, #22730, #26159, #1529, #15676, #36630, #29355, #1980, #15906, #32756, #36403, #19091, #29580, #43270, #43719, #43496, #12036, #25716, #29805, #43041, #11809, #39623, #32500, #1274, #11770, #26122, #40259, #43230, #29318, #36143, #36594, #33166, #15186, #8791, #43459, #29543, #43909, #5369, #26351, #32719, #16087, #15413, #22923, #25456, #29090, #19054, #1941, #43675, #39359, #1716, #22473, #8126, #12224, #29764, #15867, #11997, #12450, #9025, #36816, #29992, #33386, #5584, #19508, #39804, #15639, #22028, #25678, #8572, #36367, #40027, #43001, #39584, #8346, #25900, #19287, #2159, #35921, #4688, #22698, #18608, #22248, #4912, #5138, #32940, #18827, #1491, #2391, #34081, #41175, #40490, #34305, #6277, #30673, #20197, #34521, #17223, #9473, #19960, #19729, #37503, #2848, #9935, #37735, #30446, #27261, #23384, #13128, #16780, #16319, #5810, #3299, #37040, #3078, #9250, #30222, #44593, #13356, #23848, #6506, #23159, #20421, #17006, #30895, #44817, #13575, #44142, #27485, #40947, #41404, #27032, #10160, #37269, #24068, #37959, #6735, #6038, #12678, #20645, #31113, #26576, #33614, #12907 ),
 ( #26804, #40714, #33849, #2618, #16550, #44366, #9704, #23617, #14018, #324, #24505, #32000, #10821, #21525, #28154, #7611, #28599, #14685, #14237, #17660, #20859, #17438, #42282, #38176, #18332, #42063, #34737, #21300, #38607, #35183, #763, #38389, #3520, #35412, #11044, #41843, #3960, #4187, #27933, #42510, #11270, #31331, #24718, #7383, #17882, #7162, #21074, #31779, #25178, #105, #551, #10603, #39076, #28369, #7845, #21751, #6954, #34951, #14462, #3737, #31556, #35644, #24946, #38842, #18107, #4418, #45038, #13798, #27710, #41624, #10380, #24290, #18557, #22870, #5316, #43401, #5534, #18782, #26071, #25404, #36763, #15137, #43624, #4864, #32672, #39751, #21975, #1883, #22197, #29711, #12169, #25631, #15810, #25843, #1662, #32225, #19232, #39975, #12398, #40205, #35862, #998, #32449, #5085, #8738, #1223, #26298, #36093, #22646, #36542, #14913, #28824, #8971, #42734, #11499, #42952, #33115, #39303, #19001, #39534, #8074, #4636, #29043, #11718, #8295, #22423, #29488, #1440, #29267, #32888, #8520, #43181, #15362, #11947, #36315, #15586, #30622, #37904, #5985, #13299, #12629, #24016, #2338, #30844, #37213, #19910, #26974, #9197, #34254, #9415, #16950, #44537, #12853, #3029, #13076, #34030, #19451, #37685, #27207, #44767, #27434, #23106, #33334, #19673, #37450, #41125, #5753, #13526, #23327, #9884, #23795, #2108, #16036, #41356, #29944, #43857, #30171, #6458, #26527, #6222, #26754, #40436, #33561, #10113, #40663, #36984, #16267, #2799, #20367, #44088, #33795, #40894, #2567, #16496, #44318, #16725, #30396, #9647, #23569, #20146, #38788, #17610, #28318, #34899, #14408, #35357, #21474, #7116, #24448, #27658, #24234, #3910, #44990, #25126, #21026, #41571, #28102, #273, #42008, #7560, #31279, #10331, #42230, #17828, #3475, #10772, #10994, #34687, #4133, #18055, #38127, #3688, #31502, #14183, #13966, #27877, #24668, #31946, #6898, #38555, #20808, #711, #35128, #14632, #28550, #13749, #17391, #7331, #24895, #53, #31724, #21250, #496, #6682, #42454, #11220, #41791 ) ),
 .UNSPECIFIED., .F., .F., .T. ) 
 B_SPLINE_SURFACE_WITH_KNOTS ( ( 2, 2 ),
 ( 3, 2, 2, 2, 2, 2, 2, 2, 2, 2, 2, 2, 2, 2, 2, 2, 2, 2, 2, 2, 2, 2, 2, 2, 2, 2, 2, 2, 2, 2, 2, 2, 2, 2, 2, 2, 2, 2, 2, 2, 2, 2, 2, 2, 2, 2, 2, 2, 2, 2, 2, 2, 2, 2, 2, 2, 2, 2, 2, 2, 2, 2, 2, 2, 2, 2, 2, 2, 2, 2, 2, 2, 2, 2, 2, 2, 2, 2, 2, 2, 2, 2, 2, 2, 2, 2, 2, 2, 2, 2, 2, 2, 2, 2, 2, 2, 2, 2, 2, 2, 2, 2, 2, 2, 2, 2, 2, 2, 2, 2, 2, 2, 2, 2, 2, 2, 2, 2, 2, 2, 2, 2, 2, 2, 2, 2, 2, 2, 3 ),
 ( 0.000000000000000000, 1.000000000000000000 ),
 ( 0.000000000000000000, 0.007812500000000000000, 0.01562500000000000000, 0.02343750000000000000, 0.03125000000000000000, 0.03906250000000000000, 0.04687500000000000000, 0.05468750000000000000, 0.06250000000000000000, 0.07031250000000000000, 0.07812500000000000000, 0.08593750000000000000, 0.09375000000000000000, 0.1015625000000000000, 0.1093750000000000000, 0.1171875000000000000, 0.1250000000000000000, 0.1328125000000000000, 0.1406250000000000000, 0.1484375000000000000, 0.1562500000000000000, 0.1640625000000000000, 0.1718750000000000000, 0.1796875000000000000, 0.1875000000000000000, 0.1953125000000000000, 0.2031250000000000000, 0.2109375000000000000, 0.2187500000000000000, 0.2265625000000000000, 0.2343750000000000000, 0.2421875000000000000, 0.2500000000000000000, 0.2578125000000000000, 0.2656250000000000000, 0.2734375000000000000, 0.2812500000000000000, 0.2890625000000000000, 0.2968750000000000000, 0.3046875000000000000, 0.3125000000000000000, 0.3203125000000000000, 0.3281250000000000000, 0.3359375000000000000, 0.3437500000000000000, 0.3515625000000000000, 0.3593750000000000000, 0.3671875000000000000, 0.3750000000000000000, 0.3828125000000000000, 0.3906250000000000000, 0.3984375000000000000, 0.4062500000000000000, 0.4140625000000000000, 0.4218750000000000000, 0.4296875000000000000, 0.4375000000000000000, 0.4453125000000000000, 0.4531250000000000000, 0.4609375000000000000, 0.4687500000000000000, 0.4765625000000000000, 0.4843750000000000000, 0.4921875000000000000, 0.5000000000000000000, 0.5078125000000000000, 0.5156250000000000000, 0.5234375000000000000, 0.5312500000000000000, 0.5390625000000000000, 0.5468750000000000000, 0.5546875000000000000, 0.5625000000000000000, 0.5703125000000000000, 0.5781250000000000000, 0.5859375000000000000, 0.5937500000000000000, 0.6015625000000000000, 0.6093750000000000000, 0.6171875000000000000, 0.6250000000000000000, 0.6328125000000000000, 0.6406250000000000000, 0.6484375000000000000, 0.6562500000000000000, 0.6640625000000000000, 0.6718750000000000000, 0.6796875000000000000, 0.6875000000000000000, 0.6953125000000000000, 0.7031250000000000000, 0.7109375000000000000, 0.7187500000000000000, 0.7265625000000000000, 0.7343750000000000000, 0.7421875000000000000, 0.7500000000000000000, 0.7578125000000000000, 0.7656250000000000000, 0.7734375000000000000, 0.7812500000000000000, 0.7890625000000000000, 0.7968750000000000000, 0.8046875000000000000, 0.8125000000000000000, 0.8203125000000000000, 0.8281250000000000000, 0.8359375000000000000, 0.8437500000000000000, 0.8515625000000000000, 0.8593750000000000000, 0.8671875000000000000, 0.8750000000000000000, 0.8828125000000000000, 0.8906250000000000000, 0.8984375000000000000, 0.9062500000000000000, 0.9140625000000000000, 0.9218750000000000000, 0.9296875000000000000, 0.9375000000000000000, 0.9453125000000000000, 0.9531250000000000000, 0.9609375000000000000, 0.9687500000000000000, 0.9765625000000000000, 0.9843750000000000000, 0.9921875000000000000, 1.000000000000000000 ),
 .UNSPECIFIED. ) 
 GEOMETRIC_REPRESENTATION_ITEM ( )  RATIONAL_B_SPLINE_SURFACE ( (
 ( 1.000000000000000000, 0.9238795325112869605, 1.000000000000000000, 0.9238795325112869605, 1.000000000000000000, 0.9238795325112869605, 1.000000000000000000, 0.9238795325112869605, 1.000000000000000000, 0.9238795325112869605, 1.000000000000000000, 0.9238795325112869605, 1.000000000000000000, 0.9238795325112869605, 1.000000000000000000, 0.9238795325112869605, 1.000000000000000000, 0.9238795325112869605, 1.000000000000000000, 0.9238795325112869605, 1.000000000000000000, 0.9238795325112869605, 1.000000000000000000, 0.9238795325112869605, 1.000000000000000000, 0.9238795325112869605, 1.000000000000000000, 0.9238795325112869605, 1.000000000000000000, 0.9238795325112869605, 1.000000000000000000, 0.9238795325112869605, 1.000000000000000000, 0.9238795325112869605, 1.000000000000000000, 0.9238795325112869605, 1.000000000000000000, 0.9238795325112869605, 1.000000000000000000, 0.9238795325112869605, 1.000000000000000000, 0.9238795325112869605, 1.000000000000000000, 0.9238795325112869605, 1.000000000000000000, 0.9238795325112869605, 1.000000000000000000, 0.9238795325112869605, 1.000000000000000000, 0.9238795325112869605, 1.000000000000000000, 0.9238795325112869605, 1.000000000000000000, 0.9238795325112869605, 1.000000000000000000, 0.9238795325112869605, 1.000000000000000000, 0.9238795325112869605, 1.000000000000000000, 0.9238795325112869605, 1.000000000000000000, 0.9238795325112869605, 1.000000000000000000, 0.9238795325112869605, 1.000000000000000000, 0.9238795325112869605, 1.000000000000000000, 0.9238795325112869605, 1.000000000000000000, 0.9238795325112869605, 1.000000000000000000, 0.9238795325112869605, 1.000000000000000000, 0.9238795325112869605, 1.000000000000000000, 0.9238795325112869605, 1.000000000000000000, 0.9238795325112869605, 1.000000000000000000, 0.9238795325112869605, 1.000000000000000000, 0.9238795325112869605, 1.000000000000000000, 0.9238795325112869605, 1.000000000000000000, 0.9238795325112869605, 1.000000000000000000, 0.9238795325112869605, 1.000000000000000000, 0.9238795325112869605, 1.000000000000000000, 0.9238795325112869605, 1.000000000000000000, 0.9238795325112869605, 1.000000000000000000, 0.9238795325112869605, 1.000000000000000000, 0.9238795325112869605, 1.000000000000000000, 0.9238795325112869605, 1.000000000000000000, 0.9238795325112869605, 1.000000000000000000, 0.9238795325112869605, 1.000000000000000000, 0.9238795325112869605, 1.000000000000000000, 0.9238795325112869605, 1.000000000000000000, 0.9238795325112869605, 1.000000000000000000, 0.9238795325112869605, 1.000000000000000000, 0.9238795325112869605, 1.000000000000000000, 0.9238795325112869605, 1.000000000000000000, 0.9238795325112869605, 1.000000000000000000, 0.9238795325112869605, 1.000000000000000000, 0.9238795325112869605, 1.000000000000000000, 0.9238795325112869605, 1.000000000000000000, 0.9238795325112869605, 1.000000000000000000, 0.9238795325112869605, 1.000000000000000000, 0.9238795325112869605, 1.000000000000000000, 0.9238795325112869605, 1.000000000000000000, 0.9238795325112869605, 1.000000000000000000, 0.9238795325112869605, 1.000000000000000000, 0.9238795325112869605, 1.000000000000000000, 0.9238795325112869605, 1.000000000000000000, 0.9238795325112869605, 1.000000000000000000, 0.9238795325112869605, 1.000000000000000000, 0.9238795325112869605, 1.000000000000000000, 0.9238795325112869605, 1.000000000000000000, 0.9238795325112869605, 1.000000000000000000, 0.9238795325112869605, 1.000000000000000000, 0.9238795325112869605, 1.000000000000000000, 0.9238795325112869605, 1.000000000000000000, 0.9238795325112869605, 1.000000000000000000, 0.9238795325112869605, 1.000000000000000000, 0.9238795325112869605, 1.000000000000000000, 0.9238795325112869605, 1.000000000000000000, 0.9238795325112869605, 1.000000000000000000, 0.9238795325112869605, 1.000000000000000000, 0.9238795325112869605, 1.000000000000000000, 0.9238795325112869605, 1.000000000000000000, 0.9238795325112869605, 1.000000000000000000, 0.9238795325112869605, 1.000000000000000000, 0.9238795325112869605, 1.000000000000000000, 0.9238795325112869605, 1.000000000000000000, 0.9238795325112869605, 1.000000000000000000, 0.9238795325112869605, 1.000000000000000000, 0.9238795325112869605, 1.000000000000000000, 0.9238795325112869605, 1.000000000000000000, 0.9238795325112869605, 1.000000000000000000, 0.9238795325112869605, 1.000000000000000000, 0.9238795325112869605, 1.000000000000000000, 0.9238795325112869605, 1.000000000000000000, 0.9238795325112869605, 1.000000000000000000, 0.9238795325112869605, 1.000000000000000000, 0.9238795325112869605, 1.000000000000000000, 0.9238795325112869605, 1.000000000000000000, 0.9238795325112869605, 1.000000000000000000, 0.9238795325112869605, 1.000000000000000000, 0.9238795325112869605, 1.000000000000000000, 0.9238795325112869605, 1.000000000000000000, 0.9238795325112869605, 1.000000000000000000, 0.9238795325112869605, 1.000000000000000000, 0.9238795325112869605, 1.000000000000000000, 0.9238795325112869605, 1.000000000000000000, 0.9238795325112869605, 1.000000000000000000, 0.9238795325112869605, 1.000000000000000000, 0.9238795325112869605, 1.000000000000000000, 0.9238795325112869605, 1.000000000000000000, 0.9238795325112869605, 1.000000000000000000, 0.9238795325112869605, 1.000000000000000000, 0.9238795325112869605, 1.000000000000000000, 0.9238795325112869605, 1.000000000000000000, 0.9238795325112869605, 1.000000000000000000, 0.9238795325112869605, 1.000000000000000000, 0.9238795325112869605, 1.000000000000000000, 0.9238795325112869605, 1.000000000000000000, 0.9238795325112869605, 1.000000000000000000, 0.9238795325112869605, 1.000000000000000000, 0.9238795325112869605, 1.000000000000000000, 0.9238795325112869605, 1.000000000000000000, 0.9238795325112869605, 1.000000000000000000, 0.9238795325112869605, 1.000000000000000000),
 ( 1.000000000000000000, 0.9238795325112869605, 1.000000000000000000, 0.9238795325112869605, 1.000000000000000000, 0.9238795325112869605, 1.000000000000000000, 0.9238795325112869605, 1.000000000000000000, 0.9238795325112869605, 1.000000000000000000, 0.9238795325112869605, 1.000000000000000000, 0.9238795325112869605, 1.000000000000000000, 0.9238795325112869605, 1.000000000000000000, 0.9238795325112869605, 1.000000000000000000, 0.9238795325112869605, 1.000000000000000000, 0.9238795325112869605, 1.000000000000000000, 0.9238795325112869605, 1.000000000000000000, 0.9238795325112869605, 1.000000000000000000, 0.9238795325112869605, 1.000000000000000000, 0.9238795325112869605, 1.000000000000000000, 0.9238795325112869605, 1.000000000000000000, 0.9238795325112869605, 1.000000000000000000, 0.9238795325112869605, 1.000000000000000000, 0.9238795325112869605, 1.000000000000000000, 0.9238795325112869605, 1.000000000000000000, 0.9238795325112869605, 1.000000000000000000, 0.9238795325112869605, 1.000000000000000000, 0.9238795325112869605, 1.000000000000000000, 0.9238795325112869605, 1.000000000000000000, 0.9238795325112869605, 1.000000000000000000, 0.9238795325112869605, 1.000000000000000000, 0.9238795325112869605, 1.000000000000000000, 0.9238795325112869605, 1.000000000000000000, 0.9238795325112869605, 1.000000000000000000, 0.9238795325112869605, 1.000000000000000000, 0.9238795325112869605, 1.000000000000000000, 0.9238795325112869605, 1.000000000000000000, 0.9238795325112869605, 1.000000000000000000, 0.9238795325112869605, 1.000000000000000000, 0.9238795325112869605, 1.000000000000000000, 0.9238795325112869605, 1.000000000000000000, 0.9238795325112869605, 1.000000000000000000, 0.9238795325112869605, 1.000000000000000000, 0.9238795325112869605, 1.000000000000000000, 0.9238795325112869605, 1.000000000000000000, 0.9238795325112869605, 1.000000000000000000, 0.9238795325112869605, 1.000000000000000000, 0.9238795325112869605, 1.000000000000000000, 0.9238795325112869605, 1.000000000000000000, 0.9238795325112869605, 1.000000000000000000, 0.9238795325112869605, 1.000000000000000000, 0.9238795325112869605, 1.000000000000000000, 0.9238795325112869605, 1.000000000000000000, 0.9238795325112869605, 1.000000000000000000, 0.9238795325112869605, 1.000000000000000000, 0.9238795325112869605, 1.000000000000000000, 0.9238795325112869605, 1.000000000000000000, 0.9238795325112869605, 1.000000000000000000, 0.9238795325112869605, 1.000000000000000000, 0.9238795325112869605, 1.000000000000000000, 0.9238795325112869605, 1.000000000000000000, 0.9238795325112869605, 1.000000000000000000, 0.9238795325112869605, 1.000000000000000000, 0.9238795325112869605, 1.000000000000000000, 0.9238795325112869605, 1.000000000000000000, 0.9238795325112869605, 1.000000000000000000, 0.9238795325112869605, 1.000000000000000000, 0.9238795325112869605, 1.000000000000000000, 0.9238795325112869605, 1.000000000000000000, 0.9238795325112869605, 1.000000000000000000, 0.9238795325112869605, 1.000000000000000000, 0.9238795325112869605, 1.000000000000000000, 0.9238795325112869605, 1.000000000000000000, 0.9238795325112869605, 1.000000000000000000, 0.9238795325112869605, 1.000000000000000000, 0.9238795325112869605, 1.000000000000000000, 0.9238795325112869605, 1.000000000000000000, 0.9238795325112869605, 1.000000000000000000, 0.9238795325112869605, 1.000000000000000000, 0.9238795325112869605, 1.000000000000000000, 0.9238795325112869605, 1.000000000000000000, 0.9238795325112869605, 1.000000000000000000, 0.9238795325112869605, 1.000000000000000000, 0.9238795325112869605, 1.000000000000000000, 0.9238795325112869605, 1.000000000000000000, 0.9238795325112869605, 1.000000000000000000, 0.9238795325112869605, 1.000000000000000000, 0.9238795325112869605, 1.000000000000000000, 0.9238795325112869605, 1.000000000000000000, 0.9238795325112869605, 1.000000000000000000, 0.9238795325112869605, 1.000000000000000000, 0.9238795325112869605, 1.000000000000000000, 0.9238795325112869605, 1.000000000000000000, 0.9238795325112869605, 1.000000000000000000, 0.9238795325112869605, 1.000000000000000000, 0.9238795325112869605, 1.000000000000000000, 0.9238795325112869605, 1.000000000000000000, 0.9238795325112869605, 1.000000000000000000, 0.9238795325112869605, 1.000000000000000000, 0.9238795325112869605, 1.000000000000000000, 0.9238795325112869605, 1.000000000000000000, 0.9238795325112869605, 1.000000000000000000, 0.9238795325112869605, 1.000000000000000000, 0.9238795325112869605, 1.000000000000000000, 0.9238795325112869605, 1.000000000000000000, 0.9238795325112869605, 1.000000000000000000, 0.9238795325112869605, 1.000000000000000000, 0.9238795325112869605, 1.000000000000000000, 0.9238795325112869605, 1.000000000000000000, 0.9238795325112869605, 1.000000000000000000, 0.9238795325112869605, 1.000000000000000000, 0.9238795325112869605, 1.000000000000000000, 0.9238795325112869605, 1.000000000000000000, 0.9238795325112869605, 1.000000000000000000, 0.9238795325112869605, 1.000000000000000000, 0.9238795325112869605, 1.000000000000000000, 0.9238795325112869605, 1.000000000000000000, 0.9238795325112869605, 1.000000000000000000, 0.9238795325112869605, 1.000000000000000000, 0.9238795325112869605, 1.000000000000000000, 0.9238795325112869605, 1.000000000000000000, 0.9238795325112869605, 1.000000000000000000, 0.9238795325112869605, 1.000000000000000000, 0.9238795325112869605, 1.000000000000000000, 0.9238795325112869605, 1.000000000000000000, 0.9238795325112869605, 1.000000000000000000, 0.9238795325112869605, 1.000000000000000000, 0.9238795325112869605, 1.000000000000000000, 0.9238795325112869605, 1.000000000000000000, 0.9238795325112869605, 1.000000000000000000, 0.9238795325112869605, 1.000000000000000000, 0.9238795325112869605, 1.000000000000000000, 0.9238795325112869605, 1.000000000000000000) ) ) 
 REPRESENTATION_ITEM ( '' )  SURFACE ( )  );
#18308=EDGE_CURVE ( 'NONE', #43860, #17999, #5214, .T. ) ;
#18310=ORIENTED_EDGE ( 'NONE', *, *, #31803, .T. ) ;
#18315=CARTESIAN_POINT ( 'NONE',  ( 113.9307948109119906, 0.9020085738987339008, -11.91225656197089222 ) ) ;
#18317=CARTESIAN_POINT ( 'NONE',  ( 126.3539348109119800, -4.153390946401325223, -8.397313243818185668 ) ) ;
#18319=CARTESIAN_POINT ( 'NONE',  ( 118.2987481442453088, -7.894159318335828068, -9.358103419637847864 ) ) ;
#18322=CARTESIAN_POINT ( 'NONE',  ( 121.0216281442452981, -7.894159318335828068, -9.358103419637847864 ) ) ;
#18326=CARTESIAN_POINT ( 'NONE',  ( 116.2565881442452991, -9.261995988541697145, -16.69588392320189030 ) ) ;
#18328=CARTESIAN_POINT ( 'NONE',  ( 118.9794681442453026, -9.261995988541697145, -16.69588392320189030 ) ) ;
#18329=CARTESIAN_POINT ( 'NONE',  ( 113.9875214775786532, -0.4660016031367876232, -10.09054647747474220 ) ) ;
#18331=CARTESIAN_POINT ( 'NONE',  ( 114.6682414775786469, -1.561330072975668060, -17.79121239304076596 ) ) ;
#18332=CARTESIAN_POINT ( 'NONE',  ( 113.0798948109119948, -0.4660016031367893996, -10.09054647747474043 ) ) ;
#18341=CARTESIAN_POINT ( 'NONE',  ( 121.0783548109119749, -9.565557343593413364, -10.61323700422348004 ) ) ;
#18345=CARTESIAN_POINT ( 'NONE',  ( 126.3063647503471998, -4.505965723778011522, -8.361964086144073605 ) ) ;
#18346=CARTESIAN_POINT ( 'NONE',  ( 113.3635281442453504, -0.1624402480850797581, -16.17319339645315424 ) ) ;
#18348=ADVANCED_FACE ( 'NONE', ( #41060 ), #44831, .T. ) ;
#18349=CARTESIAN_POINT ( 'NONE',  ( 123.1772414775786189, -4.089484607189486809, -7.948022111789456723 ) ) ;
#18350=CARTESIAN_POINT ( 'NONE',  ( 119.6601881442453106, -8.166667518702819706, -8.995218007635861213 ) ) ;
#18352=EDGE_CURVE ( 'NONE', #31472, #2634, #41661, .T. ) ;
#18353=CARTESIAN_POINT ( 'NONE',  ( 118.5256548109119876, -8.899110576539710493, -16.42337572283490132 ) ) ;
#18356=CARTESIAN_POINT ( 'NONE',  ( 116.0864081442453113, -9.988377603198976828, -10.36322818467138340 ) ) ;
#18357=CARTESIAN_POINT ( 'NONE',  ( 118.5823814775786360, -7.643976991954077427, -18.09477374809248928 ) ) ;
#18359=CARTESIAN_POINT ( 'NONE',  ( 124.3117748109119844, 0.1319031606808879209, -14.10382304977623669 ) ) ;
#18361=CARTESIAN_POINT ( 'NONE',  ( 121.8725281442453223, -3.383040157471821630, -19.15922257007629170 ) ) ;
#18362=CARTESIAN_POINT ( 'NONE',  ( 137.5049267796298125, 0.06692046795779585389, -14.26109179921826531 ) ) ;
#18368=CARTESIAN_POINT ( 'NONE',  ( 126.2896895366256729, 0.1563366305949911439, -13.78536022922076754 ) ) ;
#18370=AXIS2_PLACEMENT_3D ( 'NONE', #36532, #29701, #12388 ) ;
#18371=CARTESIAN_POINT ( 'NONE',  ( 117.0507614775786465, -10.30919188438810075, -12.61870101168855918 ) ) ;
#18374=CARTESIAN_POINT ( 'NONE',  ( 117.1074881442453233, 0.4262465694468514643, -12.03445270309931736 ) ) ;
#18375=CARTESIAN_POINT ( 'NONE',  ( 126.2184548109108420, -0.8485035689962256988, -10.41384787932543610 ) ) ;
#18376=CARTESIAN_POINT ( 'NONE',  ( 117.0507614775786465, 0.1319031606808827028, -14.10382304977625445 ) ) ;
#18378=CARTESIAN_POINT ( 'NONE',  ( 112.3991748109119868, -1.833838273342658809, -17.42832698103878286 ) ) ;
#18383=CARTESIAN_POINT ( 'NONE',  ( 117.9583881442453048, -10.30919188438810075, -12.61870101168855918 ) ) ;
#18384=CARTESIAN_POINT ( 'NONE',  ( 119.0929214775786278, -4.153390946401325223, -8.397313243818185668 ) ) ;
#18385=CARTESIAN_POINT ( 'NONE',  ( 125.2761281442453054, -10.63000616557722466, -14.87417383870573495 ) ) ;
#18387=CARTESIAN_POINT ( 'NONE',  ( 137.2352176311238452, -8.690612541390031254, -9.760135143526762036 ) ) ;
#18388=CARTESIAN_POINT ( 'NONE',  ( 122.1561614775786353, -0.4660016031367893996, -10.09054647747474043 ) ) ;
#18390=CARTESIAN_POINT ( 'NONE',  ( 119.4332814775786318, -8.899110576539710493, -16.42337572283490132 ) ) ;
#18391=CARTESIAN_POINT ( 'NONE',  ( 117.3343948109119737, -6.222761293078241884, -8.102969835052219238 ) ) ;
#18394=CARTESIAN_POINT ( 'NONE',  ( 122.3830681442452857, -1.833838273342659697, -17.42832698103878286 ) ) ;
#18395=CARTESIAN_POINT ( 'NONE',  ( 125.7866681442452688, -8.899110576539710493, -16.42337572283490132 ) ) ;
#18400=( BOUNDED_CURVE ( )  B_SPLINE_CURVE ( 2, ( #6172, #20538, #34639, #37634, #6407 ),
 .UNSPECIFIED., .F., .F. ) 
 B_SPLINE_CURVE_WITH_KNOTS ( ( 3, 2, 3 ),
 ( 0.000000000000000000, 0.007812500000000000000, 0.01424533251905851956 ),
 .UNSPECIFIED. ) 
 CURVE ( )  GEOMETRIC_REPRESENTATION_ITEM ( )  RATIONAL_B_SPLINE_CURVE ( ( 1.000000000000000000, 0.9238795325112869605, 1.000000000000000000, 0.9373222120157009840, 0.9778625265000240319 ) ) 
 REPRESENTATION_ITEM ( '' )  );
#18403=CARTESIAN_POINT ( 'NONE',  ( 117.5045748109119756, 0.5811942927096110934, -14.16772938898807510 ) ) ;
#18404=CARTESIAN_POINT ( 'NONE',  ( 119.9438214775786378, -7.893985811506177619, -18.51759400769804742 ) ) ;
#18406=CARTESIAN_POINT ( 'NONE',  ( 113.0231681442453322, 0.9020085738987339008, -11.91225656197089222 ) ) ;
#18408=CARTESIAN_POINT ( 'NONE',  ( 117.2146229525735635, -1.111561923218657322, -17.14115599315433158 ) ) ;
#18410=CARTESIAN_POINT ( 'NONE',  ( 117.3911214775786505, -1.561330072975668504, -17.79121239304076951 ) ) ;
#18411=CARTESIAN_POINT ( 'NONE',  ( 120.3976348109119812, -7.643976991954077427, -18.09477374809248928 ) ) ;
#18413=CARTESIAN_POINT ( 'NONE',  ( 125.1059481442452750, -8.166667518702819706, -8.995218007635861213 ) ) ;
#18414=CARTESIAN_POINT ( 'NONE',  ( 122.2696148109119889, -4.089484607189486809, -7.948022111789456723 ) ) ;
#18418=CARTESIAN_POINT ( 'NONE',  ( 118.0151148109119816, 0.4262465694468514643, -12.03445270309931736 ) ) ;
#18424=CARTESIAN_POINT ( 'NONE',  ( 119.6034614775786196, -6.344957434206665248, -7.627207830600338134 ) ) ;
#18426=CARTESIAN_POINT ( 'NONE',  ( 125.0386814775786490, -5.568102603701690967, -18.34339073538286513 ) ) ;
#18428=CARTESIAN_POINT ( 'NONE',  ( 121.9966691406318660, 0.3208234527006321724, -15.99825685930877839 ) ) ;
#18429=CARTESIAN_POINT ( 'NONE',  ( 115.1220548109119761, -1.833838273342658809, -17.42832698103878286 ) ) ;
#18433=CARTESIAN_POINT ( 'NONE',  ( 118.8660148109119774, 0.1319031606808879209, -14.10382304977623669 ) ) ;
#18436=CARTESIAN_POINT ( 'NONE',  ( 121.4187148109119789, -3.505236298600246325, -18.68346056562440793 ) ) ;
#18439=CARTESIAN_POINT ( 'NONE',  ( 122.2128881442453263, -7.643976991954077427, -18.09477374809248928 ) ) ;
#18440=CARTESIAN_POINT ( 'NONE',  ( 112.3991748109119868, -8.166667518702817929, -8.995218007635859436 ) ) ;
#18441=CARTESIAN_POINT ( 'NONE',  ( 120.7379948109119709, -10.63000616557722466, -14.87417383870573495 ) ) ;
#18442=CARTESIAN_POINT ( 'NONE',  ( 113.4202548109119846, -10.30919188438810075, -12.61870101168855918 ) ) ;
#18444=CARTESIAN_POINT ( 'NONE',  ( 120.7947214775786193, -0.8288870151387760510, -10.36305467784173118 ) ) ;
#18446=CARTESIAN_POINT ( 'NONE',  ( 119.0929214775786278, -5.638512984488999180, -18.83840828888717311 ) ) ;
#18452=CARTESIAN_POINT ( 'NONE',  ( 124.9357681442453014, -1.834011780172310813, -8.268836392978581529 ) ) ;
#18454=CARTESIAN_POINT ( 'NONE',  ( 122.2696148109119889, -5.574606645277164318, -18.38911715685844683 ) ) ;
#18457=CARTESIAN_POINT ( 'NONE',  ( 125.7866681442452688, -0.4660016031367893996, -10.09054647747474043 ) ) ;
#18460=CARTESIAN_POINT ( 'NONE',  ( 114.9518748109119883, -1.834011780172310813, -8.268836392978581529 ) ) ;
#18461=CARTESIAN_POINT ( 'NONE',  ( 125.4463081442452932, -5.638512984488999180, -18.83840828888717311 ) ) ;
#18462=CARTESIAN_POINT ( 'NONE',  ( 120.1707281442453166, -9.565557343593413364, -10.61323700422348004 ) ) ;
#18463=CARTESIAN_POINT ( 'NONE',  ( 126.4750299824202102, -3.550610268942888670, -8.435960360623607102 ) ) ;
#18465=CARTESIAN_POINT ( 'NONE',  ( 111.6617281442453304, 0.4262465694468514643, -12.03445270309931736 ) ) ;
#18468=CARTESIAN_POINT ( 'NONE',  ( 111.8319081442453182, -5.638512984488999180, -18.83840828888717311 ) ) ;
#18473=CARTESIAN_POINT ( 'NONE',  ( 120.5110881442453206, -6.344957434206665248, -7.627207830600338134 ) ) ;
#18476=CARTESIAN_POINT ( 'NONE',  ( 121.1981266692503851, -2.311015703046761072, -18.04188382666269774 ) ) ;
#18477=CARTESIAN_POINT ( 'NONE',  ( 124.3685014775786328, -10.63000616557722466, -14.87417383870573495 ) ) ;
#18478=CARTESIAN_POINT ( 'NONE',  ( 127.0915067942438270, -4.531132641640684078, -18.81955951406810712 ) ) ;
#18479=CARTESIAN_POINT ( 'NONE',  ( 124.7655881442452852, -9.859900752359378018, -12.68260735090039759 ) ) ;
#18480=AXIS2_PLACEMENT_3D ( 'NONE', #38829, #10809, #24932 ) ;
#18482=CARTESIAN_POINT ( 'NONE',  ( 118.0151148109119816, -10.63000616557722466, -14.87417383870573495 ) ) ;
#18486=CARTESIAN_POINT ( 'NONE',  ( 112.0588148109119828, -9.859900752359374465, -12.68260735090039404 ) ) ;
#18487=CARTESIAN_POINT ( 'NONE',  ( 151.2860562277021472, -4.863998795839242995, -13.39321520033831447 ) ) ;
#18489=CARTESIAN_POINT ( 'NONE',  ( 111.4915481442453142, -1.833838273342658365, -17.42832698103878286 ) ) ;
#18490=CARTESIAN_POINT ( 'NONE',  ( 124.4252281442452812, -0.8288870151387760510, -10.36305467784173118 ) ) ;
#18492=CARTESIAN_POINT ( 'NONE',  ( 124.5954081442453116, -6.222761293078241884, -8.102969835052219238 ) ) ;
#18493=CARTESIAN_POINT ( 'NONE',  ( 112.8529881442453302, -7.894159318335828068, -9.358103419637847864 ) ) ;
#18494=CARTESIAN_POINT ( 'NONE',  ( 119.0361948109119652, -7.893985811506177619, -18.51759400769804742 ) ) ;
#18496=CARTESIAN_POINT ( 'NONE',  ( 126.4162218615820450, -8.599963967683439847, -16.86356328481144118 ) ) ;
#18500=CARTESIAN_POINT ( 'NONE',  ( 126.7702028005534061, -9.890968229443798165, -11.79150890346986280 ) ) ;
#18501=CARTESIAN_POINT ( 'NONE',  ( 115.4624148109119943, -5.638512984488999180, -18.83840828888717311 ) ) ;
#18503=CARTESIAN_POINT ( 'NONE',  ( 113.4202548109119846, 0.1319031606808879209, -14.10382304977623669 ) ) ;
#18506=CARTESIAN_POINT ( 'NONE',  ( 112.4559014775786778, -0.1624402480850797581, -16.17319339645315424 ) ) ;
#18507=CARTESIAN_POINT ( 'NONE',  ( 122.4965214775786251, 0.1319031606808862001, -14.10382304977622603 ) ) ;
#18509=CARTESIAN_POINT ( 'NONE',  ( 117.6180281442453150, -0.4660016031367893996, -10.09054647747474043 ) ) ;
#18513=CARTESIAN_POINT ( 'NONE',  ( 126.4262034847003520, -7.476899408362951860, -9.008790208301181934 ) ) ;
#18514=CARTESIAN_POINT ( 'NONE',  ( 118.0151148109119816, 0.4262465694468514643, -12.03445270309931736 ) ) ;
#18515=CARTESIAN_POINT ( 'NONE',  ( 116.3133148109119759, -7.893985811506177619, -18.51759400769804742 ) ) ;
#18518=CARTESIAN_POINT ( 'NONE',  ( 121.5888948109119809, 0.1319031606808879209, -14.10382304977623669 ) ) ;
#18519=CARTESIAN_POINT ( 'NONE',  ( 116.1431348109119881, 0.1319031606808879209, -14.10382304977623669 ) ) ;
#18523=CARTESIAN_POINT ( 'NONE',  ( 118.7525614775786380, -1.833838273342659253, -17.42832698103878286 ) ) ;
#18525=CARTESIAN_POINT ( 'NONE',  ( 127.7429221096414977, -10.18827139786943370, -15.59882366901442019 ) ) ;
#18526=CARTESIAN_POINT ( 'NONE',  ( 113.7038881442453402, -3.383040157471821630, -19.15922257007629170 ) ) ;
#18529=CARTESIAN_POINT ( 'NONE',  ( 125.7299414775786346, -10.15424416112533912, -14.75197769757731336 ) ) ;
#18532=CARTESIAN_POINT ( 'NONE',  ( 122.0994348109119443, -10.15424416112533912, -14.75197769757731336 ) ) ;
#18534=CARTESIAN_POINT ( 'NONE',  ( 117.5613014775786525, -10.15424416112533912, -14.75197769757731336 ) ) ;
#18535=CARTESIAN_POINT ( 'NONE',  ( 111.2184548109119788, -2.495269033102075262, -17.79652296963211455 ) ) ;
#18538=CARTESIAN_POINT ( 'NONE',  ( 112.1441723425591590, -8.920991669690657488, -16.34987411667529145 ) ) ;
#18541=CARTESIAN_POINT ( 'NONE',  ( 113.9875214775786532, -0.4660016031367893996, -10.09054647747474043 ) ) ;
#18542=CARTESIAN_POINT ( 'NONE',  ( 125.7866681442452688, -8.899110576539710493, -16.42337572283490132 ) ) ;
#18543=CARTESIAN_POINT ( 'NONE',  ( 119.7736414775786358, 0.1319031606808879209, -14.10382304977623669 ) ) ;
#18546=CARTESIAN_POINT ( 'NONE',  ( 120.2274548109119934, -9.859900752359374465, -12.68260735090039404 ) ) ;
#18548=DIRECTION ( 'NONE',  ( 1.000000000000000000, 0.000000000000000000, 0.000000000000000000 ) ) ;
#18551=CARTESIAN_POINT ( 'NONE',  ( 118.0151148109119816, -10.63000616557722466, -14.87417383870573495 ) ) ;
#18553=CARTESIAN_POINT ( 'NONE',  ( 117.7882081442453170, -6.344957434206665248, -7.627207830600338134 ) ) ;
#18556=CARTESIAN_POINT ( 'NONE',  ( 116.3133148109119759, -7.893985811506177619, -18.51759400769804742 ) ) ;
#18557=CARTESIAN_POINT ( 'NONE',  ( 115.8027748109119841, -0.4660016031367893996, -10.09054647747474043 ) ) ;
#18558=CARTESIAN_POINT ( 'NONE',  ( 126.3243314201118466, -9.906486255840077249, -13.06818223642682675 ) ) ;
#18562=VERTEX_POINT ( 'NONE', #16497 ) ;
#18565=CARTESIAN_POINT ( 'NONE',  ( 121.1918081442452859, -10.15424416112533912, -14.75197769757731336 ) ) ;
#18568=CARTESIAN_POINT ( 'NONE',  ( 112.8529881442453302, -7.894159318335828068, -9.358103419637847864 ) ) ;
#18569=CARTESIAN_POINT ( 'NONE',  ( 114.2144281442453178, -1.833838273342658809, -17.42832698103878286 ) ) ;
#18571=CARTESIAN_POINT ( 'NONE',  ( 122.6099748109119929, -9.261995988541697145, -16.69588392320189030 ) ) ;
#18572=CARTESIAN_POINT ( 'NONE',  ( 119.7169148109119874, -9.988377603198976828, -10.36322818467138340 ) ) ;
#18574=CARTESIAN_POINT ( 'NONE',  ( 118.7525614775786380, -1.833838273342659253, -17.42832698103878286 ) ) ;
#18576=CARTESIAN_POINT ( 'NONE',  ( 120.2274548109119934, 0.5811942927096110934, -14.16772938898807510 ) ) ;
#18577=CARTESIAN_POINT ( 'NONE',  ( 121.2485348109119769, -8.899110576539710493, -16.42337572283490132 ) ) ;
#18579=CARTESIAN_POINT ( 'NONE',  ( 123.9146881442452894, -10.15424416112533912, -14.75197769757731336 ) ) ;
#18581=CARTESIAN_POINT ( 'NONE',  ( 119.4332814775786318, -0.4660016031367893996, -10.09054647747474043 ) ) ;
#18582=CARTESIAN_POINT ( 'NONE',  ( 112.2289948109119848, -7.643976991954077427, -18.09477374809248928 ) ) ;
#18586=CARTESIAN_POINT ( 'NONE',  ( 126.5495342817341253, 0.3014387667525698089, -13.43723796351942923 ) ) ;
#18587=EDGE_CURVE ( 'NONE', #38119, #21905, #19772, .T. ) ;
#18589=CARTESIAN_POINT ( 'NONE',  ( 118.6391081442452986, -4.089484607189486809, -7.948022111789456723 ) ) ;
#18590=DIRECTION ( 'NONE',  ( 0.000000000000000000, 0.6004852223388321697, -0.7996358532186279566 ) ) ;
#18591=CARTESIAN_POINT ( 'NONE',  ( 117.5613014775786525, -10.15424416112533912, -14.75197769757731336 ) ) ;
#18592=CARTESIAN_POINT ( 'NONE',  ( 111.8886348109120092, -6.222761293078241884, -8.102969835052219238 ) ) ;
#18595=CARTESIAN_POINT ( 'NONE',  ( 115.4056881442453317, -7.893985811506194494, -18.51759400769804031 ) ) ;
#18596=CARTESIAN_POINT ( 'NONE',  ( 115.0644952477523901, -1.220279397241700758, -16.99638242193885063 ) ) ;
#18600=CARTESIAN_POINT ( 'NONE',  ( 120.6812681442452941, -10.30919188438810075, -12.61870101168855918 ) ) ;
#18601=CARTESIAN_POINT ( 'NONE',  ( 117.7882081442453170, -3.505236298600246325, -18.68346056562440793 ) ) ;
#18602=CARTESIAN_POINT ( 'NONE',  ( 114.0442481442453300, -7.643976991954077427, -18.09477374809248928 ) ) ;
#18607=CARTESIAN_POINT ( 'NONE',  ( 120.3409081442453044, -8.899110576539710493, -16.42337572283490132 ) ) ;
#18608=CARTESIAN_POINT ( 'NONE',  ( 123.1772414775786189, -5.574606645277164318, -18.38911715685844683 ) ) ;
#18609=CARTESIAN_POINT ( 'NONE',  ( 116.2565881442453133, -0.8288870151387760510, -10.36305467784173118 ) ) ;
#18613=CARTESIAN_POINT ( 'NONE',  ( 124.8223148109119762, -10.15424416112533912, -14.75197769757731336 ) ) ;
#18614=CARTESIAN_POINT ( 'NONE',  ( 124.3685014775786328, 0.4262465694468514643, -12.03445270309931736 ) ) ;
#18615=DIRECTION ( 'NONE',  ( 0.000000000000000000, 0.6004852223388321697, -0.7996358532186279566 ) ) ;
#18622=CARTESIAN_POINT ( 'NONE',  ( 117.7314814775786260, -4.089484607189486809, -7.948022111789456723 ) ) ;
#18623=CARTESIAN_POINT ( 'NONE',  ( 117.3911214775786505, -1.561330072975668504, -17.79121239304076951 ) ) ;
#18625=CARTESIAN_POINT ( 'NONE',  ( 114.1577014775786552, -6.344957434206662583, -7.627207830600332805 ) ) ;
#18632=CARTESIAN_POINT ( 'NONE',  ( 117.1642148109119859, -9.261995988541697145, -16.69588392320189030 ) ) ;
#18633=CARTESIAN_POINT ( 'NONE',  ( 122.3263414775786373, -3.505236298600246325, -18.68346056562440793 ) ) ;
#18634=CARTESIAN_POINT ( 'NONE',  ( 112.7395348109119766, -4.153390946401321671, -8.397313243818183892 ) ) ;
#18635=CARTESIAN_POINT ( 'NONE',  ( 120.3409081442453044, -0.4660016031367893996, -10.09054647747474043 ) ) ;
#18637=CARTESIAN_POINT ( 'NONE',  ( 118.1285681442453068, -2.084020599724406786, -8.691656652584148546 ) ) ;
#18640=ORIENTED_EDGE ( 'NONE', *, *, #13888, .F. ) ;
#18642=CARTESIAN_POINT ( 'NONE',  ( 119.0361948109119652, -7.893985811506177619, -18.51759400769804742 ) ) ;
#18648=CARTESIAN_POINT ( 'NONE',  ( 115.2355081442453155, 0.1319031606808879209, -14.10382304977623669 ) ) ;
#18651=CARTESIAN_POINT ( 'NONE',  ( 121.9292548109119849, -7.894159318335828068, -9.358103419637847864 ) ) ;
#18652=CARTESIAN_POINT ( 'NONE',  ( 121.2485348109119769, -0.4660016031367928413, -10.09054647747473510 ) ) ;
#18654=CARTESIAN_POINT ( 'NONE',  ( 125.7866681442452688, -8.899110576539710493, -16.42337572283490132 ) ) ;
#18658=CARTESIAN_POINT ( 'NONE',  ( 122.4965214775786251, 0.1319031606808879209, -14.10382304977623669 ) ) ;
#18659=CARTESIAN_POINT ( 'NONE',  ( 112.3424481442453384, -6.344957434206662583, -7.627207830600332805 ) ) ;
#18660=CARTESIAN_POINT ( 'NONE',  ( 118.6958348109119754, -6.344957434206665248, -7.627207830600338134 ) ) ;
#18661=CARTESIAN_POINT ( 'NONE',  ( 112.3424481442453384, -6.344957434206662583, -7.627207830600332805 ) ) ;
#18663=CARTESIAN_POINT ( 'NONE',  ( 119.7169148109119874, -0.1624402480850797581, -16.17319339645315424 ) ) ;
#18665=CARTESIAN_POINT ( 'NONE',  ( 119.3765548109119834, 0.9020085738987339008, -11.91225656197089222 ) ) ;
#18668=CARTESIAN_POINT ( 'NONE',  ( 113.7606148109119886, -7.894159318335828068, -9.358103419637847864 ) ) ;
#18671=CARTESIAN_POINT ( 'NONE',  ( 125.5030348109119558, -3.383040157471821630, -19.15922257007629170 ) ) ;
#18673=CARTESIAN_POINT ( 'NONE',  ( 121.5321681442453183, -0.1624402480850797581, -16.17319339645315424 ) ) ;
#18677=CARTESIAN_POINT ( 'NONE',  ( 111.8424481442453242, -6.210324830718715994, -8.151390318758329201 ) ) ;
#18681=CARTESIAN_POINT ( 'NONE',  ( 116.2565881442452991, -9.261995988541697145, -16.69588392320189030 ) ) ;
#18683=CARTESIAN_POINT ( 'NONE',  ( 122.4965214775786251, 0.1319031606808879209, -14.10382304977623669 ) ) ;
#18688=CARTESIAN_POINT ( 'NONE',  ( 123.7637130757767352, -0.9924539043446216624, -17.29976612834909133 ) ) ;
#18693=CARTESIAN_POINT ( 'NONE',  ( 119.3198281442452924, 0.5811942927096110934, -14.16772938898807510 ) ) ;
#18694=CARTESIAN_POINT ( 'NONE',  ( 137.1799701741892932, -8.482991601570400775, -17.29899319809113578 ) ) ;
#18696=CARTESIAN_POINT ( 'NONE',  ( 112.1155414775786454, 0.9020085738987339008, -11.91225656197089222 ) ) ;
#18697=CARTESIAN_POINT ( 'NONE',  ( 124.7655881442452852, 0.5811942927096110934, -14.16772938898807510 ) ) ;
#18698=CARTESIAN_POINT ( 'NONE',  ( 123.1205148109119563, -7.643976991954077427, -18.09477374809248928 ) ) ;
#18700=CARTESIAN_POINT ( 'NONE',  ( 116.4267681442453153, -3.383040157471821630, -19.15922257007629170 ) ) ;
#18705=CARTESIAN_POINT ( 'NONE',  ( 111.4361666677645957, -2.488018885432666139, -17.80617762523714021 ) ) ;
#18706=CARTESIAN_POINT ( 'NONE',  ( 126.1837548109119211, -10.63000616557722466, -14.87417383870573495 ) ) ;
#18710=CARTESIAN_POINT ( 'NONE',  ( 111.6617281442453304, 0.4262465694468514643, -12.03445270309931736 ) ) ;
#18711=CARTESIAN_POINT ( 'NONE',  ( 126.5808414775786446, -9.859900752359378018, -12.68260735090039759 ) ) ;
#18713=CARTESIAN_POINT ( 'NONE',  ( 123.0637881442452937, -8.899110576539710493, -16.42337572283490132 ) ) ;
#18715=CARTESIAN_POINT ( 'NONE',  ( 119.8870948109119752, -9.261995988541697145, -16.69588392320189030 ) ) ;
#18718=CARTESIAN_POINT ( 'NONE',  ( 117.4836465278262807, -1.036737761566197014, -17.24079555149560861 ) ) ;
#18723=CARTESIAN_POINT ( 'NONE',  ( 116.5969481442453031, 0.5811942927096154232, -14.16772938898807155 ) ) ;
#18725=CARTESIAN_POINT ( 'NONE',  ( 115.7460481442453357, -10.15424416112533912, -14.75197769757731336 ) ) ;
#18728=CARTESIAN_POINT ( 'NONE',  ( 126.0135748109119902, -8.166667518702819706, -8.995218007635861213 ) ) ;
#18731=CARTESIAN_POINT ( 'NONE',  ( 116.9373081442452929, -8.166667518702817929, -8.995218007635861213 ) ) ;
#18736=CARTESIAN_POINT ( 'NONE',  ( 117.2776681442452968, -4.153390946401321671, -8.397313243818183892 ) ) ;
#18737=CARTESIAN_POINT ( 'NONE',  ( 115.0653281442453277, -6.344957434206662583, -7.627207830600332805 ) ) ;
#18741=CARTESIAN_POINT ( 'NONE',  ( 125.7866681442452688, -8.899110576539710493, -16.42337572283490132 ) ) ;
#18742=CARTESIAN_POINT ( 'NONE',  ( 123.4608748109119745, 0.4262465694468514643, -12.03445270309931736 ) ) ;
#18743=CARTESIAN_POINT ( 'NONE',  ( 116.3700414775786527, -4.153390946401321671, -8.397313243818183892 ) ) ;
#18747=CARTESIAN_POINT ( 'NONE',  ( 119.3765548109119834, -10.15424416112533912, -14.75197769757731336 ) ) ;
#18750=CARTESIAN_POINT ( 'NONE',  ( 113.9875214775786532, -0.4660016031367893996, -10.09054647747474043 ) ) ;
#18753=CARTESIAN_POINT ( 'NONE',  ( 113.5337081442453240, -0.8288870151387760510, -10.36305467784173118 ) ) ;
#18755=ORIENTED_EDGE ( 'NONE', *, *, #40058, .F. ) ;
#18756=CARTESIAN_POINT ( 'NONE',  ( 122.3263414775786373, -3.505236298600246325, -18.68346056562440793 ) ) ;
#18757=CARTESIAN_POINT ( 'NONE',  ( 116.5402214775786405, -9.565557343593413364, -10.61323700422348004 ) ) ;
#18759=CARTESIAN_POINT ( 'NONE',  ( 116.2565881442453133, -0.8288870151387560670, -10.36305467784175605 ) ) ;
#18761=CYLINDRICAL_SURFACE ( 'NONE', #15005, 5.999999999999997335 ) ;
#18765=CARTESIAN_POINT ( 'NONE',  ( 116.6536748109119941, 0.9020085738987339008, -11.91225656197089222 ) ) ;
#18766=CARTESIAN_POINT ( 'NONE',  ( 112.6260814775786514, -9.261995988541697145, -16.69588392320189030 ) ) ;
#18767=CARTESIAN_POINT ( 'NONE',  ( 116.0864081442453113, -0.1624402480850797581, -16.17319339645315424 ) ) ;
#18768=CARTESIAN_POINT ( 'NONE',  ( 120.0005481442453146, -4.153390946401325223, -8.397313243818185668 ) ) ;
#18771=CARTESIAN_POINT ( 'NONE',  ( 118.8092881442453290, -0.1624402480850797581, -16.17319339645315424 ) ) ;
#18776=CARTESIAN_POINT ( 'NONE',  ( 117.1074881442453233, -10.63000616557722466, -14.87417383870573495 ) ) ;
#18778=CARTESIAN_POINT ( 'NONE',  ( 121.6456214775786293, -10.63000616557722466, -14.87417383870573495 ) ) ;
#18781=CARTESIAN_POINT ( 'NONE',  ( 116.7104014775786425, -0.4660016031367893996, -10.09054647747474043 ) ) ;
#18782=CARTESIAN_POINT ( 'NONE',  ( 116.0864081442453113, -9.988377603198976828, -10.36322818467138340 ) ) ;
#18784=CARTESIAN_POINT ( 'NONE',  ( 113.2858169107182249, -2.467220198592768199, -17.83387418641523325 ) ) ;
#18789=CARTESIAN_POINT ( 'NONE',  ( 119.9438214775786378, -2.084020599724406786, -8.691656652584148546 ) ) ;
#18793=CARTESIAN_POINT ( 'NONE',  ( 114.0442481442453300, -7.643976991954077427, -18.09477374809248928 ) ) ;
#18795=CARTESIAN_POINT ( 'NONE',  ( 112.0588148109119828, -9.859900752359374465, -12.68260735090039404 ) ) ;
#18796=CARTESIAN_POINT ( 'NONE',  ( 118.1285681442453068, -7.893985811506177619, -18.51759400769804742 ) ) ;
#18798=CARTESIAN_POINT ( 'NONE',  ( 119.6601881442453106, -1.833838273342659253, -17.42832698103878286 ) ) ;
#18799=CARTESIAN_POINT ( 'NONE',  ( 115.0653281442453277, -6.344957434206662583, -7.627207830600332805 ) ) ;
#18800=CARTESIAN_POINT ( 'NONE',  ( 122.7801548109119665, -3.383040157471821630, -19.15922257007629170 ) ) ;
#18801=CARTESIAN_POINT ( 'NONE',  ( 121.0216281442452981, -7.894159318335828068, -9.358103419637847864 ) ) ;
#18804=CARTESIAN_POINT ( 'NONE',  ( 122.0994348109119443, 0.9020085738987339008, -11.91225656197089222 ) ) ;
#18805=CARTESIAN_POINT ( 'NONE',  ( 112.4559014775786778, -0.1624402480850797581, -16.17319339645315424 ) ) ;
#18807=CARTESIAN_POINT ( 'NONE',  ( 127.7184548109119788, -3.484218720211406772, -13.98160872758045947 ) ) ;
#18809=CARTESIAN_POINT ( 'NONE',  ( 113.7414098793805408, -2.191907684172563986, -18.20049396185734025 ) ) ;
#18811=CARTESIAN_POINT ( 'NONE',  ( 116.7671281442453335, -7.643976991954077427, -18.09477374809248928 ) ) ;
#18812=CARTESIAN_POINT ( 'NONE',  ( 126.0135748109119902, -8.166667518702819706, -8.995218007635861213 ) ) ;
#18816=CARTESIAN_POINT ( 'NONE',  ( 115.1220548109119761, -1.833838273342658809, -17.42832698103878286 ) ) ;
#18820=CARTESIAN_POINT ( 'NONE',  ( 117.8449348109119938, -8.166667518702817929, -8.995218007635861213 ) ) ;
#18821=CARTESIAN_POINT ( 'NONE',  ( 123.2906948109119867, -1.833838273342659697, -17.42832698103878286 ) ) ;
#18824=CARTESIAN_POINT ( 'NONE',  ( 126.0703014775786102, -9.988377603198980381, -10.36322818467138518 ) ) ;
#18826=CARTESIAN_POINT ( 'NONE',  ( 121.0783548109119749, -9.565557343593413364, -10.61323700422348004 ) ) ;
#18827=CARTESIAN_POINT ( 'NONE',  ( 123.4608748109119745, 0.4262465694468514643, -12.03445270309931736 ) ) ;
#18828=CARTESIAN_POINT ( 'NONE',  ( 116.5969481442453031, -9.859900752359374465, -12.68260735090039404 ) ) ;
#18829=CARTESIAN_POINT ( 'NONE',  ( 119.6419022310133471, -1.244021962887374544, -16.96476564598603076 ) ) ;
#18831=CARTESIAN_POINT ( 'NONE',  ( 122.5532481442453019, 0.4262465694468514643, -12.03445270309931736 ) ) ;
#18832=CARTESIAN_POINT ( 'NONE',  ( 125.1626748109119802, -0.1624402480850797581, -16.17319339645315424 ) ) ;
#18839=CARTESIAN_POINT ( 'NONE',  ( 119.6601881442453106, -8.166667518702819706, -8.995218007635861213 ) ) ;
#18840=CARTESIAN_POINT ( 'NONE',  ( 116.7104014775786425, -0.4660016031367893996, -10.09054647747474043 ) ) ;
#18842=( BOUNDED_CURVE ( )  B_SPLINE_CURVE ( 2, ( #21194, #28719, #14577, #42625, #11387, #32784, #15706, #18677, #36216, #8639, #22539, #26418, #1335 ),
 .UNSPECIFIED., .F., .F. ) 
 B_SPLINE_CURVE_WITH_KNOTS ( ( 3, 2, 2, 2, 2, 2, 3 ),
 ( 0.2742732506792635028, 0.3750000000000000000, 0.5000000000000000000, 0.6250000000000000000, 0.7500000000000000000, 0.8750000000000000000, 0.9969031111431658765 ),
 .UNSPECIFIED. ) 
 CURVE ( )  GEOMETRIC_REPRESENTATION_ITEM ( )  RATIONAL_B_SPLINE_CURVE ( ( 0.9761776733140110629, 0.9386610620246970127, 1.000000000000000000, 0.9238795325112869605, 1.000000000000000000, 0.9238795325112869605, 1.000000000000000000, 0.9238795325112869605, 1.000000000000000000, 0.9238795325112869605, 1.000000000000000000, 0.9257654255316289937, 0.9963216603765929769 ) ) 
 REPRESENTATION_ITEM ( '' )  );
#18843=CARTESIAN_POINT ( 'NONE',  ( 113.9307948109119906, 0.9020085738987339008, -11.91225656197089222 ) ) ;
#18847=CARTESIAN_POINT ( 'NONE',  ( 115.3489614775786407, -9.261995988541697145, -16.69588392320189030 ) ) ;
#18848=CARTESIAN_POINT ( 'NONE',  ( 125.5030348109119558, -6.222761293078241884, -8.102969835052219238 ) ) ;
#18850=CARTESIAN_POINT ( 'NONE',  ( 112.6828081442453282, -2.084020599724406786, -8.691656652584148546 ) ) ;
#18851=CARTESIAN_POINT ( 'NONE',  ( 125.6164881442453094, 0.2603800115204892296, -16.42320221600525088 ) ) ;
#18854=CARTESIAN_POINT ( 'NONE',  ( 121.4754414775786131, -1.833838273342659697, -17.42832698103878286 ) ) ;
#18859=CARTESIAN_POINT ( 'NONE',  ( 120.7379948109119709, -10.63000616557722466, -14.87417383870573495 ) ) ;
#18861=CARTESIAN_POINT ( 'NONE',  ( 125.0836727849689254, -3.941856523015305314, -18.57470496855022901 ) ) ;
#18864=CARTESIAN_POINT ( 'NONE',  ( 118.6958348109119754, -3.505236298600246325, -18.68346056562440793 ) ) ;
#18868=CARTESIAN_POINT ( 'NONE',  ( 121.8158014775786171, -4.153390946401325223, -8.397313243818185668 ) ) ;
#18870=CARTESIAN_POINT ( 'NONE',  ( 121.5321681442453041, -9.988377603198957289, -10.36322818467135498 ) ) ;
#18871=CARTESIAN_POINT ( 'NONE',  ( 135.4265380376270684, -4.105408494840631306, -19.34504733371668195 ) ) ;
#18873=CARTESIAN_POINT ( 'NONE',  ( 119.3198281442452924, -9.859900752359374465, -12.68260735090039404 ) ) ;
#18874=CARTESIAN_POINT ( 'NONE',  ( 124.7088614775786226, -9.565557343593413364, -10.61323700422348004 ) ) ;
#18875=CARTESIAN_POINT ( 'NONE',  ( 118.8092881442453290, -9.988377603198976828, -10.36322818467138340 ) ) ;
#18876=CARTESIAN_POINT ( 'NONE',  ( 116.5402214775786405, 0.2603800115204892296, -16.42320221600525088 ) ) ;
#18878=CARTESIAN_POINT ( 'NONE',  ( 124.3685014775786328, 0.4262465694468514643, -12.03445270309931736 ) ) ;
#18880=CARTESIAN_POINT ( 'NONE',  ( 119.2063748109119814, -1.561330072975668504, -17.79121239304076951 ) ) ;
#18884=CARTESIAN_POINT ( 'NONE',  ( 113.1366214775786432, -7.643976991954077427, -18.09477374809248928 ) ) ;
#18887=CARTESIAN_POINT ( 'NONE',  ( 125.2761281442453054, -10.63000616557722466, -14.87417383870573495 ) ) ;
#18890=CARTESIAN_POINT ( 'NONE',  ( 125.7299414775786346, -10.15424416112533912, -14.75197769757731336 ) ) ;
#18895=EDGE_CURVE ( 'NONE', #22022, #32220, #6821, .T. ) ;
#18896=ORIENTED_EDGE ( 'NONE', *, *, #13074, .F. ) ;
#18897=CARTESIAN_POINT ( 'NONE',  ( 113.0798948109119948, -0.4660016031367893996, -10.09054647747474043 ) ) ;
#18899=CARTESIAN_POINT ( 'NONE',  ( 121.2485348109119769, -8.899110576539710493, -16.42337572283490132 ) ) ;
#18900=CARTESIAN_POINT ( 'NONE',  ( 113.3635281442453504, -0.1624402480850797581, -16.17319339645315424 ) ) ;
#18902=CARTESIAN_POINT ( 'NONE',  ( 124.1415948109119540, -6.344957434206689229, -7.627207830600343463 ) ) ;
#18904=CARTESIAN_POINT ( 'NONE',  ( 125.1059481442452750, -1.833838273342660141, -17.42832698103878286 ) ) ;
#18907=CARTESIAN_POINT ( 'NONE',  ( 123.6877814775786533, -3.383040157471821630, -19.15922257007629170 ) ) ;
#18908=CARTESIAN_POINT ( 'NONE',  ( 136.7741008876061244, -8.463785208514361003, -17.69369302188813364 ) ) ;
#18910=CARTESIAN_POINT ( 'NONE',  ( 112.7962614775786676, -3.383040157471821630, -19.15922257007629170 ) ) ;
#18911=CARTESIAN_POINT ( 'NONE',  ( 124.2550481442452792, -9.988377603198980381, -10.36322818467138518 ) ) ;
#18914=CARTESIAN_POINT ( 'NONE',  ( 125.2194014775786286, 0.1319031606808879209, -14.10382304977623669 ) ) ;
#18916=CARTESIAN_POINT ( 'NONE',  ( 117.8449348109119938, -8.166667518702817929, -8.995218007635861213 ) ) ;
#18921=CARTESIAN_POINT ( 'NONE',  ( 111.8319081442453182, -4.153390946401313677, -8.397313243818183892 ) ) ;
#18924=CARTESIAN_POINT ( 'NONE',  ( 136.7860375664303376, -5.353572327191975511, -7.813356190730346817 ) ) ;
#18925=CARTESIAN_POINT ( 'NONE',  ( 115.7460481442453357, -10.15424416112533912, -14.75197769757731336 ) ) ;
#18927=AXIS2_PLACEMENT_3D ( 'NONE', #12724, #33435, #32992 ) ;
#18929=CARTESIAN_POINT ( 'NONE',  ( 125.9001214775786224, -4.089484607189486809, -7.948022111789456723 ) ) ;
#18931=CARTESIAN_POINT ( 'NONE',  ( 125.7866681442452688, -8.899110576539710493, -16.42337572283490132 ) ) ;
#18933=CARTESIAN_POINT ( 'NONE',  ( 124.1983214775786166, -1.833838273342659697, -17.42832698103878286 ) ) ;
#18935=CARTESIAN_POINT ( 'NONE',  ( 118.4122014775786340, 0.5811942927096110934, -14.16772938898807510 ) ) ;
#18936=CARTESIAN_POINT ( 'NONE',  ( 121.4754414775786131, -8.166667518702819706, -8.995218007635861213 ) ) ;
#18941=CARTESIAN_POINT ( 'NONE',  ( 126.4750299824207502, -9.821253635553782502, -12.07982667344025884 ) ) ;
#18942=CARTESIAN_POINT ( 'NONE',  ( 115.8595014775786609, -1.834011780172310813, -8.268836392978581529 ) ) ;
#18946=CARTESIAN_POINT ( 'NONE',  ( 126.0703014775786102, -9.988377603198980381, -10.36322818467138518 ) ) ;
#18949=CARTESIAN_POINT ( 'NONE',  ( 120.7947214775786193, -9.261995988541697145, -16.69588392320189030 ) ) ;
#18953=CARTESIAN_POINT ( 'NONE',  ( 121.1350814775786233, -9.859900752359369136, -12.68260735090035318 ) ) ;
#18954=CARTESIAN_POINT ( 'NONE',  ( 120.0005481442453146, -4.153390946401325223, -8.397313243818185668 ) ) ;
#18955=CARTESIAN_POINT ( 'NONE',  ( 116.6536748109119941, 0.9020085738987339008, -11.91225656197089222 ) ) ;
#18957=CARTESIAN_POINT ( 'NONE',  ( 112.1155414775786454, 0.9020085738987339008, -11.91225656197089222 ) ) ;
#18959=CARTESIAN_POINT ( 'NONE',  ( 124.0281414775786146, -7.643976991954077427, -18.09477374809248928 ) ) ;
#18960=CARTESIAN_POINT ( 'NONE',  ( 114.3278814775786429, 0.1319031606808879209, -14.10382304977623669 ) ) ;
#18965=CARTESIAN_POINT ( 'NONE',  ( 115.9162281442453093, -5.574606645277164318, -18.38911715685844683 ) ) ;
#18969=CARTESIAN_POINT ( 'NONE',  ( 115.9729548109119861, -6.344957434206662583, -7.627207830600332805 ) ) ;
#18971=CARTESIAN_POINT ( 'NONE',  ( 113.2500748109119968, -3.505236298600246325, -18.68346056562440793 ) ) ;
#18975=CARTESIAN_POINT ( 'NONE',  ( 120.6812681442452941, 0.1319031606808879209, -14.10382304977623669 ) ) ;
#18976=CARTESIAN_POINT ( 'NONE',  ( 118.0718414775786442, -0.8288870151387760510, -10.36305467784173118 ) ) ;
#18982=CARTESIAN_POINT ( 'NONE',  ( 116.9373081442452929, -8.166667518702817929, -8.995218007635861213 ) ) ;
#18983=CARTESIAN_POINT ( 'NONE',  ( 113.7606148109119886, -1.561330072975668060, -17.79121239304076596 ) ) ;
#18984=CARTESIAN_POINT ( 'NONE',  ( 115.6893214775786447, -9.859900752359374465, -12.68260735090039404 ) ) ;
#18986=CARTESIAN_POINT ( 'NONE',  ( 119.7169148109119874, -0.1624402480850797581, -16.17319339645315424 ) ) ;
#18989=CARTESIAN_POINT ( 'NONE',  ( 120.6245414775786458, -0.1624402480850797581, -16.17319339645315424 ) ) ;
#18990=CARTESIAN_POINT ( 'NONE',  ( 125.6732148109119862, -9.859900752359378018, -12.68260735090039759 ) ) ;
#18994=CARTESIAN_POINT ( 'NONE',  ( 120.2841814775786276, 0.9020085738987339008, -11.91225656197089222 ) ) ;
#18997=CARTESIAN_POINT ( 'NONE',  ( 120.8514481442452961, -7.893985811506177619, -18.51759400769804742 ) ) ;
#19000=CARTESIAN_POINT ( 'NONE',  ( 118.0718414775786300, -9.261995988541697145, -16.69588392320189030 ) ) ;
#19001=CARTESIAN_POINT ( 'NONE',  ( 118.4122014775786340, 0.5811942927096110934, -14.16772938898807510 ) ) ;
#19007=CARTESIAN_POINT ( 'NONE',  ( 120.5110881442453206, -3.505236298600246325, -18.68346056562440793 ) ) ;
#19010=CARTESIAN_POINT ( 'NONE',  ( 113.4769814775786330, 0.4262465694468514643, -12.03445270309931736 ) ) ;
#19013=CARTESIAN_POINT ( 'NONE',  ( 111.4915481442453142, -1.833838273342658365, -17.42832698103878286 ) ) ;
#19014=CARTESIAN_POINT ( 'NONE',  ( 119.6034614775786196, -6.344957434206665248, -7.627207830600338134 ) ) ;
#19016=CARTESIAN_POINT ( 'NONE',  ( 119.1496481442453046, -6.222761293078241884, -8.102969835052219238 ) ) ;
#19017=CARTESIAN_POINT ( 'NONE',  ( 115.2355081442453155, -10.30919188438810075, -12.61870101168855918 ) ) ;
#19019=CARTESIAN_POINT ( 'NONE',  ( 120.2841814775786276, 0.9020085738987339008, -11.91225656197089222 ) ) ;
#19020=CARTESIAN_POINT ( 'NONE',  ( 121.5888948109119809, 0.1319031606808879209, -14.10382304977623669 ) ) ;
#19022=CARTESIAN_POINT ( 'NONE',  ( 124.5954081442453116, -6.222761293078241884, -8.102969835052219238 ) ) ;
#19023=EDGE_CURVE ( 'NONE', #39913, #6217, #17738, .T. ) ;
#19025=CARTESIAN_POINT ( 'NONE',  ( 120.0572748109119772, -3.383040157471821630, -19.15922257007629170 ) ) ;
#19026=CARTESIAN_POINT ( 'NONE',  ( 112.6828081442453282, -2.084020599724406786, -8.691656652584148546 ) ) ;
#19027=CARTESIAN_POINT ( 'NONE',  ( 120.6245414775786458, -9.988377603198976828, -10.36322818467138340 ) ) ;
#19030=CARTESIAN_POINT ( 'NONE',  ( 118.8886742554890787, -2.372251574601201174, -17.96033910819751611 ) ) ;
#19035=CARTESIAN_POINT ( 'NONE',  ( 119.1496481442453046, -6.222761293078241884, -8.102969835052219238 ) ) ;
#19036=CARTESIAN_POINT ( 'NONE',  ( 124.3685014775786328, -10.63000616557722466, -14.87417383870573495 ) ) ;
#19037=CARTESIAN_POINT ( 'NONE',  ( 111.9884129883171084, -8.997528177137620986, -16.20962724730194537 ) ) ;
#19039=CARTESIAN_POINT ( 'NONE',  ( 112.1243801106810167, -8.918668529216430940, -16.32041580884654053 ) ) ;
#19041=CARTESIAN_POINT ( 'NONE',  ( 116.1998614775786507, 0.4262465694468514643, -12.03445270309931736 ) ) ;
#19042=CARTESIAN_POINT ( 'NONE',  ( 113.4036376481213892, -2.395992375830784837, -17.92872468182854107 ) ) ;
#19047=CARTESIAN_POINT ( 'NONE',  ( 122.3263414775786373, -6.344957434206665248, -7.627207830600338134 ) ) ;
#19048=CARTESIAN_POINT ( 'NONE',  ( 123.1205148109119563, -7.643976991954077427, -18.09477374809248928 ) ) ;
#19053=CARTESIAN_POINT ( 'NONE',  ( 123.3474214775786209, -0.1624402480850797581, -16.17319339645315424 ) ) ;
#19054=CARTESIAN_POINT ( 'NONE',  ( 121.2485348109119769, -8.899110576539710493, -16.42337572283490132 ) ) ;
#19055=CARTESIAN_POINT ( 'NONE',  ( 116.3700414775786527, -4.153390946401321671, -8.397313243818183892 ) ) ;
#19062=EDGE_CURVE ( 'NONE', #6756, #17138, #4699, .T. ) ;
#19066=CARTESIAN_POINT ( 'NONE',  ( 122.7234281442452755, -5.638512984488999180, -18.83840828888717311 ) ) ;
#19067=CARTESIAN_POINT ( 'NONE',  ( 118.5823814775786360, -1.834011780172310813, -8.268836392978581529 ) ) ;
#19069=CARTESIAN_POINT ( 'NONE',  ( 117.5613014775786525, 0.9020085738987339008, -11.91225656197089222 ) ) ;
#19073=CARTESIAN_POINT ( 'NONE',  ( 123.2906948109119867, -8.166667518702819706, -8.995218007635861213 ) ) ;
#19074=CARTESIAN_POINT ( 'NONE',  ( 120.6245414775786458, -9.988377603198976828, -10.36322818467138340 ) ) ;
#19075=CARTESIAN_POINT ( 'NONE',  ( 125.3328548109119964, -0.8288870151387760510, -10.36305467784173118 ) ) ;
#19077=CARTESIAN_POINT ( 'NONE',  ( 112.4559014775786778, -0.1624402480850797581, -16.17319339645315424 ) ) ;
#19078=CARTESIAN_POINT ( 'NONE',  ( 112.0588148109119828, -9.859900752359374465, -12.68260735090039404 ) ) ;
#19081=CARTESIAN_POINT ( 'NONE',  ( 119.9438214775786378, -2.084020599724406786, -8.691656652584148546 ) ) ;
#19086=CARTESIAN_POINT ( 'NONE',  ( 123.6877814775786533, -3.383040157471821630, -19.15922257007629170 ) ) ;
#19091=CARTESIAN_POINT ( 'NONE',  ( 119.3198281442452924, -9.859900752359374465, -12.68260735090039404 ) ) ;
#19094=CARTESIAN_POINT ( 'NONE',  ( 123.5176014775786228, -0.8288870151387760510, -10.36305467784173118 ) ) ;
#19096=CARTESIAN_POINT ( 'NONE',  ( 125.2761281442453054, 0.4262465694468514643, -12.03445270309931736 ) ) ;
#19098=CARTESIAN_POINT ( 'NONE',  ( 123.0637881442452937, -0.4660016031367893996, -10.09054647747474043 ) ) ;
#19099=CARTESIAN_POINT ( 'NONE',  ( 119.0361948109119652, -2.084020599724406786, -8.691656652584148546 ) ) ;
#19100=CARTESIAN_POINT ( 'NONE',  ( 121.5888948109119809, 0.1319031606808879209, -14.10382304977623669 ) ) ;
#19102=CARTESIAN_POINT ( 'NONE',  ( 123.6310548109119765, -5.638512984488999180, -18.83840828888717311 ) ) ;
#19103=CARTESIAN_POINT ( 'NONE',  ( 115.6893214775786447, 0.5811942927096154232, -14.16772938898807155 ) ) ;
#19105=CARTESIAN_POINT ( 'NONE',  ( 113.3635281442453504, -9.988377603198976828, -10.36322818467138340 ) ) ;
#19107=CARTESIAN_POINT ( 'NONE',  ( 123.0637881442452937, -8.899110576539710493, -16.42337572283490132 ) ) ;
#19110=CARTESIAN_POINT ( 'NONE',  ( 120.0572748109119772, -3.383040157471821630, -19.15922257007629170 ) ) ;
#19114=CARTESIAN_POINT ( 'NONE',  ( 114.6115148109119986, -6.222761293078241884, -8.102969835052219238 ) ) ;
#19119=CARTESIAN_POINT ( 'NONE',  ( 125.8433948109119456, -7.643976991954077427, -18.09477374809248928 ) ) ;
#19127=CARTESIAN_POINT ( 'NONE',  ( 115.6893214775786447, 0.5811942927096154232, -14.16772938898807155 ) ) ;
#19129=CARTESIAN_POINT ( 'NONE',  ( 125.9001214775786224, -5.574606645277164318, -18.38911715685844683 ) ) ;
#19130=CARTESIAN_POINT ( 'NONE',  ( 113.0231681442453180, -10.15424416112533912, -14.75197769757731336 ) ) ;
#19133=CARTESIAN_POINT ( 'NONE',  ( 113.9307948109119906, 0.9020085738987339008, -11.91225656197089222 ) ) ;
#19136=CARTESIAN_POINT ( 'NONE',  ( 124.7655881442452852, 0.5811942927096110934, -14.16772938898807510 ) ) ;
#19138=ORIENTED_EDGE ( 'NONE', *, *, #35998, .F. ) ;
#19139=CARTESIAN_POINT ( 'NONE',  ( 115.4056881442453459, -7.893985811506177619, -18.51759400769804742 ) ) ;
#19140=CARTESIAN_POINT ( 'NONE',  ( 124.8790414775786246, -0.4660016031367893996, -10.09054647747474043 ) ) ;
#19142=CARTESIAN_POINT ( 'NONE',  ( 112.5693548109119888, -10.63000616557722466, -14.87417383870573495 ) ) ;
#19144=CARTESIAN_POINT ( 'NONE',  ( 117.0507614775786465, -10.30919188438810075, -12.61870101168855918 ) ) ;
#19147=CARTESIAN_POINT ( 'NONE',  ( 116.0506660444391969, -1.267766418764730840, -16.93314635290706605 ) ) ;
#19149=CARTESIAN_POINT ( 'NONE',  ( 123.6535389976226469, -4.507869723015496710, -15.11657223165913599 ) ) ;
#19150=CARTESIAN_POINT ( 'NONE',  ( 114.8951481442453115, -8.899110576539710493, -16.42337572283490132 ) ) ;
#19151=ADVANCED_FACE ( 'NONE', ( #44428 ), #5778, .T. ) ;
#19155=CARTESIAN_POINT ( 'NONE',  ( 125.8433948109119456, -1.834011780172310813, -8.268836392978581529 ) ) ;
#19156=CARTESIAN_POINT ( 'NONE',  ( 111.7184548109119788, -9.261995988541697145, -16.69588392320189030 ) ) ;
#19158=CARTESIAN_POINT ( 'NONE',  ( 122.3830681442452857, -1.833838273342659697, -17.42832698103878286 ) ) ;
#19160=CARTESIAN_POINT ( 'NONE',  ( 121.8158014775786171, -5.638512984488999180, -18.83840828888717311 ) ) ;
#19162=CARTESIAN_POINT ( 'NONE',  ( 121.4187148109119789, -6.344957434206665248, -7.627207830600338134 ) ) ;
#19164=CARTESIAN_POINT ( 'NONE',  ( 117.4103264091100840, -0.9924539043446216624, -17.29976612834909133 ) ) ;
#19165=EDGE_CURVE ( 'NONE', #21938, #4879, #10462, .T. ) ;
#19170=CARTESIAN_POINT ( 'NONE',  ( 113.9307948109119906, 0.9020085738987339008, -11.91225656197089222 ) ) ;
#19174=CARTESIAN_POINT ( 'NONE',  ( 114.7816948109119863, -9.859900752359374465, -12.68260735090039404 ) ) ;
#19175=CARTESIAN_POINT ( 'NONE',  ( 112.9903542721482950, -2.287189184988692059, -18.07361239780447448 ) ) ;
#19176=CARTESIAN_POINT ( 'NONE',  ( 120.2274548109119934, 0.5811942927096110934, -14.16772938898807510 ) ) ;
#19183=CARTESIAN_POINT ( 'NONE',  ( 117.5613014775786525, -10.15424416112533912, -14.75197769757731336 ) ) ;
#19185=CARTESIAN_POINT ( 'NONE',  ( 115.6893214775786447, 0.5811942927096154232, -14.16772938898807155 ) ) ;
#19186=CARTESIAN_POINT ( 'NONE',  ( 114.6115148109119986, -3.383040157471821630, -19.15922257007629170 ) ) ;
#19189=CARTESIAN_POINT ( 'NONE',  ( 121.7590748109119687, -2.084020599724406786, -8.691656652584148546 ) ) ;
#19190=CARTESIAN_POINT ( 'NONE',  ( 120.6812681442452941, 0.1319031606808879209, -14.10382304977623669 ) ) ;
#19196=CARTESIAN_POINT ( 'NONE',  ( 113.5337081442453240, -9.261995988541697145, -16.69588392320189030 ) ) ;
#19197=CARTESIAN_POINT ( 'NONE',  ( 118.6958348109119754, -3.505236298600246325, -18.68346056562440793 ) ) ;
#19200=CARTESIAN_POINT ( 'NONE',  ( 114.6682414775786469, -1.561330072975668060, -17.79121239304076596 ) ) ;
#19202=CARTESIAN_POINT ( 'NONE',  ( 117.3911214775786505, -7.894159318335828068, -9.358103419637847864 ) ) ;
#19203=VERTEX_POINT ( 'NONE', #26707 ) ;
#19205=CARTESIAN_POINT ( 'NONE',  ( 121.9859814775786333, -9.565557343593413364, -10.61323700422348004 ) ) ;
#19206=CARTESIAN_POINT ( 'NONE',  ( 119.6601881442453106, -1.833838273342659253, -17.42832698103878286 ) ) ;
#19213=CARTESIAN_POINT ( 'NONE',  ( 114.7249681442453237, 0.2603800115204892296, -16.42320221600525088 ) ) ;
#19214=CARTESIAN_POINT ( 'NONE',  ( 115.5758681442453053, -1.561330072975668060, -17.79121239304076951 ) ) ;
#19215=CARTESIAN_POINT ( 'NONE',  ( 114.5547881442453217, -4.153390946401321671, -8.397313243818183892 ) ) ;
#19216=CARTESIAN_POINT ( 'NONE',  ( 120.9649014775786355, -6.222761293078241884, -8.102969835052219238 ) ) ;
#19217=CARTESIAN_POINT ( 'NONE',  ( 151.2860562277021472, -4.863998795839242995, -13.39321520033831447 ) ) ;
#19219=CARTESIAN_POINT ( 'NONE',  ( 120.2841814775786276, -10.15424416112533912, -14.75197769757731336 ) ) ;
#19220=EDGE_CURVE ( 'NONE', #23072, #31245, #26947, .T. ) ;
#19224=CARTESIAN_POINT ( 'NONE',  ( 113.7798197424434363, -0.9924539043446216624, -17.29976612834909133 ) ) ;
#19226=CARTESIAN_POINT ( 'NONE',  ( 118.0718414775786300, -9.261995988541697145, -16.69588392320189030 ) ) ;
#19228=CARTESIAN_POINT ( 'NONE',  ( 121.9292548109119849, -1.561330072975668948, -17.79121239304076951 ) ) ;
#19231=CARTESIAN_POINT ( 'NONE',  ( 119.1496481442453046, -3.383040157471821630, -19.15922257007629170 ) ) ;
#19232=CARTESIAN_POINT ( 'NONE',  ( 117.1642148109119859, -9.261995988541697145, -16.69588392320189030 ) ) ;
#19238=CARTESIAN_POINT ( 'NONE',  ( 120.9649014775786355, -6.222761293078241884, -8.102969835052219238 ) ) ;
#19241=CARTESIAN_POINT ( 'NONE',  ( 116.5402214775786405, -9.565557343593413364, -10.61323700422348004 ) ) ;
#19244=CARTESIAN_POINT ( 'NONE',  ( 112.1722681442453222, -8.899110576539710493, -16.42337572283490132 ) ) ;
#19245=CARTESIAN_POINT ( 'NONE',  ( 118.4122014775786340, 0.5811942927096110934, -14.16772938898807510 ) ) ;
#19246=EDGE_LOOP ( 'NONE', ( #20854, #516, #44773, #30176 ) ) ;
#19249=CARTESIAN_POINT ( 'NONE',  ( 119.5467348109119712, -5.574606645277164318, -18.38911715685844683 ) ) ;
#19250=CARTESIAN_POINT ( 'NONE',  ( 116.1998614775786507, -10.63000616557722466, -14.87417383870573495 ) ) ;
#19252=CARTESIAN_POINT ( 'NONE',  ( 121.1918081442452859, 0.9020085738987339008, -11.91225656197089222 ) ) ;
#19253=B_SPLINE_CURVE_WITH_KNOTS ( 'NONE', 3,
 ( #15183, #22695, #19284, #33163, #39581, #1939, #15865, #43907, #9023, #22921, #5581, #30670, #9701, #17004, #34519, #27707, #44591, #5808, #37957, #37265, #26801, #41621, #30893, #37038, #16317, #37733, #41173, #12905, #6275, #2846 ),
 .UNSPECIFIED., .F., .F.,
 ( 4, 2, 2, 1, 2, 2, 2, 1, 1, 2, 2, 2, 1, 1, 1, 2, 2, 4 ),
 ( 0.000000000000000000, 0.03125000000003415324, 0.06250000000006830647, 0.09375000000010245971, 0.1093750000001204037, 0.1250000000001383338, 0.1875000000001745826, 0.2187500000001919298, 0.2343750000002013112, 0.2421875000002059741, 0.2500000000002106648, 0.3750000000002041145, 0.4375000000001891820, 0.4687500000001709743, 0.4843750000001516565, 0.4921875000001525446, 0.5000000000001534328, 1.000000000000000000 ),
 .UNSPECIFIED. ) ;
#19254=CARTESIAN_POINT ( 'NONE',  ( 121.9859814775786333, -9.565557343593413364, -10.61323700422348004 ) ) ;
#19256=EDGE_CURVE ( 'NONE', #15722, #1202, #23058, .T. ) ;
#19257=CARTESIAN_POINT ( 'NONE',  ( 124.3685014775786328, 0.4262465694468514643, -12.03445270309931736 ) ) ;
#19258=CARTESIAN_POINT ( 'NONE',  ( 123.2906948109119867, -8.166667518702819706, -8.995218007635861213 ) ) ;
#19260=CARTESIAN_POINT ( 'NONE',  ( 125.6732148109119862, 0.5811942927096110934, -14.16772938898807510 ) ) ;
#19263=CARTESIAN_POINT ( 'NONE',  ( 137.6867508019752506, -1.431738907681169959, -16.71479246807979635 ) ) ;
#19267=CARTESIAN_POINT ( 'NONE',  ( 137.1886586612148449, -9.913721899296946916, -11.71924858516633705 ) ) ;
#19268=CARTESIAN_POINT ( 'NONE',  ( 120.1140014775786398, -7.894159318335828068, -9.358103419637847864 ) ) ;
#19269=CARTESIAN_POINT ( 'NONE',  ( 125.9568481442452850, -6.344957434206665248, -7.627207830600338134 ) ) ;
#19274=CARTESIAN_POINT ( 'NONE',  ( 116.2565881442453133, -0.8288870151387760510, -10.36305467784173118 ) ) ;
#19275=VECTOR ( 'NONE', #18025, 1000.000000000000000 ) ;
#19280=CARTESIAN_POINT ( 'NONE',  ( 121.4187148109119789, -6.344957434206665248, -7.627207830600338134 ) ) ;
#19281=CARTESIAN_POINT ( 'NONE',  ( 122.6667014775786413, -2.084020599724406786, -8.691656652584148546 ) ) ;
#19284=CARTESIAN_POINT ( 'NONE',  ( 126.2202699136552866, 0.07868665426861087830, -14.15465197137595155 ) ) ;
#19287=CARTESIAN_POINT ( 'NONE',  ( 122.8936081442453059, -9.565557343593413364, -10.61323700422348004 ) ) ;
#19288=CARTESIAN_POINT ( 'NONE',  ( 120.2274548109119934, -9.859900752359378018, -12.68260735090039759 ) ) ;
#19297=CARTESIAN_POINT ( 'NONE',  ( 119.6034614775786196, -6.344957434206665248, -7.627207830600338134 ) ) ;
#19298=CARTESIAN_POINT ( 'NONE',  ( 122.2128881442453263, -1.834011780172310813, -8.268836392978581529 ) ) ;
#19300=CARTESIAN_POINT ( 'NONE',  ( 116.7671281442453335, -1.834011780172310813, -8.268836392978581529 ) ) ;
#19305=CARTESIAN_POINT ( 'NONE',  ( 121.1350814775786233, 0.5811942927096110934, -14.16772938898807510 ) ) ;
#19306=CARTESIAN_POINT ( 'NONE',  ( 119.8303681442453126, -10.63000616557722466, -14.87417383870573495 ) ) ;
#19307=EDGE_CURVE ( 'NONE', #19331, #21938, #11203, .T. ) ;
#19308=CARTESIAN_POINT ( 'NONE',  ( 126.2972081442452890, -2.084020599724406786, -8.691656652584148546 ) ) ;
#19309=CARTESIAN_POINT ( 'NONE',  ( 115.0653281442453277, -3.505236298600246325, -18.68346056562440793 ) ) ;
#19310=CARTESIAN_POINT ( 'NONE',  ( 123.8579614775786126, 0.5811942927096110934, -14.16772938898807510 ) ) ;
#19311=AXIS2_PLACEMENT_3D ( 'NONE', #38165, #45027, #20408 ) ;
#19313=CARTESIAN_POINT ( 'NONE',  ( 119.0361948109119652, -2.084020599724406786, -8.691656652584148546 ) ) ;
#19315=VERTEX_POINT ( 'NONE', #16224 ) ;
#19316=CARTESIAN_POINT ( 'NONE',  ( 123.8012348109119642, 0.2603800115204892296, -16.42320221600525088 ) ) ;
#19320=CARTESIAN_POINT ( 'NONE',  ( 118.5823814775786360, -7.643976991954077427, -18.09477374809248928 ) ) ;
#19323=CARTESIAN_POINT ( 'NONE',  ( 124.3117748109119844, 0.1319031606808879209, -14.10382304977623669 ) ) ;
#19329=CARTESIAN_POINT ( 'NONE',  ( 116.4267681442453153, -6.222761293078241884, -8.102969835052219238 ) ) ;
#19330=CARTESIAN_POINT ( 'NONE',  ( 123.2906948109119867, -1.833838273342659697, -17.42832698103878286 ) ) ;
#19331=VERTEX_POINT ( 'NONE', #39935 ) ;
#19332=CARTESIAN_POINT ( 'NONE',  ( 122.0994348109119443, 0.9020085738987339008, -11.91225656197089222 ) ) ;
#19333=CARTESIAN_POINT ( 'NONE',  ( 114.6115148109119986, -3.383040157471821630, -19.15922257007629170 ) ) ;
#19335=CARTESIAN_POINT ( 'NONE',  ( 112.2289948109119848, -7.643976991954077427, -18.09477374809248928 ) ) ;
#19337=CARTESIAN_POINT ( 'NONE',  ( 122.3830681442452857, -1.833838273342659697, -17.42832698103878286 ) ) ;
#19338=CARTESIAN_POINT ( 'NONE',  ( 123.7445081442452874, -1.561330072975668948, -17.79121239304076951 ) ) ;
#19342=CARTESIAN_POINT ( 'NONE',  ( 112.5126281442453120, 0.1319031606808879209, -14.10382304977623669 ) ) ;
#19346=CARTESIAN_POINT ( 'NONE',  ( 124.4819548109119722, -2.084020599724406786, -8.691656652584148546 ) ) ;
#19353=CARTESIAN_POINT ( 'NONE',  ( 117.5045748109119756, 0.5811942927096110934, -14.16772938898807510 ) ) ;
#19354=CARTESIAN_POINT ( 'NONE',  ( 123.0070614775786169, -10.15424416112533912, -14.75197769757731336 ) ) ;
#19355=ADVANCED_FACE ( 'NONE', ( #33066 ), #43583, .T. ) ;
#19356=CARTESIAN_POINT ( 'NONE',  ( 115.4624148109119943, -4.153390946401321671, -8.397313243818183892 ) ) ;
#19359=CARTESIAN_POINT ( 'NONE',  ( 114.6490365460471992, -2.191907684172563986, -18.20049396185734025 ) ) ;
#19360=CARTESIAN_POINT ( 'NONE',  ( 115.1787814775786387, -9.988377603198976828, -10.36322818467138340 ) ) ;
#19362=CARTESIAN_POINT ( 'NONE',  ( 123.1772414775786189, -4.089484607189486809, -7.948022111789456723 ) ) ;
#19364=CARTESIAN_POINT ( 'NONE',  ( 114.1577014775786552, -6.344957434206662583, -7.627207830600332805 ) ) ;
#19365=CARTESIAN_POINT ( 'NONE',  ( 113.9875214775786532, -8.899110576539710493, -16.42337572283490132 ) ) ;
#19367=CARTESIAN_POINT ( 'NONE',  ( 126.0703014775786102, -0.1624402480850797581, -16.17319339645315424 ) ) ;
#19369=CARTESIAN_POINT ( 'NONE',  ( 120.0572748109119772, -3.383040157471821630, -19.15922257007629170 ) ) ;
#19373=CARTESIAN_POINT ( 'NONE',  ( 151.2860562277021472, -3.484218720211406772, -13.98160872758045947 ) ) ;
#19374=CARTESIAN_POINT ( 'NONE',  ( 115.5758681442453053, -7.894159318335828068, -9.358103419637847864 ) ) ;
#19378=CARTESIAN_POINT ( 'NONE',  ( 112.8529881442453160, -7.894159318335828068, -9.358103419637847864 ) ) ;
#19379=CARTESIAN_POINT ( 'NONE',  ( 126.5241148109119393, -9.565557343593413364, -10.61323700422348004 ) ) ;
#19381=CARTESIAN_POINT ( 'NONE',  ( 125.5597614775786326, -7.894159318335828068, -9.358103419637847864 ) ) ;
#19382=CARTESIAN_POINT ( 'NONE',  ( 116.9373081442452929, -1.833838273342659253, -17.42832698103878286 ) ) ;
#19383=CARTESIAN_POINT ( 'NONE',  ( 123.8012348109119642, 0.2603800115204892296, -16.42320221600525088 ) ) ;
#19384=CARTESIAN_POINT ( 'NONE',  ( 121.1350814775786233, 0.5811942927096110934, -14.16772938898807510 ) ) ;
#19386=CARTESIAN_POINT ( 'NONE',  ( 117.6695424678160862, -1.149058757900091265, -17.09122335155388939 ) ) ;
#19391=CARTESIAN_POINT ( 'NONE',  ( 119.6601881442453106, -8.166667518702819706, -8.995218007635861213 ) ) ;
#19396=CARTESIAN_POINT ( 'NONE',  ( 114.2144281442453178, -1.833838273342658809, -17.42832698103878286 ) ) ;
#19399=CARTESIAN_POINT ( 'NONE',  ( 118.0151148109119816, -10.63000616557722466, -14.87417383870573495 ) ) ;
#19403=CARTESIAN_POINT ( 'NONE',  ( 120.9081748109119872, -4.153390946401307460, -8.397313243818183892 ) ) ;
#19404=CARTESIAN_POINT ( 'NONE',  ( 122.0427081442452817, -9.859900752359378018, -12.68260735090039759 ) ) ;
#19405=CARTESIAN_POINT ( 'NONE',  ( 118.8092881442453290, -9.988377603198976828, -10.36322818467138340 ) ) ;
#19406=CARTESIAN_POINT ( 'NONE',  ( 114.3846081442453197, 0.4262465694468514643, -12.03445270309931736 ) ) ;
#19407=CARTESIAN_POINT ( 'NONE',  ( 114.4413348109119823, -9.261995988541697145, -16.69588392320189030 ) ) ;
#19408=CARTESIAN_POINT ( 'NONE',  ( 118.6391081442452986, -5.574606645277192740, -18.38911715685844328 ) ) ;
#19409=CARTESIAN_POINT ( 'NONE',  ( 124.2550481442452792, -0.1624402480850797581, -16.17319339645315424 ) ) ;
#19410=CARTESIAN_POINT ( 'NONE',  ( 120.4543614775786295, -5.574606645277164318, -18.38911715685844683 ) ) ;
#19414=CARTESIAN_POINT ( 'NONE',  ( 114.4980614775786592, -7.893985811506177619, -18.51759400769804742 ) ) ;
#19415=CARTESIAN_POINT ( 'NONE',  ( 120.3976348109119812, -7.643976991954077427, -18.09477374809248928 ) ) ;
#19418=CARTESIAN_POINT ( 'NONE',  ( 120.0572748109119772, -3.383040157471821630, -19.15922257007629170 ) ) ;
#19420=CARTESIAN_POINT ( 'NONE',  ( 116.9373081442452929, -1.833838273342659253, -17.42832698103878286 ) ) ;
#19424=CARTESIAN_POINT ( 'NONE',  ( 123.8579614775786126, -9.859900752359378018, -12.68260735090039759 ) ) ;
#19425=CARTESIAN_POINT ( 'NONE',  ( 119.4900081442453086, -7.643976991954077427, -18.09477374809248928 ) ) ;
#19429=CARTESIAN_POINT ( 'NONE',  ( 116.6536748109119941, 0.9020085738987339008, -11.91225656197089222 ) ) ;
#19431=CARTESIAN_POINT ( 'NONE',  ( 117.5613014775786525, 0.9020085738987339008, -11.91225656197089222 ) ) ;
#19433=CARTESIAN_POINT ( 'NONE',  ( 113.7038881442453402, -3.383040157471821630, -19.15922257007629170 ) ) ;
#19434=CARTESIAN_POINT ( 'NONE',  ( 117.7882081442453170, -3.505236298600246325, -18.68346056562440793 ) ) ;
#19435=CARTESIAN_POINT ( 'NONE',  ( 121.9859814775786333, -9.565557343593413364, -10.61323700422348004 ) ) ;
#19436=CARTESIAN_POINT ( 'NONE',  ( 113.6471614775786492, -5.638512984488999180, -18.83840828888717311 ) ) ;
#19440=CARTESIAN_POINT ( 'NONE',  ( 123.0637881442452937, -8.899110576539710493, -16.42337572283490132 ) ) ;
#19441=CARTESIAN_POINT ( 'NONE',  ( 113.9762393335884383, -2.334846009198400019, -18.01015021110789149 ) ) ;
#19445=CARTESIAN_POINT ( 'NONE',  ( 118.2987481442453088, -1.561330072975668504, -17.79121239304076951 ) ) ;
#19447=CARTESIAN_POINT ( 'NONE',  ( 120.3976348109119812, -1.834011780172310813, -8.268836392978581529 ) ) ;
#19450=CARTESIAN_POINT ( 'NONE',  ( 121.2485348109119769, -0.4660016031367893996, -10.09054647747474043 ) ) ;
#19451=CARTESIAN_POINT ( 'NONE',  ( 120.5678148109119832, -8.166667518702819706, -8.995218007635861213 ) ) ;
#19458=CARTESIAN_POINT ( 'NONE',  ( 123.2906948109119867, -1.833838273342659697, -17.42832698103878286 ) ) ;
#19461=CARTESIAN_POINT ( 'NONE',  ( 119.7169148109119874, -0.1624402480850797581, -16.17319339645315424 ) ) ;
#19464=CARTESIAN_POINT ( 'NONE',  ( 114.3278814775786429, 0.1319031606808879209, -14.10382304977623669 ) ) ;
#19465=CARTESIAN_POINT ( 'NONE',  ( 123.6310548109119765, -5.638512984488999180, -18.83840828888717311 ) ) ;
#19469=CARTESIAN_POINT ( 'NONE',  ( 121.5321681442453183, -0.1624402480850797581, -16.17319339645315424 ) ) ;
#19470=CARTESIAN_POINT ( 'NONE',  ( 115.8027748109119841, -0.4660016031367893996, -10.09054647747474043 ) ) ;
#19471=CARTESIAN_POINT ( 'NONE',  ( 120.3409081442453044, -0.4660016031367893996, -10.09054647747474043 ) ) ;
#19472=CARTESIAN_POINT ( 'NONE',  ( 124.1983214775786166, -1.833838273342659697, -17.42832698103878286 ) ) ;
#19477=CARTESIAN_POINT ( 'NONE',  ( 124.0281414775786146, -1.834011780172310813, -8.268836392978581529 ) ) ;
#19480=CARTESIAN_POINT ( 'NONE',  ( 111.6050014775786536, 0.1319031606808879209, -14.10382304977623669 ) ) ;
#19483=CARTESIAN_POINT ( 'NONE',  ( 137.0982916334691026, -1.054555534231447878, -17.21706852322335379 ) ) ;
#19488=CARTESIAN_POINT ( 'NONE',  ( 118.1852948109119836, -4.153390946401325223, -8.397313243818185668 ) ) ;
#19489=CARTESIAN_POINT ( 'NONE',  ( 126.1270281442452870, -10.30919188438810075, -12.61870101168855918 ) ) ;
#19490=CARTESIAN_POINT ( 'NONE',  ( 126.6164971830670822, -6.329513783485987588, -18.38149871819503645 ) ) ;
#19496=CARTESIAN_POINT ( 'NONE',  ( 115.6893214775786447, -9.859900752359374465, -12.68260735090039404 ) ) ;
#19501=CARTESIAN_POINT ( 'NONE',  ( 121.1350814775786233, 0.5811942927096110934, -14.16772938898807510 ) ) ;
#19502=CARTESIAN_POINT ( 'NONE',  ( 123.3474214775786209, -0.1624402480850797581, -16.17319339645315424 ) ) ;
#19505=CARTESIAN_POINT ( 'NONE',  ( 125.4463081442452932, -5.638512984488999180, -18.83840828888717311 ) ) ;
#19507=B_SPLINE_CURVE_WITH_KNOTS ( 'NONE', 3,
 ( #44339, #30193, #37707, #16519, #27229, #12651, #16291, #13325, #33586, #41147 ),
 .UNSPECIFIED., .F., .F.,
 ( 4, 3, 3, 4 ),
 ( 0.000000000000000000, 0.0001671877548681284921, 0.0003343755096277714980, 0.0006463528481650629171 ),
 .UNSPECIFIED. ) ;
#19508=CARTESIAN_POINT ( 'NONE',  ( 122.2128881442453263, -7.643976991954077427, -18.09477374809248928 ) ) ;
#19509=CARTESIAN_POINT ( 'NONE',  ( 120.5678148109119832, -1.833838273342659253, -17.42832698103878286 ) ) ;
#19514=CARTESIAN_POINT ( 'NONE',  ( 112.4675314748722599, -0.1020945015694913471, -15.74893487844866691 ) ) ;
#19519=CARTESIAN_POINT ( 'NONE',  ( 120.0005481442453146, -5.638512984488999180, -18.83840828888717311 ) ) ;
#19520=CARTESIAN_POINT ( 'NONE',  ( 121.4187148109119789, -6.344957434206665248, -7.627207830600338134 ) ) ;
#19522=CARTESIAN_POINT ( 'NONE',  ( 115.2355081442453155, -10.30919188438810075, -12.61870101168855918 ) ) ;
#19523=DIRECTION ( 'NONE',  ( -1.000000000000000000, 0.000000000000000000, 0.000000000000000000 ) ) ;
#19526=CARTESIAN_POINT ( 'NONE',  ( 111.9453614775786434, -7.894159318335828068, -9.358103419637847864 ) ) ;
#19527=CARTESIAN_POINT ( 'NONE',  ( 121.0216281442452981, -1.561330072975668948, -17.79121239304076951 ) ) ;
#19528=CARTESIAN_POINT ( 'NONE',  ( 124.1415948109119540, -3.505236298600246325, -18.68346056562440793 ) ) ;
#19530=CARTESIAN_POINT ( 'NONE',  ( 113.7606148109119886, -7.894159318335828068, -9.358103419637847864 ) ) ;
#19532=CARTESIAN_POINT ( 'NONE',  ( 115.8595014775786609, -7.643976991954077427, -18.09477374809248928 ) ) ;
#19533=CARTESIAN_POINT ( 'NONE',  ( 124.7088614775786226, 0.2603800115204892296, -16.42320221600525088 ) ) ;
#19535=CARTESIAN_POINT ( 'NONE',  ( 121.1918081442452859, -10.15424416112533912, -14.75197769757731336 ) ) ;
#19541=CARTESIAN_POINT ( 'NONE',  ( 121.1918081442452859, 0.9020085738987339008, -11.91225656197089222 ) ) ;
#19546=CARTESIAN_POINT ( 'NONE',  ( 123.2339681442453241, -3.505236298600246325, -18.68346056562440793 ) ) ;
#19548=CARTESIAN_POINT ( 'NONE',  ( 123.4608748109119745, 0.4262465694468514643, -12.03445270309931736 ) ) ;
#19550=CARTESIAN_POINT ( 'NONE',  ( 126.0135748109119902, -8.166667518702819706, -8.995218007635861213 ) ) ;
#19551=CARTESIAN_POINT ( 'NONE',  ( 117.1074881442453233, 0.4262465694468514643, -12.03445270309931736 ) ) ;
#19554=CARTESIAN_POINT ( 'NONE',  ( 123.0637881442452937, -0.4660016031367893996, -10.09054647747474043 ) ) ;
#19556=CARTESIAN_POINT ( 'NONE',  ( 114.2144281442453178, -8.166667518702817929, -8.995218007635859436 ) ) ;
#19559=CARTESIAN_POINT ( 'NONE',  ( 122.5532481442453019, 0.4262465694468514643, -12.03445270309931736 ) ) ;
#19560=CARTESIAN_POINT ( 'NONE',  ( 123.4608748109119745, -10.63000616557722466, -14.87417383870573495 ) ) ;
#19564=CARTESIAN_POINT ( 'NONE',  ( 113.0231681442453180, -10.15424416112533912, -14.75197769757731336 ) ) ;
#19565=CARTESIAN_POINT ( 'NONE',  ( 117.9016614775786280, -0.1624402480850797581, -16.17319339645315424 ) ) ;
#19569=CARTESIAN_POINT ( 'NONE',  ( 125.0492214775786266, -3.505236298600246325, -18.68346056562440793 ) ) ;
#19572=EDGE_LOOP ( 'NONE', ( #1269, #37182, #28960, #13771 ) ) ;
#19576=CARTESIAN_POINT ( 'NONE',  ( 118.8092881442453290, -9.988377603198976828, -10.36322818467138340 ) ) ;
#19577=CARTESIAN_POINT ( 'NONE',  ( 124.1983214775786166, -1.833838273342659697, -17.42832698103878286 ) ) ;
#19578=CARTESIAN_POINT ( 'NONE',  ( 115.5758681442453053, -7.894159318335828068, -9.358103419637847864 ) ) ;
#19582=CARTESIAN_POINT ( 'NONE',  ( 113.4769814775786330, -10.63000616557722466, -14.87417383870573495 ) ) ;
#19584=CARTESIAN_POINT ( 'NONE',  ( 123.8012348109119642, 0.2603800115204892296, -16.42320221600525088 ) ) ;
#19587=CARTESIAN_POINT ( 'NONE',  ( 115.5191414775786569, -3.383040157471821630, -19.15922257007629170 ) ) ;
#19588=B_SPLINE_CURVE_WITH_KNOTS ( 'NONE', 3,
 ( #38395, #30677, #7167, #21078, #14467, #15142, #7851, #29048, #38848, #7388 ),
 .UNSPECIFIED., .F., .F.,
 ( 4, 3, 3, 4 ),
 ( 0.000000000000000000, 0.0001671877560958105107, 0.0003343755126086559717, 0.0006438490228507209303 ),
 .UNSPECIFIED. ) ;
#19589=CARTESIAN_POINT ( 'NONE',  ( 114.7816948109119863, -9.859900752359374465, -12.68260735090039404 ) ) ;
#19590=CARTESIAN_POINT ( 'NONE',  ( 126.8137406967727827, -4.694980012604976771, -18.68855277172357177 ) ) ;
#19591=CARTESIAN_POINT ( 'NONE',  ( 126.6942948109119840, -8.899110576539710493, -16.42337572283490132 ) ) ;
#19593=CARTESIAN_POINT ( 'NONE',  ( 121.4187148109119789, -6.344957434206665248, -7.627207830600338134 ) ) ;
#19597=CARTESIAN_POINT ( 'NONE',  ( 136.8340972670082181, -2.869431185927890038, -8.189930540114788826 ) ) ;
#19598=CARTESIAN_POINT ( 'NONE',  ( 112.4559014775786778, -0.1624402480850797581, -16.17319339645315424 ) ) ;
#19602=CARTESIAN_POINT ( 'NONE',  ( 116.8238548109119819, -5.574606645277164318, -18.38911715685844683 ) ) ;
#19603=CARTESIAN_POINT ( 'NONE',  ( 113.3635281442453504, -9.988377603198976828, -10.36322818467138340 ) ) ;
#19605=CARTESIAN_POINT ( 'NONE',  ( 113.7606148109119886, -1.561330072975668060, -17.79121239304076596 ) ) ;
#19606=CARTESIAN_POINT ( 'NONE',  ( 117.2209414775786485, -2.084020599724406786, -8.691656652584148546 ) ) ;
#19607=CARTESIAN_POINT ( 'NONE',  ( 124.8223148109119762, 0.9020085738987339008, -11.91225656197089222 ) ) ;
#19608=CARTESIAN_POINT ( 'NONE',  ( 122.3830681442452857, -8.166667518702819706, -8.995218007635861213 ) ) ;
#19610=CARTESIAN_POINT ( 'NONE',  ( 111.7751814775786556, -7.893985811506177619, -18.51759400769804742 ) ) ;
#19615=CARTESIAN_POINT ( 'NONE',  ( 119.4332814775786318, -0.4660016031367893996, -10.09054647747474043 ) ) ;
#19616=VERTEX_POINT ( 'NONE', #17349 ) ;
#19620=CARTESIAN_POINT ( 'NONE',  ( 115.8027748109119841, -8.899110576539710493, -16.42337572283490132 ) ) ;
#19622=CARTESIAN_POINT ( 'NONE',  ( 118.5256548109119876, -0.4660016031367893996, -10.09054647747474043 ) ) ;
#19627=CARTESIAN_POINT ( 'NONE',  ( 122.7801548109119665, -6.222761293078241884, -8.102969835052219238 ) ) ;
#19628=CARTESIAN_POINT ( 'NONE',  ( 118.9794681442453026, -9.261995988541697145, -16.69588392320189030 ) ) ;
#19630=CARTESIAN_POINT ( 'NONE',  ( 115.0653281442453277, -3.505236298600246325, -18.68346056562440793 ) ) ;
#19631=CARTESIAN_POINT ( 'NONE',  ( 116.6536748109119941, 0.9020085738987339008, -11.91225656197089222 ) ) ;
#19632=CARTESIAN_POINT ( 'NONE',  ( 118.0831236215688307, -1.135392229370316919, -17.10942237759952533 ) ) ;
#19633=CARTESIAN_POINT ( 'NONE',  ( 122.6667014775786413, -2.084020599724406786, -8.691656652584148546 ) ) ;
#19634=CARTESIAN_POINT ( 'NONE',  ( 119.9438214775786378, -2.084020599724406786, -8.691656652584148546 ) ) ;
#19636=CARTESIAN_POINT ( 'NONE',  ( 119.2737891406318766, 0.3208234527006367798, -15.99825685930877839 ) ) ;
#19637=CARTESIAN_POINT ( 'NONE',  ( 113.0798948109119948, -0.4660016031367893996, -10.09054647747474043 ) ) ;
#19638=CARTESIAN_POINT ( 'NONE',  ( 122.7801548109119665, -6.222761293078241884, -8.102969835052219238 ) ) ;
#19641=CARTESIAN_POINT ( 'NONE',  ( 120.3409081442453044, -0.4660016031367893996, -10.09054647747474043 ) ) ;
#19643=CARTESIAN_POINT ( 'NONE',  ( 115.4624148109119943, -4.153390946401321671, -8.397313243818183892 ) ) ;
#19647=CARTESIAN_POINT ( 'NONE',  ( 125.1059481442452750, -1.833838273342660141, -17.42832698103878286 ) ) ;
#19648=CARTESIAN_POINT ( 'NONE',  ( 121.1350814775786233, -9.859900752359378018, -12.68260735090039759 ) ) ;
#19652=CARTESIAN_POINT ( 'NONE',  ( 119.8303681442453126, -10.63000616557722466, -14.87417383870573495 ) ) ;
#19654=CARTESIAN_POINT ( 'NONE',  ( 117.7314814775786260, -4.089484607189486809, -7.948022111789456723 ) ) ;
#19655=CARTESIAN_POINT ( 'NONE',  ( 115.8027748109119841, -0.4660016031367893996, -10.09054647747474043 ) ) ;
#19656=CARTESIAN_POINT ( 'NONE',  ( 114.7249681442453237, -9.565557343593413364, -10.61323700422348004 ) ) ;
#19657=CARTESIAN_POINT ( 'NONE',  ( 124.8223148109119762, -10.15424416112533912, -14.75197769757731336 ) ) ;
#19658=CARTESIAN_POINT ( 'NONE',  ( 111.7184548109119788, -9.261995988541697145, -16.69588392320189030 ) ) ;
#19659=ORIENTED_EDGE ( 'NONE', *, *, #42306, .F. ) ;
#19660=CARTESIAN_POINT ( 'NONE',  ( 122.4397948109119767, -0.1624402480850797581, -16.17319339645315424 ) ) ;
#19661=CARTESIAN_POINT ( 'NONE',  ( 123.4041481442452834, -10.30919188438809364, -12.61870101168852187 ) ) ;
#19667=CARTESIAN_POINT ( 'NONE',  ( 121.6456214775786293, -10.63000616557722466, -14.87417383870573495 ) ) ;
#19669=CARTESIAN_POINT ( 'NONE',  ( 121.1350814775786233, 0.5811942927096110934, -14.16772938898807510 ) ) ;
#19670=CARTESIAN_POINT ( 'NONE',  ( 113.1933481442453058, -5.574606645277164318, -18.38911715685844683 ) ) ;
#19672=CARTESIAN_POINT ( 'NONE',  ( 119.0361948109119652, -7.893985811506177619, -18.51759400769804742 ) ) ;
#19673=CARTESIAN_POINT ( 'NONE',  ( 120.9649014775786355, -3.383040157471821630, -19.15922257007629170 ) ) ;
#19675=CARTESIAN_POINT ( 'NONE',  ( 122.4965214775786251, 0.1319031606808879209, -14.10382304977623669 ) ) ;
#19676=CARTESIAN_POINT ( 'NONE',  ( 115.5950730757767531, -0.9924539043446216624, -17.29976612834909133 ) ) ;
#19682=CARTESIAN_POINT ( 'NONE',  ( 124.1983214775786166, -1.833838273342659697, -17.42832698103878286 ) ) ;
#19686=CARTESIAN_POINT ( 'NONE',  ( 117.6180281442453150, -8.899110576539710493, -16.42337572283490132 ) ) ;
#19689=CARTESIAN_POINT ( 'NONE',  ( 111.9453614775786434, -7.894159318335828068, -9.358103419637847864 ) ) ;
#19690=CARTESIAN_POINT ( 'NONE',  ( 125.3328548109119964, -9.261995988541697145, -16.69588392320189030 ) ) ;
#19692=CARTESIAN_POINT ( 'NONE',  ( 122.7801548109119665, -6.222761293078241884, -8.102969835052219238 ) ) ;
#19693=CARTESIAN_POINT ( 'NONE',  ( 115.4056881442453459, -7.893985811506177619, -18.51759400769804742 ) ) ;
#19694=CARTESIAN_POINT ( 'NONE',  ( 125.2761281442453054, -10.63000616557722466, -14.87417383870573495 ) ) ;
#19695=CARTESIAN_POINT ( 'NONE',  ( 123.6877814775786533, -6.222761293078241884, -8.102969835052219238 ) ) ;
#19696=ORIENTED_EDGE ( 'NONE', *, *, #18895, .T. ) ;
#19699=CARTESIAN_POINT ( 'NONE',  ( 122.5532481442453019, -10.63000616557722466, -14.87417383870573495 ) ) ;
#19701=CARTESIAN_POINT ( 'NONE',  ( 114.7816948109119863, -9.859900752359374465, -12.68260735090039404 ) ) ;
#19702=CARTESIAN_POINT ( 'NONE',  ( 125.0492214775786266, -6.344957434206665248, -7.627207830600338134 ) ) ;
#19706=CARTESIAN_POINT ( 'NONE',  ( 137.6297597661404950, -1.384417142403913559, -16.77780847371255035 ) ) ;
#19708=VECTOR ( 'NONE', #32014, 1000.000000000000114 ) ;
#19711=CARTESIAN_POINT ( 'NONE',  ( 118.2420214775786320, -6.222761293078241884, -8.102969835052219238 ) ) ;
#19712=CARTESIAN_POINT ( 'NONE',  ( 115.5758681442453053, -7.894159318335828068, -9.358103419637847864 ) ) ;
#19713=CARTESIAN_POINT ( 'NONE',  ( 126.4750299824170554, -0.4299843489097670002, -10.81661262080413977 ) ) ;
#19714=VERTEX_POINT ( 'NONE', #34858 ) ;
#19715=CARTESIAN_POINT ( 'NONE',  ( 112.1240771095751114, -8.918610395140916580, -16.31999322929525675 ) ) ;
#19716=CARTESIAN_POINT ( 'NONE',  ( 115.2922348109119781, 0.4262465694468514643, -12.03445270309931736 ) ) ;
#19717=CARTESIAN_POINT ( 'NONE',  ( 112.5693548109119888, 0.4262465694468514643, -12.03445270309931736 ) ) ;
#19721=DIRECTION ( 'NONE',  ( 0.000000000000000000, 0.6004852223388321697, -0.7996358532186279566 ) ) ;
#19722=CARTESIAN_POINT ( 'NONE',  ( 122.3830681442452857, -8.166667518702819706, -8.995218007635861213 ) ) ;
#19723=CARTESIAN_POINT ( 'NONE',  ( 121.5321681442453183, -0.1624402480850797581, -16.17319339645315424 ) ) ;
#19725=DIRECTION ( 'NONE',  ( 1.000000000000000000, 0.000000000000000000, 0.000000000000000000 ) ) ;
#19726=DIRECTION ( 'NONE',  ( 1.000000000000000000, 0.000000000000000000, 0.000000000000000000 ) ) ;
#19729=CARTESIAN_POINT ( 'NONE',  ( 124.2550481442452792, -0.1624402480850797581, -16.17319339645315424 ) ) ;
#19730=CARTESIAN_POINT ( 'NONE',  ( 120.3976348109119812, -7.643976991954077427, -18.09477374809248928 ) ) ;
#19732=CARTESIAN_POINT ( 'NONE',  ( 119.4847958011494171, -1.149058757900107697, -17.09122335155391781 ) ) ;
#19734=CARTESIAN_POINT ( 'NONE',  ( 116.8805814775786587, -6.344957434206656366, -7.627207830600330141 ) ) ;
#19735=CARTESIAN_POINT ( 'NONE',  ( 112.2289948109119848, -7.643976991954077427, -18.09477374809248218 ) ) ;
#19737=CARTESIAN_POINT ( 'NONE',  ( 113.0231681442453180, -10.15424416112534622, -14.75197769757730448 ) ) ;
#19741=CARTESIAN_POINT ( 'NONE',  ( 120.6245414775786458, -9.988377603198976828, -10.36322818467138340 ) ) ;
#19742=CARTESIAN_POINT ( 'NONE',  ( 121.9859814775786333, 0.2603800115204892296, -16.42320221600525088 ) ) ;
#19744=CARTESIAN_POINT ( 'NONE',  ( 117.3343948109119737, -3.383040157471821630, -19.15922257007629170 ) ) ;
#19745=CARTESIAN_POINT ( 'NONE',  ( 112.8529881442453302, -1.561330072975668060, -17.79121239304076596 ) ) ;
#19747=CARTESIAN_POINT ( 'NONE',  ( 114.9518748109119883, -7.643976991954077427, -18.09477374809248928 ) ) ;
#19748=EDGE_CURVE ( 'NONE', #30875, #15493, #36932, .T. ) ;
#19749=CARTESIAN_POINT ( 'NONE',  ( 113.0231681442453180, -10.15424416112533912, -14.75197769757731336 ) ) ;
#19751=CARTESIAN_POINT ( 'NONE',  ( 120.9649014775786355, -3.383040157471821630, -19.15922257007629170 ) ) ;
#19752=CARTESIAN_POINT ( 'NONE',  ( 125.3895814775786448, -2.084020599724406786, -8.691656652584148546 ) ) ;
#19753=CARTESIAN_POINT ( 'NONE',  ( 112.3991748109119868, -1.833838273342658809, -17.42832698103878286 ) ) ;
#19757=CARTESIAN_POINT ( 'NONE',  ( 117.1642148109119859, -0.8288870151387760510, -10.36305467784173118 ) ) ;
#19758=CARTESIAN_POINT ( 'NONE',  ( 125.7299414775786346, 0.9020085738987339008, -11.91225656197089222 ) ) ;
#19762=CARTESIAN_POINT ( 'NONE',  ( 118.6958348109119754, -3.505236298600246325, -18.68346056562440793 ) ) ;
#19767=CARTESIAN_POINT ( 'NONE',  ( 123.2339681442453241, -6.344957434206665248, -7.627207830600338134 ) ) ;
#19772=( BOUNDED_CURVE ( )  B_SPLINE_CURVE ( 2, ( #30397, #22647, #1663, #40895, #12170 ),
 .UNSPECIFIED., .F., .T. ) 
 B_SPLINE_CURVE_WITH_KNOTS ( ( 3, 2, 3 ),
 ( 0.000000000000000000, 0.1250000000000000000, 0.2257267493207365250 ),
 .UNSPECIFIED. ) 
 CURVE ( )  GEOMETRIC_REPRESENTATION_ITEM ( )  RATIONAL_B_SPLINE_CURVE ( ( 1.000000000000000000, 0.9238795325112869605, 1.000000000000000000, 0.9386610620246970127, 0.9761776733140110629 ) ) 
 REPRESENTATION_ITEM ( '' )  );
#19777=CARTESIAN_POINT ( 'NONE',  ( 125.0969017241875321, -2.474500861266701435, -17.82417889551932788 ) ) ;
#19779=CARTESIAN_POINT ( 'NONE',  ( 117.6180281442453150, -8.899110576539710493, -16.42337572283490132 ) ) ;
#19782=CARTESIAN_POINT ( 'NONE',  ( 122.5532481442453019, -10.63000616557722466, -14.87417383870573495 ) ) ;
#19783=CARTESIAN_POINT ( 'NONE',  ( 115.0086014775786509, -4.089484607189486809, -7.948022111789456723 ) ) ;
#19785=CARTESIAN_POINT ( 'NONE',  ( 112.3424481442453384, -3.505236298600246325, -18.68346056562440793 ) ) ;
#19786=CARTESIAN_POINT ( 'NONE',  ( 123.8012348109119642, -9.565557343593413364, -10.61323700422348004 ) ) ;
#19787=CARTESIAN_POINT ( 'NONE',  ( 122.3830681442452857, -8.166667518702819706, -8.995218007635861213 ) ) ;
#19792=CARTESIAN_POINT ( 'NONE',  ( 118.4689281442453392, -10.15424416112533912, -14.75197769757731336 ) ) ;
#19793=CARTESIAN_POINT ( 'NONE',  ( 115.6325948109119821, -9.565557343593413364, -10.61323700422348004 ) ) ;
#19798=CARTESIAN_POINT ( 'NONE',  ( 111.7184548109119788, -9.261995988541697145, -16.69588392320189030 ) ) ;
#19802=CARTESIAN_POINT ( 'NONE',  ( 123.5967000642937421, -3.159363131617086484, -14.41422705066527854 ) ) ;
#19805=CARTESIAN_POINT ( 'NONE',  ( 119.4332814775786318, -0.4660016031367893996, -10.09054647747474043 ) ) ;
#19807=CARTESIAN_POINT ( 'NONE',  ( 123.2339681442453241, -3.505236298600246325, -18.68346056562440793 ) ) ;
#19808=CARTESIAN_POINT ( 'NONE',  ( 112.9664414775786412, -9.859900752359374465, -12.68260735090039404 ) ) ;
#19810=CARTESIAN_POINT ( 'NONE',  ( 123.5176014775786228, -9.261995988541697145, -16.69588392320189030 ) ) ;
#19811=CARTESIAN_POINT ( 'NONE',  ( 114.7816948109119863, 0.5811942927096154232, -14.16772938898807155 ) ) ;
#19815=CARTESIAN_POINT ( 'NONE',  ( 125.4463081442452932, -5.638512984488999180, -18.83840828888717311 ) ) ;
#19816=CARTESIAN_POINT ( 'NONE',  ( 151.2860562277021472, -1.889072916127989776, -18.60376373290417362 ) ) ;
#19818=ADVANCED_FACE ( 'NONE', ( #14587 ), #35199, .T. ) ;
#19819=CARTESIAN_POINT ( 'NONE',  ( 113.8740681442453138, 0.5811942927096154232, -14.16772938898807155 ) ) ;
#19820=CARTESIAN_POINT ( 'NONE',  ( 113.4202548109119846, 0.1319031606808879209, -14.10382304977623669 ) ) ;
#19822=CARTESIAN_POINT ( 'NONE',  ( 112.7395348109119766, -5.638512984488999180, -18.83840828888717311 ) ) ;
#19824=CARTESIAN_POINT ( 'NONE',  ( 121.1350814775786233, 0.5811942927096110934, -14.16772938898807510 ) ) ;
#19828=CARTESIAN_POINT ( 'NONE',  ( 114.4413348109119823, -0.8288870151387760510, -10.36305467784173118 ) ) ;
#19829=CARTESIAN_POINT ( 'NONE',  ( 123.4772435044479124, -4.053804398456810176, -15.72110060669333187 ) ) ;
#19831=CARTESIAN_POINT ( 'NONE',  ( 115.3489614775786407, -0.8288870151387760510, -10.36305467784173118 ) ) ;
#19835=CARTESIAN_POINT ( 'NONE',  ( 114.2711548109119803, -0.1624402480850797581, -16.17319339645315424 ) ) ;
#19836=CARTESIAN_POINT ( 'NONE',  ( 117.2209414775786485, -7.893985811506177619, -18.51759400769804742 ) ) ;
#19838=CARTESIAN_POINT ( 'NONE',  ( 112.3991748109119868, -8.166667518702817929, -8.995218007635859436 ) ) ;
#19839=CARTESIAN_POINT ( 'NONE',  ( 115.6325948109119821, -9.565557343593413364, -10.61323700422348004 ) ) ;
#19840=CARTESIAN_POINT ( 'NONE',  ( 124.3117748109119844, -10.30919188438810075, -12.61870101168855918 ) ) ;
#19841=CARTESIAN_POINT ( 'NONE',  ( 122.4965214775786251, -10.30919188438810075, -12.61870101168855918 ) ) ;
#19842=VERTEX_POINT ( 'NONE', #36444 ) ;
#19843=CARTESIAN_POINT ( 'NONE',  ( 111.8886348109120092, -3.383040157471821630, -19.15922257007629170 ) ) ;
#19849=CARTESIAN_POINT ( 'NONE',  ( 118.9794681442453026, -9.261995988541697145, -16.69588392320189030 ) ) ;
#19851=CARTESIAN_POINT ( 'NONE',  ( 125.6164881442453094, 0.2603800115204892296, -16.42320221600525088 ) ) ;
#19853=CARTESIAN_POINT ( 'NONE',  ( 114.2711548109119803, -0.1624402480850797581, -16.17319339645315424 ) ) ;
#19856=CARTESIAN_POINT ( 'NONE',  ( 119.7169148109119874, -9.988377603198976828, -10.36322818467138340 ) ) ;
#19858=CARTESIAN_POINT ( 'NONE',  ( 119.4219993335884311, -2.334846009198419559, -18.01015021110789505 ) ) ;
#19861=CARTESIAN_POINT ( 'NONE',  ( 122.7234281442452755, -4.153390946401325223, -8.397313243818185668 ) ) ;
#19862=CARTESIAN_POINT ( 'NONE',  ( 119.6034614775786196, -6.344957434206665248, -7.627207830600338134 ) ) ;
#19863=CARTESIAN_POINT ( 'NONE',  ( 112.2289948109119848, -7.643976991954077427, -18.09477374809248928 ) ) ;
#19864=( BOUNDED_CURVE ( )  B_SPLINE_CURVE ( 2, ( #22821, #15989, #33510, #33061, #5483, #9146, #19403, #5039, #33290, #2065, #18953, #32844, #16219, #1612, #29893, #15533, #12576 ),
 .UNSPECIFIED., .F., .F. ) 
 B_SPLINE_CURVE_WITH_KNOTS ( ( 3, 2, 2, 2, 2, 2, 2, 2, 3 ),
 ( 0.6421282416568590001, 0.6484375000000000000, 0.6562500000000000000, 0.6640625000000000000, 0.6718750000000000000, 0.6796875000000000000, 0.6875000000000000000, 0.6953125000000000000, 0.7016217583431409999 ),
 .UNSPECIFIED. ) 
 CURVE ( )  GEOMETRIC_REPRESENTATION_ITEM ( )  RATIONAL_B_SPLINE_CURVE ( ( 0.9763430640195950305, 0.9385262470928690259, 1.000000000000000000, 0.9238795325112869605, 1.000000000000000000, 0.9238795325112869605, 1.000000000000000000, 0.9238795325112869605, 1.000000000000000000, 0.9238795325112869605, 1.000000000000000000, 0.9238795325112869605, 1.000000000000000000, 0.9238795325112869605, 1.000000000000000000, 0.9385262470928680267, 0.9763430640195970289 ) ) 
 REPRESENTATION_ITEM ( '' )  );
#19865=CARTESIAN_POINT ( 'NONE',  ( 114.3278814775786429, -10.30919188438810075, -12.61870101168855918 ) ) ;
#19867=CARTESIAN_POINT ( 'NONE',  ( 126.2184548109105435, -0.8658195297460520301, -10.39078908864422246 ) ) ;
#19868=CARTESIAN_POINT ( 'NONE',  ( 119.0929214775786278, -4.153390946401325223, -8.397313243818185668 ) ) ;
#19872=CARTESIAN_POINT ( 'NONE',  ( 113.7038881442453402, -3.383040157471821630, -19.15922257007629170 ) ) ;
#19873=CARTESIAN_POINT ( 'NONE',  ( 121.4754414775786131, -1.833838273342659697, -17.42832698103878286 ) ) ;
#19876=CARTESIAN_POINT ( 'NONE',  ( 118.7525614775786380, -8.166667518702819706, -8.995218007635861213 ) ) ;
#19879=CARTESIAN_POINT ( 'NONE',  ( 117.4478481442453131, -9.565557343593413364, -10.61323700422348004 ) ) ;
#19883=CARTESIAN_POINT ( 'NONE',  ( 112.0020881442453344, 0.2603800115204892296, -16.42320221600525088 ) ) ;
#19884=CARTESIAN_POINT ( 'NONE',  ( 120.3409081442453044, -8.899110576539710493, -16.42337572283490132 ) ) ;
#19887=CARTESIAN_POINT ( 'NONE',  ( 117.3343948109119737, -3.383040157471821630, -19.15922257007629170 ) ) ;
#19889=CARTESIAN_POINT ( 'NONE',  ( 121.4754414775786131, -8.166667518702819706, -8.995218007635861213 ) ) ;
#19890=CARTESIAN_POINT ( 'NONE',  ( 113.5337081442453240, -9.261995988541697145, -16.69588392320189030 ) ) ;
#19891=CARTESIAN_POINT ( 'NONE',  ( 118.1285681442453068, -2.084020599724406786, -8.691656652584148546 ) ) ;
#19892=CARTESIAN_POINT ( 'NONE',  ( 124.1983214775786166, -1.833838273342659697, -17.42832698103878286 ) ) ;
#19895=CARTESIAN_POINT ( 'NONE',  ( 124.5386814775786206, -4.153390946401325223, -8.397313243818185668 ) ) ;
#19896=CARTESIAN_POINT ( 'NONE',  ( 123.6770938145250227, -3.807985514183269693, -19.09877912889401230 ) ) ;
#19903=CARTESIAN_POINT ( 'NONE',  ( 122.7234281442452755, -5.638512984488999180, -18.83840828888717311 ) ) ;
#19904=CARTESIAN_POINT ( 'NONE',  ( 124.7655881442452852, -9.859900752359378018, -12.68260735090039759 ) ) ;
#19906=CARTESIAN_POINT ( 'NONE',  ( 124.9357681442453014, -1.834011780172310813, -8.268836392978581529 ) ) ;
#19907=CARTESIAN_POINT ( 'NONE',  ( 113.8173414775786512, -9.565557343593413364, -10.61323700422348004 ) ) ;
#19908=CARTESIAN_POINT ( 'NONE',  ( 121.4964260444391755, -1.267766418764731728, -16.93314635290706605 ) ) ;
#19909=CARTESIAN_POINT ( 'NONE',  ( 120.3976348109119812, -1.834011780172310813, -8.268836392978581529 ) ) ;
#19910=CARTESIAN_POINT ( 'NONE',  ( 119.9438214775786378, -7.893985811506177619, -18.51759400769804742 ) ) ;
#19912=CARTESIAN_POINT ( 'NONE',  ( 124.9924948109119924, -5.574606645277164318, -18.38911715685844683 ) ) ;
#19917=CARTESIAN_POINT ( 'NONE',  ( 112.2857214775786474, -5.574606645277164318, -18.38911715685844683 ) ) ;
#19918=CARTESIAN_POINT ( 'NONE',  ( 122.7234281442452755, -4.153390946401325223, -8.397313243818185668 ) ) ;
#19921=CARTESIAN_POINT ( 'NONE',  ( 116.4834948109119779, -7.894159318335828068, -9.358103419637847864 ) ) ;
#19923=CARTESIAN_POINT ( 'NONE',  ( 117.3911214775786505, -7.894159318335828068, -9.358103419637847864 ) ) ;
#19924=CARTESIAN_POINT ( 'NONE',  ( 123.0637881442452937, -0.4660016031367893996, -10.09054647747474043 ) ) ;
#19926=CARTESIAN_POINT ( 'NONE',  ( 123.5743281442453139, -2.084020599724406786, -8.691656652584148546 ) ) ;
#19927=CARTESIAN_POINT ( 'NONE',  ( 117.5045748109119756, 0.5811942927096110934, -14.16772938898807510 ) ) ;
#19928=CARTESIAN_POINT ( 'NONE',  ( 124.0281414775786146, -1.834011780172310813, -8.268836392978581529 ) ) ;
#19930=CARTESIAN_POINT ( 'NONE',  ( 124.7655881442452852, -9.859900752359378018, -12.68260735090039759 ) ) ;
#19933=CONICAL_SURFACE ( 'NONE', #10464, 0.4999999999999999445, 0.7853981633974476129 ) ;
#19934=CARTESIAN_POINT ( 'NONE',  ( 122.7801548109119665, -3.383040157471821630, -19.15922257007629170 ) ) ;
#19935=CARTESIAN_POINT ( 'NONE',  ( 114.8951481442453115, -8.899110576539710493, -16.42337572283490132 ) ) ;
#19936=CARTESIAN_POINT ( 'NONE',  ( 111.8319081442453182, -4.153390946401321671, -8.397313243818183892 ) ) ;
#19944=CARTESIAN_POINT ( 'NONE',  ( 117.7314814775786260, -5.574606645277164318, -18.38911715685844683 ) ) ;
#19945=CARTESIAN_POINT ( 'NONE',  ( 115.2355081442453155, 0.1319031606808879209, -14.10382304977623669 ) ) ;
#19946=CARTESIAN_POINT ( 'NONE',  ( 126.7358418800189384, -6.436512518564030394, -18.41132298396161460 ) ) ;
#19949=CARTESIAN_POINT ( 'NONE',  ( 118.2420214775786320, -6.222761293078241884, -8.102969835052219238 ) ) ;
#19950=CARTESIAN_POINT ( 'NONE',  ( 113.5337081442453240, -0.8288870151387760510, -10.36305467784173118 ) ) ;
#19952=CARTESIAN_POINT ( 'NONE',  ( 111.4453614775786434, -1.861572684145083256, -17.39139446643145348 ) ) ;
#19954=CARTESIAN_POINT ( 'NONE',  ( 122.4965214775786251, -10.30919188438810075, -12.61870101168855918 ) ) ;
#19955=CARTESIAN_POINT ( 'NONE',  ( 126.4673881442452910, -7.894159318335828068, -9.358103419637847864 ) ) ;
#19957=CARTESIAN_POINT ( 'NONE',  ( 151.2860562277021472, -4.863998795839242995, -13.39321520033831447 ) ) ;
#19960=CARTESIAN_POINT ( 'NONE',  ( 124.1983214775786166, -1.833838273342659697, -17.42832698103878286 ) ) ;
#19961=CARTESIAN_POINT ( 'NONE',  ( 118.6391081442452986, -5.574606645277164318, -18.38911715685844683 ) ) ;
#19967=CARTESIAN_POINT ( 'NONE',  ( 114.7816948109119863, -9.859900752359374465, -12.68260735090039404 ) ) ;
#19972=CARTESIAN_POINT ( 'NONE',  ( 122.1561614775786353, -0.4660016031367893996, -10.09054647747474043 ) ) ;
#19974=CARTESIAN_POINT ( 'NONE',  ( 120.7379948109119709, -10.63000616557722466, -14.87417383870573495 ) ) ;
#19975=CARTESIAN_POINT ( 'NONE',  ( 112.9664414775786412, 0.5811942927096154232, -14.16772938898807155 ) ) ;
#19976=ORIENTED_EDGE ( 'NONE', *, *, #29317, .F. ) ;
#19977=CARTESIAN_POINT ( 'NONE',  ( 112.6260814775786514, -0.8288870151387760510, -10.36305467784173118 ) ) ;
#19978=CARTESIAN_POINT ( 'NONE',  ( 112.7395348109119766, -4.153390946401321671, -8.397313243818183892 ) ) ;
#19979=CARTESIAN_POINT ( 'NONE',  ( 122.7801548109119665, -3.383040157471821630, -19.15922257007629170 ) ) ;
#19980=CARTESIAN_POINT ( 'NONE',  ( 115.2922348109119781, -10.63000616557722466, -14.87417383870573495 ) ) ;
#19981=CARTESIAN_POINT ( 'NONE',  ( 113.0231681442453180, -10.15424416112533912, -14.75197769757731336 ) ) ;
#19982=ORIENTED_EDGE ( 'NONE', *, *, #26825, .T. ) ;
#19983=CARTESIAN_POINT ( 'NONE',  ( 118.4122014775786340, -9.859900752359374465, -12.68260735090039404 ) ) ;
#19984=CARTESIAN_POINT ( 'NONE',  ( 115.8027748109119841, -8.899110576539710493, -16.42337572283490132 ) ) ;
#19989=CARTESIAN_POINT ( 'NONE',  ( 122.5532481442453019, 0.4262465694468514643, -12.03445270309931736 ) ) ;
#19991=CARTESIAN_POINT ( 'NONE',  ( 124.2166073908105801, -2.443475742715335741, -17.86549347949429389 ) ) ;
#19997=CARTESIAN_POINT ( 'NONE',  ( 125.1626748109119802, -9.988377603198980381, -10.36322818467138518 ) ) ;
#19999=CARTESIAN_POINT ( 'NONE',  ( 112.4559014775786494, -9.988377603198976828, -10.36322818467138340 ) ) ;
#20004=CARTESIAN_POINT ( 'NONE',  ( 137.5146286042878785, -5.394418022101637789, -18.36369670353648687 ) ) ;
#20005=DIRECTION ( 'NONE',  ( 1.000000000000000000, 0.000000000000000000, 0.000000000000000000 ) ) ;
#20006=CARTESIAN_POINT ( 'NONE',  ( 125.7299414775786346, 0.9020085738987339008, -11.91225656197089222 ) ) ;
#20007=CARTESIAN_POINT ( 'NONE',  ( 120.0005481442453146, -4.153390946401325223, -8.397313243818185668 ) ) ;
#20008=CARTESIAN_POINT ( 'NONE',  ( 138.2184548109119930, 0.8652765085452543969, -12.77968882490997338 ) ) ;
#20011=CARTESIAN_POINT ( 'NONE',  ( 122.7801548109119665, -3.383040157471821630, -19.15922257007629170 ) ) ;
#20012=CARTESIAN_POINT ( 'NONE',  ( 120.7947214775786193, -9.261995988541697145, -16.69588392320189030 ) ) ;
#20013=CARTESIAN_POINT ( 'NONE',  ( 125.6732148109119862, 0.5811942927096110934, -14.16772938898807510 ) ) ;
#20014=CARTESIAN_POINT ( 'NONE',  ( 113.3635281442453504, -0.1624402480850797581, -16.17319339645315424 ) ) ;
#20017=CARTESIAN_POINT ( 'NONE',  ( 114.1577014775786552, -6.344957434206662583, -7.627207830600332805 ) ) ;
#20018=CARTESIAN_POINT ( 'NONE',  ( 124.3117748109119844, -10.30919188438810075, -12.61870101168855918 ) ) ;
#20023=CARTESIAN_POINT ( 'NONE',  ( 116.9940348109119839, -0.1624402480850797581, -16.17319339645315424 ) ) ;
#20024=CARTESIAN_POINT ( 'NONE',  ( 118.1852948109119836, -4.153390946401325223, -8.397313243818185668 ) ) ;
#20029=CARTESIAN_POINT ( 'NONE',  ( 115.0086014775786509, -4.089484607189486809, -7.948022111789456723 ) ) ;
#20030=CARTESIAN_POINT ( 'NONE',  ( 123.0133800025837019, -2.311015703046761072, -18.04188382666269774 ) ) ;
#20034=CARTESIAN_POINT ( 'NONE',  ( 123.2184548109119788, -2.211393927326563702, -15.67656524173425758 ) ) ;
#20038=CARTESIAN_POINT ( 'NONE',  ( 117.2776681442452968, -5.638512984488999180, -18.83840828888717311 ) ) ;
#20039=CARTESIAN_POINT ( 'NONE',  ( 126.1270281442452870, 0.1319031606808879209, -14.10382304977623669 ) ) ;
#20040=CARTESIAN_POINT ( 'NONE',  ( 117.8449348109119938, -1.833838273342659253, -17.42832698103878286 ) ) ;
#20043=CARTESIAN_POINT ( 'NONE',  ( 120.7947214775786193, -9.261995988541697145, -16.69588392320189030 ) ) ;
#20044=CARTESIAN_POINT ( 'NONE',  ( 113.1933481442453058, -4.089484607189486809, -7.948022111789456723 ) ) ;
#20047=CARTESIAN_POINT ( 'NONE',  ( 126.0703014775786102, -9.988377603198980381, -10.36322818467138518 ) ) ;
#20050=CARTESIAN_POINT ( 'NONE',  ( 116.4834948109119779, -1.561330072975668504, -17.79121239304076951 ) ) ;
#20052=CARTESIAN_POINT ( 'NONE',  ( 114.9518748109119883, -7.643976991954077427, -18.09477374809248928 ) ) ;
#20053=CARTESIAN_POINT ( 'NONE',  ( 126.3444272079631503, -5.154307014690458821, -18.44796746967900702 ) ) ;
#20055=CARTESIAN_POINT ( 'NONE',  ( 113.2500748109119968, -6.344957434206662583, -7.627207830600332805 ) ) ;
#20058=CARTESIAN_POINT ( 'NONE',  ( 121.7590748109119687, -7.893985811506177619, -18.51759400769804742 ) ) ;
#20060=CARTESIAN_POINT ( 'NONE',  ( 113.3068014775786594, -1.833838273342658809, -17.42832698103878286 ) ) ;
#20063=CARTESIAN_POINT ( 'NONE',  ( 117.2209414775786485, -2.084020599724406786, -8.691656652584148546 ) ) ;
#20064=CARTESIAN_POINT ( 'NONE',  ( 112.8337832127138682, -2.191907684172563986, -18.20049396185734025 ) ) ;
#20065=CARTESIAN_POINT ( 'NONE',  ( 116.8805814775786445, -3.505236298600246325, -18.68346056562440793 ) ) ;
#20067=CARTESIAN_POINT ( 'NONE',  ( 116.5402214775786405, -9.565557343593413364, -10.61323700422348004 ) ) ;
#20068=CARTESIAN_POINT ( 'NONE',  ( 116.8238548109119819, -4.089484607189486809, -7.948022111789456723 ) ) ;
#20070=CARTESIAN_POINT ( 'NONE',  ( 125.4463081442452932, -4.153390946401325223, -8.397313243818185668 ) ) ;
#20071=CARTESIAN_POINT ( 'NONE',  ( 116.1998614775786507, 0.4262465694468514643, -12.03445270309931736 ) ) ;
#20072=CARTESIAN_POINT ( 'NONE',  ( 122.5532481442453019, -10.63000616557722466, -14.87417383870573495 ) ) ;
#20074=CARTESIAN_POINT ( 'NONE',  ( 116.8238548109119819, -5.574606645277164318, -18.38911715685844683 ) ) ;
#20076=CARTESIAN_POINT ( 'NONE',  ( 113.6471614775786492, -5.638512984488999180, -18.83840828888717311 ) ) ;
#20081=CARTESIAN_POINT ( 'NONE',  ( 117.5613014775786525, 0.9020085738987339008, -11.91225656197089222 ) ) ;
#20085=EDGE_CURVE ( 'NONE', #35601, #1558, #22067, .T. ) ;
#20086=CARTESIAN_POINT ( 'NONE',  ( 113.7038881442453402, -6.222761293078241884, -8.102969835052219238 ) ) ;
#20088=CARTESIAN_POINT ( 'NONE',  ( 123.4608748109119745, -10.63000616557722466, -14.87417383870573495 ) ) ;
#20093=CARTESIAN_POINT ( 'NONE',  ( 112.1722681442453222, -0.4660016031367893996, -10.09054647747474043 ) ) ;
#20094=CARTESIAN_POINT ( 'NONE',  ( 123.7445081442452874, -7.894159318335828068, -9.358103419637847864 ) ) ;
#20095=CARTESIAN_POINT ( 'NONE',  ( 119.5467348109119712, -4.089484607189486809, -7.948022111789456723 ) ) ;
#20096=CARTESIAN_POINT ( 'NONE',  ( 113.6471614775786492, -4.153390946401321671, -8.397313243818183892 ) ) ;
#20097=CARTESIAN_POINT ( 'NONE',  ( 116.4834948109119779, -1.561330072975668504, -17.79121239304076951 ) ) ;
#20099=CARTESIAN_POINT ( 'NONE',  ( 126.5125895482200917, -1.167437683881369814, -9.811629287901746821 ) ) ;
#20100=CARTESIAN_POINT ( 'NONE',  ( 119.6034614775786196, -3.505236298600246325, -18.68346056562440793 ) ) ;
#20103=CARTESIAN_POINT ( 'NONE',  ( 119.4900081442453086, -1.834011780172310591, -8.268836392978581529 ) ) ;
#20104=CARTESIAN_POINT ( 'NONE',  ( 111.9453614775786434, -1.561330072975668060, -17.79121239304076596 ) ) ;
#20105=CARTESIAN_POINT ( 'NONE',  ( 121.5888948109119809, 0.1319031606808879209, -14.10382304977623669 ) ) ;
#20106=EDGE_LOOP ( 'NONE', ( #18208, #38860, #18896, #44708 ) ) ;
#20108=CARTESIAN_POINT ( 'NONE',  ( 137.3527759848259961, -0.3567832970757958688, -10.86681561206427027 ) ) ;
#20109=CARTESIAN_POINT ( 'NONE',  ( 118.2420214775786320, -3.383040157471821630, -19.15922257007629170 ) ) ;
#20111=CARTESIAN_POINT ( 'NONE',  ( 114.6115148109119986, -6.222761293078241884, -8.102969835052219238 ) ) ;
#20114=CARTESIAN_POINT ( 'NONE',  ( 126.2404814775786264, -0.8288870151387760510, -10.36305467784173118 ) ) ;
#20116=CARTESIAN_POINT ( 'NONE',  ( 122.4397948109119767, -0.1624402480850797581, -16.17319339645315424 ) ) ;
#20120=CARTESIAN_POINT ( 'NONE',  ( 121.0783548109119749, 0.2603800115204892296, -16.42320221600525088 ) ) ;
#20122=CARTESIAN_POINT ( 'NONE',  ( 112.1722681442453222, -8.899110576539710493, -16.42337572283490132 ) ) ;
#20123=CARTESIAN_POINT ( 'NONE',  ( 120.4543614775786295, -4.089484607189486809, -7.948022111789456723 ) ) ;
#20124=CARTESIAN_POINT ( 'NONE',  ( 119.1496481442453046, -3.383040157471821630, -19.15922257007629170 ) ) ;
#20125=CARTESIAN_POINT ( 'NONE',  ( 119.6034614775786196, -3.505236298600246325, -18.68346056562440793 ) ) ;
#20126=CARTESIAN_POINT ( 'NONE',  ( 124.1415948109119540, -3.505236298600246325, -18.68346056562440793 ) ) ;
#20127=CARTESIAN_POINT ( 'NONE',  ( 112.4559014775786494, -9.988377603198976828, -10.36322818467138340 ) ) ;
#20128=ORIENTED_EDGE ( 'NONE', *, *, #1616, .F. ) ;
#20130=CARTESIAN_POINT ( 'NONE',  ( 124.2550481442452792, -0.1624402480850797581, -16.17319339645315424 ) ) ;
#20131=DIRECTION ( 'NONE',  ( 1.000000000000000000, 0.000000000000000000, 0.000000000000000000 ) ) ;
#20136=B_SPLINE_CURVE_WITH_KNOTS ( 'NONE', 3,
 ( #9777, #20263, #9544, #6349, #41023, #44213, #37108, #13201, #23692, #16164 ),
 .UNSPECIFIED., .F., .F.,
 ( 4, 3, 3, 4 ),
 ( 0.000000000000000000, 1.701546542442319959E-05, 3.403093084891929823E-05, 6.554879158867139171E-05 ),
 .UNSPECIFIED. ) ;
#20137=CARTESIAN_POINT ( 'NONE',  ( 120.9081748109119872, -5.638512984488999180, -18.83840828888717311 ) ) ;
#20138=CARTESIAN_POINT ( 'NONE',  ( 121.3052614775786111, -7.643976991954077427, -18.09477374809248928 ) ) ;
#20141=CARTESIAN_POINT ( 'NONE',  ( 124.0848681442452772, -4.089484607189486809, -7.948022111789456723 ) ) ;
#20142=CARTESIAN_POINT ( 'NONE',  ( 114.0442481442453300, -7.643976991954077427, -18.09477374809248928 ) ) ;
#20145=CARTESIAN_POINT ( 'NONE',  ( 118.8092881442453290, -9.988377603198976828, -10.36322818467138340 ) ) ;
#20146=CARTESIAN_POINT ( 'NONE',  ( 123.0070614775786169, 0.9020085738987339008, -11.91225656197089222 ) ) ;
#20148=CARTESIAN_POINT ( 'NONE',  ( 114.2144281442453178, -8.166667518702817929, -8.995218007635859436 ) ) ;
#20152=CARTESIAN_POINT ( 'NONE',  ( 112.6828081442453282, -2.084020599724406786, -8.691656652584148546 ) ) ;
#20153=CARTESIAN_POINT ( 'NONE',  ( 125.1059481442452750, -1.833838273342660141, -17.42832698103878286 ) ) ;
#20157=CARTESIAN_POINT ( 'NONE',  ( 119.0929214775786278, -4.153390946401325223, -8.397313243818185668 ) ) ;
#20159=CARTESIAN_POINT ( 'NONE',  ( 117.9583881442453048, 0.1319031606808879209, -14.10382304977623669 ) ) ;
#20160=CARTESIAN_POINT ( 'NONE',  ( 124.3685014775786328, -10.63000616557722466, -14.87417383870573495 ) ) ;
#20163=CARTESIAN_POINT ( 'NONE',  ( 120.6245414775786458, -0.1624402480850797581, -16.17319339645315424 ) ) ;
#20164=CARTESIAN_POINT ( 'NONE',  ( 119.9438214775786378, -7.893985811506177619, -18.51759400769804742 ) ) ;
#20165=CARTESIAN_POINT ( 'NONE',  ( 123.5176014775786228, -9.261995988541697145, -16.69588392320189030 ) ) ;
#20166=CARTESIAN_POINT ( 'NONE',  ( 125.1059481442452750, -1.833838273342660141, -17.42832698103878286 ) ) ;
#20167=ORIENTED_EDGE ( 'NONE', *, *, #30914, .F. ) ;
#20170=CARTESIAN_POINT ( 'NONE',  ( 123.9714148109119805, -0.4660016031367893996, -10.09054647747474043 ) ) ;
#20171=CARTESIAN_POINT ( 'NONE',  ( 116.4267681442453153, -6.222761293078241884, -8.102969835052219238 ) ) ;
#20172=CARTESIAN_POINT ( 'NONE',  ( 124.5954081442453116, -3.383040157471821630, -19.15922257007629170 ) ) ;
#20173=DIRECTION ( 'NONE',  ( 0.000000000000000000, 0.6004852223388321697, -0.7996358532186279566 ) ) ;
#20179=CARTESIAN_POINT ( 'NONE',  ( 118.0203271540078589, -2.348512537728064675, -17.99195118506216318 ) ) ;
#20180=CARTESIAN_POINT ( 'NONE',  ( 123.2339681442453241, -3.505236298600246325, -18.68346056562440793 ) ) ;
#20181=CARTESIAN_POINT ( 'NONE',  ( 113.4769814775786330, 0.4262465694468514643, -12.03445270309931736 ) ) ;
#20182=CARTESIAN_POINT ( 'NONE',  ( 126.7706290066808492, -6.465199847775628506, -18.42047446121263121 ) ) ;
#20183=ORIENTED_EDGE ( 'NONE', *, *, #15264, .T. ) ;
#20185=CARTESIAN_POINT ( 'NONE',  ( 118.4689281442453392, -10.15424416112533912, -14.75197769757731336 ) ) ;
#20186=CARTESIAN_POINT ( 'NONE',  ( 114.1009748109119784, -5.574606645277164318, -18.38911715685844683 ) ) ;
#20187=CARTESIAN_POINT ( 'NONE',  ( 122.3620835773848654, -2.467220198592778413, -17.83387418641524391 ) ) ;
#20191=ADVANCED_FACE ( 'NONE', ( #23465 ), #3379, .T. ) ;
#20192=CARTESIAN_POINT ( 'NONE',  ( 126.6942948109119840, -8.899110576539710493, -16.42337572283490132 ) ) ;
#20193=VERTEX_POINT ( 'NONE', #9783 ) ;
#20194=CARTESIAN_POINT ( 'NONE',  ( 112.3424481442453384, -6.344957434206662583, -7.627207830600332805 ) ) ;
#20197=CARTESIAN_POINT ( 'NONE',  ( 123.9714148109119805, -8.899110576539710493, -16.42337572283490132 ) ) ;
#20198=CARTESIAN_POINT ( 'NONE',  ( 119.0361948109119652, -2.084020599724406786, -8.691656652584148546 ) ) ;
#20203=CARTESIAN_POINT ( 'NONE',  ( 112.2857214775786474, -5.574606645277164318, -18.38911715685844683 ) ) ;
#20207=CARTESIAN_POINT ( 'NONE',  ( 125.6164881442453094, 0.2603800115204892296, -16.42320221600525088 ) ) ;
#20208=CARTESIAN_POINT ( 'NONE',  ( 123.4608748109119745, -10.63000616557722466, -14.87417383870573495 ) ) ;
#20210=CARTESIAN_POINT ( 'NONE',  ( 118.6391081442452986, -4.089484607189486809, -7.948022111789456723 ) ) ;
#20211=CARTESIAN_POINT ( 'NONE',  ( 112.6828081442453282, -7.893985811506177619, -18.51759400769804742 ) ) ;
#20213=CARTESIAN_POINT ( 'NONE',  ( 114.3846081442453197, 0.4262465694468514643, -12.03445270309931736 ) ) ;
#20214=CARTESIAN_POINT ( 'NONE',  ( 111.8886348109120092, -6.222761293078241884, -8.102969835052219238 ) ) ;
#20215=CARTESIAN_POINT ( 'NONE',  ( 125.0492214775786266, -6.344957434206665248, -7.627207830600338134 ) ) ;
#20216=CARTESIAN_POINT ( 'NONE',  ( 115.9162281442453235, -4.089484607189486809, -7.948022111789456723 ) ) ;
#20217=CARTESIAN_POINT ( 'NONE',  ( 111.3213681442453264, -7.643976991954077427, -18.09477374809248928 ) ) ;
#20219=CARTESIAN_POINT ( 'NONE',  ( 116.6536748109119941, -10.15424416112533912, -14.75197769757731336 ) ) ;
#20222=CARTESIAN_POINT ( 'NONE',  ( 124.1415948109119540, -3.505236298600246325, -18.68346056562440793 ) ) ;
#20230=CARTESIAN_POINT ( 'NONE',  ( 112.1155414775786454, 0.9020085738987339008, -11.91225656197089222 ) ) ;
#20234=CARTESIAN_POINT ( 'NONE',  ( 122.9294065278262451, -1.036737761566197014, -17.24079555149560861 ) ) ;
#20235=CARTESIAN_POINT ( 'NONE',  ( 119.5467348109119712, -4.089484607189486809, -7.948022111789456723 ) ) ;
#20239=CARTESIAN_POINT ( 'NONE',  ( 125.5030348109119558, -3.383040157471821630, -19.15922257007629170 ) ) ;
#20240=CARTESIAN_POINT ( 'NONE',  ( 122.9503348109119827, -9.859900752359378018, -12.68260735090039759 ) ) ;
#20243=CARTESIAN_POINT ( 'NONE',  ( 125.2194014775786286, -10.30919188438810075, -12.61870101168855918 ) ) ;
#20244=CARTESIAN_POINT ( 'NONE',  ( 121.0216281442452981, -1.561330072975668948, -17.79121239304076951 ) ) ;
#20246=CARTESIAN_POINT ( 'NONE',  ( 115.9729548109119861, -3.505236298600246325, -18.68346056562440793 ) ) ;
#20247=CARTESIAN_POINT ( 'NONE',  ( 124.2550481442452792, -9.988377603198980381, -10.36322818467138518 ) ) ;
#20251=CARTESIAN_POINT ( 'NONE',  ( 116.8238548109119819, -5.574606645277164318, -18.38911715685844683 ) ) ;
#20252=CARTESIAN_POINT ( 'NONE',  ( 118.5256548109119876, -8.899110576539710493, -16.42337572283490132 ) ) ;
#20257=CARTESIAN_POINT ( 'NONE',  ( 114.1009748109119784, -4.089484607189486809, -7.948022111789456723 ) ) ;
#20258=CARTESIAN_POINT ( 'NONE',  ( 112.9120775202278253, -2.239543233855025850, -18.13706010537467606 ) ) ;
#20262=CARTESIAN_POINT ( 'NONE',  ( 123.7184548109119788, -3.484218720211407661, -13.98160872758045770 ) ) ;
#20263=CARTESIAN_POINT ( 'NONE',  ( 111.5085532531557106, -1.270193261574751542, -16.92991464886373976 ) ) ;
#20265=CARTESIAN_POINT ( 'NONE',  ( 117.2209414775786485, -7.893985811506177619, -18.51759400769804742 ) ) ;
#20266=CARTESIAN_POINT ( 'NONE',  ( 126.5808414775786446, -9.859900752359378018, -12.68260735090039759 ) ) ;
#20267=CARTESIAN_POINT ( 'NONE',  ( 118.7525614775786380, -1.833838273342659253, -17.42832698103878286 ) ) ;
#20270=CARTESIAN_POINT ( 'NONE',  ( 123.4041481442452834, -10.30919188438810075, -12.61870101168855918 ) ) ;
#20271=CARTESIAN_POINT ( 'NONE',  ( 116.7671281442453335, -1.834011780172310813, -8.268836392978581529 ) ) ;
#20273=CARTESIAN_POINT ( 'NONE',  ( 112.8529881442453160, -7.894159318335828068, -9.358103419637847864 ) ) ;
#20276=CARTESIAN_POINT ( 'NONE',  ( 117.6747548109119919, -1.834011780172310813, -8.268836392978581529 ) ) ;
#20279=CARTESIAN_POINT ( 'NONE',  ( 114.8384214775786489, 0.9020085738987339008, -11.91225656197089222 ) ) ;
#20281=CARTESIAN_POINT ( 'NONE',  ( 120.9081748109119872, -5.638512984488999180, -18.83840828888717311 ) ) ;
#20283=CARTESIAN_POINT ( 'NONE',  ( 113.1366214775786432, -7.643976991954077427, -18.09477374809248928 ) ) ;
#20286=CARTESIAN_POINT ( 'NONE',  ( 116.3133148109120043, -2.084020599724406786, -8.691656652584148546 ) ) ;
#20288=CARTESIAN_POINT ( 'NONE',  ( 116.4834948109119779, -7.894159318335828068, -9.358103419637847864 ) ) ;
#20290=CARTESIAN_POINT ( 'NONE',  ( 117.1074881442453233, 0.4262465694468514643, -12.03445270309931736 ) ) ;
#20291=CARTESIAN_POINT ( 'NONE',  ( 115.2922348109119781, -10.63000616557722466, -14.87417383870573495 ) ) ;
#20293=CARTESIAN_POINT ( 'NONE',  ( 112.0588148109119828, 0.5811942927096154232, -14.16772938898807155 ) ) ;
#20294=CARTESIAN_POINT ( 'NONE',  ( 116.8238548109119819, -5.574606645277164318, -18.38911715685844683 ) ) ;
#20295=CARTESIAN_POINT ( 'NONE',  ( 113.3635281442453504, -0.1624402480850797581, -16.17319339645315424 ) ) ;
#20296=CARTESIAN_POINT ( 'NONE',  ( 115.1220548109119761, -1.833838273342658809, -17.42832698103878286 ) ) ;
#20298=CARTESIAN_POINT ( 'NONE',  ( 113.9875214775786532, -0.4660016031367893996, -10.09054647747474043 ) ) ;
#20304=CARTESIAN_POINT ( 'NONE',  ( 117.1642148109119859, -9.261995988541697145, -16.69588392320189030 ) ) ;
#20306=CARTESIAN_POINT ( 'NONE',  ( 125.1626748109119802, -9.988377603198980381, -10.36322818467138518 ) ) ;
#20307=CARTESIAN_POINT ( 'NONE',  ( 117.8449348109119938, -1.833838273342659253, -17.42832698103878286 ) ) ;
#20310=CARTESIAN_POINT ( 'NONE',  ( 123.6310548109119765, -5.638512984488999180, -18.83840828888717311 ) ) ;
#20315=CARTESIAN_POINT ( 'NONE',  ( 112.2857214775786474, -4.089484607189486809, -7.948022111789456723 ) ) ;
#20316=CARTESIAN_POINT ( 'NONE',  ( 123.9146881442452894, -10.15424416112533912, -14.75197769757731336 ) ) ;
#20317=CARTESIAN_POINT ( 'NONE',  ( 119.1496481442453046, -3.383040157471821630, -19.15922257007629170 ) ) ;
#20318=CARTESIAN_POINT ( 'NONE',  ( 118.0151148109119816, 0.4262465694468514643, -12.03445270309931736 ) ) ;
#20319=CARTESIAN_POINT ( 'NONE',  ( 118.0151148109119816, -10.63000616557722466, -14.87417383870573495 ) ) ;
#20321=( BOUNDED_SURFACE ( )  B_SPLINE_SURFACE ( 1, 2, ( 
 ( #41784, #24441, #7109, #21019, #34892, #24661, #3681, #266, #14175, #11440, #1823, #40145, #15295, #25786, #29204, #29427, #39469 ),
 ( #25563, #42670, #1600, #25345, #35805, #36485, #5252, #36032, #28764, #15075, #36702, #42894, #22140, #12111, #15752, #15520, #39239 ) ),
 .UNSPECIFIED., .F., .F., .F. ) 
 B_SPLINE_SURFACE_WITH_KNOTS ( ( 2, 2 ),
 ( 3, 2, 2, 2, 2, 2, 2, 2, 3 ),
 ( 0.000000000000000000, 1.000000000000000000 ),
 ( 0.000000000000000000, 0.1250000000000000000, 0.2500000000000000000, 0.3750000000000000000, 0.5000000000000000000, 0.6250000000000000000, 0.7500000000000000000, 0.8750000000000000000, 1.000000000000000000 ),
 .UNSPECIFIED. ) 
 GEOMETRIC_REPRESENTATION_ITEM ( )  RATIONAL_B_SPLINE_SURFACE ( (
 ( 1.000000000000000000, 0.9238795325112869605, 1.000000000000000000, 0.9238795325112869605, 1.000000000000000000, 0.9238795325112869605, 1.000000000000000000, 0.9238795325112869605, 1.000000000000000000, 0.9238795325112869605, 1.000000000000000000, 0.9238795325112869605, 1.000000000000000000, 0.9238795325112869605, 1.000000000000000000, 0.9238795325112869605, 1.000000000000000000),
 ( 1.000000000000000000, 0.9238795325112869605, 1.000000000000000000, 0.9238795325112869605, 1.000000000000000000, 0.9238795325112869605, 1.000000000000000000, 0.9238795325112869605, 1.000000000000000000, 0.9238795325112869605, 1.000000000000000000, 0.9238795325112869605, 1.000000000000000000, 0.9238795325112869605, 1.000000000000000000, 0.9238795325112869605, 1.000000000000000000) ) ) 
 REPRESENTATION_ITEM ( '' )  SURFACE ( )  );
#20322=CARTESIAN_POINT ( 'NONE',  ( 126.3671785243083150, -1.099405526347972284, -9.990639651589864556 ) ) ;
#20323=CARTESIAN_POINT ( 'NONE',  ( 121.8725281442453223, -6.222761293078241884, -8.102969835052219238 ) ) ;
#20327=CARTESIAN_POINT ( 'NONE',  ( 118.2987481442453088, -1.561330072975668504, -17.79121239304076951 ) ) ;
#20328=CARTESIAN_POINT ( 'NONE',  ( 122.5532481442453019, 0.4262465694468514643, -12.03445270309931736 ) ) ;
#20332=CARTESIAN_POINT ( 'NONE',  ( 135.5837700376040118, -1.194507185862332399, -8.657517032471606200 ) ) ;
#20335=CARTESIAN_POINT ( 'NONE',  ( 118.5823814775786360, -1.834011780172310813, -8.268836392978581529 ) ) ;
#20337=CARTESIAN_POINT ( 'NONE',  ( 120.6812681442452941, 0.1319031606808879209, -14.10382304977623669 ) ) ;
#20340=CARTESIAN_POINT ( 'NONE',  ( 112.6260814775786514, -9.261995988541697145, -16.69588392320189030 ) ) ;
#20342=CARTESIAN_POINT ( 'NONE',  ( 123.0070614775786169, -10.15424416112533912, -14.75197769757731336 ) ) ;
#20346=CARTESIAN_POINT ( 'NONE',  ( 121.1350814775786233, 0.5811942927096110934, -14.16772938898807510 ) ) ;
#20348=CARTESIAN_POINT ( 'NONE',  ( 117.2252848144346729, -2.280480477428486807, -18.08254604495228435 ) ) ;
#20349=CARTESIAN_POINT ( 'NONE',  ( 120.8514481442452961, -7.893985811506177619, -18.51759400769804742 ) ) ;
#20350=CARTESIAN_POINT ( 'NONE',  ( 118.2420214775786320, -3.383040157471821630, -19.15922257007629170 ) ) ;
#20351=CARTESIAN_POINT ( 'NONE',  ( 120.5678148109119832, -1.833838273342659253, -17.42832698103878286 ) ) ;
#20353=CARTESIAN_POINT ( 'NONE',  ( 112.7395348109119766, -5.638512984488999180, -18.83840828888717311 ) ) ;
#20355=CARTESIAN_POINT ( 'NONE',  ( 121.9292548109119849, -7.894159318335828068, -9.358103419637847864 ) ) ;
#20356=CARTESIAN_POINT ( 'NONE',  ( 125.6059481442453318, -7.866424907534184996, -9.395035934245763443 ) ) ;
#20360=CARTESIAN_POINT ( 'NONE',  ( 124.0848681442452772, -4.089484607189486809, -7.948022111789456723 ) ) ;
#20361=CARTESIAN_POINT ( 'NONE',  ( 121.7590748109119687, -2.084020599724406786, -8.691656652584148546 ) ) ;
#20363=CARTESIAN_POINT ( 'NONE',  ( 125.9001214775786224, -4.089484607189486809, -7.948022111789456723 ) ) ;
#20364=CARTESIAN_POINT ( 'NONE',  ( 110.2184548109119788, -4.863998795839242995, -13.39321520033831447 ) ) ;
#20366=CARTESIAN_POINT ( 'NONE',  ( 123.1772414775786189, -4.089484607189486809, -7.948022111789456723 ) ) ;
#20367=CARTESIAN_POINT ( 'NONE',  ( 122.3830681442452857, -8.166667518702819706, -8.995218007635861213 ) ) ;
#20369=CARTESIAN_POINT ( 'NONE',  ( 125.8433948109119456, -7.643976991954077427, -18.09477374809248928 ) ) ;
#20370=CARTESIAN_POINT ( 'NONE',  ( 135.3184548109119874, -0.6896191363000483410, -17.70303589939592825 ) ) ;
#20373=CARTESIAN_POINT ( 'NONE',  ( 125.0849635773846842, -2.467220198597905867, -17.83387418641800437 ) ) ;
#20374=CARTESIAN_POINT ( 'NONE',  ( 113.1933481442453058, -5.574606645277164318, -18.38911715685844683 ) ) ;
#20375=CARTESIAN_POINT ( 'NONE',  ( 122.2696148109119889, -5.574606645277164318, -18.38911715685844683 ) ) ;
#20379=CARTESIAN_POINT ( 'NONE',  ( 122.7234281442452755, -4.153390946401325223, -8.397313243818185668 ) ) ;
#20381=CARTESIAN_POINT ( 'NONE',  ( 115.5191414775786569, -6.222761293078241884, -8.102969835052219238 ) ) ;
#20382=CARTESIAN_POINT ( 'NONE',  ( 112.2289948109119848, -7.643976991954077427, -18.09477374809248928 ) ) ;
#20385=CARTESIAN_POINT ( 'NONE',  ( 123.8012348109119642, -9.565557343593413364, -10.61323700422348004 ) ) ;
#20386=CARTESIAN_POINT ( 'NONE',  ( 118.5823814775786360, -1.834011780172310813, -8.268836392978581529 ) ) ;
#20392=VERTEX_POINT ( 'NONE', #12441 ) ;
#20394=CARTESIAN_POINT ( 'NONE',  ( 115.1787814775786387, -0.1624402480850797581, -16.17319339645315424 ) ) ;
#20395=CARTESIAN_POINT ( 'NONE',  ( 114.2711548109119803, -0.1624402480850797581, -16.17319339645315424 ) ) ;
#20397=CARTESIAN_POINT ( 'NONE',  ( 114.9518748109119883, -1.834011780172303929, -8.268836392978592187 ) ) ;
#20404=CARTESIAN_POINT ( 'NONE',  ( 121.7590748109119687, -2.084020599724406786, -8.691656652584148546 ) ) ;
#20405=CARTESIAN_POINT ( 'NONE',  ( 114.6115148109119986, -6.222761293078241884, -8.102969835052219238 ) ) ;
#20406=CARTESIAN_POINT ( 'NONE',  ( 125.2194014775786286, 0.1319031606808887813, -14.10382304977621182 ) ) ;
#20408=DIRECTION ( 'NONE',  ( 0.000000000000000000, 0.6004852223388321697, -0.7996358532186279566 ) ) ;
#20412=CARTESIAN_POINT ( 'NONE',  ( 111.8991748109119868, -7.866424907533402511, -9.395035934245173692 ) ) ;
#20414=CARTESIAN_POINT ( 'NONE',  ( 125.1059481442452750, -8.166667518702819706, -8.995218007635861213 ) ) ;
#20415=CARTESIAN_POINT ( 'NONE',  ( 126.4106614775786284, -6.222761293078241884, -8.102969835052219238 ) ) ;
#20418=CARTESIAN_POINT ( 'NONE',  ( 112.0588148109119828, 0.5811942927096154232, -14.16772938898807155 ) ) ;
#20419=CARTESIAN_POINT ( 'NONE',  ( 113.6232486830090096, -1.087735405160637603, -17.17288456429614030 ) ) ;
#20421=CARTESIAN_POINT ( 'NONE',  ( 125.5030348109119558, -6.222761293078241884, -8.102969835052219238 ) ) ;
#20422=CARTESIAN_POINT ( 'NONE',  ( 123.6877814775786533, -6.222761293078241884, -8.102969835052219238 ) ) ;
#20425=CARTESIAN_POINT ( 'NONE',  ( 120.3924224678160897, -1.149058757900107697, -17.09122335155391781 ) ) ;
#20427=CARTESIAN_POINT ( 'NONE',  ( 113.0798948109119948, -8.899110576539717599, -16.42337572283489422 ) ) ;
#20429=CARTESIAN_POINT ( 'NONE',  ( 117.7314814775786260, -4.089484607189483256, -7.948022111789462052 ) ) ;
#20431=CARTESIAN_POINT ( 'NONE',  ( 123.0637881442452937, -0.4660016031367893996, -10.09054647747474043 ) ) ;
#20432=CARTESIAN_POINT ( 'NONE',  ( 125.3328548109119964, -9.261995988541697145, -16.69588392320189030 ) ) ;
#20434=CARTESIAN_POINT ( 'NONE',  ( 119.3765548109119834, 0.9020085738987339008, -11.91225656197089222 ) ) ;
#20435=CARTESIAN_POINT ( 'NONE',  ( 113.3635281442453504, -9.988377603198976828, -10.36322818467138340 ) ) ;
#20438=CARTESIAN_POINT ( 'NONE',  ( 112.2289948109119848, -7.643976991954077427, -18.09477374809248928 ) ) ;
#20439=CARTESIAN_POINT ( 'NONE',  ( 125.4463081442452932, -5.638512984488999180, -18.83840828888717311 ) ) ;
#20440=CARTESIAN_POINT ( 'NONE',  ( 124.8223148109119762, 0.9020085738987339008, -11.91225656197089222 ) ) ;
#20442=CARTESIAN_POINT ( 'NONE',  ( 115.3489614775786407, -9.261995988541697145, -16.69588392320189030 ) ) ;
#20443=CARTESIAN_POINT ( 'NONE',  ( 113.4769814775786330, 0.4262465694468514643, -12.03445270309931736 ) ) ;
#20445=CARTESIAN_POINT ( 'NONE',  ( 117.6747548109119919, -7.643976991954077427, -18.09477374809248928 ) ) ;
#20446=CARTESIAN_POINT ( 'NONE',  ( 112.0588148109119828, 0.5811942927096154232, -14.16772938898807155 ) ) ;
#20448=CARTESIAN_POINT ( 'NONE',  ( 122.6667014775786413, -2.084020599724406786, -8.691656652584148546 ) ) ;
#20452=CONICAL_SURFACE ( 'NONE', #35676, 0.4999999999999999445, 0.7853981633974476129 ) ;
#20453=FACE_OUTER_BOUND ( 'NONE', #34044, .T. ) ;
#20458=CARTESIAN_POINT ( 'NONE',  ( 112.6260814775786514, -0.8288870151387760510, -10.36305467784173118 ) ) ;
#20461=CARTESIAN_POINT ( 'NONE',  ( 118.9794681442453026, -9.261995988541697145, -16.69588392320189030 ) ) ;
#20462=CARTESIAN_POINT ( 'NONE',  ( 137.1760413997919557, -6.546412817364553050, -18.44820575760469339 ) ) ;
#20466=CARTESIAN_POINT ( 'NONE',  ( 120.2274548109119934, -9.859900752359378018, -12.68260735090039759 ) ) ;
#20468=CARTESIAN_POINT ( 'NONE',  ( 135.9373687277912097, -9.538988841393456042, -9.739382474596094852 ) ) ;
#20469=CARTESIAN_POINT ( 'NONE',  ( 117.6747548109119919, -1.834011780172310813, -8.268836392978581529 ) ) ;
#20471=CARTESIAN_POINT ( 'NONE',  ( 116.9940348109119839, -0.1624402480850797581, -16.17319339645315424 ) ) ;
#20472=CARTESIAN_POINT ( 'NONE',  ( 111.8319081442453182, -4.153390946401321671, -8.397313243818183892 ) ) ;
#20476=CARTESIAN_POINT ( 'NONE',  ( 116.2565881442453133, -0.8288870151387760510, -10.36305467784173118 ) ) ;
#20478=CARTESIAN_POINT ( 'NONE',  ( 119.4332814775786318, -8.899110576539710493, -16.42337572283490132 ) ) ;
#20485=CARTESIAN_POINT ( 'NONE',  ( 115.3489614775786407, -9.261995988541697145, -16.69588392320189030 ) ) ;
#20486=CARTESIAN_POINT ( 'NONE',  ( 111.7184548109119788, -9.261995988541697145, -16.69588392320189030 ) ) ;
#20491=ORIENTED_EDGE ( 'NONE', *, *, #1470, .F. ) ;
#20492=CARTESIAN_POINT ( 'NONE',  ( 123.4041481442452834, -10.30919188438810075, -12.61870101168855918 ) ) ;
#20493=CARTESIAN_POINT ( 'NONE',  ( 113.5904348109119866, -7.893985811506177619, -18.51759400769804742 ) ) ;
#20494=CARTESIAN_POINT ( 'NONE',  ( 118.9794681442453026, -0.8288870151387760510, -10.36305467784173118 ) ) ;
#20496=CARTESIAN_POINT ( 'NONE',  ( 123.5743281442453139, -7.893985811506177619, -18.51759400769804742 ) ) ;
#20497=CARTESIAN_POINT ( 'NONE',  ( 118.3554748109119998, 0.2603800115204892296, -16.42320221600525088 ) ) ;
#20500=EDGE_CURVE ( 'NONE', #19315, #30808, #9555, .T. ) ;
#20501=CARTESIAN_POINT ( 'NONE',  ( 111.8319081442453182, -4.153390946401321671, -8.397313243818183892 ) ) ;
#20504=CARTESIAN_POINT ( 'NONE',  ( 118.6391081442452986, -4.089484607189486809, -7.948022111789456723 ) ) ;
#20506=CARTESIAN_POINT ( 'NONE',  ( 114.3846081442453197, -10.63000616557722466, -14.87417383870573495 ) ) ;
#20509=CARTESIAN_POINT ( 'NONE',  ( 125.9568481442452850, -6.344957434206665248, -7.627207830600338134 ) ) ;
#20511=CARTESIAN_POINT ( 'NONE',  ( 113.4202548109119846, 0.1319031606808879209, -14.10382304977623669 ) ) ;
#20513=CARTESIAN_POINT ( 'NONE',  ( 115.1220548109119761, -1.833838273342658809, -17.42832698103878286 ) ) ;
#20515=CARTESIAN_POINT ( 'NONE',  ( 116.3133148109120043, -2.084020599724406786, -8.691656652584148546 ) ) ;
#20517=CARTESIAN_POINT ( 'NONE',  ( 114.4980614775786734, -2.084020599724406786, -8.691656652584148546 ) ) ;
#20519=CARTESIAN_POINT ( 'NONE',  ( 114.6115148109119986, -3.383040157471821630, -19.15922257007629170 ) ) ;
#20520=CARTESIAN_POINT ( 'NONE',  ( 125.4463081442452932, -5.638512984488999180, -18.83840828888717311 ) ) ;
#20521=CARTESIAN_POINT ( 'NONE',  ( 118.5823814775786360, -7.643976991954077427, -18.09477374809248928 ) ) ;
#20522=ORIENTED_EDGE ( 'NONE', *, *, #37928, .F. ) ;
#20523=CARTESIAN_POINT ( 'NONE',  ( 112.2289948109119848, -1.834011780172310813, -8.268836392978581529 ) ) ;
#20529=CARTESIAN_POINT ( 'NONE',  ( 123.3474214775786209, -9.988377603198976828, -10.36322818467138340 ) ) ;
#20531=CARTESIAN_POINT ( 'NONE',  ( 120.7039275888224097, -2.372251574601201174, -17.96033910819751611 ) ) ;
#20532=CARTESIAN_POINT ( 'NONE',  ( 117.9016614775786280, -0.1624402480850797581, -16.17319339645315424 ) ) ;
#20533=CARTESIAN_POINT ( 'NONE',  ( 124.7655881442452852, -9.859900752359376241, -12.68260735090040114 ) ) ;
#20534=CARTESIAN_POINT ( 'NONE',  ( 122.8368814775786291, -1.561330072975668948, -17.79121239304076951 ) ) ;
#20538=CARTESIAN_POINT ( 'NONE',  ( 111.7751814775786556, -7.893985811506177619, -18.51759400769804742 ) ) ;
#20540=CARTESIAN_POINT ( 'NONE',  ( 125.7866681442452688, -8.899110576539710493, -16.42337572283490132 ) ) ;
#20541=CARTESIAN_POINT ( 'NONE',  ( 122.2128881442453263, -1.834011780172310813, -8.268836392978581529 ) ) ;
#20542=CARTESIAN_POINT ( 'NONE',  ( 116.3133148109120043, -2.084020599724406786, -8.691656652584148546 ) ) ;
#20543=CARTESIAN_POINT ( 'NONE',  ( 112.1722681442453222, -8.899110576539710493, -16.42337572283490132 ) ) ;
#20544=CARTESIAN_POINT ( 'NONE',  ( 117.4478481442453131, 0.2603800115204892296, -16.42320221600525088 ) ) ;
#20546=CARTESIAN_POINT ( 'NONE',  ( 127.9806007748781838, -1.226557776704764624, -8.771704985610853100 ) ) ;
#20547=CARTESIAN_POINT ( 'NONE',  ( 123.8579614775786126, -9.859900752359378018, -12.68260735090039759 ) ) ;
#20550=CARTESIAN_POINT ( 'NONE',  ( 117.9583881442453048, -10.30919188438810075, -12.61870101168855918 ) ) ;
#20551=CARTESIAN_POINT ( 'NONE',  ( 123.3474214775786209, -0.1624402480850797581, -16.17319339645315424 ) ) ;
#20555=CARTESIAN_POINT ( 'NONE',  ( 123.7445081442452874, -1.561330072975668948, -17.79121239304076951 ) ) ;
#20557=CARTESIAN_POINT ( 'NONE',  ( 120.9081748109119872, -4.153390946401325223, -8.397313243818185668 ) ) ;
#20560=EDGE_LOOP ( 'NONE', ( #32908, #4150, #10345, #43019 ) ) ;
#20562=CARTESIAN_POINT ( 'NONE',  ( 113.9875214775786532, -0.4660016031367893996, -10.09054647747474043 ) ) ;
#20563=CARTESIAN_POINT ( 'NONE',  ( 125.6732148109119862, -9.859900752359378018, -12.68260735090039759 ) ) ;
#20566=ADVANCED_FACE ( 'NONE', ( #40383 ), #27194, .T. ) ;
#20567=CARTESIAN_POINT ( 'NONE',  ( 120.6812681442452941, -10.30919188438810075, -12.61870101168855918 ) ) ;
#20569=CIRCLE ( 'NONE', #24952, 5.999999999999997335 ) ;
#20571=CARTESIAN_POINT ( 'NONE',  ( 121.3619881442452879, -4.089484607189486809, -7.948022111789456723 ) ) ;
#20572=CARTESIAN_POINT ( 'NONE',  ( 117.6747548109119919, -1.834011780172310813, -8.268836392978581529 ) ) ;
#20573=CARTESIAN_POINT ( 'NONE',  ( 118.3554748109119998, -9.565557343593413364, -10.61323700422348004 ) ) ;
#20575=CARTESIAN_POINT ( 'NONE',  ( 115.6893214775786447, 0.5811942927096154232, -14.16772938898807155 ) ) ;
#20577=CARTESIAN_POINT ( 'NONE',  ( 113.1933481442453058, -4.089484607189486809, -7.948022111789456723 ) ) ;
#20578=CARTESIAN_POINT ( 'NONE',  ( 124.9252281442453238, -8.862178061931794915, -16.39564131203325559 ) ) ;
#20582=CARTESIAN_POINT ( 'NONE',  ( 120.9649014775786355, -3.383040157471821630, -19.15922257007629170 ) ) ;
#20583=CARTESIAN_POINT ( 'NONE',  ( 124.1983214775786166, -1.833838273342659697, -17.42832698103878286 ) ) ;
#20586=CARTESIAN_POINT ( 'NONE',  ( 123.5176014775786228, -9.261995988541697145, -16.69588392320189030 ) ) ;
#20589=CARTESIAN_POINT ( 'NONE',  ( 122.8936081442453059, 0.2603800115204892296, -16.42320221600525088 ) ) ;
#20594=CARTESIAN_POINT ( 'NONE',  ( 113.9875214775786532, -0.4660016031367893996, -10.09054647747474043 ) ) ;
#20596=CARTESIAN_POINT ( 'NONE',  ( 111.7688629525735706, -1.111561923218670422, -17.14115599315433869 ) ) ;
#20600=CARTESIAN_POINT ( 'NONE',  ( 112.4559014775786778, -0.1624402480850797581, -16.17319339645315424 ) ) ;
#20602=CARTESIAN_POINT ( 'NONE',  ( 112.1155414775786454, 0.9020085738987339008, -11.91225656197089222 ) ) ;
#20605=CARTESIAN_POINT ( 'NONE',  ( 120.1707281442453166, -9.565557343593413364, -10.61323700422348004 ) ) ;
#20606=CARTESIAN_POINT ( 'NONE',  ( 116.9940348109119839, -0.1624402480850797581, -16.17319339645315424 ) ) ;
#20607=CARTESIAN_POINT ( 'NONE',  ( 113.4202548109119846, 0.1319031606808879209, -14.10382304977623669 ) ) ;
#20608=ORIENTED_EDGE ( 'NONE', *, *, #26430, .T. ) ;
#20610=CARTESIAN_POINT ( 'NONE',  ( 124.5954081442453116, -6.222761293078241884, -8.102969835052219238 ) ) ;
#20612=CARTESIAN_POINT ( 'NONE',  ( 118.1852948109119836, -5.638512984488999180, -18.83840828888717311 ) ) ;
#20613=CARTESIAN_POINT ( 'NONE',  ( 125.5030348109119558, -6.222761293078241884, -8.102969835052219238 ) ) ;
#20615=CARTESIAN_POINT ( 'NONE',  ( 126.2872529661387091, -9.070044156411084302, -16.15989887877886133 ) ) ;
#20617=CARTESIAN_POINT ( 'NONE',  ( 116.6536748109119941, -10.15424416112533912, -14.75197769757731336 ) ) ;
#20618=CARTESIAN_POINT ( 'NONE',  ( 113.4769814775786330, 0.4262465694468514643, -12.03445270309931736 ) ) ;
#20619=CARTESIAN_POINT ( 'NONE',  ( 115.1787814775786529, -9.988377603198973276, -10.36322818467138163 ) ) ;
#20627=CARTESIAN_POINT ( 'NONE',  ( 117.9417709814547095, -2.395992375830784837, -17.92872468182854107 ) ) ;
#20628=CARTESIAN_POINT ( 'NONE',  ( 122.6667014775786413, -2.084020599724406786, -8.691656652584148546 ) ) ;
#20629=CARTESIAN_POINT ( 'NONE',  ( 114.1577014775786552, -3.505236298600246325, -18.68346056562440793 ) ) ;
#20630=CARTESIAN_POINT ( 'NONE',  ( 113.8173414775786512, -9.565557343593411588, -10.61323700422346583 ) ) ;
#20632=CARTESIAN_POINT ( 'NONE',  ( 122.3620835773848654, -2.467220198592778413, -17.83387418641524391 ) ) ;
#20635=CARTESIAN_POINT ( 'NONE',  ( 122.5191809221557122, -2.372251574601201174, -17.96033910819751611 ) ) ;
#20636=CARTESIAN_POINT ( 'NONE',  ( 111.5482748109120053, -0.1624402480850797581, -16.17319339645315424 ) ) ;
#20638=CARTESIAN_POINT ( 'NONE',  ( 126.1837548109119211, -10.63000616557722466, -14.87417383870573495 ) ) ;
#20639=CARTESIAN_POINT ( 'NONE',  ( 125.2761281442453054, 0.4262465694468514643, -12.03445270309931736 ) ) ;
#20641=CARTESIAN_POINT ( 'NONE',  ( 114.2144281442453178, -8.166667518702817929, -8.995218007635859436 ) ) ;
#20645=CARTESIAN_POINT ( 'NONE',  ( 126.4673881442452910, -7.894159318335828068, -9.358103419637847864 ) ) ;
#20646=CARTESIAN_POINT ( 'NONE',  ( 123.8012348109119642, -9.565557343593413364, -10.61323700422348004 ) ) ;
#20650=CARTESIAN_POINT ( 'NONE',  ( 112.3781902440515665, -2.467220198592768199, -17.83387418641523325 ) ) ;
#20651=DIRECTION ( 'NONE',  ( 0.000000000000000000, -0.6004852223388321697, 0.7996358532186280677 ) ) ;
#20655=CARTESIAN_POINT ( 'NONE',  ( 124.6521348109119884, -1.561330072975668948, -17.79121239304076951 ) ) ;
#20656=CARTESIAN_POINT ( 'NONE',  ( 124.8223148109119762, 0.9020085738987339008, -11.91225656197089222 ) ) ;
#20659=CARTESIAN_POINT ( 'NONE',  ( 121.7023481442452777, -9.261995988541697145, -16.69588392320189030 ) ) ;
#20660=CARTESIAN_POINT ( 'NONE',  ( 114.6682414775786469, -1.561330072975668060, -17.79121239304076596 ) ) ;
#20662=CARTESIAN_POINT ( 'NONE',  ( 115.0086014775786509, -5.574606645277164318, -18.38911715685844683 ) ) ;
#20664=CARTESIAN_POINT ( 'NONE',  ( 123.1205148109119563, -1.834011780172310813, -8.268836392978581529 ) ) ;
#20665=CARTESIAN_POINT ( 'NONE',  ( 115.6893214775786447, 0.5811942927096154232, -14.16772938898807155 ) ) ;
#20666=CARTESIAN_POINT ( 'NONE',  ( 116.9940348109119839, -0.1624402480850797581, -16.17319339645315424 ) ) ;
#20668=CARTESIAN_POINT ( 'NONE',  ( 117.9016614775786280, -0.1624402480850797581, -16.17319339645315424 ) ) ;
#20670=CARTESIAN_POINT ( 'NONE',  ( 115.8595014775786609, -1.834011780172310813, -8.268836392978581529 ) ) ;
#20671=CARTESIAN_POINT ( 'NONE',  ( 124.9357681442453014, -7.643976991954077427, -18.09477374809248928 ) ) ;
#20678=CARTESIAN_POINT ( 'NONE',  ( 115.6893214775786447, 0.5811942927096154232, -14.16772938898807155 ) ) ;
#20679=CARTESIAN_POINT ( 'NONE',  ( 112.6828081442453140, -7.893985811506177619, -18.51759400769804742 ) ) ;
#20683=CARTESIAN_POINT ( 'NONE',  ( 123.0760201386228800, -1.125321370491285444, -17.12283323191017814 ) ) ;
#20685=CARTESIAN_POINT ( 'NONE',  ( 117.3911214775786505, -1.561330072975668504, -17.79121239304076951 ) ) ;
#20686=CARTESIAN_POINT ( 'NONE',  ( 136.1634721355147803, -4.175307135294594296, -19.22903496993399841 ) ) ;
#20689=CARTESIAN_POINT ( 'NONE',  ( 121.1350814775786233, -9.859900752359378018, -12.68260735090039759 ) ) ;
#20690=ORIENTED_EDGE ( 'NONE', *, *, #8321, .F. ) ;
#20692=CARTESIAN_POINT ( 'NONE',  ( 117.8449348109119938, -8.166667518702817929, -8.995218007635861213 ) ) ;
#20694=CARTESIAN_POINT ( 'NONE',  ( 117.3343948109119737, -6.222761293078241884, -8.102969835052219238 ) ) ;
#20695=CARTESIAN_POINT ( 'NONE',  ( 112.6260814775786514, -0.8288870151387760510, -10.36305467784173118 ) ) ;
#20699=CARTESIAN_POINT ( 'NONE',  ( 115.7460481442453357, -10.15424416112533912, -14.75197769757731336 ) ) ;
#20700=CARTESIAN_POINT ( 'NONE',  ( 121.5888948109119809, 0.1319031606808879209, -14.10382304977623669 ) ) ;
#20706=CARTESIAN_POINT ( 'NONE',  ( 115.6325948109119821, 0.2603800115204892296, -16.42320221600525088 ) ) ;
#20707=CARTESIAN_POINT ( 'NONE',  ( 114.1577014775786552, -6.344957434206662583, -7.627207830600332805 ) ) ;
#20710=CARTESIAN_POINT ( 'NONE',  ( 123.4721467849153527, -2.841504294525492913, -14.83747852055392968 ) ) ;
#20712=CARTESIAN_POINT ( 'NONE',  ( 122.6099748109119929, -9.261995988541697145, -16.69588392320189030 ) ) ;
#20713=CARTESIAN_POINT ( 'NONE',  ( 112.8529881442453302, -1.561330072975668060, -17.79121239304076596 ) ) ;
#20714=CARTESIAN_POINT ( 'NONE',  ( 119.5467348109119712, -5.574606645277164318, -18.38911715685844683 ) ) ;
#20716=CARTESIAN_POINT ( 'NONE',  ( 121.2485348109119769, -0.4660016031367893996, -10.09054647747474043 ) ) ;
#20717=CARTESIAN_POINT ( 'NONE',  ( 118.8092881442453290, -9.988377603198976828, -10.36322818467138340 ) ) ;
#20720=CARTESIAN_POINT ( 'NONE',  ( 113.4769814775786330, 0.4262465694468514643, -12.03445270309931736 ) ) ;
#20723=CARTESIAN_POINT ( 'NONE',  ( 118.6958348109119754, -6.344957434206665248, -7.627207830600338134 ) ) ;
#20725=CARTESIAN_POINT ( 'NONE',  ( 116.6536748109119941, 0.9020085738987339008, -11.91225656197089222 ) ) ;
#20732=CARTESIAN_POINT ( 'NONE',  ( 116.9373081442452929, -1.833838273342659253, -17.42832698103878286 ) ) ;
#20734=CARTESIAN_POINT ( 'NONE',  ( 118.4122014775786340, -9.859900752359374465, -12.68260735090039404 ) ) ;
#20737=CARTESIAN_POINT ( 'NONE',  ( 118.5256548109119876, -8.899110576539710493, -16.42337572283490132 ) ) ;
#20739=CARTESIAN_POINT ( 'NONE',  ( 116.6536748109119941, 0.9020085738987339008, -11.91225656197089222 ) ) ;
#20740=CARTESIAN_POINT ( 'NONE',  ( 125.3895814775786448, -7.893985811506177619, -18.51759400769804742 ) ) ;
#20742=CARTESIAN_POINT ( 'NONE',  ( 117.2209414775786485, -2.084020599724406786, -8.691656652584148546 ) ) ;
#20744=CARTESIAN_POINT ( 'NONE',  ( 115.3489614775786407, -9.261995988541697145, -16.69588392320189030 ) ) ;
#20750=CARTESIAN_POINT ( 'NONE',  ( 121.4754414775786131, -8.166667518702819706, -8.995218007635861213 ) ) ;
#20751=VERTEX_POINT ( 'NONE', #29436 ) ;
#20752=CARTESIAN_POINT ( 'NONE',  ( 118.4752466692503816, -2.311015703046731318, -18.04188382666268708 ) ) ;
#20753=CARTESIAN_POINT ( 'NONE',  ( 117.2209414775786485, -2.084020599724406786, -8.691656652584148546 ) ) ;
#20756=CARTESIAN_POINT ( 'NONE',  ( 122.4397948109119767, -9.988377603198976828, -10.36322818467138340 ) ) ;
#20760=CARTESIAN_POINT ( 'NONE',  ( 113.1366214775786432, -1.834011780172310813, -8.268836392978581529 ) ) ;
#20761=CARTESIAN_POINT ( 'NONE',  ( 112.2857214775786474, -4.089484607189486809, -7.948022111789456723 ) ) ;
#20762=CARTESIAN_POINT ( 'NONE',  ( 123.6877814775786533, -3.383040157471821630, -19.15922257007629170 ) ) ;
#20763=CARTESIAN_POINT ( 'NONE',  ( 118.2987481442453088, -7.894159318335828068, -9.358103419637847864 ) ) ;
#20765=CARTESIAN_POINT ( 'NONE',  ( 118.3554748109119998, 0.2603800115204892296, -16.42320221600525088 ) ) ;
#20767=CARTESIAN_POINT ( 'NONE',  ( 123.9714148109119805, -8.899110576539710493, -16.42337572283490132 ) ) ;
#20771=CARTESIAN_POINT ( 'NONE',  ( 116.1431348109119881, -10.30919188438810075, -12.61870101168855918 ) ) ;
#20772=CARTESIAN_POINT ( 'NONE',  ( 123.6310548109119765, -4.153390946401325223, -8.397313243818185668 ) ) ;
#20775=CARTESIAN_POINT ( 'NONE',  ( 136.7082020370487214, -1.261532916568094853, -9.046217426794857630 ) ) ;
#20776=CARTESIAN_POINT ( 'NONE',  ( 123.9714148109119805, -0.4660016031367893996, -10.09054647747474043 ) ) ;
#20779=CARTESIAN_POINT ( 'NONE',  ( 118.2987481442453088, -7.894159318335828068, -9.358103419637847864 ) ) ;
#20782=CARTESIAN_POINT ( 'NONE',  ( 113.7606148109119886, -1.561330072975668060, -17.79121239304076596 ) ) ;
#20783=CARTESIAN_POINT ( 'NONE',  ( 124.4252281442452812, -0.8288870151387760510, -10.36305467784173118 ) ) ;
#20784=( NAMED_UNIT ( * ) PLANE_ANGLE_UNIT ( ) SI_UNIT ( $, .RADIAN. ) );
#20786=CARTESIAN_POINT ( 'NONE',  ( 121.3052614775786111, -1.834011780172310813, -8.268836392978581529 ) ) ;
#20790=CARTESIAN_POINT ( 'NONE',  ( 120.9081748109119872, -5.638512984488999180, -18.83840828888717311 ) ) ;
#20791=CARTESIAN_POINT ( 'NONE',  ( 117.8449348109119938, -8.166667518702817929, -8.995218007635861213 ) ) ;
#20792=CARTESIAN_POINT ( 'NONE',  ( 118.6391081442452986, -5.574606645277164318, -18.38911715685844683 ) ) ;
#20794=CARTESIAN_POINT ( 'NONE',  ( 117.8449348109119938, -8.166667518702817929, -8.995218007635861213 ) ) ;
#20796=CARTESIAN_POINT ( 'NONE',  ( 125.5597614775786326, -7.894159318336616771, -9.358103419638441167 ) ) ;
#20802=CARTESIAN_POINT ( 'NONE',  ( 126.4106614775786284, -6.222761293078241884, -8.102969835052219238 ) ) ;
#20804=CARTESIAN_POINT ( 'NONE',  ( 122.7234281442452755, -5.638512984488999180, -18.83840828888717311 ) ) ;
#20807=CARTESIAN_POINT ( 'NONE',  ( 122.9503348109119827, 0.5811942927096110934, -14.16772938898807510 ) ) ;
#20808=CARTESIAN_POINT ( 'NONE',  ( 125.3328548109119964, -9.261995988541697145, -16.69588392320189030 ) ) ;
#20811=CARTESIAN_POINT ( 'NONE',  ( 113.8173414775786512, 0.2603800115204892296, -16.42320221600525088 ) ) ;
#20816=CARTESIAN_POINT ( 'NONE',  ( 114.7816948109119863, -9.859900752359374465, -12.68260735090039404 ) ) ;
#20817=CARTESIAN_POINT ( 'NONE',  ( 125.9001214775786224, -5.574606645277164318, -18.38911715685844683 ) ) ;
#20820=CARTESIAN_POINT ( 'NONE',  ( 120.3409081442453044, -8.899110576539710493, -16.42337572283490132 ) ) ;
#20821=CARTESIAN_POINT ( 'NONE',  ( 116.1998614775786507, 0.4262465694468514643, -12.03445270309931736 ) ) ;
#20822=CARTESIAN_POINT ( 'NONE',  ( 113.0798948109119948, -8.899110576539710493, -16.42337572283490132 ) ) ;
#20825=CARTESIAN_POINT ( 'NONE',  ( 125.5597614775786326, -7.894159318335828068, -9.358103419637847864 ) ) ;
#20826=CARTESIAN_POINT ( 'NONE',  ( 115.4056881442453459, -2.084020599724406786, -8.691656652584148546 ) ) ;
#20828=CARTESIAN_POINT ( 'NONE',  ( 126.4262034846904470, -9.248423787863409018, -16.00611581287409280 ) ) ;
#20829=ORIENTED_EDGE ( 'NONE', *, *, #43145, .F. ) ;
#20830=CARTESIAN_POINT ( 'NONE',  ( 120.1707281442453166, -9.565557343593413364, -10.61323700422348004 ) ) ;
#20831=CARTESIAN_POINT ( 'NONE',  ( 112.1155414775786454, -10.15424416112533912, -14.75197769757731336 ) ) ;
#20832=DIRECTION ( 'NONE',  ( 0.000000000000000000, 0.6004852223388321697, -0.7996358532186279566 ) ) ;
#20843=CARTESIAN_POINT ( 'NONE',  ( 123.8579614775786126, -9.859900752359378018, -12.68260735090039759 ) ) ;
#20844=CARTESIAN_POINT ( 'NONE',  ( 116.0864081442453113, -0.1624402480850797581, -16.17319339645315424 ) ) ;
#20848=CARTESIAN_POINT ( 'NONE',  ( 115.4056881442453459, -2.084020599724406786, -8.691656652584148546 ) ) ;
#20851=CARTESIAN_POINT ( 'NONE',  ( 125.6164881442453094, 0.2603800115204892296, -16.42320221600525088 ) ) ;
#20853=CARTESIAN_POINT ( 'NONE',  ( 111.7184548109119788, -9.261995988541697145, -16.69588392320189030 ) ) ;
#20854=ORIENTED_EDGE ( 'NONE', *, *, #14992, .T. ) ;
#20855=CARTESIAN_POINT ( 'NONE',  ( 112.5126281442453120, -10.30919188438810075, -12.61870101168855918 ) ) ;
#20858=CARTESIAN_POINT ( 'NONE',  ( 113.0798948109119948, -0.4660016031367893996, -10.09054647747474043 ) ) ;
#20859=CARTESIAN_POINT ( 'NONE',  ( 112.8529881442453302, -1.561330072975668060, -17.79121239304076596 ) ) ;
#20860=CARTESIAN_POINT ( 'NONE',  ( 122.4965214775786251, 0.1319031606808879209, -14.10382304977623669 ) ) ;
#20867=CARTESIAN_POINT ( 'NONE',  ( 116.4267681442453153, -6.222761293078241884, -8.102969835052219238 ) ) ;
#20871=CARTESIAN_POINT ( 'NONE',  ( 124.7088614775786226, 0.2603800115204892296, -16.42320221600525088 ) ) ;
#20872=CARTESIAN_POINT ( 'NONE',  ( 125.3895814775786448, -7.893985811506177619, -18.51759400769804742 ) ) ;
#20874=EDGE_CURVE ( 'NONE', #42698, #25860, #16096, .T. ) ;
#20875=CARTESIAN_POINT ( 'NONE',  ( 119.7736414775786358, -10.30919188438810075, -12.61870101168855918 ) ) ;
#20876=CARTESIAN_POINT ( 'NONE',  ( 114.6115148109119986, -3.383040157471821630, -19.15922257007629170 ) ) ;
#20877=ORIENTED_EDGE ( 'NONE', *, *, #17484, .F. ) ;
#20880=CARTESIAN_POINT ( 'NONE',  ( 115.5758681442453053, -7.894159318335828068, -9.358103419637847864 ) ) ;
#20881=CARTESIAN_POINT ( 'NONE',  ( 122.4965214775786251, -10.30919188438810075, -12.61870101168855918 ) ) ;
#20882=CARTESIAN_POINT ( 'NONE',  ( 112.9664414775786412, 0.5811942927096154232, -14.16772938898807155 ) ) ;
#20883=CARTESIAN_POINT ( 'NONE',  ( 114.9518748109119883, -7.643976991954077427, -18.09477374809248928 ) ) ;
#20885=CARTESIAN_POINT ( 'NONE',  ( 120.6812681442452941, 0.1319031606808879209, -14.10382304977623669 ) ) ;
#20887=CARTESIAN_POINT ( 'NONE',  ( 118.1285681442453068, -7.893985811506177619, -18.51759400769804742 ) ) ;
#20888=DIRECTION ( 'NONE',  ( 1.000000000000000000, 0.000000000000000000, 0.000000000000000000 ) ) ;
#20892=EDGE_CURVE ( 'NONE', #19616, #42627, #6785, .T. ) ;
#20898=CARTESIAN_POINT ( 'NONE',  ( 115.2355081442453155, -10.30919188438810075, -12.61870101168855918 ) ) ;
#20900=CARTESIAN_POINT ( 'NONE',  ( 112.7962614775786676, -6.222761293078241884, -8.102969835052219238 ) ) ;
#20905=CARTESIAN_POINT ( 'NONE',  ( 118.5256548109119876, -0.4660016031367893996, -10.09054647747474043 ) ) ;
#20909=CARTESIAN_POINT ( 'NONE',  ( 122.8368814775786291, -7.894159318335828068, -9.358103419637847864 ) ) ;
#20912=CARTESIAN_POINT ( 'NONE',  ( 119.3765548109119834, 0.9020085738987339008, -11.91225656197089222 ) ) ;
#20914=CARTESIAN_POINT ( 'NONE',  ( 117.5045748109119756, -9.859900752359374465, -12.68260735090039404 ) ) ;
#20915=CARTESIAN_POINT ( 'NONE',  ( 111.6617281442453304, 0.4262465694468514643, -12.03445270309931736 ) ) ;
#20918=CARTESIAN_POINT ( 'NONE',  ( 119.0929214775786278, -4.153390946401325223, -8.397313243818185668 ) ) ;
#20919=CARTESIAN_POINT ( 'NONE',  ( 118.5823814775786360, -7.643976991954077427, -18.09477374809248928 ) ) ;
#20925=CARTESIAN_POINT ( 'NONE',  ( 114.7249681442453237, 0.2603800115204892296, -16.42320221600525088 ) ) ;
#20926=CARTESIAN_POINT ( 'NONE',  ( 115.5758681442453053, -1.561330072975668060, -17.79121239304076951 ) ) ;
#20930=CARTESIAN_POINT ( 'NONE',  ( 117.4103264091100840, -0.9924539043446216624, -17.29976612834909133 ) ) ;
#20931=CARTESIAN_POINT ( 'NONE',  ( 122.1561614775786353, -0.4660016031367893996, -10.09054647747474043 ) ) ;
#20932=CARTESIAN_POINT ( 'NONE',  ( 114.1577014775786552, -6.344957434206662583, -7.627207830600332805 ) ) ;
#20933=CARTESIAN_POINT ( 'NONE',  ( 117.2209414775786485, -2.084020599724406786, -8.691656652584148546 ) ) ;
#20934=CARTESIAN_POINT ( 'NONE',  ( 111.3213681442453264, -7.643976991954077427, -18.09477374809248928 ) ) ;
#20935=CARTESIAN_POINT ( 'NONE',  ( 119.8303681442453126, -10.63000616557722466, -14.87417383870573495 ) ) ;
#20937=AXIS2_PLACEMENT_3D ( 'NONE', #7651, #14952, #11308 ) ;
#20940=CARTESIAN_POINT ( 'NONE',  ( 126.1270281442452870, -10.30919188438810075, -12.61870101168855918 ) ) ;
#20943=CARTESIAN_POINT ( 'NONE',  ( 117.9583881442453048, -10.30919188438810075, -12.61870101168855918 ) ) ;
#20945=CARTESIAN_POINT ( 'NONE',  ( 115.6893214775786447, 0.5811942927096154232, -14.16772938898807155 ) ) ;
#20948=CARTESIAN_POINT ( 'NONE',  ( 125.1626748109119802, -9.988377603198980381, -10.36322818467138518 ) ) ;
#20954=CARTESIAN_POINT ( 'NONE',  ( 120.0572748109119772, -6.222761293078241884, -8.102969835052219238 ) ) ;
#20956=CARTESIAN_POINT ( 'NONE',  ( 116.4267681442453153, -6.222761293078241884, -8.102969835052219238 ) ) ;
#20958=CARTESIAN_POINT ( 'NONE',  ( 118.1285681442453068, -2.084020599724406786, -8.691656652584148546 ) ) ;
#20960=CARTESIAN_POINT ( 'NONE',  ( 117.1642148109119859, -9.261995988541697145, -16.69588392320189030 ) ) ;
#20962=CARTESIAN_POINT ( 'NONE',  ( 117.3911214775786505, -7.894159318335828068, -9.358103419637847864 ) ) ;
#20964=CARTESIAN_POINT ( 'NONE',  ( 116.5402214775786405, 0.2603800115204892296, -16.42320221600525088 ) ) ;
#20966=CARTESIAN_POINT ( 'NONE',  ( 115.9613248136183614, -3.929494816604736318, -18.62311481910882094 ) ) ;
#20969=CARTESIAN_POINT ( 'NONE',  ( 124.0281414775786146, -1.834011780172310813, -8.268836392978581529 ) ) ;
#20971=CARTESIAN_POINT ( 'NONE',  ( 126.6827570900284599, -8.613729037902059460, -9.744110473525523730 ) ) ;
#20972=CARTESIAN_POINT ( 'NONE',  ( 117.3911214775786505, -7.894159318335828068, -9.358103419637847864 ) ) ;
#20973=CARTESIAN_POINT ( 'NONE',  ( 116.2565881442452991, -9.261995988541702474, -16.69588392320188319 ) ) ;
#20975=CARTESIAN_POINT ( 'NONE',  ( 124.0281414775786146, -1.834011780172310813, -8.268836392978581529 ) ) ;
#20977=CARTESIAN_POINT ( 'NONE',  ( 124.5539070589982060, -1.063912429576147511, -17.20460841810472985 ) ) ;
#20979=CARTESIAN_POINT ( 'NONE',  ( 115.5758681442453053, -1.561330072975668060, -17.79121239304076951 ) ) ;
#20980=CARTESIAN_POINT ( 'NONE',  ( 125.5597614775786326, -7.894159318335828068, -9.358103419637847864 ) ) ;
#20981=CARTESIAN_POINT ( 'NONE',  ( 122.6099748109119929, -9.261995988541697145, -16.69588392320189030 ) ) ;
#20982=CARTESIAN_POINT ( 'NONE',  ( 118.7525614775786380, -1.833838273342659253, -17.42832698103878286 ) ) ;
#20984=CARTESIAN_POINT ( 'NONE',  ( 117.3911214775786505, -1.561330072975668504, -17.79121239304076951 ) ) ;
#20986=CARTESIAN_POINT ( 'NONE',  ( 123.6877814775786533, -6.222761293078241884, -8.102969835052219238 ) ) ;
#20988=CARTESIAN_POINT ( 'NONE',  ( 110.2184548109119788, -3.410847707154508246, -16.57729307524250473 ) ) ;
#20989=CARTESIAN_POINT ( 'NONE',  ( 117.2776681442452968, -5.638512984488999180, -18.83840828888717311 ) ) ;
#20990=CARTESIAN_POINT ( 'NONE',  ( 124.2550481442452792, -0.1624402480850797581, -16.17319339645315424 ) ) ;
#20992=CARTESIAN_POINT ( 'NONE',  ( 136.0617147589318279, -1.217740506595299310, -8.750557032691128612 ) ) ;
#20993=CARTESIAN_POINT ( 'NONE',  ( 122.7234281442452755, -5.638512984488999180, -18.83840828888717311 ) ) ;
#20995=CARTESIAN_POINT ( 'NONE',  ( 119.1496481442453046, -6.222761293078241884, -8.102969835052219238 ) ) ;
#20998=CARTESIAN_POINT ( 'NONE',  ( 115.9162281442453235, -4.089484607189486809, -7.948022111789456723 ) ) ;
#21000=CARTESIAN_POINT ( 'NONE',  ( 125.7866681442452688, -8.899110576539710493, -16.42337572283490132 ) ) ;
#21001=CARTESIAN_POINT ( 'NONE',  ( 120.3409081442453044, -0.4660016031367703038, -10.09054647747476707 ) ) ;
#21003=CARTESIAN_POINT ( 'NONE',  ( 121.5888948109119809, -10.30919188438810075, -12.61870101168855918 ) ) ;
#21007=CARTESIAN_POINT ( 'NONE',  ( 122.8936081442453059, 0.2603800115204892296, -16.42320221600525088 ) ) ;
#21008=CARTESIAN_POINT ( 'NONE',  ( 118.0718414775786300, -9.261995988541697145, -16.69588392320189030 ) ) ;
#21009=CARTESIAN_POINT ( 'NONE',  ( 124.9357681442453014, -7.643976991954077427, -18.09477374809248928 ) ) ;
#21010=CARTESIAN_POINT ( 'NONE',  ( 118.5823814775786360, -7.643976991954077427, -18.09477374809248928 ) ) ;
#21012=CARTESIAN_POINT ( 'NONE',  ( 116.3133148109119759, -7.893985811506177619, -18.51759400769804742 ) ) ;
#21014=CARTESIAN_POINT ( 'NONE',  ( 124.9819548109120291, -7.618532446444632455, -18.05174138884769874 ) ) ;
#21019=CARTESIAN_POINT ( 'NONE',  ( 125.0954081442453401, -3.517672760958747702, -18.63504008191803152 ) ) ;
#21020=CARTESIAN_POINT ( 'NONE',  ( 124.8790414775786246, -8.899110576539710493, -16.42337572283490132 ) ) ;
#21022=CARTESIAN_POINT ( 'NONE',  ( 113.9307948109119764, -10.15424416112533912, -14.75197769757731336 ) ) ;
#21024=CARTESIAN_POINT ( 'NONE',  ( 122.1561614775786353, -8.899110576539724704, -16.42337572283488356 ) ) ;
#21025=CARTESIAN_POINT ( 'NONE',  ( 123.4608748109119745, -10.63000616557722466, -14.87417383870573495 ) ) ;
#21026=CARTESIAN_POINT ( 'NONE',  ( 123.8579614775786126, 0.5811942927096110934, -14.16772938898807510 ) ) ;
#21028=CARTESIAN_POINT ( 'NONE',  ( 113.7038881442453402, -3.383040157471821630, -19.15922257007629170 ) ) ;
#21031=VERTEX_POINT ( 'NONE', #15656 ) ;
#21032=CARTESIAN_POINT ( 'NONE',  ( 124.7503625628256714, -2.263366209404227281, -18.10533625161308180 ) ) ;
#21033=CARTESIAN_POINT ( 'NONE',  ( 115.0653281442453277, -3.505236298600246325, -18.68346056562440793 ) ) ;
#21034=CARTESIAN_POINT ( 'NONE',  ( 113.0231681442453322, 0.9020085738987339008, -11.91225656197089222 ) ) ;
#21038=CARTESIAN_POINT ( 'NONE',  ( 122.1561614775786353, -8.899110576539710493, -16.42337572283490132 ) ) ;
#21039=CARTESIAN_POINT ( 'NONE',  ( 118.4689281442453250, -10.15424416112533912, -14.75197769757731336 ) ) ;
#21040=CARTESIAN_POINT ( 'NONE',  ( 111.7751814775786556, -2.084020599724406786, -8.691656652584148546 ) ) ;
#21042=CARTESIAN_POINT ( 'NONE',  ( 125.5030348109119558, -6.222761293078241884, -8.102969835052219238 ) ) ;
#21044=CARTESIAN_POINT ( 'NONE',  ( 114.8951481442453115, -8.899110576539710493, -16.42337572283490132 ) ) ;
#21049=CARTESIAN_POINT ( 'NONE',  ( 120.3409081442453044, -8.899110576539710493, -16.42337572283490132 ) ) ;
#21050=CARTESIAN_POINT ( 'NONE',  ( 112.3991748109119868, -1.833838273342658809, -17.42832698103878286 ) ) ;
#21051=CARTESIAN_POINT ( 'NONE',  ( 114.7816948109119863, 0.5811942927096102052, -14.16772938898808221 ) ) ;
#21057=CARTESIAN_POINT ( 'NONE',  ( 111.8886348109120092, -3.383040157471821630, -19.15922257007629170 ) ) ;
#21058=CARTESIAN_POINT ( 'NONE',  ( 122.1561614775786353, -8.899110576539710493, -16.42337572283490132 ) ) ;
#21059=CARTESIAN_POINT ( 'NONE',  ( 119.3765548109119834, -10.15424416112533912, -14.75197769757731336 ) ) ;
#21060=CARTESIAN_POINT ( 'NONE',  ( 138.2184548109119930, -3.878253464830349273, -6.462969451276144639 ) ) ;
#21062=CARTESIAN_POINT ( 'NONE',  ( 115.0086014775786509, -5.574606645277164318, -18.38911715685844683 ) ) ;
#21064=CARTESIAN_POINT ( 'NONE',  ( 125.1269327111056953, -1.267766418764818770, -16.93314635290698078 ) ) ;
#21067=CARTESIAN_POINT ( 'NONE',  ( 114.9518748109119883, -1.834011780172310813, -8.268836392978581529 ) ) ;
#21069=CARTESIAN_POINT ( 'NONE',  ( 113.1933481442453058, -4.089484607189486809, -7.948022111789456723 ) ) ;
#21070=CIRCLE ( 'NONE', #13794, 3.999999999999997780 ) ;
#21073=CARTESIAN_POINT ( 'NONE',  ( 114.2144281442453178, -8.166667518702817929, -8.995218007635859436 ) ) ;
#21074=CARTESIAN_POINT ( 'NONE',  ( 114.3278814775786429, -10.30919188438810075, -12.61870101168855918 ) ) ;
#21075=CARTESIAN_POINT ( 'NONE',  ( 121.9292548109119849, -7.894159318335828068, -9.358103419637847864 ) ) ;
#21078=CARTESIAN_POINT ( 'NONE',  ( 112.0435892294923974, -2.263366209404214402, -18.10533625161307114 ) ) ;
#21080=CARTESIAN_POINT ( 'NONE',  ( 116.2565881442453133, -0.8288870151387760510, -10.36305467784173118 ) ) ;
#21084=CARTESIAN_POINT ( 'NONE',  ( 121.7136302882355068, -1.135392229370310258, -17.10942237759953244 ) ) ;
#21085=CARTESIAN_POINT ( 'NONE',  ( 124.1415948109119540, -6.344957434206665248, -7.627207830600338134 ) ) ;
#21086=CARTESIAN_POINT ( 'NONE',  ( 125.2194014775786286, -10.30919188438810075, -12.61870101168855918 ) ) ;
#21088=CARTESIAN_POINT ( 'NONE',  ( 117.3343948109119737, -3.383040157471821630, -19.15922257007629170 ) ) ;
#21090=CARTESIAN_POINT ( 'NONE',  ( 114.3278814775786429, 0.1319031606808879209, -14.10382304977623669 ) ) ;
#21091=CARTESIAN_POINT ( 'NONE',  ( 112.9664414775786412, 0.5811942927096154232, -14.16772938898807155 ) ) ;
#21092=CARTESIAN_POINT ( 'NONE',  ( 118.1852948109119836, -5.638512984488999180, -18.83840828888717311 ) ) ;
#21093=CARTESIAN_POINT ( 'NONE',  ( 117.5613014775786525, -10.15424416112533912, -14.75197769757731336 ) ) ;
#21094=ORIENTED_EDGE ( 'NONE', *, *, #34810, .T. ) ;
#21095=CARTESIAN_POINT ( 'NONE',  ( 121.7023481442452777, -0.8288870151387760510, -10.36305467784173118 ) ) ;
#21096=CARTESIAN_POINT ( 'NONE',  ( 116.6536748109119941, 0.9020085738987339008, -11.91225656197089222 ) ) ;
#21105=CARTESIAN_POINT ( 'NONE',  ( 115.0653281442453277, -6.344957434206662583, -7.627207830600332805 ) ) ;
#21108=CARTESIAN_POINT ( 'NONE',  ( 113.7606148109119886, -7.894159318335828068, -9.358103419637847864 ) ) ;
#21112=CARTESIAN_POINT ( 'NONE',  ( 115.2878193026122915, -1.179503403430490538, -17.05068175419388865 ) ) ;
#21114=CARTESIAN_POINT ( 'NONE',  ( 117.5613014775786525, 0.9020085738987339008, -11.91225656197089222 ) ) ;
#21119=CARTESIAN_POINT ( 'NONE',  ( 114.7816948109119863, 0.5811942927096154232, -14.16772938898807155 ) ) ;
#21120=CARTESIAN_POINT ( 'NONE',  ( 123.2906948109119867, -1.833838273342659697, -17.42832698103878286 ) ) ;
#21121=CARTESIAN_POINT ( 'NONE',  ( 119.7169148109119874, -0.1624402480850797581, -16.17319339645315424 ) ) ;
#21122=VERTEX_POINT ( 'NONE', #28269 ) ;
#21123=CARTESIAN_POINT ( 'NONE',  ( 135.5837700375767554, -9.599696963706330521, -9.723723590361398550 ) ) ;
#21124=CARTESIAN_POINT ( 'NONE',  ( 123.2906948109119867, -8.166667518702819706, -8.995218007635861213 ) ) ;
#21126=CARTESIAN_POINT ( 'NONE',  ( 114.3846081442453197, 0.4262465694468514643, -12.03445270309931736 ) ) ;
#21127=CARTESIAN_POINT ( 'NONE',  ( 114.4980614775786734, -2.084020599724406786, -8.691656652584148546 ) ) ;
#21130=CARTESIAN_POINT ( 'NONE',  ( 118.8092881442453290, -0.1624402480850797581, -16.17319339645315424 ) ) ;
#21131=CARTESIAN_POINT ( 'NONE',  ( 121.3619881442452879, -5.574606645277164318, -18.38911715685844683 ) ) ;
#21139=CARTESIAN_POINT ( 'NONE',  ( 117.1642148109119859, -9.261995988541697145, -16.69588392320189030 ) ) ;
#21140=CARTESIAN_POINT ( 'NONE',  ( 115.0086014775786509, -4.089484607189486809, -7.948022111789456723 ) ) ;
#21147=CARTESIAN_POINT ( 'NONE',  ( 120.6245414775786458, -9.988377603198976828, -10.36322818467138340 ) ) ;
#21149=CARTESIAN_POINT ( 'NONE',  ( 112.0588148109119828, 0.5811942927096154232, -14.16772938898807155 ) ) ;
#21150=CARTESIAN_POINT ( 'NONE',  ( 123.8012348109119642, -9.565557343593413364, -10.61323700422348004 ) ) ;
#21152=CARTESIAN_POINT ( 'NONE',  ( 111.2646414775786496, -8.899110576539710493, -16.42337572283490132 ) ) ;
#21153=CARTESIAN_POINT ( 'NONE',  ( 120.2841814775786276, 0.9020085738987339008, -11.91225656197089222 ) ) ;
#21155=CARTESIAN_POINT ( 'NONE',  ( 115.9162281442453093, -5.574606645277164318, -18.38911715685844683 ) ) ;
#21156=CARTESIAN_POINT ( 'NONE',  ( 111.4241771286805260, -2.495269033102075262, -17.79652296963211455 ) ) ;
#21157=VERTEX_POINT ( 'NONE', #40041 ) ;
#21158=CARTESIAN_POINT ( 'NONE',  ( 120.6812681442452941, -10.30919188438810075, -12.61870101168855918 ) ) ;
#21160=CARTESIAN_POINT ( 'NONE',  ( 114.6115148109119986, -3.383040157471821630, -19.15922257007629170 ) ) ;
#21163=CARTESIAN_POINT ( 'NONE',  ( 124.5954081442453116, -3.383040157471821630, -19.15922257007629170 ) ) ;
#21165=B_SPLINE_CURVE_WITH_KNOTS ( 'NONE', 3,
 ( #34194, #44712, #34413, #2968 ),
 .UNSPECIFIED., .F., .F.,
 ( 4, 4 ),
 ( 0.000000000000000000, 1.000000000000000000 ),
 .UNSPECIFIED. ) ;
#21166=CARTESIAN_POINT ( 'NONE',  ( 122.7234281442452755, -5.638512984489030266, -18.83840828888716601 ) ) ;
#21167=CARTESIAN_POINT ( 'NONE',  ( 116.2565881442453133, -0.8288870151387760510, -10.36305467784173118 ) ) ;
#21169=CARTESIAN_POINT ( 'NONE',  ( 120.2274548109119934, -9.859900752359378018, -12.68260735090039759 ) ) ;
#21170=CARTESIAN_POINT ( 'NONE',  ( 120.1339464975817748, -2.215723800389698184, -18.16877924232191788 ) ) ;
#21171=CARTESIAN_POINT ( 'NONE',  ( 121.7023481442452777, -0.8288870151387760510, -10.36305467784173118 ) ) ;
#21172=EDGE_CURVE ( 'NONE', #38570, #31472, #1956, .T. ) ;
#21174=DIRECTION ( 'NONE',  ( 1.000000000000000000, 0.000000000000000000, 0.000000000000000000 ) ) ;
#21175=CARTESIAN_POINT ( 'NONE',  ( 118.2987481442453088, -7.894159318335828068, -9.358103419637847864 ) ) ;
#21178=CARTESIAN_POINT ( 'NONE',  ( 114.8951481442453115, -0.4660016031367893996, -10.09054647747474043 ) ) ;
#21180=CARTESIAN_POINT ( 'NONE',  ( 121.9292548109119849, -7.894159318335828068, -9.358103419637847864 ) ) ;
#21182=CARTESIAN_POINT ( 'NONE',  ( 116.4834948109119779, -1.561330072975668504, -17.79121239304076951 ) ) ;
#21187=CARTESIAN_POINT ( 'NONE',  ( 120.9649014775786355, -3.383040157471821630, -19.15922257007629170 ) ) ;
#21188=ORIENTED_EDGE ( 'NONE', *, *, #15264, .F. ) ;
#21190=CARTESIAN_POINT ( 'NONE',  ( 117.7314814775786260, -5.574606645277164318, -18.38911715685844683 ) ) ;
#21194=CARTESIAN_POINT ( 'NONE',  ( 111.4665458264767750, -1.295815253274133161, -16.89579513612386563 ) ) ;
#21197=ORIENTED_EDGE ( 'NONE', *, *, #9730, .T. ) ;
#21198=CARTESIAN_POINT ( 'NONE',  ( 113.8173414775786512, 0.2603800115204892296, -16.42320221600525088 ) ) ;
#21199=CARTESIAN_POINT ( 'NONE',  ( 112.9664414775786412, 0.5811942927096154232, -14.16772938898807155 ) ) ;
#21200=CARTESIAN_POINT ( 'NONE',  ( 121.8158014775786171, -5.638512984488999180, -18.83840828888717311 ) ) ;
#21201=CARTESIAN_POINT ( 'NONE',  ( 115.4624148109119943, -4.153390946401321671, -8.397313243818183892 ) ) ;
#21203=CARTESIAN_POINT ( 'NONE',  ( 120.3409081442453044, -0.4660016031367893996, -10.09054647747474043 ) ) ;
#21204=CARTESIAN_POINT ( 'NONE',  ( 111.6050014775786536, 0.1319031606808879209, -14.10382304977623669 ) ) ;
#21208=CARTESIAN_POINT ( 'NONE',  ( 122.1561614775786353, -8.899110576539710493, -16.42337572283490132 ) ) ;
#21212=CARTESIAN_POINT ( 'NONE',  ( 115.2355081442453155, -10.30919188438810075, -12.61870101168855918 ) ) ;
#21213=CARTESIAN_POINT ( 'NONE',  ( 125.1059481442452750, -1.833838273342660141, -17.42832698103878286 ) ) ;
#21217=CARTESIAN_POINT ( 'NONE',  ( 136.4173705901518190, 0.4780847289399532962, -11.17367218403365925 ) ) ;
#21218=CARTESIAN_POINT ( 'NONE',  ( 123.2339681442453241, -6.344957434206665248, -7.627207830600338134 ) ) ;
#21220=CARTESIAN_POINT ( 'NONE',  ( 119.4900081442453086, -7.643976991954077427, -18.09477374809248928 ) ) ;
#21221=ORIENTED_EDGE ( 'NONE', *, *, #26446, .F. ) ;
#21222=CARTESIAN_POINT ( 'NONE',  ( 113.5337081442453240, -9.261995988541697145, -16.69588392320189030 ) ) ;
#21223=CARTESIAN_POINT ( 'NONE',  ( 124.1415948109119540, -3.505236298600246325, -18.68346056562440793 ) ) ;
#21226=CARTESIAN_POINT ( 'NONE',  ( 124.4819548109119722, -7.893985811506177619, -18.51759400769804742 ) ) ;
#21230=CARTESIAN_POINT ( 'NONE',  ( 123.6310548109119765, -5.638512984488999180, -18.83840828888717311 ) ) ;
#21231=CARTESIAN_POINT ( 'NONE',  ( 121.3052614775786111, -1.834011780172310813, -8.268836392978581529 ) ) ;
#21232=CARTESIAN_POINT ( 'NONE',  ( 122.6099748109119929, -0.8288870151387760510, -10.36305467784173118 ) ) ;
#21233=CARTESIAN_POINT ( 'NONE',  ( 119.0361948109119652, -2.084020599724406786, -8.691656652584148546 ) ) ;
#21235=CARTESIAN_POINT ( 'NONE',  ( 125.3790414775786388, -0.8658195297466895202, -10.39078908864337514 ) ) ;
#21236=CARTESIAN_POINT ( 'NONE',  ( 114.8951481442453115, -0.4660016031367893996, -10.09054647747474043 ) ) ;
#21243=CARTESIAN_POINT ( 'NONE',  ( 125.3328548109119964, -9.261995988541697145, -16.69588392320189030 ) ) ;
#21244=CARTESIAN_POINT ( 'NONE',  ( 125.4463081442452932, -4.153390946401325223, -8.397313243818185668 ) ) ;
#21246=CARTESIAN_POINT ( 'NONE',  ( 111.8319081442453182, -4.153390946401321671, -8.397313243818183892 ) ) ;
#21249=CARTESIAN_POINT ( 'NONE',  ( 123.9714148109119805, -0.4660016031367893996, -10.09054647747474043 ) ) ;
#21250=CARTESIAN_POINT ( 'NONE',  ( 125.9568481442452850, -6.344957434206665248, -7.627207830600338134 ) ) ;
#21252=CARTESIAN_POINT ( 'NONE',  ( 115.9162281442453235, -4.089484607189486809, -7.948022111789456723 ) ) ;
#21256=CARTESIAN_POINT ( 'NONE',  ( 126.9276200068739655, -7.231923266987396737, -8.590624321703938193 ) ) ;
#21257=CARTESIAN_POINT ( 'NONE',  ( 115.4624148109119943, -4.153390946401321671, -8.397313243818183892 ) ) ;
#21258=CARTESIAN_POINT ( 'NONE',  ( 114.2711548109119803, -9.988377603198976828, -10.36322818467138340 ) ) ;
#21262=CARTESIAN_POINT ( 'NONE',  ( 120.1140014775786398, -7.894159318335828068, -9.358103419637847864 ) ) ;
#21263=CARTESIAN_POINT ( 'NONE',  ( 119.3765548109119834, -10.15424416112533912, -14.75197769757731336 ) ) ;
#21264=CARTESIAN_POINT ( 'NONE',  ( 125.9568481442452850, -6.344957434206665248, -7.627207830600338134 ) ) ;
#21266=CARTESIAN_POINT ( 'NONE',  ( 124.3117748109119844, 0.1319031606808879209, -14.10382304977623669 ) ) ;
#21268=CARTESIAN_POINT ( 'NONE',  ( 115.5758681442453053, -7.894159318335828068, -9.358103419637847864 ) ) ;
#21269=ORIENTED_EDGE ( 'NONE', *, *, #18100, .T. ) ;
#21270=CARTESIAN_POINT ( 'NONE',  ( 126.2275303246267697, -8.934542061787519529, -16.30473108686274131 ) ) ;
#21273=ORIENTED_EDGE ( 'NONE', *, *, #40117, .T. ) ;
#21274=CARTESIAN_POINT ( 'NONE',  ( 120.1140014775786398, -7.894159318335828068, -9.358103419637847864 ) ) ;
#21275=CARTESIAN_POINT ( 'NONE',  ( 114.6682414775786469, -7.894159318335828068, -9.358103419637847864 ) ) ;
#21281=CARTESIAN_POINT ( 'NONE',  ( 114.4413348109119823, -9.261995988541697145, -16.69588392320189030 ) ) ;
#21282=CARTESIAN_POINT ( 'NONE',  ( 125.2761281442453054, 0.4262465694468514643, -12.03445270309931736 ) ) ;
#21283=CARTESIAN_POINT ( 'NONE',  ( 116.0296814775786345, -1.833838273342658809, -17.42832698103878286 ) ) ;
#21284=FACE_OUTER_BOUND ( 'NONE', #20560, .T. ) ;
#21287=CARTESIAN_POINT ( 'NONE',  ( 114.8384214775786489, -10.15424416112533912, -14.75197769757731336 ) ) ;
#21293=CARTESIAN_POINT ( 'NONE',  ( 115.6893214775786447, 0.5811942927096154232, -14.16772938898807155 ) ) ;
#21296=CARTESIAN_POINT ( 'NONE',  ( 118.2420214775786320, -3.383040157471821630, -19.15922257007629170 ) ) ;
#21299=CARTESIAN_POINT ( 'NONE',  ( 114.5547881442453217, -5.638512984488999180, -18.83840828888717311 ) ) ;
#21300=CARTESIAN_POINT ( 'NONE',  ( 113.2500748109119968, -6.344957434206662583, -7.627207830600332805 ) ) ;
#21302=CARTESIAN_POINT ( 'NONE',  ( 124.1415948109119540, -3.505236298600246325, -18.68346056562440793 ) ) ;
#21308=CARTESIAN_POINT ( 'NONE',  ( 115.0653281442453277, -3.505236298600246325, -18.68346056562440793 ) ) ;
#21314=CARTESIAN_POINT ( 'NONE',  ( 124.7655881442452852, 0.5811942927096110934, -14.16772938898807510 ) ) ;
#21315=CARTESIAN_POINT ( 'NONE',  ( 138.2184548109119930, -6.243778871467079661, -12.80482167309617125 ) ) ;
#21316=CARTESIAN_POINT ( 'NONE',  ( 124.4819548109119722, -7.893985811506177619, -18.51759400769804742 ) ) ;
#21317=CARTESIAN_POINT ( 'NONE',  ( 116.5402214775786405, 0.2603800115204892296, -16.42320221600525088 ) ) ;
#21319=CARTESIAN_POINT ( 'NONE',  ( 114.2711548109119803, -0.1624402480850797581, -16.17319339645315424 ) ) ;
#21320=CARTESIAN_POINT ( 'NONE',  ( 125.7866681442452688, -0.4660016031367893996, -10.09054647747474043 ) ) ;
#21321=CARTESIAN_POINT ( 'NONE',  ( 117.9016614775786280, -9.988377603198976828, -10.36322818467138340 ) ) ;
#21322=CARTESIAN_POINT ( 'NONE',  ( 118.0151148109119816, 0.4262465694468514643, -12.03445270309931736 ) ) ;
#21324=CARTESIAN_POINT ( 'NONE',  ( 119.7169148109119874, -0.1624402480850797581, -16.17319339645315424 ) ) ;
#21327=CARTESIAN_POINT ( 'NONE',  ( 117.5045748109119756, 0.5811942927096110934, -14.16772938898807510 ) ) ;
#21328=CARTESIAN_POINT ( 'NONE',  ( 136.3685138707383828, 0.4973853706319558143, -15.62000875385643184 ) ) ;
#21331=CARTESIAN_POINT ( 'NONE',  ( 126.2364674775771647, 0.1186143222450094931, -13.91482113796701547 ) ) ;
#21334=CARTESIAN_POINT ( 'NONE',  ( 115.7460481442453357, 0.9020085738987339008, -11.91225656197089222 ) ) ;
#21335=CARTESIAN_POINT ( 'NONE',  ( 135.9690293846602458, -10.74668130430289814, -14.11119591414773566 ) ) ;
#21336=CARTESIAN_POINT ( 'NONE',  ( 112.1722681442453222, -8.899110576539710493, -16.42337572283490132 ) ) ;
#21338=CARTESIAN_POINT ( 'NONE',  ( 117.1074881442453233, 0.4262465694468589028, -12.03445270309934578 ) ) ;
#21340=CARTESIAN_POINT ( 'NONE',  ( 112.9097148109120070, -9.565557343593413364, -10.61323700422348004 ) ) ;
#21343=CARTESIAN_POINT ( 'NONE',  ( 118.4122014775786340, 0.5811942927096084288, -14.16772938898808931 ) ) ;
#21344=CARTESIAN_POINT ( 'NONE',  ( 116.6536748109119941, 0.9020085738987339008, -11.91225656197089222 ) ) ;
#21345=CARTESIAN_POINT ( 'NONE',  ( 123.9146881442452894, -10.15424416112533912, -14.75197769757731336 ) ) ;
#21346=CARTESIAN_POINT ( 'NONE',  ( 117.5045748109119756, -9.859900752359374465, -12.68260735090039404 ) ) ;
#21348=CARTESIAN_POINT ( 'NONE',  ( 136.5935259641815094, -7.096270167259992157, -8.139588474309226385 ) ) ;
#21349=CARTESIAN_POINT ( 'NONE',  ( 123.6877814775786533, -3.383040157471821630, -19.15922257007629170 ) ) ;
#21351=CARTESIAN_POINT ( 'NONE',  ( 121.0216281442452981, -7.894159318335828068, -9.358103419637847864 ) ) ;
#21352=CARTESIAN_POINT ( 'NONE',  ( 111.4348214775786801, -3.505236298600246325, -18.68346056562440793 ) ) ;
#21355=CARTESIAN_POINT ( 'NONE',  ( 118.7525614775786380, -1.833838273342659253, -17.42832698103878286 ) ) ;
#21357=CARTESIAN_POINT ( 'NONE',  ( 121.7023481442452777, -0.8288870151387760510, -10.36305467784173118 ) ) ;
#21358=CARTESIAN_POINT ( 'NONE',  ( 114.5547881442453217, -4.153390946401313677, -8.397313243818183892 ) ) ;
#21363=CARTESIAN_POINT ( 'NONE',  ( 116.7671281442453335, -1.834011780172310813, -8.268836392978581529 ) ) ;
#21364=CARTESIAN_POINT ( 'NONE',  ( 116.4267681442453153, -3.383040157471821630, -19.15922257007629170 ) ) ;
#21366=CARTESIAN_POINT ( 'NONE',  ( 113.4202548109119846, -10.30919188438810075, -12.61870101168855918 ) ) ;
#21370=CARTESIAN_POINT ( 'NONE',  ( 122.6667014775786413, -7.893985811506177619, -18.51759400769804742 ) ) ;
#21371=CARTESIAN_POINT ( 'NONE',  ( 115.2922348109119781, -10.63000616557722466, -14.87417383870573495 ) ) ;
#21372=CARTESIAN_POINT ( 'NONE',  ( 121.8725281442453223, -6.222761293078241884, -8.102969835052219238 ) ) ;
#21373=CARTESIAN_POINT ( 'NONE',  ( 111.4915481442453142, -1.833838273342658365, -17.42832698103878286 ) ) ;
#21374=CARTESIAN_POINT ( 'NONE',  ( 122.6667014775786413, -7.893985811506177619, -18.51759400769804742 ) ) ;
#21375=ADVANCED_FACE ( 'NONE', ( #44380 ), #19933, .T. ) ;
#21377=CARTESIAN_POINT ( 'NONE',  ( 115.2922348109119781, 0.4262465694468514643, -12.03445270309931736 ) ) ;
#21380=CARTESIAN_POINT ( 'NONE',  ( 123.2906948109119867, -8.166667518702819706, -8.995218007635861213 ) ) ;
#21383=CARTESIAN_POINT ( 'NONE',  ( 118.7525614775786380, -8.166667518702819706, -8.995218007635861213 ) ) ;
#21387=CARTESIAN_POINT ( 'NONE',  ( 123.6877814775786533, -3.383040157471821630, -19.15922257007629170 ) ) ;
#21388=CARTESIAN_POINT ( 'NONE',  ( 120.0214764273310095, -2.236191541394345172, -18.14152338500401029 ) ) ;
#21389=CARTESIAN_POINT ( 'NONE',  ( 116.1431348109119881, 0.1319031606808879209, -14.10382304977623669 ) ) ;
#21392=CARTESIAN_POINT ( 'NONE',  ( 118.2987481442453088, -7.894159318335828068, -9.358103419637847864 ) ) ;
#21394=ADVANCED_FACE ( 'NONE', ( #12692 ), #30559, .T. ) ;
#21396=CARTESIAN_POINT ( 'NONE',  ( 119.8870948109119752, -0.8288870151387760510, -10.36305467784173118 ) ) ;
#21399=CARTESIAN_POINT ( 'NONE',  ( 118.8092881442453290, -0.1624402480850797581, -16.17319339645315424 ) ) ;
#21401=CARTESIAN_POINT ( 'NONE',  ( 116.5969481442453031, 0.5811942927096154232, -14.16772938898807155 ) ) ;
#21402=CARTESIAN_POINT ( 'NONE',  ( 113.2500748109119968, -6.344957434206662583, -7.627207830600332805 ) ) ;
#21404=CARTESIAN_POINT ( 'NONE',  ( 120.1140014775786398, -7.894159318335828068, -9.358103419637847864 ) ) ;
#21406=CARTESIAN_POINT ( 'NONE',  ( 116.5969481442453031, 0.5811942927096154232, -14.16772938898807155 ) ) ;
#21410=CARTESIAN_POINT ( 'NONE',  ( 127.9644000028953030, -4.197576873768148253, -15.52951870415910207 ) ) ;
#21411=CARTESIAN_POINT ( 'NONE',  ( 121.9859814775786333, 0.2603800115204892296, -16.42320221600525088 ) ) ;
#21414=CARTESIAN_POINT ( 'NONE',  ( 122.3263414775786373, -3.505236298600246325, -18.68346056562440793 ) ) ;
#21416=CARTESIAN_POINT ( 'NONE',  ( 125.4463081442452932, -5.638512984488999180, -18.83840828888717311 ) ) ;
#21420=CARTESIAN_POINT ( 'NONE',  ( 116.3700414775786527, -5.638512984488999180, -18.83840828888717311 ) ) ;
#21421=CARTESIAN_POINT ( 'NONE',  ( 125.8433948109119456, -7.643976991954077427, -18.09477374809248928 ) ) ;
#21422=CARTESIAN_POINT ( 'NONE',  ( 124.1983214775786166, -8.166667518702819706, -8.995218007635861213 ) ) ;
#21423=CARTESIAN_POINT ( 'NONE',  ( 121.7590748109119687, -2.084020599724406786, -8.691656652584148546 ) ) ;
#21426=CARTESIAN_POINT ( 'NONE',  ( 124.0281414775786146, -1.834011780172310813, -8.268836392978581529 ) ) ;
#21427=CARTESIAN_POINT ( 'NONE',  ( 111.8991748109119868, -7.866424907533402511, -9.395035934245173692 ) ) ;
#21431=CARTESIAN_POINT ( 'NONE',  ( 125.2761281442453054, 0.4262465694468514643, -12.03445270309931736 ) ) ;
#21434=ADVANCED_FACE ( 'NONE', ( #43080 ), #44560, .T. ) ;
#21436=CARTESIAN_POINT ( 'NONE',  ( 120.2841814775786276, 0.9020085738987339008, -11.91225656197089222 ) ) ;
#21437=CARTESIAN_POINT ( 'NONE',  ( 123.2339681442453241, -3.505236298600246325, -18.68346056562440793 ) ) ;
#21440=CARTESIAN_POINT ( 'NONE',  ( 123.2906948109119867, -8.166667518702819706, -8.995218007635861213 ) ) ;
#21442=CARTESIAN_POINT ( 'NONE',  ( 122.2128881442453263, -7.643976991954077427, -18.09477374809248928 ) ) ;
#21445=CARTESIAN_POINT ( 'NONE',  ( 115.2922348109119781, -10.63000616557722466, -14.87417383870573495 ) ) ;
#21448=EDGE_CURVE ( 'NONE', #11237, #22820, #11641, .T. ) ;
#21449=CARTESIAN_POINT ( 'NONE',  ( 135.9373687277988836, -5.586066061336491195, -7.503848139453651811 ) ) ;
#21451=CARTESIAN_POINT ( 'NONE',  ( 111.7184548109119788, -0.8288870151387760510, -10.36305467784173118 ) ) ;
#21454=CARTESIAN_POINT ( 'NONE',  ( 122.0994348109119443, 0.9020085738987339008, -11.91225656197089222 ) ) ;
#21455=CARTESIAN_POINT ( 'NONE',  ( 121.8725281442453223, -3.383040157471821630, -19.15922257007629170 ) ) ;
#21456=CARTESIAN_POINT ( 'NONE',  ( 124.0281414775786146, -7.643976991954077427, -18.09477374809248928 ) ) ;
#21457=CARTESIAN_POINT ( 'NONE',  ( 118.4122014775786340, -9.859900752359374465, -12.68260735090039404 ) ) ;
#21459=CARTESIAN_POINT ( 'NONE',  ( 118.3554748109119998, 0.2603800115204892296, -16.42320221600525088 ) ) ;
#21463=CARTESIAN_POINT ( 'NONE',  ( 125.6164881442453094, -9.565557343593953377, -10.61323700422440197 ) ) ;
#21467=CARTESIAN_POINT ( 'NONE',  ( 125.5597614775786326, -1.561330072975669392, -17.79121239304076951 ) ) ;
#21468=CARTESIAN_POINT ( 'NONE',  ( 112.4559014775786494, -9.988377603198976828, -10.36322818467138340 ) ) ;
#21470=CARTESIAN_POINT ( 'NONE',  ( 112.7962614775786676, -6.222761293078241884, -8.102969835052219238 ) ) ;
#21474=CARTESIAN_POINT ( 'NONE',  ( 123.4041481442452834, -10.30919188438810075, -12.61870101168855918 ) ) ;
#21476=CARTESIAN_POINT ( 'NONE',  ( 115.5191414775786569, -3.383040157471821630, -19.15922257007629170 ) ) ;
#21481=CARTESIAN_POINT ( 'NONE',  ( 116.5402214775786405, -9.565557343593413364, -10.61323700422348004 ) ) ;
#21482=CARTESIAN_POINT ( 'NONE',  ( 126.5241148109119393, -9.565557343593413364, -10.61323700422348004 ) ) ;
#21483=CARTESIAN_POINT ( 'NONE',  ( 113.1366214775786432, -1.834011780172310813, -8.268836392978581529 ) ) ;
#21485=CARTESIAN_POINT ( 'NONE',  ( 118.3554748109119998, -9.565557343593413364, -10.61323700422348004 ) ) ;
#21486=CARTESIAN_POINT ( 'NONE',  ( 114.1009748109119784, -5.574606645277164318, -18.38911715685844683 ) ) ;
#21489=CARTESIAN_POINT ( 'NONE',  ( 125.3328548109119964, -0.8288870151387760510, -10.36305467784173118 ) ) ;
#21491=CARTESIAN_POINT ( 'NONE',  ( 113.8740681442453138, -9.859900752359374465, -12.68260735090039404 ) ) ;
#21493=CARTESIAN_POINT ( 'NONE',  ( 126.4852516627922085, -9.308055734194462971, -15.96268377075503153 ) ) ;
#21497=CARTESIAN_POINT ( 'NONE',  ( 122.8368814775786291, -7.894159318335828068, -9.358103419637847864 ) ) ;
#21499=CARTESIAN_POINT ( 'NONE',  ( 118.8660148109119774, 0.1319031606808879209, -14.10382304977623669 ) ) ;
#21500=CARTESIAN_POINT ( 'NONE',  ( 118.2420214775786320, -6.222761293078241884, -8.102969835052219238 ) ) ;
#21509=CARTESIAN_POINT ( 'NONE',  ( 112.3991748109119868, -8.166667518702817929, -8.995218007635859436 ) ) ;
#21511=CARTESIAN_POINT ( 'NONE',  ( 116.6536748109119941, -10.15424416112533912, -14.75197769757731336 ) ) ;
#21512=DIRECTION ( 'NONE',  ( 0.000000000000000000, 0.7996358532186281787, 0.6004852223388320587 ) ) ;
#21513=ORIENTED_EDGE ( 'NONE', *, *, #35998, .T. ) ;
#21515=CARTESIAN_POINT ( 'NONE',  ( 116.5402214775786405, -9.565557343593413364, -10.61323700422348004 ) ) ;
#21519=CARTESIAN_POINT ( 'NONE',  ( 115.1220548109119761, -8.166667518702817929, -8.995218007635861213 ) ) ;
#21521=CARTESIAN_POINT ( 'NONE',  ( 115.9729548109119861, -6.344957434206662583, -7.627207830600332805 ) ) ;
#21524=CARTESIAN_POINT ( 'NONE',  ( 126.3539348109119800, -4.153390946401325223, -8.397313243818185668 ) ) ;
#21525=CARTESIAN_POINT ( 'NONE',  ( 112.4559014775786494, -9.988377603198976828, -10.36322818467138340 ) ) ;
#21526=CARTESIAN_POINT ( 'NONE',  ( 128.2184548109119930, -10.81584935473217080, -14.15181583611863303 ) ) ;
#21529=VERTEX_POINT ( 'NONE', #44225 ) ;
#21532=CARTESIAN_POINT ( 'NONE',  ( 115.1220548109119761, -1.833838273342658809, -17.42832698103878286 ) ) ;
#21538=CARTESIAN_POINT ( 'NONE',  ( 114.3278814775786429, 0.1319031606808879209, -14.10382304977623669 ) ) ;
#21540=CARTESIAN_POINT ( 'NONE',  ( 124.6521348109119884, -1.561330072975668948, -17.79121239304076951 ) ) ;
#21541=CARTESIAN_POINT ( 'NONE',  ( 114.9518748109119883, -1.834011780172310813, -8.268836392978581529 ) ) ;
#21543=CARTESIAN_POINT ( 'NONE',  ( 116.1998614775786507, 0.4262465694468514643, -12.03445270309931736 ) ) ;
#21545=CARTESIAN_POINT ( 'NONE',  ( 116.4834948109119779, -1.561330072975668504, -17.79121239304076951 ) ) ;
#21546=CARTESIAN_POINT ( 'NONE',  ( 115.6893214775786447, -9.859900752359374465, -12.68260735090039404 ) ) ;
#21547=ORIENTED_EDGE ( 'NONE', *, *, #36066, .F. ) ;
#21548=CARTESIAN_POINT ( 'NONE',  ( 121.5888948109119809, 0.1319031606808879209, -14.10382304977623669 ) ) ;
#21550=CARTESIAN_POINT ( 'NONE',  ( 116.8238548109119819, -4.089484607189486809, -7.948022111789456723 ) ) ;
#21552=CARTESIAN_POINT ( 'NONE',  ( 136.0647682600814221, 0.5678772681889172613, -15.70378451066936698 ) ) ;
#21555=CYLINDRICAL_SURFACE ( 'NONE', #28848, 1.999999999999998890 ) ;
#21557=CARTESIAN_POINT ( 'NONE',  ( 115.3489614775786407, -9.261995988541697145, -16.69588392320189030 ) ) ;
#21559=VECTOR ( 'NONE', #40901, 1000.000000000000000 ) ;
#21561=CARTESIAN_POINT ( 'NONE',  ( 115.9729548109119861, -3.505236298600246325, -18.68346056562440793 ) ) ;
#21563=CARTESIAN_POINT ( 'NONE',  ( 116.9582927111058552, -1.267766418764730840, -16.93314635290706605 ) ) ;
#21565=CARTESIAN_POINT ( 'NONE',  ( 113.7606148109119886, -7.894159318335828068, -9.358103419637847864 ) ) ;
#21570=CARTESIAN_POINT ( 'NONE',  ( 119.9438214775786378, -7.893985811506177619, -18.51759400769804742 ) ) ;
#21571=CARTESIAN_POINT ( 'NONE',  ( 118.0718414775786442, -0.8288870151387760510, -10.36305467784173118 ) ) ;
#21572=CARTESIAN_POINT ( 'NONE',  ( 125.1626748109119802, -9.988377603198980381, -10.36322818467138518 ) ) ;
#21573=ORIENTED_EDGE ( 'NONE', *, *, #39829, .T. ) ;
#21575=CARTESIAN_POINT ( 'NONE',  ( 123.5743281442453139, -7.893985811506177619, -18.51759400769804742 ) ) ;
#21577=CARTESIAN_POINT ( 'NONE',  ( 119.7169148109119874, -0.1624402480850797581, -16.17319339645315424 ) ) ;
#21579=CARTESIAN_POINT ( 'NONE',  ( 116.4834948109119779, -7.894159318335828068, -9.358103419637847864 ) ) ;
#21582=CARTESIAN_POINT ( 'NONE',  ( 121.5321681442453183, -0.1624402480850797581, -16.17319339645315424 ) ) ;
#21583=CARTESIAN_POINT ( 'NONE',  ( 124.9924948109119924, -5.574606645277164318, -18.38911715685844683 ) ) ;
#21584=CARTESIAN_POINT ( 'NONE',  ( 116.8689514802850198, -3.929494816604741203, -18.62311481910882804 ) ) ;
#21588=SHAPE_REPRESENTATION ( 'Barrel Adjuster Screw', ( #12375 ), #14045 ) ;
#21590=CARTESIAN_POINT ( 'NONE',  ( 116.9373081442452929, -8.166667518702817929, -8.995218007635861213 ) ) ;
#21591=CARTESIAN_POINT ( 'NONE',  ( 113.1933481442453058, -4.089484607189486809, -7.948022111789456723 ) ) ;
#21593=CARTESIAN_POINT ( 'NONE',  ( 114.6115148109119986, -3.383040157471821630, -19.15922257007629170 ) ) ;
#21594=ORIENTED_EDGE ( 'NONE', *, *, #40451, .F. ) ;
#21596=CARTESIAN_POINT ( 'NONE',  ( 124.4819548109119722, -7.893985811506177619, -18.51759400769804742 ) ) ;
#21597=CARTESIAN_POINT ( 'NONE',  ( 115.4056881442453459, -7.893985811506177619, -18.51759400769804742 ) ) ;
#21598=CARTESIAN_POINT ( 'NONE',  ( 120.7947214775786193, -0.8288870151387760510, -10.36305467784173118 ) ) ;
#21600=CARTESIAN_POINT ( 'NONE',  ( 125.2194014775786286, -10.30919188438810075, -12.61870101168855918 ) ) ;
#21601=CARTESIAN_POINT ( 'NONE',  ( 122.8368814775786291, -1.561330072975668948, -17.79121239304076951 ) ) ;
#21604=CARTESIAN_POINT ( 'NONE',  ( 117.2776681442452968, -4.153390946401325223, -8.397313243818185668 ) ) ;
#21608=CARTESIAN_POINT ( 'NONE',  ( 121.7590748109119687, -7.893985811506177619, -18.51759400769804742 ) ) ;
#21611=CARTESIAN_POINT ( 'NONE',  ( 119.8303681442453126, -10.63000616557722466, -14.87417383870573495 ) ) ;
#21615=CARTESIAN_POINT ( 'NONE',  ( 117.3911214775786505, -7.894159318335828068, -9.358103419637847864 ) ) ;
#21618=CARTESIAN_POINT ( 'NONE',  ( 118.9794681442453026, -0.8288870151387760510, -10.36305467784173118 ) ) ;
#21620=CARTESIAN_POINT ( 'NONE',  ( 122.8368814775786291, -7.894159318335828068, -9.358103419637847864 ) ) ;
#21623=CARTESIAN_POINT ( 'NONE',  ( 119.6601881442453106, -1.833838273342659253, -17.42832698103878286 ) ) ;
#21624=CARTESIAN_POINT ( 'NONE',  ( 114.4413348109119823, -9.261995988541697145, -16.69588392320189030 ) ) ;
#21625=CARTESIAN_POINT ( 'NONE',  ( 118.4122014775786340, 0.5811942927096110934, -14.16772938898807510 ) ) ;
#21626=CARTESIAN_POINT ( 'NONE',  ( 126.2404814775786264, -0.8288870151387760510, -10.36305467784173118 ) ) ;
#21627=CARTESIAN_POINT ( 'NONE',  ( 126.2184548109105435, -4.159894987975746972, -8.443039665293909479 ) ) ;
#21628=CARTESIAN_POINT ( 'NONE',  ( 121.9859814775786333, -9.565557343593413364, -10.61323700422348004 ) ) ;
#21630=CARTESIAN_POINT ( 'NONE',  ( 121.0783548109119749, 0.2603800115204892296, -16.42320221600525088 ) ) ;
#21633=CARTESIAN_POINT ( 'NONE',  ( 115.1904114748722492, -0.1020945015694959546, -15.74893487844866691 ) ) ;
#21636=CARTESIAN_POINT ( 'NONE',  ( 125.9001214775786224, -4.089484607189486809, -7.948022111789456723 ) ) ;
#21639=CARTESIAN_POINT ( 'NONE',  ( 123.0070614775786169, -10.15424416112533912, -14.75197769757731336 ) ) ;
#21641=CARTESIAN_POINT ( 'NONE',  ( 126.0703014775786102, -9.988377603198980381, -10.36322818467138518 ) ) ;
#21644=CARTESIAN_POINT ( 'NONE',  ( 113.9307948109119906, 0.9020085738987339008, -11.91225656197089222 ) ) ;
#21645=CARTESIAN_POINT ( 'NONE',  ( 113.0231681442453322, 0.9020085738987339008, -11.91225656197089222 ) ) ;
#21646=CARTESIAN_POINT ( 'NONE',  ( 125.9568481442452850, -6.344957434206665248, -7.627207830600338134 ) ) ;
#21647=CARTESIAN_POINT ( 'NONE',  ( 122.2696148109119889, -5.574606645277164318, -18.38911715685844683 ) ) ;
#21648=CARTESIAN_POINT ( 'NONE',  ( 112.3991748109119868, -1.833838273342658809, -17.42832698103878286 ) ) ;
#21649=DIRECTION ( 'NONE',  ( 0.000000000000000000, 0.000000000000000000, 1.000000000000000000 ) ) ;
#21650=CARTESIAN_POINT ( 'NONE',  ( 123.4608748109119745, -10.63000616557722466, -14.87417383870573495 ) ) ;
#21651=CARTESIAN_POINT ( 'NONE',  ( 111.4453614775786434, -1.861572684145083256, -17.39139446643145348 ) ) ;
#21654=CARTESIAN_POINT ( 'NONE',  ( 125.4463081442452932, -4.153390946401325223, -8.397313243818185668 ) ) ;
#21660=CARTESIAN_POINT ( 'NONE',  ( 120.3976348109119812, -1.834011780172310813, -8.268836392978581529 ) ) ;
#21661=CARTESIAN_POINT ( 'NONE',  ( 136.7860375664299966, -8.463374175688866075, -17.68495210800635675 ) ) ;
#21663=CARTESIAN_POINT ( 'NONE',  ( 121.1589942721482771, -2.287189184988711155, -18.07361239780447448 ) ) ;
#21664=CARTESIAN_POINT ( 'NONE',  ( 125.6164881442453094, 0.2603800115204892296, -16.42320221600525088 ) ) ;
#21666=CARTESIAN_POINT ( 'NONE',  ( 124.2550481442452792, -0.1624402480850797581, -16.17319339645315424 ) ) ;
#21668=CARTESIAN_POINT ( 'NONE',  ( 119.1496481442453046, -3.383040157471821630, -19.15922257007629170 ) ) ;
#21672=CARTESIAN_POINT ( 'NONE',  ( 136.0617147589328226, -5.568559906631047163, -7.532066164982730960 ) ) ;
#21673=CARTESIAN_POINT ( 'NONE',  ( 125.9568481442452850, -6.344957434206665248, -7.627207830600338134 ) ) ;
#21674=EDGE_CURVE ( 'NONE', #30998, #31663, #16630, .T. ) ;
#21677=CARTESIAN_POINT ( 'NONE',  ( 124.9357681442453014, -1.834011780172310813, -8.268836392978581529 ) ) ;
#21678=CARTESIAN_POINT ( 'NONE',  ( 123.6310548109119765, -5.638512984488999180, -18.83840828888717311 ) ) ;
#21679=CARTESIAN_POINT ( 'NONE',  ( 124.8223148109119762, -10.15424416112533912, -14.75197769757731336 ) ) ;
#21681=CARTESIAN_POINT ( 'NONE',  ( 124.0848681442452772, -5.574606645277164318, -18.38911715685844683 ) ) ;
#21682=CARTESIAN_POINT ( 'NONE',  ( 113.1933481442453058, -5.574606645277164318, -18.38911715685844683 ) ) ;
#21683=CARTESIAN_POINT ( 'NONE',  ( 121.1350814775786233, 0.5811942927096110934, -14.16772938898807510 ) ) ;
#21687=CARTESIAN_POINT ( 'NONE',  ( 122.5584604873411791, -2.348512537728041583, -17.99195118506215962 ) ) ;
#21694=CARTESIAN_POINT ( 'NONE',  ( 112.3991748109119868, -8.166667518702817929, -8.995218007635859436 ) ) ;
#21696=CARTESIAN_POINT ( 'NONE',  ( 113.9875214775786532, -8.899110576539710493, -16.42337572283490132 ) ) ;
#21702=CARTESIAN_POINT ( 'NONE',  ( 114.5547881442453217, -5.638512984488999180, -18.83840828888717311 ) ) ;
#21706=ORIENTED_EDGE ( 'NONE', *, *, #20892, .T. ) ;
#21708=CARTESIAN_POINT ( 'NONE',  ( 114.6115148109119986, -6.222761293078241884, -8.102969835052219238 ) ) ;
#21709=CARTESIAN_POINT ( 'NONE',  ( 117.4478481442453131, 0.2603800115204892296, -16.42320221600525088 ) ) ;
#21712=CARTESIAN_POINT ( 'NONE',  ( 119.3198281442452924, -9.859900752359374465, -12.68260735090039404 ) ) ;
#21713=CARTESIAN_POINT ( 'NONE',  ( 114.2711548109119803, -0.1624402480850797581, -16.17319339645315424 ) ) ;
#21718=DIRECTION ( 'NONE',  ( 0.000000000000000000, 0.6004852223388321697, -0.7996358532186279566 ) ) ;
#21719=CARTESIAN_POINT ( 'NONE',  ( 118.9794681442453026, -0.8288870151387760510, -10.36305467784173118 ) ) ;
#21722=CARTESIAN_POINT ( 'NONE',  ( 116.8238548109119819, -4.089484607189486809, -7.948022111789456723 ) ) ;
#21726=ORIENTED_EDGE ( 'NONE', *, *, #14445, .F. ) ;
#21727=CARTESIAN_POINT ( 'NONE',  ( 117.6180281442453150, -8.899110576539710493, -16.42337572283490132 ) ) ;
#21728=B_SPLINE_CURVE_WITH_KNOTS ( 'NONE', 3,
 ( #13136, #34530, #9944, #45047 ),
 .UNSPECIFIED., .F., .F.,
 ( 4, 4 ),
 ( 0.000000000000000000, 1.000000000000000000 ),
 .UNSPECIFIED. ) ;
#21729=CARTESIAN_POINT ( 'NONE',  ( 119.0929214775786278, -4.153390946401325223, -8.397313243818185668 ) ) ;
#21736=CARTESIAN_POINT ( 'NONE',  ( 113.5337081442453240, -9.261995988541697145, -16.69588392320189030 ) ) ;
#21737=CARTESIAN_POINT ( 'NONE',  ( 112.7962614775786676, -3.383040157471821630, -19.15922257007629170 ) ) ;
#21738=CARTESIAN_POINT ( 'NONE',  ( 117.5613014775786525, -10.15424416112533912, -14.75197769757731336 ) ) ;
#21739=DIRECTION ( 'NONE',  ( 0.000000000000000000, 0.6004852223388321697, -0.7996358532186279566 ) ) ;
#21741=CARTESIAN_POINT ( 'NONE',  ( 114.9518748109119883, -7.643976991954077427, -18.09477374809248928 ) ) ;
#21745=CARTESIAN_POINT ( 'NONE',  ( 116.4834948109119779, -1.561330072975668504, -17.79121239304076951 ) ) ;
#21747=CARTESIAN_POINT ( 'NONE',  ( 117.6180281442453150, -0.4660016031367893996, -10.09054647747474043 ) ) ;
#21750=CARTESIAN_POINT ( 'NONE',  ( 115.3489614775786407, -9.261995988541697145, -16.69588392320189030 ) ) ;
#21751=CARTESIAN_POINT ( 'NONE',  ( 114.8384214775786489, 0.9020085738987339008, -11.91225656197089222 ) ) ;
#21759=CARTESIAN_POINT ( 'NONE',  ( 116.1998614775786507, 0.4262465694468514643, -12.03445270309931736 ) ) ;
#21761=CARTESIAN_POINT ( 'NONE',  ( 118.2313338145250441, -3.807985514183284348, -19.09877912889400520 ) ) ;
#21763=CARTESIAN_POINT ( 'NONE',  ( 126.5125895482226639, -4.782699052591321554, -8.246788084914983941 ) ) ;
#21764=CARTESIAN_POINT ( 'NONE',  ( 115.1220548109119761, -1.833838273342658809, -17.42832698103878286 ) ) ;
#21766=CARTESIAN_POINT ( 'NONE',  ( 124.8223148109119762, 0.9020085738987339008, -11.91225656197089222 ) ) ;
#21767=CARTESIAN_POINT ( 'NONE',  ( 120.2841814775786276, 0.9020085738987339008, -11.91225656197089222 ) ) ;
#21770=CARTESIAN_POINT ( 'NONE',  ( 118.9227414775786542, 0.4262465694468514643, -12.03445270309931736 ) ) ;
#21771=CARTESIAN_POINT ( 'NONE',  ( 112.9097148109120070, 0.2603800115204892296, -16.42320221600525088 ) ) ;
#21773=CARTESIAN_POINT ( 'NONE',  ( 118.6958348109119754, -6.344957434206665248, -7.627207830600338134 ) ) ;
#21774=CARTESIAN_POINT ( 'NONE',  ( 118.2420214775786320, -6.222761293078241884, -8.102969835052219238 ) ) ;
#21777=CARTESIAN_POINT ( 'NONE',  ( 123.0070614775786169, -10.15424416112533912, -14.75197769757731336 ) ) ;
#21779=CARTESIAN_POINT ( 'NONE',  ( 120.9081748109119872, -5.638512984488999180, -18.83840828888717311 ) ) ;
#21780=CARTESIAN_POINT ( 'NONE',  ( 135.7500233008185830, 0.6216732964927550453, -15.76311964996550685 ) ) ;
#21782=CARTESIAN_POINT ( 'NONE',  ( 114.3801926359456331, -1.179503403430479658, -17.05068175419387799 ) ) ;
#21783=CARTESIAN_POINT ( 'NONE',  ( 126.6479178317288188, 0.3508773515938530818, -13.34825603011022466 ) ) ;
#21785=CARTESIAN_POINT ( 'NONE',  ( 118.9227414775786400, -10.63000616557722466, -14.87417383870573495 ) ) ;
#21787=CARTESIAN_POINT ( 'NONE',  ( 114.9518748109119883, -7.643976991954077427, -18.09477374809248928 ) ) ;
#21793=CARTESIAN_POINT ( 'NONE',  ( 120.5110881442453206, -6.344957434206665248, -7.627207830600338134 ) ) ;
#21794=CARTESIAN_POINT ( 'NONE',  ( 118.7525614775786380, -1.833838273342659253, -17.42832698103878286 ) ) ;
#21795=CARTESIAN_POINT ( 'NONE',  ( 111.7184548109119788, -0.8288870151387760510, -10.36305467784173118 ) ) ;
#21797=CARTESIAN_POINT ( 'NONE',  ( 137.3527759848290373, -7.390398384115297148, -8.885999701577917520 ) ) ;
#21798=CARTESIAN_POINT ( 'NONE',  ( 122.9503348109119827, 0.5811942927096110934, -14.16772938898807510 ) ) ;
#21800=CARTESIAN_POINT ( 'NONE',  ( 119.0361948109119652, -2.084020599724406786, -8.691656652584148546 ) ) ;
#21801=EDGE_CURVE ( 'NONE', #2299, #6072, #29089, .T. ) ;
#21802=CARTESIAN_POINT ( 'NONE',  ( 118.0718414775786442, -0.8288870151387760510, -10.36305467784173118 ) ) ;
#21805=CARTESIAN_POINT ( 'NONE',  ( 121.9859814775786333, -9.565557343593413364, -10.61323700422348004 ) ) ;
#21806=CARTESIAN_POINT ( 'NONE',  ( 123.1772414775786189, -5.574606645277164318, -18.38911715685844683 ) ) ;
#21813=CARTESIAN_POINT ( 'NONE',  ( 117.4478481442453131, 0.2603800115204892296, -16.42320221600525088 ) ) ;
#21814=CARTESIAN_POINT ( 'NONE',  ( 119.7736414775786358, -10.30919188438810075, -12.61870101168855918 ) ) ;
#21816=CARTESIAN_POINT ( 'NONE',  ( 113.3068014775786594, -8.166667518702817929, -8.995218007635859436 ) ) ;
#21817=ORIENTED_EDGE ( 'NONE', *, *, #37297, .T. ) ;
#21818=CARTESIAN_POINT ( 'NONE',  ( 117.2928937256648965, -1.063912429576147511, -17.20460841810472985 ) ) ;
#21819=CARTESIAN_POINT ( 'NONE',  ( 116.0864081442453113, -9.988377603198976828, -10.36322818467138340 ) ) ;
#21822=CARTESIAN_POINT ( 'NONE',  ( 122.5532481442453019, 0.4262465694468514643, -12.03445270309931736 ) ) ;
#21823=B_SPLINE_CURVE_WITH_KNOTS ( 'NONE', 3,
 ( #22368, #15301, #35356, #11889 ),
 .UNSPECIFIED., .F., .F.,
 ( 4, 4 ),
 ( 0.000000000000000000, 1.000000000000000000 ),
 .UNSPECIFIED. ) ;
#21825=CARTESIAN_POINT ( 'NONE',  ( 124.1415948109119540, -6.344957434206665248, -7.627207830600338134 ) ) ;
#21826=CARTESIAN_POINT ( 'NONE',  ( 123.2906948109119867, -8.166667518702819706, -8.995218007635861213 ) ) ;
#21828=CARTESIAN_POINT ( 'NONE',  ( 117.8449348109119938, -1.833838273342659253, -17.42832698103878286 ) ) ;
#21834=CARTESIAN_POINT ( 'NONE',  ( 119.3198281442452924, 0.5811942927096110934, -14.16772938898807510 ) ) ;
#21836=CARTESIAN_POINT ( 'NONE',  ( 124.9819548109120291, -7.618532446444633344, -18.05174138884769874 ) ) ;
#21837=CARTESIAN_POINT ( 'NONE',  ( 127.8924691488517453, -7.120506250460368669, -18.77659918890763890 ) ) ;
#21838=CARTESIAN_POINT ( 'NONE',  ( 119.7963009221557513, -2.372251574601201174, -17.96033910819751611 ) ) ;
#21839=CARTESIAN_POINT ( 'NONE',  ( 116.1998614775786507, 0.4262465694468514643, -12.03445270309931736 ) ) ;
#21842=CARTESIAN_POINT ( 'NONE',  ( 119.0929214775786278, -4.153390946401325223, -8.397313243818185668 ) ) ;
#21843=CARTESIAN_POINT ( 'NONE',  ( 121.4754414775786131, -8.166667518702800166, -8.995218007635847002 ) ) ;
#21844=CARTESIAN_POINT ( 'NONE',  ( 121.8158014775786171, -4.153390946401325223, -8.397313243818185668 ) ) ;
#21847=CARTESIAN_POINT ( 'NONE',  ( 123.8012348109119642, -9.565557343593413364, -10.61323700422348004 ) ) ;
#21848=CARTESIAN_POINT ( 'NONE',  ( 113.0798948109119948, -0.4660016031367893996, -10.09054647747474043 ) ) ;
#21849=CARTESIAN_POINT ( 'NONE',  ( 120.0572748109119772, -3.383040157471821630, -19.15922257007629170 ) ) ;
#21850=CARTESIAN_POINT ( 'NONE',  ( 112.8529881442453302, -1.561330072975668060, -17.79121239304076596 ) ) ;
#21852=CARTESIAN_POINT ( 'NONE',  ( 119.8870948109119752, -0.8288870151387760510, -10.36305467784173118 ) ) ;
#21854=CARTESIAN_POINT ( 'NONE',  ( 120.5110881442453206, -6.344957434206665248, -7.627207830600338134 ) ) ;
#21864=CARTESIAN_POINT ( 'NONE',  ( 123.2339681442453241, -3.505236298600246325, -18.68346056562440793 ) ) ;
#21867=CARTESIAN_POINT ( 'NONE',  ( 125.5597614775786326, -1.561330072975669392, -17.79121239304076951 ) ) ;
#21870=CARTESIAN_POINT ( 'NONE',  ( 114.2144281442453178, -8.166667518702817929, -8.995218007635859436 ) ) ;
#21871=CARTESIAN_POINT ( 'NONE',  ( 113.3635281442453504, -9.988377603198976828, -10.36322818467138340 ) ) ;
#21872=CARTESIAN_POINT ( 'NONE',  ( 126.0703014775786102, -9.988377603198980381, -10.36322818467138518 ) ) ;
#21873=CARTESIAN_POINT ( 'NONE',  ( 121.8158014775786171, -4.153390946401325223, -8.397313243818185668 ) ) ;
#21876=CARTESIAN_POINT ( 'NONE',  ( 122.5532481442453019, -10.63000616557722466, -14.87417383870573495 ) ) ;
#21882=CARTESIAN_POINT ( 'NONE',  ( 120.7379948109119709, -10.63000616557722466, -14.87417383870573495 ) ) ;
#21885=CARTESIAN_POINT ( 'NONE',  ( 112.0588148109119828, 0.5811942927096154232, -14.16772938898807155 ) ) ;
#21886=CARTESIAN_POINT ( 'NONE',  ( 124.5954081442453116, -3.383040157471821630, -19.15922257007629170 ) ) ;
#21887=CARTESIAN_POINT ( 'NONE',  ( 127.4620922276975818, -4.355667135866661432, -18.99210946691642832 ) ) ;
#21888=CARTESIAN_POINT ( 'NONE',  ( 123.9714148109119805, -8.899110576539710493, -16.42337572283490132 ) ) ;
#21889=VERTEX_POINT ( 'NONE', #17736 ) ;
#21891=CARTESIAN_POINT ( 'NONE',  ( 119.3765548109119834, 0.9020085738987339008, -11.91225656197089222 ) ) ;
#21895=CARTESIAN_POINT ( 'NONE',  ( 137.5098831408921001, -4.032236636546677744, -8.461637928299781564 ) ) ;
#21896=CARTESIAN_POINT ( 'NONE',  ( 123.8579614775786126, 0.5811942927096110934, -14.16772938898807510 ) ) ;
#21899=CARTESIAN_POINT ( 'NONE',  ( 125.3328548109119964, -9.261995988541697145, -16.69588392320189030 ) ) ;
#21900=CARTESIAN_POINT ( 'NONE',  ( 123.8579614775786126, -9.859900752359378018, -12.68260735090039759 ) ) ;
#21902=CARTESIAN_POINT ( 'NONE',  ( 125.1626748109119802, -0.1624402480850797581, -16.17319339645315424 ) ) ;
#21904=CARTESIAN_POINT ( 'NONE',  ( 119.4900081442453086, -1.834011780172310813, -8.268836392978581529 ) ) ;
#21905=VERTEX_POINT ( 'NONE', #21156 ) ;
#21906=ORIENTED_EDGE ( 'NONE', *, *, #45118, .F. ) ;
#21907=CARTESIAN_POINT ( 'NONE',  ( 127.9806007748781838, -8.501439814973640097, -18.01472541506584335 ) ) ;
#21912=CARTESIAN_POINT ( 'NONE',  ( 126.2184548109108420, -9.810113536895345376, -12.66056213194485558 ) ) ;
#21913=CARTESIAN_POINT ( 'NONE',  ( 114.5547881442453217, -5.638512984488999180, -18.83840828888717311 ) ) ;
#21915=CARTESIAN_POINT ( 'NONE',  ( 112.4559014775786778, -0.1624402480850797581, -16.17319339645315424 ) ) ;
#21918=CARTESIAN_POINT ( 'NONE',  ( 112.2857214775786474, -5.574606645277164318, -18.38911715685844683 ) ) ;
#21921=CARTESIAN_POINT ( 'NONE',  ( 116.2565881442452991, -9.261995988541697145, -16.69588392320189030 ) ) ;
#21925=CARTESIAN_POINT ( 'NONE',  ( 126.3999550322324410, -7.499531571443311506, -9.037731752716881672 ) ) ;
#21926=CARTESIAN_POINT ( 'NONE',  ( 119.9438214775786378, -2.084020599724406786, -8.691656652584148546 ) ) ;
#21927=CARTESIAN_POINT ( 'NONE',  ( 115.7460481442453357, 0.9020085738987339008, -11.91225656197089222 ) ) ;
#21928=CARTESIAN_POINT ( 'NONE',  ( 113.4769814775786330, -10.63000616557722466, -14.87417383870573495 ) ) ;
#21930=CARTESIAN_POINT ( 'NONE',  ( 118.1285681442452926, -2.084020599724404121, -8.691656652584155651 ) ) ;
#21931=CARTESIAN_POINT ( 'NONE',  ( 119.1496481442453046, -6.222761293078241884, -8.102969835052219238 ) ) ;
#21932=CARTESIAN_POINT ( 'NONE',  ( 114.3846081442453197, 0.4262465694468514643, -12.03445270309931736 ) ) ;
#21937=CARTESIAN_POINT ( 'NONE',  ( 116.7104014775786425, -8.899110576539710493, -16.42337572283490132 ) ) ;
#21938=VERTEX_POINT ( 'NONE', #44900 ) ;
#21940=CARTESIAN_POINT ( 'NONE',  ( 115.1220548109119761, -8.166667518702817929, -8.995218007635861213 ) ) ;
#21943=CARTESIAN_POINT ( 'NONE',  ( 113.4202548109119846, 0.1319031606808879209, -14.10382304977623669 ) ) ;
#21947=CARTESIAN_POINT ( 'NONE',  ( 122.2696148109119889, -5.574606645277164318, -18.38911715685844683 ) ) ;
#21948=CARTESIAN_POINT ( 'NONE',  ( 118.5823814775786360, -7.643976991954077427, -18.09477374809248928 ) ) ;
#21956=CARTESIAN_POINT ( 'NONE',  ( 113.7606148109119886, -1.561330072975668060, -17.79121239304076596 ) ) ;
#21959=CARTESIAN_POINT ( 'NONE',  ( 112.4559014775786494, -9.988377603198976828, -10.36322818467138340 ) ) ;
#21960=CARTESIAN_POINT ( 'NONE',  ( 119.8870948109119752, -0.8288870151387760510, -10.36305467784173118 ) ) ;
#21963=EDGE_CURVE ( 'NONE', #15771, #41059, #22832, .T. ) ;
#21965=CARTESIAN_POINT ( 'NONE',  ( 120.0572748109119772, -6.222761293078241884, -8.102969835052219238 ) ) ;
#21966=CARTESIAN_POINT ( 'NONE',  ( 111.7184548109119788, -8.862178061932382889, -16.39564131203247399 ) ) ;
#21969=CARTESIAN_POINT ( 'NONE',  ( 117.5613014775786525, 0.9020085738987339008, -11.91225656197089222 ) ) ;
#21971=CARTESIAN_POINT ( 'NONE',  ( 118.6391081442452986, -4.089484607189486809, -7.948022111789456723 ) ) ;
#21974=CARTESIAN_POINT ( 'NONE',  ( 115.9162281442453235, -4.089484607189486809, -7.948022111789456723 ) ) ;
#21975=CARTESIAN_POINT ( 'NONE',  ( 116.5969481442453031, 0.5811942927096154232, -14.16772938898807155 ) ) ;
#21976=CARTESIAN_POINT ( 'NONE',  ( 127.1653849502121858, -10.32489337370534166, -13.76497012726351876 ) ) ;
#21983=CARTESIAN_POINT ( 'NONE',  ( 120.0572748109119772, -6.222761293078241884, -8.102969835052219238 ) ) ;
#21986=CARTESIAN_POINT ( 'NONE',  ( 121.6412059692789427, -1.179503403430468333, -17.05068175419387089 ) ) ;
#21987=CARTESIAN_POINT ( 'NONE',  ( 112.5693548109119888, 0.4262465694468514643, -12.03445270309931736 ) ) ;
#21989=CARTESIAN_POINT ( 'NONE',  ( 123.2906948109119867, -8.166667518702819706, -8.995218007635861213 ) ) ;
#21990=CARTESIAN_POINT ( 'NONE',  ( 119.8870948109119752, -9.261995988541697145, -16.69588392320189030 ) ) ;
#21993=CARTESIAN_POINT ( 'NONE',  ( 117.1642148109119859, -0.8288870151387760510, -10.36305467784173118 ) ) ;
#21994=CARTESIAN_POINT ( 'NONE',  ( 112.1722681442453222, -0.4660016031367893996, -10.09054647747474043 ) ) ;
#21995=CARTESIAN_POINT ( 'NONE',  ( 119.4900081442453086, -1.834011780172310813, -8.268836392978581529 ) ) ;
#21996=CARTESIAN_POINT ( 'NONE',  ( 118.8660148109119774, 0.1319031606808879209, -14.10382304977623669 ) ) ;
#21998=CARTESIAN_POINT ( 'NONE',  ( 116.3461286830089989, -1.087735405160625834, -17.17288456429612964 ) ) ;
#21999=CARTESIAN_POINT ( 'NONE',  ( 121.0783548109119749, 0.2603800115204892296, -16.42320221600525088 ) ) ;
#22000=CARTESIAN_POINT ( 'NONE',  ( 113.1366214775786432, -7.643976991954077427, -18.09477374809248928 ) ) ;
#22006=CARTESIAN_POINT ( 'NONE',  ( 119.7736414775786358, -10.30919188438810075, -12.61870101168855918 ) ) ;
#22008=CARTESIAN_POINT ( 'NONE',  ( 116.5969481442453031, -9.859900752359374465, -12.68260735090039404 ) ) ;
#22009=CARTESIAN_POINT ( 'NONE',  ( 126.0703014775786102, -9.988377603198980381, -10.36322818467138518 ) ) ;
#22010=CARTESIAN_POINT ( 'NONE',  ( 126.2758031835797254, -0.6776192674585240772, -10.60718350710181035 ) ) ;
#22014=CARTESIAN_POINT ( 'NONE',  ( 113.5904348109119866, -2.084020599724406786, -8.691656652584148546 ) ) ;
#22015=CARTESIAN_POINT ( 'NONE',  ( 115.1037688976800268, -1.244021962887382315, -16.96476564598603787 ) ) ;
#22019=CARTESIAN_POINT ( 'NONE',  ( 120.0572748109119772, -3.383040157471821630, -19.15922257007629170 ) ) ;
#22020=CARTESIAN_POINT ( 'NONE',  ( 119.9438214775786378, -2.084020599724406786, -8.691656652584148546 ) ) ;
#22021=CARTESIAN_POINT ( 'NONE',  ( 113.9307948109119764, -10.15424416112533912, -14.75197769757731336 ) ) ;
#22022=VERTEX_POINT ( 'NONE', #13438 ) ;
#22023=CARTESIAN_POINT ( 'NONE',  ( 137.0134976903368340, -7.178400362679481006, -8.454421406160578911 ) ) ;
#22025=CARTESIAN_POINT ( 'NONE',  ( 121.5888948109119809, -10.30919188438810075, -12.61870101168855918 ) ) ;
#22027=CARTESIAN_POINT ( 'NONE',  ( 120.0005481442453146, -4.153390946401325223, -8.397313243818185668 ) ) ;
#22028=CARTESIAN_POINT ( 'NONE',  ( 122.3830681442452857, -1.833838273342659697, -17.42832698103878286 ) ) ;
#22029=CARTESIAN_POINT ( 'NONE',  ( 115.9729548109119861, -3.505236298600246325, -18.68346056562440793 ) ) ;
#22032=CARTESIAN_POINT ( 'NONE',  ( 122.2696148109119889, -5.574606645277164318, -18.38911715685844683 ) ) ;
#22033=CARTESIAN_POINT ( 'NONE',  ( 122.6667014775786413, -2.084020599724406786, -8.691656652584148546 ) ) ;
#22040=CARTESIAN_POINT ( 'NONE',  ( 116.5402214775786405, 0.2603800115204892296, -16.42320221600525088 ) ) ;
#22041=CARTESIAN_POINT ( 'NONE',  ( 118.8660148109119774, -10.30919188438810075, -12.61870101168855918 ) ) ;
#22044=CARTESIAN_POINT ( 'NONE',  ( 113.9875214775786532, -0.4660016031367893996, -10.09054647747474043 ) ) ;
#22049=CARTESIAN_POINT ( 'NONE',  ( 117.9016614775786280, -9.988377603198976828, -10.36322818467138340 ) ) ;
#22050=CARTESIAN_POINT ( 'NONE',  ( 121.2485348109119769, -8.899110576539710493, -16.42337572283490132 ) ) ;
#22052=CARTESIAN_POINT ( 'NONE',  ( 113.2500748109119968, -3.505236298600246325, -18.68346056562440793 ) ) ;
#22053=CARTESIAN_POINT ( 'NONE',  ( 122.6099748109119929, -9.261995988541697145, -16.69588392320189030 ) ) ;
#22056=CARTESIAN_POINT ( 'NONE',  ( 114.7816948109119863, -9.859900752359374465, -12.68260735090039404 ) ) ;
#22062=CARTESIAN_POINT ( 'NONE',  ( 118.2420214775786320, -3.383040157471821630, -19.15922257007629170 ) ) ;
#22067=B_SPLINE_CURVE_WITH_KNOTS ( 'NONE', 3,
 ( #22546, #15714, #16170, #29616, #12300, #9325, #43760, #30074, #26426, #26650 ),
 .UNSPECIFIED., .F., .F.,
 ( 4, 3, 3, 4 ),
 ( 0.000000000000000000, 0.0001671877548681249956, 0.0003343755096277635291, 0.0006463528481650629171 ),
 .UNSPECIFIED. ) ;
#22068=CARTESIAN_POINT ( 'NONE',  ( 114.2711548109119803, -0.1624402480850797581, -16.17319339645315424 ) ) ;
#22071=CARTESIAN_POINT ( 'NONE',  ( 121.8725281442453223, -6.222761293078241884, -8.102969835052219238 ) ) ;
#22072=DIRECTION ( 'NONE',  ( -0.7071067811865475727, -0.4246071727180998345, 0.5654279342907827521 ) ) ;
#22074=CARTESIAN_POINT ( 'NONE',  ( 125.1626748109119802, -0.1624402480850797581, -16.17319339645315424 ) ) ;
#22079=CARTESIAN_POINT ( 'NONE',  ( 124.3685014775786328, 0.4262465694468514643, -12.03445270309931736 ) ) ;
#22080=CARTESIAN_POINT ( 'NONE',  ( 113.1933481442453058, -4.089484607189486809, -7.948022111789456723 ) ) ;
#22081=CARTESIAN_POINT ( 'NONE',  ( 120.5678148109119832, -8.166667518702819706, -8.995218007635861213 ) ) ;
#22082=CARTESIAN_POINT ( 'NONE',  ( 113.8173414775786512, 0.2603800115204892296, -16.42320221600525088 ) ) ;
#22084=CARTESIAN_POINT ( 'NONE',  ( 122.1561614775786353, -8.899110576539710493, -16.42337572283490132 ) ) ;
#22086=CARTESIAN_POINT ( 'NONE',  ( 120.5678148109119832, -8.166667518702819706, -8.995218007635861213 ) ) ;
#22090=CARTESIAN_POINT ( 'NONE',  ( 112.9097148109120070, -9.565557343593413364, -10.61323700422348004 ) ) ;
#22091=CARTESIAN_POINT ( 'NONE',  ( 138.0748658142820204, -3.091679250359711695, -17.00231359494076955 ) ) ;
#22094=CARTESIAN_POINT ( 'NONE',  ( 120.6245414775786458, -0.1624402480850797581, -16.17319339645315424 ) ) ;
#22095=DIRECTION ( 'NONE',  ( -0.7071067811865481278, -0.5654279342906992634, -0.4246071727182101907 ) ) ;
#22097=CARTESIAN_POINT ( 'NONE',  ( 126.1837548109119211, -10.63000616557722466, -14.87417383870573495 ) ) ;
#22100=CARTESIAN_POINT ( 'NONE',  ( 113.7606148109119886, -1.561330072975668060, -17.79121239304076596 ) ) ;
#22102=CARTESIAN_POINT ( 'NONE',  ( 122.2128881442453263, -7.643976991954077427, -18.09477374809248928 ) ) ;
#22103=CARTESIAN_POINT ( 'NONE',  ( 112.8529881442453302, -7.894159318335828068, -9.358103419637847864 ) ) ;
#22105=CARTESIAN_POINT ( 'NONE',  ( 111.8319081442453182, -4.153390946401321671, -8.397313243818183892 ) ) ;
#22111=CARTESIAN_POINT ( 'NONE',  ( 122.3263414775786373, -6.344957434206665248, -7.627207830600338134 ) ) ;
#22112=CARTESIAN_POINT ( 'NONE',  ( 136.4173705901596350, -10.20608232061555576, -15.61275821664342978 ) ) ;
#22115=CARTESIAN_POINT ( 'NONE',  ( 125.7299414775786346, 0.9020085738987339008, -11.91225656197089222 ) ) ;
#22117=CARTESIAN_POINT ( 'NONE',  ( 123.4608748109119745, 0.4262465694468514643, -12.03445270309931736 ) ) ;
#22119=CARTESIAN_POINT ( 'NONE',  ( 119.6034614775786196, -6.344957434206665248, -7.627207830600338134 ) ) ;
#22124=CARTESIAN_POINT ( 'NONE',  ( 112.2289948109119848, -7.643976991954077427, -18.09477374809248928 ) ) ;
#22128=CARTESIAN_POINT ( 'NONE',  ( 112.3424481442453384, -3.505236298600246325, -18.68346056562440793 ) ) ;
#22129=CARTESIAN_POINT ( 'NONE',  ( 125.2761281442453054, 0.4262465694468514643, -12.03445270309931736 ) ) ;
#22131=CARTESIAN_POINT ( 'NONE',  ( 122.2128881442453263, -7.643976991954077427, -18.09477374809248928 ) ) ;
#22132=CARTESIAN_POINT ( 'NONE',  ( 113.0231681442453180, -10.15424416112533912, -14.75197769757731336 ) ) ;
#22133=CARTESIAN_POINT ( 'NONE',  ( 118.0718414775786300, -9.261995988541697145, -16.69588392320189030 ) ) ;
#22136=CARTESIAN_POINT ( 'NONE',  ( 126.4536383592497231, -8.582534964477776640, -16.90949643156282889 ) ) ;
#22140=CARTESIAN_POINT ( 'NONE',  ( 125.5597614775786326, -7.894159318336616771, -9.358103419638441167 ) ) ;
#22141=CARTESIAN_POINT ( 'NONE',  ( 115.8027748109119841, -0.4660016031367893996, -10.09054647747474043 ) ) ;
#22143=CARTESIAN_POINT ( 'NONE',  ( 115.0086014775786509, -5.574606645277164318, -18.38911715685844683 ) ) ;
#22149=CARTESIAN_POINT ( 'NONE',  ( 115.2922348109119781, -10.63000616557722466, -14.87417383870573495 ) ) ;
#22154=CARTESIAN_POINT ( 'NONE',  ( 119.6601881442453106, -1.833838273342659253, -17.42832698103878286 ) ) ;
#22155=CARTESIAN_POINT ( 'NONE',  ( 116.0296814775786345, -8.166667518702817929, -8.995218007635861213 ) ) ;
#22156=CARTESIAN_POINT ( 'NONE',  ( 113.0798948109119948, -0.4660016031367893996, -10.09054647747474043 ) ) ;
#22157=CARTESIAN_POINT ( 'NONE',  ( 124.7088614775786226, -9.565557343593413364, -10.61323700422348004 ) ) ;
#22158=CARTESIAN_POINT ( 'NONE',  ( 122.1561614775786353, -8.899110576539710493, -16.42337572283490132 ) ) ;
#22159=CARTESIAN_POINT ( 'NONE',  ( 116.3133148109120043, -2.084020599724406786, -8.691656652584148546 ) ) ;
#22163=CARTESIAN_POINT ( 'NONE',  ( 117.2776681442452968, -4.153390946401325223, -8.397313243818185668 ) ) ;
#22165=CARTESIAN_POINT ( 'NONE',  ( 116.1998614775786507, -10.63000616557722466, -14.87417383870573495 ) ) ;
#22168=CARTESIAN_POINT ( 'NONE',  ( 112.6828081442453282, -2.084020599724406786, -8.691656652584148546 ) ) ;
#22171=CARTESIAN_POINT ( 'NONE',  ( 121.3052614775786111, -7.643976991954077427, -18.09477374809248928 ) ) ;
#22172=CARTESIAN_POINT ( 'NONE',  ( 116.8805814775786445, -3.505236298600246325, -18.68346056562440793 ) ) ;
#22174=CARTESIAN_POINT ( 'NONE',  ( 116.6536748109119941, -10.15424416112534267, -14.75197769757730804 ) ) ;
#22176=CARTESIAN_POINT ( 'NONE',  ( 112.1708206037811948, -8.908198244330842286, -16.40957177738907191 ) ) ;
#22179=CARTESIAN_POINT ( 'NONE',  ( 116.4267681442453153, -3.383040157471821630, -19.15922257007629170 ) ) ;
#22180=CARTESIAN_POINT ( 'NONE',  ( 125.5030348109119558, -6.222761293078241884, -8.102969835052219238 ) ) ;
#22181=CARTESIAN_POINT ( 'NONE',  ( 115.9729548109119861, -3.505236298600246325, -18.68346056562440793 ) ) ;
#22182=CARTESIAN_POINT ( 'NONE',  ( 122.3830681442452857, -1.833838273342659697, -17.42832698103878286 ) ) ;
#22185=CARTESIAN_POINT ( 'NONE',  ( 119.0929214775786278, -4.153390946401325223, -8.397313243818185668 ) ) ;
#22186=DIRECTION ( 'NONE',  ( 0.000000000000000000, -0.6004852223388321697, 0.7996358532186280677 ) ) ;
#22191=CARTESIAN_POINT ( 'NONE',  ( 119.8870948109119752, -9.261995988541697145, -16.69588392320189030 ) ) ;
#22193=CARTESIAN_POINT ( 'NONE',  ( 117.1642148109119859, -9.261995988541697145, -16.69588392320189030 ) ) ;
#22194=CARTESIAN_POINT ( 'NONE',  ( 115.1403407241439396, -2.443475742715333965, -17.86549347949429389 ) ) ;
#22196=CARTESIAN_POINT ( 'NONE',  ( 115.9729548109119861, -6.344957434206662583, -7.627207830600332805 ) ) ;
#22197=CARTESIAN_POINT ( 'NONE',  ( 116.7104014775786425, -0.4660016031367893996, -10.09054647747474043 ) ) ;
#22198=CARTESIAN_POINT ( 'NONE',  ( 127.0400190879688012, -10.26619878979528799, -13.69785579496253014 ) ) ;
#22205=CARTESIAN_POINT ( 'NONE',  ( 121.9292548109119849, -7.894159318335828068, -9.358103419637847864 ) ) ;
#22208=CARTESIAN_POINT ( 'NONE',  ( 115.8595014775786609, -7.643976991954077427, -18.09477374809248928 ) ) ;
#22210=CARTESIAN_POINT ( 'NONE',  ( 113.9307948109119764, -10.15424416112533912, -14.75197769757731336 ) ) ;
#22211=CARTESIAN_POINT ( 'NONE',  ( 120.0005481442453146, -5.638512984488999180, -18.83840828888717311 ) ) ;
#22213=CARTESIAN_POINT ( 'NONE',  ( 120.0572748109119772, -6.222761293078241884, -8.102969835052219238 ) ) ;
#22214=CARTESIAN_POINT ( 'NONE',  ( 115.9729548109119861, -6.344957434206662583, -7.627207830600332805 ) ) ;
#22215=CARTESIAN_POINT ( 'NONE',  ( 120.6812681442452941, -10.30919188438810075, -12.61870101168855918 ) ) ;
#22217=CARTESIAN_POINT ( 'NONE',  ( 120.1707281442453166, -9.565557343593413364, -10.61323700422348004 ) ) ;
#22219=CARTESIAN_POINT ( 'NONE',  ( 124.7655881442452852, -9.859900752359378018, -12.68260735090039759 ) ) ;
#22222=CARTESIAN_POINT ( 'NONE',  ( 121.8158014775786171, -5.638512984488999180, -18.83840828888717311 ) ) ;
#22229=CARTESIAN_POINT ( 'NONE',  ( 117.5045748109119756, -9.859900752359374465, -12.68260735090039404 ) ) ;
#22230=CARTESIAN_POINT ( 'NONE',  ( 111.8319081442453182, -4.153390946401321671, -8.397313243818183892 ) ) ;
#22234=CARTESIAN_POINT ( 'NONE',  ( 115.0086014775786509, -5.574606645277164318, -18.38911715685844683 ) ) ;
#22235=CARTESIAN_POINT ( 'NONE',  ( 114.7607665278262630, -1.036737761566196570, -17.24079555149560505 ) ) ;
#22239=CARTESIAN_POINT ( 'NONE',  ( 118.9794681442453026, -9.261995988541697145, -16.69588392320189030 ) ) ;
#22241=CARTESIAN_POINT ( 'NONE',  ( 121.1918081442452859, -10.15424416112533912, -14.75197769757731336 ) ) ;
#22242=ORIENTED_EDGE ( 'NONE', *, *, #6637, .T. ) ;
#22243=CARTESIAN_POINT ( 'NONE',  ( 137.3019930433568447, -8.583162301624891910, -9.736487546999564202 ) ) ;
#22244=CARTESIAN_POINT ( 'NONE',  ( 125.7299414775786346, 0.9020085738987339008, -11.91225656197089222 ) ) ;
#22246=CARTESIAN_POINT ( 'NONE',  ( 119.3198281442452924, -9.859900752359374465, -12.68260735090039404 ) ) ;
#22248=CARTESIAN_POINT ( 'NONE',  ( 123.2339681442453241, -3.505236298600246325, -18.68346056562440793 ) ) ;
#22249=CARTESIAN_POINT ( 'NONE',  ( 116.1998614775786507, 0.4262465694468514643, -12.03445270309931736 ) ) ;
#22254=CARTESIAN_POINT ( 'NONE',  ( 124.5954081442453116, -6.222761293078241884, -8.102969835052219238 ) ) ;
#22255=CARTESIAN_POINT ( 'NONE',  ( 124.7655881442452852, -9.859900752359378018, -12.68260735090039759 ) ) ;
#22262=CARTESIAN_POINT ( 'NONE',  ( 121.6456214775786293, -10.63000616557722466, -14.87417383870573495 ) ) ;
#22263=CARTESIAN_POINT ( 'NONE',  ( 118.4689281442453392, 0.9020085738987339008, -11.91225656197089222 ) ) ;
#22265=CARTESIAN_POINT ( 'NONE',  ( 112.9664414775786412, 0.5811942927096154232, -14.16772938898807155 ) ) ;
#22271=CARTESIAN_POINT ( 'NONE',  ( 118.2987481442453088, -1.561330072975668504, -17.79121239304076951 ) ) ;
#22272=CARTESIAN_POINT ( 'NONE',  ( 125.6732148109119862, -9.859900752359378018, -12.68260735090039759 ) ) ;
#22273=SHAPE_DEFINITION_REPRESENTATION ( #25240, #21588 ) ;
#22275=CARTESIAN_POINT ( 'NONE',  ( 114.1577014775786552, -3.505236298600246325, -18.68346056562440793 ) ) ;
#22276=CARTESIAN_POINT ( 'NONE',  ( 125.1626748109119802, -9.988377603198980381, -10.36322818467138518 ) ) ;
#22280=CARTESIAN_POINT ( 'NONE',  ( 119.7736414775786358, 0.1319031606808879209, -14.10382304977623669 ) ) ;
#22286=CARTESIAN_POINT ( 'NONE',  ( 119.7169148109119874, -9.988377603198976828, -10.36322818467138340 ) ) ;
#22291=CARTESIAN_POINT ( 'NONE',  ( 118.0151148109119816, 0.4262465694468514643, -12.03445270309931736 ) ) ;
#22294=CARTESIAN_POINT ( 'NONE',  ( 124.4252281442452812, -0.8288870151387760510, -10.36305467784173118 ) ) ;
#22296=CARTESIAN_POINT ( 'NONE',  ( 124.7088614775786226, -9.565557343593413364, -10.61323700422348004 ) ) ;
#22298=CARTESIAN_POINT ( 'NONE',  ( 116.5402214775786405, -9.565557343593413364, -10.61323700422348004 ) ) ;
#22299=CARTESIAN_POINT ( 'NONE',  ( 121.4754414775786131, -1.833838273342659697, -17.42832698103878286 ) ) ;
#22300=CARTESIAN_POINT ( 'NONE',  ( 112.0588148109119828, 0.5811942927096154232, -14.16772938898807155 ) ) ;
#22301=CARTESIAN_POINT ( 'NONE',  ( 118.0718414775786300, -9.261995988541697145, -16.69588392320189030 ) ) ;
#22302=CARTESIAN_POINT ( 'NONE',  ( 117.0507614775786465, -10.30919188438810075, -12.61870101168855918 ) ) ;
#22305=CARTESIAN_POINT ( 'NONE',  ( 125.5597614775786326, -7.894159318335828068, -9.358103419637847864 ) ) ;
#22307=CARTESIAN_POINT ( 'NONE',  ( 120.8514481442452961, -7.893985811506177619, -18.51759400769804742 ) ) ;
#22311=CARTESIAN_POINT ( 'NONE',  ( 112.3991748109119868, -1.833838273342658809, -17.42832698103878286 ) ) ;
#22313=AXIS2_PLACEMENT_3D ( 'NONE', #5759, #8525, #12174 ) ;
#22314=CARTESIAN_POINT ( 'NONE',  ( 126.1837548109119211, -10.63000616557722466, -14.87417383870573495 ) ) ;
#22316=CARTESIAN_POINT ( 'NONE',  ( 122.8936081442453059, -9.565557343593413364, -10.61323700422348004 ) ) ;
#22323=CARTESIAN_POINT ( 'NONE',  ( 114.0442481442453300, -1.834011780172310813, -8.268836392978581529 ) ) ;
#22325=CARTESIAN_POINT ( 'NONE',  ( 119.6601881442453106, -1.833838273342659253, -17.42832698103878286 ) ) ;
#22326=CARTESIAN_POINT ( 'NONE',  ( 113.0798948109119948, -8.899110576539710493, -16.42337572283490132 ) ) ;
#22328=CARTESIAN_POINT ( 'NONE',  ( 115.1010702440515558, -2.467220198592777525, -17.83387418641524391 ) ) ;
#22329=CARTESIAN_POINT ( 'NONE',  ( 125.6164881442453094, -9.565557343593413364, -10.61323700422348004 ) ) ;
#22333=CARTESIAN_POINT ( 'NONE',  ( 118.7525614775786380, -8.166667518702819706, -8.995218007635861213 ) ) ;
#22334=CARTESIAN_POINT ( 'NONE',  ( 135.8497638153270373, -10.40529151342853709, -15.59585623059315651 ) ) ;
#22337=CARTESIAN_POINT ( 'NONE',  ( 112.7395348109119766, -5.638512984488999180, -18.83840828888717311 ) ) ;
#22338=CARTESIAN_POINT ( 'NONE',  ( 125.8433948109119456, -1.834011780172310813, -8.268836392978581529 ) ) ;
#22339=CARTESIAN_POINT ( 'NONE',  ( 135.3184548109119874, -4.863998795839242995, -13.39321520033831447 ) ) ;
#22340=CARTESIAN_POINT ( 'NONE',  ( 124.9357681442453014, -7.643976991954077427, -18.09477374809248928 ) ) ;
#22341=VERTEX_POINT ( 'NONE', #10902 ) ;
#22342=CARTESIAN_POINT ( 'NONE',  ( 118.4122014775786340, 0.5811942927096110934, -14.16772938898807510 ) ) ;
#22347=CARTESIAN_POINT ( 'NONE',  ( 135.3184548109119874, -5.622599431619523358, -7.441364641445410655 ) ) ;
#22348=CARTESIAN_POINT ( 'NONE',  ( 114.0442481442453300, -7.643976991954077427, -18.09477374809248928 ) ) ;
#22351=CARTESIAN_POINT ( 'NONE',  ( 112.4559014775786778, -0.1624402480850797581, -16.17319339645315424 ) ) ;
#22352=CARTESIAN_POINT ( 'NONE',  ( 112.5693548109119888, -10.63000616557722466, -14.87417383870573495 ) ) ;
#22354=CARTESIAN_POINT ( 'NONE',  ( 124.7655881442452852, -9.859900752359378018, -12.68260735090039759 ) ) ;
#22355=CARTESIAN_POINT ( 'NONE',  ( 112.5693548109119888, 0.4262465694468514643, -12.03445270309931736 ) ) ;
#22356=CARTESIAN_POINT ( 'NONE',  ( 120.2274548109119934, 0.5811942927096110934, -14.16772938898807510 ) ) ;
#22358=CARTESIAN_POINT ( 'NONE',  ( 120.3976348109119812, -1.834011780172310813, -8.268836392978581529 ) ) ;
#22363=CARTESIAN_POINT ( 'NONE',  ( 126.4599182912947413, -9.818254414970132515, -12.09804486832614856 ) ) ;
#22364=CARTESIAN_POINT ( 'NONE',  ( 115.5191414775786569, -3.383040157471821630, -19.15922257007629170 ) ) ;
#22368=CARTESIAN_POINT ( 'NONE',  ( 111.2646414775786496, -8.899110576539710493, -16.42337572283490132 ) ) ;
#22370=CARTESIAN_POINT ( 'NONE',  ( 122.9351092294923831, -2.263366209404226392, -18.10533625161308180 ) ) ;
#22371=CARTESIAN_POINT ( 'NONE',  ( 119.1496481442453046, -3.383040157471821630, -19.15922257007629170 ) ) ;
#22375=CARTESIAN_POINT ( 'NONE',  ( 118.6958348109119754, -3.505236298600246325, -18.68346056562440793 ) ) ;
#22376=CARTESIAN_POINT ( 'NONE',  ( 115.9162281442453235, -4.089484607189486809, -7.948022111789456723 ) ) ;
#22379=CARTESIAN_POINT ( 'NONE',  ( 123.4608748109119745, 0.4262465694468514643, -12.03445270309931736 ) ) ;
#22381=CARTESIAN_POINT ( 'NONE',  ( 123.6310548109119765, -4.153390946401325223, -8.397313243818185668 ) ) ;
#22382=CARTESIAN_POINT ( 'NONE',  ( 113.9875214775786532, -8.899110576539710493, -16.42337572283490132 ) ) ;
#22387=CARTESIAN_POINT ( 'NONE',  ( 117.0507614775786465, 0.1319031606808879209, -14.10382304977623669 ) ) ;
#22390=CARTESIAN_POINT ( 'NONE',  ( 115.2922348109119781, -10.63000616557722466, -14.87417383870573495 ) ) ;
#22393=CARTESIAN_POINT ( 'NONE',  ( 112.7962614775786676, -6.222761293078241884, -8.102969835052219238 ) ) ;
#22396=CARTESIAN_POINT ( 'NONE',  ( 122.1561614775786353, -8.899110576539710493, -16.42337572283490132 ) ) ;
#22397=CARTESIAN_POINT ( 'NONE',  ( 117.8449348109119938, -1.833838273342659253, -17.42832698103878286 ) ) ;
#22405=CARTESIAN_POINT ( 'NONE',  ( 115.9729548109119861, -6.344957434206662583, -7.627207830600332805 ) ) ;
#22406=CARTESIAN_POINT ( 'NONE',  ( 115.1220548109119761, -8.166667518702817929, -8.995218007635861213 ) ) ;
#22407=CARTESIAN_POINT ( 'NONE',  ( 114.3846081442453197, 0.4262465694468514643, -12.03445270309931736 ) ) ;
#22408=CARTESIAN_POINT ( 'NONE',  ( 120.1707281442453166, -9.565557343593413364, -10.61323700422348004 ) ) ;
#22411=CARTESIAN_POINT ( 'NONE',  ( 120.3976348109119812, -7.643976991954077427, -18.09477374809248928 ) ) ;
#22412=CARTESIAN_POINT ( 'NONE',  ( 124.8790414775786246, -8.899110576539710493, -16.42337572283490132 ) ) ;
#22416=CARTESIAN_POINT ( 'NONE',  ( 116.8805814775786445, -6.344957434206662583, -7.627207830600332805 ) ) ;
#22418=CARTESIAN_POINT ( 'NONE',  ( 119.6601881442453106, -8.166667518702819706, -8.995218007635861213 ) ) ;
#22419=DIRECTION ( 'NONE',  ( 0.000000000000000000, 0.6004852223388321697, -0.7996358532186279566 ) ) ;
#22421=CARTESIAN_POINT ( 'NONE',  ( 118.0151148109119816, -10.63000616557722466, -14.87417383870573495 ) ) ;
#22423=CARTESIAN_POINT ( 'NONE',  ( 118.8092881442453290, -9.988377603198976828, -10.36322818467138340 ) ) ;
#22429=CARTESIAN_POINT ( 'NONE',  ( 120.0005481442453146, -4.153390946401325223, -8.397313243818185668 ) ) ;
#22432=CARTESIAN_POINT ( 'NONE',  ( 113.0798948109119948, -8.899110576539710493, -16.42337572283490132 ) ) ;
#22435=CARTESIAN_POINT ( 'NONE',  ( 112.6828081442453282, -2.084020599724406786, -8.691656652584148546 ) ) ;
#22436=CARTESIAN_POINT ( 'NONE',  ( 119.0361948109119652, -7.893985811506177619, -18.51759400769804742 ) ) ;
#22438=CARTESIAN_POINT ( 'NONE',  ( 116.8238548109119819, -5.574606645277164318, -18.38911715685844683 ) ) ;
#22439=CARTESIAN_POINT ( 'NONE',  ( 114.0442481442453300, -1.834011780172310813, -8.268836392978581529 ) ) ;
#22440=CARTESIAN_POINT ( 'NONE',  ( 122.4397948109119767, -9.988377603198976828, -10.36322818467138340 ) ) ;
#22442=CARTESIAN_POINT ( 'NONE',  ( 119.8303681442453126, 0.4262465694468514643, -12.03445270309931736 ) ) ;
#22444=CARTESIAN_POINT ( 'NONE',  ( 125.1626748109119802, -0.1624402480850797581, -16.17319339645315424 ) ) ;
#22445=CARTESIAN_POINT ( 'NONE',  ( 119.6601881442453106, -8.166667518702819706, -8.995218007635861213 ) ) ;
#22447=CARTESIAN_POINT ( 'NONE',  ( 122.0994348109119443, 0.9020085738987339008, -11.91225656197089222 ) ) ;
#22448=CARTESIAN_POINT ( 'NONE',  ( 151.2860562277021472, -1.295815253274133161, -16.89579513612386563 ) ) ;
#22450=CARTESIAN_POINT ( 'NONE',  ( 128.0347018188450932, -2.863786252703732771, -14.80791975478640587 ) ) ;
#22454=CARTESIAN_POINT ( 'NONE',  ( 116.1431348109119881, 0.1319031606808879209, -14.10382304977623669 ) ) ;
#22455=CARTESIAN_POINT ( 'NONE',  ( 112.1722681442453222, -8.899110576539710493, -16.42337572283490132 ) ) ;
#22460=CARTESIAN_POINT ( 'NONE',  ( 116.5402214775786405, -9.565557343593413364, -10.61323700422348004 ) ) ;
#22461=CARTESIAN_POINT ( 'NONE',  ( 113.6680897606643441, -2.236191541394345172, -18.14152338500401029 ) ) ;
#22462=CARTESIAN_POINT ( 'NONE',  ( 119.1871698793805194, -2.191907684172563986, -18.20049396185734025 ) ) ;
#22465=CARTESIAN_POINT ( 'NONE',  ( 124.2550481442452792, -9.988377603198980381, -10.36322818467138518 ) ) ;
#22466=CARTESIAN_POINT ( 'NONE',  ( 122.5532481442453019, 0.4262465694468514643, -12.03445270309931736 ) ) ;
#22471=CARTESIAN_POINT ( 'NONE',  ( 124.2550481442452792, -0.1624402480850797581, -16.17319339645315424 ) ) ;
#22473=CARTESIAN_POINT ( 'NONE',  ( 121.5321681442453183, -0.1624402480850797581, -16.17319339645315424 ) ) ;
#22474=CARTESIAN_POINT ( 'NONE',  ( 114.6682414775786469, -7.894159318335828068, -9.358103419637847864 ) ) ;
#22477=CARTESIAN_POINT ( 'NONE',  ( 123.2906948109119867, -1.833838273342659697, -17.42832698103878286 ) ) ;
#22478=CARTESIAN_POINT ( 'NONE',  ( 122.7801548109119665, -6.222761293078241884, -8.102969835052219238 ) ) ;
#22484=CARTESIAN_POINT ( 'NONE',  ( 119.7736414775786358, -10.30919188438810075, -12.61870101168855918 ) ) ;
#22485=CARTESIAN_POINT ( 'NONE',  ( 118.6958348109119754, -6.344957434206665248, -7.627207830600338134 ) ) ;
#22487=CARTESIAN_POINT ( 'NONE',  ( 116.9940348109119839, -9.988377603198976828, -10.36322818467138340 ) ) ;
#22491=CARTESIAN_POINT ( 'NONE',  ( 120.3409081442453044, -0.4660016031367893996, -10.09054647747474043 ) ) ;
#22492=CARTESIAN_POINT ( 'NONE',  ( 124.8223148109119762, -10.15424416112533912, -14.75197769757731336 ) ) ;
#22494=CARTESIAN_POINT ( 'NONE',  ( 114.5547881442453217, -4.153390946401321671, -8.397313243818183892 ) ) ;
#22495=CARTESIAN_POINT ( 'NONE',  ( 111.9453614775786434, -7.894159318335828068, -9.358103419637847864 ) ) ;
#22499=CARTESIAN_POINT ( 'NONE',  ( 119.6601881442453106, -1.833838273342659253, -17.42832698103878286 ) ) ;
#22506=CARTESIAN_POINT ( 'NONE',  ( 122.8368814775786291, -1.561330072975668948, -17.79121239304076951 ) ) ;
#22509=CARTESIAN_POINT ( 'NONE',  ( 117.6747548109119919, -7.643976991954077427, -18.09477374809248928 ) ) ;
#22510=CARTESIAN_POINT ( 'NONE',  ( 112.1722681442453222, -0.4660016031367893996, -10.09054647747474043 ) ) ;
#22512=CARTESIAN_POINT ( 'NONE',  ( 122.2696148109119889, -5.574606645277164318, -18.38911715685844683 ) ) ;
#22514=CARTESIAN_POINT ( 'NONE',  ( 124.5954081442453116, -6.222761293078241884, -8.102969835052219238 ) ) ;
#22516=CARTESIAN_POINT ( 'NONE',  ( 121.7590748109119687, -7.893985811506177619, -18.51759400769804742 ) ) ;
#22517=CARTESIAN_POINT ( 'NONE',  ( 118.4689281442453250, -10.15424416112533912, -14.75197769757731336 ) ) ;
#22518=CARTESIAN_POINT ( 'NONE',  ( 124.7655881442452852, -9.859900752359378018, -12.68260735090039759 ) ) ;
#22520=CARTESIAN_POINT ( 'NONE',  ( 118.1852948109119836, -5.638512984488999180, -18.83840828888717311 ) ) ;
#22521=CARTESIAN_POINT ( 'NONE',  ( 115.4056881442453459, -7.893985811506177619, -18.51759400769804742 ) ) ;
#22525=CARTESIAN_POINT ( 'NONE',  ( 123.5176014775786228, -0.8288870151387760510, -10.36305467784173118 ) ) ;
#22526=ORIENTED_EDGE ( 'NONE', *, *, #37026, .F. ) ;
#22527=CARTESIAN_POINT ( 'NONE',  ( 119.3198281442452924, 0.5811942927096110934, -14.16772938898807510 ) ) ;
#22530=DIRECTION ( 'NONE',  ( 0.000000000000000000, -0.6004852223388319477, 0.7996358532186282897 ) ) ;
#22531=CARTESIAN_POINT ( 'NONE',  ( 114.0442481442453300, -7.643976991954077427, -18.09477374809248928 ) ) ;
#22533=CARTESIAN_POINT ( 'NONE',  ( 124.3117748109119844, -10.30919188438810075, -12.61870101168855918 ) ) ;
#22534=ORIENTED_EDGE ( 'NONE', *, *, #41606, .F. ) ;
#22536=CARTESIAN_POINT ( 'NONE',  ( 123.5176014775786228, -0.8288870151387760510, -10.36305467784173118 ) ) ;
#22539=CARTESIAN_POINT ( 'NONE',  ( 112.0126281442453120, -9.814174330883659536, -12.68911139247490105 ) ) ;
#22542=CARTESIAN_POINT ( 'NONE',  ( 113.2500748109119968, -6.344957434206662583, -7.627207830600332805 ) ) ;
#22544=CARTESIAN_POINT ( 'NONE',  ( 122.8368814775786291, -7.894159318335828068, -9.358103419637847864 ) ) ;
#22545=CARTESIAN_POINT ( 'NONE',  ( 115.0086014775786509, -5.574606645277164318, -18.38911715685844683 ) ) ;
#22546=CARTESIAN_POINT ( 'NONE',  ( 116.0086969107182142, -2.467220198592777525, -17.83387418641524391 ) ) ;
#22548=CARTESIAN_POINT ( 'NONE',  ( 115.7460481442453357, 0.9020085738987339008, -11.91225656197089222 ) ) ;
#22550=CARTESIAN_POINT ( 'NONE',  ( 124.0848681442452772, -4.089484607189486809, -7.948022111789456723 ) ) ;
#22551=B_SPLINE_CURVE_WITH_KNOTS ( 'NONE', 3,
 ( #35503, #38703, #18193, #7470, #21838, #10471, #13882, #35270, #21388, #27793 ),
 .UNSPECIFIED., .F., .F.,
 ( 4, 3, 3, 4 ),
 ( 0.000000000000000000, 0.0001671877548681299829, 0.0003343755096277750216, 0.0006463528481650629171 ),
 .UNSPECIFIED. ) ;
#22554=CARTESIAN_POINT ( 'NONE',  ( 115.2922348109119781, -10.63000616557722466, -14.87417383870573495 ) ) ;
#22555=CARTESIAN_POINT ( 'NONE',  ( 111.9453614775786434, -7.894159318335828068, -9.358103419637847864 ) ) ;
#22557=CARTESIAN_POINT ( 'NONE',  ( 112.0020881442453344, 0.2603800115204892296, -16.42320221600525088 ) ) ;
#22559=CARTESIAN_POINT ( 'NONE',  ( 118.5256548109119876, -0.4660016031367893996, -10.09054647747474043 ) ) ;
#22563=CARTESIAN_POINT ( 'NONE',  ( 111.6050014775786536, 0.1319031606808879209, -14.10382304977624379 ) ) ;
#22564=CARTESIAN_POINT ( 'NONE',  ( 136.1673833308556993, -2.578395149234233852, -7.983002144439000247 ) ) ;
#22565=CARTESIAN_POINT ( 'NONE',  ( 113.8740681442453138, -9.859900752359374465, -12.68260735090039404 ) ) ;
#22569=CARTESIAN_POINT ( 'NONE',  ( 113.9307948109119764, -10.15424416112533912, -14.75197769757731336 ) ) ;
#22571=CARTESIAN_POINT ( 'NONE',  ( 113.4769814775786330, -10.63000616557722466, -14.87417383870573495 ) ) ;
#22573=CARTESIAN_POINT ( 'NONE',  ( 123.4041481442452834, 0.1319031606808879209, -14.10382304977623669 ) ) ;
#22574=CARTESIAN_POINT ( 'NONE',  ( 112.1722681442453222, -8.899110576539710493, -16.42337572283490132 ) ) ;
#22575=CARTESIAN_POINT ( 'NONE',  ( 122.4397948109119767, -9.988377603198976828, -10.36322818467138340 ) ) ;
#22577=CARTESIAN_POINT ( 'NONE',  ( 122.3263414775786373, -6.344957434206665248, -7.627207830600338134 ) ) ;
#22579=CARTESIAN_POINT ( 'NONE',  ( 127.2313854076963509, -8.461403773221835678, -17.56217400450200472 ) ) ;
#22583=EDGE_CURVE ( 'NONE', #10303, #30977, #24173, .T. ) ;
#22584=CARTESIAN_POINT ( 'NONE',  ( 126.9276200068699723, -9.934318824270198078, -11.67164607367653417 ) ) ;
#22585=CARTESIAN_POINT ( 'NONE',  ( 116.7104014775786425, -0.4660016031367893996, -10.09054647747474043 ) ) ;
#22589=ADVANCED_FACE ( 'NONE', ( #43940 ), #12936, .F. ) ;
#22590=CARTESIAN_POINT ( 'NONE',  ( 115.9729548109119861, -3.505236298600246325, -18.68346056562440793 ) ) ;
#22592=CARTESIAN_POINT ( 'NONE',  ( 118.0718414775786300, -9.261995988541697145, -16.69588392320189030 ) ) ;
#22596=CARTESIAN_POINT ( 'NONE',  ( 127.7184548109119788, -4.683672500039348208, -14.88233656108870662 ) ) ;
#22597=CARTESIAN_POINT ( 'NONE',  ( 119.3765548109119834, -10.15424416112533912, -14.75197769757731336 ) ) ;
#22598=CARTESIAN_POINT ( 'NONE',  ( 115.2922348109119781, -10.63000616557722466, -14.87417383870573495 ) ) ;
#22600=CARTESIAN_POINT ( 'NONE',  ( 116.5402214775786405, 0.2603800115204892296, -16.42320221600525088 ) ) ;
#22602=CARTESIAN_POINT ( 'NONE',  ( 122.7801548109119665, -6.222761293078241884, -8.102969835052219238 ) ) ;
#22603=CARTESIAN_POINT ( 'NONE',  ( 117.9016614775786280, -0.1624402480850797581, -16.17319339645315424 ) ) ;
#22607=CARTESIAN_POINT ( 'NONE',  ( 114.2144281442453178, -8.166667518702817929, -8.995218007635859436 ) ) ;
#22608=CARTESIAN_POINT ( 'NONE',  ( 118.5256548109119876, -8.899110576539710493, -16.42337572283490132 ) ) ;
#22612=CARTESIAN_POINT ( 'NONE',  ( 114.1009748109119784, -4.089484607189486809, -7.948022111789456723 ) ) ;
#22616=EDGE_LOOP ( 'NONE', ( #39737, #27725, #27153, #21197 ) ) ;
#22617=CARTESIAN_POINT ( 'NONE',  ( 120.5678148109119832, -1.833838273342659253, -17.42832698103878286 ) ) ;
#22618=CARTESIAN_POINT ( 'NONE',  ( 120.9081748109119872, -4.153390946401325223, -8.397313243818185668 ) ) ;
#22626=CARTESIAN_POINT ( 'NONE',  ( 116.2565881442452991, -9.261995988541697145, -16.69588392320189030 ) ) ;
#22627=CARTESIAN_POINT ( 'NONE',  ( 113.9875214775786532, -0.4660016031367893996, -10.09054647747474043 ) ) ;
#22628=CARTESIAN_POINT ( 'NONE',  ( 115.2922348109119781, 0.4262465694468514643, -12.03445270309931736 ) ) ;
#22629=CARTESIAN_POINT ( 'NONE',  ( 120.7947214775786193, -0.8288870151387760510, -10.36305467784173118 ) ) ;
#22632=CARTESIAN_POINT ( 'NONE',  ( 120.8514481442452961, -2.084020599724406786, -8.691656652584148546 ) ) ;
#22633=CARTESIAN_POINT ( 'NONE',  ( 123.5176014775786228, -0.8288870151387760510, -10.36305467784173118 ) ) ;
#22639=CARTESIAN_POINT ( 'NONE',  ( 116.9373081442452929, -8.166667518702817929, -8.995218007635861213 ) ) ;
#22642=CARTESIAN_POINT ( 'NONE',  ( 119.4332814775786318, -0.4660016031367893996, -10.09054647747474043 ) ) ;
#22645=CARTESIAN_POINT ( 'NONE',  ( 117.3911214775786505, -1.561330072975668504, -17.79121239304076951 ) ) ;
#22646=CARTESIAN_POINT ( 'NONE',  ( 117.8449348109119938, -8.166667518702817929, -8.995218007635861213 ) ) ;
#22647=CARTESIAN_POINT ( 'NONE',  ( 111.2751814775786556, -7.618532446445550832, -18.05174138884716939 ) ) ;
#22652=CARTESIAN_POINT ( 'NONE',  ( 120.7947214775786193, -0.8288870151387760510, -10.36305467784173118 ) ) ;
#22655=CARTESIAN_POINT ( 'NONE',  ( 119.2063748109119814, -7.894159318335828068, -9.358103419637847864 ) ) ;
#22658=CARTESIAN_POINT ( 'NONE',  ( 112.5693548109119888, 0.4262465694468514643, -12.03445270309931736 ) ) ;
#22659=CARTESIAN_POINT ( 'NONE',  ( 121.3052614775786111, -1.834011780172310813, -8.268836392978581529 ) ) ;
#22661=CARTESIAN_POINT ( 'NONE',  ( 120.3409081442453044, -8.899110576539710493, -16.42337572283490132 ) ) ;
#22662=CARTESIAN_POINT ( 'NONE',  ( 116.4267681442453153, -3.383040157471821630, -19.15922257007629170 ) ) ;
#22664=CARTESIAN_POINT ( 'NONE',  ( 120.3976348109119812, -1.834011780172310813, -8.268836392978581529 ) ) ;
#22665=CARTESIAN_POINT ( 'NONE',  ( 118.4689281442453250, -10.15424416112533912, -14.75197769757731336 ) ) ;
#22667=CARTESIAN_POINT ( 'NONE',  ( 125.5030348109119558, -6.222761293078241884, -8.102969835052219238 ) ) ;
#22669=CARTESIAN_POINT ( 'NONE',  ( 120.8514481442452961, -7.893985811506177619, -18.51759400769804742 ) ) ;
#22671=CARTESIAN_POINT ( 'NONE',  ( 124.6521348109119884, -1.561330072975668948, -17.79121239304076951 ) ) ;
#22674=CARTESIAN_POINT ( 'NONE',  ( 137.4462468446473338, -1.251634937223135013, -16.95462783242788518 ) ) ;
#22677=CARTESIAN_POINT ( 'NONE',  ( 136.8611794030155409, -10.05647304890296212, -11.41738541814965124 ) ) ;
#22678=CARTESIAN_POINT ( 'NONE',  ( 119.7169148109119874, -0.1624402480850797581, -16.17319339645315424 ) ) ;
#22679=CARTESIAN_POINT ( 'NONE',  ( 125.8433948109119456, -1.834011780172310813, -8.268836392978581529 ) ) ;
#22684=CARTESIAN_POINT ( 'NONE',  ( 116.8238548109119819, -5.574606645277164318, -18.38911715685844683 ) ) ;
#22690=CARTESIAN_POINT ( 'NONE',  ( 124.5954081442453116, -3.383040157471821630, -19.15922257007629170 ) ) ;
#22692=CARTESIAN_POINT ( 'NONE',  ( 123.9714148109119805, -8.899110576539710493, -16.42337572283490132 ) ) ;
#22693=ORIENTED_EDGE ( 'NONE', *, *, #19023, .F. ) ;
#22695=CARTESIAN_POINT ( 'NONE',  ( 126.2184548109120072, 0.08211594521788213863, -14.12586826872868961 ) ) ;
#22698=CARTESIAN_POINT ( 'NONE',  ( 123.1205148109119563, -7.643976991954077427, -18.09477374809248928 ) ) ;
#22699=CARTESIAN_POINT ( 'NONE',  ( 119.0929214775786278, -4.153390946401325223, -8.397313243818185668 ) ) ;
#22707=CARTESIAN_POINT ( 'NONE',  ( 120.9649014775786355, -3.383040157471821630, -19.15922257007629170 ) ) ;
#22708=CARTESIAN_POINT ( 'NONE',  ( 117.4478481442453131, 0.2603800115204892296, -16.42320221600525088 ) ) ;
#22710=CARTESIAN_POINT ( 'NONE',  ( 116.2565881442452991, -9.261995988541697145, -16.69588392320189030 ) ) ;
#22712=ORIENTED_EDGE ( 'NONE', *, *, #26957, .F. ) ;
#22714=CARTESIAN_POINT ( 'NONE',  ( 122.7234281442452755, -5.638512984488999180, -18.83840828888717311 ) ) ;
#22715=CARTESIAN_POINT ( 'NONE',  ( 121.3052614775786111, -1.834011780172310813, -8.268836392978581529 ) ) ;
#22716=CARTESIAN_POINT ( 'NONE',  ( 125.7866681442452688, -8.899110576539710493, -16.42337572283490132 ) ) ;
#22717=CARTESIAN_POINT ( 'NONE',  ( 114.4980614775786734, -2.084020599724406786, -8.691656652584148546 ) ) ;
#22718=CARTESIAN_POINT ( 'NONE',  ( 124.7655881442452852, 0.5811942927096110934, -14.16772938898807510 ) ) ;
#22720=CARTESIAN_POINT ( 'NONE',  ( 118.3554748109119998, -9.565557343593413364, -10.61323700422348004 ) ) ;
#22723=ORIENTED_EDGE ( 'NONE', *, *, #7558, .T. ) ;
#22726=CARTESIAN_POINT ( 'NONE',  ( 123.5176014775786228, -9.261995988541697145, -16.69588392320189030 ) ) ;
#22727=CARTESIAN_POINT ( 'NONE',  ( 125.3328548109119964, -0.8288870151387760510, -10.36305467784173118 ) ) ;
#22730=CARTESIAN_POINT ( 'NONE',  ( 118.7525614775786380, -1.833838273342659253, -17.42832698103878286 ) ) ;
#22731=CARTESIAN_POINT ( 'NONE',  ( 112.2857214775786474, -4.089484607189486809, -7.948022111789456723 ) ) ;
#22733=CARTESIAN_POINT ( 'NONE',  ( 122.6099748109119929, -0.8288870151387760510, -10.36305467784173118 ) ) ;
#22735=CARTESIAN_POINT ( 'NONE',  ( 125.2194014775786286, 0.1319031606808879209, -14.10382304977623669 ) ) ;
#22737=CARTESIAN_POINT ( 'NONE',  ( 122.2696148109119889, -4.089484607189486809, -7.948022111789456723 ) ) ;
#22738=CARTESIAN_POINT ( 'NONE',  ( 116.6536748109119941, -10.15424416112533912, -14.75197769757731336 ) ) ;
#22739=CARTESIAN_POINT ( 'NONE',  ( 121.2485348109119769, -8.899110576539710493, -16.42337572283490132 ) ) ;
#22741=CARTESIAN_POINT ( 'NONE',  ( 123.0070614775786169, 0.9020085738987339008, -11.91225656197089222 ) ) ;
#22742=CARTESIAN_POINT ( 'NONE',  ( 115.1787814775786387, -9.988377603198976828, -10.36322818467138340 ) ) ;
#22744=FACE_OUTER_BOUND ( 'NONE', #32752, .T. ) ;
#22745=CARTESIAN_POINT ( 'NONE',  ( 124.0848681442452772, -5.574606645277164318, -18.38911715685844683 ) ) ;
#22747=CARTESIAN_POINT ( 'NONE',  ( 123.6877814775786533, -3.383040157471821630, -19.15922257007629170 ) ) ;
#22750=CYLINDRICAL_SURFACE ( 'NONE', #16093, 1.999999999999999556 ) ;
#22751=CARTESIAN_POINT ( 'NONE',  ( 114.4980614775786734, -2.084020599724406786, -8.691656652584148546 ) ) ;
#22752=AXIS2_PLACEMENT_3D ( 'NONE', #8348, #12680, #29320 ) ;
#22756=CARTESIAN_POINT ( 'NONE',  ( 124.0848681442452772, -5.574606645277164318, -18.38911715685844683 ) ) ;
#22764=CARTESIAN_POINT ( 'NONE',  ( 120.0005481442453146, -5.638512984488999180, -18.83840828888717311 ) ) ;
#22765=CARTESIAN_POINT ( 'NONE',  ( 113.0798948109119948, -0.4660016031367885114, -10.09054647747474220 ) ) ;
#22766=CARTESIAN_POINT ( 'NONE',  ( 123.1772414775786189, -5.574606645277164318, -18.38911715685844683 ) ) ;
#22767=CARTESIAN_POINT ( 'NONE',  ( 116.3133148109120043, -2.084020599724406786, -8.691656652584148546 ) ) ;
#22770=CARTESIAN_POINT ( 'NONE',  ( 114.6115148109119986, -3.383040157471821630, -19.15922257007629170 ) ) ;
#22772=CARTESIAN_POINT ( 'NONE',  ( 122.4397948109119767, -9.988377603198976828, -10.36322818467138340 ) ) ;
#22777=CARTESIAN_POINT ( 'NONE',  ( 112.6828081442453282, -7.893985811506177619, -18.51759400769804742 ) ) ;
#22780=CARTESIAN_POINT ( 'NONE',  ( 114.5547881442453217, -4.153390946401321671, -8.397313243818183892 ) ) ;
#22782=CARTESIAN_POINT ( 'NONE',  ( 126.2455040230458536, -5.344711546414948167, -18.38488247629714678 ) ) ;
#22783=CARTESIAN_POINT ( 'NONE',  ( 125.7299414775786346, -10.15424416112533912, -14.75197769757731336 ) ) ;
#22785=CARTESIAN_POINT ( 'NONE',  ( 122.6667014775786413, -7.893985811506177619, -18.51759400769804742 ) ) ;
#22787=CARTESIAN_POINT ( 'NONE',  ( 115.8150068052895563, -1.125321370491268125, -17.12283323191015327 ) ) ;
#22788=CARTESIAN_POINT ( 'NONE',  ( 111.5125327111057345, -1.267766418764825875, -16.93314635290698789 ) ) ;
#22789=CARTESIAN_POINT ( 'NONE',  ( 123.4844656136282026, -4.072025463651757882, -15.69684013478500972 ) ) ;
#22790=CARTESIAN_POINT ( 'NONE',  ( 113.9875214775786532, -8.899110576539710493, -16.42337572283490132 ) ) ;
#22794=CARTESIAN_POINT ( 'NONE',  ( 126.0703014775786102, -9.988377603198980381, -10.36322818467138518 ) ) ;
#22795=CARTESIAN_POINT ( 'NONE',  ( 112.9664414775786412, 0.5811942927096154232, -14.16772938898807155 ) ) ;
#22797=CARTESIAN_POINT ( 'NONE',  ( 126.2404814775786264, -0.8288870151387760510, -10.36305467784173118 ) ) ;
#22798=CARTESIAN_POINT ( 'NONE',  ( 116.0864081442453113, -0.1624402480850797581, -16.17319339645315424 ) ) ;
#22799=CARTESIAN_POINT ( 'NONE',  ( 122.6099748109119929, -9.261995988541697145, -16.69588392320189030 ) ) ;
#22800=CARTESIAN_POINT ( 'NONE',  ( 120.1707281442453166, 0.2603800115204892296, -16.42320221600525088 ) ) ;
#22808=CARTESIAN_POINT ( 'NONE',  ( 116.7671281442453335, -1.834011780172310813, -8.268836392978581529 ) ) ;
#22813=CARTESIAN_POINT ( 'NONE',  ( 114.1009748109119784, -5.574606645277164318, -18.38911715685844683 ) ) ;
#22816=CARTESIAN_POINT ( 'NONE',  ( 118.4122014775786340, 0.5811942927096110934, -14.16772938898807510 ) ) ;
#22820=VERTEX_POINT ( 'NONE', #3771 ) ;
#22821=CARTESIAN_POINT ( 'NONE',  ( 120.5887993777725029, -1.267766418764730840, -16.93314635290706605 ) ) ;
#22822=CARTESIAN_POINT ( 'NONE',  ( 117.1642148109119859, -0.8288870151387760510, -10.36305467784173118 ) ) ;
#22824=CARTESIAN_POINT ( 'NONE',  ( 119.0361948109119652, -7.893985811506177619, -18.51759400769804742 ) ) ;
#22825=CARTESIAN_POINT ( 'NONE',  ( 112.9664414775786412, -9.859900752359374465, -12.68260735090039404 ) ) ;
#22826=CARTESIAN_POINT ( 'NONE',  ( 114.7816948109119863, 0.5811942927096154232, -14.16772938898807155 ) ) ;
#22828=CARTESIAN_POINT ( 'NONE',  ( 122.7234281442452755, -4.153390946401325223, -8.397313243818185668 ) ) ;
#22829=CARTESIAN_POINT ( 'NONE',  ( 121.0783548109119749, -9.565557343593413364, -10.61323700422348004 ) ) ;
#22832=CIRCLE ( 'NONE', #9732, 5.999999999999997335 ) ;
#22833=CARTESIAN_POINT ( 'NONE',  ( 114.0442481442453300, -1.834011780172310813, -8.268836392978581529 ) ) ;
#22834=CARTESIAN_POINT ( 'NONE',  ( 120.3409081442453044, -8.899110576539710493, -16.42337572283490132 ) ) ;
#22840=CARTESIAN_POINT ( 'NONE',  ( 119.8870948109119752, -9.261995988541697145, -16.69588392320189030 ) ) ;
#22842=CARTESIAN_POINT ( 'NONE',  ( 117.6180281442453150, -8.899110576539710493, -16.42337572283490132 ) ) ;
#22845=CARTESIAN_POINT ( 'NONE',  ( 120.7947214775786193, -0.8288870151387760510, -10.36305467784173118 ) ) ;
#22846=CARTESIAN_POINT ( 'NONE',  ( 121.3619881442452879, -5.574606645277164318, -18.38911715685844683 ) ) ;
#22851=CARTESIAN_POINT ( 'NONE',  ( 116.5969481442453031, 0.5811942927096154232, -14.16772938898807155 ) ) ;
#22853=CARTESIAN_POINT ( 'NONE',  ( 117.5045748109119756, 0.5811942927096110934, -14.16772938898807510 ) ) ;
#22854=CARTESIAN_POINT ( 'NONE',  ( 114.3846081442453197, -10.63000616557722466, -14.87417383870573495 ) ) ;
#22855=CARTESIAN_POINT ( 'NONE',  ( 115.2355081442453155, 0.1319031606808879209, -14.10382304977623669 ) ) ;
#22856=CARTESIAN_POINT ( 'NONE',  ( 122.6099748109119929, -0.8288870151387760510, -10.36305467784173118 ) ) ;
#22857=CARTESIAN_POINT ( 'NONE',  ( 113.5904348109119866, -7.893985811506177619, -18.51759400769804742 ) ) ;
#22859=CARTESIAN_POINT ( 'NONE',  ( 124.3685014775786328, 0.4262465694468514643, -12.03445270309931736 ) ) ;
#22860=CARTESIAN_POINT ( 'NONE',  ( 113.8197041868944979, -2.239543233855025850, -18.13706010537467606 ) ) ;
#22864=CARTESIAN_POINT ( 'NONE',  ( 120.4543614775786295, -4.089484607189486809, -7.948022111789456723 ) ) ;
#22866=CARTESIAN_POINT ( 'NONE',  ( 119.9438214775786378, -7.893985811506177619, -18.51759400769804742 ) ) ;
#22869=CARTESIAN_POINT ( 'NONE',  ( 120.5678148109119832, -8.166667518702819706, -8.995218007635861213 ) ) ;
#22870=CARTESIAN_POINT ( 'NONE',  ( 115.8595014775786609, -1.834011780172310813, -8.268836392978581529 ) ) ;
#22874=CYLINDRICAL_SURFACE ( 'NONE', #22313, 5.999999999999997335 ) ;
#22876=CARTESIAN_POINT ( 'NONE',  ( 119.3198281442452924, -9.859900752359374465, -12.68260735090039404 ) ) ;
#22879=CARTESIAN_POINT ( 'NONE',  ( 119.5467348109119712, -5.574606645277164318, -18.38911715685844683 ) ) ;
#22882=CARTESIAN_POINT ( 'NONE',  ( 114.1577014775786552, -3.505236298600246325, -18.68346056562440793 ) ) ;
#22883=CARTESIAN_POINT ( 'NONE',  ( 123.0070614775786169, 0.9020085738987339008, -11.91225656197089222 ) ) ;
#22887=CARTESIAN_POINT ( 'NONE',  ( 122.2696148109119889, -5.574606645277164318, -18.38911715685844683 ) ) ;
#22888=CARTESIAN_POINT ( 'NONE',  ( 113.3635281442453504, -9.988377603198976828, -10.36322818467138340 ) ) ;
#22889=CARTESIAN_POINT ( 'NONE',  ( 122.3263414775786373, -6.344957434206665248, -7.627207830600338134 ) ) ;
#22890=CARTESIAN_POINT ( 'NONE',  ( 123.0070614775786169, -10.15424416112533912, -14.75197769757731336 ) ) ;
#22892=CARTESIAN_POINT ( 'NONE',  ( 123.9714148109119805, -8.899110576539710493, -16.42337572283490132 ) ) ;
#22893=CARTESIAN_POINT ( 'NONE',  ( 124.7088614775786226, 0.2603800115204892296, -16.42320221600525088 ) ) ;
#22895=CARTESIAN_POINT ( 'NONE',  ( 126.2404814775786264, -9.261995988541697145, -16.69588392320189030 ) ) ;
#22900=CARTESIAN_POINT ( 'NONE',  ( 127.7500697630001554, -3.418455135964745484, -14.06918277244200510 ) ) ;
#22904=CARTESIAN_POINT ( 'NONE',  ( 117.1519828165343853, -2.324775150319241757, -18.02356106541842706 ) ) ;
#22905=CARTESIAN_POINT ( 'NONE',  ( 120.3976348109119812, -7.643976991954077427, -18.09477374809248928 ) ) ;
#22906=CARTESIAN_POINT ( 'NONE',  ( 123.8579614775786126, 0.5811942927096110934, -14.16772938898807510 ) ) ;
#22907=CARTESIAN_POINT ( 'NONE',  ( 126.2184548109119788, -5.614349408395407970, -18.33681267546239724 ) ) ;
#22911=CARTESIAN_POINT ( 'NONE',  ( 116.3133148109120043, -2.084020599724406786, -8.691656652584148546 ) ) ;
#22917=CARTESIAN_POINT ( 'NONE',  ( 121.3619881442452879, -4.089484607189486809, -7.948022111789456723 ) ) ;
#22918=CARTESIAN_POINT ( 'NONE',  ( 122.0994348109119443, -10.15424416112533912, -14.75197769757731336 ) ) ;
#22921=CARTESIAN_POINT ( 'NONE',  ( 126.2940345447965456, 0.06676713698955166754, -14.42618009100540277 ) ) ;
#22923=CARTESIAN_POINT ( 'NONE',  ( 121.0783548109119749, -9.565557343593413364, -10.61323700422348004 ) ) ;
#22924=CARTESIAN_POINT ( 'NONE',  ( 118.4122014775786340, -9.859900752359374465, -12.68260735090039404 ) ) ;
#22925=CARTESIAN_POINT ( 'NONE',  ( 119.4455134719562182, -1.125321370491285444, -17.12283323191017814 ) ) ;
#22933=CARTESIAN_POINT ( 'NONE',  ( 119.4900081442453086, -1.834011780172310813, -8.268836392978581529 ) ) ;
#22934=CARTESIAN_POINT ( 'NONE',  ( 121.3052614775786111, -1.834011780172310813, -8.268836392978581529 ) ) ;
#22936=CARTESIAN_POINT ( 'NONE',  ( 116.3700414775786527, -5.638512984488999180, -18.83840828888717311 ) ) ;
#22937=CARTESIAN_POINT ( 'NONE',  ( 112.5693548109119888, -10.63000616557722466, -14.87417383870573495 ) ) ;
#22942=CARTESIAN_POINT ( 'NONE',  ( 122.4965214775786251, -10.30919188438810075, -12.61870101168855918 ) ) ;
#22943=CARTESIAN_POINT ( 'NONE',  ( 121.7590748109119687, -7.893985811506177619, -18.51759400769804742 ) ) ;
#22944=CARTESIAN_POINT ( 'NONE',  ( 111.8319081442453182, -5.638512984488999180, -18.83840828888717311 ) ) ;
#22946=CARTESIAN_POINT ( 'NONE',  ( 125.9001214775786224, -4.089484607189486809, -7.948022111789456723 ) ) ;
#22947=CARTESIAN_POINT ( 'NONE',  ( 114.6115148109119986, -6.222761293078241884, -8.102969835052219238 ) ) ;
#22948=CARTESIAN_POINT ( 'NONE',  ( 124.0848681442452772, -4.089484607189486809, -7.948022111789456723 ) ) ;
#22952=CARTESIAN_POINT ( 'NONE',  ( 121.0216281442452981, -7.894159318335828068, -9.358103419637847864 ) ) ;
#22957=CARTESIAN_POINT ( 'NONE',  ( 123.2906948109119867, -8.166667518702819706, -8.995218007635861213 ) ) ;
#22964=CARTESIAN_POINT ( 'NONE',  ( 124.2550481442452792, -0.1624402480850797581, -16.17319339645315424 ) ) ;
#22966=CARTESIAN_POINT ( 'NONE',  ( 123.9146881442452894, -10.15424416112533912, -14.75197769757731336 ) ) ;
#22967=AXIS2_PLACEMENT_3D ( 'NONE', #33146, #4668, #18590 ) ;
#22969=EDGE_CURVE ( 'NONE', #18093, #3055, #23127, .T. ) ;
#22970=CARTESIAN_POINT ( 'NONE',  ( 125.5597614775786326, -1.561330072975669392, -17.79121239304076951 ) ) ;
#22971=CARTESIAN_POINT ( 'NONE',  ( 116.7671281442453335, -7.643976991954077427, -18.09477374809248928 ) ) ;
#22973=EDGE_LOOP ( 'NONE', ( #35774, #38524, #44521, #14478 ) ) ;
#22974=CARTESIAN_POINT ( 'NONE',  ( 124.8223148109119762, 0.9020085738987339008, -11.91225656197089222 ) ) ;
#22975=CARTESIAN_POINT ( 'NONE',  ( 115.3489614775786407, -9.261995988541697145, -16.69588392320189030 ) ) ;
#22977=CARTESIAN_POINT ( 'NONE',  ( 113.4202548109119846, 0.1319031606808879209, -14.10382304977623669 ) ) ;
#22979=CARTESIAN_POINT ( 'NONE',  ( 124.7655881442452852, -9.859900752359378018, -12.68260735090039759 ) ) ;
#22980=CARTESIAN_POINT ( 'NONE',  ( 122.7234281442452755, -5.638512984488999180, -18.83840828888717311 ) ) ;
#22985=CARTESIAN_POINT ( 'NONE',  ( 115.9162281442453093, -5.574606645277164318, -18.38911715685844683 ) ) ;
#22989=CARTESIAN_POINT ( 'NONE',  ( 124.1415948109119540, -3.505236298600246325, -18.68346056562440793 ) ) ;
#22996=CARTESIAN_POINT ( 'NONE',  ( 117.6180281442453150, -0.4660016031367893996, -10.09054647747474043 ) ) ;
#22997=CARTESIAN_POINT ( 'NONE',  ( 125.2761281442453054, 0.4262465694468514643, -12.03445270309931736 ) ) ;
#22998=CARTESIAN_POINT ( 'NONE',  ( 114.0442481442453300, -7.643976991954077427, -18.09477374809248928 ) ) ;
#23001=CARTESIAN_POINT ( 'NONE',  ( 115.6893214775786447, 0.5811942927096154232, -14.16772938898807155 ) ) ;
#23003=CARTESIAN_POINT ( 'NONE',  ( 125.8433948109119456, -1.834011780172310813, -8.268836392978581529 ) ) ;
#23007=CARTESIAN_POINT ( 'NONE',  ( 114.8384214775786489, 0.9020085738987339008, -11.91225656197089222 ) ) ;
#23008=CARTESIAN_POINT ( 'NONE',  ( 115.2355081442453155, 0.1319031606808879209, -14.10382304977623669 ) ) ;
#23011=CARTESIAN_POINT ( 'NONE',  ( 125.7866681442452688, -8.899110576539710493, -16.42337572283490132 ) ) ;
#23013=CARTESIAN_POINT ( 'NONE',  ( 121.8158014775786171, -5.638512984488999180, -18.83840828888717311 ) ) ;
#23018=CARTESIAN_POINT ( 'NONE',  ( 123.6047240866468684, -4.379635970098219921, -15.28718505432590113 ) ) ;
#23019=CARTESIAN_POINT ( 'NONE',  ( 113.2500748109119968, -3.505236298600246325, -18.68346056562440793 ) ) ;
#23023=AXIS2_PLACEMENT_3D ( 'NONE', #40209, #16040, #2112 ) ;
#23024=CARTESIAN_POINT ( 'NONE',  ( 125.5597614775786326, -1.561330072975669392, -17.79121239304076951 ) ) ;
#23025=APPLICATION_CONTEXT ( 'automotive_design' ) ;
#23026=CARTESIAN_POINT ( 'NONE',  ( 112.2289948109119848, -1.834011780172310813, -8.268836392978581529 ) ) ;
#23028=CARTESIAN_POINT ( 'NONE',  ( 113.6471614775786492, -5.638512984488999180, -18.83840828888717311 ) ) ;
#23029=CARTESIAN_POINT ( 'NONE',  ( 117.1074881442453233, 0.4262465694468514643, -12.03445270309931736 ) ) ;
#23030=CARTESIAN_POINT ( 'NONE',  ( 121.6456214775786293, -10.63000616557722466, -14.87417383870573495 ) ) ;
#23031=CARTESIAN_POINT ( 'NONE',  ( 121.2485348109119769, -0.4660016031367893996, -10.09054647747474043 ) ) ;
#23039=CARTESIAN_POINT ( 'NONE',  ( 119.1496481442453046, -3.383040157471821630, -19.15922257007629170 ) ) ;
#23041=CARTESIAN_POINT ( 'NONE',  ( 125.2761281442453054, -10.63000616557722466, -14.87417383870573495 ) ) ;
#23043=CARTESIAN_POINT ( 'NONE',  ( 120.7432071540078340, -2.348512537728041583, -17.99195118506215962 ) ) ;
#23044=CARTESIAN_POINT ( 'NONE',  ( 115.5758681442453053, -7.894159318335828068, -9.358103419637847864 ) ) ;
#23048=CARTESIAN_POINT ( 'NONE',  ( 121.5888948109119809, -10.30919188438810075, -12.61870101168855918 ) ) ;
#23053=CARTESIAN_POINT ( 'NONE',  ( 122.6667014775786413, -2.084020599724406786, -8.691656652584148546 ) ) ;
#23054=CARTESIAN_POINT ( 'NONE',  ( 118.7525614775786380, -8.166667518702819706, -8.995218007635861213 ) ) ;
#23055=CARTESIAN_POINT ( 'NONE',  ( 114.2144281442453178, -1.833838273342658809, -17.42832698103878286 ) ) ;
#23056=( BOUNDED_CURVE ( )  B_SPLINE_CURVE ( 2, ( #8578, #19735, #33620, #13581, #20650 ),
 .UNSPECIFIED., .F., .T. ) 
 B_SPLINE_CURVE_WITH_KNOTS ( ( 3, 2, 3 ),
 ( 0.06250000000000000000, 0.07031250000000000000, 0.07662175834314119416 ),
 .UNSPECIFIED. ) 
 CURVE ( )  GEOMETRIC_REPRESENTATION_ITEM ( )  RATIONAL_B_SPLINE_CURVE ( ( 1.000000000000000000, 0.9238795325112869605, 1.000000000000000000, 0.9385262470928680267, 0.9763430640195970289 ) ) 
 REPRESENTATION_ITEM ( '' )  );
#23057=CARTESIAN_POINT ( 'NONE',  ( 116.1998614775786507, -10.63000616557722466, -14.87417383870573495 ) ) ;
#23058=LINE ( 'NONE', #5714, #40975 ) ;
#23059=CARTESIAN_POINT ( 'NONE',  ( 121.7023481442452777, -0.8288870151387760510, -10.36305467784173118 ) ) ;
#23060=CARTESIAN_POINT ( 'NONE',  ( 117.9583881442453048, 0.1319031606808879209, -14.10382304977623669 ) ) ;
#23064=CARTESIAN_POINT ( 'NONE',  ( 113.6471614775786492, -5.638512984488999180, -18.83840828888717311 ) ) ;
#23065=CARTESIAN_POINT ( 'NONE',  ( 122.3830681442452857, -1.833838273342659697, -17.42832698103878286 ) ) ;
#23068=CARTESIAN_POINT ( 'NONE',  ( 119.2631014775786298, 0.2603800115204892296, -16.42320221600525088 ) ) ;
#23070=CARTESIAN_POINT ( 'NONE',  ( 116.8238548109119819, -5.574606645277164318, -18.38911715685844683 ) ) ;
#23072=VERTEX_POINT ( 'NONE', #29746 ) ;
#23074=CARTESIAN_POINT ( 'NONE',  ( 124.5954081442453116, -6.222761293078241884, -8.102969835052219238 ) ) ;
#23075=CARTESIAN_POINT ( 'NONE',  ( 119.9438214775786378, -2.084020599724406786, -8.691656652584148546 ) ) ;
#23081=CARTESIAN_POINT ( 'NONE',  ( 117.8449348109119938, -8.166667518702817929, -8.995218007635861213 ) ) ;
#23083=CARTESIAN_POINT ( 'NONE',  ( 115.4056881442453459, -7.893985811506177619, -18.51759400769804742 ) ) ;
#23084=CARTESIAN_POINT ( 'NONE',  ( 114.6682414775786469, -1.561330072975668060, -17.79121239304076596 ) ) ;
#23085=CARTESIAN_POINT ( 'NONE',  ( 116.3133148109120043, -2.084020599724406786, -8.691656652584148546 ) ) ;
#23086=CARTESIAN_POINT ( 'NONE',  ( 123.5743281442453139, -2.084020599724406786, -8.691656652584148546 ) ) ;
#23089=CARTESIAN_POINT ( 'NONE',  ( 122.2128881442453263, -7.643976991954077427, -18.09477374809248928 ) ) ;
#23090=DIRECTION ( 'NONE',  ( -1.000000000000000000, 0.000000000000000000, 0.000000000000000000 ) ) ;
#23091=EDGE_CURVE ( 'NONE', #34606, #25201, #39905, .T. ) ;
#23092=CARTESIAN_POINT ( 'NONE',  ( 113.7414098793805408, -2.191907684172563986, -18.20049396185734025 ) ) ;
#23096=CONICAL_SURFACE ( 'NONE', #33259, 5.999999999999997335, 0.4636476090008060935 ) ;
#23097=CARTESIAN_POINT ( 'NONE',  ( 123.1772414775786189, -4.089484607189486809, -7.948022111789456723 ) ) ;
#23099=EDGE_CURVE ( 'NONE', #34005, #11415, #31189, .T. ) ;
#23100=CARTESIAN_POINT ( 'NONE',  ( 119.3198281442452924, 0.5811942927096110934, -14.16772938898807510 ) ) ;
#23103=CARTESIAN_POINT ( 'NONE',  ( 119.3198281442452924, 0.5811942927096110934, -14.16772938898807510 ) ) ;
#23105=EDGE_CURVE ( 'NONE', #44717, #1202, #26162, .T. ) ;
#23106=CARTESIAN_POINT ( 'NONE',  ( 120.8514481442452961, -7.893985811506177619, -18.51759400769804742 ) ) ;
#23113=CARTESIAN_POINT ( 'NONE',  ( 114.3898204873411970, -2.348512537728063787, -17.99195118506216318 ) ) ;
#23114=CARTESIAN_POINT ( 'NONE',  ( 122.4965214775786251, 0.1319031606808879209, -14.10382304977623669 ) ) ;
#23117=CARTESIAN_POINT ( 'NONE',  ( 116.1998614775786507, 0.4262465694468514643, -12.03445270309931736 ) ) ;
#23118=CARTESIAN_POINT ( 'NONE',  ( 138.2184548109119930, -2.458068653496962686, -15.34808096303632396 ) ) ;
#23120=CARTESIAN_POINT ( 'NONE',  ( 113.1933481442453058, -5.574606645277164318, -18.38911715685844683 ) ) ;
#23121=CARTESIAN_POINT ( 'NONE',  ( 122.7801548109119665, -3.383040157471821630, -19.15922257007629170 ) ) ;
#23124=CARTESIAN_POINT ( 'NONE',  ( 122.0994348109119443, -10.15424416112533912, -14.75197769757731336 ) ) ;
#23125=CARTESIAN_POINT ( 'NONE',  ( 114.8384214775786489, 0.9020085738987339008, -11.91225656197089222 ) ) ;
#23126=CARTESIAN_POINT ( 'NONE',  ( 123.6877814775786533, -3.383040157471821630, -19.15922257007629170 ) ) ;
#23127=B_SPLINE_CURVE_WITH_KNOTS ( 'NONE', 3,
 ( #14948, #19037, #1700, #11534 ),
 .UNSPECIFIED., .F., .F.,
 ( 4, 4 ),
 ( 3.976470764362284670E-06, 0.0005769793764277350448 ),
 .UNSPECIFIED. ) ;
#23128=CARTESIAN_POINT ( 'NONE',  ( 122.7801548109119665, -6.222761293078241884, -8.102969835052219238 ) ) ;
#23130=CARTESIAN_POINT ( 'NONE',  ( 123.7184548109119788, -5.764726629347491027, -12.19376142051037348 ) ) ;
#23131=CARTESIAN_POINT ( 'NONE',  ( 122.6667014775786413, -7.893985811506177619, -18.51759400769804742 ) ) ;
#23132=CARTESIAN_POINT ( 'NONE',  ( 113.8173414775786512, -9.565557343593413364, -10.61323700422348004 ) ) ;
#23134=CARTESIAN_POINT ( 'NONE',  ( 123.6310548109119765, -5.638512984488999180, -18.83840828888717311 ) ) ;
#23138=CARTESIAN_POINT ( 'NONE',  ( 136.7822455296790736, -0.9253760310430724223, -17.38909034558905020 ) ) ;
#23142=CARTESIAN_POINT ( 'NONE',  ( 120.7947214775786193, -0.8288870151387760510, -10.36305467784173118 ) ) ;
#23143=CARTESIAN_POINT ( 'NONE',  ( 113.5904348109119866, -2.084020599724406786, -8.691656652584148546 ) ) ;
#23144=CARTESIAN_POINT ( 'NONE',  ( 125.7866681442453256, -8.899110576539104756, -16.42337572283570424 ) ) ;
#23145=VERTEX_POINT ( 'NONE', #35399 ) ;
#23147=CARTESIAN_POINT ( 'NONE',  ( 118.1285681442453068, -2.084020599724406786, -8.691656652584148546 ) ) ;
#23152=CARTESIAN_POINT ( 'NONE',  ( 123.9714148109119805, -0.4660016031367893996, -10.09054647747474043 ) ) ;
#23153=CARTESIAN_POINT ( 'NONE',  ( 122.1561614775786353, -8.899110576539710493, -16.42337572283490132 ) ) ;
#23155=CARTESIAN_POINT ( 'NONE',  ( 119.2255797424434149, -0.9924539043446216624, -17.29976612834909133 ) ) ;
#23156=CARTESIAN_POINT ( 'NONE',  ( 125.9568481442452850, -6.344957434206665248, -7.627207830600338134 ) ) ;
#23158=ADVANCED_FACE ( 'NONE', ( #14449 ), #3725, .F. ) ;
#23159=CARTESIAN_POINT ( 'NONE',  ( 125.4463081442452932, -4.153390946401325223, -8.397313243818185668 ) ) ;
#23160=CARTESIAN_POINT ( 'NONE',  ( 118.2420214775786320, -6.222761293078241884, -8.102969835052219238 ) ) ;
#23164=ADVANCED_FACE ( 'NONE', ( #311 ), #41612, .F. ) ;
#23166=CARTESIAN_POINT ( 'NONE',  ( 114.2144281442453178, -1.833838273342658809, -17.42832698103878286 ) ) ;
#23171=CARTESIAN_POINT ( 'NONE',  ( 122.1561614775786353, -0.4660016031367893996, -10.09054647747474043 ) ) ;
#23172=CARTESIAN_POINT ( 'NONE',  ( 121.4754414775786131, -8.166667518702819706, -8.995218007635861213 ) ) ;
#23173=CARTESIAN_POINT ( 'NONE',  ( 119.6811727111058588, -1.267766418764730840, -16.93314635290706605 ) ) ;
#23174=EDGE_CURVE ( 'NONE', #24392, #40113, #4314, .T. ) ;
#23175=CARTESIAN_POINT ( 'NONE',  ( 116.1998614775786507, -10.63000616557722466, -14.87417383870573495 ) ) ;
#23178=CARTESIAN_POINT ( 'NONE',  ( 112.9097148109120070, -9.565557343593413364, -10.61323700422348004 ) ) ;
#23179=CARTESIAN_POINT ( 'NONE',  ( 112.7962614775786676, -6.222761293078241884, -8.102969835052219238 ) ) ;
#23180=CARTESIAN_POINT ( 'NONE',  ( 120.5110881442453206, -6.344957434206665248, -7.627207830600338134 ) ) ;
#23181=CARTESIAN_POINT ( 'NONE',  ( 124.0281414775786146, -7.643976991954077427, -18.09477374809248928 ) ) ;
#23182=CARTESIAN_POINT ( 'NONE',  ( 112.6260814775786514, -0.8288870151387760510, -10.36305467784173118 ) ) ;
#23184=CARTESIAN_POINT ( 'NONE',  ( 116.1431348109119881, 0.1319031606808879209, -14.10382304977623669 ) ) ;
#23185=CARTESIAN_POINT ( 'NONE',  ( 125.9568481442452850, -6.344957434206665248, -7.627207830600338134 ) ) ;
#23187=CARTESIAN_POINT ( 'NONE',  ( 120.4543614775786295, -5.574606645277164318, -18.38911715685844683 ) ) ;
#23192=CARTESIAN_POINT ( 'NONE',  ( 124.6521348109119884, -1.561330072975668948, -17.79121239304076951 ) ) ;
#23201=CARTESIAN_POINT ( 'NONE',  ( 136.4689272580752686, -7.050714571525749541, -18.72418924296322729 ) ) ;
#23203=CARTESIAN_POINT ( 'NONE',  ( 125.9001214775786224, -4.089484607189486809, -7.948022111789456723 ) ) ;
#23204=CARTESIAN_POINT ( 'NONE',  ( 117.4478481442453131, -9.565557343593413364, -10.61323700422348004 ) ) ;
#23207=CARTESIAN_POINT ( 'NONE',  ( 124.0848681442452772, -4.089484607189486809, -7.948022111789456723 ) ) ;
#23208=CARTESIAN_POINT ( 'NONE',  ( 115.8027748109119841, -0.4660016031367893996, -10.09054647747474043 ) ) ;
#23210=CARTESIAN_POINT ( 'NONE',  ( 112.1722681442453222, -8.899110576539710493, -16.42337572283490132 ) ) ;
#23211=CARTESIAN_POINT ( 'NONE',  ( 122.4397948109119767, -0.1624402480850797581, -16.17319339645315424 ) ) ;
#23212=CARTESIAN_POINT ( 'NONE',  ( 125.7866681442452688, -0.4660016031367893996, -10.09054647747474043 ) ) ;
#23216=CARTESIAN_POINT ( 'NONE',  ( 117.6180281442453150, -8.899110576539710493, -16.42337572283490132 ) ) ;
#23217=CARTESIAN_POINT ( 'NONE',  ( 117.6180281442453150, -8.899110576539710493, -16.42337572283490132 ) ) ;
#23218=ADVANCED_FACE ( 'NONE', ( #21284 ), #31766, .T. ) ;
#23222=CARTESIAN_POINT ( 'NONE',  ( 122.9503348109119827, -9.859900752359369136, -12.68260735090035318 ) ) ;
#23223=CARTESIAN_POINT ( 'NONE',  ( 126.5241148109119393, -9.565557343593413364, -10.61323700422348004 ) ) ;
#23229=CARTESIAN_POINT ( 'NONE',  ( 117.3343948109119737, -3.383040157471821630, -19.15922257007629170 ) ) ;
#23230=CARTESIAN_POINT ( 'NONE',  ( 123.2906948109119867, -1.833838273342659697, -17.42832698103878286 ) ) ;
#23231=CARTESIAN_POINT ( 'NONE',  ( 114.7816948109119863, -9.859900752359374465, -12.68260735090039404 ) ) ;
#23234=CARTESIAN_POINT ( 'NONE',  ( 114.2711548109119803, -9.988377603198976828, -10.36322818467138340 ) ) ;
#23237=CARTESIAN_POINT ( 'NONE',  ( 124.6521348109119884, -1.561330072975668948, -17.79121239304076951 ) ) ;
#23240=( BOUNDED_SURFACE ( )  B_SPLINE_SURFACE ( 1, 2, ( 
 ( #10944, #25076, #668, #35538, #21648, #32126, #1119, #15037, #42856, #25526, #39431, #8195, #22103, #35991, #19808, #19130, #22326, #2237, #16169, #36890, #29391, #18900, #36222, #43303, #4987, #5437, #5886, #9097, #12525, #12748, #12072, #25974, #8645, #22998, #37113, #40105, #26198, #33013, #33458, #30072, #39880, #5659, #40332, #26425, #40791, #43984, #23231, #29615, #12979, #12299, #22545, #36443, #2467, #16391, #26649, #40564, #32791, #43759, #19356, #1563, #19578, #9324, #33696, #8866, #30291, #44218, #26875, #15486, #5211, #1787, #15712, #36664, #43530, #22767, #33243, #2016, #15941, #29841, #27106, #41028, #37582, #27335, #3376, #24356, #38243, #23463, #44892, #7022, #23696, #20933, #23920, #44669, #34807, #37801, #44439, #30969, #38030, #37349, #31188, #3156, #20040, #9781, #17504, #2923, #9548, #6122, #24137, #17296, #10452, #3593, #17076, #31402, #45106, #34375, #6806, #6355, #20267, #10011, #34154, #41690, #20494, #13865, #6577, #27778, #171, #14087, #2693, #13652, #27558, #33922, #20714, #16623, #28004, #41471, #30517, #10230, #34593, #13205, #16854, #30745, #13431, #41253, #7913, #38687, #840, #18411, #24794, #25476, #11568, #396, #11120, #7684, #21598, #4032, #17953, #14759, #8147, #28228, #35485, #10895, #22050, #25250, #39381, #4712, #35023, #14310, #4259, #3806, #42134, #35943, #7452, #21372, #32072, #39148, #35255, #38913, #42578, #18177, #28675, #18633, #31853, #32520, #14983, #21822, #15207, #28447, #35715, #17731, #1295, #622, #41911, #14533, #42358, #11340, #31628, #10674, #25020, #24577, #4489, #32303, #38462, #1070, #7234, #28895, #42807, #21150, #32961, #25699, #8594, #23181, #39606, #19528, #26597, #40510, #39826, #2181, #40047, #1738, #11792, #29112, #9271, #33636, #8367, #22492, #40280, #2411, #1961, #36387, #37059, #43254, #5832, #43480, #19075, #19752, #12247, #18848, #5390, #12471, #22272, #5605, #22716, #15889, #36615, #43023, #36166, #25922, #5158, #4933, #8814, #19308, #26371, #9045, #15662, #43698, #29564, #26144, #33187 ),
 ( #29785, #43930, #22944, #32740, #36837, #33405, #1514, #16111, #15433, #30012, #29341, #12019, #12697, #13817, #27728, #27052, #34540, #27281, #34101, #44163, #16338, #41645, #20882, #40735, #40970, #27505, #34757, #34325, #23637, #26824, #2638, #24310, #9725, #30241, #12927, #30917, #10179, #17242, #10400, #23869, #38196, #37980, #41196, #44840, #30465, #44385, #16799, #37523, #3321, #9956, #6754, #44613, #24086, #45057, #31133, #9492, #37755, #6525, #23407, #13596, #37290, #6060, #30695, #19980, #20442, #3098, #17026, #6973, #6296, #33869, #20665, #41424, #13149, #16570, #20216, #2869, #13380, #18356, #7182, #17903, #14481, #28391, #10843, #24738, #21545, #14933, #34970, #42301, #17679, #28844, #32021, #1017, #38412, #24967, #786, #31351, #25198, #11065, #35434, #38863, #25424, #8093, #345, #38628, #10623, #7631, #4209, #14707, #28620, #21321, #18126, #14258, #3980, #42530, #21092, #41861, #39325, #27954, #39096, #125, #3758, #11290, #7866, #21773, #35665, #31800, #24525, #7403, #31577, #571, #28175, #35207, #42083, #3540, #42756, #11519, #4438, #21995, #32246, #17455, #14037, #32689, #35885, #15831, #29728, #5334, #42970, #32468, #4655, #11738, #18576, #19019, #19471, #22664, #26088, #26317, #25649, #39553, #22215, #36560, #5553, #8539, #39768, #1459, #1902, #43642, #8315, #19252, #8758, #39992, #9217, #12416, #36782, #43199, #26544, #25864, #36112, #4883, #16055, #29961, #40225, #8989, #1244, #12188, #32906, #15155, #33132, #22889, #33353, #22440, #2126, #43877, #12648, #40455, #29061, #18800, #15381, #5103, #29285, #11965, #36333, #1681, #15603, #29507, #43423, #44108, #26774, #6006, #20165, #30639, #44556, #23126, #26994, #27226, #12875, #41144, #2585, #19928, #9903, #16516, #23816, #37704, #2357, #40683, #13095, #16288, #30190, #37003, #9435, #23348, #40914, #34048, #37232, #30415, #37470, #9668, #44335, #5774, #33815, #19694, #33582, #23586, #6242, #2816, #16745, #13322, #20013, #23897, #13625, #27083, #16601, #151, #2668, #13842, #33898, #13180, #41449 ) ),
 .UNSPECIFIED., .F., .F., .T. ) 
 B_SPLINE_SURFACE_WITH_KNOTS ( ( 2, 2 ),
 ( 3, 2, 2, 2, 2, 2, 2, 2, 2, 2, 2, 2, 2, 2, 2, 2, 2, 2, 2, 2, 2, 2, 2, 2, 2, 2, 2, 2, 2, 2, 2, 2, 2, 2, 2, 2, 2, 2, 2, 2, 2, 2, 2, 2, 2, 2, 2, 2, 2, 2, 2, 2, 2, 2, 2, 2, 2, 2, 2, 2, 2, 2, 2, 2, 2, 2, 2, 2, 2, 2, 2, 2, 2, 2, 2, 2, 2, 2, 2, 2, 2, 2, 2, 2, 2, 2, 2, 2, 2, 2, 2, 2, 2, 2, 2, 2, 2, 2, 2, 2, 2, 2, 2, 2, 2, 2, 2, 2, 2, 2, 2, 2, 2, 2, 2, 2, 2, 2, 2, 2, 2, 2, 2, 2, 2, 2, 2, 2, 3 ),
 ( 0.000000000000000000, 1.000000000000000000 ),
 ( 0.000000000000000000, 0.007812500000000000000, 0.01562500000000000000, 0.02343750000000000000, 0.03125000000000000000, 0.03906250000000000000, 0.04687500000000000000, 0.05468750000000000000, 0.06250000000000000000, 0.07031250000000000000, 0.07812500000000000000, 0.08593750000000000000, 0.09375000000000000000, 0.1015625000000000000, 0.1093750000000000000, 0.1171875000000000000, 0.1250000000000000000, 0.1328125000000000000, 0.1406250000000000000, 0.1484375000000000000, 0.1562500000000000000, 0.1640625000000000000, 0.1718750000000000000, 0.1796875000000000000, 0.1875000000000000000, 0.1953125000000000000, 0.2031250000000000000, 0.2109375000000000000, 0.2187500000000000000, 0.2265625000000000000, 0.2343750000000000000, 0.2421875000000000000, 0.2500000000000000000, 0.2578125000000000000, 0.2656250000000000000, 0.2734375000000000000, 0.2812500000000000000, 0.2890625000000000000, 0.2968750000000000000, 0.3046875000000000000, 0.3125000000000000000, 0.3203125000000000000, 0.3281250000000000000, 0.3359375000000000000, 0.3437500000000000000, 0.3515625000000000000, 0.3593750000000000000, 0.3671875000000000000, 0.3750000000000000000, 0.3828125000000000000, 0.3906250000000000000, 0.3984375000000000000, 0.4062500000000000000, 0.4140625000000000000, 0.4218750000000000000, 0.4296875000000000000, 0.4375000000000000000, 0.4453125000000000000, 0.4531250000000000000, 0.4609375000000000000, 0.4687500000000000000, 0.4765625000000000000, 0.4843750000000000000, 0.4921875000000000000, 0.5000000000000000000, 0.5078125000000000000, 0.5156250000000000000, 0.5234375000000000000, 0.5312500000000000000, 0.5390625000000000000, 0.5468750000000000000, 0.5546875000000000000, 0.5625000000000000000, 0.5703125000000000000, 0.5781250000000000000, 0.5859375000000000000, 0.5937500000000000000, 0.6015625000000000000, 0.6093750000000000000, 0.6171875000000000000, 0.6250000000000000000, 0.6328125000000000000, 0.6406250000000000000, 0.6484375000000000000, 0.6562500000000000000, 0.6640625000000000000, 0.6718750000000000000, 0.6796875000000000000, 0.6875000000000000000, 0.6953125000000000000, 0.7031250000000000000, 0.7109375000000000000, 0.7187500000000000000, 0.7265625000000000000, 0.7343750000000000000, 0.7421875000000000000, 0.7500000000000000000, 0.7578125000000000000, 0.7656250000000000000, 0.7734375000000000000, 0.7812500000000000000, 0.7890625000000000000, 0.7968750000000000000, 0.8046875000000000000, 0.8125000000000000000, 0.8203125000000000000, 0.8281250000000000000, 0.8359375000000000000, 0.8437500000000000000, 0.8515625000000000000, 0.8593750000000000000, 0.8671875000000000000, 0.8750000000000000000, 0.8828125000000000000, 0.8906250000000000000, 0.8984375000000000000, 0.9062500000000000000, 0.9140625000000000000, 0.9218750000000000000, 0.9296875000000000000, 0.9375000000000000000, 0.9453125000000000000, 0.9531250000000000000, 0.9609375000000000000, 0.9687500000000000000, 0.9765625000000000000, 0.9843750000000000000, 0.9921875000000000000, 1.000000000000000000 ),
 .UNSPECIFIED. ) 
 GEOMETRIC_REPRESENTATION_ITEM ( )  RATIONAL_B_SPLINE_SURFACE ( (
 ( 1.000000000000000000, 0.9238795325112869605, 1.000000000000000000, 0.9238795325112869605, 1.000000000000000000, 0.9238795325112869605, 1.000000000000000000, 0.9238795325112869605, 1.000000000000000000, 0.9238795325112869605, 1.000000000000000000, 0.9238795325112869605, 1.000000000000000000, 0.9238795325112869605, 1.000000000000000000, 0.9238795325112869605, 1.000000000000000000, 0.9238795325112869605, 1.000000000000000000, 0.9238795325112869605, 1.000000000000000000, 0.9238795325112869605, 1.000000000000000000, 0.9238795325112869605, 1.000000000000000000, 0.9238795325112869605, 1.000000000000000000, 0.9238795325112869605, 1.000000000000000000, 0.9238795325112869605, 1.000000000000000000, 0.9238795325112869605, 1.000000000000000000, 0.9238795325112869605, 1.000000000000000000, 0.9238795325112869605, 1.000000000000000000, 0.9238795325112869605, 1.000000000000000000, 0.9238795325112869605, 1.000000000000000000, 0.9238795325112869605, 1.000000000000000000, 0.9238795325112869605, 1.000000000000000000, 0.9238795325112869605, 1.000000000000000000, 0.9238795325112869605, 1.000000000000000000, 0.9238795325112869605, 1.000000000000000000, 0.9238795325112869605, 1.000000000000000000, 0.9238795325112869605, 1.000000000000000000, 0.9238795325112869605, 1.000000000000000000, 0.9238795325112869605, 1.000000000000000000, 0.9238795325112869605, 1.000000000000000000, 0.9238795325112869605, 1.000000000000000000, 0.9238795325112869605, 1.000000000000000000, 0.9238795325112869605, 1.000000000000000000, 0.9238795325112869605, 1.000000000000000000, 0.9238795325112869605, 1.000000000000000000, 0.9238795325112869605, 1.000000000000000000, 0.9238795325112869605, 1.000000000000000000, 0.9238795325112869605, 1.000000000000000000, 0.9238795325112869605, 1.000000000000000000, 0.9238795325112869605, 1.000000000000000000, 0.9238795325112869605, 1.000000000000000000, 0.9238795325112869605, 1.000000000000000000, 0.9238795325112869605, 1.000000000000000000, 0.9238795325112869605, 1.000000000000000000, 0.9238795325112869605, 1.000000000000000000, 0.9238795325112869605, 1.000000000000000000, 0.9238795325112869605, 1.000000000000000000, 0.9238795325112869605, 1.000000000000000000, 0.9238795325112869605, 1.000000000000000000, 0.9238795325112869605, 1.000000000000000000, 0.9238795325112869605, 1.000000000000000000, 0.9238795325112869605, 1.000000000000000000, 0.9238795325112869605, 1.000000000000000000, 0.9238795325112869605, 1.000000000000000000, 0.9238795325112869605, 1.000000000000000000, 0.9238795325112869605, 1.000000000000000000, 0.9238795325112869605, 1.000000000000000000, 0.9238795325112869605, 1.000000000000000000, 0.9238795325112869605, 1.000000000000000000, 0.9238795325112869605, 1.000000000000000000, 0.9238795325112869605, 1.000000000000000000, 0.9238795325112869605, 1.000000000000000000, 0.9238795325112869605, 1.000000000000000000, 0.9238795325112869605, 1.000000000000000000, 0.9238795325112869605, 1.000000000000000000, 0.9238795325112869605, 1.000000000000000000, 0.9238795325112869605, 1.000000000000000000, 0.9238795325112869605, 1.000000000000000000, 0.9238795325112869605, 1.000000000000000000, 0.9238795325112869605, 1.000000000000000000, 0.9238795325112869605, 1.000000000000000000, 0.9238795325112869605, 1.000000000000000000, 0.9238795325112869605, 1.000000000000000000, 0.9238795325112869605, 1.000000000000000000, 0.9238795325112869605, 1.000000000000000000, 0.9238795325112869605, 1.000000000000000000, 0.9238795325112869605, 1.000000000000000000, 0.9238795325112869605, 1.000000000000000000, 0.9238795325112869605, 1.000000000000000000, 0.9238795325112869605, 1.000000000000000000, 0.9238795325112869605, 1.000000000000000000, 0.9238795325112869605, 1.000000000000000000, 0.9238795325112869605, 1.000000000000000000, 0.9238795325112869605, 1.000000000000000000, 0.9238795325112869605, 1.000000000000000000, 0.9238795325112869605, 1.000000000000000000, 0.9238795325112869605, 1.000000000000000000, 0.9238795325112869605, 1.000000000000000000, 0.9238795325112869605, 1.000000000000000000, 0.9238795325112869605, 1.000000000000000000, 0.9238795325112869605, 1.000000000000000000, 0.9238795325112869605, 1.000000000000000000, 0.9238795325112869605, 1.000000000000000000, 0.9238795325112869605, 1.000000000000000000, 0.9238795325112869605, 1.000000000000000000, 0.9238795325112869605, 1.000000000000000000, 0.9238795325112869605, 1.000000000000000000, 0.9238795325112869605, 1.000000000000000000, 0.9238795325112869605, 1.000000000000000000, 0.9238795325112869605, 1.000000000000000000, 0.9238795325112869605, 1.000000000000000000, 0.9238795325112869605, 1.000000000000000000, 0.9238795325112869605, 1.000000000000000000, 0.9238795325112869605, 1.000000000000000000, 0.9238795325112869605, 1.000000000000000000, 0.9238795325112869605, 1.000000000000000000, 0.9238795325112869605, 1.000000000000000000, 0.9238795325112869605, 1.000000000000000000, 0.9238795325112869605, 1.000000000000000000, 0.9238795325112869605, 1.000000000000000000, 0.9238795325112869605, 1.000000000000000000, 0.9238795325112869605, 1.000000000000000000, 0.9238795325112869605, 1.000000000000000000, 0.9238795325112869605, 1.000000000000000000, 0.9238795325112869605, 1.000000000000000000, 0.9238795325112869605, 1.000000000000000000, 0.9238795325112869605, 1.000000000000000000, 0.9238795325112869605, 1.000000000000000000, 0.9238795325112869605, 1.000000000000000000, 0.9238795325112869605, 1.000000000000000000, 0.9238795325112869605, 1.000000000000000000, 0.9238795325112869605, 1.000000000000000000, 0.9238795325112869605, 1.000000000000000000, 0.9238795325112869605, 1.000000000000000000, 0.9238795325112869605, 1.000000000000000000, 0.9238795325112869605, 1.000000000000000000, 0.9238795325112869605, 1.000000000000000000, 0.9238795325112869605, 1.000000000000000000),
 ( 1.000000000000000000, 0.9238795325112869605, 1.000000000000000000, 0.9238795325112869605, 1.000000000000000000, 0.9238795325112869605, 1.000000000000000000, 0.9238795325112869605, 1.000000000000000000, 0.9238795325112869605, 1.000000000000000000, 0.9238795325112869605, 1.000000000000000000, 0.9238795325112869605, 1.000000000000000000, 0.9238795325112869605, 1.000000000000000000, 0.9238795325112869605, 1.000000000000000000, 0.9238795325112869605, 1.000000000000000000, 0.9238795325112869605, 1.000000000000000000, 0.9238795325112869605, 1.000000000000000000, 0.9238795325112869605, 1.000000000000000000, 0.9238795325112869605, 1.000000000000000000, 0.9238795325112869605, 1.000000000000000000, 0.9238795325112869605, 1.000000000000000000, 0.9238795325112869605, 1.000000000000000000, 0.9238795325112869605, 1.000000000000000000, 0.9238795325112869605, 1.000000000000000000, 0.9238795325112869605, 1.000000000000000000, 0.9238795325112869605, 1.000000000000000000, 0.9238795325112869605, 1.000000000000000000, 0.9238795325112869605, 1.000000000000000000, 0.9238795325112869605, 1.000000000000000000, 0.9238795325112869605, 1.000000000000000000, 0.9238795325112869605, 1.000000000000000000, 0.9238795325112869605, 1.000000000000000000, 0.9238795325112869605, 1.000000000000000000, 0.9238795325112869605, 1.000000000000000000, 0.9238795325112869605, 1.000000000000000000, 0.9238795325112869605, 1.000000000000000000, 0.9238795325112869605, 1.000000000000000000, 0.9238795325112869605, 1.000000000000000000, 0.9238795325112869605, 1.000000000000000000, 0.9238795325112869605, 1.000000000000000000, 0.9238795325112869605, 1.000000000000000000, 0.9238795325112869605, 1.000000000000000000, 0.9238795325112869605, 1.000000000000000000, 0.9238795325112869605, 1.000000000000000000, 0.9238795325112869605, 1.000000000000000000, 0.9238795325112869605, 1.000000000000000000, 0.9238795325112869605, 1.000000000000000000, 0.9238795325112869605, 1.000000000000000000, 0.9238795325112869605, 1.000000000000000000, 0.9238795325112869605, 1.000000000000000000, 0.9238795325112869605, 1.000000000000000000, 0.9238795325112869605, 1.000000000000000000, 0.9238795325112869605, 1.000000000000000000, 0.9238795325112869605, 1.000000000000000000, 0.9238795325112869605, 1.000000000000000000, 0.9238795325112869605, 1.000000000000000000, 0.9238795325112869605, 1.000000000000000000, 0.9238795325112869605, 1.000000000000000000, 0.9238795325112869605, 1.000000000000000000, 0.9238795325112869605, 1.000000000000000000, 0.9238795325112869605, 1.000000000000000000, 0.9238795325112869605, 1.000000000000000000, 0.9238795325112869605, 1.000000000000000000, 0.9238795325112869605, 1.000000000000000000, 0.9238795325112869605, 1.000000000000000000, 0.9238795325112869605, 1.000000000000000000, 0.9238795325112869605, 1.000000000000000000, 0.9238795325112869605, 1.000000000000000000, 0.9238795325112869605, 1.000000000000000000, 0.9238795325112869605, 1.000000000000000000, 0.9238795325112869605, 1.000000000000000000, 0.9238795325112869605, 1.000000000000000000, 0.9238795325112869605, 1.000000000000000000, 0.9238795325112869605, 1.000000000000000000, 0.9238795325112869605, 1.000000000000000000, 0.9238795325112869605, 1.000000000000000000, 0.9238795325112869605, 1.000000000000000000, 0.9238795325112869605, 1.000000000000000000, 0.9238795325112869605, 1.000000000000000000, 0.9238795325112869605, 1.000000000000000000, 0.9238795325112869605, 1.000000000000000000, 0.9238795325112869605, 1.000000000000000000, 0.9238795325112869605, 1.000000000000000000, 0.9238795325112869605, 1.000000000000000000, 0.9238795325112869605, 1.000000000000000000, 0.9238795325112869605, 1.000000000000000000, 0.9238795325112869605, 1.000000000000000000, 0.9238795325112869605, 1.000000000000000000, 0.9238795325112869605, 1.000000000000000000, 0.9238795325112869605, 1.000000000000000000, 0.9238795325112869605, 1.000000000000000000, 0.9238795325112869605, 1.000000000000000000, 0.9238795325112869605, 1.000000000000000000, 0.9238795325112869605, 1.000000000000000000, 0.9238795325112869605, 1.000000000000000000, 0.9238795325112869605, 1.000000000000000000, 0.9238795325112869605, 1.000000000000000000, 0.9238795325112869605, 1.000000000000000000, 0.9238795325112869605, 1.000000000000000000, 0.9238795325112869605, 1.000000000000000000, 0.9238795325112869605, 1.000000000000000000, 0.9238795325112869605, 1.000000000000000000, 0.9238795325112869605, 1.000000000000000000, 0.9238795325112869605, 1.000000000000000000, 0.9238795325112869605, 1.000000000000000000, 0.9238795325112869605, 1.000000000000000000, 0.9238795325112869605, 1.000000000000000000, 0.9238795325112869605, 1.000000000000000000, 0.9238795325112869605, 1.000000000000000000, 0.9238795325112869605, 1.000000000000000000, 0.9238795325112869605, 1.000000000000000000, 0.9238795325112869605, 1.000000000000000000, 0.9238795325112869605, 1.000000000000000000, 0.9238795325112869605, 1.000000000000000000, 0.9238795325112869605, 1.000000000000000000, 0.9238795325112869605, 1.000000000000000000, 0.9238795325112869605, 1.000000000000000000, 0.9238795325112869605, 1.000000000000000000, 0.9238795325112869605, 1.000000000000000000, 0.9238795325112869605, 1.000000000000000000, 0.9238795325112869605, 1.000000000000000000, 0.9238795325112869605, 1.000000000000000000, 0.9238795325112869605, 1.000000000000000000, 0.9238795325112869605, 1.000000000000000000, 0.9238795325112869605, 1.000000000000000000, 0.9238795325112869605, 1.000000000000000000, 0.9238795325112869605, 1.000000000000000000, 0.9238795325112869605, 1.000000000000000000, 0.9238795325112869605, 1.000000000000000000, 0.9238795325112869605, 1.000000000000000000, 0.9238795325112869605, 1.000000000000000000, 0.9238795325112869605, 1.000000000000000000, 0.9238795325112869605, 1.000000000000000000) ) ) 
 REPRESENTATION_ITEM ( '' )  SURFACE ( )  );
#23241=CARTESIAN_POINT ( 'NONE',  ( 112.5126281442453120, -10.30919188438810075, -12.61870101168855918 ) ) ;
#23242=CARTESIAN_POINT ( 'NONE',  ( 113.5337081442453240, -0.8288870151387760510, -10.36305467784173118 ) ) ;
#23244=CARTESIAN_POINT ( 'NONE',  ( 113.4769814775786330, -10.63000616557722466, -14.87417383870573495 ) ) ;
#23246=CARTESIAN_POINT ( 'NONE',  ( 123.4041481442452834, -10.30919188438810075, -12.61870101168855918 ) ) ;
#23250=CARTESIAN_POINT ( 'NONE',  ( 117.7314814775786260, -5.574606645277164318, -18.38911715685844683 ) ) ;
#23251=CARTESIAN_POINT ( 'NONE',  ( 123.6018618195759160, -4.372193249654628744, -15.29709325109553930 ) ) ;
#23252=CARTESIAN_POINT ( 'NONE',  ( 114.6682414775786469, -7.894159318335828068, -9.358103419637847864 ) ) ;
#23255=CARTESIAN_POINT ( 'NONE',  ( 116.1998614775786507, 0.4262465694468514643, -12.03445270309931736 ) ) ;
#23256=CARTESIAN_POINT ( 'NONE',  ( 116.9940348109119839, -9.988377603198976828, -10.36322818467138340 ) ) ;
#23259=CARTESIAN_POINT ( 'NONE',  ( 112.5693548109119888, -10.63000616557722466, -14.87417383870573495 ) ) ;
#23260=CARTESIAN_POINT ( 'NONE',  ( 114.9518748109119883, -7.643976991954077427, -18.09477374809248928 ) ) ;
#23261=CARTESIAN_POINT ( 'NONE',  ( 121.8725281442453223, -3.383040157471821630, -19.15922257007629170 ) ) ;
#23262=CARTESIAN_POINT ( 'NONE',  ( 123.4608748109119745, -10.63000616557722466, -14.87417383870573495 ) ) ;
#23263=ORIENTED_EDGE ( 'NONE', *, *, #42780, .F. ) ;
#23264=CARTESIAN_POINT ( 'NONE',  ( 114.6115148109119986, -3.383040157471821630, -19.15922257007629170 ) ) ;
#23269=CARTESIAN_POINT ( 'NONE',  ( 119.0361948109119652, -7.893985811506177619, -18.51759400769804742 ) ) ;
#23271=CARTESIAN_POINT ( 'NONE',  ( 125.9001214775786224, -4.089484607189486809, -7.948022111789456723 ) ) ;
#23272=CARTESIAN_POINT ( 'NONE',  ( 124.8223148109119762, 0.9020085738987273505, -11.91225656197088512 ) ) ;
#23273=CARTESIAN_POINT ( 'NONE',  ( 113.1933481442453058, -5.574606645277164318, -18.38911715685844683 ) ) ;
#23275=CARTESIAN_POINT ( 'NONE',  ( 118.4689281442453392, 0.9020085738987339008, -11.91225656197089222 ) ) ;
#23280=CARTESIAN_POINT ( 'NONE',  ( 123.2906948109119867, -1.833838273342659697, -17.42832698103878286 ) ) ;
#23281=CARTESIAN_POINT ( 'NONE',  ( 121.5888948109119809, -10.30919188438810075, -12.61870101168855918 ) ) ;
#23282=CARTESIAN_POINT ( 'NONE',  ( 114.4980614775786734, -2.084020599724406786, -8.691656652584148546 ) ) ;
#23283=CARTESIAN_POINT ( 'NONE',  ( 115.6893214775786447, 0.5811942927096154232, -14.16772938898807155 ) ) ;
#23285=CARTESIAN_POINT ( 'NONE',  ( 125.5597614775786326, -7.894159318335828068, -9.358103419637847864 ) ) ;
#23286=CARTESIAN_POINT ( 'NONE',  ( 119.7169148109119874, -0.1624402480850797581, -16.17319339645315424 ) ) ;
#23288=CARTESIAN_POINT ( 'NONE',  ( 119.8303681442452984, -10.63000616557722466, -14.87417383870573495 ) ) ;
#23290=CARTESIAN_POINT ( 'NONE',  ( 114.8951481442453115, -0.4660016031367893996, -10.09054647747474043 ) ) ;
#23291=CARTESIAN_POINT ( 'NONE',  ( 120.2841814775786276, -10.15424416112533912, -14.75197769757731336 ) ) ;
#23294=CARTESIAN_POINT ( 'NONE',  ( 118.1852948109119836, -5.638512984488999180, -18.83840828888717311 ) ) ;
#23296=CARTESIAN_POINT ( 'NONE',  ( 117.5045748109119756, -9.859900752359374465, -12.68260735090039404 ) ) ;
#23300=CARTESIAN_POINT ( 'NONE',  ( 125.6164881442453094, -9.565557343593413364, -10.61323700422348004 ) ) ;
#23301=CARTESIAN_POINT ( 'NONE',  ( 122.2696148109119889, -5.574606645277164318, -18.38911715685844683 ) ) ;
#23305=CARTESIAN_POINT ( 'NONE',  ( 119.2063748109119814, -1.561330072975668504, -17.79121239304076951 ) ) ;
#23307=CARTESIAN_POINT ( 'NONE',  ( 121.2485348109119769, -0.4660016031367893996, -10.09054647747474043 ) ) ;
#23308=CARTESIAN_POINT ( 'NONE',  ( 113.8740681442453138, 0.5811942927096154232, -14.16772938898807155 ) ) ;
#23309=CARTESIAN_POINT ( 'NONE',  ( 120.4543614775786295, -5.574606645277164318, -18.38911715685844683 ) ) ;
#23310=CARTESIAN_POINT ( 'NONE',  ( 123.4608748109119745, 0.4262465694468514643, -12.03445270309931736 ) ) ;
#23311=CARTESIAN_POINT ( 'NONE',  ( 114.2144281442453178, -8.166667518702817929, -8.995218007635859436 ) ) ;
#23313=CARTESIAN_POINT ( 'NONE',  ( 124.0848681442452772, -5.574606645277164318, -18.38911715685844683 ) ) ;
#23314=CARTESIAN_POINT ( 'NONE',  ( 122.0217798611595867, -1.036737761566197014, -17.24079555149560861 ) ) ;
#23320=CARTESIAN_POINT ( 'NONE',  ( 121.4754414775786131, -8.166667518702819706, -8.995218007635861213 ) ) ;
#23321=CARTESIAN_POINT ( 'NONE',  ( 123.1772414775786189, -5.574606645277164318, -18.38911715685844683 ) ) ;
#23323=CARTESIAN_POINT ( 'NONE',  ( 120.6812681442452941, -10.30919188438810075, -12.61870101168855918 ) ) ;
#23324=CARTESIAN_POINT ( 'NONE',  ( 113.3635281442453504, -0.1624402480850797581, -16.17319339645315424 ) ) ;
#23326=CARTESIAN_POINT ( 'NONE',  ( 120.5110881442453206, -6.344957434206665248, -7.627207830600338134 ) ) ;
#23327=CARTESIAN_POINT ( 'NONE',  ( 121.2485348109119769, -0.4660016031367893996, -10.09054647747474043 ) ) ;
#23329=CARTESIAN_POINT ( 'NONE',  ( 122.7234281442452755, -4.153390946401325223, -8.397313243818185668 ) ) ;
#23332=EDGE_CURVE ( 'NONE', #37016, #19714, #9965, .T. ) ;
#23336=CARTESIAN_POINT ( 'NONE',  ( 122.3830681442452857, -1.833838273342659697, -17.42832698103878286 ) ) ;
#23339=AXIS2_PLACEMENT_3D ( 'NONE', #18487, #11425, #1369 ) ;
#23340=CARTESIAN_POINT ( 'NONE',  ( 117.8449348109119938, -1.833838273342659253, -17.42832698103878286 ) ) ;
#23342=CARTESIAN_POINT ( 'NONE',  ( 115.6325948109119821, -9.565557343593413364, -10.61323700422348004 ) ) ;
#23343=CARTESIAN_POINT ( 'NONE',  ( 122.2128881442453263, -1.834011780172310813, -8.268836392978581529 ) ) ;
#23344=ORIENTED_EDGE ( 'NONE', *, *, #41477, .T. ) ;
#23346=CARTESIAN_POINT ( 'NONE',  ( 121.8158014775786171, -4.153390946401325223, -8.397313243818185668 ) ) ;
#23347=CARTESIAN_POINT ( 'NONE',  ( 118.6958348109119754, -6.344957434206665248, -7.627207830600338134 ) ) ;
#23348=CARTESIAN_POINT ( 'NONE',  ( 124.7088614775786226, 0.2603800115204892296, -16.42320221600525088 ) ) ;
#23349=CARTESIAN_POINT ( 'NONE',  ( 123.2339681442453241, -3.505236298600246325, -18.68346056562440793 ) ) ;
#23352=CARTESIAN_POINT ( 'NONE',  ( 125.2761281442453054, -10.63000616557722466, -14.87417383870573495 ) ) ;
#23354=CARTESIAN_POINT ( 'NONE',  ( 115.8027748109119841, -8.899110576539710493, -16.42337572283490132 ) ) ;
#23355=CARTESIAN_POINT ( 'NONE',  ( 126.1270281442452870, -10.30919188438810075, -12.61870101168855918 ) ) ;
#23356=ADVANCED_FACE ( 'NONE', ( #985 ), #7833, .T. ) ;
#23367=CARTESIAN_POINT ( 'NONE',  ( 121.1350814775786233, -9.859900752359378018, -12.68260735090039759 ) ) ;
#23368=CARTESIAN_POINT ( 'NONE',  ( 113.1933481442453058, -5.574606645277164318, -18.38911715685844683 ) ) ;
#23369=CARTESIAN_POINT ( 'NONE',  ( 126.6390922358299207, -0.2797733988919791637, -10.91602890339326137 ) ) ;
#23370=ORIENTED_EDGE ( 'NONE', *, *, #18308, .F. ) ;
#23372=CARTESIAN_POINT ( 'NONE',  ( 120.8514481442452961, -2.084020599724406786, -8.691656652584148546 ) ) ;
#23374=CARTESIAN_POINT ( 'NONE',  ( 112.3991748109119868, -1.833838273342658809, -17.42832698103878286 ) ) ;
#23376=CARTESIAN_POINT ( 'NONE',  ( 112.1722681442453222, -8.899110576539710493, -16.42337572283490132 ) ) ;
#23378=CARTESIAN_POINT ( 'NONE',  ( 122.6667014775786413, -7.893985811506177619, -18.51759400769804742 ) ) ;
#23379=CARTESIAN_POINT ( 'NONE',  ( 126.5808414775786446, -9.859900752359378018, -12.68260735090039759 ) ) ;
#23384=CARTESIAN_POINT ( 'NONE',  ( 124.6521348109119884, -7.894159318335828068, -9.358103419637847864 ) ) ;
#23385=CARTESIAN_POINT ( 'NONE',  ( 118.9227414775786542, 0.4262465694468514643, -12.03445270309931736 ) ) ;
#23389=CARTESIAN_POINT ( 'NONE',  ( 116.6536748109119941, 0.9020085738987385637, -11.91225656197091887 ) ) ;
#23391=CARTESIAN_POINT ( 'NONE',  ( 112.9664414775786412, -9.859900752359374465, -12.68260735090037983 ) ) ;
#23393=CARTESIAN_POINT ( 'NONE',  ( 117.4103264091100840, -0.9924539043446216624, -17.29976612834909133 ) ) ;
#23395=CARTESIAN_POINT ( 'NONE',  ( 123.5743281442453139, -7.893985811506177619, -18.51759400769804742 ) ) ;
#23396=CARTESIAN_POINT ( 'NONE',  ( 122.4397948109119767, -9.988377603198976828, -10.36322818467138340 ) ) ;
#23398=CARTESIAN_POINT ( 'NONE',  ( 118.4689281442453392, 0.9020085738987339008, -11.91225656197089222 ) ) ;
#23399=B_SPLINE_CURVE_WITH_KNOTS ( 'NONE', 3,
 ( #330, #42069, #10827, #44822, #17228, #20425, #31561, #34743, #27266, #27714 ),
 .UNSPECIFIED., .F., .F.,
 ( 4, 3, 3, 4 ),
 ( 1.939479807224430197E-18, 0.0001671877548681309858, 0.0003343755096277730159, 0.0006463528481650640013 ),
 .UNSPECIFIED. ) ;
#23400=CARTESIAN_POINT ( 'NONE',  ( 113.7606148109119886, -1.561330072975668060, -17.79121239304076596 ) ) ;
#23402=CARTESIAN_POINT ( 'NONE',  ( 113.9875214775786532, -8.899110576539710493, -16.42337572283490132 ) ) ;
#23404=CARTESIAN_POINT ( 'NONE',  ( 112.0588148109119828, -9.859900752359374465, -12.68260735090039404 ) ) ;
#23406=CARTESIAN_POINT ( 'NONE',  ( 121.8725281442453223, -3.383040157471821630, -19.15922257007629170 ) ) ;
#23407=CARTESIAN_POINT ( 'NONE',  ( 115.0086014775786509, -4.089484607189486809, -7.948022111789456723 ) ) ;
#23408=CARTESIAN_POINT ( 'NONE',  ( 113.7038881442453402, -6.222761293078241884, -8.102969835052219238 ) ) ;
#23411=CARTESIAN_POINT ( 'NONE',  ( 119.4900081442453086, -7.643976991954077427, -18.09477374809248928 ) ) ;
#23412=CARTESIAN_POINT ( 'NONE',  ( 114.3278814775786429, 0.1319031606808879209, -14.10382304977623669 ) ) ;
#23415=CARTESIAN_POINT ( 'NONE',  ( 122.2696148109119889, -5.574606645277164318, -18.38911715685844683 ) ) ;
#23421=CARTESIAN_POINT ( 'NONE',  ( 122.5532481442453019, -10.63000616557722466, -14.87417383870573495 ) ) ;
#23429=CARTESIAN_POINT ( 'NONE',  ( 123.3840568734310779, -1.223627541775709426, -16.99192386690442547 ) ) ;
#23430=CARTESIAN_POINT ( 'NONE',  ( 137.4076159488029134, -6.138040881925985737, -18.34368890900572424 ) ) ;
#23432=CARTESIAN_POINT ( 'NONE',  ( 125.1162100278347111, -2.486277384090758602, -17.80849669464902973 ) ) ;
#23434=CARTESIAN_POINT ( 'NONE',  ( 120.2841814775786276, -10.15424416112533912, -14.75197769757731336 ) ) ;
#23437=CARTESIAN_POINT ( 'NONE',  ( 121.7590748109119687, -7.893985811506177619, -18.51759400769804742 ) ) ;
#23438=CARTESIAN_POINT ( 'NONE',  ( 120.5678148109119832, -8.166667518702819706, -8.995218007635861213 ) ) ;
#23440=CARTESIAN_POINT ( 'NONE',  ( 113.5904348109119866, -2.084020599724406786, -8.691656652584148546 ) ) ;
#23441=CARTESIAN_POINT ( 'NONE',  ( 112.7962614775786676, -3.383040157471821630, -19.15922257007629170 ) ) ;
#23442=CARTESIAN_POINT ( 'NONE',  ( 124.3685014775786328, -10.63000616557722466, -14.87417383870573495 ) ) ;
#23446=CARTESIAN_POINT ( 'NONE',  ( 115.0653281442453277, -3.505236298600246325, -18.68346056562440793 ) ) ;
#23447=CARTESIAN_POINT ( 'NONE',  ( 118.0718414775786442, -0.8288870151387760510, -10.36305467784173118 ) ) ;
#23452=CARTESIAN_POINT ( 'NONE',  ( 124.0848681442452772, -5.574606645277146555, -18.38911715685845394 ) ) ;
#23453=CARTESIAN_POINT ( 'NONE',  ( 124.8223148109119762, -10.15424416112533912, -14.75197769757731336 ) ) ;
#23454=CARTESIAN_POINT ( 'NONE',  ( 112.0588148109119828, 0.5811942927096154232, -14.16772938898807155 ) ) ;
#23458=CARTESIAN_POINT ( 'NONE',  ( 123.5659569693743265, -3.079928505020781415, -14.51995809183469710 ) ) ;
#23461=CARTESIAN_POINT ( 'NONE',  ( 120.0572748109119772, -3.383040157471821630, -19.15922257007629170 ) ) ;
#23462=CARTESIAN_POINT ( 'NONE',  ( 126.0135748109119902, -1.833838273342660141, -17.42832698103878286 ) ) ;
#23463=CARTESIAN_POINT ( 'NONE',  ( 116.9940348109119839, -0.1624402480850797581, -16.17319339645315424 ) ) ;
#23465=FACE_OUTER_BOUND ( 'NONE', #39185, .T. ) ;
#23466=CARTESIAN_POINT ( 'NONE',  ( 120.7379948109119709, -10.63000616557722466, -14.87417383870573495 ) ) ;
#23467=CARTESIAN_POINT ( 'NONE',  ( 114.2144281442453178, -8.166667518702817929, -8.995218007635859436 ) ) ;
#23471=CARTESIAN_POINT ( 'NONE',  ( 124.5954081442453116, -3.383040157471821630, -19.15922257007629170 ) ) ;
#23473=ORIENTED_EDGE ( 'NONE', *, *, #26430, .F. ) ;
#23474=CARTESIAN_POINT ( 'NONE',  ( 117.7314814775786260, -4.089484607189486809, -7.948022111789456723 ) ) ;
#23475=CARTESIAN_POINT ( 'NONE',  ( 113.8740681442453138, -9.859900752359374465, -12.68260735090039404 ) ) ;
#23476=CARTESIAN_POINT ( 'NONE',  ( 126.5010429760490496, -4.957175668312200578, -18.53366791911779288 ) ) ;
#23477=CARTESIAN_POINT ( 'NONE',  ( 111.9453614775786434, -1.561330072975668060, -17.79121239304076596 ) ) ;
#23479=CARTESIAN_POINT ( 'NONE',  ( 121.2485348109119769, -0.4660016031367893996, -10.09054647747474043 ) ) ;
#23484=CARTESIAN_POINT ( 'NONE',  ( 116.8805814775786445, -3.505236298600246325, -18.68346056562440793 ) ) ;
#23485=CARTESIAN_POINT ( 'NONE',  ( 112.7604630939976857, -2.236191541394345172, -18.14152338500401029 ) ) ;
#23487=CARTESIAN_POINT ( 'NONE',  ( 116.7671281442453335, -7.643976991954077427, -18.09477374809248928 ) ) ;
#23491=CARTESIAN_POINT ( 'NONE',  ( 117.1642148109119859, -0.8288870151387760510, -10.36305467784173118 ) ) ;
#23492=CARTESIAN_POINT ( 'NONE',  ( 116.1431348109119881, -10.30919188438810075, -12.61870101168855918 ) ) ;
#23494=CARTESIAN_POINT ( 'NONE',  ( 112.2289948109119848, -1.834011780172310813, -8.268836392978581529 ) ) ;
#23495=CARTESIAN_POINT ( 'NONE',  ( 116.3133148109120043, -2.084020599724406786, -8.691656652584148546 ) ) ;
#23496=CARTESIAN_POINT ( 'NONE',  ( 122.3263414775786373, -6.344957434206665248, -7.627207830600338134 ) ) ;
#23497=CARTESIAN_POINT ( 'NONE',  ( 115.2922348109119781, 0.4262465694468514643, -12.03445270309931736 ) ) ;
#23499=CARTESIAN_POINT ( 'NONE',  ( 113.5337081442453240, -9.261995988541697145, -16.69588392320189030 ) ) ;
#23505=CARTESIAN_POINT ( 'NONE',  ( 118.0718414775786300, -9.261995988541697145, -16.69588392320189030 ) ) ;
#23506=ORIENTED_EDGE ( 'NONE', *, *, #3698, .F. ) ;
#23508=CARTESIAN_POINT ( 'NONE',  ( 124.9357681442453014, -1.834011780172303929, -8.268836392978592187 ) ) ;
#23509=CARTESIAN_POINT ( 'NONE',  ( 115.8595014775786609, -7.643976991954077427, -18.09477374809248928 ) ) ;
#23511=CARTESIAN_POINT ( 'NONE',  ( 124.5386814775786206, -5.638512984488999180, -18.83840828888717311 ) ) ;
#23515=CARTESIAN_POINT ( 'NONE',  ( 111.7184548109119788, -9.261995988541697145, -16.69588392320189030 ) ) ;
#23516=CARTESIAN_POINT ( 'NONE',  ( 121.5321681442453183, -0.1624402480850797581, -16.17319339645315424 ) ) ;
#23517=CARTESIAN_POINT ( 'NONE',  ( 118.6958348109119754, -6.344957434206665248, -7.627207830600338134 ) ) ;
#23518=CARTESIAN_POINT ( 'NONE',  ( 112.6260814775786514, -0.8288870151387760510, -10.36305467784173118 ) ) ;
#23519=CARTESIAN_POINT ( 'NONE',  ( 116.0296814775786345, -8.166667518702817929, -8.995218007635861213 ) ) ;
#23520=CARTESIAN_POINT ( 'NONE',  ( 151.2860562277021472, -4.863998795839242995, -13.39321520033831447 ) ) ;
#23522=CARTESIAN_POINT ( 'NONE',  ( 125.2761281442453054, 0.4262465694468514643, -12.03445270309931736 ) ) ;
#23523=CARTESIAN_POINT ( 'NONE',  ( 118.0151148109119816, 0.4262465694468514643, -12.03445270309931736 ) ) ;
#23528=B_SPLINE_CURVE_WITH_KNOTS ( 'NONE', 3,
 ( #30822, #41550, #2776, #44745, #34446, #38104, #24212 ),
 .UNSPECIFIED., .F., .F.,
 ( 4, 3, 4 ),
 ( 0.000000000000000000, 0.0003208458851410865066, 0.0006416917706845399550 ),
 .UNSPECIFIED. ) ;
#23529=CARTESIAN_POINT ( 'NONE',  ( 115.0086014775786509, -4.089484607189486809, -7.948022111789456723 ) ) ;
#23530=CARTESIAN_POINT ( 'NONE',  ( 122.0994348109119443, -10.15424416112533912, -14.75197769757731336 ) ) ;
#23531=ORIENTED_EDGE ( 'NONE', *, *, #30147, .F. ) ;
#23533=CARTESIAN_POINT ( 'NONE',  ( 137.4478226697587502, -0.5562480781206902147, -10.71977384483395568 ) ) ;
#23534=CARTESIAN_POINT ( 'NONE',  ( 120.4543614775786295, -4.089484607189486809, -7.948022111789456723 ) ) ;
#23537=CARTESIAN_POINT ( 'NONE',  ( 117.0507614775786465, 0.1319031606808879209, -14.10382304977623669 ) ) ;
#23541=CARTESIAN_POINT ( 'NONE',  ( 126.5241148109119393, -9.565557343593413364, -10.61323700422348004 ) ) ;
#23544=CARTESIAN_POINT ( 'NONE',  ( 121.8158014775786171, -4.153390946401325223, -8.397313243818185668 ) ) ;
#23546=CARTESIAN_POINT ( 'NONE',  ( 123.2339681442453241, -6.344957434206665248, -7.627207830600338134 ) ) ;
#23548=CARTESIAN_POINT ( 'NONE',  ( 118.4689281442453392, 0.9020085738987339008, -11.91225656197089222 ) ) ;
#23549=CARTESIAN_POINT ( 'NONE',  ( 118.8092881442453290, -9.988377603198976828, -10.36322818467138340 ) ) ;
#23550=CARTESIAN_POINT ( 'NONE',  ( 118.5256548109119876, -8.899110576539710493, -16.42337572283490132 ) ) ;
#23551=CARTESIAN_POINT ( 'NONE',  ( 123.2339681442453241, -3.505236298600246325, -18.68346056562440793 ) ) ;
#23554=CARTESIAN_POINT ( 'NONE',  ( 123.3474214775786209, -0.1624402480850797581, -16.17319339645315424 ) ) ;
#23555=DIRECTION ( 'NONE',  ( 0.000000000000000000, -0.7996358532186280677, -0.6004852223388321697 ) ) ;
#23562=CARTESIAN_POINT ( 'NONE',  ( 123.8012348109119642, 0.2603800115204892296, -16.42320221600525088 ) ) ;
#23563=CARTESIAN_POINT ( 'NONE',  ( 124.3685014775786328, 0.4262465694468514643, -12.03445270309931736 ) ) ;
#23565=CARTESIAN_POINT ( 'NONE',  ( 124.0281414775786146, -1.834011780172310813, -8.268836392978581529 ) ) ;
#23566=CARTESIAN_POINT ( 'NONE',  ( 112.9097148109120070, -9.565557343593413364, -10.61323700422348004 ) ) ;
#23568=CARTESIAN_POINT ( 'NONE',  ( 120.4543614775786295, -4.089484607189486809, -7.948022111789456723 ) ) ;
#23569=CARTESIAN_POINT ( 'NONE',  ( 122.9503348109119827, 0.5811942927096110934, -14.16772938898807510 ) ) ;
#23571=CARTESIAN_POINT ( 'NONE',  ( 122.2128881442453263, -7.643976991954077427, -18.09477374809248928 ) ) ;
#23577=CARTESIAN_POINT ( 'NONE',  ( 123.3474214775786209, -0.1624402480850797581, -16.17319339645315424 ) ) ;
#23580=CARTESIAN_POINT ( 'NONE',  ( 117.3343948109119737, -6.222761293078241884, -8.102969835052219238 ) ) ;
#23581=CARTESIAN_POINT ( 'NONE',  ( 117.6747548109119919, -7.643976991954077427, -18.09477374809248928 ) ) ;
#23582=CARTESIAN_POINT ( 'NONE',  ( 123.2339681442453241, -6.344957434206665248, -7.627207830600338134 ) ) ;
#23584=CARTESIAN_POINT ( 'NONE',  ( 122.0427081442452817, -9.859900752359378018, -12.68260735090039759 ) ) ;
#23585=CARTESIAN_POINT ( 'NONE',  ( 118.6391081442452986, -4.089484607189486809, -7.948022111789456723 ) ) ;
#23586=CARTESIAN_POINT ( 'NONE',  ( 125.3895814775786448, -7.893985811506177619, -18.51759400769804742 ) ) ;
#23587=CARTESIAN_POINT ( 'NONE',  ( 122.3830681442452857, -1.833838273342659697, -17.42832698103878286 ) ) ;
#23591=CARTESIAN_POINT ( 'NONE',  ( 125.7866681442452688, -0.4660016031367893996, -10.09054647747474043 ) ) ;
#23592=CARTESIAN_POINT ( 'NONE',  ( 116.3133148109120043, -2.084020599724406786, -8.691656652584148546 ) ) ;
#23593=CARTESIAN_POINT ( 'NONE',  ( 124.3685014775786328, -10.63000616557722466, -14.87417383870573495 ) ) ;
#23594=CARTESIAN_POINT ( 'NONE',  ( 117.6067460002551002, -2.334846009198389805, -18.01015021110788439 ) ) ;
#23596=EDGE_LOOP ( 'NONE', ( #11258, #24413, #36960, #30660, #35329 ) ) ;
#23601=CARTESIAN_POINT ( 'NONE',  ( 118.1285681442453068, -2.084020599724406786, -8.691656652584148546 ) ) ;
#23602=CARTESIAN_POINT ( 'NONE',  ( 113.3635281442453504, -0.1624402480850797581, -16.17319339645315424 ) ) ;
#23603=CARTESIAN_POINT ( 'NONE',  ( 126.4262034846834126, -0.4795738038250874635, -10.78031458779252638 ) ) ;
#23605=CARTESIAN_POINT ( 'NONE',  ( 138.2184548109119930, -7.252096815532139473, -18.89748516540533529 ) ) ;
#23606=CARTESIAN_POINT ( 'NONE',  ( 120.0572748109119772, -6.222761293078241884, -8.102969835052219238 ) ) ;
#23607=CARTESIAN_POINT ( 'NONE',  ( 112.5126281442453120, 0.1319031606808879209, -14.10382304977623669 ) ) ;
#23612=CARTESIAN_POINT ( 'NONE',  ( 125.2194014775786286, 0.1319031606808879209, -14.10382304977623669 ) ) ;
#23614=CARTESIAN_POINT ( 'NONE',  ( 111.8319081442453182, -5.638512984488999180, -18.83840828888717311 ) ) ;
#23617=CARTESIAN_POINT ( 'NONE',  ( 112.1155414775786454, 0.9020085738987339008, -11.91225656197089222 ) ) ;
#23618=CARTESIAN_POINT ( 'NONE',  ( 121.5321681442453183, -0.1624402480850797581, -16.17319339645315424 ) ) ;
#23622=CARTESIAN_POINT ( 'NONE',  ( 113.8740681442453138, -9.859900752359374465, -12.68260735090039404 ) ) ;
#23627=CARTESIAN_POINT ( 'NONE',  ( 124.9924948109119924, -4.089484607189486809, -7.948022111789456723 ) ) ;
#23628=CARTESIAN_POINT ( 'NONE',  ( 121.7023481442452777, -9.261995988541697145, -16.69588392320189030 ) ) ;
#23629=DIRECTION ( 'NONE',  ( 0.000000000000000000, -0.6004852223388321697, 0.7996358532186280677 ) ) ;
#23630=CARTESIAN_POINT ( 'NONE',  ( 122.0994348109119443, 0.9020085738987339008, -11.91225656197089222 ) ) ;
#23632=CARTESIAN_POINT ( 'NONE',  ( 114.3278814775786429, -10.30919188438810075, -12.61870101168855918 ) ) ;
#23634=CARTESIAN_POINT ( 'NONE',  ( 113.7038881442453402, -6.222761293078241884, -8.102969835052219238 ) ) ;
#23635=CARTESIAN_POINT ( 'NONE',  ( 126.1837548109119211, -10.63000616557722466, -14.87417383870573495 ) ) ;
#23636=CARTESIAN_POINT ( 'NONE',  ( 123.3474214775786209, -9.988377603198976828, -10.36322818467138340 ) ) ;
#23637=CARTESIAN_POINT ( 'NONE',  ( 113.3068014775786594, -8.166667518702817929, -8.995218007635859436 ) ) ;
#23638=CARTESIAN_POINT ( 'NONE',  ( 114.3278814775786429, 0.1319031606808879209, -14.10382304977623669 ) ) ;
#23640=CARTESIAN_POINT ( 'NONE',  ( 118.1852948109119836, -4.153390946401325223, -8.397313243818185668 ) ) ;
#23641=CARTESIAN_POINT ( 'NONE',  ( 112.5126281442453120, -10.30919188438810075, -12.61870101168855918 ) ) ;
#23644=CARTESIAN_POINT ( 'NONE',  ( 122.0427081442452817, -9.859900752359378018, -12.68260735090039759 ) ) ;
#23649=DIRECTION ( 'NONE',  ( 1.000000000000000000, 0.000000000000000000, 0.000000000000000000 ) ) ;
#23657=CARTESIAN_POINT ( 'NONE',  ( 123.2331352477523723, -1.220279397241712971, -16.99638242193887194 ) ) ;
#23658=CARTESIAN_POINT ( 'NONE',  ( 116.7671281442453335, -1.834011780172310813, -8.268836392978581529 ) ) ;
#23661=CARTESIAN_POINT ( 'NONE',  ( 125.1048602609374001, -2.479354771058042584, -17.81771518891497763 ) ) ;
#23663=CARTESIAN_POINT ( 'NONE',  ( 122.4965214775786251, 0.1319031606808879209, -14.10382304977623669 ) ) ;
#23666=CARTESIAN_POINT ( 'NONE',  ( 135.4522060580443394, -9.608978949641880263, -9.721040106140581116 ) ) ;
#23667=CARTESIAN_POINT ( 'NONE',  ( 119.6034614775786196, -6.344957434206665248, -7.627207830600338134 ) ) ;
#23669=CARTESIAN_POINT ( 'NONE',  ( 115.6325948109119821, -9.565557343593413364, -10.61323700422348004 ) ) ;
#23671=CARTESIAN_POINT ( 'NONE',  ( 123.9146881442452894, 0.9020085738987339008, -11.91225656197089222 ) ) ;
#23676=CARTESIAN_POINT ( 'NONE',  ( 115.1220548109119761, -1.833838273342658809, -17.42832698103878286 ) ) ;
#23677=CARTESIAN_POINT ( 'NONE',  ( 116.3700414775786527, -4.153390946401321671, -8.397313243818183892 ) ) ;
#23681=EDGE_CURVE ( 'NONE', #41698, #1633, #26259, .T. ) ;
#23683=CARTESIAN_POINT ( 'NONE',  ( 113.1933481442453058, -4.089484607189486809, -7.948022111789456723 ) ) ;
#23692=CARTESIAN_POINT ( 'NONE',  ( 111.4739159103406223, -1.291319350021640888, -16.90178210349550625 ) ) ;
#23694=CARTESIAN_POINT ( 'NONE',  ( 117.1074881442453233, -10.63000616557722466, -14.87417383870573495 ) ) ;
#23695=CARTESIAN_POINT ( 'NONE',  ( 112.0020881442453344, 0.2603800115204892296, -16.42320221600525088 ) ) ;
#23696=CARTESIAN_POINT ( 'NONE',  ( 117.1642148109119859, -0.8288870151387760510, -10.36305467784173118 ) ) ;
#23698=CARTESIAN_POINT ( 'NONE',  ( 121.5888948109119809, -10.30919188438810075, -12.61870101168855918 ) ) ;
#23699=CARTESIAN_POINT ( 'NONE',  ( 119.6601881442453106, -8.166667518702819706, -8.995218007635861213 ) ) ;
#23701=CARTESIAN_POINT ( 'NONE',  ( 114.4413348109119823, -0.8288870151387760510, -10.36305467784173118 ) ) ;
#23704=CARTESIAN_POINT ( 'NONE',  ( 118.9227414775786400, -10.63000616557722466, -14.87417383870573495 ) ) ;
#23706=CARTESIAN_POINT ( 'NONE',  ( 116.2565881442452991, -9.261995988541697145, -16.69588392320189030 ) ) ;
#23708=ORIENTED_EDGE ( 'NONE', *, *, #6757, .F. ) ;
#23709=CARTESIAN_POINT ( 'NONE',  ( 122.3263414775786373, -6.344957434206665248, -7.627207830600338134 ) ) ;
#23710=DIRECTION ( 'NONE',  ( 0.000000000000000000, 0.6004852223388318366, -0.7996358532186281787 ) ) ;
#23711=CARTESIAN_POINT ( 'NONE',  ( 112.8529881442453302, -7.894159318335828068, -9.358103419637847864 ) ) ;
#23713=CARTESIAN_POINT ( 'NONE',  ( 114.6115148109119986, -6.222761293078241884, -8.102969835052219238 ) ) ;
#23716=CARTESIAN_POINT ( 'NONE',  ( 118.9794681442453026, -0.8288870151387760510, -10.36305467784173118 ) ) ;
#23717=CARTESIAN_POINT ( 'NONE',  ( 151.2860562277021472, -3.719473736431747390, -16.16631137400202078 ) ) ;
#23718=CARTESIAN_POINT ( 'NONE',  ( 114.6115148109119986, -6.222761293078241884, -8.102969835052219238 ) ) ;
#23719=CARTESIAN_POINT ( 'NONE',  ( 114.0442481442453300, -1.834011780172310813, -8.268836392978581529 ) ) ;
#23721=CARTESIAN_POINT ( 'NONE',  ( 126.3539348109119800, -4.153390946401325223, -8.397313243818185668 ) ) ;
#23722=CARTESIAN_POINT ( 'NONE',  ( 116.5402214775786405, -9.565557343593413364, -10.61323700422348004 ) ) ;
#23723=CARTESIAN_POINT ( 'NONE',  ( 113.0231681442453180, -10.15424416112533912, -14.75197769757731336 ) ) ;
#23724=CARTESIAN_POINT ( 'NONE',  ( 117.3343948109119737, -6.222761293078241884, -8.102969835052219238 ) ) ;
#23726=CARTESIAN_POINT ( 'NONE',  ( 111.7184548109119788, -9.261995988541697145, -16.69588392320189030 ) ) ;
#23732=CARTESIAN_POINT ( 'NONE',  ( 117.6747548109119919, -1.834011780172310813, -8.268836392978581529 ) ) ;
#23734=CARTESIAN_POINT ( 'NONE',  ( 125.8433948109119456, -1.834011780172310813, -8.268836392978581529 ) ) ;
#23737=CARTESIAN_POINT ( 'NONE',  ( 119.5467348109119712, -5.574606645277164318, -18.38911715685844683 ) ) ;
#23739=CARTESIAN_POINT ( 'NONE',  ( 124.9357681442453014, -1.834011780172310813, -8.268836392978581529 ) ) ;
#23741=CARTESIAN_POINT ( 'NONE',  ( 127.7184548109119788, -4.863998795839242995, -13.39321520033831447 ) ) ;
#23744=CARTESIAN_POINT ( 'NONE',  ( 124.3685014775786328, 0.4262465694468514643, -12.03445270309931736 ) ) ;
#23745=CARTESIAN_POINT ( 'NONE',  ( 120.1707281442453166, 0.2603800115204892296, -16.42320221600525088 ) ) ;
#23746=CARTESIAN_POINT ( 'NONE',  ( 113.5904348109119866, -2.084020599724406786, -8.691656652584148546 ) ) ;
#23747=CARTESIAN_POINT ( 'NONE',  ( 117.7314814775786260, -4.089484607189486809, -7.948022111789456723 ) ) ;
#23749=ADVANCED_FACE ( 'NONE', ( #33780 ), #8993, .T. ) ;
#23750=CARTESIAN_POINT ( 'NONE',  ( 127.0553483106876058, -1.260408809135023178, -9.346765518329249289 ) ) ;
#23751=CARTESIAN_POINT ( 'NONE',  ( 123.5743281442453139, -2.084020599724406786, -8.691656652584148546 ) ) ;
#23755=CARTESIAN_POINT ( 'NONE',  ( 118.1852948109119836, -5.638512984488999180, -18.83840828888717311 ) ) ;
#23756=CARTESIAN_POINT ( 'NONE',  ( 120.1140014775786398, -7.894159318335828068, -9.358103419637847864 ) ) ;
#23760=CARTESIAN_POINT ( 'NONE',  ( 119.4900081442453086, -1.834011780172310813, -8.268836392978581529 ) ) ;
#23762=CARTESIAN_POINT ( 'NONE',  ( 115.8027748109119841, -8.899110576539710493, -16.42337572283490132 ) ) ;
#23764=ORIENTED_EDGE ( 'NONE', *, *, #9323, .F. ) ;
#23765=CARTESIAN_POINT ( 'NONE',  ( 125.5030348109119558, -6.222761293078241884, -8.102969835052219238 ) ) ;
#23766=VECTOR ( 'NONE', #35870, 999.9999999999998863 ) ;
#23767=CARTESIAN_POINT ( 'NONE',  ( 124.0848681442452772, -5.574606645277164318, -18.38911715685844683 ) ) ;
#23770=CARTESIAN_POINT ( 'NONE',  ( 120.8514481442452961, -7.893985811506177619, -18.51759400769804742 ) ) ;
#23772=CARTESIAN_POINT ( 'NONE',  ( 117.0734209221557336, -2.372251574601226043, -17.96033910819752322 ) ) ;
#23773=CARTESIAN_POINT ( 'NONE',  ( 119.2631014775786298, 0.2603800115204892296, -16.42320221600525088 ) ) ;
#23774=CARTESIAN_POINT ( 'NONE',  ( 120.5110881442453206, -6.344957434206665248, -7.627207830600338134 ) ) ;
#23775=CARTESIAN_POINT ( 'NONE',  ( 118.6958348109119754, -3.505236298600246325, -18.68346056562440793 ) ) ;
#23776=CARTESIAN_POINT ( 'NONE',  ( 124.2550481442452792, -0.1624402480850797581, -16.17319339645315424 ) ) ;
#23777=CARTESIAN_POINT ( 'NONE',  ( 113.0798948109119948, -0.4660016031367893996, -10.09054647747474043 ) ) ;
#23781=CARTESIAN_POINT ( 'NONE',  ( 122.1561614775786353, -8.899110576539710493, -16.42337572283490132 ) ) ;
#23782=CARTESIAN_POINT ( 'NONE',  ( 122.4040527111058339, -1.267766418764731728, -16.93314635290706605 ) ) ;
#23787=CARTESIAN_POINT ( 'NONE',  ( 123.9714148109119805, -0.4660016031367893996, -10.09054647747474043 ) ) ;
#23788=CARTESIAN_POINT ( 'NONE',  ( 122.0427081442452817, -9.859900752359378018, -12.68260735090039759 ) ) ;
#23789=ORIENTED_EDGE ( 'NONE', *, *, #5890, .T. ) ;
#23790=CARTESIAN_POINT ( 'NONE',  ( 124.8790414775786246, -0.4660016031367893996, -10.09054647747474043 ) ) ;
#23791=CARTESIAN_POINT ( 'NONE',  ( 114.2711548109119803, -0.1624402480850797581, -16.17319339645315424 ) ) ;
#23793=CARTESIAN_POINT ( 'NONE',  ( 122.2696148109119889, -4.089484607189486809, -7.948022111789456723 ) ) ;
#23795=CARTESIAN_POINT ( 'NONE',  ( 121.3619881442452879, -4.089484607189486809, -7.948022111789456723 ) ) ;
#23797=CARTESIAN_POINT ( 'NONE',  ( 111.9453614775786434, -1.561330072975668060, -17.79121239304076596 ) ) ;
#23800=ORIENTED_EDGE ( 'NONE', *, *, #42891, .F. ) ;
#23801=CARTESIAN_POINT ( 'NONE',  ( 124.8286333359170186, -2.311015703046761960, -18.04188382666269774 ) ) ;
#23802=CARTESIAN_POINT ( 'NONE',  ( 113.1366214775786432, -7.643976991954077427, -18.09477374809248928 ) ) ;
#23803=CARTESIAN_POINT ( 'NONE',  ( 125.5030348109119558, -6.222761293078241884, -8.102969835052219238 ) ) ;
#23805=CIRCLE ( 'NONE', #29602, 5.999999999999997335 ) ;
#23808=CARTESIAN_POINT ( 'NONE',  ( 122.7801548109119665, -6.222761293078241884, -8.102969835052219238 ) ) ;
#23810=CARTESIAN_POINT ( 'NONE',  ( 115.4056881442453459, -2.084020599724406786, -8.691656652584148546 ) ) ;
#23811=CARTESIAN_POINT ( 'NONE',  ( 124.4252281442452812, -9.261995988541697145, -16.69588392320189030 ) ) ;
#23814=CARTESIAN_POINT ( 'NONE',  ( 123.1772414775786189, -5.574606645277164318, -18.38911715685844683 ) ) ;
#23815=CARTESIAN_POINT ( 'NONE',  ( 118.8092881442453290, -9.988377603198976828, -10.36322818467138340 ) ) ;
#23816=CARTESIAN_POINT ( 'NONE',  ( 124.1983214775786166, -8.166667518702819706, -8.995218007635861213 ) ) ;
#23819=CARTESIAN_POINT ( 'NONE',  ( 128.2184548109119930, -4.863998795839242995, -13.39321520033831447 ) ) ;
#23821=CARTESIAN_POINT ( 'NONE',  ( 123.4041481442452834, -10.30919188438810075, -12.61870101168855918 ) ) ;
#23823=CARTESIAN_POINT ( 'NONE',  ( 116.0864081442453113, -0.1624402480850797581, -16.17319339645315424 ) ) ;
#23824=CARTESIAN_POINT ( 'NONE',  ( 113.7606148109119886, -7.894159318335828068, -9.358103419637847864 ) ) ;
#23827=ORIENTED_EDGE ( 'NONE', *, *, #2188, .F. ) ;
#23833=CARTESIAN_POINT ( 'NONE',  ( 122.6099748109119929, -0.8288870151387760510, -10.36305467784173118 ) ) ;
#23834=CARTESIAN_POINT ( 'NONE',  ( 113.8740681442453138, -9.859900752359374465, -12.68260735090039404 ) ) ;
#23837=CARTESIAN_POINT ( 'NONE',  ( 114.3846081442453197, 0.4262465694468514643, -12.03445270309931736 ) ) ;
#23843=CARTESIAN_POINT ( 'NONE',  ( 126.0135748109119902, -1.833838273342660141, -17.42832698103878286 ) ) ;
#23844=ORIENTED_EDGE ( 'NONE', *, *, #36698, .T. ) ;
#23845=CARTESIAN_POINT ( 'NONE',  ( 113.3068014775786594, -8.166667518702817929, -8.995218007635859436 ) ) ;
#23846=CARTESIAN_POINT ( 'NONE',  ( 113.5449902882355104, -1.135392229370320694, -17.10942237759953954 ) ) ;
#23848=CARTESIAN_POINT ( 'NONE',  ( 125.3328548109119964, -0.8288870151387760510, -10.36305467784173118 ) ) ;
#23850=CARTESIAN_POINT ( 'NONE',  ( 122.2696148109119889, -5.574606645277164318, -18.38911715685844683 ) ) ;
#23855=CARTESIAN_POINT ( 'NONE',  ( 113.9875214775786532, -8.899110576539710493, -16.42337572283490132 ) ) ;
#23860=CARTESIAN_POINT ( 'NONE',  ( 123.4041481442452834, -10.30919188438810075, -12.61870101168855918 ) ) ;
#23861=CARTESIAN_POINT ( 'NONE',  ( 124.7088614775786226, 0.2603800115204892296, -16.42320221600525088 ) ) ;
#23863=CARTESIAN_POINT ( 'NONE',  ( 119.7169148109119874, -9.988377603198976828, -10.36322818467138340 ) ) ;
#23866=CARTESIAN_POINT ( 'NONE',  ( 113.1366214775786432, -7.643976991954077427, -18.09477374809248928 ) ) ;
#23867=CARTESIAN_POINT ( 'NONE',  ( 124.7655881442452852, 0.5811942927096110934, -14.16772938898807510 ) ) ;
#23868=CARTESIAN_POINT ( 'NONE',  ( 123.0637881442452937, -0.4660016031367893996, -10.09054647747474043 ) ) ;
#23869=CARTESIAN_POINT ( 'NONE',  ( 113.9307948109119906, 0.9020085738987339008, -11.91225656197089222 ) ) ;
#23871=CARTESIAN_POINT ( 'NONE',  ( 112.2289948109119848, -7.643976991954077427, -18.09477374809248928 ) ) ;
#23873=CARTESIAN_POINT ( 'NONE',  ( 116.5402214775786405, -9.565557343593413364, -10.61323700422348004 ) ) ;
#23875=CARTESIAN_POINT ( 'NONE',  ( 123.9146881442452894, -10.15424416112533912, -14.75197769757731336 ) ) ;
#23881=CARTESIAN_POINT ( 'NONE',  ( 125.2761281442453054, -10.63000616557722466, -14.87417383870573495 ) ) ;
#23887=CARTESIAN_POINT ( 'NONE',  ( 115.5559231242421703, -1.016270020561755860, -17.26805140881366896 ) ) ;
#23888=CARTESIAN_POINT ( 'NONE',  ( 119.8870948109119752, -9.261995988541697145, -16.69588392320189030 ) ) ;
#23892=CARTESIAN_POINT ( 'NONE',  ( 125.4463081442452932, -5.638512984488999180, -18.83840828888717311 ) ) ;
#23893=CARTESIAN_POINT ( 'NONE',  ( 119.7736414775786358, 0.1319031606808879209, -14.10382304977623669 ) ) ;
#23896=CARTESIAN_POINT ( 'NONE',  ( 118.5256548109119876, -0.4660016031367893996, -10.09054647747474043 ) ) ;
#23897=CARTESIAN_POINT ( 'NONE',  ( 125.7299414775786346, 0.9020085738987339008, -11.91225656197089222 ) ) ;
#23898=CARTESIAN_POINT ( 'NONE',  ( 115.1220548109119761, -1.833838273342658809, -17.42832698103878286 ) ) ;
#23899=CARTESIAN_POINT ( 'NONE',  ( 113.1366214775786432, -7.643976991954077427, -18.09477374809248928 ) ) ;
#23903=CARTESIAN_POINT ( 'NONE',  ( 117.9583881442453048, 0.1319031606808879209, -14.10382304977623669 ) ) ;
#23904=CARTESIAN_POINT ( 'NONE',  ( 119.7736414775786358, 0.1319031606808879209, -14.10382304977623669 ) ) ;
#23910=CARTESIAN_POINT ( 'NONE',  ( 112.6828081442453282, -7.893985811506177619, -18.51759400769804742 ) ) ;
#23918=CARTESIAN_POINT ( 'NONE',  ( 121.7023481442452777, -9.261995988541697145, -16.69588392320189030 ) ) ;
#23919=CARTESIAN_POINT ( 'NONE',  ( 111.7184548109119788, -9.261995988541697145, -16.69588392320189030 ) ) ;
#23920=CARTESIAN_POINT ( 'NONE',  ( 117.2776681442452968, -4.153390946401321671, -8.397313243818183892 ) ) ;
#23923=CARTESIAN_POINT ( 'NONE',  ( 123.3474214775786209, -9.988377603198976828, -10.36322818467138340 ) ) ;
#23924=CARTESIAN_POINT ( 'NONE',  ( 119.4332814775786318, -0.4660016031367893996, -10.09054647747474043 ) ) ;
#23928=CARTESIAN_POINT ( 'NONE',  ( 112.1155414775786454, -10.15424416112533912, -14.75197769757731336 ) ) ;
#23931=CARTESIAN_POINT ( 'NONE',  ( 118.1285681442453068, -7.893985811506177619, -18.51759400769804742 ) ) ;
#23933=CARTESIAN_POINT ( 'NONE',  ( 116.9940348109119839, -9.988377603198976828, -10.36322818467138340 ) ) ;
#23936=CARTESIAN_POINT ( 'NONE',  ( 113.8173414775786512, -9.565557343593413364, -10.61323700422348004 ) ) ;
#23939=CARTESIAN_POINT ( 'NONE',  ( 114.9518748109119883, -7.643976991954077427, -18.09477374809248928 ) ) ;
#23941=EDGE_CURVE ( 'NONE', #16862, #26433, #26434, .T. ) ;
#23943=CARTESIAN_POINT ( 'NONE',  ( 117.5613014775786525, -10.15424416112533912, -14.75197769757731336 ) ) ;
#23945=CARTESIAN_POINT ( 'NONE',  ( 116.4834948109119779, -7.894159318335828068, -9.358103419637847864 ) ) ;
#23946=CARTESIAN_POINT ( 'NONE',  ( 114.6682414775786469, -1.561330072975668060, -17.79121239304076596 ) ) ;
#23948=CARTESIAN_POINT ( 'NONE',  ( 116.9373081442452929, -8.166667518702817929, -8.995218007635861213 ) ) ;
#23949=CARTESIAN_POINT ( 'NONE',  ( 112.3424481442453384, -3.505236298600246325, -18.68346056562440793 ) ) ;
#23950=CARTESIAN_POINT ( 'NONE',  ( 118.0151148109119816, 0.4262465694468514643, -12.03445270309931736 ) ) ;
#23952=CARTESIAN_POINT ( 'NONE',  ( 113.5904348109119866, -7.893985811506177619, -18.51759400769804742 ) ) ;
#23957=CARTESIAN_POINT ( 'NONE',  ( 117.9583881442453048, -10.30919188438810075, -12.61870101168855918 ) ) ;
#23960=CARTESIAN_POINT ( 'NONE',  ( 118.3554748109119998, -9.565557343593413364, -10.61323700422348004 ) ) ;
#23962=CARTESIAN_POINT ( 'NONE',  ( 122.4965214775786251, -10.30919188438810075, -12.61870101168855918 ) ) ;
#23965=ORIENTED_EDGE ( 'NONE', *, *, #9969, .T. ) ;
#23966=CARTESIAN_POINT ( 'NONE',  ( 125.4463081442452932, -4.153390946401325223, -8.397313243818185668 ) ) ;
#23967=CARTESIAN_POINT ( 'NONE',  ( 125.2194014775786286, -10.30919188438810075, -12.61870101168855918 ) ) ;
#23968=CARTESIAN_POINT ( 'NONE',  ( 117.3343948109119737, -6.222761293078241884, -8.102969835052219238 ) ) ;
#23970=CARTESIAN_POINT ( 'NONE',  ( 120.3976348109119812, -1.834011780172310813, -8.268836392978581529 ) ) ;
#23972=CARTESIAN_POINT ( 'NONE',  ( 126.4162218615806950, -1.128033623988350831, -9.922867115873357236 ) ) ;
#23973=CARTESIAN_POINT ( 'NONE',  ( 122.4397948109119767, -0.1624402480850797581, -16.17319339645315424 ) ) ;
#23977=CARTESIAN_POINT ( 'NONE',  ( 116.7671281442453335, -1.834011780172310813, -8.268836392978581529 ) ) ;
#23978=CARTESIAN_POINT ( 'NONE',  ( 125.7299414775786346, -10.15424416112533912, -14.75197769757731336 ) ) ;
#23982=CARTESIAN_POINT ( 'NONE',  ( 135.9690293846647364, -1.212003134032930030, -8.725841475540576653 ) ) ;
#23983=CARTESIAN_POINT ( 'NONE',  ( 121.2485348109119769, -0.4660016031367893996, -10.09054647747474043 ) ) ;
#23985=CARTESIAN_POINT ( 'NONE',  ( 119.3198281442452924, -9.859900752359374465, -12.68260735090039404 ) ) ;
#23988=CARTESIAN_POINT ( 'NONE',  ( 112.3424481442453384, -6.344957434206662583, -7.627207830600332805 ) ) ;
#23994=CARTESIAN_POINT ( 'NONE',  ( 120.7379948109119709, -10.63000616557722466, -14.87417383870573495 ) ) ;
#23997=CARTESIAN_POINT ( 'NONE',  ( 120.7379948109119709, -10.63000616557722466, -14.87417383870573495 ) ) ;
#23998=CARTESIAN_POINT ( 'NONE',  ( 118.3554748109119998, 0.2603800115204892296, -16.42320221600525088 ) ) ;
#23999=CARTESIAN_POINT ( 'NONE',  ( 119.4900081442453086, -7.643976991954077427, -18.09477374809248928 ) ) ;
#24002=CARTESIAN_POINT ( 'NONE',  ( 115.7460481442453357, 0.9020085738987339008, -11.91225656197089222 ) ) ;
#24004=CARTESIAN_POINT ( 'NONE',  ( 126.5241148109119393, -9.565557343593413364, -10.61323700422348004 ) ) ;
#24005=FACE_OUTER_BOUND ( 'NONE', #14200, .T. ) ;
#24009=CARTESIAN_POINT ( 'NONE',  ( 122.0427081442452817, 0.5811942927096110934, -14.16772938898807510 ) ) ;
#24010=CARTESIAN_POINT ( 'NONE',  ( 123.6877814775786533, -6.222761293078241884, -8.102969835052219238 ) ) ;
#24012=CARTESIAN_POINT ( 'NONE',  ( 125.9568481442452850, -6.344957434206665248, -7.627207830600338134 ) ) ;
#24015=CARTESIAN_POINT ( 'NONE',  ( 124.2550481442452792, -9.988377603198980381, -10.36322818467138518 ) ) ;
#24016=CARTESIAN_POINT ( 'NONE',  ( 119.7169148109119874, -9.988377603198976828, -10.36322818467138340 ) ) ;
#24018=CARTESIAN_POINT ( 'NONE',  ( 112.0588148109119828, 0.5811942927096154232, -14.16772938898807155 ) ) ;
#24023=CARTESIAN_POINT ( 'NONE',  ( 112.1722681442453222, -8.899110576539710493, -16.42337572283490132 ) ) ;
#24024=CARTESIAN_POINT ( 'NONE',  ( 122.6667014775786413, -2.084020599724406786, -8.691656652584148546 ) ) ;
#24027=CARTESIAN_POINT ( 'NONE',  ( 122.2128881442453263, -7.643976991954077427, -18.09477374809248928 ) ) ;
#24029=CARTESIAN_POINT ( 'NONE',  ( 115.9162281442453093, -5.574606645277164318, -18.38911715685844683 ) ) ;
#24030=CARTESIAN_POINT ( 'NONE',  ( 113.5904348109119866, -2.084020599724406786, -8.691656652584148546 ) ) ;
#24033=CARTESIAN_POINT ( 'NONE',  ( 119.4332814775786318, -0.4660016031367893996, -10.09054647747474043 ) ) ;
#24040=CARTESIAN_POINT ( 'NONE',  ( 113.5904348109119866, -2.084020599724406786, -8.691656652584148546 ) ) ;
#24041=CARTESIAN_POINT ( 'NONE',  ( 115.2922348109119781, 0.4262465694468514643, -12.03445270309931736 ) ) ;
#24051=CARTESIAN_POINT ( 'NONE',  ( 124.6521348109119884, -7.894159318335828068, -9.358103419637847864 ) ) ;
#24052=CARTESIAN_POINT ( 'NONE',  ( 114.5547881442453217, -4.153390946401321671, -8.397313243818183892 ) ) ;
#24056=CARTESIAN_POINT ( 'NONE',  ( 112.2857214775786474, -5.574606645277164318, -18.38911715685844683 ) ) ;
#24061=CARTESIAN_POINT ( 'NONE',  ( 125.9568481442452850, -6.344957434206665248, -7.627207830600338134 ) ) ;
#24062=CARTESIAN_POINT ( 'NONE',  ( 125.1626748109119802, -0.1624402480850797581, -16.17319339645315424 ) ) ;
#24065=CARTESIAN_POINT ( 'NONE',  ( 113.3635281442453504, -9.988377603198976828, -10.36322818467138340 ) ) ;
#24068=CARTESIAN_POINT ( 'NONE',  ( 126.1837548109119496, 0.4262465694468514643, -12.03445270309931736 ) ) ;
#24069=CARTESIAN_POINT ( 'NONE',  ( 124.3117748109119844, 0.1319031606808879209, -14.10382304977623669 ) ) ;
#24073=CARTESIAN_POINT ( 'NONE',  ( 114.1009748109119784, -5.574606645277164318, -18.38911715685844683 ) ) ;
#24077=CARTESIAN_POINT ( 'NONE',  ( 124.8790414775786246, -0.4660016031367893996, -10.09054647747474043 ) ) ;
#24078=CARTESIAN_POINT ( 'NONE',  ( 112.1722681442453222, -8.899110576539710493, -16.42337572283490132 ) ) ;
#24080=CARTESIAN_POINT ( 'NONE',  ( 120.2274548109119934, 0.5811942927096110934, -14.16772938898807510 ) ) ;
#24081=CARTESIAN_POINT ( 'NONE',  ( 117.2776681442452968, -5.638512984488999180, -18.83840828888717311 ) ) ;
#24083=CARTESIAN_POINT ( 'NONE',  ( 125.1626748109119802, -9.988377603198980381, -10.36322818467138518 ) ) ;
#24084=CARTESIAN_POINT ( 'NONE',  ( 123.0070614775786169, 0.9020085738987339008, -11.91225656197089222 ) ) ;
#24086=CARTESIAN_POINT ( 'NONE',  ( 114.6682414775786469, -1.561330072975668060, -17.79121239304076596 ) ) ;
#24087=CARTESIAN_POINT ( 'NONE',  ( 114.7816948109119863, -9.859900752359374465, -12.68260735090039404 ) ) ;
#24089=CARTESIAN_POINT ( 'NONE',  ( 117.0507614775786465, 0.1319031606808879209, -14.10382304977623669 ) ) ;
#24091=CARTESIAN_POINT ( 'NONE',  ( 116.2565881442452991, -9.261995988541697145, -16.69588392320189030 ) ) ;
#24092=CARTESIAN_POINT ( 'NONE',  ( 124.1983214775786166, -1.833838273342659697, -17.42832698103878286 ) ) ;
#24098=CARTESIAN_POINT ( 'NONE',  ( 125.5030348109119558, -3.383040157471821630, -19.15922257007629170 ) ) ;
#24103=CARTESIAN_POINT ( 'NONE',  ( 112.2857214775786474, -5.574606645277164318, -18.38911715685844683 ) ) ;
#24106=CARTESIAN_POINT ( 'NONE',  ( 118.0718414775786300, -9.261995988541697145, -16.69588392320189030 ) ) ;
#24107=CARTESIAN_POINT ( 'NONE',  ( 136.5266930377887888, -4.268568095932804951, -19.09868834485503442 ) ) ;
#24111=CARTESIAN_POINT ( 'NONE',  ( 120.8514481442452961, -2.084020599724406786, -8.691656652584148546 ) ) ;
#24113=CARTESIAN_POINT ( 'NONE',  ( 125.1059481442452750, -8.166667518702819706, -8.995218007635861213 ) ) ;
#24114=CARTESIAN_POINT ( 'NONE',  ( 120.6245414775786458, -9.988377603198976828, -10.36322818467138340 ) ) ;
#24116=CARTESIAN_POINT ( 'NONE',  ( 117.1074881442453233, 0.4262465694468514643, -12.03445270309931736 ) ) ;
#24117=CARTESIAN_POINT ( 'NONE',  ( 112.1722681442453222, -8.899110576539710493, -16.42337572283490132 ) ) ;
#24121=CARTESIAN_POINT ( 'NONE',  ( 118.1852948109119836, -4.153390946401325223, -8.397313243818185668 ) ) ;
#24123=CARTESIAN_POINT ( 'NONE',  ( 121.3052614775786111, -7.643976991954077427, -18.09477374809248928 ) ) ;
#24129=CARTESIAN_POINT ( 'NONE',  ( 115.0653281442453277, -6.344957434206662583, -7.627207830600332805 ) ) ;
#24130=CARTESIAN_POINT ( 'NONE',  ( 114.1009748109119784, -4.089484607189486809, -7.948022111789456723 ) ) ;
#24132=ORIENTED_EDGE ( 'NONE', *, *, #43997, .F. ) ;
#24133=CARTESIAN_POINT ( 'NONE',  ( 123.4428756873493569, -2.767871776335191658, -14.93546065993297667 ) ) ;
#24135=CARTESIAN_POINT ( 'NONE',  ( 122.0994348109119443, 0.9020085738987339008, -11.91225656197089222 ) ) ;
#24136=CARTESIAN_POINT ( 'NONE',  ( 126.6942948109119840, -8.899110576539710493, -16.42337572283490132 ) ) ;
#24137=CARTESIAN_POINT ( 'NONE',  ( 118.1852948109119836, -4.153390946401325223, -8.397313243818185668 ) ) ;
#24138=FILL_AREA_STYLE ('',( #3807 ) ) ;
#24140=CARTESIAN_POINT ( 'NONE',  ( 123.2906948109119867, -8.166667518702819706, -8.995218007635861213 ) ) ;
#24141=CARTESIAN_POINT ( 'NONE',  ( 117.6180281442453150, -0.4660016031367893996, -10.09054647747474043 ) ) ;
#24144=CARTESIAN_POINT ( 'NONE',  ( 112.3424481442453384, -3.505236298600246325, -18.68346056562440793 ) ) ;
#24148=CARTESIAN_POINT ( 'NONE',  ( 116.8238548109119819, -4.089484607189486809, -7.948022111789456723 ) ) ;
#24150=CARTESIAN_POINT ( 'NONE',  ( 116.3700414775786527, -5.638512984488999180, -18.83840828888717311 ) ) ;
#24154=CARTESIAN_POINT ( 'NONE',  ( 125.5030348109119558, -3.383040157471821630, -19.15922257007629170 ) ) ;
#24156=CARTESIAN_POINT ( 'NONE',  ( 113.2500748109119968, -3.505236298600246325, -18.68346056562440793 ) ) ;
#24158=CARTESIAN_POINT ( 'NONE',  ( 116.5402214775786405, -9.565557343593413364, -10.61323700422348004 ) ) ;
#24159=CARTESIAN_POINT ( 'NONE',  ( 120.1730908535611491, -2.239543233855044946, -18.13706010537467606 ) ) ;
#24160=CARTESIAN_POINT ( 'NONE',  ( 118.1852948109119836, -4.153390946401325223, -8.397313243818185668 ) ) ;
#24162=CARTESIAN_POINT ( 'NONE',  ( 118.5823814775786360, -7.643976991954077427, -18.09477374809248928 ) ) ;
#24164=CARTESIAN_POINT ( 'NONE',  ( 116.0296814775786345, -8.166667518702817929, -8.995218007635861213 ) ) ;
#24165=CARTESIAN_POINT ( 'NONE',  ( 125.9001214775786224, -4.089484607189486809, -7.948022111789456723 ) ) ;
#24166=CARTESIAN_POINT ( 'NONE',  ( 118.6958348109119754, -3.505236298600246325, -18.68346056562440793 ) ) ;
#24168=CARTESIAN_POINT ( 'NONE',  ( 117.3911214775786505, -1.561330072975668504, -17.79121239304076951 ) ) ;
#24173=B_SPLINE_CURVE_WITH_KNOTS ( 'NONE', 3,
 ( #15669, #19991, #2422, #37067, #29348, #29797, #29571, #16120, #26379, #16346 ),
 .UNSPECIFIED., .F., .F.,
 ( 4, 3, 3, 4 ),
 ( 0.000000000000000000, 0.0001671877548681284921, 0.0003343755096277730159, 0.0006463528481650619413 ),
 .UNSPECIFIED. ) ;
#24174=CARTESIAN_POINT ( 'NONE',  ( 120.7379948109119709, -10.63000616557722466, -14.87417383870573495 ) ) ;
#24176=CARTESIAN_POINT ( 'NONE',  ( 126.3063647503472851, -8.168462963394901521, -9.582415806495719224 ) ) ;
#24177=CARTESIAN_POINT ( 'NONE',  ( 116.5969481442453031, -9.859900752359374465, -12.68260735090039404 ) ) ;
#24178=CARTESIAN_POINT ( 'NONE',  ( 124.8223148109119904, -10.15424416112542083, -14.75197769757788713 ) ) ;
#24179=CARTESIAN_POINT ( 'NONE',  ( 124.4252281442452812, -9.261995988541697145, -16.69588392320189030 ) ) ;
#24183=CARTESIAN_POINT ( 'NONE',  ( 112.7962614775786676, -3.383040157471821630, -19.15922257007629170 ) ) ;
#24184=CARTESIAN_POINT ( 'NONE',  ( 111.7751814775786556, -7.893985811506177619, -18.51759400769804742 ) ) ;
#24185=CARTESIAN_POINT ( 'NONE',  ( 121.6456214775786293, -10.63000616557722466, -14.87417383870573495 ) ) ;
#24186=CARTESIAN_POINT ( 'NONE',  ( 116.1998614775786507, 0.4262465694468514643, -12.03445270309931736 ) ) ;
#24188=CARTESIAN_POINT ( 'NONE',  ( 120.7379948109119709, -10.63000616557722466, -14.87417383870573495 ) ) ;
#24191=CARTESIAN_POINT ( 'NONE',  ( 122.4965214775786251, 0.1319031606808879209, -14.10382304977623669 ) ) ;
#24196=CARTESIAN_POINT ( 'NONE',  ( 115.6893214775786447, 0.5811942927096154232, -14.16772938898807155 ) ) ;
#24197=CARTESIAN_POINT ( 'NONE',  ( 135.9373687277985425, -8.517831521581461729, -18.06820524589254262 ) ) ;
#24201=CARTESIAN_POINT ( 'NONE',  ( 123.1205148109119563, -1.834011780172310813, -8.268836392978581529 ) ) ;
#24203=CARTESIAN_POINT ( 'NONE',  ( 119.7169148109119874, -0.1624402480850797581, -16.17319339645315424 ) ) ;
#24204=EDGE_LOOP ( 'NONE', ( #12276, #12756, #24284, #41293, #4723, #17305, #28574, #10073, #25110, #8861, #42299, #44963, #28387, #17396, #33274, #10461, #37654, #7060, #12823, #2310, #12173, #37345, #37384, #4379, #44701, #8755, #37909, #28238, #36283, #15515, #44616, #26691, #3929, #10816, #20128, #1331, #34622, #17405, #24385, #14908, #31695, #22723, #30963, #40762, #9775 ) ) ;
#24205=VERTEX_POINT ( 'NONE', #1977 ) ;
#24207=CARTESIAN_POINT ( 'NONE',  ( 113.0798948109119948, -0.4660016031367893996, -10.09054647747474043 ) ) ;
#24208=CARTESIAN_POINT ( 'NONE',  ( 122.8936081442453059, -9.565557343593413364, -10.61323700422348004 ) ) ;
#24210=CARTESIAN_POINT ( 'NONE',  ( 122.4397948109119767, -9.988377603198976828, -10.36322818467138340 ) ) ;
#24211=EDGE_CURVE ( 'NONE', #37424, #10826, #2885, .T. ) ;
#24212=CARTESIAN_POINT ( 'NONE',  ( 111.2647102085435193, -8.897589485953298905, -16.42540022429002633 ) ) ;
#24213=CARTESIAN_POINT ( 'NONE',  ( 117.0341443147880511, -2.395992375830784837, -17.92872468182854107 ) ) ;
#24214=CARTESIAN_POINT ( 'NONE',  ( 119.4900081442453086, -1.834011780172310813, -8.268836392978581529 ) ) ;
#24215=CARTESIAN_POINT ( 'NONE',  ( 119.6034614775786196, -6.344957434206665248, -7.627207830600338134 ) ) ;
#24216=CARTESIAN_POINT ( 'NONE',  ( 119.0361948109119652, -2.084020599724406786, -8.691656652584148546 ) ) ;
#24218=CARTESIAN_POINT ( 'NONE',  ( 117.0507614775786465, -10.30919188438810075, -12.61870101168855918 ) ) ;
#24221=CARTESIAN_POINT ( 'NONE',  ( 112.6260814775786514, -9.261995988541697145, -16.69588392320189030 ) ) ;
#24223=CARTESIAN_POINT ( 'NONE',  ( 125.7194014775786286, -9.814174330883794539, -12.68911139247586739 ) ) ;
#24228=CARTESIAN_POINT ( 'NONE',  ( 113.1933481442453058, -4.089484607189486809, -7.948022111789456723 ) ) ;
#24230=CARTESIAN_POINT ( 'NONE',  ( 126.2404814775786264, -9.261995988541697145, -16.69588392320189030 ) ) ;
#24233=CARTESIAN_POINT ( 'NONE',  ( 124.3685014775786328, -10.63000616557722466, -14.87417383870573495 ) ) ;
#24234=CARTESIAN_POINT ( 'NONE',  ( 123.6310548109119765, -5.638512984488999180, -18.83840828888717311 ) ) ;
#24236=CARTESIAN_POINT ( 'NONE',  ( 112.2857214775786474, -4.089484607189486809, -7.948022111789456723 ) ) ;
#24240=CARTESIAN_POINT ( 'NONE',  ( 123.7184548109119788, -4.863998795839242995, -13.39321520033831447 ) ) ;
#24241=CARTESIAN_POINT ( 'NONE',  ( 114.1577014775786552, -3.505236298600246325, -18.68346056562440793 ) ) ;
#24243=CARTESIAN_POINT ( 'NONE',  ( 111.8319081442453182, -5.638512984488999180, -18.83840828888717311 ) ) ;
#24247=CARTESIAN_POINT ( 'NONE',  ( 120.6245414775786458, -0.1624402480850797581, -16.17319339645315424 ) ) ;
#24248=CARTESIAN_POINT ( 'NONE',  ( 116.5969481442453031, -9.859900752359374465, -12.68260735090039404 ) ) ;
#24249=CARTESIAN_POINT ( 'NONE',  ( 125.3895814775786448, -7.893985811506177619, -18.51759400769804742 ) ) ;
#24257=CARTESIAN_POINT ( 'NONE',  ( 113.3635281442453504, -0.1624402480850797581, -16.17319339645315424 ) ) ;
#24261=CARTESIAN_POINT ( 'NONE',  ( 120.0005481442453146, -4.153390946401325223, -8.397313243818185668 ) ) ;
#24263=CARTESIAN_POINT ( 'NONE',  ( 114.8384214775786489, -10.15424416112533912, -14.75197769757731336 ) ) ;
#24266=EDGE_LOOP ( 'NONE', ( #13008, #34161, #27813, #25747, #6730 ) ) ;
#24273=CARTESIAN_POINT ( 'NONE',  ( 123.8012348109119642, -9.565557343593413364, -10.61323700422348004 ) ) ;
#24274=CARTESIAN_POINT ( 'NONE',  ( 117.2776681442452968, -4.153390946401325223, -8.397313243818185668 ) ) ;
#24275=CARTESIAN_POINT ( 'NONE',  ( 119.8259526359456260, -1.179503403430467667, -17.05068175419387089 ) ) ;
#24278=CARTESIAN_POINT ( 'NONE',  ( 119.1496481442453046, -6.222761293078241884, -8.102969835052219238 ) ) ;
#24279=CARTESIAN_POINT ( 'NONE',  ( 115.2922348109119781, 0.4262465694468514643, -12.03445270309931736 ) ) ;
#24281=DIRECTION ( 'NONE',  ( 1.000000000000000000, 0.000000000000000000, 0.000000000000000000 ) ) ;
#24283=CARTESIAN_POINT ( 'NONE',  ( 112.3424481442453384, -6.344957434206662583, -7.627207830600332805 ) ) ;
#24284=ORIENTED_EDGE ( 'NONE', *, *, #9401, .F. ) ;
#24285=CARTESIAN_POINT ( 'NONE',  ( 115.1787814775786387, -9.988377603198976828, -10.36322818467138340 ) ) ;
#24286=CARTESIAN_POINT ( 'NONE',  ( 114.1577014775786552, -6.344957434206662583, -7.627207830600333693 ) ) ;
#24288=CARTESIAN_POINT ( 'NONE',  ( 112.9664414775786412, 0.5811942927096154232, -14.16772938898807155 ) ) ;
#24290=CARTESIAN_POINT ( 'NONE',  ( 115.7460481442453357, 0.9020085738987339008, -11.91225656197089222 ) ) ;
#24291=CARTESIAN_POINT ( 'NONE',  ( 123.2339681442453241, -3.505236298600246325, -18.68346056562440793 ) ) ;
#24296=CARTESIAN_POINT ( 'NONE',  ( 118.0718414775786442, -0.8288870151387760510, -10.36305467784173118 ) ) ;
#24298=CARTESIAN_POINT ( 'NONE',  ( 120.5468302440515203, -2.467220198592778413, -17.83387418641524391 ) ) ;
#24300=CARTESIAN_POINT ( 'NONE',  ( 123.1772414775786189, -4.089484607189486809, -7.948022111789456723 ) ) ;
#24301=CARTESIAN_POINT ( 'NONE',  ( 125.8433948109119456, -1.834011780172310813, -8.268836392978581529 ) ) ;
#24302=CARTESIAN_POINT ( 'NONE',  ( 119.9438214775786520, -2.084020599724394796, -8.691656652584146769 ) ) ;
#24304=CARTESIAN_POINT ( 'NONE',  ( 120.1140014775786398, -1.561330072975668504, -17.79121239304076951 ) ) ;
#24305=CARTESIAN_POINT ( 'NONE',  ( 116.7671281442453335, -1.834011780172310813, -8.268836392978581529 ) ) ;
#24308=CARTESIAN_POINT ( 'NONE',  ( 115.4056881442453459, -2.084020599724406786, -8.691656652584148546 ) ) ;
#24309=CARTESIAN_POINT ( 'NONE',  ( 125.4463081442452932, -5.638512984488999180, -18.83840828888717311 ) ) ;
#24310=CARTESIAN_POINT ( 'NONE',  ( 113.4769814775786330, -10.63000616557722466, -14.87417383870573495 ) ) ;
#24311=CARTESIAN_POINT ( 'NONE',  ( 116.8805814775786445, -3.505236298600246325, -18.68346056562440793 ) ) ;
#24312=EDGE_LOOP ( 'NONE', ( #40175, #31415, #8424, #21273 ) ) ;
#24314=CARTESIAN_POINT ( 'NONE',  ( 121.5321681442453183, -0.1624402480850797581, -16.17319339645315424 ) ) ;
#24315=AXIS2_PLACEMENT_3D ( 'NONE', #749, #538, #21512 ) ;
#24316=CARTESIAN_POINT ( 'NONE',  ( 116.0296814775786345, -8.166667518702817929, -8.995218007635861213 ) ) ;
#24319=ORIENTED_EDGE ( 'NONE', *, *, #42051, .T. ) ;
#24321=CARTESIAN_POINT ( 'NONE',  ( 125.4463081442452932, -5.638512984488999180, -18.83840828888717311 ) ) ;
#24323=CARTESIAN_POINT ( 'NONE',  ( 115.2922348109119781, -10.63000616557722466, -14.87417383870573495 ) ) ;
#24324=CARTESIAN_POINT ( 'NONE',  ( 135.9373687278040563, -10.75336585672390299, -14.11528246583558577 ) ) ;
#24325=CARTESIAN_POINT ( 'NONE',  ( 113.4769814775786330, 0.4262465694468514643, -12.03445270309931736 ) ) ;
#24329=CARTESIAN_POINT ( 'NONE',  ( 117.2776681442452968, -5.638512984488999180, -18.83840828888717311 ) ) ;
#24334=CARTESIAN_POINT ( 'NONE',  ( 122.6099748109119929, -0.8288870151387760510, -10.36305467784173118 ) ) ;
#24336=CARTESIAN_POINT ( 'NONE',  ( 125.8433948109119456, -1.834011780172310813, -8.268836392978581529 ) ) ;
#24337=CARTESIAN_POINT ( 'NONE',  ( 120.2841814775786276, 0.9020085738987339008, -11.91225656197089222 ) ) ;
#24339=CARTESIAN_POINT ( 'NONE',  ( 117.4478481442453131, -9.565557343593413364, -10.61323700422348004 ) ) ;
#24340=CARTESIAN_POINT ( 'NONE',  ( 112.0588148109119828, -9.859900752359374465, -12.68260735090039404 ) ) ;
#24343=CARTESIAN_POINT ( 'NONE',  ( 121.8158014775786171, -4.153390946401325223, -8.397313243818185668 ) ) ;
#24344=CARTESIAN_POINT ( 'NONE',  ( 119.0929214775786278, -4.153390946401325223, -8.397313243818185668 ) ) ;
#24348=CARTESIAN_POINT ( 'NONE',  ( 113.8173414775786512, 0.2603800115204892296, -16.42320221600525088 ) ) ;
#24349=CARTESIAN_POINT ( 'NONE',  ( 113.7606148109119886, -1.561330072975668060, -17.79121239304076596 ) ) ;
#24353=CARTESIAN_POINT ( 'NONE',  ( 121.3619881442452879, -4.089484607189486809, -7.948022111789456723 ) ) ;
#24354=CARTESIAN_POINT ( 'NONE',  ( 112.5693548109119888, -10.63000616557722466, -14.87417383870573495 ) ) ;
#24356=CARTESIAN_POINT ( 'NONE',  ( 116.8805814775786445, -3.505236298600246325, -18.68346056562440793 ) ) ;
#24358=CARTESIAN_POINT ( 'NONE',  ( 125.3895814775786448, -7.893985811506177619, -18.51759400769804742 ) ) ;
#24359=CARTESIAN_POINT ( 'NONE',  ( 119.3198281442452924, 0.5811942927096110934, -14.16772938898807510 ) ) ;
#24362=CARTESIAN_POINT ( 'NONE',  ( 112.9664414775786412, -9.859900752359374465, -12.68260735090039404 ) ) ;
#24364=ORIENTED_EDGE ( 'NONE', *, *, #23099, .F. ) ;
#24365=CARTESIAN_POINT ( 'NONE',  ( 116.7671281442453335, -1.834011780172310813, -8.268836392978581529 ) ) ;
#24367=CARTESIAN_POINT ( 'NONE',  ( 116.0296814775786345, -8.166667518702817929, -8.995218007635861213 ) ) ;
#24375=CARTESIAN_POINT ( 'NONE',  ( 119.8870948109119752, -0.8288870151387760510, -10.36305467784173118 ) ) ;
#24377=CARTESIAN_POINT ( 'NONE',  ( 119.2631014775786298, -9.565557343593413364, -10.61323700422348004 ) ) ;
#24380=CARTESIAN_POINT ( 'NONE',  ( 120.7947214775786193, -0.8288870151387760510, -10.36305467784173118 ) ) ;
#24381=CARTESIAN_POINT ( 'NONE',  ( 111.8319081442453182, -5.638512984488999180, -18.83840828888717311 ) ) ;
#24382=CARTESIAN_POINT ( 'NONE',  ( 116.3700414775786527, -5.638512984488999180, -18.83840828888717311 ) ) ;
#24383=AXIS2_PLACEMENT_3D ( 'NONE', #31594, #14724, #32039 ) ;
#24384=CARTESIAN_POINT ( 'NONE',  ( 117.0507614775786465, 0.1319031606808879209, -14.10382304977623669 ) ) ;
#24385=ORIENTED_EDGE ( 'NONE', *, *, #40070, .F. ) ;
#24386=CARTESIAN_POINT ( 'NONE',  ( 116.0296814775786345, -8.166667518702817929, -8.995218007635861213 ) ) ;
#24391=CARTESIAN_POINT ( 'NONE',  ( 122.3263414775786373, -6.344957434206665248, -7.627207830600338134 ) ) ;
#24392=VERTEX_POINT ( 'NONE', #27519 ) ;
#24393=CARTESIAN_POINT ( 'NONE',  ( 127.0915067942438839, -8.936375571992021705, -9.791582253908270417 ) ) ;
#24394=CARTESIAN_POINT ( 'NONE',  ( 119.2631014775786298, -9.565557343593413364, -10.61323700422348004 ) ) ;
#24397=CARTESIAN_POINT ( 'NONE',  ( 123.2906948109119867, -8.166667518702819706, -8.995218007635861213 ) ) ;
#24402=CARTESIAN_POINT ( 'NONE',  ( 112.7395348109119766, -5.638512984488999180, -18.83840828888717311 ) ) ;
#24403=CARTESIAN_POINT ( 'NONE',  ( 123.5176014775786228, -9.261995988541697145, -16.69588392320189030 ) ) ;
#24404=CARTESIAN_POINT ( 'NONE',  ( 118.4122014775786340, -9.859900752359374465, -12.68260735090039404 ) ) ;
#24406=CARTESIAN_POINT ( 'NONE',  ( 120.0572748109119772, -3.383040157471821630, -19.15922257007629170 ) ) ;
#24408=CARTESIAN_POINT ( 'NONE',  ( 122.3830681442452857, -1.833838273342659697, -17.42832698103878286 ) ) ;
#24411=CARTESIAN_POINT ( 'NONE',  ( 118.4122014775786340, 0.5811942927096110934, -14.16772938898807510 ) ) ;
#24412=CARTESIAN_POINT ( 'NONE',  ( 135.7778351054865595, -8.526057075361061166, -18.10094121367604814 ) ) ;
#24413=ORIENTED_EDGE ( 'NONE', *, *, #13888, .T. ) ;
#24416=CARTESIAN_POINT ( 'NONE',  ( 120.9649014775786355, -3.383040157471821630, -19.15922257007629170 ) ) ;
#24419=CARTESIAN_POINT ( 'NONE',  ( 121.2485348109119769, -8.899110576539710493, -16.42337572283490132 ) ) ;
#24422=CARTESIAN_POINT ( 'NONE',  ( 114.1577014775786552, -6.344957434206662583, -7.627207830600332805 ) ) ;
#24423=CARTESIAN_POINT ( 'NONE',  ( 125.1059481442452750, -1.833838273342660141, -17.42832698103878286 ) ) ;
#24425=CARTESIAN_POINT ( 'NONE',  ( 121.9859814775786333, 0.2603800115204892296, -16.42320221600525088 ) ) ;
#24428=CARTESIAN_POINT ( 'NONE',  ( 124.7655881442452852, 0.5811942927096110934, -14.16772938898807510 ) ) ;
#24429=CARTESIAN_POINT ( 'NONE',  ( 120.0572748109119772, -3.383040157471821630, -19.15922257007629170 ) ) ;
#24430=CARTESIAN_POINT ( 'NONE',  ( 122.8368814775786291, -7.894159318335828068, -9.358103419637847864 ) ) ;
#24431=CARTESIAN_POINT ( 'NONE',  ( 121.1350814775786233, -9.859900752359378018, -12.68260735090039759 ) ) ;
#24434=CARTESIAN_POINT ( 'NONE',  ( 115.9162281442453235, -4.089484607189486809, -7.948022111789456723 ) ) ;
#24436=ORIENTED_EDGE ( 'NONE', *, *, #19165, .T. ) ;
#24437=CARTESIAN_POINT ( 'NONE',  ( 125.4924948109119924, -4.159894987976798575, -8.443039665293765594 ) ) ;
#24441=CARTESIAN_POINT ( 'NONE',  ( 124.9819548109120291, -7.618532446444632455, -18.05174138884769874 ) ) ;
#24442=CARTESIAN_POINT ( 'NONE',  ( 111.9453614775786434, -1.561330072975668060, -17.79121239304076596 ) ) ;
#24444=CARTESIAN_POINT ( 'NONE',  ( 112.6260814775786514, -0.8288870151387760510, -10.36305467784173118 ) ) ;
#24447=CARTESIAN_POINT ( 'NONE',  ( 122.6099748109119929, -9.261995988541697145, -16.69588392320189030 ) ) ;
#24448=CARTESIAN_POINT ( 'NONE',  ( 123.5176014775786228, -9.261995988541697145, -16.69588392320189030 ) ) ;
#24450=CARTESIAN_POINT ( 'NONE',  ( 113.4769814775786330, -10.63000616557722466, -14.87417383870573495 ) ) ;
#24455=CARTESIAN_POINT ( 'NONE',  ( 115.6893214775786447, -9.859900752359374465, -12.68260735090039404 ) ) ;
#24456=CARTESIAN_POINT ( 'NONE',  ( 126.0703014775786102, -0.1624402480850797581, -16.17319339645315424 ) ) ;
#24459=CARTESIAN_POINT ( 'NONE',  ( 121.9859814775786333, -9.565557343593413364, -10.61323700422348004 ) ) ;
#24460=CARTESIAN_POINT ( 'NONE',  ( 119.4900081442453086, -7.643976991954077427, -18.09477374809248928 ) ) ;
#24461=CARTESIAN_POINT ( 'NONE',  ( 125.7866681442452688, -0.4660016031367893996, -10.09054647747474043 ) ) ;
#24462=ORIENTED_EDGE ( 'NONE', *, *, #3633, .F. ) ;
#24464=CARTESIAN_POINT ( 'NONE',  ( 125.0492214775786266, -3.505236298600246325, -18.68346056562440793 ) ) ;
#24466=CARTESIAN_POINT ( 'NONE',  ( 125.4463081442452932, -4.153390946401325223, -8.397313243818185668 ) ) ;
#24467=CARTESIAN_POINT ( 'NONE',  ( 113.9307948109119764, -10.15424416112533912, -14.75197769757731336 ) ) ;
#24474=CARTESIAN_POINT ( 'NONE',  ( 117.1074881442453233, 0.4262465694468514643, -12.03445270309931736 ) ) ;
#24475=CARTESIAN_POINT ( 'NONE',  ( 113.4202548109119846, 0.1319031606808879209, -14.10382304977623669 ) ) ;
#24481=CARTESIAN_POINT ( 'NONE',  ( 112.1599289911621327, -8.918981166868261923, -16.37818325645714168 ) ) ;
#24485=CARTESIAN_POINT ( 'NONE',  ( 113.1933481442453058, -4.089484607189486809, -7.948022111789456723 ) ) ;
#24487=CARTESIAN_POINT ( 'NONE',  ( 122.0427081442452817, -9.859900752359378018, -12.68260735090039759 ) ) ;
#24488=CARTESIAN_POINT ( 'NONE',  ( 116.1998614775786507, 0.4262465694468514643, -12.03445270309931736 ) ) ;
#24489=CARTESIAN_POINT ( 'NONE',  ( 113.9875214775786532, -8.899110576539717599, -16.42337572283489067 ) ) ;
#24494=CARTESIAN_POINT ( 'NONE',  ( 117.5613014775786525, -10.15424416112533912, -14.75197769757731336 ) ) ;
#24495=CARTESIAN_POINT ( 'NONE',  ( 125.2194014775786286, 0.1319031606808879209, -14.10382304977623669 ) ) ;
#24499=CARTESIAN_POINT ( 'NONE',  ( 116.0296814775786345, -8.166667518702817929, -8.995218007635861213 ) ) ;
#24501=CARTESIAN_POINT ( 'NONE',  ( 113.1366214775786432, -1.834011780172310813, -8.268836392978581529 ) ) ;
#24504=CARTESIAN_POINT ( 'NONE',  ( 126.1270281442452870, 0.1319031606808879209, -14.10382304977623669 ) ) ;
#24505=CARTESIAN_POINT ( 'NONE',  ( 112.2857214775786474, -4.089484607189486809, -7.948022111789456723 ) ) ;
#24506=CARTESIAN_POINT ( 'NONE',  ( 122.3263414775786373, -3.505236298600246325, -18.68346056562440793 ) ) ;
#24512=CARTESIAN_POINT ( 'NONE',  ( 118.4122014775786340, -9.859900752359374465, -12.68260735090039404 ) ) ;
#24514=CARTESIAN_POINT ( 'NONE',  ( 122.8560864091100768, -0.9924539043446216624, -17.29976612834909133 ) ) ;
#24517=CARTESIAN_POINT ( 'NONE',  ( 124.4252281442452812, -9.261995988541697145, -16.69588392320189030 ) ) ;
#24518=CARTESIAN_POINT ( 'NONE',  ( 120.0947965460471920, -2.191907684172563986, -18.20049396185734025 ) ) ;
#24519=CARTESIAN_POINT ( 'NONE',  ( 119.6034614775786196, -6.344957434206665248, -7.627207830600338134 ) ) ;
#24520=CARTESIAN_POINT ( 'NONE',  ( 115.5191414775786569, -3.383040157471821630, -19.15922257007629170 ) ) ;
#24523=CARTESIAN_POINT ( 'NONE',  ( 116.3700414775786527, -4.153390946401321671, -8.397313243818183892 ) ) ;
#24524=CARTESIAN_POINT ( 'NONE',  ( 122.7234281442452755, -5.638512984488999180, -18.83840828888717311 ) ) ;
#24525=CARTESIAN_POINT ( 'NONE',  ( 118.8660148109119774, -10.30919188438810075, -12.61870101168855918 ) ) ;
#24527=CARTESIAN_POINT ( 'NONE',  ( 115.8595014775786609, -7.643976991954077427, -18.09477374809248928 ) ) ;
#24529=CARTESIAN_POINT ( 'NONE',  ( 121.6456214775786293, 0.4262465694468514643, -12.03445270309931736 ) ) ;
#24531=CARTESIAN_POINT ( 'NONE',  ( 117.2776681442452968, -5.638512984488999180, -18.83840828888717311 ) ) ;
#24532=CARTESIAN_POINT ( 'NONE',  ( 136.2190063926907726, 0.5346461494345294829, -15.66526563388532090 ) ) ;
#24535=CARTESIAN_POINT ( 'NONE',  ( 124.8790414775786246, -0.4660016031367893996, -10.09054647747474043 ) ) ;
#24538=CARTESIAN_POINT ( 'NONE',  ( 115.1220548109119761, -8.166667518702817929, -8.995218007635861213 ) ) ;
#24539=CARTESIAN_POINT ( 'NONE',  ( 135.3184548109119874, -10.81584935473217080, -14.15181583611863303 ) ) ;
#24540=CARTESIAN_POINT ( 'NONE',  ( 113.3635281442453504, -0.1624402480850797581, -16.17319339645315424 ) ) ;
#24543=CARTESIAN_POINT ( 'NONE',  ( 115.5167787682627960, -1.040089454026966287, -17.23633227186632766 ) ) ;
#24546=CARTESIAN_POINT ( 'NONE',  ( 117.5045748109119756, 0.5811942927096110934, -14.16772938898807510 ) ) ;
#24550=CARTESIAN_POINT ( 'NONE',  ( 124.2550481442452792, -0.1624402480850797581, -16.17319339645315424 ) ) ;
#24551=CARTESIAN_POINT ( 'NONE',  ( 117.8449348109119938, -1.833838273342659253, -17.42832698103878286 ) ) ;
#24552=ORIENTED_EDGE ( 'NONE', *, *, #42051, .F. ) ;
#24553=CARTESIAN_POINT ( 'NONE',  ( 136.2267163767933766, -9.456939161313274056, -9.757884007028398088 ) ) ;
#24555=CARTESIAN_POINT ( 'NONE',  ( 123.6310548109119765, -5.638512984488999180, -18.83840828888717311 ) ) ;
#24557=CARTESIAN_POINT ( 'NONE',  ( 116.8238548109119819, -5.574606645277164318, -18.38911715685844683 ) ) ;
#24558=CARTESIAN_POINT ( 'NONE',  ( 113.9307948109119764, -10.15424416112533912, -14.75197769757731336 ) ) ;
#24561=CARTESIAN_POINT ( 'NONE',  ( 120.5678148109119832, -1.833838273342659253, -17.42832698103878286 ) ) ;
#24562=CARTESIAN_POINT ( 'NONE',  ( 119.3198281442452924, -9.859900752359374465, -12.68260735090039404 ) ) ;
#24563=CARTESIAN_POINT ( 'NONE',  ( 138.2184548109119930, -4.863998795839242995, -13.39321520033831447 ) ) ;
#24569=CARTESIAN_POINT ( 'NONE',  ( 117.2209414775786485, -7.893985811506177619, -18.51759400769804742 ) ) ;
#24570=CARTESIAN_POINT ( 'NONE',  ( 114.0442481442453300, -1.834011780172310813, -8.268836392978581529 ) ) ;
#24575=CARTESIAN_POINT ( 'NONE',  ( 121.3052614775786111, -1.834011780172310813, -8.268836392978581529 ) ) ;
#24576=CARTESIAN_POINT ( 'NONE',  ( 126.5241148109119393, -9.565557343593413364, -10.61323700422348004 ) ) ;
#24577=CARTESIAN_POINT ( 'NONE',  ( 123.3474214775786209, -0.1624402480850797581, -16.17319339645315424 ) ) ;
#24578=CARTESIAN_POINT ( 'NONE',  ( 126.0703014775786102, -9.988377603198980381, -10.36322818467138518 ) ) ;
#24579=CARTESIAN_POINT ( 'NONE',  ( 116.4834948109119779, -1.561330072975668504, -17.79121239304076951 ) ) ;
#24582=CARTESIAN_POINT ( 'NONE',  ( 117.2209414775786485, -2.084020599724406786, -8.691656652584148546 ) ) ;
#24585=CARTESIAN_POINT ( 'NONE',  ( 121.4187148109119789, -6.344957434206665248, -7.627207830600338134 ) ) ;
#24588=CARTESIAN_POINT ( 'NONE',  ( 117.3911214775786505, -1.561330072975668504, -17.79121239304076951 ) ) ;
#24591=CARTESIAN_POINT ( 'NONE',  ( 125.8433948109119456, -1.834011780172310813, -8.268836392978581529 ) ) ;
#24592=AXIS2_PLACEMENT_3D ( 'NONE', #41151, #9912, #38366 ) ;
#24594=CARTESIAN_POINT ( 'NONE',  ( 115.9162281442453235, -5.574606645277164318, -18.38911715685844683 ) ) ;
#24596=CARTESIAN_POINT ( 'NONE',  ( 120.0005481442453146, -4.153390946401325223, -8.397313243818185668 ) ) ;
#24598=CARTESIAN_POINT ( 'NONE',  ( 119.8303681442453126, 0.4262465694468514643, -12.03445270309931736 ) ) ;
#24601=CARTESIAN_POINT ( 'NONE',  ( 117.6180281442453150, -8.899110576539710493, -16.42337572283490132 ) ) ;
#24603=CARTESIAN_POINT ( 'NONE',  ( 117.6180281442453150, -0.4660016031367893996, -10.09054647747474043 ) ) ;
#24604=CARTESIAN_POINT ( 'NONE',  ( 138.2184548109119930, 0.6402711692277546218, -15.78131322003127579 ) ) ;
#24605=CARTESIAN_POINT ( 'NONE',  ( 120.1707281442453166, -9.565557343593413364, -10.61323700422348004 ) ) ;
#24607=CARTESIAN_POINT ( 'NONE',  ( 115.5758681442453053, -1.561330072975668060, -17.79121239304076951 ) ) ;
#24612=CARTESIAN_POINT ( 'NONE',  ( 124.1983214775786166, -8.166667518702819706, -8.995218007635861213 ) ) ;
#24615=CARTESIAN_POINT ( 'NONE',  ( 117.2776681442452968, -4.153390946401321671, -8.397313243818183892 ) ) ;
#24616=CARTESIAN_POINT ( 'NONE',  ( 116.4160804811916989, -3.807985514183284348, -19.09877912889400520 ) ) ;
#24622=CARTESIAN_POINT ( 'NONE',  ( 116.0296814775786345, -8.166667518702817929, -8.995218007635861213 ) ) ;
#24623=CARTESIAN_POINT ( 'NONE',  ( 124.7655881442452852, -9.859900752359378018, -12.68260735090039759 ) ) ;
#24624=CARTESIAN_POINT ( 'NONE',  ( 124.7655881442452852, 0.5811942927096110934, -14.16772938898807510 ) ) ;
#24625=CARTESIAN_POINT ( 'NONE',  ( 116.1431348109119881, 0.1319031606808879209, -14.10382304977623669 ) ) ;
#24628=CARTESIAN_POINT ( 'NONE',  ( 120.1707281442453166, 0.2603800115204892296, -16.42320221600525088 ) ) ;
#24632=CARTESIAN_POINT ( 'NONE',  ( 121.7590748109119687, -2.084020599724406786, -8.691656652584148546 ) ) ;
#24635=CARTESIAN_POINT ( 'NONE',  ( 118.2420214775786320, -3.383040157471821630, -19.15922257007629170 ) ) ;
#24636=CARTESIAN_POINT ( 'NONE',  ( 124.8223148109119762, -10.15424416112533912, -14.75197769757731336 ) ) ;
#24637=ORIENTED_EDGE ( 'NONE', *, *, #12793, .F. ) ;
#24638=CARTESIAN_POINT ( 'NONE',  ( 112.3424481442453384, -6.344957434206662583, -7.627207830600332805 ) ) ;
#24639=CARTESIAN_POINT ( 'NONE',  ( 123.4041481442452834, -10.30919188438810075, -12.61870101168855918 ) ) ;
#24641=CARTESIAN_POINT ( 'NONE',  ( 119.2631014775786298, -9.565557343593413364, -10.61323700422348004 ) ) ;
#24644=CARTESIAN_POINT ( 'NONE',  ( 115.9729548109119861, -6.344957434206662583, -7.627207830600332805 ) ) ;
#24645=CARTESIAN_POINT ( 'NONE',  ( 125.1626748109119802, -0.1624402480850797581, -16.17319339645315424 ) ) ;
#24647=CARTESIAN_POINT ( 'NONE',  ( 124.3685014775786328, -10.63000616557722466, -14.87417383870573495 ) ) ;
#24651=CARTESIAN_POINT ( 'NONE',  ( 122.5532481442453019, -10.63000616557722466, -14.87417383870573495 ) ) ;
#24652=CARTESIAN_POINT ( 'NONE',  ( 123.3474214775786209, -9.988377603198976828, -10.36322818467138340 ) ) ;
#24653=CARTESIAN_POINT ( 'NONE',  ( 121.9292548109119849, -7.894159318335828068, -9.358103419637847864 ) ) ;
#24654=CARTESIAN_POINT ( 'NONE',  ( 119.6034614775786196, -3.505236298600246325, -18.68346056562440793 ) ) ;
#24655=CARTESIAN_POINT ( 'NONE',  ( 115.0086014775786509, -4.089484607189486809, -7.948022111789456723 ) ) ;
#24657=CARTESIAN_POINT ( 'NONE',  ( 124.9357681442453156, -7.643976991953167044, -18.09477374809303285 ) ) ;
#24661=CARTESIAN_POINT ( 'NONE',  ( 125.2088614775786510, -0.2054726073298613620, -16.14774885094370660 ) ) ;
#24662=CARTESIAN_POINT ( 'NONE',  ( 112.1722681442453222, -0.4660016031367893996, -10.09054647747474043 ) ) ;
#24664=CARTESIAN_POINT ( 'NONE',  ( 113.0231681442453180, -10.15424416112533912, -14.75197769757731336 ) ) ;
#24667=CARTESIAN_POINT ( 'NONE',  ( 121.9859814775786333, 0.2603800115204892296, -16.42320221600525088 ) ) ;
#24668=CARTESIAN_POINT ( 'NONE',  ( 125.1059481442452750, -8.166667518702819706, -8.995218007635861213 ) ) ;
#24670=CARTESIAN_POINT ( 'NONE',  ( 114.6115148109119986, -3.383040157471821630, -19.15922257007629170 ) ) ;
#24674=CARTESIAN_POINT ( 'NONE',  ( 127.3434826497568935, -7.118825987476567363, -8.305226122375637843 ) ) ;
#24675=CARTESIAN_POINT ( 'NONE',  ( 114.5547881442453217, -4.153390946401321671, -8.397313243818183892 ) ) ;
#24676=CARTESIAN_POINT ( 'NONE',  ( 112.5693548109119888, -10.63000616557722466, -14.87417383870573495 ) ) ;
#24679=CARTESIAN_POINT ( 'NONE',  ( 122.3830681442452857, -1.833838273342659697, -17.42832698103878286 ) ) ;
#24681=CARTESIAN_POINT ( 'NONE',  ( 119.6034614775786196, -3.505236298600246325, -18.68346056562440793 ) ) ;
#24682=CARTESIAN_POINT ( 'NONE',  ( 112.3991748109119868, -1.833838273342658809, -17.42832698103878286 ) ) ;
#24684=CARTESIAN_POINT ( 'NONE',  ( 124.5386814775786206, -4.153390946401325223, -8.397313243818185668 ) ) ;
#24685=CARTESIAN_POINT ( 'NONE',  ( 125.6732148109119862, -9.859900752359378018, -12.68260735090039759 ) ) ;
#24686=CARTESIAN_POINT ( 'NONE',  ( 114.2711548109119803, -0.1624402480850797581, -16.17319339645315424 ) ) ;
#24691=ORIENTED_EDGE ( 'NONE', *, *, #31852, .F. ) ;
#24692=CARTESIAN_POINT ( 'NONE',  ( 119.4332814775786318, -8.899110576539710493, -16.42337572283490132 ) ) ;
#24693=CARTESIAN_POINT ( 'NONE',  ( 114.4980614775786734, -2.084020599724406786, -8.691656652584148546 ) ) ;
#24694=( BOUNDED_SURFACE ( )  B_SPLINE_SURFACE ( 1, 2, ( 
 ( #17011, #17230, #20203, #40955, #43915, #44600, #3084, #30902, #2624, #13582, #27492, #30227, #33855, #16557, #6512, #41410, #13134, #13363, #40496, #44149, #27038, #9710, #27268, #12914, #26810, #9479, #30452, #37741, #10166, #41181, #23622, #9942, #23855, #9257, #24073, #37966, #23166, #6742, #37277, #37046, #34528, #3306, #5817, #33621, #2397, #6044, #19967, #44372, #14245, #14694, #17889, #21308, #21532, #771, #332, #38850, #31563, #28608, #3744, #34957, #41849, #4196, #3968, #28377, #39084, #31787, #35191, #4425, #11052, #32007, #38397, #21759, #21080, #42517, #31120, #20867, #24726, #7619, #18114, #45044, #7391, #28161, #13804, #559, #35420, #11277, #17667, #25185, #7853, #3526, #42071, #10829, #35651, #27716, #38614, #14469, #41631, #17444, #42290, #24955, #10387, #31337, #112, #14025, #24296, #38183, #6960, #34745, #27939, #10609, #24512, #7169, #29717, #32679, #8303, #15818, #1448, #8081, #39757, #1669, #1005, #39981, #11953, #36321, #25851, #40212, #22876, #15144, #25638, #25411, #43189, #8527, #15592, #43408, #36100, #32893, #29050, #18789, #22429, #21983, #11507, #8978, #42742, #8745, #14921, #35872, #5091, #19007, #29495, #12176, #28831, #26077, #22652, #36548, #5322, #19238, #4643, #18341, #32234, #18565, #33121, #1889, #43630, #12404, #36770, #26304, #39311, #42958, #32456, #1231, #11725, #39542, #22205, #29273, #4872, #15369, #13309, #34262, #20375, #5995, #23336, #26533, #23114, #2806, #43864, #24024, #19918, #40443, #26983, #44326, #40903, #6466, #30179, #9204, #27216, #2346, #19458, #23577, #33341, #33569, #3037, #16959, #36991, #33803, #16504, #30404, #12861, #26762, #37459, #30853, #5761, #13084, #19682, #44776, #34037, #13535, #27442, #12636, #16276, #9657, #44097, #40671, #41364, #9423, #37221, #6231, #16732, #2575, #20153, #30629, #44545, #41134, #10121, #9893, #5540, #23803, #37693, #2114, #16043, #29950, #31070, #42464, #20817, #4142, #10559, #24456, #283, #27666, #7569, #27887, #35367, #17838, #31287, #21482, #31511, #7340, #11228 ),
 ( #10780, #14416, #24243, #31734, #31954, #37913, #28326, #20602, #6690, #18063, #34477, #3919, #3483, #44998, #3256, #24676, #61, #17181, #38136, #719, #13974, #3697, #42238, #21034, #504, #14641, #28558, #38347, #7124, #13757, #10339, #35138, #41580, #6907, #34907, #34695, #14193, #28111, #42015, #38797, #17399, #41801, #11003, #17618, #38563, #21258, #24903, #8020, #8693, #39933, #28780, #39484, #36048, #4816, #32406, #1176, #43129, #36499, #11455, #18737, #39255, #5268, #8474, #22598, #33063, #18286, #42687, #32630, #32182, #25361, #19185, #21927, #35820, #15311, #22376, #4593, #22155, #25800, #1396, #29220, #1837, #18515, #15766, #43356, #36273, #43580, #11672, #18955, #953, #29667, #15091, #25135, #42910, #25581, #11899, #14870, #39029, #29002, #7800, #5041, #8248, #21709, #39710, #32846, #35596, #12125, #1614, #4366, #15536, #29440, #26027, #12578, #30347, #33980, #43812, #6174, #6409, #16904, #2748, #40161, #12350, #9835, #30796, #23517, #23054, #19405, #26248, #44270, #19628, #22824, #26483, #20317, #5711, #8922, #36715, #29895, #37163, #37405, #20095, #19862, #34201, #16672, #5940, #36940, #30568, #40846, #13027, #33512, #44487, #23745, #5485, #13254, #2293, #33292, #2067, #26925, #16221, #15991, #40387, #2975, #30126, #9148, #44039, #12803, #33751, #27156, #41079, #2520, #26703, #37636, #16447, #40614, #9372, #9601, #23281, #24185, #31674, #10502, #21200, #27827, #7284, #28273, #14360, #6, #17344, #20541, #17125, #41959, #37853, #18002, #13916, #34420, #20981, #38292, #34854, #444, #38077, #3201, #35078, #41523, #13480, #17558, #27383, #27609, #42182, #10942, #31014, #41738, #24403, #7070, #6855, #20762, #31453, #24845, #44944, #3640, #13701, #38737, #28051, #7507, #21422, #6627, #10280, #222, #34641, #3427, #35306, #31234, #14135, #10724, #24624, #38507, #3859, #17781, #4078, #44720, #41305, #10065, #23967, #4985, #43073, #5208, #18461, #25749, #25074, #36441, #14811, #43301, #4537, #32351, #39427, #21646, #1560, #21872, #29388, #11842, #25303 ) ),
 .UNSPECIFIED., .F., .F., .T. ) 
 B_SPLINE_SURFACE_WITH_KNOTS ( ( 2, 2 ),
 ( 3, 2, 2, 2, 2, 2, 2, 2, 2, 2, 2, 2, 2, 2, 2, 2, 2, 2, 2, 2, 2, 2, 2, 2, 2, 2, 2, 2, 2, 2, 2, 2, 2, 2, 2, 2, 2, 2, 2, 2, 2, 2, 2, 2, 2, 2, 2, 2, 2, 2, 2, 2, 2, 2, 2, 2, 2, 2, 2, 2, 2, 2, 2, 2, 2, 2, 2, 2, 2, 2, 2, 2, 2, 2, 2, 2, 2, 2, 2, 2, 2, 2, 2, 2, 2, 2, 2, 2, 2, 2, 2, 2, 2, 2, 2, 2, 2, 2, 2, 2, 2, 2, 2, 2, 2, 2, 2, 2, 2, 2, 2, 2, 2, 2, 2, 2, 2, 2, 2, 2, 2, 2, 2, 2, 2, 2, 2, 2, 3 ),
 ( 0.000000000000000000, 1.000000000000000000 ),
 ( 0.000000000000000000, 0.007812500000000000000, 0.01562500000000000000, 0.02343750000000000000, 0.03125000000000000000, 0.03906250000000000000, 0.04687500000000000000, 0.05468750000000000000, 0.06250000000000000000, 0.07031250000000000000, 0.07812500000000000000, 0.08593750000000000000, 0.09375000000000000000, 0.1015625000000000000, 0.1093750000000000000, 0.1171875000000000000, 0.1250000000000000000, 0.1328125000000000000, 0.1406250000000000000, 0.1484375000000000000, 0.1562500000000000000, 0.1640625000000000000, 0.1718750000000000000, 0.1796875000000000000, 0.1875000000000000000, 0.1953125000000000000, 0.2031250000000000000, 0.2109375000000000000, 0.2187500000000000000, 0.2265625000000000000, 0.2343750000000000000, 0.2421875000000000000, 0.2500000000000000000, 0.2578125000000000000, 0.2656250000000000000, 0.2734375000000000000, 0.2812500000000000000, 0.2890625000000000000, 0.2968750000000000000, 0.3046875000000000000, 0.3125000000000000000, 0.3203125000000000000, 0.3281250000000000000, 0.3359375000000000000, 0.3437500000000000000, 0.3515625000000000000, 0.3593750000000000000, 0.3671875000000000000, 0.3750000000000000000, 0.3828125000000000000, 0.3906250000000000000, 0.3984375000000000000, 0.4062500000000000000, 0.4140625000000000000, 0.4218750000000000000, 0.4296875000000000000, 0.4375000000000000000, 0.4453125000000000000, 0.4531250000000000000, 0.4609375000000000000, 0.4687500000000000000, 0.4765625000000000000, 0.4843750000000000000, 0.4921875000000000000, 0.5000000000000000000, 0.5078125000000000000, 0.5156250000000000000, 0.5234375000000000000, 0.5312500000000000000, 0.5390625000000000000, 0.5468750000000000000, 0.5546875000000000000, 0.5625000000000000000, 0.5703125000000000000, 0.5781250000000000000, 0.5859375000000000000, 0.5937500000000000000, 0.6015625000000000000, 0.6093750000000000000, 0.6171875000000000000, 0.6250000000000000000, 0.6328125000000000000, 0.6406250000000000000, 0.6484375000000000000, 0.6562500000000000000, 0.6640625000000000000, 0.6718750000000000000, 0.6796875000000000000, 0.6875000000000000000, 0.6953125000000000000, 0.7031250000000000000, 0.7109375000000000000, 0.7187500000000000000, 0.7265625000000000000, 0.7343750000000000000, 0.7421875000000000000, 0.7500000000000000000, 0.7578125000000000000, 0.7656250000000000000, 0.7734375000000000000, 0.7812500000000000000, 0.7890625000000000000, 0.7968750000000000000, 0.8046875000000000000, 0.8125000000000000000, 0.8203125000000000000, 0.8281250000000000000, 0.8359375000000000000, 0.8437500000000000000, 0.8515625000000000000, 0.8593750000000000000, 0.8671875000000000000, 0.8750000000000000000, 0.8828125000000000000, 0.8906250000000000000, 0.8984375000000000000, 0.9062500000000000000, 0.9140625000000000000, 0.9218750000000000000, 0.9296875000000000000, 0.9375000000000000000, 0.9453125000000000000, 0.9531250000000000000, 0.9609375000000000000, 0.9687500000000000000, 0.9765625000000000000, 0.9843750000000000000, 0.9921875000000000000, 1.000000000000000000 ),
 .UNSPECIFIED. ) 
 GEOMETRIC_REPRESENTATION_ITEM ( )  RATIONAL_B_SPLINE_SURFACE ( (
 ( 1.000000000000000000, 0.9238795325112869605, 1.000000000000000000, 0.9238795325112869605, 1.000000000000000000, 0.9238795325112869605, 1.000000000000000000, 0.9238795325112869605, 1.000000000000000000, 0.9238795325112869605, 1.000000000000000000, 0.9238795325112869605, 1.000000000000000000, 0.9238795325112869605, 1.000000000000000000, 0.9238795325112869605, 1.000000000000000000, 0.9238795325112869605, 1.000000000000000000, 0.9238795325112869605, 1.000000000000000000, 0.9238795325112869605, 1.000000000000000000, 0.9238795325112869605, 1.000000000000000000, 0.9238795325112869605, 1.000000000000000000, 0.9238795325112869605, 1.000000000000000000, 0.9238795325112869605, 1.000000000000000000, 0.9238795325112869605, 1.000000000000000000, 0.9238795325112869605, 1.000000000000000000, 0.9238795325112869605, 1.000000000000000000, 0.9238795325112869605, 1.000000000000000000, 0.9238795325112869605, 1.000000000000000000, 0.9238795325112869605, 1.000000000000000000, 0.9238795325112869605, 1.000000000000000000, 0.9238795325112869605, 1.000000000000000000, 0.9238795325112869605, 1.000000000000000000, 0.9238795325112869605, 1.000000000000000000, 0.9238795325112869605, 1.000000000000000000, 0.9238795325112869605, 1.000000000000000000, 0.9238795325112869605, 1.000000000000000000, 0.9238795325112869605, 1.000000000000000000, 0.9238795325112869605, 1.000000000000000000, 0.9238795325112869605, 1.000000000000000000, 0.9238795325112869605, 1.000000000000000000, 0.9238795325112869605, 1.000000000000000000, 0.9238795325112869605, 1.000000000000000000, 0.9238795325112869605, 1.000000000000000000, 0.9238795325112869605, 1.000000000000000000, 0.9238795325112869605, 1.000000000000000000, 0.9238795325112869605, 1.000000000000000000, 0.9238795325112869605, 1.000000000000000000, 0.9238795325112869605, 1.000000000000000000, 0.9238795325112869605, 1.000000000000000000, 0.9238795325112869605, 1.000000000000000000, 0.9238795325112869605, 1.000000000000000000, 0.9238795325112869605, 1.000000000000000000, 0.9238795325112869605, 1.000000000000000000, 0.9238795325112869605, 1.000000000000000000, 0.9238795325112869605, 1.000000000000000000, 0.9238795325112869605, 1.000000000000000000, 0.9238795325112869605, 1.000000000000000000, 0.9238795325112869605, 1.000000000000000000, 0.9238795325112869605, 1.000000000000000000, 0.9238795325112869605, 1.000000000000000000, 0.9238795325112869605, 1.000000000000000000, 0.9238795325112869605, 1.000000000000000000, 0.9238795325112869605, 1.000000000000000000, 0.9238795325112869605, 1.000000000000000000, 0.9238795325112869605, 1.000000000000000000, 0.9238795325112869605, 1.000000000000000000, 0.9238795325112869605, 1.000000000000000000, 0.9238795325112869605, 1.000000000000000000, 0.9238795325112869605, 1.000000000000000000, 0.9238795325112869605, 1.000000000000000000, 0.9238795325112869605, 1.000000000000000000, 0.9238795325112869605, 1.000000000000000000, 0.9238795325112869605, 1.000000000000000000, 0.9238795325112869605, 1.000000000000000000, 0.9238795325112869605, 1.000000000000000000, 0.9238795325112869605, 1.000000000000000000, 0.9238795325112869605, 1.000000000000000000, 0.9238795325112869605, 1.000000000000000000, 0.9238795325112869605, 1.000000000000000000, 0.9238795325112869605, 1.000000000000000000, 0.9238795325112869605, 1.000000000000000000, 0.9238795325112869605, 1.000000000000000000, 0.9238795325112869605, 1.000000000000000000, 0.9238795325112869605, 1.000000000000000000, 0.9238795325112869605, 1.000000000000000000, 0.9238795325112869605, 1.000000000000000000, 0.9238795325112869605, 1.000000000000000000, 0.9238795325112869605, 1.000000000000000000, 0.9238795325112869605, 1.000000000000000000, 0.9238795325112869605, 1.000000000000000000, 0.9238795325112869605, 1.000000000000000000, 0.9238795325112869605, 1.000000000000000000, 0.9238795325112869605, 1.000000000000000000, 0.9238795325112869605, 1.000000000000000000, 0.9238795325112869605, 1.000000000000000000, 0.9238795325112869605, 1.000000000000000000, 0.9238795325112869605, 1.000000000000000000, 0.9238795325112869605, 1.000000000000000000, 0.9238795325112869605, 1.000000000000000000, 0.9238795325112869605, 1.000000000000000000, 0.9238795325112869605, 1.000000000000000000, 0.9238795325112869605, 1.000000000000000000, 0.9238795325112869605, 1.000000000000000000, 0.9238795325112869605, 1.000000000000000000, 0.9238795325112869605, 1.000000000000000000, 0.9238795325112869605, 1.000000000000000000, 0.9238795325112869605, 1.000000000000000000, 0.9238795325112869605, 1.000000000000000000, 0.9238795325112869605, 1.000000000000000000, 0.9238795325112869605, 1.000000000000000000, 0.9238795325112869605, 1.000000000000000000, 0.9238795325112869605, 1.000000000000000000, 0.9238795325112869605, 1.000000000000000000, 0.9238795325112869605, 1.000000000000000000, 0.9238795325112869605, 1.000000000000000000, 0.9238795325112869605, 1.000000000000000000, 0.9238795325112869605, 1.000000000000000000, 0.9238795325112869605, 1.000000000000000000, 0.9238795325112869605, 1.000000000000000000, 0.9238795325112869605, 1.000000000000000000, 0.9238795325112869605, 1.000000000000000000, 0.9238795325112869605, 1.000000000000000000, 0.9238795325112869605, 1.000000000000000000, 0.9238795325112869605, 1.000000000000000000, 0.9238795325112869605, 1.000000000000000000, 0.9238795325112869605, 1.000000000000000000, 0.9238795325112869605, 1.000000000000000000, 0.9238795325112869605, 1.000000000000000000, 0.9238795325112869605, 1.000000000000000000, 0.9238795325112869605, 1.000000000000000000, 0.9238795325112869605, 1.000000000000000000, 0.9238795325112869605, 1.000000000000000000, 0.9238795325112869605, 1.000000000000000000, 0.9238795325112869605, 1.000000000000000000, 0.9238795325112869605, 1.000000000000000000, 0.9238795325112869605, 1.000000000000000000),
 ( 1.000000000000000000, 0.9238795325112869605, 1.000000000000000000, 0.9238795325112869605, 1.000000000000000000, 0.9238795325112869605, 1.000000000000000000, 0.9238795325112869605, 1.000000000000000000, 0.9238795325112869605, 1.000000000000000000, 0.9238795325112869605, 1.000000000000000000, 0.9238795325112869605, 1.000000000000000000, 0.9238795325112869605, 1.000000000000000000, 0.9238795325112869605, 1.000000000000000000, 0.9238795325112869605, 1.000000000000000000, 0.9238795325112869605, 1.000000000000000000, 0.9238795325112869605, 1.000000000000000000, 0.9238795325112869605, 1.000000000000000000, 0.9238795325112869605, 1.000000000000000000, 0.9238795325112869605, 1.000000000000000000, 0.9238795325112869605, 1.000000000000000000, 0.9238795325112869605, 1.000000000000000000, 0.9238795325112869605, 1.000000000000000000, 0.9238795325112869605, 1.000000000000000000, 0.9238795325112869605, 1.000000000000000000, 0.9238795325112869605, 1.000000000000000000, 0.9238795325112869605, 1.000000000000000000, 0.9238795325112869605, 1.000000000000000000, 0.9238795325112869605, 1.000000000000000000, 0.9238795325112869605, 1.000000000000000000, 0.9238795325112869605, 1.000000000000000000, 0.9238795325112869605, 1.000000000000000000, 0.9238795325112869605, 1.000000000000000000, 0.9238795325112869605, 1.000000000000000000, 0.9238795325112869605, 1.000000000000000000, 0.9238795325112869605, 1.000000000000000000, 0.9238795325112869605, 1.000000000000000000, 0.9238795325112869605, 1.000000000000000000, 0.9238795325112869605, 1.000000000000000000, 0.9238795325112869605, 1.000000000000000000, 0.9238795325112869605, 1.000000000000000000, 0.9238795325112869605, 1.000000000000000000, 0.9238795325112869605, 1.000000000000000000, 0.9238795325112869605, 1.000000000000000000, 0.9238795325112869605, 1.000000000000000000, 0.9238795325112869605, 1.000000000000000000, 0.9238795325112869605, 1.000000000000000000, 0.9238795325112869605, 1.000000000000000000, 0.9238795325112869605, 1.000000000000000000, 0.9238795325112869605, 1.000000000000000000, 0.9238795325112869605, 1.000000000000000000, 0.9238795325112869605, 1.000000000000000000, 0.9238795325112869605, 1.000000000000000000, 0.9238795325112869605, 1.000000000000000000, 0.9238795325112869605, 1.000000000000000000, 0.9238795325112869605, 1.000000000000000000, 0.9238795325112869605, 1.000000000000000000, 0.9238795325112869605, 1.000000000000000000, 0.9238795325112869605, 1.000000000000000000, 0.9238795325112869605, 1.000000000000000000, 0.9238795325112869605, 1.000000000000000000, 0.9238795325112869605, 1.000000000000000000, 0.9238795325112869605, 1.000000000000000000, 0.9238795325112869605, 1.000000000000000000, 0.9238795325112869605, 1.000000000000000000, 0.9238795325112869605, 1.000000000000000000, 0.9238795325112869605, 1.000000000000000000, 0.9238795325112869605, 1.000000000000000000, 0.9238795325112869605, 1.000000000000000000, 0.9238795325112869605, 1.000000000000000000, 0.9238795325112869605, 1.000000000000000000, 0.9238795325112869605, 1.000000000000000000, 0.9238795325112869605, 1.000000000000000000, 0.9238795325112869605, 1.000000000000000000, 0.9238795325112869605, 1.000000000000000000, 0.9238795325112869605, 1.000000000000000000, 0.9238795325112869605, 1.000000000000000000, 0.9238795325112869605, 1.000000000000000000, 0.9238795325112869605, 1.000000000000000000, 0.9238795325112869605, 1.000000000000000000, 0.9238795325112869605, 1.000000000000000000, 0.9238795325112869605, 1.000000000000000000, 0.9238795325112869605, 1.000000000000000000, 0.9238795325112869605, 1.000000000000000000, 0.9238795325112869605, 1.000000000000000000, 0.9238795325112869605, 1.000000000000000000, 0.9238795325112869605, 1.000000000000000000, 0.9238795325112869605, 1.000000000000000000, 0.9238795325112869605, 1.000000000000000000, 0.9238795325112869605, 1.000000000000000000, 0.9238795325112869605, 1.000000000000000000, 0.9238795325112869605, 1.000000000000000000, 0.9238795325112869605, 1.000000000000000000, 0.9238795325112869605, 1.000000000000000000, 0.9238795325112869605, 1.000000000000000000, 0.9238795325112869605, 1.000000000000000000, 0.9238795325112869605, 1.000000000000000000, 0.9238795325112869605, 1.000000000000000000, 0.9238795325112869605, 1.000000000000000000, 0.9238795325112869605, 1.000000000000000000, 0.9238795325112869605, 1.000000000000000000, 0.9238795325112869605, 1.000000000000000000, 0.9238795325112869605, 1.000000000000000000, 0.9238795325112869605, 1.000000000000000000, 0.9238795325112869605, 1.000000000000000000, 0.9238795325112869605, 1.000000000000000000, 0.9238795325112869605, 1.000000000000000000, 0.9238795325112869605, 1.000000000000000000, 0.9238795325112869605, 1.000000000000000000, 0.9238795325112869605, 1.000000000000000000, 0.9238795325112869605, 1.000000000000000000, 0.9238795325112869605, 1.000000000000000000, 0.9238795325112869605, 1.000000000000000000, 0.9238795325112869605, 1.000000000000000000, 0.9238795325112869605, 1.000000000000000000, 0.9238795325112869605, 1.000000000000000000, 0.9238795325112869605, 1.000000000000000000, 0.9238795325112869605, 1.000000000000000000, 0.9238795325112869605, 1.000000000000000000, 0.9238795325112869605, 1.000000000000000000, 0.9238795325112869605, 1.000000000000000000, 0.9238795325112869605, 1.000000000000000000, 0.9238795325112869605, 1.000000000000000000, 0.9238795325112869605, 1.000000000000000000, 0.9238795325112869605, 1.000000000000000000, 0.9238795325112869605, 1.000000000000000000, 0.9238795325112869605, 1.000000000000000000, 0.9238795325112869605, 1.000000000000000000, 0.9238795325112869605, 1.000000000000000000, 0.9238795325112869605, 1.000000000000000000, 0.9238795325112869605, 1.000000000000000000, 0.9238795325112869605, 1.000000000000000000, 0.9238795325112869605, 1.000000000000000000) ) ) 
 REPRESENTATION_ITEM ( '' )  SURFACE ( )  );
#24696=DIRECTION ( 'NONE',  ( 0.000000000000000000, 0.6004852223388321697, -0.7996358532186279566 ) ) ;
#24698=CARTESIAN_POINT ( 'NONE',  ( 121.4964260444391755, -1.267766418764731728, -16.93314635290706605 ) ) ;
#24701=CARTESIAN_POINT ( 'NONE',  ( 114.3846081442453197, -10.63000616557722466, -14.87417383870573495 ) ) ;
#24702=CARTESIAN_POINT ( 'NONE',  ( 112.0588148109119828, 0.5811942927096154232, -14.16772938898807155 ) ) ;
#24703=CARTESIAN_POINT ( 'NONE',  ( 116.5402214775786405, -9.565557343593413364, -10.61323700422348004 ) ) ;
#24704=CARTESIAN_POINT ( 'NONE',  ( 113.3751581415389040, -0.1020945015694913471, -15.74893487844866691 ) ) ;
#24706=CARTESIAN_POINT ( 'NONE',  ( 114.4980614775786734, -2.084020599724406786, -8.691656652584148546 ) ) ;
#24711=CARTESIAN_POINT ( 'NONE',  ( 114.2144281442453178, -8.166667518702817929, -8.995218007635859436 ) ) ;
#24712=EDGE_LOOP ( 'NONE', ( #36310, #24319, #23531, #27449, #8711 ) ) ;
#24713=CARTESIAN_POINT ( 'NONE',  ( 116.0296814775786345, -8.166667518702817929, -8.995218007635861213 ) ) ;
#24717=CARTESIAN_POINT ( 'NONE',  ( 112.8529881442453302, -1.561330072975668060, -17.79121239304076596 ) ) ;
#24718=CARTESIAN_POINT ( 'NONE',  ( 114.1009748109119784, -4.089484607189486809, -7.948022111789456723 ) ) ;
#24719=CARTESIAN_POINT ( 'NONE',  ( 124.2550481442452792, -0.1624402480850797581, -16.17319339645315424 ) ) ;
#24726=CARTESIAN_POINT ( 'NONE',  ( 116.4834948109119779, -7.894159318335828068, -9.358103419637847864 ) ) ;
#24730=CARTESIAN_POINT ( 'NONE',  ( 124.1773369107181821, -2.467220198592779301, -17.83387418641524391 ) ) ;
#24731=CARTESIAN_POINT ( 'NONE',  ( 111.6617281442453304, 0.4262465694468514643, -12.03445270309931736 ) ) ;
#24733=CARTESIAN_POINT ( 'NONE',  ( 125.3895814775786448, -7.893985811506177619, -18.51759400769804742 ) ) ;
#24734=CARTESIAN_POINT ( 'NONE',  ( 116.2565881442452991, -9.261995988541697145, -16.69588392320189030 ) ) ;
#24736=CARTESIAN_POINT ( 'NONE',  ( 113.2500748109119968, -3.505236298600246325, -18.68346056562440793 ) ) ;
#24737=CARTESIAN_POINT ( 'NONE',  ( 125.6732148109119862, 0.5811942927096110934, -14.16772938898807510 ) ) ;
#24738=CARTESIAN_POINT ( 'NONE',  ( 116.4267681442453153, -3.383040157471821630, -19.15922257007629170 ) ) ;
#24739=CARTESIAN_POINT ( 'NONE',  ( 117.7882081442453170, -3.505236298600246325, -18.68346056562440793 ) ) ;
#24742=CARTESIAN_POINT ( 'NONE',  ( 123.1205148109119563, -7.643976991954077427, -18.09477374809248928 ) ) ;
#24745=CARTESIAN_POINT ( 'NONE',  ( 114.9518748109119883, -1.834011780172310813, -8.268836392978581529 ) ) ;
#24747=CARTESIAN_POINT ( 'NONE',  ( 136.5795292550376132, 0.4320203884789947102, -15.53198663114375222 ) ) ;
#24750=CARTESIAN_POINT ( 'NONE',  ( 126.7218814084904182, 0.3870001044524405964, -13.29043313491086842 ) ) ;
#24753=CARTESIAN_POINT ( 'NONE',  ( 115.9729548109119861, -6.344957434206662583, -7.627207830600332805 ) ) ;
#24754=VECTOR ( 'NONE', #16125, 1000.000000000000000 ) ;
#24759=CARTESIAN_POINT ( 'NONE',  ( 114.1009748109119784, -5.574606645277164318, -18.38911715685844683 ) ) ;
#24760=EDGE_CURVE ( 'NONE', #11611, #29815, #86, .T. ) ;
#24763=CARTESIAN_POINT ( 'NONE',  ( 115.4624148109119943, -5.638512984488999180, -18.83840828888717311 ) ) ;
#24765=CARTESIAN_POINT ( 'NONE',  ( 117.7314814775786260, -5.574606645277164318, -18.38911715685844683 ) ) ;
#24767=CARTESIAN_POINT ( 'NONE',  ( 136.7860375664301102, -9.155735703506769241, -9.793839820488711823 ) ) ;
#24768=CARTESIAN_POINT ( 'NONE',  ( 122.7801548109119665, -3.383040157471821630, -19.15922257007629170 ) ) ;
#24770=CARTESIAN_POINT ( 'NONE',  ( 118.5823814775786360, -7.643976991954077427, -18.09477374809248928 ) ) ;
#24772=CARTESIAN_POINT ( 'NONE',  ( 113.3635281442453504, -0.1624402480850797581, -16.17319339645315424 ) ) ;
#24773=EDGE_CURVE ( 'NONE', #3515, #41752, #23528, .T. ) ;
#24776=CARTESIAN_POINT ( 'NONE',  ( 118.9794681442453026, -0.8288870151387760510, -10.36305467784173118 ) ) ;
#24777=CARTESIAN_POINT ( 'NONE',  ( 119.2631014775786298, -9.565557343593413364, -10.61323700422348004 ) ) ;
#24785=CARTESIAN_POINT ( 'NONE',  ( 118.7525614775786380, -8.166667518702819706, -8.995218007635861213 ) ) ;
#24786=CARTESIAN_POINT ( 'NONE',  ( 116.3700414775786527, -5.638512984488999180, -18.83840828888717311 ) ) ;
#24788=CARTESIAN_POINT ( 'NONE',  ( 112.4559014775786494, -9.988377603198976828, -10.36322818467138340 ) ) ;
#24790=CARTESIAN_POINT ( 'NONE',  ( 112.9455131944929462, -1.036737761566191018, -17.24079555149560150 ) ) ;
#24791=CARTESIAN_POINT ( 'NONE',  ( 122.5532481442453019, -10.63000616557722466, -14.87417383870573495 ) ) ;
#24793=CARTESIAN_POINT ( 'NONE',  ( 116.2565881442452991, -9.261995988541697145, -16.69588392320189030 ) ) ;
#24794=CARTESIAN_POINT ( 'NONE',  ( 120.4543614775786295, -5.574606645277164318, -18.38911715685844683 ) ) ;
#24795=( LENGTH_UNIT ( ) NAMED_UNIT ( * ) SI_UNIT ( .MILLI., .METRE. ) );
#24797=CARTESIAN_POINT ( 'NONE',  ( 112.1155414775786454, -10.15424416112533912, -14.75197769757731336 ) ) ;
#24798=CARTESIAN_POINT ( 'NONE',  ( 123.2339681442453241, -6.344957434206665248, -7.627207830600338134 ) ) ;
#24799=ADVANCED_FACE ( 'NONE', ( #37883 ), #16702, .F. ) ;
#24801=CARTESIAN_POINT ( 'NONE',  ( 115.0653281442453277, -3.505236298600246325, -18.68346056562440793 ) ) ;
#24804=CARTESIAN_POINT ( 'NONE',  ( 123.0637881442452937, -0.4660016031367893996, -10.09054647747474043 ) ) ;
#24806=CARTESIAN_POINT ( 'NONE',  ( 119.4332814775786318, -0.4660016031367893996, -10.09054647747474043 ) ) ;
#24809=CARTESIAN_POINT ( 'NONE',  ( 124.3117748109119844, -10.30919188438810075, -12.61870101168855918 ) ) ;
#24812=CARTESIAN_POINT ( 'NONE',  ( 116.4834948109119779, -7.894159318335828068, -9.358103419637847864 ) ) ;
#24814=CARTESIAN_POINT ( 'NONE',  ( 121.4187148109119789, -3.505236298600246325, -18.68346056562440793 ) ) ;
#24815=CARTESIAN_POINT ( 'NONE',  ( 121.0408330757767459, -0.9924539043446216624, -17.29976612834909133 ) ) ;
#24816=CARTESIAN_POINT ( 'NONE',  ( 122.7234281442452755, -4.153390946401325223, -8.397313243818185668 ) ) ;
#24819=CARTESIAN_POINT ( 'NONE',  ( 117.9583881442453048, 0.1319031606808879209, -14.10382304977623669 ) ) ;
#24822=CARTESIAN_POINT ( 'NONE',  ( 116.4834948109119779, -1.561330072975668504, -17.79121239304076951 ) ) ;
#24824=ADVANCED_BREP_SHAPE_REPRESENTATION ( '', ( #36408, #12375 ), #14045 ) ;
#24825=CARTESIAN_POINT ( 'NONE',  ( 119.2631014775786298, -9.565557343593413364, -10.61323700422348004 ) ) ;
#24827=CARTESIAN_POINT ( 'NONE',  ( 115.1787814775786387, -9.988377603198976828, -10.36322818467138340 ) ) ;
#24832=CARTESIAN_POINT ( 'NONE',  ( 123.4041481442452834, -10.30919188438810075, -12.61870101168855918 ) ) ;
#24835=CARTESIAN_POINT ( 'NONE',  ( 120.9649014775786355, -6.222761293078241884, -8.102969835052219238 ) ) ;
#24839=CARTESIAN_POINT ( 'NONE',  ( 125.9001214775786224, -4.089484607189486809, -7.948022111789456723 ) ) ;
#24843=CARTESIAN_POINT ( 'NONE',  ( 116.1998614775786507, -10.63000616557722466, -14.87417383870573495 ) ) ;
#24844=CARTESIAN_POINT ( 'NONE',  ( 125.0492214775786266, -3.505236298600246325, -18.68346056562440793 ) ) ;
#24845=CARTESIAN_POINT ( 'NONE',  ( 123.8012348109119642, 0.2603800115204892296, -16.42320221600525088 ) ) ;
#24847=CARTESIAN_POINT ( 'NONE',  ( 117.8449348109119938, -1.833838273342659253, -17.42832698103878286 ) ) ;
#24848=CARTESIAN_POINT ( 'NONE',  ( 126.9733055311760239, -3.110392498322739563, -8.309745536333537075 ) ) ;
#24849=CARTESIAN_POINT ( 'NONE',  ( 123.6877814775786533, -3.383040157471821630, -19.15922257007629170 ) ) ;
#24850=CARTESIAN_POINT ( 'NONE',  ( 111.3319081442453182, -5.568102603702657305, -18.34339073538273013 ) ) ;
#24853=CARTESIAN_POINT ( 'NONE',  ( 125.5030348109119558, -6.222761293078241884, -8.102969835052219238 ) ) ;
#24857=CARTESIAN_POINT ( 'NONE',  ( 120.7947214775786193, -9.261995988541697145, -16.69588392320189030 ) ) ;
#24858=CARTESIAN_POINT ( 'NONE',  ( 135.3184548109119874, -8.536181032868617180, -18.13822074491315561 ) ) ;
#24863=CARTESIAN_POINT ( 'NONE',  ( 120.7947214775786193, -9.261995988541697145, -16.69588392320189030 ) ) ;
#24865=CARTESIAN_POINT ( 'NONE',  ( 118.9227414775786542, 0.4262465694468514643, -12.03445270309931736 ) ) ;
#24867=CARTESIAN_POINT ( 'NONE',  ( 116.1998614775786507, -10.63000616557722466, -14.87417383870573495 ) ) ;
#24869=CARTESIAN_POINT ( 'NONE',  ( 120.9542138145250192, -3.807985514183305664, -19.09877912889402651 ) ) ;
#24871=CARTESIAN_POINT ( 'NONE',  ( 125.6164881442453094, 0.2603800115204892296, -16.42320221600525088 ) ) ;
#24875=CARTESIAN_POINT ( 'NONE',  ( 121.9859814775786333, 0.2603800115204892296, -16.42320221600525088 ) ) ;
#24876=CARTESIAN_POINT ( 'NONE',  ( 121.8158014775786171, -5.638512984488999180, -18.83840828888717311 ) ) ;
#24877=CARTESIAN_POINT ( 'NONE',  ( 121.6456214775786293, 0.4262465694468514643, -12.03445270309931736 ) ) ;
#24878=CARTESIAN_POINT ( 'NONE',  ( 120.3409081442453044, -8.899110576539710493, -16.42337572283490132 ) ) ;
#24879=CARTESIAN_POINT ( 'NONE',  ( 125.3223148109119904, 0.3778260857404744377, -12.04688916545782007 ) ) ;
#24880=CARTESIAN_POINT ( 'NONE',  ( 117.2209414775786485, -7.893985811506177619, -18.51759400769804742 ) ) ;
#24888=CARTESIAN_POINT ( 'NONE',  ( 125.6732148109119862, 0.5811942927096110934, -14.16772938898807510 ) ) ;
#24889=CARTESIAN_POINT ( 'NONE',  ( 125.7299414775786346, -10.15424416112533912, -14.75197769757731336 ) ) ;
#24891=CARTESIAN_POINT ( 'NONE',  ( 114.7816948109119863, -9.859900752359374465, -12.68260735090039404 ) ) ;
#24893=CARTESIAN_POINT ( 'NONE',  ( 118.9794681442453026, -0.8288870151387751628, -10.36305467784173118 ) ) ;
#24895=CARTESIAN_POINT ( 'NONE',  ( 125.7866681442452688, -0.4660016031367893996, -10.09054647747474043 ) ) ;
#24897=CARTESIAN_POINT ( 'NONE',  ( 117.7314814775786260, -4.089484607189486809, -7.948022111789456723 ) ) ;
#24901=CARTESIAN_POINT ( 'NONE',  ( 126.8396850857720324, -7.259892949939295015, -8.653599086628718240 ) ) ;
#24902=CARTESIAN_POINT ( 'NONE',  ( 115.9162281442453235, -5.574606645277164318, -18.38911715685844683 ) ) ;
#24903=CARTESIAN_POINT ( 'NONE',  ( 114.3278814775786429, -10.30919188438810075, -12.61870101168855918 ) ) ;
#24904=CARTESIAN_POINT ( 'NONE',  ( 112.8529881442453302, -1.561330072975668060, -17.79121239304076596 ) ) ;
#24905=CARTESIAN_POINT ( 'NONE',  ( 123.6310548109119765, -4.153390946401325223, -8.397313243818185668 ) ) ;
#24906=CARTESIAN_POINT ( 'NONE',  ( 118.8660148109119774, 0.1319031606808879209, -14.10382304977623669 ) ) ;
#24907=CARTESIAN_POINT ( 'NONE',  ( 112.1722681442453222, -8.899110576539710493, -16.42337572283490132 ) ) ;
#24909=CARTESIAN_POINT ( 'NONE',  ( 124.8790414775786246, -8.899110576539710493, -16.42337572283490132 ) ) ;
#24910=VECTOR ( 'NONE', #15261, 1000.000000000000000 ) ;
#24912=CARTESIAN_POINT ( 'NONE',  ( 121.4937273908105908, -2.443475742715334853, -17.86549347949429389 ) ) ;
#24913=CARTESIAN_POINT ( 'NONE',  ( 112.7962614775786676, -6.222761293078241884, -8.102969835052219238 ) ) ;
#24915=CARTESIAN_POINT ( 'NONE',  ( 126.2184548109090940, -8.862178061931365036, -16.39564131203211517 ) ) ;
#24918=CARTESIAN_POINT ( 'NONE',  ( 125.3895814775786448, -2.084020599724406786, -8.691656652584148546 ) ) ;
#24919=VECTOR ( 'NONE', #23090, 1000.000000000000000 ) ;
#24921=CARTESIAN_POINT ( 'NONE',  ( 119.3765548109119834, -10.15424416112533912, -14.75197769757731336 ) ) ;
#24922=CARTESIAN_POINT ( 'NONE',  ( 117.5045748109119756, -9.859900752359374465, -12.68260735090039404 ) ) ;
#24925=ORIENTED_EDGE ( 'NONE', *, *, #37870, .T. ) ;
#24930=CARTESIAN_POINT ( 'NONE',  ( 113.3635281442453504, -9.988377603198976828, -10.36322818467138340 ) ) ;
#24931=CARTESIAN_POINT ( 'NONE',  ( 115.9162281442453093, -5.574606645277164318, -18.38911715685844683 ) ) ;
#24932=DIRECTION ( 'NONE',  ( 0.000000000000000000, -0.6004852223388322807, 0.7996358532186280677 ) ) ;
#24934=CARTESIAN_POINT ( 'NONE',  ( 116.9373081442452929, -1.833838273342659253, -17.42832698103878286 ) ) ;
#24938=CARTESIAN_POINT ( 'NONE',  ( 125.1344018827933411, -1.272282569755609494, -16.92713242264453655 ) ) ;
#24939=CARTESIAN_POINT ( 'NONE',  ( 116.6493314740559413, -1.081026697600512732, -17.18181821144401056 ) ) ;
#24940=CARTESIAN_POINT ( 'NONE',  ( 114.2711548109119803, -9.988377603198976828, -10.36322818467138340 ) ) ;
#24942=CARTESIAN_POINT ( 'NONE',  ( 117.2776681442452968, -5.638512984488999180, -18.83840828888717311 ) ) ;
#24943=CARTESIAN_POINT ( 'NONE',  ( 114.5547881442453217, -5.638512984488999180, -18.83840828888717311 ) ) ;
#24945=CARTESIAN_POINT ( 'NONE',  ( 126.2404814775786264, -0.8288870151387760510, -10.36305467784173118 ) ) ;
#24946=CARTESIAN_POINT ( 'NONE',  ( 115.2355081442453155, -10.30919188438810075, -12.61870101168855918 ) ) ;
#24952=AXIS2_PLACEMENT_3D ( 'NONE', #22339, #681, #38986 ) ;
#24955=CARTESIAN_POINT ( 'NONE',  ( 117.7882081442453170, -3.505236298600246325, -18.68346056562440793 ) ) ;
#24957=CARTESIAN_POINT ( 'NONE',  ( 118.0718414775786300, -9.261995988541702474, -16.69588392320188319 ) ) ;
#24960=CARTESIAN_POINT ( 'NONE',  ( 115.9162281442453093, -5.574606645277164318, -18.38911715685844683 ) ) ;
#24961=CARTESIAN_POINT ( 'NONE',  ( 135.3184548109119874, 1.087851763053662602, -12.63461456455805276 ) ) ;
#24962=CARTESIAN_POINT ( 'NONE',  ( 123.5743281442453139, -7.893985811506177619, -18.51759400769804742 ) ) ;
#24963=CARTESIAN_POINT ( 'NONE',  ( 117.3911214775786505, -1.561330072975668504, -17.79121239304076951 ) ) ;
#24965=CARTESIAN_POINT ( 'NONE',  ( 114.4980614775786734, -2.084020599724406786, -8.691656652584148546 ) ) ;
#24966=CARTESIAN_POINT ( 'NONE',  ( 112.0020881442453344, 0.2603800115204892296, -16.42320221600525088 ) ) ;
#24967=CARTESIAN_POINT ( 'NONE',  ( 116.9940348109119839, -9.988377603198976828, -10.36322818467138340 ) ) ;
#24968=CARTESIAN_POINT ( 'NONE',  ( 116.4834948109119779, -7.894159318335828068, -9.358103419637847864 ) ) ;
#24970=CARTESIAN_POINT ( 'NONE',  ( 121.9292548109119849, -7.894159318335828068, -9.358103419637847864 ) ) ;
#24973=CARTESIAN_POINT ( 'NONE',  ( 115.2355081442453155, -10.30919188438810075, -12.61870101168855918 ) ) ;
#24974=CARTESIAN_POINT ( 'NONE',  ( 137.2016500469330538, 0.1791020294301809146, -15.04270252157057719 ) ) ;
#24977=CARTESIAN_POINT ( 'NONE',  ( 126.4168230350732358, 0.2316726006529284954, -13.58249618387747581 ) ) ;
#24979=VECTOR ( 'NONE', #12884, 1000.000000000000000 ) ;
#24980=CARTESIAN_POINT ( 'NONE',  ( 113.9307948109119906, 0.9020085738987339008, -11.91225656197089222 ) ) ;
#24982=CARTESIAN_POINT ( 'NONE',  ( 115.0086014775786509, -5.574606645277164318, -18.38911715685844683 ) ) ;
#24986=CARTESIAN_POINT ( 'NONE',  ( 114.3846081442453197, 0.4262465694468514643, -12.03445270309931736 ) ) ;
#24990=CARTESIAN_POINT ( 'NONE',  ( 118.5823814775786360, -1.834011780172310813, -8.268836392978581529 ) ) ;
#24991=FACE_OUTER_BOUND ( 'NONE', #12645, .T. ) ;
#24992=CARTESIAN_POINT ( 'NONE',  ( 120.7947214775786193, -0.8288870151387760510, -10.36305467784173118 ) ) ;
#24993=CARTESIAN_POINT ( 'NONE',  ( 125.5597614775786326, -1.561330072975669392, -17.79121239304076951 ) ) ;
#24996=CARTESIAN_POINT ( 'NONE',  ( 122.0427081442452817, 0.5811942927096110934, -14.16772938898807510 ) ) ;
#24998=CARTESIAN_POINT ( 'NONE',  ( 120.4543614775786295, -5.574606645277164318, -18.38911715685844683 ) ) ;
#25000=CARTESIAN_POINT ( 'NONE',  ( 117.5045748109119756, -9.859900752359374465, -12.68260735090039404 ) ) ;
#25003=CARTESIAN_POINT ( 'NONE',  ( 121.3619881442452879, -5.574606645277164318, -18.38911715685844683 ) ) ;
#25004=VECTOR ( 'NONE', #22095, 1000.000000000000000 ) ;
#25005=CARTESIAN_POINT ( 'NONE',  ( 125.6164881442453094, -9.565557343593413364, -10.61323700422348004 ) ) ;
#25011=CARTESIAN_POINT ( 'NONE',  ( 116.2565881442452991, -9.261995988541697145, -16.69588392320189030 ) ) ;
#25012=CARTESIAN_POINT ( 'NONE',  ( 113.8740681442453138, 0.5811942927096154232, -14.16772938898807155 ) ) ;
#25014=CARTESIAN_POINT ( 'NONE',  ( 113.7606148109119886, -1.561330072975668060, -17.79121239304076596 ) ) ;
#25015=ORIENTED_EDGE ( 'NONE', *, *, #32499, .T. ) ;
#25016=CARTESIAN_POINT ( 'NONE',  ( 135.3184548109119874, -4.863998795839242995, -13.39321520033831447 ) ) ;
#25018=CARTESIAN_POINT ( 'NONE',  ( 124.1983214775786166, -8.166667518702819706, -8.995218007635861213 ) ) ;
#25019=CARTESIAN_POINT ( 'NONE',  ( 115.8027748109119841, -0.4660016031367893996, -10.09054647747474043 ) ) ;
#25020=CARTESIAN_POINT ( 'NONE',  ( 123.2906948109119867, -1.833838273342659697, -17.42832698103878286 ) ) ;
#25021=CARTESIAN_POINT ( 'NONE',  ( 112.2289948109119848, -7.643976991954077427, -18.09477374809248928 ) ) ;
#25022=CARTESIAN_POINT ( 'NONE',  ( 123.4608748109119745, -10.63000616557722466, -14.87417383870573495 ) ) ;
#25023=ADVANCED_FACE ( 'NONE', ( #14385 ), #20452, .T. ) ;
#25025=CARTESIAN_POINT ( 'NONE',  ( 116.6536748109119941, -10.15424416112533912, -14.75197769757731336 ) ) ;
#25028=CARTESIAN_POINT ( 'NONE',  ( 120.2274548109119934, 0.5811942927096110934, -14.16772938898807510 ) ) ;
#25033=CARTESIAN_POINT ( 'NONE',  ( 118.3554748109119998, 0.2603800115204892296, -16.42320221600525088 ) ) ;
#25038=CARTESIAN_POINT ( 'NONE',  ( 117.1074881442453233, 0.4262465694468514643, -12.03445270309931736 ) ) ;
#25041=CARTESIAN_POINT ( 'NONE',  ( 118.4122014775786340, -9.859900752359374465, -12.68260735090039404 ) ) ;
#25042=CARTESIAN_POINT ( 'NONE',  ( 121.3052614775786395, -1.834011780172307704, -8.268836392978586858 ) ) ;
#25044=CARTESIAN_POINT ( 'NONE',  ( 122.2128881442453263, -7.643976991954077427, -18.09477374809248928 ) ) ;
#25045=AXIS2_PLACEMENT_3D ( 'NONE', #21060, #31542, #28355 ) ;
#25047=CARTESIAN_POINT ( 'NONE',  ( 119.3765548109119834, -10.15424416112533912, -14.75197769757731336 ) ) ;
#25049=CARTESIAN_POINT ( 'NONE',  ( 112.1722681442453222, -0.4660016031367893996, -10.09054647747474043 ) ) ;
#25050=CARTESIAN_POINT ( 'NONE',  ( 119.6034614775786196, -6.344957434206665248, -7.627207830600338134 ) ) ;
#25051=CARTESIAN_POINT ( 'NONE',  ( 126.0135748109119902, -1.833838273342660141, -17.42832698103878286 ) ) ;
#25054=ADVANCED_FACE ( 'NONE', ( #29188 ), #4561, .T. ) ;
#25055=CARTESIAN_POINT ( 'NONE',  ( 121.4754414775786131, -1.833838273342659697, -17.42832698103878286 ) ) ;
#25057=CARTESIAN_POINT ( 'NONE',  ( 117.9016614775786280, -9.988377603198976828, -10.36322818467138340 ) ) ;
#25062=CARTESIAN_POINT ( 'NONE',  ( 124.9924948109119924, -4.089484607189486809, -7.948022111789456723 ) ) ;
#25065=CARTESIAN_POINT ( 'NONE',  ( 121.1350814775786233, -9.859900752359378018, -12.68260735090039759 ) ) ;
#25072=CARTESIAN_POINT ( 'NONE',  ( 114.2711548109119803, -9.988377603198976828, -10.36322818467138340 ) ) ;
#25073=CARTESIAN_POINT ( 'NONE',  ( 114.2144281442453178, -8.166667518702817929, -8.995218007635859436 ) ) ;
#25074=CARTESIAN_POINT ( 'NONE',  ( 125.5597614775786326, -1.561330072975669392, -17.79121239304076951 ) ) ;
#25075=CARTESIAN_POINT ( 'NONE',  ( 120.0005481442453146, -4.153390946401325223, -8.397313243818185668 ) ) ;
#25076=CARTESIAN_POINT ( 'NONE',  ( 112.2289948109119848, -7.643976991954077427, -18.09477374809248928 ) ) ;
#25078=CARTESIAN_POINT ( 'NONE',  ( 123.0070614775786169, 0.9020085738987339008, -11.91225656197089222 ) ) ;
#25079=CARTESIAN_POINT ( 'NONE',  ( 123.9146881442452894, -10.15424416112534978, -14.75197769757730093 ) ) ;
#25082=CARTESIAN_POINT ( 'NONE',  ( 125.2194014775786286, 0.1319031606808879209, -14.10382304977623669 ) ) ;
#25085=CARTESIAN_POINT ( 'NONE',  ( 119.9438214775786378, -7.893985811506177619, -18.51759400769804742 ) ) ;
#25086=CARTESIAN_POINT ( 'NONE',  ( 137.3527759848290657, -9.371214294599425898, -15.91961478861451340 ) ) ;
#25087=ORIENTED_EDGE ( 'NONE', *, *, #29223, .T. ) ;
#25088=CARTESIAN_POINT ( 'NONE',  ( 121.4544569107182070, -2.467220198592778413, -17.83387418641524391 ) ) ;
#25090=CARTESIAN_POINT ( 'NONE',  ( 124.9357681442453014, -1.834011780172310813, -8.268836392978581529 ) ) ;
#25092=CARTESIAN_POINT ( 'NONE',  ( 123.2339681442453241, -3.505236298600246325, -18.68346056562440793 ) ) ;
#25095=CARTESIAN_POINT ( 'NONE',  ( 115.2355081442453155, -10.30919188438810075, -12.61870101168855918 ) ) ;
#25097=CARTESIAN_POINT ( 'NONE',  ( 121.0024232127138504, -2.191907684172563986, -18.20049396185734025 ) ) ;
#25100=CARTESIAN_POINT ( 'NONE',  ( 125.8433948109119456, -1.834011780172310813, -8.268836392978581529 ) ) ;
#25104=CARTESIAN_POINT ( 'NONE',  ( 124.8790414775786246, -0.4660016031367893996, -10.09054647747474043 ) ) ;
#25105=CARTESIAN_POINT ( 'NONE',  ( 123.9714148109119805, -0.4660016031367893996, -10.09054647747474043 ) ) ;
#25106=CARTESIAN_POINT ( 'NONE',  ( 122.8936081442453059, -9.565557343593413364, -10.61323700422348004 ) ) ;
#25107=CARTESIAN_POINT ( 'NONE',  ( 123.4608748109119745, 0.4262465694468514643, -12.03445270309931736 ) ) ;
#25109=CARTESIAN_POINT ( 'NONE',  ( 120.9649014775786355, -3.383040157471821630, -19.15922257007629170 ) ) ;
#25110=ORIENTED_EDGE ( 'NONE', *, *, #12253, .F. ) ;
#25113=CARTESIAN_POINT ( 'NONE',  ( 112.1234697116520920, -8.918491192341182483, -16.31914947962552631 ) ) ;
#25118=CARTESIAN_POINT ( 'NONE',  ( 126.0703014775786102, -9.988377603198980381, -10.36322818467138518 ) ) ;
#25119=CARTESIAN_POINT ( 'NONE',  ( 126.2972081442452890, -2.084020599724406786, -8.691656652584148546 ) ) ;
#25121=CARTESIAN_POINT ( 'NONE',  ( 111.3780948109119890, -5.574606645277164318, -18.38911715685844683 ) ) ;
#25125=CARTESIAN_POINT ( 'NONE',  ( 125.6164881442453094, 0.2603800115204892296, -16.42320221600525088 ) ) ;
#25126=CARTESIAN_POINT ( 'NONE',  ( 123.8012348109119642, 0.2603800115204892296, -16.42320221600525088 ) ) ;
#25128=CARTESIAN_POINT ( 'NONE',  ( 117.3343948109119737, -3.383040157471821630, -19.15922257007629170 ) ) ;
#25134=CARTESIAN_POINT ( 'NONE',  ( 116.4267681442453153, -6.222761293078241884, -8.102969835052219238 ) ) ;
#25135=CARTESIAN_POINT ( 'NONE',  ( 116.8805814775786445, -6.344957434206662583, -7.627207830600332805 ) ) ;
#25136=CARTESIAN_POINT ( 'NONE',  ( 112.5693548109119888, -10.63000616557722466, -14.87417383870573495 ) ) ;
#25137=CARTESIAN_POINT ( 'NONE',  ( 123.8012348109119642, -9.565557343593413364, -10.61323700422348004 ) ) ;
#25139=CARTESIAN_POINT ( 'NONE',  ( 120.5678148109119832, -1.833838273342659253, -17.42832698103878286 ) ) ;
#25140=CARTESIAN_POINT ( 'NONE',  ( 116.1998614775786507, 0.4262465694468514643, -12.03445270309931736 ) ) ;
#25142=CONICAL_SURFACE ( 'NONE', #24383, 5.999999999999997335, 0.4636476090008060935 ) ;
#25145=CARTESIAN_POINT ( 'NONE',  ( 116.8238548109119819, -5.574606645277164318, -18.38911715685844683 ) ) ;
#25150=CARTESIAN_POINT ( 'NONE',  ( 112.3991748109119868, -1.833838273342658809, -17.42832698103878286 ) ) ;
#25153=CARTESIAN_POINT ( 'NONE',  ( 118.4122014775786340, -9.859900752359374465, -12.68260735090039404 ) ) ;
#25154=CARTESIAN_POINT ( 'NONE',  ( 118.8660148109119774, 0.1319031606808879209, -14.10382304977623669 ) ) ;
#25163=CARTESIAN_POINT ( 'NONE',  ( 124.9924948109119924, -5.574606645277164318, -18.38911715685844683 ) ) ;
#25164=CARTESIAN_POINT ( 'NONE',  ( 116.5969481442453031, -9.859900752359374465, -12.68260735090039404 ) ) ;
#25166=ORIENTED_EDGE ( 'NONE', *, *, #5904, .T. ) ;
#25167=CARTESIAN_POINT ( 'NONE',  ( 116.2565881442453133, -0.8288870151387760510, -10.36305467784173118 ) ) ;
#25172=CARTESIAN_POINT ( 'NONE',  ( 113.4769814775786330, -10.63000616557722466, -14.87417383870573495 ) ) ;
#25174=CARTESIAN_POINT ( 'NONE',  ( 117.9016614775786280, -9.988377603198976828, -10.36322818467138340 ) ) ;
#25177=CARTESIAN_POINT ( 'NONE',  ( 117.3343948109119737, -3.383040157471821630, -19.15922257007629170 ) ) ;
#25178=CARTESIAN_POINT ( 'NONE',  ( 114.4413348109119823, -9.261995988541697145, -16.69588392320189030 ) ) ;
#25179=CARTESIAN_POINT ( 'NONE',  ( 126.2455040230450720, -9.855666071798866668, -12.91250244977849526 ) ) ;
#25185=CARTESIAN_POINT ( 'NONE',  ( 117.1074881442453233, 0.4262465694468514643, -12.03445270309931736 ) ) ;
#25191=CARTESIAN_POINT ( 'NONE',  ( 114.5547881442453217, -4.153390946401321671, -8.397313243818183892 ) ) ;
#25193=CARTESIAN_POINT ( 'NONE',  ( 123.7445081442452874, -1.561330072975668948, -17.79121239304076951 ) ) ;
#25194=CARTESIAN_POINT ( 'NONE',  ( 121.5321681442453183, -9.988377603198976828, -10.36322818467138340 ) ) ;
#25195=ORIENTED_EDGE ( 'NONE', *, *, #28663, .T. ) ;
#25196=CARTESIAN_POINT ( 'NONE',  ( 113.9875214775786532, -8.899110576539710493, -16.42337572283490132 ) ) ;
#25197=CARTESIAN_POINT ( 'NONE',  ( 113.3068014775786594, -8.166667518702817929, -8.995218007635859436 ) ) ;
#25198=CARTESIAN_POINT ( 'NONE',  ( 117.1642148109119859, -9.261995988541697145, -16.69588392320189030 ) ) ;
#25200=CARTESIAN_POINT ( 'NONE',  ( 119.5467348109119712, -5.574606645277164318, -18.38911715685844683 ) ) ;
#25201=VERTEX_POINT ( 'NONE', #8445 ) ;
#25202=CARTESIAN_POINT ( 'NONE',  ( 122.8368814775786291, -7.894159318335828068, -9.358103419637847864 ) ) ;
#25204=CARTESIAN_POINT ( 'NONE',  ( 121.4754414775786131, -8.166667518702819706, -8.995218007635861213 ) ) ;
#25205=CARTESIAN_POINT ( 'NONE',  ( 137.3172077154941348, 0.1253259204073826072, -14.86998863374360447 ) ) ;
#25210=CARTESIAN_POINT ( 'NONE',  ( 114.1009748109119784, -4.089484607189486809, -7.948022111789456723 ) ) ;
#25211=CARTESIAN_POINT ( 'NONE',  ( 137.2352176311238452, -10.13879886906272887, -13.53006418403055733 ) ) ;
#25212=CARTESIAN_POINT ( 'NONE',  ( 114.6682414775786469, -7.894159318335828068, -9.358103419637847864 ) ) ;
#25216=CARTESIAN_POINT ( 'NONE',  ( 121.9100498793805230, -2.191907684172563986, -18.20049396185734025 ) ) ;
#25221=CARTESIAN_POINT ( 'NONE',  ( 120.2841814775786276, 0.9020085738987339008, -11.91225656197089222 ) ) ;
#25223=CARTESIAN_POINT ( 'NONE',  ( 120.3409081442453044, -8.899110576539710493, -16.42337572283490132 ) ) ;
#25224=CARTESIAN_POINT ( 'NONE',  ( 126.0135748109119902, -8.166667518702819706, -8.995218007635861213 ) ) ;
#25226=CARTESIAN_POINT ( 'NONE',  ( 136.4173705901494316, -7.083541812144162897, -8.051131675560494472 ) ) ;
#25227=CARTESIAN_POINT ( 'NONE',  ( 124.4819548109119722, -7.893985811506177619, -18.51759400769804742 ) ) ;
#25229=CARTESIAN_POINT ( 'NONE',  ( 118.0151148109119816, 0.4262465694468514643, -12.03445270309931736 ) ) ;
#25231=CARTESIAN_POINT ( 'NONE',  ( 114.8951481442453115, -8.899110576539710493, -16.42337572283490132 ) ) ;
#25234=CARTESIAN_POINT ( 'NONE',  ( 121.8725281442453223, -6.222761293078241884, -8.102969835052219238 ) ) ;
#25235=CARTESIAN_POINT ( 'NONE',  ( 125.5030348109119558, -6.222761293078241884, -8.102969835052219238 ) ) ;
#25240=PRODUCT_DEFINITION_SHAPE ( 'NONE', 'NONE',  #7964 ) ;
#25243=CARTESIAN_POINT ( 'NONE',  ( 116.5969481442453031, 0.5811942927096154232, -14.16772938898807155 ) ) ;
#25244=CARTESIAN_POINT ( 'NONE',  ( 119.4332814775786318, -0.4660016031367893996, -10.09054647747474043 ) ) ;
#25246=( BOUNDED_CURVE ( )  B_SPLINE_CURVE ( 2, ( #190, #11139, #28246, #4734, #18652, #25042, #43045, #8390, #21843, #18870, #864, #25720, #15004, #35275, #28696, #38938, #32094 ),
 .UNSPECIFIED., .F., .T. ) 
 B_SPLINE_CURVE_WITH_KNOTS ( ( 3, 2, 2, 2, 2, 2, 2, 2, 3 ),
 ( 0.6420046674808920217, 0.6484375000000000000, 0.6562500000000000000, 0.6640625000000000000, 0.6718750000000000000, 0.6796875000000000000, 0.6875000000000000000, 0.6953125000000000000, 0.7017453325190590174 ),
 .UNSPECIFIED. ) 
 CURVE ( )  GEOMETRIC_REPRESENTATION_ITEM ( )  RATIONAL_B_SPLINE_CURVE ( ( 0.9778625265006449796, 0.9373222120152220338, 1.000000000000000000, 0.9238795325112869605, 1.000000000000000000, 0.9238795325112869605, 1.000000000000000000, 0.9238795325112869605, 1.000000000000000000, 0.9238795325112869605, 1.000000000000000000, 0.9238795325112869605, 1.000000000000000000, 0.9238795325112869605, 1.000000000000000000, 0.9373222120157009840, 0.9778625265000250311 ) ) 
 REPRESENTATION_ITEM ( '' )  );
#25248=CARTESIAN_POINT ( 'NONE',  ( 113.2492419144190592, -1.220279397241706532, -16.99638242193885773 ) ) ;
#25249=CARTESIAN_POINT ( 'NONE',  ( 115.1787814775786387, -9.988377603198976828, -10.36322818467138340 ) ) ;
#25250=CARTESIAN_POINT ( 'NONE',  ( 121.3052614775786111, -7.643976991954077427, -18.09477374809248928 ) ) ;
#25253=CARTESIAN_POINT ( 'NONE',  ( 124.4819548109119722, -7.893985811506177619, -18.51759400769804742 ) ) ;
#25254=CARTESIAN_POINT ( 'NONE',  ( 123.5743281442453139, -7.893985811506177619, -18.51759400769804742 ) ) ;
#25255=CIRCLE ( 'NONE', #11424, 5.999999999999997335 ) ;
#25257=CARTESIAN_POINT ( 'NONE',  ( 116.1998614775786507, 0.4262465694468514643, -12.03445270309931736 ) ) ;
#25263=CARTESIAN_POINT ( 'NONE',  ( 118.8092881442453290, -9.988377603198976828, -10.36322818467138340 ) ) ;
#25268=CARTESIAN_POINT ( 'NONE',  ( 114.9518748109119883, -7.643976991954077427, -18.09477374809248928 ) ) ;
#25271=CARTESIAN_POINT ( 'NONE',  ( 118.1285681442453068, -2.084020599724406786, -8.691656652584148546 ) ) ;
#25273=CARTESIAN_POINT ( 'NONE',  ( 122.5532481442453019, 0.4262465694468514643, -12.03445270309931736 ) ) ;
#25276=CARTESIAN_POINT ( 'NONE',  ( 123.4041481442452834, 0.1319031606808879209, -14.10382304977623669 ) ) ;
#25277=CARTESIAN_POINT ( 'NONE',  ( 114.1009748109119784, -4.089484607189486809, -7.948022111789456723 ) ) ;
#25278=CARTESIAN_POINT ( 'NONE',  ( 120.6245414775786458, -9.988377603198976828, -10.36322818467138340 ) ) ;
#25279=CARTESIAN_POINT ( 'NONE',  ( 126.6375681442452930, -10.15424416112533912, -14.75197769757731336 ) ) ;
#25281=CARTESIAN_POINT ( 'NONE',  ( 122.3263414775786373, -3.505236298600246325, -18.68346056562440793 ) ) ;
#25283=CARTESIAN_POINT ( 'NONE',  ( 119.4332814775786318, -0.4660016031367893996, -10.09054647747474043 ) ) ;
#25287=CARTESIAN_POINT ( 'NONE',  ( 115.2922348109119781, 0.4262465694468551280, -12.03445270309932269 ) ) ;
#25292=CARTESIAN_POINT ( 'NONE',  ( 128.2184548109119930, -1.889072916127989776, -18.60376373290417362 ) ) ;
#25293=CARTESIAN_POINT ( 'NONE',  ( 121.3052614775786111, -7.643976991954077427, -18.09477374809248928 ) ) ;
#25301=CARTESIAN_POINT ( 'NONE',  ( 114.3278814775786429, -10.30919188438810075, -12.61870101168855918 ) ) ;
#25302=CARTESIAN_POINT ( 'NONE',  ( 115.5191414775786569, -3.383040157471821630, -19.15922257007629170 ) ) ;
#25303=CARTESIAN_POINT ( 'NONE',  ( 126.2404814775786264, -9.261995988541697145, -16.69588392320189030 ) ) ;
#25304=CARTESIAN_POINT ( 'NONE',  ( 119.1496481442453046, -6.222761293078241884, -8.102969835052219238 ) ) ;
#25306=CARTESIAN_POINT ( 'NONE',  ( 121.5888948109119809, -10.30919188438810075, -12.61870101168855918 ) ) ;
#25307=CARTESIAN_POINT ( 'NONE',  ( 111.7751814775786556, -2.084020599724406786, -8.691656652584148546 ) ) ;
#25310=CARTESIAN_POINT ( 'NONE',  ( 112.7395348109119766, -5.638512984488999180, -18.83840828888717311 ) ) ;
#25314=CARTESIAN_POINT ( 'NONE',  ( 119.2063748109119814, -1.561330072975668504, -17.79121239304076951 ) ) ;
#25315=CARTESIAN_POINT ( 'NONE',  ( 137.4478226697684136, -9.171749513548395072, -16.06665655585063135 ) ) ;
#25318=CARTESIAN_POINT ( 'NONE',  ( 111.7751814775786556, -7.893985811506177619, -18.51759400769804742 ) ) ;
#25321=CARTESIAN_POINT ( 'NONE',  ( 124.8223148109119762, 0.9020085738987339008, -11.91225656197089222 ) ) ;
#25323=CARTESIAN_POINT ( 'NONE',  ( 123.6310548109119765, -4.153390946401325223, -8.397313243818185668 ) ) ;
#25325=CARTESIAN_POINT ( 'NONE',  ( 118.4689281442453392, 0.9020085738987339008, -11.91225656197089222 ) ) ;
#25329=CARTESIAN_POINT ( 'NONE',  ( 137.2352176311223673, -5.000847779533773796, -8.118415127113269847 ) ) ;
#25330=CARTESIAN_POINT ( 'NONE',  ( 125.4463081442452932, -5.638512984488999180, -18.83840828888717311 ) ) ;
#25333=CARTESIAN_POINT ( 'NONE',  ( 124.8223148109119762, 0.9020085738987339008, -11.91225656197089222 ) ) ;
#25334=CARTESIAN_POINT ( 'NONE',  ( 123.0070614775786169, -10.15424416112533912, -14.75197769757731336 ) ) ;
#25336=CARTESIAN_POINT ( 'NONE',  ( 121.8725281442453223, -6.222761293078241884, -8.102969835052219238 ) ) ;
#25337=CARTESIAN_POINT ( 'NONE',  ( 112.6260814775786514, -0.8288870151387760510, -10.36305467784173118 ) ) ;
#25338=CARTESIAN_POINT ( 'NONE',  ( 119.6601881442453106, -8.166667518702819706, -8.995218007635861213 ) ) ;
#25340=ORIENTED_EDGE ( 'NONE', *, *, #42891, .T. ) ;
#25342=CARTESIAN_POINT ( 'NONE',  ( 125.6732148109119862, -9.859900752359514797, -12.68260735090137459 ) ) ;
#25345=CARTESIAN_POINT ( 'NONE',  ( 125.0492214775786408, -3.505236298599212041, -18.68346056562414859 ) ) ;
#25346=CARTESIAN_POINT ( 'NONE',  ( 115.4056881442453459, -7.893985811506177619, -18.51759400769804742 ) ) ;
#25347=VERTEX_POINT ( 'NONE', #2262 ) ;
#25348=CARTESIAN_POINT ( 'NONE',  ( 112.1722681442453222, -8.899110576539710493, -16.42337572283490132 ) ) ;
#25354=CARTESIAN_POINT ( 'NONE',  ( 115.3489614775786407, -9.261995988541697145, -16.69588392320189030 ) ) ;
#25360=CARTESIAN_POINT ( 'NONE',  ( 119.7736414775786358, 0.1319031606808879209, -14.10382304977623669 ) ) ;
#25361=CARTESIAN_POINT ( 'NONE',  ( 115.6325948109119821, 0.2603800115204892296, -16.42320221600525088 ) ) ;
#25363=CARTESIAN_POINT ( 'NONE',  ( 124.4252281442452812, -0.8288870151387760510, -10.36305467784173118 ) ) ;
#25364=CARTESIAN_POINT ( 'NONE',  ( 118.1852948109119836, -4.153390946401325223, -8.397313243818185668 ) ) ;
#25365=CARTESIAN_POINT ( 'NONE',  ( 116.0296814775786345, -1.833838273342658809, -17.42832698103878286 ) ) ;
#25366=ORIENTED_EDGE ( 'NONE', *, *, #42558, .T. ) ;
#25369=CARTESIAN_POINT ( 'NONE',  ( 118.9227414775786542, 0.4262465694468514643, -12.03445270309931736 ) ) ;
#25374=CARTESIAN_POINT ( 'NONE',  ( 114.0442481442453300, -1.834011780172310813, -8.268836392978581529 ) ) ;
#25376=FACE_OUTER_BOUND ( 'NONE', #1776, .T. ) ;
#25379=CARTESIAN_POINT ( 'NONE',  ( 121.7590748109119687, -2.084020599724406786, -8.691656652584148546 ) ) ;
#25381=CARTESIAN_POINT ( 'NONE',  ( 115.7460481442453357, -10.15424416112533912, -14.75197769757731336 ) ) ;
#25389=CARTESIAN_POINT ( 'NONE',  ( 112.0588148109119828, 0.5811942927096154232, -14.16772938898807155 ) ) ;
#25390=CARTESIAN_POINT ( 'NONE',  ( 125.4463081442452932, -4.153390946401325223, -8.397313243818185668 ) ) ;
#25391=CARTESIAN_POINT ( 'NONE',  ( 121.3052614775786111, -7.643976991954077427, -18.09477374809248928 ) ) ;
#25394=CARTESIAN_POINT ( 'NONE',  ( 121.3619881442452879, -5.574606645277164318, -18.38911715685844683 ) ) ;
#25396=CARTESIAN_POINT ( 'NONE',  ( 114.1961422310133685, -1.244021962887382315, -16.96476564598603787 ) ) ;
#25398=CARTESIAN_POINT ( 'NONE',  ( 116.8238548109119819, -4.089484607189486809, -7.948022111789456723 ) ) ;
#25400=CARTESIAN_POINT ( 'NONE',  ( 115.9162281442453235, -4.089484607189486809, -7.948022111789456723 ) ) ;
#25403=CARTESIAN_POINT ( 'NONE',  ( 117.0507614775786465, -10.30919188438810075, -12.61870101168855918 ) ) ;
#25404=CARTESIAN_POINT ( 'NONE',  ( 116.1998614775786507, -10.63000616557722466, -14.87417383870573495 ) ) ;
#25405=CARTESIAN_POINT ( 'NONE',  ( 125.6732148109119862, -9.859900752359378018, -12.68260735090039759 ) ) ;
#25408=ORIENTED_EDGE ( 'NONE', *, *, #19220, .F. ) ;
#25411=CARTESIAN_POINT ( 'NONE',  ( 119.4900081442453086, -7.643976991954077427, -18.09477374809248928 ) ) ;
#25416=CARTESIAN_POINT ( 'NONE',  ( 115.2355081442453155, 0.1319031606808879209, -14.10382304977623669 ) ) ;
#25418=CARTESIAN_POINT ( 'NONE',  ( 122.1561614775786353, -0.4660016031367893996, -10.09054647747474043 ) ) ;
#25419=CARTESIAN_POINT ( 'NONE',  ( 118.9794681442453026, -9.261995988541697145, -16.69588392320189030 ) ) ;
#25422=CARTESIAN_POINT ( 'NONE',  ( 119.7169148109119874, -0.1624402480850797581, -16.17319339645315424 ) ) ;
#25423=CARTESIAN_POINT ( 'NONE',  ( 126.1270281442452870, -10.30919188438810075, -12.61870101168855918 ) ) ;
#25424=CARTESIAN_POINT ( 'NONE',  ( 117.3911214775786505, -1.561330072975668504, -17.79121239304076951 ) ) ;
#25425=CARTESIAN_POINT ( 'NONE',  ( 121.1918081442452859, -10.15424416112533912, -14.75197769757731336 ) ) ;
#25427=CARTESIAN_POINT ( 'NONE',  ( 124.4252281442452812, -0.8288870151387760510, -10.36305467784173118 ) ) ;
#25428=CARTESIAN_POINT ( 'NONE',  ( 120.7947214775786193, -9.261995988541697145, -16.69588392320189030 ) ) ;
#25430=CARTESIAN_POINT ( 'NONE',  ( 137.0998855943435615, 0.2258552152529801627, -15.16215999076406362 ) ) ;
#25436=CARTESIAN_POINT ( 'NONE',  ( 117.6180281442453150, -0.4660016031367893996, -10.09054647747474043 ) ) ;
#25440=CARTESIAN_POINT ( 'NONE',  ( 116.8805814775786445, -3.505236298600246325, -18.68346056562440793 ) ) ;
#25444=CARTESIAN_POINT ( 'NONE',  ( 122.2173036525449987, -2.378957183258595176, -17.95140958770220863 ) ) ;
#25448=CARTESIAN_POINT ( 'NONE',  ( 119.0361948109119652, -7.893985811506177619, -18.51759400769804742 ) ) ;
#25449=CARTESIAN_POINT ( 'NONE',  ( 118.6958348109119754, -3.505236298600246325, -18.68346056562440793 ) ) ;
#25450=CARTESIAN_POINT ( 'NONE',  ( 113.7606148109119886, -7.894159318335828068, -9.358103419637847864 ) ) ;
#25452=CARTESIAN_POINT ( 'NONE',  ( 135.3184548109119874, -7.067465109756605912, -7.812468278694988832 ) ) ;
#25453=CARTESIAN_POINT ( 'NONE',  ( 123.7445081442452874, -1.561330072975668948, -17.79121239304076951 ) ) ;
#25455=CARTESIAN_POINT ( 'NONE',  ( 119.8870948109119752, -0.8288870151387760510, -10.36305467784173118 ) ) ;
#25456=CARTESIAN_POINT ( 'NONE',  ( 121.1350814775786233, -9.859900752359378018, -12.68260735090039759 ) ) ;
#25457=CARTESIAN_POINT ( 'NONE',  ( 118.0151148109119816, 0.4262465694468514643, -12.03445270309931736 ) ) ;
#25460=CARTESIAN_POINT ( 'NONE',  ( 124.0848681442452772, -5.574606645277164318, -18.38911715685844683 ) ) ;
#25461=CARTESIAN_POINT ( 'NONE',  ( 123.5743281442453139, -2.084020599724406786, -8.691656652584148546 ) ) ;
#25468=CARTESIAN_POINT ( 'NONE',  ( 117.7882081442453170, -6.344957434206665248, -7.627207830600338134 ) ) ;
#25469=CARTESIAN_POINT ( 'NONE',  ( 120.1707281442453166, 0.2603800115204892296, -16.42320221600525088 ) ) ;
#25471=CARTESIAN_POINT ( 'NONE',  ( 113.6471614775786492, -5.638512984488999180, -18.83840828888717311 ) ) ;
#25474=CARTESIAN_POINT ( 'NONE',  ( 118.0151148109119816, -10.63000616557722466, -14.87417383870573495 ) ) ;
#25476=CARTESIAN_POINT ( 'NONE',  ( 120.5110881442453206, -3.505236298600246325, -18.68346056562440793 ) ) ;
#25477=CARTESIAN_POINT ( 'NONE',  ( 114.7249681442453237, -9.565557343593413364, -10.61323700422348004 ) ) ;
#25478=CARTESIAN_POINT ( 'NONE',  ( 121.6456214775786293, -10.63000616557722466, -14.87417383870573495 ) ) ;
#25482=CARTESIAN_POINT ( 'NONE',  ( 115.0086014775786509, -5.574606645277164318, -18.38911715685844683 ) ) ;
#25488=CARTESIAN_POINT ( 'NONE',  ( 117.6180281442453150, -0.4660016031367893996, -10.09054647747474043 ) ) ;
#25489=ORIENTED_EDGE ( 'NONE', *, *, #7813, .F. ) ;
#25490=CARTESIAN_POINT ( 'NONE',  ( 125.1309504620138284, -2.495269033102075262, -17.79652296963211455 ) ) ;
#25493=CARTESIAN_POINT ( 'NONE',  ( 114.5547881442453217, -4.153390946401321671, -8.397313243818183892 ) ) ;
#25495=CARTESIAN_POINT ( 'NONE',  ( 123.9210066692503602, -2.311015703046761072, -18.04188382666269774 ) ) ;
#25496=CARTESIAN_POINT ( 'NONE',  ( 123.9146881442452894, -10.15424416112533912, -14.75197769757731336 ) ) ;
#25498=CARTESIAN_POINT ( 'NONE',  ( 119.9438214775786378, -2.084020599724406786, -8.691656652584148546 ) ) ;
#25501=CARTESIAN_POINT ( 'NONE',  ( 123.9714148109119805, -8.899110576539710493, -16.42337572283490132 ) ) ;
#25502=CARTESIAN_POINT ( 'NONE',  ( 113.3068014775786594, -8.166667518702817929, -8.995218007635859436 ) ) ;
#25503=CARTESIAN_POINT ( 'NONE',  ( 117.7882081442453170, -6.344957434206665248, -7.627207830600338134 ) ) ;
#25504=CARTESIAN_POINT ( 'NONE',  ( 112.4559014775786494, -9.988377603198976828, -10.36322818467138340 ) ) ;
#25506=CARTESIAN_POINT ( 'NONE',  ( 121.7023481442452919, -0.8288870151387760510, -10.36305467784173118 ) ) ;
#25508=CARTESIAN_POINT ( 'NONE',  ( 122.2696148109119889, -4.089484607189486809, -7.948022111789456723 ) ) ;
#25513=CARTESIAN_POINT ( 'NONE',  ( 138.1290508867525659, -3.202662983232241523, -16.85452216123445623 ) ) ;
#25517=CARTESIAN_POINT ( 'NONE',  ( 119.9438214775786378, -2.084020599724406786, -8.691656652584148546 ) ) ;
#25520=CARTESIAN_POINT ( 'NONE',  ( 125.2761281442453054, -10.63000616557722466, -14.87417383870573495 ) ) ;
#25523=CARTESIAN_POINT ( 'NONE',  ( 116.0864081442453113, -9.988377603198976828, -10.36322818467138340 ) ) ;
#25525=CARTESIAN_POINT ( 'NONE',  ( 121.3619881442452879, -5.574606645277164318, -18.38911715685844683 ) ) ;
#25526=CARTESIAN_POINT ( 'NONE',  ( 112.6828081442453282, -2.084020599724406786, -8.691656652584148546 ) ) ;
#25528=CARTESIAN_POINT ( 'NONE',  ( 123.6877814775786675, -6.222761293078255207, -8.102969835052217462 ) ) ;
#25531=CARTESIAN_POINT ( 'NONE',  ( 125.1626748109119802, -0.1624402480850797581, -16.17319339645315424 ) ) ;
#25535=CARTESIAN_POINT ( 'NONE',  ( 121.8158014775786171, -5.638512984488999180, -18.83840828888717311 ) ) ;
#25536=CARTESIAN_POINT ( 'NONE',  ( 137.5082292857711082, -8.696096796519196204, -16.61830971866196549 ) ) ;
#25537=ORIENTED_EDGE ( 'NONE', *, *, #37021, .T. ) ;
#25538=CARTESIAN_POINT ( 'NONE',  ( 136.7036351578996403, 0.3218787459907788695, -11.14856471978897190 ) ) ;
#25539=CARTESIAN_POINT ( 'NONE',  ( 125.1059481442452750, -8.166667518702819706, -8.995218007635861213 ) ) ;
#25541=CARTESIAN_POINT ( 'NONE',  ( 122.3830681442452857, -1.833838273342659697, -17.42832698103878286 ) ) ;
#25542=ORIENTED_EDGE ( 'NONE', *, *, #43174, .T. ) ;
#25544=CARTESIAN_POINT ( 'NONE',  ( 119.0361948109119652, -7.893985811506177619, -18.51759400769804742 ) ) ;
#25545=CARTESIAN_POINT ( 'NONE',  ( 116.6991193335884418, -2.334846009198389805, -18.01015021110788439 ) ) ;
#25548=CARTESIAN_POINT ( 'NONE',  ( 136.5278073585037077, -5.459964313008185854, -7.687332562961293192 ) ) ;
#25549=CARTESIAN_POINT ( 'NONE',  ( 125.7299414775786346, 0.9020085738987339008, -11.91225656197089222 ) ) ;
#25551=FACE_OUTER_BOUND ( 'NONE', #10625, .T. ) ;
#25552=CARTESIAN_POINT ( 'NONE',  ( 125.4463081442452932, -5.638512984488999180, -18.83840828888717311 ) ) ;
#25553=CARTESIAN_POINT ( 'NONE',  ( 113.4202548109119846, -10.30919188438810075, -12.61870101168855918 ) ) ;
#25555=CARTESIAN_POINT ( 'NONE',  ( 122.9503348109119827, -9.859900752359378018, -12.68260735090039759 ) ) ;
#25557=CARTESIAN_POINT ( 'NONE',  ( 120.0572748109119772, -3.383040157471821630, -19.15922257007629170 ) ) ;
#25558=CARTESIAN_POINT ( 'NONE',  ( 126.2184548109090940, -8.862178061931365036, -16.39564131203211517 ) ) ;
#25563=CARTESIAN_POINT ( 'NONE',  ( 124.8790414775786388, -8.899110576539117190, -16.42337572283568647 ) ) ;
#25564=CARTESIAN_POINT ( 'NONE',  ( 114.7816948109119863, 0.5811942927096154232, -14.16772938898807155 ) ) ;
#25566=CARTESIAN_POINT ( 'NONE',  ( 116.4834948109119779, -7.894159318335828068, -9.358103419637847864 ) ) ;
#25574=CARTESIAN_POINT ( 'NONE',  ( 116.7671281442453335, -1.834011780172310813, -8.268836392978581529 ) ) ;
#25580=CARTESIAN_POINT ( 'NONE',  ( 120.3409081442453044, -8.899110576539710493, -16.42337572283490132 ) ) ;
#25581=CARTESIAN_POINT ( 'NONE',  ( 116.9940348109119839, -9.988377603198976828, -10.36322818467138340 ) ) ;
#25582=CARTESIAN_POINT ( 'NONE',  ( 112.7395348109119766, -5.638512984488999180, -18.83840828888717311 ) ) ;
#25584=CARTESIAN_POINT ( 'NONE',  ( 125.1626748109119802, -0.1624402480850797581, -16.17319339645315424 ) ) ;
#25585=CARTESIAN_POINT ( 'NONE',  ( 122.2696148109119889, -5.574606645277164318, -18.38911715685844683 ) ) ;
#25586=CARTESIAN_POINT ( 'NONE',  ( 114.9518748109119883, -7.643976991954077427, -18.09477374809248928 ) ) ;
#25587=ORIENTED_EDGE ( 'NONE', *, *, #23099, .T. ) ;
#25590=CARTESIAN_POINT ( 'NONE',  ( 118.0718414775786442, -0.8288870151387760510, -10.36305467784173118 ) ) ;
#25593=CARTESIAN_POINT ( 'NONE',  ( 116.5969481442453031, 0.5811942927096154232, -14.16772938898807155 ) ) ;
#25595=CARTESIAN_POINT ( 'NONE',  ( 112.2289948109119848, -7.643976991954077427, -18.09477374809248928 ) ) ;
#25597=ORIENTED_EDGE ( 'NONE', *, *, #19748, .T. ) ;
#25600=CARTESIAN_POINT ( 'NONE',  ( 123.7445081442452874, -7.894159318335828068, -9.358103419637847864 ) ) ;
#25601=CARTESIAN_POINT ( 'NONE',  ( 116.6536748109119941, -10.15424416112533912, -14.75197769757731336 ) ) ;
#25604=CARTESIAN_POINT ( 'NONE',  ( 116.4834948109119779, -7.894159318335808528, -9.358103419637833653 ) ) ;
#25611=CARTESIAN_POINT ( 'NONE',  ( 114.9518748109119883, -1.834011780172310813, -8.268836392978581529 ) ) ;
#25612=CARTESIAN_POINT ( 'NONE',  ( 125.8433948109119456, -7.643976991954077427, -18.09477374809248928 ) ) ;
#25613=CARTESIAN_POINT ( 'NONE',  ( 120.7379948109119709, 0.4262465694468514643, -12.03445270309931736 ) ) ;
#25616=CARTESIAN_POINT ( 'NONE',  ( 121.3052614775786111, -7.643976991954077427, -18.09477374809248928 ) ) ;
#25620=CARTESIAN_POINT ( 'NONE',  ( 116.5026997424434114, -0.9924539043446216624, -17.29976612834909133 ) ) ;
#25622=CARTESIAN_POINT ( 'NONE',  ( 120.2274548109119934, 0.5811942927096110934, -14.16772938898807510 ) ) ;
#25625=CARTESIAN_POINT ( 'NONE',  ( 116.8238548109119819, -4.089484607189486809, -7.948022111789456723 ) ) ;
#25628=CARTESIAN_POINT ( 'NONE',  ( 115.6325948109119821, 0.2603800115204892296, -16.42320221600525088 ) ) ;
#25631=CARTESIAN_POINT ( 'NONE',  ( 116.8805814775786445, -6.344957434206662583, -7.627207830600332805 ) ) ;
#25638=CARTESIAN_POINT ( 'NONE',  ( 119.4332814775786318, -8.899110576539710493, -16.42337572283490132 ) ) ;
#25642=CARTESIAN_POINT ( 'NONE',  ( 114.3846081442453197, 0.4262465694468514643, -12.03445270309931736 ) ) ;
#25644=CARTESIAN_POINT ( 'NONE',  ( 124.9357681442453014, -1.834011780172310813, -8.268836392978581529 ) ) ;
#25645=CARTESIAN_POINT ( 'NONE',  ( 121.4187148109119789, -6.344957434206665248, -7.627207830600338134 ) ) ;
#25647=CARTESIAN_POINT ( 'NONE',  ( 117.5613014775786525, -10.15424416112533912, -14.75197769757731336 ) ) ;
#25648=CARTESIAN_POINT ( 'NONE',  ( 113.1366214775786432, -1.834011780172310813, -8.268836392978581529 ) ) ;
#25649=CARTESIAN_POINT ( 'NONE',  ( 120.5678148109119832, -8.166667518702819706, -8.995218007635861213 ) ) ;
#25650=CARTESIAN_POINT ( 'NONE',  ( 119.0929214775786278, -4.153390946401325223, -8.397313243818185668 ) ) ;
#25651=ORIENTED_EDGE ( 'NONE', *, *, #4716, .F. ) ;
#25653=CARTESIAN_POINT ( 'NONE',  ( 121.6456214775786293, -10.63000616557722466, -14.87417383870573495 ) ) ;
#25657=CARTESIAN_POINT ( 'NONE',  ( 126.9675933030687531, 0.5041375662892478848, -13.12963104399455894 ) ) ;
#25661=CARTESIAN_POINT ( 'NONE',  ( 114.8951481442453115, -8.899110576539710493, -16.42337572283490132 ) ) ;
#25662=CARTESIAN_POINT ( 'NONE',  ( 124.1983214775786166, -8.166667518702819706, -8.995218007635861213 ) ) ;
#25667=CARTESIAN_POINT ( 'NONE',  ( 112.5693548109119888, 0.4262465694468514643, -12.03445270309931736 ) ) ;
#25671=CARTESIAN_POINT ( 'NONE',  ( 121.0216281442452981, -1.561330072975668948, -17.79121239304076951 ) ) ;
#25672=CARTESIAN_POINT ( 'NONE',  ( 124.3117748109119844, 0.1319031606808879209, -14.10382304977623669 ) ) ;
#25674=CARTESIAN_POINT ( 'NONE',  ( 136.7478768735679751, -9.183261188161861099, -9.792427337551218969 ) ) ;
#25677=CARTESIAN_POINT ( 'NONE',  ( 117.5613014775786525, -10.15424416112533912, -14.75197769757731336 ) ) ;
#25678=CARTESIAN_POINT ( 'NONE',  ( 122.4397948109119767, -0.1624402480850797581, -16.17319339645315424 ) ) ;
#25679=CARTESIAN_POINT ( 'NONE',  ( 116.7671281442453335, -7.643976991954077427, -18.09477374809248928 ) ) ;
#25680=CARTESIAN_POINT ( 'NONE',  ( 120.7335793026122701, -1.179503403430468333, -17.05068175419387089 ) ) ;
#25682=CARTESIAN_POINT ( 'NONE',  ( 123.6877814775786533, -6.222761293078241884, -8.102969835052219238 ) ) ;
#25683=CARTESIAN_POINT ( 'NONE',  ( 122.9503348109119827, -9.859900752359378018, -12.68260735090039759 ) ) ;
#25690=CARTESIAN_POINT ( 'NONE',  ( 122.4965214775786251, -10.30919188438810075, -12.61870101168855918 ) ) ;
#25691=CARTESIAN_POINT ( 'NONE',  ( 117.1074881442453233, -10.63000616557722466, -14.87417383870573495 ) ) ;
#25694=CARTESIAN_POINT ( 'NONE',  ( 111.7184548109119788, -9.261995988541697145, -16.69588392320189030 ) ) ;
#25698=CARTESIAN_POINT ( 'NONE',  ( 115.0653281442453277, -6.344957434206662583, -7.627207830600332805 ) ) ;
#25699=CARTESIAN_POINT ( 'NONE',  ( 123.9146881442452894, -10.15424416112533912, -14.75197769757731336 ) ) ;
#25701=CARTESIAN_POINT ( 'NONE',  ( 114.6682414775786469, -7.894159318335828068, -9.358103419637847864 ) ) ;
#25702=CARTESIAN_POINT ( 'NONE',  ( 120.1140014775786398, -1.561330072975668504, -17.79121239304076951 ) ) ;
#25706=CARTESIAN_POINT ( 'NONE',  ( 118.8092881442453290, -0.1624402480850797581, -16.17319339645315424 ) ) ;
#25711=CARTESIAN_POINT ( 'NONE',  ( 118.4689281442453392, 0.9020085738987339008, -11.91225656197089222 ) ) ;
#25713=CARTESIAN_POINT ( 'NONE',  ( 125.3895814775786448, -2.084020599724406786, -8.691656652584148546 ) ) ;
#25716=CARTESIAN_POINT ( 'NONE',  ( 119.6601881442453106, -1.833838273342659253, -17.42832698103878286 ) ) ;
#25719=CARTESIAN_POINT ( 'NONE',  ( 122.4965214775786251, 0.1319031606808879209, -14.10382304977623669 ) ) ;
#25720=CARTESIAN_POINT ( 'NONE',  ( 121.6456214775786435, -10.63000616557722999, -14.87417383870568877 ) ) ;
#25722=CARTESIAN_POINT ( 'NONE',  ( 125.3895814775786448, -2.084020599724406786, -8.691656652584148546 ) ) ;
#25724=CARTESIAN_POINT ( 'NONE',  ( 117.7314814775786260, -5.574606645277164318, -18.38911715685844683 ) ) ;
#25725=CARTESIAN_POINT ( 'NONE',  ( 122.7234281442452755, -4.153390946401325223, -8.397313243818185668 ) ) ;
#25726=CARTESIAN_POINT ( 'NONE',  ( 114.6115148109119986, -3.383040157471821630, -19.15922257007629170 ) ) ;
#25727=CARTESIAN_POINT ( 'NONE',  ( 121.0783548109119749, 0.2603800115204892296, -16.42320221600525088 ) ) ;
#25728=CARTESIAN_POINT ( 'NONE',  ( 116.9373081442452929, -8.166667518702817929, -8.995218007635861213 ) ) ;
#25730=CARTESIAN_POINT ( 'NONE',  ( 123.8579614775786126, -9.859900752359378018, -12.68260735090039759 ) ) ;
#25732=CARTESIAN_POINT ( 'NONE',  ( 119.1496481442453046, -3.383040157471821630, -19.15922257007629170 ) ) ;
#25737=CARTESIAN_POINT ( 'NONE',  ( 114.6682414775786469, -7.894159318335828068, -9.358103419637847864 ) ) ;
#25740=CARTESIAN_POINT ( 'NONE',  ( 126.0703014775786102, -9.988377603198980381, -10.36322818467138518 ) ) ;
#25742=CARTESIAN_POINT ( 'NONE',  ( 122.6099748109119929, -0.8288870151387760510, -10.36305467784173118 ) ) ;
#25747=ORIENTED_EDGE ( 'NONE', *, *, #33171, .F. ) ;
#25748=CARTESIAN_POINT ( 'NONE',  ( 114.6115148109119986, -3.383040157471821630, -19.15922257007629170 ) ) ;
#25749=CARTESIAN_POINT ( 'NONE',  ( 125.5030348109119558, -3.383040157471821630, -19.15922257007629170 ) ) ;
#25750=CARTESIAN_POINT ( 'NONE',  ( 119.0361948109119652, -2.084020599724406786, -8.691656652584148546 ) ) ;
#25754=CARTESIAN_POINT ( 'NONE',  ( 124.6329298793804981, -2.191907684172563986, -18.20049396185734025 ) ) ;
#25759=CARTESIAN_POINT ( 'NONE',  ( 121.0216281442452981, -1.561330072975668948, -17.79121239304076951 ) ) ;
#25760=CARTESIAN_POINT ( 'NONE',  ( 137.0596819398251967, -9.757506281569700235, -15.72392196484829974 ) ) ;
#25762=CARTESIAN_POINT ( 'NONE',  ( 115.6325948109119821, 0.2603800115204892296, -16.42320221600525088 ) ) ;
#25763=CARTESIAN_POINT ( 'NONE',  ( 111.6050014775786536, 0.1319031606808879209, -14.10382304977623669 ) ) ;
#25765=CARTESIAN_POINT ( 'NONE',  ( 121.8725281442453223, -6.222761293078241884, -8.102969835052219238 ) ) ;
#25768=CARTESIAN_POINT ( 'NONE',  ( 118.8092881442453290, -9.988377603198976828, -10.36322818467138340 ) ) ;
#25773=CARTESIAN_POINT ( 'NONE',  ( 114.3278814775786429, 0.1319031606808879209, -14.10382304977623669 ) ) ;
#25776=CARTESIAN_POINT ( 'NONE',  ( 111.4348214775786801, -3.505236298600246325, -18.68346056562440793 ) ) ;
#25777=CARTESIAN_POINT ( 'NONE',  ( 125.6164881442453094, -9.565557343593413364, -10.61323700422348004 ) ) ;
#25778=CARTESIAN_POINT ( 'NONE',  ( 122.8560864091100768, -0.9924539043446216624, -17.29976612834909133 ) ) ;
#25779=CARTESIAN_POINT ( 'NONE',  ( 122.7234281442452755, -4.153390946401325223, -8.397313243818185668 ) ) ;
#25781=CARTESIAN_POINT ( 'NONE',  ( 120.7379948109119709, -10.63000616557722466, -14.87417383870573495 ) ) ;
#25783=CARTESIAN_POINT ( 'NONE',  ( 125.7866681442453256, -8.899110576539117190, -16.42337572283568647 ) ) ;
#25786=CARTESIAN_POINT ( 'NONE',  ( 125.6626748109119802, -9.522524984348629928, -10.63868154973292413 ) ) ;
#25787=CARTESIAN_POINT ( 'NONE',  ( 115.0653281442453277, -6.344957434206662583, -7.627207830600332805 ) ) ;
#25790=CARTESIAN_POINT ( 'NONE',  ( 119.5918314802850091, -3.929494816604741203, -18.62311481910882804 ) ) ;
#25791=CARTESIAN_POINT ( 'NONE',  ( 126.1837548109119211, -10.63000616557722466, -14.87417383870573495 ) ) ;
#25793=CARTESIAN_POINT ( 'NONE',  ( 112.3424481442453384, -6.344957434206662583, -7.627207830600332805 ) ) ;
#25794=CARTESIAN_POINT ( 'NONE',  ( 120.6812681442452941, -10.30919188438810075, -12.61870101168855918 ) ) ;
#25799=CARTESIAN_POINT ( 'NONE',  ( 118.4122014775786340, -9.859900752359374465, -12.68260735090039404 ) ) ;
#25800=CARTESIAN_POINT ( 'NONE',  ( 116.0864081442453113, -9.988377603198976828, -10.36322818467138340 ) ) ;
#25801=CARTESIAN_POINT ( 'NONE',  ( 112.3424481442453384, -6.344957434206662583, -7.627207830600332805 ) ) ;
#25802=CARTESIAN_POINT ( 'NONE',  ( 123.9714148109119805, -8.899110576539710493, -16.42337572283490132 ) ) ;
#25803=CARTESIAN_POINT ( 'NONE',  ( 124.4252281442452812, -0.8288870151387760510, -10.36305467784173118 ) ) ;
#25804=CARTESIAN_POINT ( 'NONE',  ( 116.5969481442453031, -9.859900752359374465, -12.68260735090039404 ) ) ;
#25809=CARTESIAN_POINT ( 'NONE',  ( 118.0151148109119816, 0.4262465694468514643, -12.03445270309931736 ) ) ;
#25811=CARTESIAN_POINT ( 'NONE',  ( 126.9733055311764502, -9.698541571718097387, -15.74778416720804763 ) ) ;
#25812=CARTESIAN_POINT ( 'NONE',  ( 114.3846081442453197, -10.63000616557722466, -14.87417383870573495 ) ) ;
#25814=CARTESIAN_POINT ( 'NONE',  ( 114.3846081442453197, 0.4262465694468514643, -12.03445270309931736 ) ) ;
#25816=EDGE_LOOP ( 'NONE', ( #42303, #32779, #4059, #23370, #31135 ) ) ;
#25817=CARTESIAN_POINT ( 'NONE',  ( 121.0783548109119749, -9.565557343593413364, -10.61323700422348004 ) ) ;
#25818=CARTESIAN_POINT ( 'NONE',  ( 115.8027748109119841, -8.899110576539710493, -16.42337572283490132 ) ) ;
#25822=CARTESIAN_POINT ( 'NONE',  ( 112.1721994132789320, -8.900630651041904429, -16.42135045828372597 ) ) ;
#25825=CARTESIAN_POINT ( 'NONE',  ( 118.0151148109119816, -10.63000616557722466, -14.87417383870573495 ) ) ;
#25826=CARTESIAN_POINT ( 'NONE',  ( 114.8384214775786489, 0.9020085738987339008, -11.91225656197089222 ) ) ;
#25827=CARTESIAN_POINT ( 'NONE',  ( 115.0086014775786509, -5.574606645277164318, -18.38911715685844683 ) ) ;
#25828=CARTESIAN_POINT ( 'NONE',  ( 121.4187148109119789, -3.505236298600246325, -18.68346056562440793 ) ) ;
#25831=CARTESIAN_POINT ( 'NONE',  ( 118.9794681442453026, -0.8288870151387760510, -10.36305467784173118 ) ) ;
#25832=CARTESIAN_POINT ( 'NONE',  ( 124.0848681442452772, -5.574606645277164318, -18.38911715685844683 ) ) ;
#25837=CARTESIAN_POINT ( 'NONE',  ( 119.4332814775786318, -0.4660016031367893996, -10.09054647747474043 ) ) ;
#25839=CARTESIAN_POINT ( 'NONE',  ( 120.9649014775786355, -3.383040157471821630, -19.15922257007629170 ) ) ;
#25842=CARTESIAN_POINT ( 'NONE',  ( 117.7882081442453170, -6.344957434206665248, -7.627207830600338134 ) ) ;
#25843=CARTESIAN_POINT ( 'NONE',  ( 116.9940348109119839, -9.988377603198976828, -10.36322818467138340 ) ) ;
#25844=CARTESIAN_POINT ( 'NONE',  ( 125.7866681442452688, -8.899110576539710493, -16.42337572283490132 ) ) ;
#25851=CARTESIAN_POINT ( 'NONE',  ( 119.2063748109119814, -7.894159318335828068, -9.358103419637847864 ) ) ;
#25854=CARTESIAN_POINT ( 'NONE',  ( 114.9518748109119883, -7.643976991954077427, -18.09477374809248928 ) ) ;
#25858=CARTESIAN_POINT ( 'NONE',  ( 111.6617281442453304, 0.4262465694468514643, -12.03445270309931736 ) ) ;
#25859=CARTESIAN_POINT ( 'NONE',  ( 118.4689281442453392, 0.9020085738987339008, -11.91225656197089222 ) ) ;
#25860=VERTEX_POINT ( 'NONE', #40375 ) ;
#25862=CARTESIAN_POINT ( 'NONE',  ( 119.0361948109119652, -2.084020599724406786, -8.691656652584148546 ) ) ;
#25863=CARTESIAN_POINT ( 'NONE',  ( 115.2922348109119781, -10.63000616557722466, -14.87417383870573495 ) ) ;
#25864=CARTESIAN_POINT ( 'NONE',  ( 121.6456214775786293, -10.63000616557722466, -14.87417383870573495 ) ) ;
#25866=CARTESIAN_POINT ( 'NONE',  ( 119.7169148109119874, -0.1624402480850797581, -16.17319339645315424 ) ) ;
#25868=CARTESIAN_POINT ( 'NONE',  ( 124.2550481442452792, -0.1624402480850797581, -16.17319339645315424 ) ) ;
#25870=CARTESIAN_POINT ( 'NONE',  ( 121.3052614775786111, -1.834011780172310813, -8.268836392978581529 ) ) ;
#25872=CARTESIAN_POINT ( 'NONE',  ( 121.3052614775786111, -1.834011780172310813, -8.268836392978581529 ) ) ;
#25878=CARTESIAN_POINT ( 'NONE',  ( 138.1466326771052024, -2.059073704699106333, -15.87940239184555757 ) ) ;
#25881=CARTESIAN_POINT ( 'NONE',  ( 136.9394333025885260, -10.02432842090376575, -11.47584239480924495 ) ) ;
#25882=CARTESIAN_POINT ( 'NONE',  ( 115.7460481442453357, -10.15424416112533912, -14.75197769757731336 ) ) ;
#25883=CARTESIAN_POINT ( 'NONE',  ( 125.3895814775786448, -7.893985811506177619, -18.51759400769804742 ) ) ;
#25887=CARTESIAN_POINT ( 'NONE',  ( 115.8595014775786609, -7.643976991954077427, -18.09477374809248928 ) ) ;
#25891=CARTESIAN_POINT ( 'NONE',  ( 118.2987481442453088, -1.561330072975668504, -17.79121239304076951 ) ) ;
#25893=CARTESIAN_POINT ( 'NONE',  ( 121.9859814775786333, -9.565557343593413364, -10.61323700422348004 ) ) ;
#25896=CARTESIAN_POINT ( 'NONE',  ( 125.2761281442453054, -10.63000616557722466, -14.87417383870573495 ) ) ;
#25898=CARTESIAN_POINT ( 'NONE',  ( 122.4397948109119767, -0.1624402480850797581, -16.17319339645315424 ) ) ;
#25899=( BOUNDED_CURVE ( )  B_SPLINE_CURVE ( 2, ( #23173, #37052, #5823, #42296, #34751, #24302, #41637, #3533, #10393, #10835, #11284, #14475, #17896, #18120, #17449, #31344, #14031 ),
 .UNSPECIFIED., .F., .T. ) 
 B_SPLINE_CURVE_WITH_KNOTS ( ( 3, 2, 2, 2, 2, 2, 2, 2, 3 ),
 ( 0.5796282416568590001, 0.5859375000000000000, 0.5937500000000000000, 0.6015625000000000000, 0.6093750000000000000, 0.6171875000000000000, 0.6250000000000000000, 0.6328125000000000000, 0.6391217583431409999 ),
 .UNSPECIFIED. ) 
 CURVE ( )  GEOMETRIC_REPRESENTATION_ITEM ( )  RATIONAL_B_SPLINE_CURVE ( ( 0.9763430640195970289, 0.9385262470928680267, 1.000000000000000000, 0.9238795325112869605, 1.000000000000000000, 0.9238795325112869605, 1.000000000000000000, 0.9238795325112869605, 1.000000000000000000, 0.9238795325112869605, 1.000000000000000000, 0.9238795325112869605, 1.000000000000000000, 0.9238795325112869605, 1.000000000000000000, 0.9385262470928670275, 0.9763430640195980281 ) ) 
 REPRESENTATION_ITEM ( '' )  );
#25900=CARTESIAN_POINT ( 'NONE',  ( 122.8368814775786291, -7.894159318335828068, -9.358103419637847864 ) ) ;
#25901=CARTESIAN_POINT ( 'NONE',  ( 117.2209414775786485, -2.084020599724406786, -8.691656652584148546 ) ) ;
#25904=CARTESIAN_POINT ( 'NONE',  ( 125.2761281442453054, 0.4262465694468514643, -12.03445270309931736 ) ) ;
#25905=CARTESIAN_POINT ( 'NONE',  ( 123.7445081442452874, -7.894159318335828068, -9.358103419637847864 ) ) ;
#25912=CARTESIAN_POINT ( 'NONE',  ( 122.7801548109119665, -3.383040157471821630, -19.15922257007629170 ) ) ;
#25913=CARTESIAN_POINT ( 'NONE',  ( 116.9373081442452929, -8.166667518702817929, -8.995218007635861213 ) ) ;
#25915=CARTESIAN_POINT ( 'NONE',  ( 116.5402214775786405, 0.2603800115204892296, -16.42320221600525088 ) ) ;
#25918=DIRECTION ( 'NONE',  ( 0.000000000000000000, 0.6004852223388321697, -0.7996358532186279566 ) ) ;
#25921=CARTESIAN_POINT ( 'NONE',  ( 119.6034614775786196, -6.344957434206665248, -7.627207830600338134 ) ) ;
#25922=CARTESIAN_POINT ( 'NONE',  ( 126.0703014775786102, -0.1624402480850797581, -16.17319339645315424 ) ) ;
#25924=CARTESIAN_POINT ( 'NONE',  ( 113.6471614775786492, -4.153390946401321671, -8.397313243818183892 ) ) ;
#25925=CARTESIAN_POINT ( 'NONE',  ( 111.7751814775786556, -2.084020599724406786, -8.691656652584148546 ) ) ;
#25927=CARTESIAN_POINT ( 'NONE',  ( 121.8158014775786171, -4.153390946401325223, -8.397313243818185668 ) ) ;
#25932=ADVANCED_FACE ( 'NONE', ( #15193 ), #8798, .T. ) ;
#25934=CARTESIAN_POINT ( 'NONE',  ( 122.2696148109119889, -4.089484607189486809, -7.948022111789456723 ) ) ;
#25938=CARTESIAN_POINT ( 'NONE',  ( 117.9583881442453048, 0.1319031606808879209, -14.10382304977623669 ) ) ;
#25942=CARTESIAN_POINT ( 'NONE',  ( 124.0281414775786146, -7.643976991954077427, -18.09477374809248928 ) ) ;
#25943=CARTESIAN_POINT ( 'NONE',  ( 123.7245631242421382, -1.016270020561755860, -17.26805140881366896 ) ) ;
#25945=CARTESIAN_POINT ( 'NONE',  ( 124.4252281442452812, -0.8288870151387760510, -10.36305467784173118 ) ) ;
#25947=CARTESIAN_POINT ( 'NONE',  ( 124.1983214775786166, -8.166667518702819706, -8.995218007635861213 ) ) ;
#25948=CARTESIAN_POINT ( 'NONE',  ( 118.5256548109119876, -8.899110576539710493, -16.42337572283490132 ) ) ;
#25949=CARTESIAN_POINT ( 'NONE',  ( 122.6667014775786413, -2.084020599724406786, -8.691656652584148546 ) ) ;
#25950=CARTESIAN_POINT ( 'NONE',  ( 120.1140014775786398, -1.561330072975668504, -17.79121239304076951 ) ) ;
#25951=CARTESIAN_POINT ( 'NONE',  ( 116.0864081442453113, -9.988377603198976828, -10.36322818467138340 ) ) ;
#25953=CARTESIAN_POINT ( 'NONE',  ( 123.7445081442452874, -7.894159318335828068, -9.358103419637847864 ) ) ;
#25955=CARTESIAN_POINT ( 'NONE',  ( 120.4543614775786295, -4.089484607189486809, -7.948022111789456723 ) ) ;
#25959=CARTESIAN_POINT ( 'NONE',  ( 113.9875214775786532, -8.899110576539710493, -16.42337572283490132 ) ) ;
#25963=B_SPLINE_CURVE_WITH_KNOTS ( 'NONE', 3,
 ( #10420, #23887, #24543, #13832, #30483, #37998, #7199, #21112, #37771, #16819 ),
 .UNSPECIFIED., .F., .F.,
 ( 4, 3, 3, 4 ),
 ( 0.000000000000000000, 0.0001671877560958124893, 0.0003343755126086590075, 0.0006438490228505489759 ),
 .UNSPECIFIED. ) ;
#25965=CARTESIAN_POINT ( 'NONE',  ( 125.6732148109119862, -9.859900752359378018, -12.68260735090039759 ) ) ;
#25971=CARTESIAN_POINT ( 'NONE',  ( 114.7249681442453237, 0.2603800115204892296, -16.42320221600525088 ) ) ;
#25973=CARTESIAN_POINT ( 'NONE',  ( 124.1415948109119540, -3.505236298600246325, -18.68346056562440793 ) ) ;
#25974=CARTESIAN_POINT ( 'NONE',  ( 113.9307948109119764, -10.15424416112533912, -14.75197769757731336 ) ) ;
#25979=CARTESIAN_POINT ( 'NONE',  ( 113.8740681442453138, 0.5811942927096154232, -14.16772938898807155 ) ) ;
#25983=CARTESIAN_POINT ( 'NONE',  ( 123.9146881442452894, 0.9020085738987339008, -11.91225656197089222 ) ) ;
#25984=( BOUNDED_CURVE ( )  B_SPLINE_CURVE ( 2, ( #12791, #40604, #9592, #23272, #30787, #23508, #34192, #37393, #6400, #27372, #13471, #36930, #2738 ),
 .UNSPECIFIED., .F., .T. ) 
 B_SPLINE_CURVE_WITH_KNOTS ( ( 3, 2, 2, 2, 2, 2, 3 ),
 ( 0.8920046674808920217, 0.8984375000000000000, 0.9062500000000000000, 0.9140625000000000000, 0.9218750000000000000, 0.9296875000000000000, 0.9375000000000000000 ),
 .UNSPECIFIED. ) 
 CURVE ( )  GEOMETRIC_REPRESENTATION_ITEM ( )  RATIONAL_B_SPLINE_CURVE ( ( 0.9778625265006449796, 0.9373222120152220338, 1.000000000000000000, 0.9238795325112869605, 1.000000000000000000, 0.9238795325112869605, 1.000000000000000000, 0.9238795325112869605, 1.000000000000000000, 0.9238795325112869605, 1.000000000000000000, 0.9238795325112759693, 1.000000000000000000 ) ) 
 REPRESENTATION_ITEM ( '' )  );
#25985=CARTESIAN_POINT ( 'NONE',  ( 136.9115742440178281, -8.459698128447302068, -17.59059153831742961 ) ) ;
#25987=CARTESIAN_POINT ( 'NONE',  ( 112.9664414775786412, 0.5811942927096154232, -14.16772938898807155 ) ) ;
#25988=CARTESIAN_POINT ( 'NONE',  ( 125.7866681442452688, -0.4660016031367893996, -10.09054647747474043 ) ) ;
#25990=CARTESIAN_POINT ( 'NONE',  ( 125.3328548109119964, -0.8288870151387760510, -10.36305467784173118 ) ) ;
#25992=CARTESIAN_POINT ( 'NONE',  ( 117.7882081442453170, -6.344957434206665248, -7.627207830600338134 ) ) ;
#25997=CARTESIAN_POINT ( 'NONE',  ( 136.9115742440145880, -5.289448686423090074, -7.882678547363988208 ) ) ;
#25998=CARTESIAN_POINT ( 'NONE',  ( 113.1933481442453058, -5.574606645277164318, -18.38911715685844683 ) ) ;
#26002=CARTESIAN_POINT ( 'NONE',  ( 125.7866681442452688, -0.4660016031367893996, -10.09054647747474043 ) ) ;
#26003=CARTESIAN_POINT ( 'NONE',  ( 126.6942948109119840, -8.899110576539710493, -16.42337572283490132 ) ) ;
#26005=CARTESIAN_POINT ( 'NONE',  ( 121.9292548109119849, -7.894159318335828068, -9.358103419637847864 ) ) ;
#26007=CARTESIAN_POINT ( 'NONE',  ( 118.8092881442453290, -9.988377603198976828, -10.36322818467138340 ) ) ;
#26008=CARTESIAN_POINT ( 'NONE',  ( 121.8725281442453223, -3.383040157471821630, -19.15922257007629170 ) ) ;
#26010=CARTESIAN_POINT ( 'NONE',  ( 126.5125895482244971, -8.560559907796994494, -16.97480111277819148 ) ) ;
#26014=CARTESIAN_POINT ( 'NONE',  ( 127.0150841466605698, -9.959652887476131866, -11.61104853207065979 ) ) ;
#26015=CARTESIAN_POINT ( 'NONE',  ( 116.4834948109119779, -1.561330072975668504, -17.79121239304076951 ) ) ;
#26019=CARTESIAN_POINT ( 'NONE',  ( 113.4769814775786330, 0.4262465694468514643, -12.03445270309931736 ) ) ;
#26020=CARTESIAN_POINT ( 'NONE',  ( 112.6828081442453282, -7.893985811506177619, -18.51759400769804742 ) ) ;
#26021=CARTESIAN_POINT ( 'NONE',  ( 118.9794681442453026, -9.261995988541697145, -16.69588392320189030 ) ) ;
#26023=DIRECTION ( 'NONE',  ( 0.000000000000000000, 0.6004852223388321697, -0.7996358532186279566 ) ) ;
#26026=CARTESIAN_POINT ( 'NONE',  ( 118.5823814775786360, -7.643976991954077427, -18.09477374809248928 ) ) ;
#26027=CARTESIAN_POINT ( 'NONE',  ( 117.9583881442453048, -10.30919188438810075, -12.61870101168855918 ) ) ;
#26029=CARTESIAN_POINT ( 'NONE',  ( 117.1074881442453233, -10.63000616557722466, -14.87417383870573495 ) ) ;
#26030=CARTESIAN_POINT ( 'NONE',  ( 118.2396587682627995, -1.040089454026966287, -17.23633227186632766 ) ) ;
#26031=CARTESIAN_POINT ( 'NONE',  ( 123.4041481442452834, 0.1319031606808879209, -14.10382304977623669 ) ) ;
#26032=CARTESIAN_POINT ( 'NONE',  ( 116.9373081442452929, -1.833838273342659253, -17.42832698103878286 ) ) ;
#26035=CARTESIAN_POINT ( 'NONE',  ( 112.2857214775786474, -4.089484607189486809, -7.948022111789456723 ) ) ;
#26036=CARTESIAN_POINT ( 'NONE',  ( 116.0864081442453113, -0.1624402480850797581, -16.17319339645315424 ) ) ;
#26039=CARTESIAN_POINT ( 'NONE',  ( 115.0653281442453277, -6.344957434206662583, -7.627207830600332805 ) ) ;
#26042=CARTESIAN_POINT ( 'NONE',  ( 119.1864297909088179, -1.016270020561755860, -17.26805140881366896 ) ) ;
#26045=CARTESIAN_POINT ( 'NONE',  ( 123.0637881442452937, -8.899110576539710493, -16.42337572283490132 ) ) ;
#26047=CARTESIAN_POINT ( 'NONE',  ( 122.6667014775786413, -2.084020599724406786, -8.691656652584148546 ) ) ;
#26054=CARTESIAN_POINT ( 'NONE',  ( 115.7460481442453357, 0.9020085738987339008, -11.91225656197089222 ) ) ;
#26055=CARTESIAN_POINT ( 'NONE',  ( 115.9729548109119861, -6.344957434206662583, -7.627207830600332805 ) ) ;
#26056=CARTESIAN_POINT ( 'NONE',  ( 117.3343948109119737, -6.222761293078241884, -8.102969835052219238 ) ) ;
#26057=CARTESIAN_POINT ( 'NONE',  ( 122.8936081442453059, -9.565557343593413364, -10.61323700422348004 ) ) ;
#26060=CARTESIAN_POINT ( 'NONE',  ( 120.1140014775786398, -7.894159318335828068, -9.358103419637847864 ) ) ;
#26061=CARTESIAN_POINT ( 'NONE',  ( 125.2761281442453054, 0.4262465694468514643, -12.03445270309931736 ) ) ;
#26063=CARTESIAN_POINT ( 'NONE',  ( 114.1568685810857176, -1.220279397241700758, -16.99638242193885063 ) ) ;
#26065=CARTESIAN_POINT ( 'NONE',  ( 119.9438214775786378, -7.893985811506177619, -18.51759400769804742 ) ) ;
#26067=CARTESIAN_POINT ( 'NONE',  ( 122.2696148109119889, -4.089484607189486809, -7.948022111789456723 ) ) ;
#26070=CARTESIAN_POINT ( 'NONE',  ( 114.9518748109119883, -1.834011780172310813, -8.268836392978581529 ) ) ;
#26071=CARTESIAN_POINT ( 'NONE',  ( 116.1431348109119881, -10.30919188438810075, -12.61870101168855918 ) ) ;
#26077=CARTESIAN_POINT ( 'NONE',  ( 120.7379948109119709, 0.4262465694468514643, -12.03445270309931736 ) ) ;
#26080=CARTESIAN_POINT ( 'NONE',  ( 118.6391081442452986, -5.574606645277164318, -18.38911715685844683 ) ) ;
#26083=CARTESIAN_POINT ( 'NONE',  ( 113.8740681442453138, -9.859900752359374465, -12.68260735090039404 ) ) ;
#26084=CARTESIAN_POINT ( 'NONE',  ( 121.1350814775786233, 0.5811942927096110934, -14.16772938898807510 ) ) ;
#26086=CARTESIAN_POINT ( 'NONE',  ( 116.8805814775786445, -3.505236298600246325, -18.68346056562440793 ) ) ;
#26087=CARTESIAN_POINT ( 'NONE',  ( 114.1009748109119784, -4.089484607189486809, -7.948022111789456723 ) ) ;
#26088=CARTESIAN_POINT ( 'NONE',  ( 120.4543614775786295, -4.089484607189486809, -7.948022111789456723 ) ) ;
#26090=CARTESIAN_POINT ( 'NONE',  ( 121.6456214775786293, 0.4262465694468514643, -12.03445270309931736 ) ) ;
#26092=CARTESIAN_POINT ( 'NONE',  ( 123.2339681442453241, -3.505236298600246325, -18.68346056562440793 ) ) ;
#26093=CARTESIAN_POINT ( 'NONE',  ( 120.4543614775786295, -4.089484607189486809, -7.948022111789456723 ) ) ;
#26095=CARTESIAN_POINT ( 'NONE',  ( 120.7379948109119709, -10.63000616557722466, -14.87417383870573495 ) ) ;
#26102=CARTESIAN_POINT ( 'NONE',  ( 118.7525614775786380, -1.833838273342659253, -17.42832698103878286 ) ) ;
#26103=CARTESIAN_POINT ( 'NONE',  ( 125.1626748109119802, -9.988377603198980381, -10.36322818467138518 ) ) ;
#26106=CARTESIAN_POINT ( 'NONE',  ( 115.5958131642484545, -2.215723800389698184, -18.16877924232191788 ) ) ;
#26108=CARTESIAN_POINT ( 'NONE',  ( 114.8384214775786489, -10.15424416112533912, -14.75197769757731336 ) ) ;
#26114=CARTESIAN_POINT ( 'NONE',  ( 124.4819548109119722, -7.893985811506177619, -18.51759400769804742 ) ) ;
#26116=CARTESIAN_POINT ( 'NONE',  ( 123.8579614775786126, -9.859900752359378018, -12.68260735090039759 ) ) ;
#26121=CARTESIAN_POINT ( 'NONE',  ( 124.5954081442453116, -6.222761293078241884, -8.102969835052219238 ) ) ;
#26122=CARTESIAN_POINT ( 'NONE',  ( 120.1140014775786398, -7.894159318335828068, -9.358103419637847864 ) ) ;
#26123=CARTESIAN_POINT ( 'NONE',  ( 118.5823814775786360, -7.643976991954077427, -18.09477374809248928 ) ) ;
#26127=CARTESIAN_POINT ( 'NONE',  ( 115.5566632127138575, -2.191907684172563986, -18.20049396185734025 ) ) ;
#26133=CARTESIAN_POINT ( 'NONE',  ( 122.3830681442452857, -8.166667518702819706, -8.995218007635861213 ) ) ;
#26134=CARTESIAN_POINT ( 'NONE',  ( 119.2631014775786298, 0.2603800115204892296, -16.42320221600525088 ) ) ;
#26136=CARTESIAN_POINT ( 'NONE',  ( 118.2420214775786320, -3.383040157471821630, -19.15922257007629170 ) ) ;
#26142=CARTESIAN_POINT ( 'NONE',  ( 123.5176014775786228, -9.261995988541697145, -16.69588392320189030 ) ) ;
#26143=CARTESIAN_POINT ( 'NONE',  ( 120.8514481442452961, -7.893985811506177619, -18.51759400769804742 ) ) ;
#26144=CARTESIAN_POINT ( 'NONE',  ( 126.6375681442452930, -10.15424416112533912, -14.75197769757731336 ) ) ;
#26146=CARTESIAN_POINT ( 'NONE',  ( 114.2711548109119803, -0.1624402480850797581, -16.17319339645315424 ) ) ;
#26147=CARTESIAN_POINT ( 'NONE',  ( 126.2404814775786264, -9.261995988541697145, -16.69588392320189030 ) ) ;
#26149=CARTESIAN_POINT ( 'NONE',  ( 120.2841814775786276, -10.15424416112533912, -14.75197769757731336 ) ) ;
#26151=DIRECTION ( 'NONE',  ( 0.000000000000000000, 0.6004852223388323917, -0.7996358532186279566 ) ) ;
#26152=ORIENTED_EDGE ( 'NONE', *, *, #34810, .F. ) ;
#26154=CARTESIAN_POINT ( 'NONE',  ( 121.4754414775786131, -8.166667518702819706, -8.995218007635861213 ) ) ;
#26159=CARTESIAN_POINT ( 'NONE',  ( 118.8092881442453290, -0.1624402480850797581, -16.17319339645315424 ) ) ;
#26162=( BOUNDED_CURVE ( )  B_SPLINE_CURVE ( 2, ( #16073, #9686, #20406, #30432, #37488, #16535, #40474, #30882, #2603, #43894, #9455, #9235, #23144 ),
 .UNSPECIFIED., .F., .T. ) 
 B_SPLINE_CURVE_WITH_KNOTS ( ( 3, 2, 2, 2, 2, 2, 3 ),
 ( 0.8921282416568590001, 0.8984375000000000000, 0.9062500000000000000, 0.9140625000000000000, 0.9218750000000000000, 0.9296875000000000000, 0.9375000000000000000 ),
 .UNSPECIFIED. ) 
 CURVE ( )  GEOMETRIC_REPRESENTATION_ITEM ( )  RATIONAL_B_SPLINE_CURVE ( ( 0.9763430640195950305, 0.9385262470928690259, 1.000000000000000000, 0.9238795325112869605, 1.000000000000000000, 0.9238795325112869605, 1.000000000000000000, 0.9238795325112869605, 1.000000000000000000, 0.9238795325112869605, 1.000000000000000000, 0.9238795325112479917, 1.000000000000039968 ) ) 
 REPRESENTATION_ITEM ( '' )  );
#26164=CARTESIAN_POINT ( 'NONE',  ( 124.0848681442452772, -5.574606645277164318, -18.38911715685844683 ) ) ;
#26167=EDGE_CURVE ( 'NONE', #41698, #17138, #13660, .T. ) ;
#26169=CARTESIAN_POINT ( 'NONE',  ( 123.2339681442453241, -6.344957434206665248, -7.627207830600338134 ) ) ;
#26170=CARTESIAN_POINT ( 'NONE',  ( 116.0296814775786345, -1.833838273342658809, -17.42832698103878286 ) ) ;
#26171=CARTESIAN_POINT ( 'NONE',  ( 123.6310548109119765, -4.153390946401325223, -8.397313243818185668 ) ) ;
#26173=CARTESIAN_POINT ( 'NONE',  ( 122.6099748109119929, -9.261995988541697145, -16.69588392320189030 ) ) ;
#26174=CARTESIAN_POINT ( 'NONE',  ( 114.6682414775786469, -1.561330072975668060, -17.79121239304076596 ) ) ;
#26177=CARTESIAN_POINT ( 'NONE',  ( 125.9568481442452850, -3.505236298600246325, -18.68346056562440793 ) ) ;
#26178=CARTESIAN_POINT ( 'NONE',  ( 121.7023481442452777, -9.261995988541697145, -16.69588392320189030 ) ) ;
#26182=CARTESIAN_POINT ( 'NONE',  ( 113.3635281442453504, -0.1624402480850797581, -16.17319339645315424 ) ) ;
#26187=CARTESIAN_POINT ( 'NONE',  ( 125.5030348109119558, -6.222761293078241884, -8.102969835052219238 ) ) ;
#26190=ADVANCED_FACE ( 'NONE', ( #16326 ), #37509, .F. ) ;
#26191=ADVANCED_FACE ( 'NONE', ( #2854 ), #24694, .T. ) ;
#26195=CARTESIAN_POINT ( 'NONE',  ( 119.6601881442453106, -8.166667518702819706, -8.995218007635861213 ) ) ;
#26196=CARTESIAN_POINT ( 'NONE',  ( 112.9664414775786412, 0.5811942927096110934, -14.16772938898807510 ) ) ;
#26197=CARTESIAN_POINT ( 'NONE',  ( 123.1205148109119563, -7.643976991954077427, -18.09477374809248928 ) ) ;
#26198=CARTESIAN_POINT ( 'NONE',  ( 114.2144281442453178, -1.833838273342658809, -17.42832698103878286 ) ) ;
#26202=CARTESIAN_POINT ( 'NONE',  ( 114.3846081442453197, -10.63000616557722466, -14.87417383870573495 ) ) ;
#26204=CARTESIAN_POINT ( 'NONE',  ( 124.2550481442452792, -9.988377603198980381, -10.36322818467138518 ) ) ;
#26207=CARTESIAN_POINT ( 'NONE',  ( 113.3635281442453504, -9.988377603198976828, -10.36322818467138340 ) ) ;
#26208=CARTESIAN_POINT ( 'NONE',  ( 114.2711548109119803, -0.1624402480850797581, -16.17319339645315424 ) ) ;
#26210=CARTESIAN_POINT ( 'NONE',  ( 113.0798948109119948, -0.4660016031367893996, -10.09054647747474043 ) ) ;
#26212=CARTESIAN_POINT ( 'NONE',  ( 117.2209414775786485, -7.893985811506177619, -18.51759400769804742 ) ) ;
#26215=CARTESIAN_POINT ( 'NONE',  ( 115.9328453070359046, -1.196538596002799215, -17.02799684832027083 ) ) ;
#26216=CARTESIAN_POINT ( 'NONE',  ( 111.7751814775786556, -2.084020599724394796, -8.691656652584146769 ) ) ;
#26217=CARTESIAN_POINT ( 'NONE',  ( 112.5352875888224133, -2.372251574601220270, -17.96033910819751966 ) ) ;
#26218=CARTESIAN_POINT ( 'NONE',  ( 115.0086014775786509, -5.574606645277164318, -18.38911715685844683 ) ) ;
#26221=CARTESIAN_POINT ( 'NONE',  ( 111.3780948109119890, -5.574606645277164318, -18.38911715685844683 ) ) ;
#26223=CARTESIAN_POINT ( 'NONE',  ( 126.1270281442452870, 0.1319031606808879209, -14.10382304977623669 ) ) ;
#26225=CARTESIAN_POINT ( 'NONE',  ( 125.5030348109119558, -6.222761293078241884, -8.102969835052219238 ) ) ;
#26226=CARTESIAN_POINT ( 'NONE',  ( 113.0798948109119948, -8.899110576539710493, -16.42337572283490132 ) ) ;
#26227=CARTESIAN_POINT ( 'NONE',  ( 122.0427081442452817, 0.5811942927096110934, -14.16772938898807510 ) ) ;
#26229=CARTESIAN_POINT ( 'NONE',  ( 123.0070614775786169, 0.9020085738987339008, -11.91225656197089222 ) ) ;
#26231=CARTESIAN_POINT ( 'NONE',  ( 127.7617783745704543, -8.479500832906602170, -17.89265013408903471 ) ) ;
#26236=CARTESIAN_POINT ( 'NONE',  ( 115.3489614775786407, -9.261995988541697145, -16.69588392320189030 ) ) ;
#26237=ORIENTED_EDGE ( 'NONE', *, *, #1684, .T. ) ;
#26238=CARTESIAN_POINT ( 'NONE',  ( 125.3328548109119964, -9.261995988541697145, -16.69588392320189030 ) ) ;
#26241=CARTESIAN_POINT ( 'NONE',  ( 113.3068014775786594, -1.833838273342658809, -17.42832698103878286 ) ) ;
#26242=CARTESIAN_POINT ( 'NONE',  ( 120.9649014775786355, -3.383040157471821630, -19.15922257007629170 ) ) ;
#26247=CARTESIAN_POINT ( 'NONE',  ( 118.8092881442453290, -0.1624402480850797581, -16.17319339645315424 ) ) ;
#26248=CARTESIAN_POINT ( 'NONE',  ( 118.8660148109119774, -10.30919188438810075, -12.61870101168855918 ) ) ;
#26251=CARTESIAN_POINT ( 'NONE',  ( 113.9307948109119906, 0.9020085738987339008, -11.91225656197089222 ) ) ;
#26254=CARTESIAN_POINT ( 'NONE',  ( 123.9714148109119805, -8.899110576539710493, -16.42337572283490132 ) ) ;
#26255=CARTESIAN_POINT ( 'NONE',  ( 120.9081748109119872, -4.153390946401325223, -8.397313243818185668 ) ) ;
#26259=B_SPLINE_CURVE_WITH_KNOTS ( 'NONE', 3,
 ( #15345, #8505, #9631, #41110, #44073, #1867, #5969, #6205, #37435, #5739 ),
 .UNSPECIFIED., .F., .F.,
 ( 4, 3, 3, 4 ),
 ( 4.336808689942019662E-19, 0.0001671877548681264863, 0.0003343755096277665107, 0.0006463528481650619413 ),
 .UNSPECIFIED. ) ;
#26260=FACE_OUTER_BOUND ( 'NONE', #11604, .T. ) ;
#26261=CARTESIAN_POINT ( 'NONE',  ( 123.0637881442452937, -8.899110576539710493, -16.42337572283490132 ) ) ;
#26265=CARTESIAN_POINT ( 'NONE',  ( 115.5758681442453053, -1.561330072975668060, -17.79121239304076951 ) ) ;
#26267=CARTESIAN_POINT ( 'NONE',  ( 115.9162281442453235, -5.574606645277164318, -18.38911715685844683 ) ) ;
#26268=ORIENTED_EDGE ( 'NONE', *, *, #40638, .F. ) ;
#26270=CARTESIAN_POINT ( 'NONE',  ( 123.6310548109119765, -4.153390946401325223, -8.397313243818185668 ) ) ;
#26271=B_SPLINE_CURVE_WITH_KNOTS ( 'NONE', 3,
 ( #20930, #4487, #39146, #21818, #35712, #18408, #14980, #31398, #42805, #38239 ),
 .UNSPECIFIED., .F., .F.,
 ( 4, 3, 3, 4 ),
 ( 0.000000000000000000, 0.0001671877560958109985, 0.0003343755126086590075, 0.0006438490228505489759 ),
 .UNSPECIFIED. ) ;
#26272=CARTESIAN_POINT ( 'NONE',  ( 120.0572748109119772, -6.222761293078241884, -8.102969835052219238 ) ) ;
#26276=CARTESIAN_POINT ( 'NONE',  ( 120.0005481442453146, -5.638512984488999180, -18.83840828888717311 ) ) ;
#26279=CARTESIAN_POINT ( 'NONE',  ( 117.1074881442453233, -10.63000616557722466, -14.87417383870573495 ) ) ;
#26280=CARTESIAN_POINT ( 'NONE',  ( 116.4267681442453153, -3.383040157471821630, -19.15922257007629170 ) ) ;
#26281=CARTESIAN_POINT ( 'NONE',  ( 116.0296814775786345, -1.833838273342658809, -17.42832698103878286 ) ) ;
#26282=CARTESIAN_POINT ( 'NONE',  ( 121.1918081442452859, -10.15424416112533912, -14.75197769757731336 ) ) ;
#26283=CARTESIAN_POINT ( 'NONE',  ( 113.4202548109119846, -10.30919188438810075, -12.61870101168855918 ) ) ;
#26285=CARTESIAN_POINT ( 'NONE',  ( 119.3765548109119834, -10.15424416112533912, -14.75197769757731336 ) ) ;
#26286=CARTESIAN_POINT ( 'NONE',  ( 113.7805598309151236, -2.215723800389698184, -18.16877924232191788 ) ) ;
#26291=CARTESIAN_POINT ( 'NONE',  ( 120.0572748109119772, -3.383040157471821630, -19.15922257007629170 ) ) ;
#26294=CARTESIAN_POINT ( 'NONE',  ( 121.1918081442452859, 0.9020085738987339008, -11.91225656197089222 ) ) ;
#26297=CARTESIAN_POINT ( 'NONE',  ( 119.8870948109119752, -9.261995988541697145, -16.69588392320189030 ) ) ;
#26298=CARTESIAN_POINT ( 'NONE',  ( 117.7314814775786260, -4.089484607189486809, -7.948022111789456723 ) ) ;
#26304=CARTESIAN_POINT ( 'NONE',  ( 121.5321681442453183, -0.1624402480850797581, -16.17319339645315424 ) ) ;
#26308=CARTESIAN_POINT ( 'NONE',  ( 119.3198281442452924, -9.859900752359374465, -12.68260735090039404 ) ) ;
#26311=CARTESIAN_POINT ( 'NONE',  ( 113.6471614775786492, -4.153390946401321671, -8.397313243818183892 ) ) ;
#26312=CARTESIAN_POINT ( 'NONE',  ( 122.7234281442452755, -5.638512984488999180, -18.83840828888717311 ) ) ;
#26314=CARTESIAN_POINT ( 'NONE',  ( 121.0783548109119749, -9.565557343593413364, -10.61323700422348004 ) ) ;
#26315=CARTESIAN_POINT ( 'NONE',  ( 114.9518748109119883, -1.834011780172310813, -8.268836392978581529 ) ) ;
#26317=CARTESIAN_POINT ( 'NONE',  ( 120.5110881442453206, -6.344957434206665248, -7.627207830600338134 ) ) ;
#26318=CARTESIAN_POINT ( 'NONE',  ( 122.0994348109119443, -10.15424416112533912, -14.75197769757731336 ) ) ;
#26320=CARTESIAN_POINT ( 'NONE',  ( 125.3328548109119964, -0.8288870151387760510, -10.36305467784173118 ) ) ;
#26322=CARTESIAN_POINT ( 'NONE',  ( 122.4965214775786251, -10.30919188438810075, -12.61870101168855918 ) ) ;
#26325=CARTESIAN_POINT ( 'NONE',  ( 111.4915481442453142, -1.833838273342658365, -17.42832698103878286 ) ) ;
#26331=CARTESIAN_POINT ( 'NONE',  ( 137.3930029278077427, -9.820525849186804379, -12.08282185636668338 ) ) ;
#26332=CARTESIAN_POINT ( 'NONE',  ( 118.4689281442453392, -10.15424416112533912, -14.75197769757731336 ) ) ;
#26333=CARTESIAN_POINT ( 'NONE',  ( 124.1415948109119540, -6.344957434206665248, -7.627207830600338134 ) ) ;
#26335=ORIENTED_EDGE ( 'NONE', *, *, #44279, .F. ) ;
#26338=CARTESIAN_POINT ( 'NONE',  ( 117.7314814775786260, -5.574606645277164318, -18.38911715685844683 ) ) ;
#26339=CARTESIAN_POINT ( 'NONE',  ( 114.8340781407226103, -1.081026697600512732, -17.18181821144401056 ) ) ;
#26340=B_SPLINE_CURVE_WITH_KNOTS ( 'NONE', 3,
 ( #38205, #7192, #3765, #44397, #13161, #27062, #14489, #21782, #39334, #580 ),
 .UNSPECIFIED., .F., .F.,
 ( 4, 3, 3, 4 ),
 ( 0.000000000000000000, 0.0001671877560958105107, 0.0003343755126086565138, 0.0006438490228505459401 ),
 .UNSPECIFIED. ) ;
#26345=CARTESIAN_POINT ( 'NONE',  ( 122.8936081442453059, 0.2603800115204892296, -16.42320221600525088 ) ) ;
#26346=CARTESIAN_POINT ( 'NONE',  ( 123.4608748109119745, 0.4262465694468514643, -12.03445270309931736 ) ) ;
#26348=CARTESIAN_POINT ( 'NONE',  ( 111.7751814775786556, -7.893985811506177619, -18.51759400769804742 ) ) ;
#26351=CARTESIAN_POINT ( 'NONE',  ( 120.8514481442452961, -2.084020599724406786, -8.691656652584148546 ) ) ;
#26352=CARTESIAN_POINT ( 'NONE',  ( 121.7590748109119687, -2.084020599724406786, -8.691656652584148546 ) ) ;
#26353=CARTESIAN_POINT ( 'NONE',  ( 119.6026285810857104, -1.220279397241718966, -16.99638242193886484 ) ) ;
#26356=CARTESIAN_POINT ( 'NONE',  ( 116.5969481442453031, 0.5811942927096102052, -14.16772938898808221 ) ) ;
#26362=CARTESIAN_POINT ( 'NONE',  ( 122.0427081442452817, 0.5811942927096110934, -14.16772938898807510 ) ) ;
#26363=CARTESIAN_POINT ( 'NONE',  ( 121.1918081442452859, 0.9020085738987339008, -11.91225656197089222 ) ) ;
#26365=CARTESIAN_POINT ( 'NONE',  ( 116.9373081442452929, -8.166667518702817929, -8.995218007635861213 ) ) ;
#26368=FACE_OUTER_BOUND ( 'NONE', #12664, .T. ) ;
#26369=CARTESIAN_POINT ( 'NONE',  ( 121.5321681442453183, -9.988377603198976828, -10.36322818467138340 ) ) ;
#26370=CARTESIAN_POINT ( 'NONE',  ( 118.5256548109119876, -0.4660016031367893996, -10.09054647747474043 ) ) ;
#26371=CARTESIAN_POINT ( 'NONE',  ( 126.3539348109119800, -4.153390946401325223, -8.397313243818185668 ) ) ;
#26372=CARTESIAN_POINT ( 'NONE',  ( 111.9453614775786434, -7.894159318335828068, -9.358103419637847864 ) ) ;
#26373=CARTESIAN_POINT ( 'NONE',  ( 115.5191414775786569, -6.222761293078241884, -8.102969835052219238 ) ) ;
#26374=CARTESIAN_POINT ( 'NONE',  ( 123.9714148109119805, -0.4660016031367893996, -10.09054647747474043 ) ) ;
#26377=CARTESIAN_POINT ( 'NONE',  ( 120.3409081442453044, -8.899110576539710493, -16.42337572283490132 ) ) ;
#26379=CARTESIAN_POINT ( 'NONE',  ( 124.5596097606643298, -2.236191541394346061, -18.14152338500401029 ) ) ;
#26382=CARTESIAN_POINT ( 'NONE',  ( 122.3263414775786373, -6.344957434206665248, -7.627207830600338134 ) ) ;
#26389=CARTESIAN_POINT ( 'NONE',  ( 124.8223148109119762, -10.15424416112533912, -14.75197769757731336 ) ) ;
#26392=CARTESIAN_POINT ( 'NONE',  ( 124.8223148109119762, -10.15424416112533912, -14.75197769757731336 ) ) ;
#26394=CARTESIAN_POINT ( 'NONE',  ( 124.7655881442452852, 0.5811942927096110934, -14.16772938898807510 ) ) ;
#26395=CARTESIAN_POINT ( 'NONE',  ( 118.7525614775786380, -1.833838273342659253, -17.42832698103878286 ) ) ;
#26398=CARTESIAN_POINT ( 'NONE',  ( 123.6877814775786533, -3.383040157471821630, -19.15922257007629170 ) ) ;
#26399=CARTESIAN_POINT ( 'NONE',  ( 116.4834948109119779, -1.561330072975668504, -17.79121239304076951 ) ) ;
#26401=CARTESIAN_POINT ( 'NONE',  ( 112.8529881442453302, -7.894159318335828068, -9.358103419637847864 ) ) ;
#26402=CARTESIAN_POINT ( 'NONE',  ( 125.6164881442453094, -9.565557343593413364, -10.61323700422348004 ) ) ;
#26403=CARTESIAN_POINT ( 'NONE',  ( 123.4041481442452834, -10.30919188438810075, -12.61870101168855918 ) ) ;
#26407=CARTESIAN_POINT ( 'NONE',  ( 113.7038881442453402, -6.222761293078241884, -8.102969835052219238 ) ) ;
#26409=CARTESIAN_POINT ( 'NONE',  ( 117.1074881442453233, 0.4262465694468514643, -12.03445270309931736 ) ) ;
#26410=CARTESIAN_POINT ( 'NONE',  ( 135.7024735266973323, -1.889072916127992219, -18.60376373290417362 ) ) ;
#26413=CARTESIAN_POINT ( 'NONE',  ( 124.9357681442453014, -7.643976991954077427, -18.09477374809248928 ) ) ;
#26418=CARTESIAN_POINT ( 'NONE',  ( 112.0678367055514570, -10.09801862800623518, -14.68466812670380506 ) ) ;
#26423=CARTESIAN_POINT ( 'NONE',  ( 118.6391081442452986, -4.089484607189486809, -7.948022111789456723 ) ) ;
#26424=CARTESIAN_POINT ( 'NONE',  ( 123.8579614775786126, -9.859900752359378018, -12.68260735090039759 ) ) ;
#26425=CARTESIAN_POINT ( 'NONE',  ( 114.6115148109119986, -6.222761293078241884, -8.102969835052219238 ) ) ;
#26426=CARTESIAN_POINT ( 'NONE',  ( 116.3909697606643476, -2.236191541394345172, -18.14152338500401029 ) ) ;
#26429=CARTESIAN_POINT ( 'NONE',  ( 113.9875214775786532, -0.4660016031367893996, -10.09054647747474043 ) ) ;
#26430=EDGE_CURVE ( 'NONE', #40611, #14254, #41638, .T. ) ;
#26432=CARTESIAN_POINT ( 'NONE',  ( 122.7801548109119665, -3.383040157471821630, -19.15922257007629170 ) ) ;
#26433=VERTEX_POINT ( 'NONE', #33667 ) ;
#26434=( BOUNDED_CURVE ( )  B_SPLINE_CURVE ( 2, ( #28910, #21836, #18426, #18861, #25490 ),
 .UNSPECIFIED., .F., .T. ) 
 B_SPLINE_CURVE_WITH_KNOTS ( ( 3, 2, 3 ),
 ( 0.000000000000000000, 0.1250000000000000000, 0.2257267493207054943 ),
 .UNSPECIFIED. ) 
 CURVE ( )  GEOMETRIC_REPRESENTATION_ITEM ( )  RATIONAL_B_SPLINE_CURVE ( ( 1.000000000000000000, 0.9238795325112869605, 1.000000000000000000, 0.9386610620247159975, 0.9761776733139879703 ) ) 
 REPRESENTATION_ITEM ( '' )  );
#26435=CARTESIAN_POINT ( 'NONE',  ( 113.6471614775786492, -5.638512984488999180, -18.83840828888717311 ) ) ;
#26436=CARTESIAN_POINT ( 'NONE',  ( 113.0798948109119948, -8.899110576539710493, -16.42337572283490132 ) ) ;
#26437=ADVANCED_FACE ( 'NONE', ( #44415 ), #5188, .F. ) ;
#26440=CARTESIAN_POINT ( 'NONE',  ( 112.6828081442453282, -7.893985811506177619, -18.51759400769804742 ) ) ;
#26443=CARTESIAN_POINT ( 'NONE',  ( 120.4543614775786295, -4.089484607189486809, -7.948022111789456723 ) ) ;
#26446=EDGE_CURVE ( 'NONE', #30023, #16801, #34916, .T. ) ;
#26447=DIRECTION ( 'NONE',  ( 0.000000000000000000, 0.6004852223388321697, -0.7996358532186279566 ) ) ;
#26448=ADVANCED_FACE ( 'NONE', ( #5419 ), #33221, .F. ) ;
#26450=CARTESIAN_POINT ( 'NONE',  ( 123.5300843491906733, -4.187684698237162273, -15.54286723766359479 ) ) ;
#26451=CARTESIAN_POINT ( 'NONE',  ( 115.8027748109119841, -8.899110576539710493, -16.42337572283490132 ) ) ;
#26455=CARTESIAN_POINT ( 'NONE',  ( 112.9097148109120070, -9.565557343593413364, -10.61323700422348004 ) ) ;
#26456=CARTESIAN_POINT ( 'NONE',  ( 113.7038881442453402, -3.383040157471821630, -19.15922257007629170 ) ) ;
#26458=CARTESIAN_POINT ( 'NONE',  ( 113.1366214775786432, -1.834011780172310813, -8.268836392978581529 ) ) ;
#26459=CARTESIAN_POINT ( 'NONE',  ( 114.6115148109119986, -6.222761293078241884, -8.102969835052219238 ) ) ;
#26460=CARTESIAN_POINT ( 'NONE',  ( 122.2128881442453263, -1.834011780172310813, -8.268836392978581529 ) ) ;
#26461=CARTESIAN_POINT ( 'NONE',  ( 123.5743281442453139, -7.893985811506177619, -18.51759400769804742 ) ) ;
#26463=CARTESIAN_POINT ( 'NONE',  ( 112.1155414775786454, 0.9020085738987339008, -11.91225656197089222 ) ) ;
#26468=CARTESIAN_POINT ( 'NONE',  ( 119.0929214775786278, -5.638512984488999180, -18.83840828888717311 ) ) ;
#26470=CARTESIAN_POINT ( 'NONE',  ( 125.0492214775786266, -6.344957434206665248, -7.627207830600338134 ) ) ;
#26473=B_SPLINE_CURVE_WITH_KNOTS ( 'NONE', 3,
 ( #9606, #20546, #16678, #30130, #40619, #13485, #44043, #37409, #23750, #27387, #33756, #13257, #6634, #33517, #41311, #41083, #10071, #9839, #20099, #37640, #2524, #6414, #23972, #20322, #16451, #37858, #34425, #12807, #2297, #16226, #19867 ),
 .UNSPECIFIED., .F., .F.,
 ( 4, 2, 2, 1, 1, 1, 2, 2, 2, 1, 1, 1, 2, 2, 2, 1, 2, 2, 4 ),
 ( 0.000000000000000000, 0.2500000000000044964, 0.3750000000000062172, 0.4375000000000071054, 0.4687500000000212053, 0.4843750000000144329, 0.4921875000000255351, 0.5000000000000366374, 0.6250000000000016653, 0.6874999999999731326, 0.7187499999999706901, 0.7343749999999695799, 0.7421874999999682476, 0.7499999999999669154, 0.8124999999999887867, 0.8437499999999990008, 0.8593749999999964473, 0.8749999999999940048, 1.000000000000000000 ),
 .UNSPECIFIED. ) ;
#26474=CARTESIAN_POINT ( 'NONE',  ( 115.2922348109119781, 0.4262465694468514643, -12.03445270309931736 ) ) ;
#26476=CARTESIAN_POINT ( 'NONE',  ( 121.4754414775786131, -8.166667518702819706, -8.995218007635861213 ) ) ;
#26481=CARTESIAN_POINT ( 'NONE',  ( 122.2128881442453263, -7.643976991954077427, -18.09477374809248928 ) ) ;
#26483=CARTESIAN_POINT ( 'NONE',  ( 119.0929214775786278, -5.638512984488999180, -18.83840828888717311 ) ) ;
#26484=FACE_OUTER_BOUND ( 'NONE', #24312, .T. ) ;
#26485=CARTESIAN_POINT ( 'NONE',  ( 115.6325948109119821, 0.2603800115204892296, -16.42320221600525088 ) ) ;
#26487=CARTESIAN_POINT ( 'NONE',  ( 124.5386814775786206, -4.153390946401325223, -8.397313243818185668 ) ) ;
#26488=CARTESIAN_POINT ( 'NONE',  ( 119.8303681442453126, 0.4262465694468514643, -12.03445270309931736 ) ) ;
#26489=ORIENTED_EDGE ( 'NONE', *, *, #4499, .F. ) ;
#26492=CARTESIAN_POINT ( 'NONE',  ( 114.3278814775786429, -10.30919188438810075, -12.61870101168855918 ) ) ;
#26493=CARTESIAN_POINT ( 'NONE',  ( 120.5678148109119832, -1.833838273342659253, -17.42832698103878286 ) ) ;
#26494=ORIENTED_EDGE ( 'NONE', *, *, #28781, .T. ) ;
#26496=CARTESIAN_POINT ( 'NONE',  ( 117.3343948109119737, -3.383040157471821630, -19.15922257007629170 ) ) ;
#26498=CARTESIAN_POINT ( 'NONE',  ( 116.4834948109119779, -7.894159318335828068, -9.358103419637847864 ) ) ;
#26500=EDGE_LOOP ( 'NONE', ( #40746, #37722, #9922, #27093 ) ) ;
#26501=CARTESIAN_POINT ( 'NONE',  ( 126.0135748109119902, -1.833838273342660141, -17.42832698103878286 ) ) ;
#26502=CARTESIAN_POINT ( 'NONE',  ( 120.3976348109119812, -7.643976991954077427, -18.09477374809248928 ) ) ;
#26505=CARTESIAN_POINT ( 'NONE',  ( 118.9794681442453026, -9.261995988541697145, -16.69588392320189030 ) ) ;
#26507=ADVANCED_FACE ( 'NONE', ( #22744 ), #43347, .T. ) ;
#26508=CARTESIAN_POINT ( 'NONE',  ( 114.6682414775786469, -1.561330072975668060, -17.79121239304076596 ) ) ;
#26509=CARTESIAN_POINT ( 'NONE',  ( 115.2355081442453155, -10.30919188438810075, -12.61870101168855918 ) ) ;
#26510=CARTESIAN_POINT ( 'NONE',  ( 114.9518748109119883, -7.643976991954077427, -18.09477374809248928 ) ) ;
#26512=CARTESIAN_POINT ( 'NONE',  ( 125.3895814775786448, -2.084020599724406786, -8.691656652584148546 ) ) ;
#26513=CARTESIAN_POINT ( 'NONE',  ( 113.8740681442453138, 0.5811942927096154232, -14.16772938898807155 ) ) ;
#26515=CARTESIAN_POINT ( 'NONE',  ( 123.2906948109119867, -1.833838273342659697, -17.42832698103878286 ) ) ;
#26521=CARTESIAN_POINT ( 'NONE',  ( 119.6601881442453106, -8.166667518702819706, -8.995218007635861213 ) ) ;
#26523=CARTESIAN_POINT ( 'NONE',  ( 120.7379948109119709, -10.63000616557722466, -14.87417383870573495 ) ) ;
#26526=CARTESIAN_POINT ( 'NONE',  ( 120.1707281442453166, 0.2603800115204892296, -16.42320221600525088 ) ) ;
#26527=CARTESIAN_POINT ( 'NONE',  ( 121.8158014775786171, -5.638512984488999180, -18.83840828888717311 ) ) ;
#26533=CARTESIAN_POINT ( 'NONE',  ( 122.4397948109119767, -0.1624402480850797581, -16.17319339645315424 ) ) ;
#26536=CARTESIAN_POINT ( 'NONE',  ( 117.7882081442453170, -3.505236298600246325, -18.68346056562440793 ) ) ;
#26539=CARTESIAN_POINT ( 'NONE',  ( 112.2857214775786474, -5.574606645277164318, -18.38911715685844683 ) ) ;
#26540=CARTESIAN_POINT ( 'NONE',  ( 125.1626748109119802, -9.988377603198980381, -10.36322818467138518 ) ) ;
#26541=ORIENTED_EDGE ( 'NONE', *, *, #39558, .T. ) ;
#26542=CARTESIAN_POINT ( 'NONE',  ( 123.0070614775786169, -10.15424416112533912, -14.75197769757731336 ) ) ;
#26543=CARTESIAN_POINT ( 'NONE',  ( 113.4202548109119846, -10.30919188438810075, -12.61870101168855918 ) ) ;
#26544=CARTESIAN_POINT ( 'NONE',  ( 121.5888948109119809, -10.30919188438810075, -12.61870101168855918 ) ) ;
#26545=CARTESIAN_POINT ( 'NONE',  ( 121.9292548109119849, -7.894159318335828068, -9.358103419637847864 ) ) ;
#26549=CARTESIAN_POINT ( 'NONE',  ( 124.5954081442453116, -3.383040157471821630, -19.15922257007629170 ) ) ;
#26550=CARTESIAN_POINT ( 'NONE',  ( 115.1220548109119761, -1.833838273342658809, -17.42832698103878286 ) ) ;
#26551=CARTESIAN_POINT ( 'NONE',  ( 123.8012348109119642, 0.2603800115204892296, -16.42320221600525088 ) ) ;
#26555=CARTESIAN_POINT ( 'NONE',  ( 128.1199079201516327, -2.703369936665986462, -15.02142562904077039 ) ) ;
#26559=CARTESIAN_POINT ( 'NONE',  ( 118.6958348109119754, -3.505236298600246325, -18.68346056562440793 ) ) ;
#26560=CARTESIAN_POINT ( 'NONE',  ( 113.6471614775786492, -4.153390946401321671, -8.397313243818183892 ) ) ;
#26561=CARTESIAN_POINT ( 'NONE',  ( 126.4038788492663770, -6.085149154362555990, -18.33735632256993142 ) ) ;
#26564=CARTESIAN_POINT ( 'NONE',  ( 118.0718414775786442, -0.8288870151387760510, -10.36305467784173118 ) ) ;
#26566=CARTESIAN_POINT ( 'NONE',  ( 112.8529881442453302, -7.894159318335828068, -9.358103419637847864 ) ) ;
#26570=CARTESIAN_POINT ( 'NONE',  ( 123.8012348109119642, 0.2603800115204892296, -16.42320221600525088 ) ) ;
#26571=CARTESIAN_POINT ( 'NONE',  ( 123.8012348109119642, -9.565557343593413364, -10.61323700422348004 ) ) ;
#26576=CARTESIAN_POINT ( 'NONE',  ( 126.5808414775786446, -9.859900752359378018, -12.68260735090039759 ) ) ;
#26577=CARTESIAN_POINT ( 'NONE',  ( 118.2987481442453088, -7.894159318335828068, -9.358103419637847864 ) ) ;
#26580=CARTESIAN_POINT ( 'NONE',  ( 116.9373081442452929, -8.166667518702805495, -8.995218007635850554 ) ) ;
#26582=CARTESIAN_POINT ( 'NONE',  ( 113.2858169107182107, -2.467220198592768199, -17.83387418641523325 ) ) ;
#26587=CARTESIAN_POINT ( 'NONE',  ( 119.8303681442453126, -10.63000616557722466, -14.87417383870573495 ) ) ;
#26588=CARTESIAN_POINT ( 'NONE',  ( 120.6812681442452941, -10.30919188438810075, -12.61870101168855918 ) ) ;
#26589=LINE ( 'NONE', #5382, #34974 ) ;
#26590=CARTESIAN_POINT ( 'NONE',  ( 115.6325948109119821, 0.2603800115204892296, -16.42320221600525088 ) ) ;
#26591=CARTESIAN_POINT ( 'NONE',  ( 111.7751814775786556, -7.893985811506177619, -18.51759400769804742 ) ) ;
#26593=CARTESIAN_POINT ( 'NONE',  ( 114.4980614775786734, -2.084020599724406786, -8.691656652584148546 ) ) ;
#26595=CARTESIAN_POINT ( 'NONE',  ( 112.9664414775786412, -9.859900752359374465, -12.68260735090039404 ) ) ;
#26596=CARTESIAN_POINT ( 'NONE',  ( 118.6958348109119754, -6.344957434206665248, -7.627207830600338134 ) ) ;
#26597=CARTESIAN_POINT ( 'NONE',  ( 124.1983214775786166, -1.833838273342659697, -17.42832698103878286 ) ) ;
#26598=CARTESIAN_POINT ( 'NONE',  ( 112.0588148109119828, -9.859900752359374465, -12.68260735090039404 ) ) ;
#26600=CARTESIAN_POINT ( 'NONE',  ( 119.1496481442453046, -6.222761293078241884, -8.102969835052219238 ) ) ;
#26601=CARTESIAN_POINT ( 'NONE',  ( 126.0703014775786102, -9.988377603198980381, -10.36322818467138518 ) ) ;
#26603=CARTESIAN_POINT ( 'NONE',  ( 119.8303681442453126, 0.4262465694468514643, -12.03445270309931736 ) ) ;
#26608=CARTESIAN_POINT ( 'NONE',  ( 124.4819548109119722, -7.893985811506177619, -18.51759400769804742 ) ) ;
#26610=CARTESIAN_POINT ( 'NONE',  ( 112.1722681442453222, -0.4660016031367893996, -10.09054647747474043 ) ) ;
#26617=CARTESIAN_POINT ( 'NONE',  ( 135.6920194349522717, -4.118011552333871172, -19.32288967780376865 ) ) ;
#26618=CONICAL_SURFACE ( 'NONE', #29547, 3.499999999999999556, 1.325817663668031887 ) ;
#26620=CARTESIAN_POINT ( 'NONE',  ( 111.9261565460472099, -2.191907684172563986, -18.20049396185734025 ) ) ;
#26621=CARTESIAN_POINT ( 'NONE',  ( 116.7104014775786425, -8.899110576539710493, -16.42337572283490132 ) ) ;
#26622=CARTESIAN_POINT ( 'NONE',  ( 125.6732148109119862, -9.859900752359378018, -12.68260735090039759 ) ) ;
#26624=CARTESIAN_POINT ( 'NONE',  ( 122.8936081442453059, 0.2603800115204892296, -16.42320221600525088 ) ) ;
#26625=CARTESIAN_POINT ( 'NONE',  ( 116.1431348109119881, -10.30919188438810075, -12.61870101168855918 ) ) ;
#26629=CARTESIAN_POINT ( 'NONE',  ( 124.5386814775786206, -4.153390946401325223, -8.397313243818185668 ) ) ;
#26630=CARTESIAN_POINT ( 'NONE',  ( 123.5176014775786228, -9.261995988541697145, -16.69588392320189030 ) ) ;
#26634=CARTESIAN_POINT ( 'NONE',  ( 116.1431348109119881, 0.1319031606808879209, -14.10382304977623669 ) ) ;
#26635=CARTESIAN_POINT ( 'NONE',  ( 115.6893214775786447, -9.859900752359374465, -12.68260735090039404 ) ) ;
#26640=CARTESIAN_POINT ( 'NONE',  ( 124.8790414775786246, -8.899110576539710493, -16.42337572283490132 ) ) ;
#26647=CARTESIAN_POINT ( 'NONE',  ( 117.8449348109119938, -8.166667518702817929, -8.995218007635861213 ) ) ;
#26648=CARTESIAN_POINT ( 'NONE',  ( 124.9357681442453014, -7.643976991954077427, -18.09477374809248928 ) ) ;
#26649=CARTESIAN_POINT ( 'NONE',  ( 115.2355081442453155, 0.1319031606808879209, -14.10382304977623669 ) ) ;
#26650=CARTESIAN_POINT ( 'NONE',  ( 116.4642898793805443, -2.191907684172563986, -18.20049396185734025 ) ) ;
#26651=CARTESIAN_POINT ( 'NONE',  ( 124.0848681442452772, -4.089484607189435295, -7.948022111789469157 ) ) ;
#26652=CARTESIAN_POINT ( 'NONE',  ( 114.0442481442453300, -1.834011780172310813, -8.268836392978581529 ) ) ;
#26655=CARTESIAN_POINT ( 'NONE',  ( 125.2194014775786286, -10.30919188438810075, -12.61870101168855918 ) ) ;
#26656=DIRECTION ( 'NONE',  ( -1.000000000000000000, 0.000000000000000000, 0.000000000000000000 ) ) ;
#26658=CARTESIAN_POINT ( 'NONE',  ( 112.8529881442453302, -1.561330072975668060, -17.79121239304076596 ) ) ;
#26659=CARTESIAN_POINT ( 'NONE',  ( 115.6325948109119821, -9.565557343593413364, -10.61323700422348004 ) ) ;
#26661=CARTESIAN_POINT ( 'NONE',  ( 126.3115243456300050, -5.212275628432266217, -18.42773177175248733 ) ) ;
#26662=CARTESIAN_POINT ( 'NONE',  ( 125.6732148109119862, -9.859900752359378018, -12.68260735090039759 ) ) ;
#26664=CARTESIAN_POINT ( 'NONE',  ( 123.2339681442453241, -6.344957434206665248, -7.627207830600338134 ) ) ;
#26669=CARTESIAN_POINT ( 'NONE',  ( 117.6747548109119919, -7.643976991954077427, -18.09477374809248928 ) ) ;
#26670=CARTESIAN_POINT ( 'NONE',  ( 112.5745671540078661, -2.348512537728058902, -17.99195118506215962 ) ) ;
#26671=CARTESIAN_POINT ( 'NONE',  ( 113.0231681442453180, -10.15424416112533912, -14.75197769757731336 ) ) ;
#26676=CARTESIAN_POINT ( 'NONE',  ( 116.5969481442453031, -9.859900752359374465, -12.68260735090039404 ) ) ;
#26677=CARTESIAN_POINT ( 'NONE',  ( 116.7671281442453335, -1.834011780172310813, -8.268836392978581529 ) ) ;
#26679=CARTESIAN_POINT ( 'NONE',  ( 113.9875214775786532, -0.4660016031367893996, -10.09054647747474043 ) ) ;
#26680=CARTESIAN_POINT ( 'NONE',  ( 114.4413348109119823, -0.8288870151387760510, -10.36305467784173118 ) ) ;
#26681=CARTESIAN_POINT ( 'NONE',  ( 123.2906948109119867, -8.166667518702819706, -8.995218007635861213 ) ) ;
#26682=CARTESIAN_POINT ( 'NONE',  ( 123.6310548109119765, -5.638512984488999180, -18.83840828888717311 ) ) ;
#26684=CARTESIAN_POINT ( 'NONE',  ( 114.2711548109119803, -9.988377603198976828, -10.36322818467138340 ) ) ;
#26690=CARTESIAN_POINT ( 'NONE',  ( 120.2841814775786276, 0.9020085738987339008, -11.91225656197089222 ) ) ;
#26691=ORIENTED_EDGE ( 'NONE', *, *, #31803, .F. ) ;
#26692=CARTESIAN_POINT ( 'NONE',  ( 124.6521348109119884, -1.561330072975668948, -17.79121239304076951 ) ) ;
#26694=CARTESIAN_POINT ( 'NONE',  ( 116.1998614775786507, 0.4262465694468514643, -12.03445270309931736 ) ) ;
#26697=CARTESIAN_POINT ( 'NONE',  ( 118.1285681442453068, -7.893985811506177619, -18.51759400769804742 ) ) ;
#26702=CARTESIAN_POINT ( 'NONE',  ( 123.4608748109119745, 0.4262465694468514643, -12.03445270309931736 ) ) ;
#26703=CARTESIAN_POINT ( 'NONE',  ( 121.2485348109119769, -0.4660016031367893996, -10.09054647747474043 ) ) ;
#26705=CARTESIAN_POINT ( 'NONE',  ( 117.2776681442452968, -5.638512984488999180, -18.83840828888717311 ) ) ;
#26706=EDGE_CURVE ( 'NONE', #3839, #38119, #28609, .T. ) ;
#26707=CARTESIAN_POINT ( 'NONE',  ( 128.2184548109119930, -2.520019956603805511, -15.26558354049377009 ) ) ;
#26708=( BOUNDED_SURFACE ( )  B_SPLINE_SURFACE ( 1, 2, ( 
 ( #36506, #36727, #13035, #2076, #20104, #30357, #5277, #29676, #43822, #15774, #26035, #33522, #2758, #16684, #33300, #12360, #40396, #43364, #43588, #16000, #29907, #5948, #2529, #2302, #19637, #12133, #33761, #9380, #40168, #40856, #33990, #39941, #19196, #9160, #23064, #19872, #36948, #44282, #33073, #8932, #12588, #22833, #8702, #16232, #22607, #1845, #26492, #5493, #5719, #19414, #30135, #44049, #12813, #16456, #9610, #40623, #23290, #37174, #23529, #37415, #44730, #28061, #21212, #30577, #6419, #41532, #10290, #7080, #27618, #34862, #24196, #38517, #27167, #44497, #6863, #13711, #13261, #38087, #20771, #34651, #17136, #7295, #31243, #27394, #3436, #35089, #31464, #10510, #41316, #23977, #41088, #233, #10075, #37863, #17354, #34213, #13489, #9846, #20989, #3650, #6641, #14146, #10736, #15, #3872, #3210, #41970, #13927, #37645, #31023, #20550, #34431, #44954, #27836, #23755, #24635, #20327, #41750, #24411, #38301, #2985, #17570, #16912, #30805, #22333, #904, #10954, #11408, #35548, #42863, #15262, #8428, #25314, #31687, #18693, #18013, #7520, #32136, #1351, #14594, #42193, #36000, #35778, #4771, #7974, #25085, #38749, #36229, #7748, #455, #14371, #21436, #4546, #21660, #35318, #18473, #32582, #11183, #38980, #21882, #24857, #4320, #29170, #18241, #25759, #11623, #14824, #43084, #28284, #15046, #11852, #28735, #17791, #32361, #4090, #31911, #42639, #39665, #25535, #39208, #676, #28513, #28958, #42417, #1128, #39441, #8202, #22111, #29398, #22772, #8875, #29621, #5219, #12078, #40569, #26432, #33466, #44224, #26880, #32796, #4994, #5666, #19362, #9329, #8650, #2023, #15947, #39888, #36671, #40799, #43993, #18907, #43309, #19584, #9102, #25983, #33250, #29849, #22550, #12985, #1570, #26204, #2245, #36451, #15491, #12306, #43765, #23471, #23237, #16399, #19136, #16175, #33019, #37119, #5893, #12754, #9554, #30079, #26655, #12531, #1793, #15720, #19815, #30297, #5442, #40338, #43537, #33702, #2474, #23003, #40111, #36896, #10236, #20047, #20940, #27782, #10459 ),
 ( #3161, #17083, #13872, #34380, #41695, #30975, #176, #33930, #37356, #13657, #20501, #6128, #44899, #27565, #41479, #23928, #14091, #38037, #34159, #24144, #28010, #38248, #17303, #2931, #30752, #2700, #7028, #16860, #20273, #16629, #24362, #34813, #44674, #3597, #17510, #6812, #41916, #10019, #31409, #20720, #44445, #37808, #13437, #41261, #27341, #34599, #10680, #30523, #13212, #3384, #31194, #6583, #27111, #45114, #41034, #9790, #23701, #37590, #6362, #18183, #42364, #4495, #22056, #15212, #32078, #38466, #25482, #24801, #14317, #38920, #8152, #21377, #3813, #42812, #42584, #11574, #14768, #31858, #402, #29118, #14538, #7240, #21155, #28233, #11345, #28454, #42140, #25257, #39386, #17959, #626, #28681, #17735, #11125, #35948, #25025, #32527, #4720, #31633, #10901, #7689, #38693, #35030, #39154, #43030, #24582, #21604, #7459, #35492, #35260, #4036, #4264, #846, #32310, #28902, #7919, #21828, #35722, #14988, #18418, #1076, #18637, #1300, #11798, #32745, #22720, #36620, #33411, #8819, #16118, #5395, #19762, #8373, #25706, #33193, #40053, #39611, #19313, #1969, #15895, #43486, #33644, #12478, #8599, #29795, #2420, #12703, #36843, #22499, #5164, #22280, #26603, #36393, #19081, #43706, #15440, #32968, #40517, #30020, #26149, #26377, #40288, #23187, #39836, #2191, #12255, #1743, #36173, #15667, #5838, #9050, #5612, #22952, #9279, #4939, #19535, #37065, #43938, #16344, #30247, #18854, #1519, #29568, #29346, #43259, #12025, #25927, #6069, #10186, #13156, #23644, #40743, #27511, #9734, #23415, #16807, #2878, #37531, #44392, #19989, #34547, #20448, #41429, #38814, #21497, #26831, #44171, #44849, #13386, #3328, #2645, #41203, #9962, #33876, #30700, #35382, #37986, #12934, #37303, #13601, #3105, #16577, #27290, #23875, #30472, #7583, #9501, #20222, #24092, #27058, #40978, #6303, #37761, #18076, #17250, #11017, #34108, #6762, #44620, #31138, #521, #20671, #4161, #14433, #28341, #6530, #34331, #17032, #42254, #24918, #30922, #29016, #42702, #39723, #8488, #18529, #28796 ) ),
 .UNSPECIFIED., .F., .F., .F. ) 
 B_SPLINE_SURFACE_WITH_KNOTS ( ( 2, 2 ),
 ( 3, 2, 2, 2, 2, 2, 2, 2, 2, 2, 2, 2, 2, 2, 2, 2, 2, 2, 2, 2, 2, 2, 2, 2, 2, 2, 2, 2, 2, 2, 2, 2, 2, 2, 2, 2, 2, 2, 2, 2, 2, 2, 2, 2, 2, 2, 2, 2, 2, 2, 2, 2, 2, 2, 2, 2, 2, 2, 2, 2, 2, 2, 2, 2, 2, 2, 2, 2, 2, 2, 2, 2, 2, 2, 2, 2, 2, 2, 2, 2, 2, 2, 2, 2, 2, 2, 2, 2, 2, 2, 2, 2, 2, 2, 2, 2, 2, 2, 2, 2, 2, 2, 2, 2, 2, 2, 2, 2, 2, 2, 2, 2, 2, 2, 2, 2, 2, 2, 2, 2, 2, 2, 2, 2, 2, 2, 2, 2, 3 ),
 ( 0.000000000000000000, 1.000000000000000000 ),
 ( 0.000000000000000000, 0.007812500000000000000, 0.01562500000000000000, 0.02343750000000000000, 0.03125000000000000000, 0.03906250000000000000, 0.04687500000000000000, 0.05468750000000000000, 0.06250000000000000000, 0.07031250000000000000, 0.07812500000000000000, 0.08593750000000000000, 0.09375000000000000000, 0.1015625000000000000, 0.1093750000000000000, 0.1171875000000000000, 0.1250000000000000000, 0.1328125000000000000, 0.1406250000000000000, 0.1484375000000000000, 0.1562500000000000000, 0.1640625000000000000, 0.1718750000000000000, 0.1796875000000000000, 0.1875000000000000000, 0.1953125000000000000, 0.2031250000000000000, 0.2109375000000000000, 0.2187500000000000000, 0.2265625000000000000, 0.2343750000000000000, 0.2421875000000000000, 0.2500000000000000000, 0.2578125000000000000, 0.2656250000000000000, 0.2734375000000000000, 0.2812500000000000000, 0.2890625000000000000, 0.2968750000000000000, 0.3046875000000000000, 0.3125000000000000000, 0.3203125000000000000, 0.3281250000000000000, 0.3359375000000000000, 0.3437500000000000000, 0.3515625000000000000, 0.3593750000000000000, 0.3671875000000000000, 0.3750000000000000000, 0.3828125000000000000, 0.3906250000000000000, 0.3984375000000000000, 0.4062500000000000000, 0.4140625000000000000, 0.4218750000000000000, 0.4296875000000000000, 0.4375000000000000000, 0.4453125000000000000, 0.4531250000000000000, 0.4609375000000000000, 0.4687500000000000000, 0.4765625000000000000, 0.4843750000000000000, 0.4921875000000000000, 0.5000000000000000000, 0.5078125000000000000, 0.5156250000000000000, 0.5234375000000000000, 0.5312500000000000000, 0.5390625000000000000, 0.5468750000000000000, 0.5546875000000000000, 0.5625000000000000000, 0.5703125000000000000, 0.5781250000000000000, 0.5859375000000000000, 0.5937500000000000000, 0.6015625000000000000, 0.6093750000000000000, 0.6171875000000000000, 0.6250000000000000000, 0.6328125000000000000, 0.6406250000000000000, 0.6484375000000000000, 0.6562500000000000000, 0.6640625000000000000, 0.6718750000000000000, 0.6796875000000000000, 0.6875000000000000000, 0.6953125000000000000, 0.7031250000000000000, 0.7109375000000000000, 0.7187500000000000000, 0.7265625000000000000, 0.7343750000000000000, 0.7421875000000000000, 0.7500000000000000000, 0.7578125000000000000, 0.7656250000000000000, 0.7734375000000000000, 0.7812500000000000000, 0.7890625000000000000, 0.7968750000000000000, 0.8046875000000000000, 0.8125000000000000000, 0.8203125000000000000, 0.8281250000000000000, 0.8359375000000000000, 0.8437500000000000000, 0.8515625000000000000, 0.8593750000000000000, 0.8671875000000000000, 0.8750000000000000000, 0.8828125000000000000, 0.8906250000000000000, 0.8984375000000000000, 0.9062500000000000000, 0.9140625000000000000, 0.9218750000000000000, 0.9296875000000000000, 0.9375000000000000000, 0.9453125000000000000, 0.9531250000000000000, 0.9609375000000000000, 0.9687500000000000000, 0.9765625000000000000, 0.9843750000000000000, 0.9921875000000000000, 1.000000000000000000 ),
 .UNSPECIFIED. ) 
 GEOMETRIC_REPRESENTATION_ITEM ( )  RATIONAL_B_SPLINE_SURFACE ( (
 ( 1.000000000000000000, 0.9238795325112869605, 1.000000000000000000, 0.9238795325112869605, 1.000000000000000000, 0.9238795325112869605, 1.000000000000000000, 0.9238795325112869605, 1.000000000000000000, 0.9238795325112869605, 1.000000000000000000, 0.9238795325112869605, 1.000000000000000000, 0.9238795325112869605, 1.000000000000000000, 0.9238795325112869605, 1.000000000000000000, 0.9238795325112869605, 1.000000000000000000, 0.9238795325112869605, 1.000000000000000000, 0.9238795325112869605, 1.000000000000000000, 0.9238795325112869605, 1.000000000000000000, 0.9238795325112869605, 1.000000000000000000, 0.9238795325112869605, 1.000000000000000000, 0.9238795325112869605, 1.000000000000000000, 0.9238795325112869605, 1.000000000000000000, 0.9238795325112869605, 1.000000000000000000, 0.9238795325112869605, 1.000000000000000000, 0.9238795325112869605, 1.000000000000000000, 0.9238795325112869605, 1.000000000000000000, 0.9238795325112869605, 1.000000000000000000, 0.9238795325112869605, 1.000000000000000000, 0.9238795325112869605, 1.000000000000000000, 0.9238795325112869605, 1.000000000000000000, 0.9238795325112869605, 1.000000000000000000, 0.9238795325112869605, 1.000000000000000000, 0.9238795325112869605, 1.000000000000000000, 0.9238795325112869605, 1.000000000000000000, 0.9238795325112869605, 1.000000000000000000, 0.9238795325112869605, 1.000000000000000000, 0.9238795325112869605, 1.000000000000000000, 0.9238795325112869605, 1.000000000000000000, 0.9238795325112869605, 1.000000000000000000, 0.9238795325112869605, 1.000000000000000000, 0.9238795325112869605, 1.000000000000000000, 0.9238795325112869605, 1.000000000000000000, 0.9238795325112869605, 1.000000000000000000, 0.9238795325112869605, 1.000000000000000000, 0.9238795325112869605, 1.000000000000000000, 0.9238795325112869605, 1.000000000000000000, 0.9238795325112869605, 1.000000000000000000, 0.9238795325112869605, 1.000000000000000000, 0.9238795325112869605, 1.000000000000000000, 0.9238795325112869605, 1.000000000000000000, 0.9238795325112869605, 1.000000000000000000, 0.9238795325112869605, 1.000000000000000000, 0.9238795325112869605, 1.000000000000000000, 0.9238795325112869605, 1.000000000000000000, 0.9238795325112869605, 1.000000000000000000, 0.9238795325112869605, 1.000000000000000000, 0.9238795325112869605, 1.000000000000000000, 0.9238795325112869605, 1.000000000000000000, 0.9238795325112869605, 1.000000000000000000, 0.9238795325112869605, 1.000000000000000000, 0.9238795325112869605, 1.000000000000000000, 0.9238795325112869605, 1.000000000000000000, 0.9238795325112869605, 1.000000000000000000, 0.9238795325112869605, 1.000000000000000000, 0.9238795325112869605, 1.000000000000000000, 0.9238795325112869605, 1.000000000000000000, 0.9238795325112869605, 1.000000000000000000, 0.9238795325112869605, 1.000000000000000000, 0.9238795325112869605, 1.000000000000000000, 0.9238795325112869605, 1.000000000000000000, 0.9238795325112869605, 1.000000000000000000, 0.9238795325112869605, 1.000000000000000000, 0.9238795325112869605, 1.000000000000000000, 0.9238795325112869605, 1.000000000000000000, 0.9238795325112869605, 1.000000000000000000, 0.9238795325112869605, 1.000000000000000000, 0.9238795325112869605, 1.000000000000000000, 0.9238795325112869605, 1.000000000000000000, 0.9238795325112869605, 1.000000000000000000, 0.9238795325112869605, 1.000000000000000000, 0.9238795325112869605, 1.000000000000000000, 0.9238795325112869605, 1.000000000000000000, 0.9238795325112869605, 1.000000000000000000, 0.9238795325112869605, 1.000000000000000000, 0.9238795325112869605, 1.000000000000000000, 0.9238795325112869605, 1.000000000000000000, 0.9238795325112869605, 1.000000000000000000, 0.9238795325112869605, 1.000000000000000000, 0.9238795325112869605, 1.000000000000000000, 0.9238795325112869605, 1.000000000000000000, 0.9238795325112869605, 1.000000000000000000, 0.9238795325112869605, 1.000000000000000000, 0.9238795325112869605, 1.000000000000000000, 0.9238795325112869605, 1.000000000000000000, 0.9238795325112869605, 1.000000000000000000, 0.9238795325112869605, 1.000000000000000000, 0.9238795325112869605, 1.000000000000000000, 0.9238795325112869605, 1.000000000000000000, 0.9238795325112869605, 1.000000000000000000, 0.9238795325112869605, 1.000000000000000000, 0.9238795325112869605, 1.000000000000000000, 0.9238795325112869605, 1.000000000000000000, 0.9238795325112869605, 1.000000000000000000, 0.9238795325112869605, 1.000000000000000000, 0.9238795325112869605, 1.000000000000000000, 0.9238795325112869605, 1.000000000000000000, 0.9238795325112869605, 1.000000000000000000, 0.9238795325112869605, 1.000000000000000000, 0.9238795325112869605, 1.000000000000000000, 0.9238795325112869605, 1.000000000000000000, 0.9238795325112869605, 1.000000000000000000, 0.9238795325112869605, 1.000000000000000000, 0.9238795325112869605, 1.000000000000000000, 0.9238795325112869605, 1.000000000000000000, 0.9238795325112869605, 1.000000000000000000, 0.9238795325112869605, 1.000000000000000000, 0.9238795325112869605, 1.000000000000000000, 0.9238795325112869605, 1.000000000000000000, 0.9238795325112869605, 1.000000000000000000, 0.9238795325112869605, 1.000000000000000000, 0.9238795325112869605, 1.000000000000000000, 0.9238795325112869605, 1.000000000000000000, 0.9238795325112869605, 1.000000000000000000, 0.9238795325112869605, 1.000000000000000000, 0.9238795325112869605, 1.000000000000000000, 0.9238795325112869605, 1.000000000000000000, 0.9238795325112869605, 1.000000000000000000, 0.9238795325112869605, 1.000000000000000000, 0.9238795325112869605, 1.000000000000000000, 0.9238795325112869605, 1.000000000000000000, 0.9238795325112869605, 1.000000000000000000, 0.9238795325112869605, 1.000000000000000000, 0.9238795325112869605, 1.000000000000000000, 0.9238795325112869605, 1.000000000000000000),
 ( 1.000000000000000000, 0.9238795325112869605, 1.000000000000000000, 0.9238795325112869605, 1.000000000000000000, 0.9238795325112869605, 1.000000000000000000, 0.9238795325112869605, 1.000000000000000000, 0.9238795325112869605, 1.000000000000000000, 0.9238795325112869605, 1.000000000000000000, 0.9238795325112869605, 1.000000000000000000, 0.9238795325112869605, 1.000000000000000000, 0.9238795325112869605, 1.000000000000000000, 0.9238795325112869605, 1.000000000000000000, 0.9238795325112869605, 1.000000000000000000, 0.9238795325112869605, 1.000000000000000000, 0.9238795325112869605, 1.000000000000000000, 0.9238795325112869605, 1.000000000000000000, 0.9238795325112869605, 1.000000000000000000, 0.9238795325112869605, 1.000000000000000000, 0.9238795325112869605, 1.000000000000000000, 0.9238795325112869605, 1.000000000000000000, 0.9238795325112869605, 1.000000000000000000, 0.9238795325112869605, 1.000000000000000000, 0.9238795325112869605, 1.000000000000000000, 0.9238795325112869605, 1.000000000000000000, 0.9238795325112869605, 1.000000000000000000, 0.9238795325112869605, 1.000000000000000000, 0.9238795325112869605, 1.000000000000000000, 0.9238795325112869605, 1.000000000000000000, 0.9238795325112869605, 1.000000000000000000, 0.9238795325112869605, 1.000000000000000000, 0.9238795325112869605, 1.000000000000000000, 0.9238795325112869605, 1.000000000000000000, 0.9238795325112869605, 1.000000000000000000, 0.9238795325112869605, 1.000000000000000000, 0.9238795325112869605, 1.000000000000000000, 0.9238795325112869605, 1.000000000000000000, 0.9238795325112869605, 1.000000000000000000, 0.9238795325112869605, 1.000000000000000000, 0.9238795325112869605, 1.000000000000000000, 0.9238795325112869605, 1.000000000000000000, 0.9238795325112869605, 1.000000000000000000, 0.9238795325112869605, 1.000000000000000000, 0.9238795325112869605, 1.000000000000000000, 0.9238795325112869605, 1.000000000000000000, 0.9238795325112869605, 1.000000000000000000, 0.9238795325112869605, 1.000000000000000000, 0.9238795325112869605, 1.000000000000000000, 0.9238795325112869605, 1.000000000000000000, 0.9238795325112869605, 1.000000000000000000, 0.9238795325112869605, 1.000000000000000000, 0.9238795325112869605, 1.000000000000000000, 0.9238795325112869605, 1.000000000000000000, 0.9238795325112869605, 1.000000000000000000, 0.9238795325112869605, 1.000000000000000000, 0.9238795325112869605, 1.000000000000000000, 0.9238795325112869605, 1.000000000000000000, 0.9238795325112869605, 1.000000000000000000, 0.9238795325112869605, 1.000000000000000000, 0.9238795325112869605, 1.000000000000000000, 0.9238795325112869605, 1.000000000000000000, 0.9238795325112869605, 1.000000000000000000, 0.9238795325112869605, 1.000000000000000000, 0.9238795325112869605, 1.000000000000000000, 0.9238795325112869605, 1.000000000000000000, 0.9238795325112869605, 1.000000000000000000, 0.9238795325112869605, 1.000000000000000000, 0.9238795325112869605, 1.000000000000000000, 0.9238795325112869605, 1.000000000000000000, 0.9238795325112869605, 1.000000000000000000, 0.9238795325112869605, 1.000000000000000000, 0.9238795325112869605, 1.000000000000000000, 0.9238795325112869605, 1.000000000000000000, 0.9238795325112869605, 1.000000000000000000, 0.9238795325112869605, 1.000000000000000000, 0.9238795325112869605, 1.000000000000000000, 0.9238795325112869605, 1.000000000000000000, 0.9238795325112869605, 1.000000000000000000, 0.9238795325112869605, 1.000000000000000000, 0.9238795325112869605, 1.000000000000000000, 0.9238795325112869605, 1.000000000000000000, 0.9238795325112869605, 1.000000000000000000, 0.9238795325112869605, 1.000000000000000000, 0.9238795325112869605, 1.000000000000000000, 0.9238795325112869605, 1.000000000000000000, 0.9238795325112869605, 1.000000000000000000, 0.9238795325112869605, 1.000000000000000000, 0.9238795325112869605, 1.000000000000000000, 0.9238795325112869605, 1.000000000000000000, 0.9238795325112869605, 1.000000000000000000, 0.9238795325112869605, 1.000000000000000000, 0.9238795325112869605, 1.000000000000000000, 0.9238795325112869605, 1.000000000000000000, 0.9238795325112869605, 1.000000000000000000, 0.9238795325112869605, 1.000000000000000000, 0.9238795325112869605, 1.000000000000000000, 0.9238795325112869605, 1.000000000000000000, 0.9238795325112869605, 1.000000000000000000, 0.9238795325112869605, 1.000000000000000000, 0.9238795325112869605, 1.000000000000000000, 0.9238795325112869605, 1.000000000000000000, 0.9238795325112869605, 1.000000000000000000, 0.9238795325112869605, 1.000000000000000000, 0.9238795325112869605, 1.000000000000000000, 0.9238795325112869605, 1.000000000000000000, 0.9238795325112869605, 1.000000000000000000, 0.9238795325112869605, 1.000000000000000000, 0.9238795325112869605, 1.000000000000000000, 0.9238795325112869605, 1.000000000000000000, 0.9238795325112869605, 1.000000000000000000, 0.9238795325112869605, 1.000000000000000000, 0.9238795325112869605, 1.000000000000000000, 0.9238795325112869605, 1.000000000000000000, 0.9238795325112869605, 1.000000000000000000, 0.9238795325112869605, 1.000000000000000000, 0.9238795325112869605, 1.000000000000000000, 0.9238795325112869605, 1.000000000000000000, 0.9238795325112869605, 1.000000000000000000, 0.9238795325112869605, 1.000000000000000000, 0.9238795325112869605, 1.000000000000000000, 0.9238795325112869605, 1.000000000000000000, 0.9238795325112869605, 1.000000000000000000, 0.9238795325112869605, 1.000000000000000000, 0.9238795325112869605, 1.000000000000000000, 0.9238795325112869605, 1.000000000000000000, 0.9238795325112869605, 1.000000000000000000, 0.9238795325112869605, 1.000000000000000000, 0.9238795325112869605, 1.000000000000000000, 0.9238795325112869605, 1.000000000000000000, 0.9238795325112869605, 1.000000000000000000, 0.9238795325112869605, 1.000000000000000000) ) ) 
 REPRESENTATION_ITEM ( '' )  SURFACE ( )  );
#26709=CARTESIAN_POINT ( 'NONE',  ( 125.6164881442453094, -9.565557343593413364, -10.61323700422348004 ) ) ;
#26710=CARTESIAN_POINT ( 'NONE',  ( 118.0718414775786442, -0.8288870151387760510, -10.36305467784173118 ) ) ;
#26715=CARTESIAN_POINT ( 'NONE',  ( 119.8303681442453126, 0.4262465694468514643, -12.03445270309931736 ) ) ;
#26718=CARTESIAN_POINT ( 'NONE',  ( 117.9583881442453048, -10.30919188438810075, -12.61870101168855918 ) ) ;
#26720=CARTESIAN_POINT ( 'NONE',  ( 116.7671281442453335, -7.643976991954077427, -18.09477374809248928 ) ) ;
#26721=CONICAL_SURFACE ( 'NONE', #10706, 5.999999999999997335, 0.4636476090008060935 ) ;
#26722=ORIENTED_EDGE ( 'NONE', *, *, #37597, .T. ) ;
#26724=CARTESIAN_POINT ( 'NONE',  ( 125.5597614775786326, -7.894159318335828068, -9.358103419637847864 ) ) ;
#26725=CARTESIAN_POINT ( 'NONE',  ( 120.8514481442452961, -2.084020599724406786, -8.691656652584148546 ) ) ;
#26729=CARTESIAN_POINT ( 'NONE',  ( 117.5613014775786525, 0.9020085738987339008, -11.91225656197089222 ) ) ;
#26732=CARTESIAN_POINT ( 'NONE',  ( 118.6958348109119754, -6.344957434206665248, -7.627207830600338134 ) ) ;
#26734=CARTESIAN_POINT ( 'NONE',  ( 115.3489614775786407, -9.261995988541697145, -16.69588392320189030 ) ) ;
#26735=CARTESIAN_POINT ( 'NONE',  ( 114.6115148109119986, -6.222761293078241884, -8.102969835052219238 ) ) ;
#26737=CARTESIAN_POINT ( 'NONE',  ( 114.1577014775786552, -6.344957434206662583, -7.627207830600332805 ) ) ;
#26739=CARTESIAN_POINT ( 'NONE',  ( 123.6877814775786533, -6.222761293078241884, -8.102969835052219238 ) ) ;
#26740=CARTESIAN_POINT ( 'NONE',  ( 123.5176014775786228, -9.261995988541684710, -16.69588392320190806 ) ) ;
#26742=B_SPLINE_CURVE_WITH_KNOTS ( 'NONE', 3,
 ( #9802, #2486, #16640, #44687, #6140, #27353, #16872, #33715, #40581, #34611 ),
 .UNSPECIFIED., .F., .F.,
 ( 4, 3, 3, 4 ),
 ( 0.000000000000000000, 0.0001671877548681284921, 0.0003343755096277705222, 0.0006463528481650609656 ),
 .UNSPECIFIED. ) ;
#26748=CARTESIAN_POINT ( 'NONE',  ( 122.4965214775786251, -10.30919188438810075, -12.61870101168855918 ) ) ;
#26750=CARTESIAN_POINT ( 'NONE',  ( 120.5678148109119832, -8.166667518702819706, -8.995218007635861213 ) ) ;
#26751=CARTESIAN_POINT ( 'NONE',  ( 112.5126281442453120, 0.1319031606808879209, -14.10382304977623669 ) ) ;
#26753=CARTESIAN_POINT ( 'NONE',  ( 121.4187148109119789, -6.344957434206665248, -7.627207830600338134 ) ) ;
#26754=CARTESIAN_POINT ( 'NONE',  ( 121.9292548109119849, -1.561330072975668948, -17.79121239304076951 ) ) ;
#26756=CARTESIAN_POINT ( 'NONE',  ( 123.0637881442452937, -8.899110576539710493, -16.42337572283490132 ) ) ;
#26758=CARTESIAN_POINT ( 'NONE',  ( 111.8471337256649036, -1.063912429576150842, -17.20460841810474406 ) ) ;
#26761=CARTESIAN_POINT ( 'NONE',  ( 118.7342755643466745, -1.244021962887374544, -16.96476564598603076 ) ) ;
#26762=CARTESIAN_POINT ( 'NONE',  ( 123.9146881442452894, -10.15424416112533912, -14.75197769757731336 ) ) ;
#26765=CARTESIAN_POINT ( 'NONE',  ( 116.3133148109120043, -2.084020599724406786, -8.691656652584148546 ) ) ;
#26768=CARTESIAN_POINT ( 'NONE',  ( 115.6893214775786447, -9.859900752359374465, -12.68260735090039404 ) ) ;
#26769=CARTESIAN_POINT ( 'NONE',  ( 121.8158014775786171, -5.638512984488999180, -18.83840828888717311 ) ) ;
#26772=CARTESIAN_POINT ( 'NONE',  ( 120.8514481442452961, -2.084020599724406786, -8.691656652584148546 ) ) ;
#26773=CARTESIAN_POINT ( 'NONE',  ( 117.6180281442453150, -0.4660016031367893996, -10.09054647747474043 ) ) ;
#26774=CARTESIAN_POINT ( 'NONE',  ( 123.4041481442452834, -10.30919188438810075, -12.61870101168855918 ) ) ;
#26775=CARTESIAN_POINT ( 'NONE',  ( 121.7023481442452777, -0.8288870151387760510, -10.36305467784173118 ) ) ;
#26779=CARTESIAN_POINT ( 'NONE',  ( 123.5743281442453139, -7.893985811506177619, -18.51759400769804742 ) ) ;
#26780=CARTESIAN_POINT ( 'NONE',  ( 113.3068014775786594, -1.833838273342658809, -17.42832698103878286 ) ) ;
#26782=CARTESIAN_POINT ( 'NONE',  ( 124.1983214775786166, -8.166667518702819706, -8.995218007635861213 ) ) ;
#26788=CARTESIAN_POINT ( 'NONE',  ( 120.9649014775786355, -6.222761293078241884, -8.102969835052219238 ) ) ;
#26789=CARTESIAN_POINT ( 'NONE',  ( 115.1787814775786387, -0.1624402480850797581, -16.17319339645315424 ) ) ;
#26790=CARTESIAN_POINT ( 'NONE',  ( 127.0545391123781798, -6.690369086889063510, -18.49686471125335530 ) ) ;
#26791=ORIENTED_EDGE ( 'NONE', *, *, #20500, .T. ) ;
#26793=CARTESIAN_POINT ( 'NONE',  ( 117.5045748109119756, -9.859900752359374465, -12.68260735090039404 ) ) ;
#26794=CARTESIAN_POINT ( 'NONE',  ( 113.4202548109119846, 0.1319031606808879209, -14.10382304977623669 ) ) ;
#26796=CARTESIAN_POINT ( 'NONE',  ( 128.2184548109119930, -4.863998795839242995, -13.39321520033831447 ) ) ;
#26797=CARTESIAN_POINT ( 'NONE',  ( 121.8158014775786171, -5.638512984488999180, -18.83840828888717311 ) ) ;
#26798=CARTESIAN_POINT ( 'NONE',  ( 112.7962614775786676, -3.383040157471821630, -19.15922257007629170 ) ) ;
#26801=CARTESIAN_POINT ( 'NONE',  ( 126.7702028005564756, 0.1629706377663181216, -14.99492149720868994 ) ) ;
#26804=CARTESIAN_POINT ( 'NONE',  ( 111.7184548109119788, -9.261995988541697145, -16.69588392320189030 ) ) ;
#26805=CARTESIAN_POINT ( 'NONE',  ( 120.6245414775786458, -0.1624402480850797581, -16.17319339645315424 ) ) ;
#26810=CARTESIAN_POINT ( 'NONE',  ( 113.5337081442453240, -0.8288870151387760510, -10.36305467784173118 ) ) ;
#26814=CARTESIAN_POINT ( 'NONE',  ( 125.1626748109119802, -9.988377603198980381, -10.36322818467138518 ) ) ;
#26815=CARTESIAN_POINT ( 'NONE',  ( 120.9081748109119872, -5.638512984488999180, -18.83840828888717311 ) ) ;
#26817=CARTESIAN_POINT ( 'NONE',  ( 118.3554748109119998, 0.2603800115204892296, -16.42320221600525088 ) ) ;
#26818=CARTESIAN_POINT ( 'NONE',  ( 112.2289948109119848, -1.834011780172310813, -8.268836392978581529 ) ) ;
#26820=CARTESIAN_POINT ( 'NONE',  ( 113.9307948109119764, -10.15424416112533912, -14.75197769757731336 ) ) ;
#26821=CARTESIAN_POINT ( 'NONE',  ( 112.3424481442453384, -3.505236298600246325, -18.68346056562440793 ) ) ;
#26822=CARTESIAN_POINT ( 'NONE',  ( 120.1140014775786398, -1.561330072975668504, -17.79121239304076951 ) ) ;
#26824=CARTESIAN_POINT ( 'NONE',  ( 113.3635281442453504, -9.988377603198976828, -10.36322818467138340 ) ) ;
#26825=EDGE_CURVE ( 'NONE', #22022, #40242, #3322, .T. ) ;
#26826=CARTESIAN_POINT ( 'NONE',  ( 126.1837548109119211, -10.63000616557722466, -14.87417383870573495 ) ) ;
#26827=EDGE_LOOP ( 'NONE', ( #26942, #11690, #1348, #35499, #4859 ) ) ;
#26828=CARTESIAN_POINT ( 'NONE',  ( 117.5045748109119756, -9.859900752359374465, -12.68260735090039404 ) ) ;
#26829=CARTESIAN_POINT ( 'NONE',  ( 124.8223148109119762, 0.9020085738987339008, -11.91225656197089222 ) ) ;
#26831=CARTESIAN_POINT ( 'NONE',  ( 122.8936081442453059, -9.565557343593413364, -10.61323700422348004 ) ) ;
#26833=DIRECTION ( 'NONE',  ( 1.000000000000000000, 0.000000000000000000, 0.000000000000000000 ) ) ;
#26836=CARTESIAN_POINT ( 'NONE',  ( 124.4252281442452812, -9.261995988541697145, -16.69588392320189030 ) ) ;
#26838=CARTESIAN_POINT ( 'NONE',  ( 111.9453614775786434, -1.561330072975668060, -17.79121239304076596 ) ) ;
#26843=CARTESIAN_POINT ( 'NONE',  ( 123.6462803923315334, -1.063912429576147511, -17.20460841810472985 ) ) ;
#26844=CARTESIAN_POINT ( 'NONE',  ( 137.3111100276077821, -4.833481128352631551, -18.60023654913463531 ) ) ;
#26846=CARTESIAN_POINT ( 'NONE',  ( 125.3895814775786448, -7.893985811506177619, -18.51759400769804742 ) ) ;
#26847=CARTESIAN_POINT ( 'NONE',  ( 121.4754414775786131, -1.833838273342659697, -17.42832698103878286 ) ) ;
#26850=CARTESIAN_POINT ( 'NONE',  ( 121.8725281442453223, -3.383040157471821630, -19.15922257007629170 ) ) ;
#26851=CARTESIAN_POINT ( 'NONE',  ( 118.6391081442452986, -4.089484607189486809, -7.948022111789456723 ) ) ;
#26853=CARTESIAN_POINT ( 'NONE',  ( 113.2500748109119968, -3.505236298600246325, -18.68346056562440793 ) ) ;
#26854=CARTESIAN_POINT ( 'NONE',  ( 112.7395348109119766, -5.638512984488999180, -18.83840828888717311 ) ) ;
#26855=CARTESIAN_POINT ( 'NONE',  ( 125.2761281442453054, -10.63000616557722466, -14.87417383870573495 ) ) ;
#26859=CARTESIAN_POINT ( 'NONE',  ( 115.8595014775786609, -7.643976991954077427, -18.09477374809248928 ) ) ;
#26860=CARTESIAN_POINT ( 'NONE',  ( 115.5758681442453053, -7.894159318335828068, -9.358103419637847864 ) ) ;
#26865=CARTESIAN_POINT ( 'NONE',  ( 123.8579614775786126, -9.859900752359378018, -12.68260735090039759 ) ) ;
#26866=CARTESIAN_POINT ( 'NONE',  ( 111.9453614775786434, -1.561330072975668060, -17.79121239304076596 ) ) ;
#26869=EDGE_LOOP ( 'NONE', ( #43071, #15815, #24691, #16182 ) ) ;
#26872=CARTESIAN_POINT ( 'NONE',  ( 117.4478481442453131, 0.2603800115204892296, -16.42320221600525088 ) ) ;
#26873=CARTESIAN_POINT ( 'NONE',  ( 125.5030348109119558, -6.222761293078241884, -8.102969835052219238 ) ) ;
#26875=CARTESIAN_POINT ( 'NONE',  ( 115.9162281442453235, -5.574606645277164318, -18.38911715685844683 ) ) ;
#26877=CARTESIAN_POINT ( 'NONE',  ( 120.1140014775786398, -1.561330072975668504, -17.79121239304076951 ) ) ;
#26878=CARTESIAN_POINT ( 'NONE',  ( 115.4056881442453459, -7.893985811506177619, -18.51759400769804742 ) ) ;
#26880=CARTESIAN_POINT ( 'NONE',  ( 122.9503348109119827, 0.5811942927096110934, -14.16772938898807510 ) ) ;
#26883=CARTESIAN_POINT ( 'NONE',  ( 119.6601881442453106, -8.166667518702819706, -8.995218007635861213 ) ) ;
#26884=CARTESIAN_POINT ( 'NONE',  ( 113.4769814775786330, 0.4262465694468514643, -12.03445270309931736 ) ) ;
#26885=CARTESIAN_POINT ( 'NONE',  ( 126.5561942423801014, -4.902127430340050829, -18.56199476000752568 ) ) ;
#26886=CARTESIAN_POINT ( 'NONE',  ( 125.9001214775786224, -5.574606645277164318, -18.38911715685844683 ) ) ;
#26888=CARTESIAN_POINT ( 'NONE',  ( 122.6099748109119929, -9.261995988541697145, -16.69588392320189030 ) ) ;
#26890=CARTESIAN_POINT ( 'NONE',  ( 115.8542891344827552, -1.149058757900091265, -17.09122335155388939 ) ) ;
#26893=CARTESIAN_POINT ( 'NONE',  ( 116.2565881442453133, -0.8288870151387760510, -10.36305467784173118 ) ) ;
#26894=CARTESIAN_POINT ( 'NONE',  ( 137.3374356171257489, -3.432627534740069652, -8.412905839694147403 ) ) ;
#26895=CARTESIAN_POINT ( 'NONE',  ( 117.1642148109119859, -0.8288870151387760510, -10.36305467784173118 ) ) ;
#26899=CARTESIAN_POINT ( 'NONE',  ( 115.5758681442453053, -7.894159318335828068, -9.358103419637847864 ) ) ;
#26900=CARTESIAN_POINT ( 'NONE',  ( 115.8595014775786609, -1.834011780172310813, -8.268836392978581529 ) ) ;
#26903=CARTESIAN_POINT ( 'NONE',  ( 112.1155414775786454, 0.9020085738987339008, -11.91225656197089222 ) ) ;
#26904=CARTESIAN_POINT ( 'NONE',  ( 115.1220548109119761, -1.833838273342658809, -17.42832698103878286 ) ) ;
#26905=CARTESIAN_POINT ( 'NONE',  ( 124.0281414775786146, -1.834011780172310813, -8.268836392978581529 ) ) ;
#26906=CARTESIAN_POINT ( 'NONE',  ( 120.2274548109119934, 0.5811942927096110934, -14.16772938898807510 ) ) ;
#26908=CARTESIAN_POINT ( 'NONE',  ( 114.7249681442453237, 0.2603800115204892296, -16.42320221600525088 ) ) ;
#26912=CARTESIAN_POINT ( 'NONE',  ( 128.0094361930251523, -4.111821299675517238, -15.64381207447768851 ) ) ;
#26913=CARTESIAN_POINT ( 'NONE',  ( 119.4900081442453086, -1.834011780172310813, -8.268836392978581529 ) ) ;
#26915=CARTESIAN_POINT ( 'NONE',  ( 125.1059481442452750, -8.166667518702819706, -8.995218007635861213 ) ) ;
#26916=FACE_OUTER_BOUND ( 'NONE', #736, .T. ) ;
#26917=CARTESIAN_POINT ( 'NONE',  ( 114.6682414775786469, -7.894159318335828068, -9.358103419637847864 ) ) ;
#26919=CARTESIAN_POINT ( 'NONE',  ( 121.7023481442452777, -9.261995988541697145, -16.69588392320189030 ) ) ;
#26921=CARTESIAN_POINT ( 'NONE',  ( 128.2184548109119930, -4.863998795839242995, -13.39321520033831447 ) ) ;
#26924=CARTESIAN_POINT ( 'NONE',  ( 123.9714148109119805, -8.899110576539710493, -16.42337572283490132 ) ) ;
#26925=CARTESIAN_POINT ( 'NONE',  ( 120.5110881442453206, -6.344957434206665248, -7.627207830600338134 ) ) ;
#26926=CARTESIAN_POINT ( 'NONE',  ( 113.1933481442453058, -5.574606645277164318, -18.38911715685844683 ) ) ;
#26927=CARTESIAN_POINT ( 'NONE',  ( 115.9162281442453235, -4.089484607189486809, -7.948022111789456723 ) ) ;
#26930=CARTESIAN_POINT ( 'NONE',  ( 120.1707281442453166, -9.565557343593413364, -10.61323700422348004 ) ) ;
#26932=CARTESIAN_POINT ( 'NONE',  ( 119.9438214775786520, -7.893985811506198047, -18.51759400769803676 ) ) ;
#26935=CARTESIAN_POINT ( 'NONE',  ( 121.2485348109119769, -8.899110576539710493, -16.42337572283490132 ) ) ;
#26938=CARTESIAN_POINT ( 'NONE',  ( 120.1707281442453166, 0.2603800115204892296, -16.42320221600525088 ) ) ;
#26940=CARTESIAN_POINT ( 'NONE',  ( 116.1431348109119881, 0.1319031606808879209, -14.10382304977623669 ) ) ;
#26942=ORIENTED_EDGE ( 'NONE', *, *, #33669, .F. ) ;
#26944=CARTESIAN_POINT ( 'NONE',  ( 112.1722681442453222, -0.4660016031367893996, -10.09054647747474043 ) ) ;
#26945=CARTESIAN_POINT ( 'NONE',  ( 119.2631014775786298, -9.565557343593413364, -10.61323700422348004 ) ) ;
#26947=B_SPLINE_CURVE_WITH_KNOTS ( 'NONE', 3,
 ( #5488, #40390, #5270, #43358, #36719, #2071, #15994, #29899 ),
 .UNSPECIFIED., .F., .F.,
 ( 4, 2, 2, 4 ),
 ( 0.000000000000000000, 0.2499999999999995559, 0.4999999999999991118, 1.000000000000000000 ),
 .UNSPECIFIED. ) ;
#26950=CARTESIAN_POINT ( 'NONE',  ( 117.2209414775786485, -7.893985811506177619, -18.51759400769804742 ) ) ;
#26952=CARTESIAN_POINT ( 'NONE',  ( 118.8092881442453290, -9.988377603198976828, -10.36322818467138340 ) ) ;
#26953=CARTESIAN_POINT ( 'NONE',  ( 117.7882081442453170, -6.344957434206665248, -7.627207830600338134 ) ) ;
#26954=CARTESIAN_POINT ( 'NONE',  ( 119.2063748109119814, -7.894159318335828068, -9.358103419637847864 ) ) ;
#26955=CARTESIAN_POINT ( 'NONE',  ( 123.4041481442452834, 0.1319031606808879209, -14.10382304977623669 ) ) ;
#26956=CARTESIAN_POINT ( 'NONE',  ( 112.0020881442453344, 0.2603800115204892296, -16.42320221600525088 ) ) ;
#26957=EDGE_CURVE ( 'NONE', #33070, #39008, #1127, .T. ) ;
#26959=CARTESIAN_POINT ( 'NONE',  ( 123.5743281442453139, -2.084020599724406786, -8.691656652584148546 ) ) ;
#26966=CARTESIAN_POINT ( 'NONE',  ( 121.3619881442452879, -4.089484607189486809, -7.948022111789456723 ) ) ;
#26967=CARTESIAN_POINT ( 'NONE',  ( 121.4754414775786131, -1.833838273342659697, -17.42832698103878286 ) ) ;
#26969=CARTESIAN_POINT ( 'NONE',  ( 125.3895814775786448, -7.893985811506177619, -18.51759400769804742 ) ) ;
#26970=CARTESIAN_POINT ( 'NONE',  ( 113.0798948109119948, -8.899110576539710493, -16.42337572283490132 ) ) ;
#26971=CARTESIAN_POINT ( 'NONE',  ( 121.5888948109119809, 0.1319031606808809820, -14.10382304977626156 ) ) ;
#26972=CARTESIAN_POINT ( 'NONE',  ( 120.9081748109119872, -5.638512984488999180, -18.83840828888717311 ) ) ;
#26974=CARTESIAN_POINT ( 'NONE',  ( 120.0005481442453146, -5.638512984488999180, -18.83840828888717311 ) ) ;
#26976=CARTESIAN_POINT ( 'NONE',  ( 125.2194014775786286, 0.1319031606808879209, -14.10382304977623669 ) ) ;
#26981=AXIS2_PLACEMENT_3D ( 'NONE', #7792, #29211, #37101 ) ;
#26983=CARTESIAN_POINT ( 'NONE',  ( 122.8368814775786291, -7.894159318335828068, -9.358103419637847864 ) ) ;
#26987=CARTESIAN_POINT ( 'NONE',  ( 118.0718414775786442, -0.8288870151387760510, -10.36305467784173118 ) ) ;
#26988=CARTESIAN_POINT ( 'NONE',  ( 114.7816948109119863, -9.859900752359374465, -12.68260735090039404 ) ) ;
#26989=CARTESIAN_POINT ( 'NONE',  ( 123.8012348109119642, 0.2603800115204892296, -16.42320221600525088 ) ) ;
#26992=CARTESIAN_POINT ( 'NONE',  ( 123.6310548109119765, -4.153390946401325223, -8.397313243818185668 ) ) ;
#26993=CARTESIAN_POINT ( 'NONE',  ( 119.7169148109119874, -9.988377603198976828, -10.36322818467138340 ) ) ;
#26994=CARTESIAN_POINT ( 'NONE',  ( 123.7445081442452874, -1.561330072975668948, -17.79121239304076951 ) ) ;
#26995=CARTESIAN_POINT ( 'NONE',  ( 124.0848681442452772, -5.574606645277164318, -18.38911715685844683 ) ) ;
#27000=CARTESIAN_POINT ( 'NONE',  ( 125.5030348109119558, -3.383040157471821630, -19.15922257007629170 ) ) ;
#27002=CARTESIAN_POINT ( 'NONE',  ( 116.1998614775786507, 0.4262465694468514643, -12.03445270309931736 ) ) ;
#27003=CARTESIAN_POINT ( 'NONE',  ( 124.8223148109119762, 0.9020085738987339008, -11.91225656197089222 ) ) ;
#27013=ADVANCED_FACE ( 'NONE', ( #28738 ), #16863, .T. ) ;
#27014=CARTESIAN_POINT ( 'NONE',  ( 120.3409081442453044, -8.899110576539710493, -16.42337572283490132 ) ) ;
#27015=CARTESIAN_POINT ( 'NONE',  ( 112.6828081442453282, -2.084020599724406786, -8.691656652584148546 ) ) ;
#27016=CARTESIAN_POINT ( 'NONE',  ( 126.3618269276777255, -6.022947313180186946, -18.33077713658678221 ) ) ;
#27020=CARTESIAN_POINT ( 'NONE',  ( 126.2184548109119788, -2.495269033102075262, -17.79652296963211455 ) ) ;
#27021=CARTESIAN_POINT ( 'NONE',  ( 118.8660148109119774, 0.1319031606808879209, -14.10382304977623669 ) ) ;
#27022=CARTESIAN_POINT ( 'NONE',  ( 113.7038881442453402, -6.222761293078241884, -8.102969835052219238 ) ) ;
#27024=CARTESIAN_POINT ( 'NONE',  ( 111.3213681442453264, -7.643976991954077427, -18.09477374809248928 ) ) ;
#27026=CARTESIAN_POINT ( 'NONE',  ( 124.0848681442452772, -4.089484607189486809, -7.948022111789456723 ) ) ;
#27027=CARTESIAN_POINT ( 'NONE',  ( 113.0798948109119948, -0.4660016031367893996, -10.09054647747474043 ) ) ;
#27029=CARTESIAN_POINT ( 'NONE',  ( 114.6682414775786469, -1.561330072975668060, -17.79121239304076596 ) ) ;
#27032=CARTESIAN_POINT ( 'NONE',  ( 126.0135748109119902, -1.833838273342660141, -17.42832698103878286 ) ) ;
#27033=CARTESIAN_POINT ( 'NONE',  ( 119.8303681442453126, 0.4262465694468514643, -12.03445270309931736 ) ) ;
#27038=CARTESIAN_POINT ( 'NONE',  ( 113.3068014775786594, -1.833838273342658809, -17.42832698103878286 ) ) ;
#27042=CARTESIAN_POINT ( 'NONE',  ( 123.8012348109119642, 0.2603800115204892296, -16.42320221600525088 ) ) ;
#27043=CARTESIAN_POINT ( 'NONE',  ( 120.3976348109119812, -1.834011780172310813, -8.268836392978581529 ) ) ;
#27045=CARTESIAN_POINT ( 'NONE',  ( 119.2631014775786298, 0.2603800115204892296, -16.42320221600525088 ) ) ;
#27046=CARTESIAN_POINT ( 'NONE',  ( 113.5337081442453240, -9.261995988541697145, -16.69588392320189030 ) ) ;
#27048=CARTESIAN_POINT ( 'NONE',  ( 112.8529881442453302, -7.894159318335828068, -9.358103419637847864 ) ) ;
#27049=CARTESIAN_POINT ( 'NONE',  ( 124.5954081442453116, -3.383040157471821630, -19.15922257007629170 ) ) ;
#27051=CARTESIAN_POINT ( 'NONE',  ( 125.3895814775786448, -7.893985811506177619, -18.51759400769804742 ) ) ;
#27052=CARTESIAN_POINT ( 'NONE',  ( 112.5693548109119888, -10.63000616557722466, -14.87417383870573495 ) ) ;
#27053=CARTESIAN_POINT ( 'NONE',  ( 111.8319081442453182, -4.153390946401321671, -8.397313243818183892 ) ) ;
#27055=CARTESIAN_POINT ( 'NONE',  ( 117.2776681442452968, -4.153390946401325223, -8.397313243818185668 ) ) ;
#27056=CARTESIAN_POINT ( 'NONE',  ( 112.9664414775786412, 0.5811942927096154232, -14.16772938898807155 ) ) ;
#27058=CARTESIAN_POINT ( 'NONE',  ( 124.2550481442452792, -0.1624402480850797581, -16.17319339645315424 ) ) ;
#27062=CARTESIAN_POINT ( 'NONE',  ( 114.4917429525735741, -1.111561923218669534, -17.14115599315433869 ) ) ;
#27072=CARTESIAN_POINT ( 'NONE',  ( 119.3198281442452924, 0.5811942927096110934, -14.16772938898807510 ) ) ;
#27073=CARTESIAN_POINT ( 'NONE',  ( 136.9082792203374197, -4.441316609263642690, -18.90303633254767846 ) ) ;
#27077=CARTESIAN_POINT ( 'NONE',  ( 122.4397948109119767, -0.1624402480850797581, -16.17319339645315424 ) ) ;
#27078=CARTESIAN_POINT ( 'NONE',  ( 125.3328548109119964, -0.8288870151387760510, -10.36305467784173118 ) ) ;
#27080=CARTESIAN_POINT ( 'NONE',  ( 122.7234281442452755, -5.638512984488999180, -18.83840828888717311 ) ) ;
#27082=CARTESIAN_POINT ( 'NONE',  ( 118.2420214775786320, -3.383040157471821630, -19.15922257007629170 ) ) ;
#27083=CARTESIAN_POINT ( 'NONE',  ( 125.8433948109119456, -1.834011780172310813, -8.268836392978581529 ) ) ;
#27084=CARTESIAN_POINT ( 'NONE',  ( 113.4769814775786330, 0.4262465694468514643, -12.03445270309931736 ) ) ;
#27085=CARTESIAN_POINT ( 'NONE',  ( 125.5597614775786326, -1.561330072975669392, -17.79121239304076951 ) ) ;
#27089=CARTESIAN_POINT ( 'NONE',  ( 115.9162281442453235, -5.574606645277164318, -18.38911715685844683 ) ) ;
#27090=CARTESIAN_POINT ( 'NONE',  ( 118.4122014775786340, -9.859900752359374465, -12.68260735090039404 ) ) ;
#27093=ORIENTED_EDGE ( 'NONE', *, *, #29098, .T. ) ;
#27095=CARTESIAN_POINT ( 'NONE',  ( 112.4559014775786494, -9.988377603198976828, -10.36322818467138340 ) ) ;
#27103=CARTESIAN_POINT ( 'NONE',  ( 117.9583881442453048, -10.30919188438810075, -12.61870101168855918 ) ) ;
#27105=CARTESIAN_POINT ( 'NONE',  ( 111.9453614775786434, -1.561330072975668060, -17.79121239304076596 ) ) ;
#27106=CARTESIAN_POINT ( 'NONE',  ( 116.5969481442453031, -9.859900752359374465, -12.68260735090039404 ) ) ;
#27108=CARTESIAN_POINT ( 'NONE',  ( 122.2128881442453263, -1.834011780172310813, -8.268836392978581529 ) ) ;
#27109=CARTESIAN_POINT ( 'NONE',  ( 117.1642148109119859, -9.261995988541697145, -16.69588392320189030 ) ) ;
#27111=CARTESIAN_POINT ( 'NONE',  ( 114.2144281442453178, -1.833838273342658809, -17.42832698103878286 ) ) ;
#27113=CARTESIAN_POINT ( 'NONE',  ( 117.1642148109119859, -9.261995988541697145, -16.69588392320189030 ) ) ;
#27116=CARTESIAN_POINT ( 'NONE',  ( 115.9162281442453235, -4.089484607189486809, -7.948022111789456723 ) ) ;
#27118=CARTESIAN_POINT ( 'NONE',  ( 120.5678148109119832, -8.166667518702819706, -8.995218007635861213 ) ) ;
#27120=CARTESIAN_POINT ( 'NONE',  ( 113.0231681442453180, -10.15424416112533912, -14.75197769757731336 ) ) ;
#27122=CARTESIAN_POINT ( 'NONE',  ( 117.9583881442453048, 0.1319031606808879209, -14.10382304977623669 ) ) ;
#27123=CARTESIAN_POINT ( 'NONE',  ( 123.4754274106697522, -4.049225749020625820, -15.72719735404760577 ) ) ;
#27125=CARTESIAN_POINT ( 'NONE',  ( 118.6958348109119754, -3.505236298600246325, -18.68346056562440793 ) ) ;
#27128=CARTESIAN_POINT ( 'NONE',  ( 115.4056881442453459, -2.084020599724406786, -8.691656652584148546 ) ) ;
#27129=CARTESIAN_POINT ( 'NONE',  ( 115.6325948109119821, 0.2603800115204892296, -16.42320221600525088 ) ) ;
#27131=CARTESIAN_POINT ( 'NONE',  ( 126.4106614775786284, -6.222761293078241884, -8.102969835052219238 ) ) ;
#27132=CARTESIAN_POINT ( 'NONE',  ( 115.6893214775786447, -9.859900752359374465, -12.68260735090039404 ) ) ;
#27133=CARTESIAN_POINT ( 'NONE',  ( 121.7590748109119687, -7.893985811506177619, -18.51759400769804742 ) ) ;
#27135=CARTESIAN_POINT ( 'NONE',  ( 116.5402214775786405, -9.565557343593413364, -10.61323700422348004 ) ) ;
#27137=CARTESIAN_POINT ( 'NONE',  ( 114.1009748109119784, -4.089484607189486809, -7.948022111789456723 ) ) ;
#27144=CARTESIAN_POINT ( 'NONE',  ( 118.1285681442453068, -7.893985811506177619, -18.51759400769804742 ) ) ;
#27148=CARTESIAN_POINT ( 'NONE',  ( 116.7104014775786425, -8.899110576539710493, -16.42337572283490132 ) ) ;
#27150=CARTESIAN_POINT ( 'NONE',  ( 124.8790414775786246, -0.4660016031367893996, -10.09054647747474043 ) ) ;
#27153=ORIENTED_EDGE ( 'NONE', *, *, #28781, .F. ) ;
#27154=CARTESIAN_POINT ( 'NONE',  ( 112.8529881442453302, -1.561330072975668060, -17.79121239304076596 ) ) ;
#27155=CARTESIAN_POINT ( 'NONE',  ( 123.5176014775786228, -0.8288870151387760510, -10.36305467784173118 ) ) ;
#27156=CARTESIAN_POINT ( 'NONE',  ( 121.0783548109119749, 0.2603800115204892296, -16.42320221600525088 ) ) ;
#27158=CARTESIAN_POINT ( 'NONE',  ( 112.7395348109119766, -4.153390946401321671, -8.397313243818183892 ) ) ;
#27159=CARTESIAN_POINT ( 'NONE',  ( 118.5823814775786360, -1.834011780172310813, -8.268836392978581529 ) ) ;
#27162=CARTESIAN_POINT ( 'NONE',  ( 124.3117748109119844, 0.1319031606808879209, -14.10382304977623669 ) ) ;
#27163=ORIENTED_EDGE ( 'NONE', *, *, #23174, .F. ) ;
#27167=CARTESIAN_POINT ( 'NONE',  ( 115.8027748109119841, -0.4660016031367893996, -10.09054647747474043 ) ) ;
#27168=CARTESIAN_POINT ( 'NONE',  ( 119.7169148109119874, -0.1624402480850797581, -16.17319339645315424 ) ) ;
#27172=CARTESIAN_POINT ( 'NONE',  ( 118.8092881442453290, -9.988377603198976828, -10.36322818467138340 ) ) ;
#27174=CARTESIAN_POINT ( 'NONE',  ( 117.2209414775786485, -2.084020599724406786, -8.691656652584148546 ) ) ;
#27175=ORIENTED_EDGE ( 'NONE', *, *, #914, .F. ) ;
#27178=CARTESIAN_POINT ( 'NONE',  ( 125.8433948109119456, -7.643976991954077427, -18.09477374809248928 ) ) ;
#27182=CARTESIAN_POINT ( 'NONE',  ( 122.1561614775786353, -0.4660016031367893996, -10.09054647747474043 ) ) ;
#27183=CARTESIAN_POINT ( 'NONE',  ( 112.1722566881651915, -8.899626691430476910, -16.42270751673093798 ) ) ;
#27185=CARTESIAN_POINT ( 'NONE',  ( 116.9163235773848726, -2.467220198592778413, -17.83387418641524391 ) ) ;
#27186=CARTESIAN_POINT ( 'NONE',  ( 121.0783548109119749, 0.2603800115204892296, -16.42320221600525088 ) ) ;
#27187=CARTESIAN_POINT ( 'NONE',  ( 120.4543614775786295, -4.089484607189486809, -7.948022111789456723 ) ) ;
#27188=CARTESIAN_POINT ( 'NONE',  ( 118.0151148109119816, 0.4262465694468514643, -12.03445270309931736 ) ) ;
#27189=CARTESIAN_POINT ( 'NONE',  ( 124.6521348109119884, -7.894159318335828068, -9.358103419637847864 ) ) ;
#27190=CARTESIAN_POINT ( 'NONE',  ( 113.1933481442453058, -4.089484607189486809, -7.948022111789456723 ) ) ;
#27192=CARTESIAN_POINT ( 'NONE',  ( 122.9503348109119827, -9.859900752359378018, -12.68260735090039759 ) ) ;
#27193=CARTESIAN_POINT ( 'NONE',  ( 122.9042958072984959, 0.3208234527006196823, -15.99825685930876595 ) ) ;
#27194=CONICAL_SURFACE ( 'NONE', #28624, 5.999999999999997335, 0.4636476090008060935 ) ;
#27200=CARTESIAN_POINT ( 'NONE',  ( 120.5110881442453206, -6.344957434206665248, -7.627207830600338134 ) ) ;
#27201=CARTESIAN_POINT ( 'NONE',  ( 121.4187148109119789, -3.505236298600246325, -18.68346056562440793 ) ) ;
#27203=CARTESIAN_POINT ( 'NONE',  ( 125.5030348109119558, -3.383040157471821630, -19.15922257007629170 ) ) ;
#27204=CARTESIAN_POINT ( 'NONE',  ( 112.2857214775786474, -5.574606645277164318, -18.38911715685844683 ) ) ;
#27206=CARTESIAN_POINT ( 'NONE',  ( 121.8158014775786171, -5.638512984488999180, -18.83840828888717311 ) ) ;
#27207=CARTESIAN_POINT ( 'NONE',  ( 120.6812681442452941, -10.30919188438810075, -12.61870101168855918 ) ) ;
#27209=CARTESIAN_POINT ( 'NONE',  ( 112.6260814775786514, -9.261995988541697145, -16.69588392320189030 ) ) ;
#27215=CARTESIAN_POINT ( 'NONE',  ( 113.0798948109119948, -8.899110576539710493, -16.42337572283490132 ) ) ;
#27216=CARTESIAN_POINT ( 'NONE',  ( 123.1772414775786189, -5.574606645277164318, -18.38911715685844683 ) ) ;
#27219=CARTESIAN_POINT ( 'NONE',  ( 121.3619881442452879, -5.574606645277164318, -18.38911715685844683 ) ) ;
#27221=CARTESIAN_POINT ( 'NONE',  ( 116.3700414775786527, -4.153390946401321671, -8.397313243818183892 ) ) ;
#27222=CARTESIAN_POINT ( 'NONE',  ( 124.8790414775786246, -0.4660016031367893996, -10.09054647747474043 ) ) ;
#27224=CARTESIAN_POINT ( 'NONE',  ( 122.8936081442453059, -9.565557343593413364, -10.61323700422348004 ) ) ;
#27225=CARTESIAN_POINT ( 'NONE',  ( 117.1074881442453233, -10.63000616557722466, -14.87417383870573495 ) ) ;
#27226=CARTESIAN_POINT ( 'NONE',  ( 123.8012348109119642, 0.2603800115204892296, -16.42320221600525088 ) ) ;
#27227=CARTESIAN_POINT ( 'NONE',  ( 124.3117748109119844, 0.1319031606808879209, -14.10382304977623669 ) ) ;
#27229=CARTESIAN_POINT ( 'NONE',  ( 123.4268075888223848, -2.372251574601201174, -17.96033910819751611 ) ) ;
#27230=EDGE_CURVE ( 'NONE', #1558, #44110, #4921, .T. ) ;
#27233=CARTESIAN_POINT ( 'NONE',  ( 125.5597614775786326, -1.561330072975669392, -17.79121239304076951 ) ) ;
#27234=CARTESIAN_POINT ( 'NONE',  ( 114.4980614775786734, -2.084020599724406786, -8.691656652584148546 ) ) ;
#27235=CARTESIAN_POINT ( 'NONE',  ( 125.5597614775786326, -1.561330072975669392, -17.79121239304076951 ) ) ;
#27236=CARTESIAN_POINT ( 'NONE',  ( 114.8951481442453115, -0.4660016031367867906, -10.09054647747474398 ) ) ;
#27244=CARTESIAN_POINT ( 'NONE',  ( 123.7445081442452874, -7.894159318335828068, -9.358103419637847864 ) ) ;
#27245=CARTESIAN_POINT ( 'NONE',  ( 113.0231681442453180, -10.15424416112533912, -14.75197769757731336 ) ) ;
#27246=CARTESIAN_POINT ( 'NONE',  ( 126.4852516627911427, -0.4199418574856381703, -10.82374662991991343 ) ) ;
#27249=CARTESIAN_POINT ( 'NONE',  ( 112.9097148109120070, -9.565557343593413364, -10.61323700422348004 ) ) ;
#27252=CARTESIAN_POINT ( 'NONE',  ( 111.7857214775786474, -4.159894987975828684, -8.443039665293898821 ) ) ;
#27254=CARTESIAN_POINT ( 'NONE',  ( 124.8790414775786246, -0.4660016031367893996, -10.09054647747474043 ) ) ;
#27255=CARTESIAN_POINT ( 'NONE',  ( 126.0703014775786102, -0.1624402480850797581, -16.17319339645315424 ) ) ;
#27257=CARTESIAN_POINT ( 'NONE',  ( 114.0442481442453300, -1.834011780172310813, -8.268836392978581529 ) ) ;
#27261=CARTESIAN_POINT ( 'NONE',  ( 124.5954081442453116, -6.222761293078241884, -8.102969835052219238 ) ) ;
#27262=CARTESIAN_POINT ( 'NONE',  ( 123.9714148109119805, -8.899110576539710493, -16.42337572283490132 ) ) ;
#27264=CARTESIAN_POINT ( 'NONE',  ( 138.2184548109119930, -3.657522433324904565, -16.24880879654457289 ) ) ;
#27266=CARTESIAN_POINT ( 'NONE',  ( 120.2065265278262700, -1.036737761566197014, -17.24079555149560861 ) ) ;
#27268=CARTESIAN_POINT ( 'NONE',  ( 113.4202548109119846, 0.1319031606808879209, -14.10382304977623669 ) ) ;
#27272=CARTESIAN_POINT ( 'NONE',  ( 125.9568481442452850, -6.344957434206665248, -7.627207830600338134 ) ) ;
#27273=CARTESIAN_POINT ( 'NONE',  ( 123.6877814775786533, -3.383040157471821630, -19.15922257007629170 ) ) ;
#27275=CARTESIAN_POINT ( 'NONE',  ( 119.0929214775786278, -5.638512984488999180, -18.83840828888717311 ) ) ;
#27276=CARTESIAN_POINT ( 'NONE',  ( 113.3068014775786594, -8.166667518702817929, -8.995218007635859436 ) ) ;
#27278=CARTESIAN_POINT ( 'NONE',  ( 112.4559014775786778, -0.1624402480850797581, -16.17319339645315424 ) ) ;
#27279=CARTESIAN_POINT ( 'NONE',  ( 112.8529881442453160, -7.894159318335828068, -9.358103419637847864 ) ) ;
#27280=CARTESIAN_POINT ( 'NONE',  ( 124.1415948109119540, -6.344957434206665248, -7.627207830600338134 ) ) ;
#27281=CARTESIAN_POINT ( 'NONE',  ( 112.6828081442453282, -7.893985811506177619, -18.51759400769804742 ) ) ;
#27282=CARTESIAN_POINT ( 'NONE',  ( 112.1155414775786454, -10.15424416112533912, -14.75197769757731336 ) ) ;
#27285=CARTESIAN_POINT ( 'NONE',  ( 118.2987481442453088, -7.894159318335828068, -9.358103419637847864 ) ) ;
#27290=CARTESIAN_POINT ( 'NONE',  ( 123.8579614775786126, -9.859900752359378018, -12.68260735090039759 ) ) ;
#27295=CARTESIAN_POINT ( 'NONE',  ( 125.8433948109119456, -1.834011780172310813, -8.268836392978581529 ) ) ;
#27297=CARTESIAN_POINT ( 'NONE',  ( 112.9097148109120070, 0.2603800115204892296, -16.42320221600525088 ) ) ;
#27302=CARTESIAN_POINT ( 'NONE',  ( 118.7525614775786380, -8.166667518702819706, -8.995218007635861213 ) ) ;
#27306=CARTESIAN_POINT ( 'NONE',  ( 119.5467348109119712, -5.574606645277164318, -18.38911715685844683 ) ) ;
#27309=CARTESIAN_POINT ( 'NONE',  ( 118.4122014775786340, 0.5811942927096110934, -14.16772938898807510 ) ) ;
#27311=CARTESIAN_POINT ( 'NONE',  ( 115.0086014775786509, -5.574606645277164318, -18.38911715685844683 ) ) ;
#27312=CARTESIAN_POINT ( 'NONE',  ( 123.8579614775786126, 0.5811942927096110934, -14.16772938898807510 ) ) ;
#27314=ADVANCED_FACE ( 'NONE', ( #31921 ), #1139, .T. ) ;
#27318=CARTESIAN_POINT ( 'NONE',  ( 116.4267681442453153, -6.222761293078241884, -8.102969835052219238 ) ) ;
#27319=CARTESIAN_POINT ( 'NONE',  ( 119.5467348109119712, -5.574606645277164318, -18.38911715685844683 ) ) ;
#27325=CARTESIAN_POINT ( 'NONE',  ( 112.3424481442453384, -6.344957434206662583, -7.627207830600332805 ) ) ;
#27326=CARTESIAN_POINT ( 'NONE',  ( 123.0525060002550788, -2.334846009198419559, -18.01015021110789505 ) ) ;
#27333=CARTESIAN_POINT ( 'NONE',  ( 123.1205148109119563, -1.834011780172310813, -8.268836392978581529 ) ) ;
#27334=CARTESIAN_POINT ( 'NONE',  ( 112.4559014775786494, -9.988377603198976828, -10.36322818467138340 ) ) ;
#27335=CARTESIAN_POINT ( 'NONE',  ( 116.7671281442453335, -7.643976991954077427, -18.09477374809248928 ) ) ;
#27336=CARTESIAN_POINT ( 'NONE',  ( 121.1350814775786233, 0.5811942927096110934, -14.16772938898807510 ) ) ;
#27337=CARTESIAN_POINT ( 'NONE',  ( 119.1496481442453046, -3.383040157471821630, -19.15922257007629170 ) ) ;
#27341=CARTESIAN_POINT ( 'NONE',  ( 113.7606148109119886, -7.894159318335828068, -9.358103419637847864 ) ) ;
#27345=CARTESIAN_POINT ( 'NONE',  ( 116.5402214775786405, 0.2603800115204892296, -16.42320221600525088 ) ) ;
#27347=CARTESIAN_POINT ( 'NONE',  ( 115.3489614775786407, -9.261995988541697145, -16.69588392320189030 ) ) ;
#27350=CARTESIAN_POINT ( 'NONE',  ( 125.7866681442452688, -0.4660016031367893996, -10.09054647747474043 ) ) ;
#27353=CARTESIAN_POINT ( 'NONE',  ( 124.9305558011493957, -1.149058757900108585, -17.09122335155391781 ) ) ;
#27354=CARTESIAN_POINT ( 'NONE',  ( 114.8384214775786489, -10.15424416112533912, -14.75197769757731336 ) ) ;
#27356=CARTESIAN_POINT ( 'NONE',  ( 118.2420214775786320, -6.222761293078241884, -8.102969835052219238 ) ) ;
#27358=CARTESIAN_POINT ( 'NONE',  ( 114.6682414775786469, -7.894159318335828068, -9.358103419637847864 ) ) ;
#27359=CARTESIAN_POINT ( 'NONE',  ( 115.8027748109119841, -0.4660016031367893996, -10.09054647747474043 ) ) ;
#27361=CARTESIAN_POINT ( 'NONE',  ( 117.3343948109119737, -3.383040157471821630, -19.15922257007629170 ) ) ;
#27362=CARTESIAN_POINT ( 'NONE',  ( 112.2289948109119848, -7.643976991954077427, -18.09477374809248928 ) ) ;
#27363=CARTESIAN_POINT ( 'NONE',  ( 116.6536748109119941, -10.15424416112533912, -14.75197769757731336 ) ) ;
#27365=CARTESIAN_POINT ( 'NONE',  ( 112.3424481442453384, -6.344957434206662583, -7.627207830600332805 ) ) ;
#27370=CARTESIAN_POINT ( 'NONE',  ( 118.8660148109119774, -10.30919188438810075, -12.61870101168855918 ) ) ;
#27372=CARTESIAN_POINT ( 'NONE',  ( 125.1626748109119802, -9.988377603198957289, -10.36322818467135498 ) ) ;
#27373=CARTESIAN_POINT ( 'NONE',  ( 116.3133148109120043, -2.084020599724406786, -8.691656652584148546 ) ) ;
#27374=CARTESIAN_POINT ( 'NONE',  ( 124.2193060444391790, -1.267766418764731728, -16.93314635290706605 ) ) ;
#27376=CARTESIAN_POINT ( 'NONE',  ( 122.8936081442453059, 0.2603800115204892296, -16.42320221600525088 ) ) ;
#27380=ORIENTED_EDGE ( 'NONE', *, *, #40058, .T. ) ;
#27382=CARTESIAN_POINT ( 'NONE',  ( 122.2696148109119889, -5.574606645277164318, -18.38911715685844683 ) ) ;
#27383=CARTESIAN_POINT ( 'NONE',  ( 123.1772414775786189, -4.089484607189486809, -7.948022111789456723 ) ) ;
#27384=CARTESIAN_POINT ( 'NONE',  ( 118.1285681442453068, -2.084020599724406786, -8.691656652584148546 ) ) ;
#27385=CARTESIAN_POINT ( 'NONE',  ( 120.2274548109119934, 0.5811942927096110934, -14.16772938898807510 ) ) ;
#27387=CARTESIAN_POINT ( 'NONE',  ( 127.0400190879707765, -1.259479977070091294, -9.357869521001603630 ) ) ;
#27388=CARTESIAN_POINT ( 'NONE',  ( 122.7801548109119665, -6.222761293078241884, -8.102969835052219238 ) ) ;
#27389=ORIENTED_EDGE ( 'NONE', *, *, #6378, .F. ) ;
#27394=CARTESIAN_POINT ( 'NONE',  ( 116.4267681442453153, -3.383040157471821630, -19.15922257007629170 ) ) ;
#27395=CARTESIAN_POINT ( 'NONE',  ( 124.4252281442452812, -0.8288870151387760510, -10.36305467784173118 ) ) ;
#27398=CARTESIAN_POINT ( 'NONE',  ( 136.5278073585092216, -1.250741748839698575, -8.937135636257391269 ) ) ;
#27399=CARTESIAN_POINT ( 'NONE',  ( 117.5613014775786525, 0.9020085738987339008, -11.91225656197089222 ) ) ;
#27401=CARTESIAN_POINT ( 'NONE',  ( 118.2420214775786320, -6.222761293078241884, -8.102969835052219238 ) ) ;
#27405=CARTESIAN_POINT ( 'NONE',  ( 111.9453614775786434, -1.561330072975668060, -17.79121239304076596 ) ) ;
#27407=CARTESIAN_POINT ( 'NONE',  ( 123.1772414775786189, -5.574606645277164318, -18.38911715685844683 ) ) ;
#27408=( NAMED_UNIT ( * ) SI_UNIT ( $, .STERADIAN. ) SOLID_ANGLE_UNIT ( ) );
#27410=CARTESIAN_POINT ( 'NONE',  ( 120.9649014775786355, -3.383040157471821630, -19.15922257007629170 ) ) ;
#27414=B_SPLINE_CURVE_WITH_KNOTS ( 'NONE', 3,
 ( #8735, #22194, #35859, #29264, #43176, #36090, #11715, #15134, #43621, #1659 ),
 .UNSPECIFIED., .F., .F.,
 ( 4, 3, 3, 4 ),
 ( 0.000000000000000000, 0.0001671877548681239927, 0.0003343755096277610354, 0.0006463528481650629171 ),
 .UNSPECIFIED. ) ;
#27415=CARTESIAN_POINT ( 'NONE',  ( 118.7525614775786380, -8.166667518702819706, -8.995218007635861213 ) ) ;
#27416=CARTESIAN_POINT ( 'NONE',  ( 117.5613014775786525, 0.9020085738987339008, -11.91225656197089222 ) ) ;
#27417=CARTESIAN_POINT ( 'NONE',  ( 121.3052614775786111, -7.643976991954077427, -18.09477374809248928 ) ) ;
#27419=CARTESIAN_POINT ( 'NONE',  ( 116.9940348109119839, -9.988377603198976828, -10.36322818467138340 ) ) ;
#27422=CARTESIAN_POINT ( 'NONE',  ( 124.3117748109119844, 0.1319031606808879209, -14.10382304977623669 ) ) ;
#27423=CARTESIAN_POINT ( 'NONE',  ( 125.2194014775786286, 0.1319031606810284196, -14.10382304977525614 ) ) ;
#27427=CARTESIAN_POINT ( 'NONE',  ( 121.3052614775786111, -1.834011780172310813, -8.268836392978581529 ) ) ;
#27428=CARTESIAN_POINT ( 'NONE',  ( 122.5532481442453019, 0.4262465694468514643, -12.03445270309931736 ) ) ;
#27430=CARTESIAN_POINT ( 'NONE',  ( 124.1983214775786166, -8.166667518702819706, -8.995218007635861213 ) ) ;
#27433=CARTESIAN_POINT ( 'NONE',  ( 122.8368814775786291, -1.561330072975668948, -17.79121239304076951 ) ) ;
#27434=CARTESIAN_POINT ( 'NONE',  ( 120.7947214775786193, -9.261995988541697145, -16.69588392320189030 ) ) ;
#27436=CARTESIAN_POINT ( 'NONE',  ( 112.9664414775786412, 0.5811942927096154232, -14.16772938898807155 ) ) ;
#27437=CARTESIAN_POINT ( 'NONE',  ( 111.5849102067643770, -1.223627541775779370, -16.99192386690437928 ) ) ;
#27441=CARTESIAN_POINT ( 'NONE',  ( 114.3112643147880476, -2.395992375830784837, -17.92872468182854107 ) ) ;
#27442=CARTESIAN_POINT ( 'NONE',  ( 124.4252281442452812, -0.8288870151387760510, -10.36305467784173118 ) ) ;
#27446=CARTESIAN_POINT ( 'NONE',  ( 123.1772414775786189, -5.574606645277164318, -18.38911715685844683 ) ) ;
#27447=CARTESIAN_POINT ( 'NONE',  ( 117.3343948109119737, -6.222761293078241884, -8.102969835052219238 ) ) ;
#27448=CARTESIAN_POINT ( 'NONE',  ( 113.4769814775786330, 0.4262465694468514643, -12.03445270309931736 ) ) ;
#27449=ORIENTED_EDGE ( 'NONE', *, *, #10351, .F. ) ;
#27451=CARTESIAN_POINT ( 'NONE',  ( 118.9794681442453026, -9.261995988541697145, -16.69588392320189030 ) ) ;
#27458=CARTESIAN_POINT ( 'NONE',  ( 114.2711548109119803, -0.1624402480850797581, -16.17319339645315424 ) ) ;
#27460=CARTESIAN_POINT ( 'NONE',  ( 115.2355081442453155, 0.1319031606808879209, -14.10382304977623669 ) ) ;
#27469=CARTESIAN_POINT ( 'NONE',  ( 123.5743281442453139, -2.084020599724406786, -8.691656652584148546 ) ) ;
#27470=CARTESIAN_POINT ( 'NONE',  ( 114.2144281442453178, -1.833838273342658809, -17.42832698103878286 ) ) ;
#27479=CARTESIAN_POINT ( 'NONE',  ( 125.2194014775786286, -10.30919188438810075, -12.61870101168855918 ) ) ;
#27480=CARTESIAN_POINT ( 'NONE',  ( 126.6375681442452930, -10.15424416112533912, -14.75197769757731336 ) ) ;
#27482=CARTESIAN_POINT ( 'NONE',  ( 112.9097148109120070, 0.2603800115204892296, -16.42320221600525088 ) ) ;
#27483=DIRECTION ( 'NONE',  ( 0.000000000000000000, 0.6004852223388321697, -0.7996358532186279566 ) ) ;
#27485=CARTESIAN_POINT ( 'NONE',  ( 125.8433948109119456, -7.643976991954077427, -18.09477374809248928 ) ) ;
#27487=CARTESIAN_POINT ( 'NONE',  ( 122.2128881442453263, -7.643976991954077427, -18.09477374809248928 ) ) ;
#27492=CARTESIAN_POINT ( 'NONE',  ( 112.7395348109119766, -4.153390946401321671, -8.397313243818183892 ) ) ;
#27494=CARTESIAN_POINT ( 'NONE',  ( 117.9016614775786280, -9.988377603198960841, -10.36322818467135853 ) ) ;
#27497=CARTESIAN_POINT ( 'NONE',  ( 112.0020881442453344, -9.565557343593413364, -10.61323700422348004 ) ) ;
#27499=CARTESIAN_POINT ( 'NONE',  ( 120.2841814775786276, 0.9020085738987339008, -11.91225656197089222 ) ) ;
#27500=CARTESIAN_POINT ( 'NONE',  ( 116.8238548109119819, -4.089484607189486809, -7.948022111789456723 ) ) ;
#27502=CARTESIAN_POINT ( 'NONE',  ( 114.3278814775786429, 0.1319031606808879209, -14.10382304977623669 ) ) ;
#27503=CARTESIAN_POINT ( 'NONE',  ( 111.5482748109120053, -0.1624402480850797581, -16.17319339645315424 ) ) ;
#27504=CARTESIAN_POINT ( 'NONE',  ( 123.1772414775786189, -4.089484607189486809, -7.948022111789456723 ) ) ;
#27505=CARTESIAN_POINT ( 'NONE',  ( 113.1366214775786432, -1.834011780172310813, -8.268836392978581529 ) ) ;
#27507=CARTESIAN_POINT ( 'NONE',  ( 115.4624148109119943, -4.153390946401321671, -8.397313243818183892 ) ) ;
#27509=CARTESIAN_POINT ( 'NONE',  ( 116.8238548109119819, -5.574606645277164318, -18.38911715685844683 ) ) ;
#27510=CARTESIAN_POINT ( 'NONE',  ( 116.8805814775786445, -6.344957434206662583, -7.627207830600332805 ) ) ;
#27511=CARTESIAN_POINT ( 'NONE',  ( 122.1561614775786353, -8.899110576539710493, -16.42337572283490132 ) ) ;
#27519=CARTESIAN_POINT ( 'NONE',  ( 113.3277860444392076, -1.267766418764742165, -16.93314635290707315 ) ) ;
#27522=CARTESIAN_POINT ( 'NONE',  ( 112.9097148109120070, -9.565557343593413364, -10.61323700422348004 ) ) ;
#27525=CARTESIAN_POINT ( 'NONE',  ( 117.7882081442453170, -6.344957434206665248, -7.627207830600338134 ) ) ;
#27530=CARTESIAN_POINT ( 'NONE',  ( 122.2696148109119889, -5.574606645277164318, -18.38911715685844683 ) ) ;
#27533=CARTESIAN_POINT ( 'NONE',  ( 125.0492214775786266, -6.344957434206665248, -7.627207830600338134 ) ) ;
#27534=CARTESIAN_POINT ( 'NONE',  ( 120.3976348109119812, -1.834011780172310813, -8.268836392978581529 ) ) ;
#27536=CARTESIAN_POINT ( 'NONE',  ( 115.4056881442453459, -2.084020599724406786, -8.691656652584148546 ) ) ;
#27539=CARTESIAN_POINT ( 'NONE',  ( 112.7962614775786676, -6.222761293078241884, -8.102969835052219238 ) ) ;
#27543=CARTESIAN_POINT ( 'NONE',  ( 116.8805814775786445, -3.505236298600246325, -18.68346056562440793 ) ) ;
#27544=CARTESIAN_POINT ( 'NONE',  ( 120.7947214775786193, -0.8288870151387760510, -10.36305467784173118 ) ) ;
#27549=CARTESIAN_POINT ( 'NONE',  ( 112.1155414775786454, 0.9020085738987339008, -11.91225656197089222 ) ) ;
#27550=CARTESIAN_POINT ( 'NONE',  ( 115.9162281442453235, -4.089484607189486809, -7.948022111789456723 ) ) ;
#27554=CARTESIAN_POINT ( 'NONE',  ( 123.3791889291123880, -2.608644173476851069, -15.14726574760354261 ) ) ;
#27556=CARTESIAN_POINT ( 'NONE',  ( 120.5110881442453206, -6.344957434206665248, -7.627207830600338134 ) ) ;
#27557=CARTESIAN_POINT ( 'NONE',  ( 114.1009748109119784, -4.089484607189486809, -7.948022111789456723 ) ) ;
#27558=CARTESIAN_POINT ( 'NONE',  ( 119.4332814775786318, -8.899110576539710493, -16.42337572283490132 ) ) ;
#27560=CARTESIAN_POINT ( 'NONE',  ( 122.6099748109119929, -9.261995988541697145, -16.69588392320189030 ) ) ;
#27561=CARTESIAN_POINT ( 'NONE',  ( 117.9583881442453048, -10.30919188438810075, -12.61870101168855918 ) ) ;
#27562=EDGE_CURVE ( 'NONE', #20193, #41948, #31578, .T. ) ;
#27565=CARTESIAN_POINT ( 'NONE',  ( 112.0020881442453344, -9.565557343593413364, -10.61323700422348004 ) ) ;
#27568=CARTESIAN_POINT ( 'NONE',  ( 116.5969481442453031, 0.5811942927096154232, -14.16772938898807155 ) ) ;
#27572=CARTESIAN_POINT ( 'NONE',  ( 117.2209414775786485, -7.893985811506177619, -18.51759400769804742 ) ) ;
#27577=CARTESIAN_POINT ( 'NONE',  ( 112.9097148109120070, -9.565557343593413364, -10.61323700422348004 ) ) ;
#27579=CARTESIAN_POINT ( 'NONE',  ( 117.4478481442453131, -9.565557343593413364, -10.61323700422348004 ) ) ;
#27580=CARTESIAN_POINT ( 'NONE',  ( 120.4020503192116820, -2.378957183258601393, -17.95140958770220152 ) ) ;
#27581=CARTESIAN_POINT ( 'NONE',  ( 117.4478481442453131, -9.565557343593413364, -10.61323700422348004 ) ) ;
#27583=B_SPLINE_CURVE_WITH_KNOTS ( 'NONE', 3,
 ( #9002, #36342, #5347, #16300, #23138, #19483, #43436, #22674, #4890, #19706, #19263, #44120, #33143, #8549, #1915, #36120, #25878, #15845, #43651, #2136 ),
 .UNSPECIFIED., .F., .F.,
 ( 4, 2, 2, 2, 2, 2, 2, 2, 2, 4 ),
 ( 0.000000000000000000, 0.2500000000000117129, 0.3750000000000175415, 0.5000000000000234257, 0.5625000000000199840, 0.6250000000000166533, 0.7500000000000097700, 0.8125000000000064393, 0.8750000000000031086, 1.000000000000000000 ),
 .UNSPECIFIED. ) ;
#27584=CARTESIAN_POINT ( 'NONE',  ( 115.0086014775786509, -5.574606645277164318, -18.38911715685844683 ) ) ;
#27585=EDGE_CURVE ( 'NONE', #7925, #30998, #13863, .T. ) ;
#27587=CARTESIAN_POINT ( 'NONE',  ( 114.8384214775786489, 0.9020085738987339008, -11.91225656197089222 ) ) ;
#27588=CARTESIAN_POINT ( 'NONE',  ( 111.6617281442453304, 0.4262465694468514643, -12.03445270309931736 ) ) ;
#27591=CARTESIAN_POINT ( 'NONE',  ( 115.3489614775786407, -0.8288870151387760510, -10.36305467784173118 ) ) ;
#27593=CARTESIAN_POINT ( 'NONE',  ( 118.1852948109119836, -5.638512984488999180, -18.83840828888717311 ) ) ;
#27598=CARTESIAN_POINT ( 'NONE',  ( 122.8368814775786291, -1.561330072975668948, -17.79121239304076951 ) ) ;
#27601=CARTESIAN_POINT ( 'NONE',  ( 116.4834948109119779, -7.894159318335828068, -9.358103419637847864 ) ) ;
#27603=CARTESIAN_POINT ( 'NONE',  ( 123.1772414775786189, -4.089484607189486809, -7.948022111789456723 ) ) ;
#27607=CARTESIAN_POINT ( 'NONE',  ( 112.2289948109119848, -1.834011780172310813, -8.268836392978581529 ) ) ;
#27608=CARTESIAN_POINT ( 'NONE',  ( 112.1155414775786454, 0.9020085738987339008, -11.91225656197089222 ) ) ;
#27609=CARTESIAN_POINT ( 'NONE',  ( 123.2339681442453241, -6.344957434206665248, -7.627207830600338134 ) ) ;
#27610=CARTESIAN_POINT ( 'NONE',  ( 117.7314814775786260, -5.574606645277164318, -18.38911715685844683 ) ) ;
#27612=CARTESIAN_POINT ( 'NONE',  ( 118.9227414775786400, -10.63000616557722466, -14.87417383870573495 ) ) ;
#27615=CARTESIAN_POINT ( 'NONE',  ( 123.2339681442453241, -3.505236298600246325, -18.68346056562440793 ) ) ;
#27618=CARTESIAN_POINT ( 'NONE',  ( 115.5758681442453053, -1.561330072975668060, -17.79121239304076951 ) ) ;
#27619=CARTESIAN_POINT ( 'NONE',  ( 124.3117748109119844, 0.1319031606808879209, -14.10382304977623669 ) ) ;
#27622=CARTESIAN_POINT ( 'NONE',  ( 136.7860375664297408, -1.264623415989550859, -9.101478292670408976 ) ) ;
#27623=CARTESIAN_POINT ( 'NONE',  ( 120.6245414775786458, -9.988377603198976828, -10.36322818467138340 ) ) ;
#27625=CARTESIAN_POINT ( 'NONE',  ( 118.5823814775786360, -7.643976991954077427, -18.09477374809248928 ) ) ;
#27628=CARTESIAN_POINT ( 'NONE',  ( 113.0231681442453322, 0.9020085738987339008, -11.91225656197089222 ) ) ;
#27630=CARTESIAN_POINT ( 'NONE',  ( 123.5743281442453139, -2.084020599724406786, -8.691656652584148546 ) ) ;
#27635=CARTESIAN_POINT ( 'NONE',  ( 123.4041481442452834, -10.30919188438810075, -12.61870101168855918 ) ) ;
#27638=CARTESIAN_POINT ( 'NONE',  ( 118.9794681442453026, -9.261995988541697145, -16.69588392320189030 ) ) ;
#27639=CARTESIAN_POINT ( 'NONE',  ( 117.7314814775786260, -4.089484607189486809, -7.948022111789456723 ) ) ;
#27640=CARTESIAN_POINT ( 'NONE',  ( 118.4122014775786340, -9.859900752359374465, -12.68260735090039404 ) ) ;
#27642=CARTESIAN_POINT ( 'NONE',  ( 125.1733191598100916, -1.295815253274133383, -16.89579513612386563 ) ) ;
#27643=CARTESIAN_POINT ( 'NONE',  ( 114.8384214775786489, 0.9020085738987339008, -11.91225656197089222 ) ) ;
#27645=CARTESIAN_POINT ( 'NONE',  ( 111.8886348109120092, -3.383040157471821630, -19.15922257007629170 ) ) ;
#27646=CARTESIAN_POINT ( 'NONE',  ( 125.5030348109119842, -6.222761293079280165, -8.102969835052485692 ) ) ;
#27650=CARTESIAN_POINT ( 'NONE',  ( 123.0070614775786169, 0.9020085738987339008, -11.91225656197089222 ) ) ;
#27651=CARTESIAN_POINT ( 'NONE',  ( 112.0588148109119828, 0.5811942927096154232, -14.16772938898807155 ) ) ;
#27653=CARTESIAN_POINT ( 'NONE',  ( 126.1270281442452870, -10.30919188438810075, -12.61870101168855918 ) ) ;
#27656=ADVANCED_FACE ( 'NONE', ( #16639 ), #18306, .T. ) ;
#27657=CARTESIAN_POINT ( 'NONE',  ( 122.5532481442453019, -10.63000616557722466, -14.87417383870573495 ) ) ;
#27658=CARTESIAN_POINT ( 'NONE',  ( 123.5743281442453139, -7.893985811506177619, -18.51759400769804742 ) ) ;
#27660=CARTESIAN_POINT ( 'NONE',  ( 126.6375681442452930, -10.15424416112533912, -14.75197769757731336 ) ) ;
#27665=CARTESIAN_POINT ( 'NONE',  ( 114.4980614775786734, -2.084020599724406786, -8.691656652584148546 ) ) ;
#27666=CARTESIAN_POINT ( 'NONE',  ( 126.1837548109119496, 0.4262465694468514643, -12.03445270309931736 ) ) ;
#27670=CARTESIAN_POINT ( 'NONE',  ( 120.8514481442452961, -2.084020599724406786, -8.691656652584148546 ) ) ;
#27671=CARTESIAN_POINT ( 'NONE',  ( 116.2565881442453133, -0.8288870151387760510, -10.36305467784173118 ) ) ;
#27672=CARTESIAN_POINT ( 'NONE',  ( 126.0135748109119902, -8.166667518702819706, -8.995218007635861213 ) ) ;
#27675=CARTESIAN_POINT ( 'NONE',  ( 117.4478481442453131, 0.2603800115204892296, -16.42320221600525088 ) ) ;
#27678=CARTESIAN_POINT ( 'NONE',  ( 113.2500748109119968, -3.505236298600246325, -18.68346056562440793 ) ) ;
#27683=CARTESIAN_POINT ( 'NONE',  ( 119.1496481442453046, -6.222761293078241884, -8.102969835052219238 ) ) ;
#27684=CARTESIAN_POINT ( 'NONE',  ( 113.3635281442453504, -0.1624402480850797581, -16.17319339645315424 ) ) ;
#27685=CARTESIAN_POINT ( 'NONE',  ( 117.8239502440515452, -2.467220198592778413, -17.83387418641524391 ) ) ;
#27687=ORIENTED_EDGE ( 'NONE', *, *, #22969, .T. ) ;
#27693=CARTESIAN_POINT ( 'NONE',  ( 122.4965214775786251, 0.1319031606808879209, -14.10382304977623669 ) ) ;
#27694=CARTESIAN_POINT ( 'NONE',  ( 118.4689281442453250, -10.15424416112533912, -14.75197769757731336 ) ) ;
#27695=CARTESIAN_POINT ( 'NONE',  ( 119.8983769549021758, -1.135392229370309369, -17.10942237759952889 ) ) ;
#27698=CARTESIAN_POINT ( 'NONE',  ( 115.6893214775786447, -9.859900752359374465, -12.68260735090039404 ) ) ;
#27700=CARTESIAN_POINT ( 'NONE',  ( 125.1418709397587037, -1.276798789163246850, -16.92111840127481059 ) ) ;
#27703=CARTESIAN_POINT ( 'NONE',  ( 111.7751814775786556, -7.893985811506177619, -18.51759400769804742 ) ) ;
#27704=ORIENTED_EDGE ( 'NONE', *, *, #1616, .T. ) ;
#27706=CARTESIAN_POINT ( 'NONE',  ( 113.7606148109119886, -1.561330072975668060, -17.79121239304076596 ) ) ;
#27707=CARTESIAN_POINT ( 'NONE',  ( 126.4750299824214324, 0.09325604387533485695, -14.70660372723753895 ) ) ;
#27709=CARTESIAN_POINT ( 'NONE',  ( 112.4559014775786494, -9.988377603198976828, -10.36322818467138340 ) ) ;
#27710=CARTESIAN_POINT ( 'NONE',  ( 115.5758681442453053, -1.561330072975668060, -17.79121239304076951 ) ) ;
#27711=CARTESIAN_POINT ( 'NONE',  ( 125.1059481442452750, -1.833838273342660141, -17.42832698103878286 ) ) ;
#27714=CARTESIAN_POINT ( 'NONE',  ( 120.1332064091100733, -0.9924539043446216624, -17.29976612834909133 ) ) ;
#27716=CARTESIAN_POINT ( 'NONE',  ( 117.4478481442453131, -9.565557343593413364, -10.61323700422348004 ) ) ;
#27720=CARTESIAN_POINT ( 'NONE',  ( 126.0703014775786102, -9.988377603198980381, -10.36322818467138518 ) ) ;
#27721=CARTESIAN_POINT ( 'NONE',  ( 126.0135748109119902, -8.166667518702819706, -8.995218007635861213 ) ) ;
#27723=CARTESIAN_POINT ( 'NONE',  ( 118.9794681442453026, -9.261995988541697145, -16.69588392320189030 ) ) ;
#27724=CARTESIAN_POINT ( 'NONE',  ( 117.7314814775786260, -4.089484607189486809, -7.948022111789456723 ) ) ;
#27725=ORIENTED_EDGE ( 'NONE', *, *, #14445, .T. ) ;
#27726=CARTESIAN_POINT ( 'NONE',  ( 113.8740681442453138, -9.859900752359374465, -12.68260735090039404 ) ) ;
#27727=CARTESIAN_POINT ( 'NONE',  ( 125.3328548109119964, -9.261995988541697145, -16.69588392320189030 ) ) ;
#27728=CARTESIAN_POINT ( 'NONE',  ( 112.5126281442453120, -10.30919188438810075, -12.61870101168855918 ) ) ;
#27731=CARTESIAN_POINT ( 'NONE',  ( 115.4056881442453459, -2.084020599724406786, -8.691656652584148546 ) ) ;
#27733=CARTESIAN_POINT ( 'NONE',  ( 120.5678148109119832, -1.833838273342659253, -17.42832698103878286 ) ) ;
#27735=CARTESIAN_POINT ( 'NONE',  ( 117.7882081442453170, -6.344957434206665248, -7.627207830600338134 ) ) ;
#27738=ORIENTED_EDGE ( 'NONE', *, *, #11170, .T. ) ;
#27741=CARTESIAN_POINT ( 'NONE',  ( 125.3895814775786448, -7.893985811506177619, -18.51759400769804742 ) ) ;
#27743=CARTESIAN_POINT ( 'NONE',  ( 114.2144281442453178, -8.166667518702817929, -8.995218007635859436 ) ) ;
#27745=CARTESIAN_POINT ( 'NONE',  ( 113.3068014775786594, -1.833838273342658809, -17.42832698103878286 ) ) ;
#27749=CARTESIAN_POINT ( 'NONE',  ( 117.9583881442453048, -10.30919188438810075, -12.61870101168855918 ) ) ;
#27750=CARTESIAN_POINT ( 'NONE',  ( 136.8445491832674463, -6.866345705054112791, -18.59485542995252771 ) ) ;
#27754=CARTESIAN_POINT ( 'NONE',  ( 120.5110881442453206, -3.505236298600246325, -18.68346056562440793 ) ) ;
#27756=CARTESIAN_POINT ( 'NONE',  ( 126.1837548109119211, -10.63000616557722466, -14.87417383870573495 ) ) ;
#27757=CARTESIAN_POINT ( 'NONE',  ( 118.0151148109119816, -10.63000616557722466, -14.87417383870573495 ) ) ;
#27759=CARTESIAN_POINT ( 'NONE',  ( 117.3911214775786505, -7.894159318335828068, -9.358103419637847864 ) ) ;
#27760=CARTESIAN_POINT ( 'NONE',  ( 113.7606148109119886, -7.894159318335828068, -9.358103419637847864 ) ) ;
#27763=CARTESIAN_POINT ( 'NONE',  ( 119.6034614775786196, -3.505236298600246325, -18.68346056562440793 ) ) ;
#27764=CARTESIAN_POINT ( 'NONE',  ( 119.7169148109119874, -0.1624402480850797581, -16.17319339645315424 ) ) ;
#27768=AXIS2_PLACEMENT_3D ( 'NONE', #43735, #12280, #16144 ) ;
#27770=CARTESIAN_POINT ( 'NONE',  ( 113.1366214775786432, -1.834011780172310813, -8.268836392978581529 ) ) ;
#27771=CARTESIAN_POINT ( 'NONE',  ( 114.3278814775786429, -10.30919188438810075, -12.61870101168855918 ) ) ;
#27776=CARTESIAN_POINT ( 'NONE',  ( 122.3263414775786373, -6.344957434206665248, -7.627207830600338134 ) ) ;
#27777=CARTESIAN_POINT ( 'NONE',  ( 111.8886348109120092, -3.383040157471821630, -19.15922257007629170 ) ) ;
#27778=CARTESIAN_POINT ( 'NONE',  ( 119.1496481442453046, -6.222761293078241884, -8.102969835052219238 ) ) ;
#27779=CARTESIAN_POINT ( 'NONE',  ( 121.3619881442452879, -4.089484607189486809, -7.948022111789456723 ) ) ;
#27780=CARTESIAN_POINT ( 'NONE',  ( 118.9794681442453026, -9.261995988541697145, -16.69588392320189030 ) ) ;
#27782=CARTESIAN_POINT ( 'NONE',  ( 126.1837548109119211, -10.63000616557722466, -14.87417383870573495 ) ) ;
#27785=CARTESIAN_POINT ( 'NONE',  ( 119.2631014775786298, 0.2603800115204892296, -16.42320221600525088 ) ) ;
#27788=CARTESIAN_POINT ( 'NONE',  ( 115.8027748109119841, -0.4660016031367893996, -10.09054647747474043 ) ) ;
#27793=CARTESIAN_POINT ( 'NONE',  ( 120.0947965460471920, -2.191907684172563986, -18.20049396185734025 ) ) ;
#27796=CARTESIAN_POINT ( 'NONE',  ( 119.7736414775786358, 0.1319031606808879209, -14.10382304977623669 ) ) ;
#27798=CARTESIAN_POINT ( 'NONE',  ( 116.1431348109119881, 0.1319031606808879209, -14.10382304977623669 ) ) ;
#27800=CARTESIAN_POINT ( 'NONE',  ( 120.7379948109119709, 0.4262465694468514643, -12.03445270309931736 ) ) ;
#27802=CARTESIAN_POINT ( 'NONE',  ( 115.8027748109119841, -0.4660016031367893996, -10.09054647747474043 ) ) ;
#27803=CARTESIAN_POINT ( 'NONE',  ( 116.0296814775786345, -1.833838273342658809, -17.42832698103878286 ) ) ;
#27805=CARTESIAN_POINT ( 'NONE',  ( 118.6391081442452986, -4.089484607189486809, -7.948022111789456723 ) ) ;
#27808=CARTESIAN_POINT ( 'NONE',  ( 115.6325948109119821, -9.565557343593402706, -10.61323700422346228 ) ) ;
#27812=CARTESIAN_POINT ( 'NONE',  ( 122.9503348109119827, 0.5811942927096110934, -14.16772938898807510 ) ) ;
#27813=ORIENTED_EDGE ( 'NONE', *, *, #16520, .T. ) ;
#27814=CARTESIAN_POINT ( 'NONE',  ( 127.2313854076961803, -9.032957600002841758, -9.795810222955712021 ) ) ;
#27815=CARTESIAN_POINT ( 'NONE',  ( 116.9940348109119839, -0.1624402480850797581, -16.17319339645315424 ) ) ;
#27816=ADVANCED_FACE ( 'NONE', ( #43973 ), #9313, .F. ) ;
#27819=CARTESIAN_POINT ( 'NONE',  ( 123.9714148109119805, -0.4660016031367893996, -10.09054647747474043 ) ) ;
#27820=EDGE_CURVE ( 'NONE', #28126, #6217, #11920, .T. ) ;
#27824=CARTESIAN_POINT ( 'NONE',  ( 113.2500748109119968, -6.344957434206662583, -7.627207830600332805 ) ) ;
#27826=CARTESIAN_POINT ( 'NONE',  ( 124.8790414775786246, -8.899110576539710493, -16.42337572283490132 ) ) ;
#27827=CARTESIAN_POINT ( 'NONE',  ( 121.8725281442453223, -3.383040157471821630, -19.15922257007629170 ) ) ;
#27828=CARTESIAN_POINT ( 'NONE',  ( 116.2565881442453133, -0.8288870151387760510, -10.36305467784173118 ) ) ;
#27830=CARTESIAN_POINT ( 'NONE',  ( 119.8303681442453126, -10.63000616557722466, -14.87417383870573495 ) ) ;
#27832=CARTESIAN_POINT ( 'NONE',  ( 122.5532481442453019, 0.4262465694468514643, -12.03445270309931736 ) ) ;
#27836=CARTESIAN_POINT ( 'NONE',  ( 118.1285681442453068, -7.893985811506177619, -18.51759400769804742 ) ) ;
#27837=CARTESIAN_POINT ( 'NONE',  ( 136.5847729262652592, -8.473408049995818203, -17.81764962400096763 ) ) ;
#27841=CARTESIAN_POINT ( 'NONE',  ( 135.7778351055028452, -1.201940516317425711, -8.685489187000964506 ) ) ;
#27843=B_SPLINE_CURVE_WITH_KNOTS ( 'NONE', 3,
 ( #34825, #38932, #35734, #413 ),
 .UNSPECIFIED., .F., .F.,
 ( 4, 4 ),
 ( 0.004629286548550820037, 0.006869623107310019426 ),
 .UNSPECIFIED. ) ;
#27845=CARTESIAN_POINT ( 'NONE',  ( 122.2696148109119889, -4.089484607189486809, -7.948022111789456723 ) ) ;
#27847=CARTESIAN_POINT ( 'NONE',  ( 120.9649014775786355, -6.222761293078241884, -8.102969835052219238 ) ) ;
#27848=VERTEX_POINT ( 'NONE', #34142 ) ;
#27851=CARTESIAN_POINT ( 'NONE',  ( 115.6325948109119821, 0.2603800115204892296, -16.42320221600525088 ) ) ;
#27852=CARTESIAN_POINT ( 'NONE',  ( 123.8579614775786126, -9.859900752359378018, -12.68260735090039759 ) ) ;
#27855=CARTESIAN_POINT ( 'NONE',  ( 121.3619881442452879, -4.089484607189486809, -7.948022111789456723 ) ) ;
#27859=CARTESIAN_POINT ( 'NONE',  ( 123.8012348109119642, 0.2603800115204892296, -16.42320221600525088 ) ) ;
#27860=CARTESIAN_POINT ( 'NONE',  ( 120.6245414775786458, -9.988377603198976828, -10.36322818467138340 ) ) ;
#27861=CARTESIAN_POINT ( 'NONE',  ( 124.7655881442452852, -9.859900752359378018, -12.68260735090039759 ) ) ;
#27862=CARTESIAN_POINT ( 'NONE',  ( 118.6391081442452986, -5.574606645277164318, -18.38911715685844683 ) ) ;
#27864=CARTESIAN_POINT ( 'NONE',  ( 115.8595014775786609, -1.834011780172310813, -8.268836392978581529 ) ) ;
#27871=CARTESIAN_POINT ( 'NONE',  ( 126.0703014775786102, -0.1624402480850797581, -16.17319339645315424 ) ) ;
#27873=CARTESIAN_POINT ( 'NONE',  ( 123.6877814775786533, -3.383040157471821630, -19.15922257007629170 ) ) ;
#27876=CARTESIAN_POINT ( 'NONE',  ( 122.4965214775786251, -10.30919188438810075, -12.61870101168855918 ) ) ;
#27877=CARTESIAN_POINT ( 'NONE',  ( 125.0492214775786266, -6.344957434206665248, -7.627207830600338134 ) ) ;
#27879=CARTESIAN_POINT ( 'NONE',  ( 112.0020881442453344, 0.2603800115204892296, -16.42320221600525088 ) ) ;
#27885=CARTESIAN_POINT ( 'NONE',  ( 113.9307948109119764, -10.15424416112533912, -14.75197769757731336 ) ) ;
#27887=CARTESIAN_POINT ( 'NONE',  ( 126.2972081442452890, -2.084020599724406786, -8.691656652584148546 ) ) ;
#27890=CARTESIAN_POINT ( 'NONE',  ( 121.8725281442453223, -6.222761293078241884, -8.102969835052219238 ) ) ;
#27892=CARTESIAN_POINT ( 'NONE',  ( 118.6391081442452986, -5.574606645277164318, -18.38911715685844683 ) ) ;
#27893=CARTESIAN_POINT ( 'NONE',  ( 126.1837548109119211, -10.63000616557722466, -14.87417383870573495 ) ) ;
#27894=EDGE_LOOP ( 'NONE', ( #42934, #28545, #8716, #40255 ) ) ;
#27898=CARTESIAN_POINT ( 'NONE',  ( 113.4202548109119846, 0.1319031606808879209, -14.10382304977623669 ) ) ;
#27904=CARTESIAN_POINT ( 'NONE',  ( 118.0151148109119816, 0.4262465694468514643, -12.03445270309931736 ) ) ;
#27905=CARTESIAN_POINT ( 'NONE',  ( 112.7395348109119766, -4.153390946401321671, -8.397313243818183892 ) ) ;
#27906=EDGE_CURVE ( 'NONE', #15493, #10303, #16588, .T. ) ;
#27908=CARTESIAN_POINT ( 'NONE',  ( 117.4103264091100840, -0.9924539043446216624, -17.29976612834909133 ) ) ;
#27910=ORIENTED_EDGE ( 'NONE', *, *, #2319, .T. ) ;
#27916=CARTESIAN_POINT ( 'NONE',  ( 118.1329114811013312, -2.280480477428486807, -18.08254604495228435 ) ) ;
#27917=CARTESIAN_POINT ( 'NONE',  ( 121.8725281442453223, -6.222761293078241884, -8.102969835052219238 ) ) ;
#27918=CARTESIAN_POINT ( 'NONE',  ( 117.1074881442453233, 0.4262465694468514643, -12.03445270309931736 ) ) ;
#27919=CARTESIAN_POINT ( 'NONE',  ( 113.6471614775786492, -4.153390946401318118, -8.397313243818187445 ) ) ;
#27922=CARTESIAN_POINT ( 'NONE',  ( 115.8595014775786609, -7.643976991954077427, -18.09477374809248928 ) ) ;
#27927=CARTESIAN_POINT ( 'NONE',  ( 116.0864081442453113, -9.988377603198976828, -10.36322818467138340 ) ) ;
#27929=CARTESIAN_POINT ( 'NONE',  ( 114.5547881442453217, -5.638512984488999180, -18.83840828888717311 ) ) ;
#27930=CARTESIAN_POINT ( 'NONE',  ( 151.2860562277021472, -0.6896191363000483410, -17.70303589939592825 ) ) ;
#27932=CARTESIAN_POINT ( 'NONE',  ( 113.9307948109119906, 0.9020085738987339008, -11.91225656197089222 ) ) ;
#27933=CARTESIAN_POINT ( 'NONE',  ( 113.8740681442453138, 0.5811942927096154232, -14.16772938898807155 ) ) ;
#27934=CARTESIAN_POINT ( 'NONE',  ( 125.3328548109119964, -0.8288870151387760510, -10.36305467784173118 ) ) ;
#27939=CARTESIAN_POINT ( 'NONE',  ( 118.2987481442453088, -7.894159318335828068, -9.358103419637847864 ) ) ;
#27943=CARTESIAN_POINT ( 'NONE',  ( 126.5561942423915838, -4.825870161346100140, -8.224435640663250169 ) ) ;
#27944=CARTESIAN_POINT ( 'NONE',  ( 124.9924948109119924, -4.089484607189486809, -7.948022111789456723 ) ) ;
#27946=CARTESIAN_POINT ( 'NONE',  ( 121.1350814775786233, 0.5811942927096110934, -14.16772938898807510 ) ) ;
#27947=CARTESIAN_POINT ( 'NONE',  ( 116.4267681442453153, -3.383040157471821630, -19.15922257007629170 ) ) ;
#27951=CARTESIAN_POINT ( 'NONE',  ( 115.3489614775786407, -0.8288870151387760510, -10.36305467784173118 ) ) ;
#27953=CARTESIAN_POINT ( 'NONE',  ( 124.8790414775786246, -0.4660016031367893996, -10.09054647747474043 ) ) ;
#27954=CARTESIAN_POINT ( 'NONE',  ( 118.3554748109119998, 0.2603800115204892296, -16.42320221600525088 ) ) ;
#27955=CARTESIAN_POINT ( 'NONE',  ( 117.3343948109119737, -6.222761293078241884, -8.102969835052219238 ) ) ;
#27957=CARTESIAN_POINT ( 'NONE',  ( 122.3830681442452857, -1.833838273342659697, -17.42832698103878286 ) ) ;
#27959=CARTESIAN_POINT ( 'NONE',  ( 115.2922348109119781, -10.63000616557722466, -14.87417383870573495 ) ) ;
#27966=CARTESIAN_POINT ( 'NONE',  ( 116.0864081442453113, -9.988377603198976828, -10.36322818467138340 ) ) ;
#27969=CARTESIAN_POINT ( 'NONE',  ( 113.1366214775786432, -7.643976991954077427, -18.09477374809248928 ) ) ;
#27973=CARTESIAN_POINT ( 'NONE',  ( 116.6536748109119941, 0.9020085738987339008, -11.91225656197089222 ) ) ;
#27978=CARTESIAN_POINT ( 'NONE',  ( 119.0929214775786278, -5.638512984489023161, -18.83840828888716601 ) ) ;
#27980=CARTESIAN_POINT ( 'NONE',  ( 120.8514481442452961, -2.084020599724406786, -8.691656652584148546 ) ) ;
#27982=CARTESIAN_POINT ( 'NONE',  ( 136.0617147589354090, -9.506656963484036993, -9.746956911094994069 ) ) ;
#27983=CARTESIAN_POINT ( 'NONE',  ( 121.3619881442452879, -4.089484607189486809, -7.948022111789456723 ) ) ;
#27985=CARTESIAN_POINT ( 'NONE',  ( 115.5191414775786569, -6.222761293078241884, -8.102969835052219238 ) ) ;
#27986=CARTESIAN_POINT ( 'NONE',  ( 114.2711548109119803, -0.1624402480850797581, -16.17319339645315424 ) ) ;
#27989=CARTESIAN_POINT ( 'NONE',  ( 122.0994348109119443, -10.15424416112533912, -14.75197769757731336 ) ) ;
#27990=CARTESIAN_POINT ( 'NONE',  ( 121.1918081442452859, -10.15424416112533912, -14.75197769757731336 ) ) ;
#27996=CARTESIAN_POINT ( 'NONE',  ( 113.6471614775786492, -5.638512984488999180, -18.83840828888717311 ) ) ;
#27997=CARTESIAN_POINT ( 'NONE',  ( 116.3133148109119759, -7.893985811506177619, -18.51759400769804742 ) ) ;
#27999=LINE ( 'NONE', #10669, #9723 ) ;
#28002=CARTESIAN_POINT ( 'NONE',  ( 122.2128881442453263, -1.834011780172310813, -8.268836392978581529 ) ) ;
#28003=CARTESIAN_POINT ( 'NONE',  ( 112.1722681442453222, -0.4660016031367893996, -10.09054647747474043 ) ) ;
#28004=CARTESIAN_POINT ( 'NONE',  ( 119.6601881442453106, -1.833838273342659253, -17.42832698103878286 ) ) ;
#28005=CARTESIAN_POINT ( 'NONE',  ( 125.8433948109119456, -1.834011780172310813, -8.268836392978581529 ) ) ;
#28006=CARTESIAN_POINT ( 'NONE',  ( 117.4478481442453131, 0.2603800115204892296, -16.42320221600525088 ) ) ;
#28007=AXIS2_PLACEMENT_3D ( 'NONE', #6655, #34444, #17150 ) ;
#28010=CARTESIAN_POINT ( 'NONE',  ( 112.3991748109119868, -1.833838273342658809, -17.42832698103878286 ) ) ;
#28013=CARTESIAN_POINT ( 'NONE',  ( 119.7736414775786358, -10.30919188438810075, -12.61870101168855918 ) ) ;
#28015=CARTESIAN_POINT ( 'NONE',  ( 114.7249681442453237, 0.2603800115204892296, -16.42320221600525088 ) ) ;
#28018=LINE ( 'NONE', #3605, #17976 ) ;
#28022=CARTESIAN_POINT ( 'NONE',  ( 120.3409081442453044, -8.899110576539710493, -16.42337572283490132 ) ) ;
#28024=CARTESIAN_POINT ( 'NONE',  ( 120.6245414775786458, -0.1624402480850797581, -16.17319339645315424 ) ) ;
#28026=DIRECTION ( 'NONE',  ( 0.000000000000000000, 0.6004852223388321697, -0.7996358532186279566 ) ) ;
#28027=CARTESIAN_POINT ( 'NONE',  ( 119.9438214775786378, -2.084020599724406786, -8.691656652584148546 ) ) ;
#28029=CARTESIAN_POINT ( 'NONE',  ( 114.7816948109119863, 0.5811942927096154232, -14.16772938898807155 ) ) ;
#28032=CARTESIAN_POINT ( 'NONE',  ( 116.9940348109119839, -0.1624402480850797581, -16.17319339645315424 ) ) ;
#28034=CARTESIAN_POINT ( 'NONE',  ( 117.1074881442453233, -10.63000616557722466, -14.87417383870573495 ) ) ;
#28036=CARTESIAN_POINT ( 'NONE',  ( 115.5191414775786427, -6.222761293078232114, -8.102969835052212133 ) ) ;
#28039=CARTESIAN_POINT ( 'NONE',  ( 121.5888948109119809, -10.30919188438810075, -12.61870101168855918 ) ) ;
#28041=CARTESIAN_POINT ( 'NONE',  ( 126.5254139958957040, -8.459460868501995634, -9.701178152251141995 ) ) ;
#28042=CARTESIAN_POINT ( 'NONE',  ( 118.1852948109119836, -4.153390946401325223, -8.397313243818185668 ) ) ;
#28045=CARTESIAN_POINT ( 'NONE',  ( 126.2404814775786264, -9.261995988541697145, -16.69588392320189030 ) ) ;
#28049=CARTESIAN_POINT ( 'NONE',  ( 115.5191414775786569, -3.383040157471821630, -19.15922257007629170 ) ) ;
#28050=CARTESIAN_POINT ( 'NONE',  ( 125.6732148109119862, -9.859900752359378018, -12.68260735090039759 ) ) ;
#28051=CARTESIAN_POINT ( 'NONE',  ( 124.0848681442452772, -4.089484607189486809, -7.948022111789456723 ) ) ;
#28052=CARTESIAN_POINT ( 'NONE',  ( 115.9729548109119861, -3.505236298600246325, -18.68346056562440793 ) ) ;
#28054=CARTESIAN_POINT ( 'NONE',  ( 118.2987481442453088, -1.561330072975668504, -17.79121239304076951 ) ) ;
#28057=CARTESIAN_POINT ( 'NONE',  ( 124.6521348109119884, -7.894159318335828068, -9.358103419637847864 ) ) ;
#28061=CARTESIAN_POINT ( 'NONE',  ( 115.1787814775786387, -9.988377603198976828, -10.36322818467138340 ) ) ;
#28062=CARTESIAN_POINT ( 'NONE',  ( 123.8579614775786126, -9.859900752359378018, -12.68260735090039759 ) ) ;
#28064=CARTESIAN_POINT ( 'NONE',  ( 121.0807175202278074, -2.239543233855044946, -18.13706010537467606 ) ) ;
#28065=CARTESIAN_POINT ( 'NONE',  ( 122.2128881442453263, -1.834011780172310813, -8.268836392978581529 ) ) ;
#28066=CONICAL_SURFACE ( 'NONE', #29518, 5.999999999999997335, 0.4636476090008060935 ) ;
#28068=CARTESIAN_POINT ( 'NONE',  ( 121.5321681442453183, -0.1624402480850797581, -16.17319339645315424 ) ) ;
#28072=CARTESIAN_POINT ( 'NONE',  ( 112.7962614775786676, -3.383040157471821630, -19.15922257007629170 ) ) ;
#28073=CARTESIAN_POINT ( 'NONE',  ( 123.0637881442452937, -8.899110576539710493, -16.42337572283490132 ) ) ;
#28077=CARTESIAN_POINT ( 'NONE',  ( 123.9146881442452894, 0.9020085738987339008, -11.91225656197089222 ) ) ;
#28080=CARTESIAN_POINT ( 'NONE',  ( 123.7445081442452874, -1.561330072975668948, -17.79121239304076951 ) ) ;
#28081=CARTESIAN_POINT ( 'NONE',  ( 120.7379948109119709, -10.63000616557722466, -14.87417383870573495 ) ) ;
#28082=CARTESIAN_POINT ( 'NONE',  ( 125.1059481442452750, -1.833838273342660141, -17.42832698103878286 ) ) ;
#28083=CARTESIAN_POINT ( 'NONE',  ( 119.1496481442453046, -6.222761293078241884, -8.102969835052219238 ) ) ;
#28084=LINE ( 'NONE', #41992, #41497 ) ;
#28085=CARTESIAN_POINT ( 'NONE',  ( 114.3278814775786429, -10.30919188438810075, -12.61870101168855918 ) ) ;
#28092=CARTESIAN_POINT ( 'NONE',  ( 125.9568481442452850, -6.344957434206665248, -7.627207830600338134 ) ) ;
#28093=CARTESIAN_POINT ( 'NONE',  ( 125.3895814775786448, -2.084020599724406786, -8.691656652584148546 ) ) ;
#28096=CARTESIAN_POINT ( 'NONE',  ( 114.6115148109119986, -6.222761293078241884, -8.102969835052219238 ) ) ;
#28099=CARTESIAN_POINT ( 'NONE',  ( 124.1983214775786166, -8.166667518702819706, -8.995218007635861213 ) ) ;
#28102=CARTESIAN_POINT ( 'NONE',  ( 123.9714148109119805, -0.4660016031367893996, -10.09054647747474043 ) ) ;
#28105=CARTESIAN_POINT ( 'NONE',  ( 126.0135748109119902, -1.833838273342660141, -17.42832698103878286 ) ) ;
#28109=CARTESIAN_POINT ( 'NONE',  ( 126.4599182912984077, -7.451362815295157205, -8.974203731756436042 ) ) ;
#28110=CARTESIAN_POINT ( 'NONE',  ( 113.5337081442453240, -0.8288870151387760510, -10.36305467784173118 ) ) ;
#28111=CARTESIAN_POINT ( 'NONE',  ( 113.8173414775786512, 0.2603800115204892296, -16.42320221600525088 ) ) ;
#28114=CARTESIAN_POINT ( 'NONE',  ( 121.0783548109119749, -9.565557343593413364, -10.61323700422348004 ) ) ;
#28115=CARTESIAN_POINT ( 'NONE',  ( 119.2063748109119814, -7.894159318335828068, -9.358103419637847864 ) ) ;
#28116=CARTESIAN_POINT ( 'NONE',  ( 112.4559014775786778, -0.1624402480850797581, -16.17319339645315424 ) ) ;
#28120=CARTESIAN_POINT ( 'NONE',  ( 114.9518748109119883, -7.643976991954077427, -18.09477374809248928 ) ) ;
#28122=CARTESIAN_POINT ( 'NONE',  ( 126.2758031835854098, -9.050378324229031435, -16.17924689356632584 ) ) ;
#28126=VERTEX_POINT ( 'NONE', #14523 ) ;
#28127=CARTESIAN_POINT ( 'NONE',  ( 119.0361948109119652, -2.084020599724406786, -8.691656652584148546 ) ) ;
#28128=CARTESIAN_POINT ( 'NONE',  ( 112.3424481442453384, -3.505236298600246325, -18.68346056562440793 ) ) ;
#28137=CARTESIAN_POINT ( 'NONE',  ( 113.0798948109119948, -0.4660016031367893996, -10.09054647747474043 ) ) ;
#28138=CARTESIAN_POINT ( 'NONE',  ( 123.1772414775786189, -5.574606645277164318, -18.38911715685844683 ) ) ;
#28139=CARTESIAN_POINT ( 'NONE',  ( 118.3554748109119998, -9.565557343593413364, -10.61323700422348004 ) ) ;
#28140=CARTESIAN_POINT ( 'NONE',  ( 113.3277860444392076, -1.267766418764742387, -16.93314635290707315 ) ) ;
#28142=CARTESIAN_POINT ( 'NONE',  ( 116.7104014775786425, -8.899110576539710493, -16.42337572283490132 ) ) ;
#28145=CARTESIAN_POINT ( 'NONE',  ( 116.9582927111058552, -1.267766418764730840, -16.93314635290706605 ) ) ;
#28147=CARTESIAN_POINT ( 'NONE',  ( 113.8173414775786512, 0.2603800115204892296, -16.42320221600525088 ) ) ;
#28149=CARTESIAN_POINT ( 'NONE',  ( 115.8595014775786609, -1.834011780172310813, -8.268836392978581529 ) ) ;
#28152=CARTESIAN_POINT ( 'NONE',  ( 114.1009748109119784, -4.089484607189486809, -7.948022111789456723 ) ) ;
#28154=CARTESIAN_POINT ( 'NONE',  ( 112.5126281442453120, -10.30919188438810075, -12.61870101168855918 ) ) ;
#28155=CARTESIAN_POINT ( 'NONE',  ( 124.1983214775786166, -1.833838273342659697, -17.42832698103878286 ) ) ;
#28158=ORIENTED_EDGE ( 'NONE', *, *, #20085, .T. ) ;
#28161=CARTESIAN_POINT ( 'NONE',  ( 116.7671281442453335, -7.643976991954077427, -18.09477374809248928 ) ) ;
#28163=CARTESIAN_POINT ( 'NONE',  ( 118.2795432127138611, -2.191907684172563986, -18.20049396185734025 ) ) ;
#28165=CARTESIAN_POINT ( 'NONE',  ( 127.9806007748884298, -5.559840797202522999, -7.553254777380711715 ) ) ;
#28166=CARTESIAN_POINT ( 'NONE',  ( 125.7866681442452688, -0.4660016031367893996, -10.09054647747474043 ) ) ;
#28169=CARTESIAN_POINT ( 'NONE',  ( 123.8579614775786126, 0.5811942927096110934, -14.16772938898807510 ) ) ;
#28170=CARTESIAN_POINT ( 'NONE',  ( 115.7460481442453357, 0.9020085738987339008, -11.91225656197089222 ) ) ;
#28173=CARTESIAN_POINT ( 'NONE',  ( 114.2144281442453178, -1.833838273342658809, -17.42832698103878286 ) ) ;
#28175=CARTESIAN_POINT ( 'NONE',  ( 119.0929214775786278, -5.638512984488999180, -18.83840828888717311 ) ) ;
#28176=CARTESIAN_POINT ( 'NONE',  ( 117.6747548109119919, -7.643976991954077427, -18.09477374809248928 ) ) ;
#28178=CARTESIAN_POINT ( 'NONE',  ( 122.9503348109119827, -9.859900752359378018, -12.68260735090039759 ) ) ;
#28180=CARTESIAN_POINT ( 'NONE',  ( 116.1431348109119881, -10.30919188438810075, -12.61870101168855918 ) ) ;
#28181=CARTESIAN_POINT ( 'NONE',  ( 136.6050546525240463, 0.4234926033938513634, -15.51982212705869735 ) ) ;
#28185=CARTESIAN_POINT ( 'NONE',  ( 127.0728412258224580, 0.5536521883242400133, -13.06923365641767276 ) ) ;
#28188=CARTESIAN_POINT ( 'NONE',  ( 115.8027748109119841, -0.4660016031367893996, -10.09054647747474043 ) ) ;
#28189=CARTESIAN_POINT ( 'NONE',  ( 137.2528433483957997, -10.12362414824511347, -13.50737840558690017 ) ) ;
#28195=CARTESIAN_POINT ( 'NONE',  ( 121.9491998309151057, -2.215723800389698184, -18.16877924232191788 ) ) ;
#28200=CARTESIAN_POINT ( 'NONE',  ( 116.2565881442452991, -9.261995988541697145, -16.69588392320189030 ) ) ;
#28201=CYLINDRICAL_SURFACE ( 'NONE', #36572, 1.999999999999999778 ) ;
#28202=CARTESIAN_POINT ( 'NONE',  ( 119.1496481442453046, -6.222761293078241884, -8.102969835052219238 ) ) ;
#28203=EDGE_LOOP ( 'NONE', ( #25340, #33710, #8535, #36453 ) ) ;
#28205=CARTESIAN_POINT ( 'NONE',  ( 121.3052614775786111, -1.834011780172310813, -8.268836392978581529 ) ) ;
#28207=CARTESIAN_POINT ( 'NONE',  ( 114.7249681442453237, -9.565557343593413364, -10.61323700422348004 ) ) ;
#28208=CARTESIAN_POINT ( 'NONE',  ( 113.1933481442453058, -5.574606645277164318, -18.38911715685844683 ) ) ;
#28211=CARTESIAN_POINT ( 'NONE',  ( 121.2485348109119769, -8.899110576539710493, -16.42337572283490132 ) ) ;
#28212=CARTESIAN_POINT ( 'NONE',  ( 121.1350814775786233, -9.859900752359378018, -12.68260735090039759 ) ) ;
#28213=CARTESIAN_POINT ( 'NONE',  ( 114.4980614775786734, -2.084020599724388578, -8.691656652584157428 ) ) ;
#28219=CARTESIAN_POINT ( 'NONE',  ( 116.1431348109119881, -10.30919188438810075, -12.61870101168855918 ) ) ;
#28220=CARTESIAN_POINT ( 'NONE',  ( 115.7460481442453357, 0.9020085738987339008, -11.91225656197089222 ) ) ;
#28222=CARTESIAN_POINT ( 'NONE',  ( 114.3846081442453197, -10.63000616557722466, -14.87417383870573495 ) ) ;
#28226=CARTESIAN_POINT ( 'NONE',  ( 121.5888948109119809, -10.30919188438810075, -12.61870101168855918 ) ) ;
#28227=CARTESIAN_POINT ( 'NONE',  ( 114.9518748109119883, -1.834011780172310813, -8.268836392978581529 ) ) ;
#28228=CARTESIAN_POINT ( 'NONE',  ( 121.0783548109119749, -9.565557343593413364, -10.61323700422348004 ) ) ;
#28229=CARTESIAN_POINT ( 'NONE',  ( 111.5482748109120053, -0.1624402480850797581, -16.17319339645315424 ) ) ;
#28230=CARTESIAN_POINT ( 'NONE',  ( 120.5678148109119832, -8.166667518702819706, -8.995218007635861213 ) ) ;
#28233=CARTESIAN_POINT ( 'NONE',  ( 115.9729548109119861, -3.505236298600246325, -18.68346056562440793 ) ) ;
#28236=CARTESIAN_POINT ( 'NONE',  ( 122.6099748109119929, -9.261995988541697145, -16.69588392320189030 ) ) ;
#28237=CARTESIAN_POINT ( 'NONE',  ( 119.2631014775786298, 0.2603800115204892296, -16.42320221600525088 ) ) ;
#28238=ORIENTED_EDGE ( 'NONE', *, *, #41477, .F. ) ;
#28240=CARTESIAN_POINT ( 'NONE',  ( 124.6521348109119884, -1.561330072975668948, -17.79121239304076951 ) ) ;
#28243=CARTESIAN_POINT ( 'NONE',  ( 116.7104014775786425, -8.899110576539710493, -16.42337572283490132 ) ) ;
#28245=CARTESIAN_POINT ( 'NONE',  ( 121.4754414775786131, -1.833838273342659697, -17.42832698103878286 ) ) ;
#28246=CARTESIAN_POINT ( 'NONE',  ( 121.1350814775786233, 0.5811942927096136469, -14.16772938898805378 ) ) ;
#28247=CARTESIAN_POINT ( 'NONE',  ( 122.9503348109119827, -9.859900752359378018, -12.68260735090039759 ) ) ;
#28249=CARTESIAN_POINT ( 'NONE',  ( 120.2274548109119934, -9.859900752359378018, -12.68260735090039759 ) ) ;
#28251=CARTESIAN_POINT ( 'NONE',  ( 116.1431348109119881, -10.30919188438810075, -12.61870101168855918 ) ) ;
#28253=CARTESIAN_POINT ( 'NONE',  ( 119.5467348109119712, -5.574606645277164318, -18.38911715685844683 ) ) ;
#28255=CARTESIAN_POINT ( 'NONE',  ( 118.4122014775786340, 0.5811942927096110934, -14.16772938898807510 ) ) ;
#28261=CARTESIAN_POINT ( 'NONE',  ( 124.0848681442452772, -4.089484607189486809, -7.948022111789456723 ) ) ;
#28263=CARTESIAN_POINT ( 'NONE',  ( 126.2184548109108420, -7.957993755341922437, -9.463799409162998444 ) ) ;
#28264=CARTESIAN_POINT ( 'NONE',  ( 120.3976348109119812, -7.643976991954077427, -18.09477374809248928 ) ) ;
#28267=CARTESIAN_POINT ( 'NONE',  ( 126.1270281442452870, -10.30919188438810075, -12.61870101168855918 ) ) ;
#28269=CARTESIAN_POINT ( 'NONE',  ( 123.2184548109119788, -2.211393927326563702, -15.67656524173425758 ) ) ;
#28271=CARTESIAN_POINT ( 'NONE',  ( 113.7606148109119886, -1.561330072975668060, -17.79121239304076596 ) ) ;
#28272=CARTESIAN_POINT ( 'NONE',  ( 124.9357681442453014, -7.643976991954077427, -18.09477374809248928 ) ) ;
#28273=CARTESIAN_POINT ( 'NONE',  ( 121.9859814775786333, 0.2603800115204892296, -16.42320221600525088 ) ) ;
#28274=CARTESIAN_POINT ( 'NONE',  ( 117.7882081442453170, -3.505236298600246325, -18.68346056562440793 ) ) ;
#28276=CARTESIAN_POINT ( 'NONE',  ( 126.5621572004008755, -3.449551328269489403, -8.418040804988667247 ) ) ;
#28277=CARTESIAN_POINT ( 'NONE',  ( 123.6310548109119765, -5.638512984488999180, -18.83840828888717311 ) ) ;
#28278=CARTESIAN_POINT ( 'NONE',  ( 111.7857214775786474, -4.159894987975828684, -8.443039665293898821 ) ) ;
#28281=CARTESIAN_POINT ( 'NONE',  ( 125.7299414775786346, -10.15424416112533912, -14.75197769757731336 ) ) ;
#28284=CARTESIAN_POINT ( 'NONE',  ( 121.2485348109119769, -0.4660016031367893996, -10.09054647747474043 ) ) ;
#28285=CARTESIAN_POINT ( 'NONE',  ( 135.9690293846555278, -8.515994457645518878, -18.06058892513630099 ) ) ;
#28288=CARTESIAN_POINT ( 'NONE',  ( 122.3263414775786373, -6.344957434206665248, -7.627207830600338134 ) ) ;
#28290=CARTESIAN_POINT ( 'NONE',  ( 120.7379948109119709, 0.4262465694468514643, -12.03445270309931736 ) ) ;
#28292=CARTESIAN_POINT ( 'NONE',  ( 116.1431348109119881, -10.30919188438810075, -12.61870101168855918 ) ) ;
#28294=CARTESIAN_POINT ( 'NONE',  ( 112.5649393026123022, -1.179503403430478770, -17.05068175419387799 ) ) ;
#28296=CARTESIAN_POINT ( 'NONE',  ( 125.9001214775786224, -4.089484607189486809, -7.948022111789456723 ) ) ;
#28297=DIRECTION ( 'NONE',  ( -1.000000000000000000, 0.000000000000000000, 0.000000000000000000 ) ) ;
#28299=CARTESIAN_POINT ( 'NONE',  ( 124.5954081442453116, -3.383040157471821630, -19.15922257007629170 ) ) ;
#28300=CARTESIAN_POINT ( 'NONE',  ( 123.6877814775786533, -3.383040157471821630, -19.15922257007629170 ) ) ;
#28301=CARTESIAN_POINT ( 'NONE',  ( 121.8725281442453223, -6.222761293078241884, -8.102969835052219238 ) ) ;
#28302=CARTESIAN_POINT ( 'NONE',  ( 118.5256548109119876, -8.899110576539710493, -16.42337572283490132 ) ) ;
#28304=CARTESIAN_POINT ( 'NONE',  ( 117.1642148109119859, -9.261995988541697145, -16.69588392320189030 ) ) ;
#28306=CARTESIAN_POINT ( 'NONE',  ( 122.8176765460471813, -2.191907684172563986, -18.20049396185734025 ) ) ;
#28307=CARTESIAN_POINT ( 'NONE',  ( 125.5492214775786550, -6.210324830719740064, -8.151390318758597431 ) ) ;
#28311=CARTESIAN_POINT ( 'NONE',  ( 124.4819548109119722, -7.893985811506177619, -18.51759400769804742 ) ) ;
#28312=CARTESIAN_POINT ( 'NONE',  ( 112.7395348109119766, -5.638512984488999180, -18.83840828888717311 ) ) ;
#28314=CARTESIAN_POINT ( 'NONE',  ( 112.0588148109119828, -9.859900752359374465, -12.68260735090039404 ) ) ;
#28317=CARTESIAN_POINT ( 'NONE',  ( 122.2128881442453263, -1.834011780172310813, -8.268836392978581529 ) ) ;
#28318=CARTESIAN_POINT ( 'NONE',  ( 123.1772414775786189, -4.089484607189486809, -7.948022111789456723 ) ) ;
#28320=CARTESIAN_POINT ( 'NONE',  ( 117.6747548109119919, -1.834011780172310813, -8.268836392978581529 ) ) ;
#28324=CARTESIAN_POINT ( 'NONE',  ( 126.4852516627942265, -7.433467366253567299, -8.949158261980540985 ) ) ;
#28325=CARTESIAN_POINT ( 'NONE',  ( 113.9875214775786532, -8.899110576539710493, -16.42337572283490132 ) ) ;
#28326=CARTESIAN_POINT ( 'NONE',  ( 112.0588148109119828, 0.5811942927096154232, -14.16772938898807155 ) ) ;
#28329=CARTESIAN_POINT ( 'NONE',  ( 123.8579614775786126, -9.859900752359378018, -12.68260735090039759 ) ) ;
#28330=CARTESIAN_POINT ( 'NONE',  ( 121.1918081442452859, -10.15424416112533912, -14.75197769757731336 ) ) ;
#28331=CARTESIAN_POINT ( 'NONE',  ( 125.6732148109119862, 0.5811942927096110934, -14.16772938898807510 ) ) ;
#28336=CARTESIAN_POINT ( 'NONE',  ( 115.1787814775786387, -0.1624402480850797581, -16.17319339645315424 ) ) ;
#28338=CARTESIAN_POINT ( 'NONE',  ( 126.4915402333597854, -9.314160179844931164, -15.95839630942495724 ) ) ;
#28341=CARTESIAN_POINT ( 'NONE',  ( 125.1059481442452750, -1.833838273342660141, -17.42832698103878286 ) ) ;
#28343=CARTESIAN_POINT ( 'NONE',  ( 117.9016614775786280, -0.1624402480850797581, -16.17319339645315424 ) ) ;
#28344=CARTESIAN_POINT ( 'NONE',  ( 112.4559014775786778, -0.1624402480850797581, -16.17319339645315424 ) ) ;
#28352=CARTESIAN_POINT ( 'NONE',  ( 113.2500748109119968, -6.344957434206662583, -7.627207830600332805 ) ) ;
#28353=CARTESIAN_POINT ( 'NONE',  ( 112.0020881442453344, 0.2603800115204892296, -16.42320221600525088 ) ) ;
#28354=CARTESIAN_POINT ( 'NONE',  ( 119.3198281442452924, -9.859900752359374465, -12.68260735090039404 ) ) ;
#28355=DIRECTION ( 'NONE',  ( 0.000000000000000000, -0.6004852223388319477, 0.7996358532186282897 ) ) ;
#28357=CARTESIAN_POINT ( 'NONE',  ( 117.6180281442453150, -8.899110576539710493, -16.42337572283490132 ) ) ;
#28362=CARTESIAN_POINT ( 'NONE',  ( 113.2500748109119968, -6.344957434206662583, -7.627207830600332805 ) ) ;
#28364=CARTESIAN_POINT ( 'NONE',  ( 116.5402214775786405, 0.2603800115204892296, -16.42320221600525088 ) ) ;
#28368=CARTESIAN_POINT ( 'NONE',  ( 112.1722681442453222, -0.4660016031367893996, -10.09054647747474043 ) ) ;
#28369=CARTESIAN_POINT ( 'NONE',  ( 114.7249681442453237, 0.2603800115204892296, -16.42320221600525088 ) ) ;
#28370=CARTESIAN_POINT ( 'NONE',  ( 127.0553483106841810, -10.27339372193082312, -13.70636429400185285 ) ) ;
#28377=CARTESIAN_POINT ( 'NONE',  ( 115.7460481442453357, -10.15424416112533912, -14.75197769757731336 ) ) ;
#28381=CARTESIAN_POINT ( 'NONE',  ( 126.9115046738381096, -5.096111321019845875, -8.051413078099821874 ) ) ;
#28382=CARTESIAN_POINT ( 'NONE',  ( 125.1626748109119802, -9.988377603198980381, -10.36322818467138518 ) ) ;
#28385=CARTESIAN_POINT ( 'NONE',  ( 125.6164881442453094, 0.2603800115204892296, -16.42320221600525088 ) ) ;
#28386=CARTESIAN_POINT ( 'NONE',  ( 117.5045748109119756, 0.5811942927096110934, -14.16772938898807510 ) ) ;
#28387=ORIENTED_EDGE ( 'NONE', *, *, #7278, .F. ) ;
#28389=CARTESIAN_POINT ( 'NONE',  ( 115.2355081442453155, 0.1319031606808879209, -14.10382304977623669 ) ) ;
#28390=CARTESIAN_POINT ( 'NONE',  ( 111.7751814775786556, -7.893985811506177619, -18.51759400769804742 ) ) ;
#28391=CARTESIAN_POINT ( 'NONE',  ( 116.3133148109119759, -7.893985811506177619, -18.51759400769804742 ) ) ;
#28392=CARTESIAN_POINT ( 'NONE',  ( 115.1787814775786387, -0.1624402480850797581, -16.17319339645315424 ) ) ;
#28394=CARTESIAN_POINT ( 'NONE',  ( 122.0427081442452817, -9.859900752359378018, -12.68260735090039759 ) ) ;
#28396=CARTESIAN_POINT ( 'NONE',  ( 115.6325948109119821, 0.2603800115204892296, -16.42320221600525088 ) ) ;
#28398=CARTESIAN_POINT ( 'NONE',  ( 137.4531891128992811, 0.2004337171367315540, -13.63196781300515781 ) ) ;
#28404=CARTESIAN_POINT ( 'NONE',  ( 126.4552522132384667, 0.2524518362947308914, -13.53592757502032917 ) ) ;
#28407=CARTESIAN_POINT ( 'NONE',  ( 114.4413348109119823, -9.261995988541697145, -16.69588392320189030 ) ) ;
#28409=CARTESIAN_POINT ( 'NONE',  ( 114.2144281442453178, -1.833838273342658809, -17.42832698103878286 ) ) ;
#28413=CARTESIAN_POINT ( 'NONE',  ( 112.1722681442453222, -8.899110576539710493, -16.42337572283490132 ) ) ;
#28417=CARTESIAN_POINT ( 'NONE',  ( 118.0151148109119816, -10.63000616557722466, -14.87417383870573495 ) ) ;
#28418=CARTESIAN_POINT ( 'NONE',  ( 124.8223148109119762, -10.15424416112533912, -14.75197769757731336 ) ) ;
#28419=CARTESIAN_POINT ( 'NONE',  ( 119.2631014775786298, -9.565557343593413364, -10.61323700422348004 ) ) ;
#28420=CARTESIAN_POINT ( 'NONE',  ( 113.0798948109119948, -8.899110576539710493, -16.42337572283490132 ) ) ;
#28423=CARTESIAN_POINT ( 'NONE',  ( 124.7088614775786226, 0.2603800115204892296, -16.42320221600525088 ) ) ;
#28425=CARTESIAN_POINT ( 'NONE',  ( 117.7882081442453170, -3.505236298600246325, -18.68346056562440793 ) ) ;
#28426=CARTESIAN_POINT ( 'NONE',  ( 115.3489614775786407, -0.8288870151387760510, -10.36305467784173118 ) ) ;
#28429=CARTESIAN_POINT ( 'NONE',  ( 121.1918081442452859, -10.15424416112533912, -14.75197769757731336 ) ) ;
#28430=CARTESIAN_POINT ( 'NONE',  ( 124.1415948109119540, -3.505236298600246325, -18.68346056562440793 ) ) ;
#28431=CARTESIAN_POINT ( 'NONE',  ( 114.6682414775786469, -7.894159318335810305, -9.358103419637833653 ) ) ;
#28437=CARTESIAN_POINT ( 'NONE',  ( 115.9729548109119861, -6.344957434206662583, -7.627207830600332805 ) ) ;
#28438=CARTESIAN_POINT ( 'NONE',  ( 113.4769814775786330, -10.63000616557722466, -14.87417383870573495 ) ) ;
#28441=CARTESIAN_POINT ( 'NONE',  ( 112.1722681442453222, -0.4660016031367893996, -10.09054647747474043 ) ) ;
#28443=CARTESIAN_POINT ( 'NONE',  ( 113.0188248073892794, -1.081026697600518283, -17.18181821144401766 ) ) ;
#28444=CARTESIAN_POINT ( 'NONE',  ( 123.9714148109119805, -0.4660016031367893996, -10.09054647747474043 ) ) ;
#28446=CARTESIAN_POINT ( 'NONE',  ( 114.8384214775786489, 0.9020085738987339008, -11.91225656197089222 ) ) ;
#28447=CARTESIAN_POINT ( 'NONE',  ( 122.6667014775786413, -2.084020599724406786, -8.691656652584148546 ) ) ;
#28450=CARTESIAN_POINT ( 'NONE',  ( 124.3117748109119844, -10.30919188438810075, -12.61870101168855918 ) ) ;
#28451=CARTESIAN_POINT ( 'NONE',  ( 120.7379948109119709, -10.63000616557722466, -14.87417383870573495 ) ) ;
#28454=CARTESIAN_POINT ( 'NONE',  ( 116.0864081442453113, -0.1624402480850797581, -16.17319339645315424 ) ) ;
#28455=B_SPLINE_CURVE_WITH_KNOTS ( 'NONE', 3,
 ( #42131, #14757, #25248, #38459, #10891, #14529, #4028, #28443, #24790, #28893 ),
 .UNSPECIFIED., .F., .F.,
 ( 4, 3, 3, 4 ),
 ( 4.336808689942019662E-19, 0.0001671877548681264863, 0.0003343755096277690043, 0.0006463528481650629171 ),
 .UNSPECIFIED. ) ;
#28458=CARTESIAN_POINT ( 'NONE',  ( 123.3474214775786209, -9.988377603198976828, -10.36322818467138340 ) ) ;
#28459=ADVANCED_FACE ( 'NONE', ( #32729 ), #1503, .T. ) ;
#28461=CARTESIAN_POINT ( 'NONE',  ( 118.1285681442453068, -7.893985811506177619, -18.51759400769804742 ) ) ;
#28462=ORIENTED_EDGE ( 'NONE', *, *, #43997, .T. ) ;
#28466=CARTESIAN_POINT ( 'NONE',  ( 122.7694671478583501, -3.807985514183312326, -19.09877912889401941 ) ) ;
#28467=CARTESIAN_POINT ( 'NONE',  ( 114.3278814775786429, 0.1319031606808879209, -14.10382304977623669 ) ) ;
#28469=EDGE_CURVE ( 'NONE', #10826, #32004, #44496, .T. ) ;
#28470=CARTESIAN_POINT ( 'NONE',  ( 118.8092881442453290, -0.1624402480850797581, -16.17319339645315424 ) ) ;
#28472=CARTESIAN_POINT ( 'NONE',  ( 120.9081748109119872, -4.153390946401325223, -8.397313243818185668 ) ) ;
#28475=CARTESIAN_POINT ( 'NONE',  ( 118.3554748109119998, -9.565557343593413364, -10.61323700422348004 ) ) ;
#28477=CARTESIAN_POINT ( 'NONE',  ( 113.3635281442453504, -9.988377603198976828, -10.36322818467138340 ) ) ;
#28478=CARTESIAN_POINT ( 'NONE',  ( 119.2063748109119814, -1.561330072975668504, -17.79121239304076951 ) ) ;
#28479=CARTESIAN_POINT ( 'NONE',  ( 113.0231681442453322, 0.9020085738987339008, -11.91225656197089222 ) ) ;
#28481=CARTESIAN_POINT ( 'NONE',  ( 120.7379948109119709, 0.4262465694468514643, -12.03445270309931736 ) ) ;
#28482=VERTEX_POINT ( 'NONE', #3308 ) ;
#28483=CARTESIAN_POINT ( 'NONE',  ( 117.7882081442453170, -6.344957434206665248, -7.627207830600338134 ) ) ;
#28485=CARTESIAN_POINT ( 'NONE',  ( 151.2860562277021472, -2.495269033102075262, -17.79652296963211455 ) ) ;
#28488=CARTESIAN_POINT ( 'NONE',  ( 122.0994348109119443, 0.9020085738987339008, -11.91225656197089222 ) ) ;
#28489=EDGE_LOOP ( 'NONE', ( #12624, #28462, #17244, #4942, #24462 ) ) ;
#28491=CARTESIAN_POINT ( 'NONE',  ( 122.0994348109119443, -10.15424416112533912, -14.75197769757731336 ) ) ;
#28496=ORIENTED_EDGE ( 'NONE', *, *, #5477, .F. ) ;
#28497=CARTESIAN_POINT ( 'NONE',  ( 114.6115148109119986, -3.383040157471821630, -19.15922257007629170 ) ) ;
#28498=CARTESIAN_POINT ( 'NONE',  ( 125.1059481442452750, -1.833838273342660141, -17.42832698103878286 ) ) ;
#28501=CARTESIAN_POINT ( 'NONE',  ( 120.9081748109119872, -4.153390946401325223, -8.397313243818185668 ) ) ;
#28504=CARTESIAN_POINT ( 'NONE',  ( 121.0216281442452981, -1.561330072975668948, -17.79121239304076951 ) ) ;
#28508=CARTESIAN_POINT ( 'NONE',  ( 112.4559014775786494, -9.988377603198976828, -10.36322818467138340 ) ) ;
#28513=CARTESIAN_POINT ( 'NONE',  ( 121.9859814775786333, 0.2603800115204892296, -16.42320221600525088 ) ) ;
#28514=CARTESIAN_POINT ( 'NONE',  ( 137.4945747550012811, -9.029089147476250687, -16.19493358130536365 ) ) ;
#28515=ORIENTED_EDGE ( 'NONE', *, *, #42306, .T. ) ;
#28517=CARTESIAN_POINT ( 'NONE',  ( 112.1722681442453222, -0.4660016031367893996, -10.09054647747474043 ) ) ;
#28518=CARTESIAN_POINT ( 'NONE',  ( 112.3991748109119868, -1.833838273342658809, -17.42832698103878286 ) ) ;
#28520=CARTESIAN_POINT ( 'NONE',  ( 122.3263414775786373, -3.505236298600246325, -18.68346056562440793 ) ) ;
#28522=CARTESIAN_POINT ( 'NONE',  ( 114.7249681442453237, 0.2603800115204892296, -16.42320221600525088 ) ) ;
#28524=DIRECTION ( 'NONE',  ( -1.000000000000000000, 0.000000000000000000, 0.000000000000000000 ) ) ;
#28526=CARTESIAN_POINT ( 'NONE',  ( 111.4241771286805260, -2.495269033102075262, -17.79652296963211455 ) ) ;
#28527=CARTESIAN_POINT ( 'NONE',  ( 125.3895814775786448, -7.893985811506177619, -18.51759400769804742 ) ) ;
#28529=CARTESIAN_POINT ( 'NONE',  ( 124.4252281442452812, -9.261995988541697145, -16.69588392320189030 ) ) ;
#28530=CARTESIAN_POINT ( 'NONE',  ( 123.5743281442453139, -7.893985811506177619, -18.51759400769804742 ) ) ;
#28531=CARTESIAN_POINT ( 'NONE',  ( 124.4819548109119722, -2.084020599724406786, -8.691656652584148546 ) ) ;
#28532=CARTESIAN_POINT ( 'NONE',  ( 119.8870948109119752, -0.8288870151387760510, -10.36305467784173118 ) ) ;
#28534=CARTESIAN_POINT ( 'NONE',  ( 118.9227414775786400, -10.63000616557722466, -14.87417383870573495 ) ) ;
#28543=CARTESIAN_POINT ( 'NONE',  ( 125.6164881442453094, 0.2603800115204892296, -16.42320221600525088 ) ) ;
#28544=CARTESIAN_POINT ( 'NONE',  ( 125.8433948109119456, -7.643976991954077427, -18.09477374809248928 ) ) ;
#28545=ORIENTED_EDGE ( 'NONE', *, *, #7813, .T. ) ;
#28546=CARTESIAN_POINT ( 'NONE',  ( 111.4348214775786801, -3.505236298600246325, -18.68346056562440793 ) ) ;
#28549=CARTESIAN_POINT ( 'NONE',  ( 125.5030348109119558, -3.383040157471821630, -19.15922257007629170 ) ) ;
#28550=CARTESIAN_POINT ( 'NONE',  ( 125.5597614775786326, -1.561330072975669392, -17.79121239304076951 ) ) ;
#28552=CARTESIAN_POINT ( 'NONE',  ( 114.7249681442453237, 0.2603800115204892296, -16.42320221600525088 ) ) ;
#28555=ORIENTED_EDGE ( 'NONE', *, *, #19062, .T. ) ;
#28557=CARTESIAN_POINT ( 'NONE',  ( 116.6536748109119941, -10.15424416112533912, -14.75197769757731336 ) ) ;
#28558=CARTESIAN_POINT ( 'NONE',  ( 113.1933481442453058, -4.089484607189486809, -7.948022111789456723 ) ) ;
#28560=CARTESIAN_POINT ( 'NONE',  ( 123.5743281442453139, -2.084020599724406786, -8.691656652584148546 ) ) ;
#28561=CARTESIAN_POINT ( 'NONE',  ( 120.8514481442452961, -2.084020599724406786, -8.691656652584148546 ) ) ;
#28562=CARTESIAN_POINT ( 'NONE',  ( 115.6893214775786447, -9.859900752359374465, -12.68260735090039404 ) ) ;
#28566=CARTESIAN_POINT ( 'NONE',  ( 116.0296814775786345, -1.833838273342658809, -17.42832698103878286 ) ) ;
#28569=CARTESIAN_POINT ( 'NONE',  ( 112.1155414775786454, 0.9020085738987339008, -11.91225656197089222 ) ) ;
#28574=ORIENTED_EDGE ( 'NONE', *, *, #33669, .T. ) ;
#28575=CARTESIAN_POINT ( 'NONE',  ( 116.9373081442452929, -1.833838273342659253, -17.42832698103878286 ) ) ;
#28577=CARTESIAN_POINT ( 'NONE',  ( 118.5256548109119876, -8.899110576539710493, -16.42337572283490132 ) ) ;
#28584=CARTESIAN_POINT ( 'NONE',  ( 111.7751814775786556, -7.893985811506177619, -18.51759400769804742 ) ) ;
#28585=CARTESIAN_POINT ( 'NONE',  ( 111.9453614775786434, -1.561330072975668060, -17.79121239304076596 ) ) ;
#28586=CARTESIAN_POINT ( 'NONE',  ( 116.2565881442453133, -0.8288870151387760510, -10.36305467784173118 ) ) ;
#28587=DIRECTION ( 'NONE',  ( 1.000000000000000000, 0.000000000000000000, 0.000000000000000000 ) ) ;
#28588=VERTEX_POINT ( 'NONE', #24298 ) ;
#28589=CARTESIAN_POINT ( 'NONE',  ( 114.6682414775786469, -7.894159318335828068, -9.358103419637847864 ) ) ;
#28593=CARTESIAN_POINT ( 'NONE',  ( 115.6325948109119821, 0.2603800115204892296, -16.42320221600525088 ) ) ;
#28594=EDGE_LOOP ( 'NONE', ( #34590, #26541, #23800, #25195, #39496 ) ) ;
#28595=CARTESIAN_POINT ( 'NONE',  ( 116.6536748109119941, 0.9020085738987339008, -11.91225656197089222 ) ) ;
#28596=CARTESIAN_POINT ( 'NONE',  ( 114.3846081442453197, -10.63000616557721756, -14.87417383870574206 ) ) ;
#28598=CARTESIAN_POINT ( 'NONE',  ( 116.2565881442452991, -9.261995988541697145, -16.69588392320189030 ) ) ;
#28599=CARTESIAN_POINT ( 'NONE',  ( 112.6260814775786514, -9.261995988541697145, -16.69588392320189030 ) ) ;
#28601=CARTESIAN_POINT ( 'NONE',  ( 127.9806007748621255, -10.70395921878446011, -14.08905720169468978 ) ) ;
#28608=CARTESIAN_POINT ( 'NONE',  ( 115.4056881442453459, -2.084020599724406786, -8.691656652584148546 ) ) ;
#28609=LINE ( 'NONE', #38615, #18288 ) ;
#28612=CARTESIAN_POINT ( 'NONE',  ( 121.9093097909088215, -1.016270020561755860, -17.26805140881366896 ) ) ;
#28613=CARTESIAN_POINT ( 'NONE',  ( 113.8740681442453138, -9.859900752359374465, -12.68260735090039404 ) ) ;
#28615=CARTESIAN_POINT ( 'NONE',  ( 122.8936081442453059, 0.2603800115204892296, -16.42320221600525088 ) ) ;
#28616=CARTESIAN_POINT ( 'NONE',  ( 119.2063748109119814, -1.561330072975668504, -17.79121239304076951 ) ) ;
#28618=CARTESIAN_POINT ( 'NONE',  ( 116.7104014775786425, -8.899110576539710493, -16.42337572283490132 ) ) ;
#28619=CARTESIAN_POINT ( 'NONE',  ( 112.7395348109119766, -5.638512984488999180, -18.83840828888717311 ) ) ;
#28620=CARTESIAN_POINT ( 'NONE',  ( 117.8449348109119938, -8.166667518702817929, -8.995218007635861213 ) ) ;
#28621=CARTESIAN_POINT ( 'NONE',  ( 120.1140014775786398, -7.894159318335828068, -9.358103419637847864 ) ) ;
#28623=CARTESIAN_POINT ( 'NONE',  ( 120.3409081442453044, -8.899110576539710493, -16.42337572283490132 ) ) ;
#28624=AXIS2_PLACEMENT_3D ( 'NONE', #26921, #9368, #26023 ) ;
#28625=CARTESIAN_POINT ( 'NONE',  ( 120.6812681442452941, -10.30919188438810075, -12.61870101168855918 ) ) ;
#28626=CARTESIAN_POINT ( 'NONE',  ( 136.4689272580744444, 0.8652765085456386451, -12.77968882490968561 ) ) ;
#28633=CARTESIAN_POINT ( 'NONE',  ( 115.5191414775786569, -3.383040157471821630, -19.15922257007629170 ) ) ;
#28634=CARTESIAN_POINT ( 'NONE',  ( 137.0105207745574774, -10.31073456892766593, -13.75249372251127689 ) ) ;
#28635=CARTESIAN_POINT ( 'NONE',  ( 115.5191414775786569, -6.222761293078241884, -8.102969835052219238 ) ) ;
#28639=CARTESIAN_POINT ( 'NONE',  ( 113.0798948109119948, -8.899110576539710493, -16.42337572283490132 ) ) ;
#28644=CARTESIAN_POINT ( 'NONE',  ( 120.1140014775786398, -1.561330072975668504, -17.79121239304076951 ) ) ;
#28645=CARTESIAN_POINT ( 'NONE',  ( 119.4900081442453086, -7.643976991954077427, -18.09477374809248928 ) ) ;
#28646=CARTESIAN_POINT ( 'NONE',  ( 125.7299414775786346, 0.9020085738987339008, -11.91225656197089222 ) ) ;
#28648=CARTESIAN_POINT ( 'NONE',  ( 136.3568202015625275, -7.080281580350018089, -8.023828915629925618 ) ) ;
#28649=CARTESIAN_POINT ( 'NONE',  ( 124.3117748109119844, -10.30919188438810075, -12.61870101168855918 ) ) ;
#28651=CARTESIAN_POINT ( 'NONE',  ( 117.6747548109119919, -7.643976991954077427, -18.09477374809248928 ) ) ;
#28653=CARTESIAN_POINT ( 'NONE',  ( 117.9583881442453048, 0.1319031606808879209, -14.10382304977623669 ) ) ;
#28656=CARTESIAN_POINT ( 'NONE',  ( 119.9438214775786378, -2.084020599724406786, -8.691656652584148546 ) ) ;
#28658=CARTESIAN_POINT ( 'NONE',  ( 124.1983214775786166, -1.833838273342659697, -17.42832698103878286 ) ) ;
#28663=EDGE_CURVE ( 'NONE', #12393, #3515, #21728, .T. ) ;
#28665=CARTESIAN_POINT ( 'NONE',  ( 118.9227414775786400, -10.63000616557722466, -14.87417383870573495 ) ) ;
#28666=CARTESIAN_POINT ( 'NONE',  ( 119.3765548109119834, 0.9020085738987339008, -11.91225656197089222 ) ) ;
#28668=CARTESIAN_POINT ( 'NONE',  ( 112.3991748109119868, -8.166667518702817929, -8.995218007635859436 ) ) ;
#28672=DIRECTION ( 'NONE',  ( 1.000000000000000000, 0.000000000000000000, 0.000000000000000000 ) ) ;
#28674=CARTESIAN_POINT ( 'NONE',  ( 116.8805814775786445, -6.344957434206662583, -7.627207830600332805 ) ) ;
#28675=CARTESIAN_POINT ( 'NONE',  ( 122.2696148109119889, -5.574606645277164318, -18.38911715685844683 ) ) ;
#28677=CARTESIAN_POINT ( 'NONE',  ( 126.0135748109119902, -8.166667518702819706, -8.995218007635861213 ) ) ;
#28678=CARTESIAN_POINT ( 'NONE',  ( 121.3619881442452879, -4.089484607189486809, -7.948022111789456723 ) ) ;
#28680=B_SPLINE_CURVE_WITH_KNOTS ( 'NONE', 3,
 ( #40029, #1493, #39808, #12227, #8574, #39587, #40492, #25680, #15415, #8793 ),
 .UNSPECIFIED., .F., .F.,
 ( 4, 3, 3, 4 ),
 ( 0.000000000000000000, 0.0001671877560958085049, 0.0003343755126086549959, 0.0006438490228505480001 ),
 .UNSPECIFIED. ) ;
#28681=CARTESIAN_POINT ( 'NONE',  ( 116.4267681442453153, -6.222761293078241884, -8.102969835052219238 ) ) ;
#28687=CARTESIAN_POINT ( 'NONE',  ( 119.3765548109119834, 0.9020085738987339008, -11.91225656197089222 ) ) ;
#28691=CARTESIAN_POINT ( 'NONE',  ( 122.3263414775786373, -6.344957434206689229, -7.627207830600343463 ) ) ;
#28692=CARTESIAN_POINT ( 'NONE',  ( 115.4624148109119943, -4.153390946401321671, -8.397313243818183892 ) ) ;
#28695=CARTESIAN_POINT ( 'NONE',  ( 118.6958348109119754, -3.505236298600246325, -18.68346056562440793 ) ) ;
#28696=CARTESIAN_POINT ( 'NONE',  ( 121.8158014775786171, -5.638512984488987634, -18.83840828888717311 ) ) ;
#28697=CARTESIAN_POINT ( 'NONE',  ( 120.0005481442453146, -4.153390946401325223, -8.397313243818185668 ) ) ;
#28700=CARTESIAN_POINT ( 'NONE',  ( 119.3198281442452924, -9.859900752359374465, -12.68260735090039404 ) ) ;
#28701=CARTESIAN_POINT ( 'NONE',  ( 113.2500748109119968, -6.344957434206662583, -7.627207830600332805 ) ) ;
#28702=CARTESIAN_POINT ( 'NONE',  ( 120.3976348109119812, -1.834011780172310813, -8.268836392978581529 ) ) ;
#28703=CARTESIAN_POINT ( 'NONE',  ( 111.7751814775786556, -7.893985811506177619, -18.51759400769804742 ) ) ;
#28705=CARTESIAN_POINT ( 'NONE',  ( 119.7736414775786358, 0.1319031606808879209, -14.10382304977623669 ) ) ;
#28706=ORIENTED_EDGE ( 'NONE', *, *, #11278, .F. ) ;
#28707=CARTESIAN_POINT ( 'NONE',  ( 119.7169148109119874, -9.988377603198976828, -10.36322818467138340 ) ) ;
#28715=CARTESIAN_POINT ( 'NONE',  ( 123.4041481442452834, 0.1319031606808879209, -14.10382304977623669 ) ) ;
#28719=CARTESIAN_POINT ( 'NONE',  ( 111.5138235035216780, -0.1451374939625849625, -15.72356508888860738 ) ) ;
#28722=CARTESIAN_POINT ( 'NONE',  ( 115.1787814775786387, -9.988377603198976828, -10.36322818467138340 ) ) ;
#28723=CARTESIAN_POINT ( 'NONE',  ( 114.3278814775786429, -10.30919188438810075, -12.61870101168855918 ) ) ;
#28725=CARTESIAN_POINT ( 'NONE',  ( 119.6034614775786196, -3.505236298600246325, -18.68346056562440793 ) ) ;
#28726=CARTESIAN_POINT ( 'NONE',  ( 126.3999550322235308, -3.647810012370235722, -8.449820221509870777 ) ) ;
#28727=CARTESIAN_POINT ( 'NONE',  ( 122.3830681442452857, -8.166667518702819706, -8.995218007635861213 ) ) ;
#28728=CARTESIAN_POINT ( 'NONE',  ( 123.9714148109119805, -8.899110576539726480, -16.42337572283488001 ) ) ;
#28732=CARTESIAN_POINT ( 'NONE',  ( 112.6260814775786514, -9.261995988541697145, -16.69588392320189030 ) ) ;
#28735=CARTESIAN_POINT ( 'NONE',  ( 121.4187148109119789, -6.344957434206665248, -7.627207830600338134 ) ) ;
#28738=FACE_OUTER_BOUND ( 'NONE', #28594, .T. ) ;
#28739=CARTESIAN_POINT ( 'NONE',  ( 126.2404814775786264, -9.261995988541697145, -16.69588392320189030 ) ) ;
#28741=CARTESIAN_POINT ( 'NONE',  ( 122.1561614775786353, -8.899110576539710493, -16.42337572283490132 ) ) ;
#28744=CARTESIAN_POINT ( 'NONE',  ( 119.0929214775786278, -5.638512984488999180, -18.83840828888717311 ) ) ;
#28747=CARTESIAN_POINT ( 'NONE',  ( 137.1799701741848025, -5.066786549864910505, -8.072398738317787092 ) ) ;
#28748=CARTESIAN_POINT ( 'NONE',  ( 124.0281414775786146, -1.834011780172310813, -8.268836392978581529 ) ) ;
#28751=CARTESIAN_POINT ( 'NONE',  ( 123.5176014775786228, -9.261995988541697145, -16.69588392320189030 ) ) ;
#28752=CARTESIAN_POINT ( 'NONE',  ( 124.2550481442452792, -9.988377603198980381, -10.36322818467138518 ) ) ;
#28753=CARTESIAN_POINT ( 'NONE',  ( 123.1772414775786189, -5.574606645277164318, -18.38911715685844683 ) ) ;
#28755=CARTESIAN_POINT ( 'NONE',  ( 123.1772414775786189, -5.574606645277164318, -18.38911715685844683 ) ) ;
#28757=CARTESIAN_POINT ( 'NONE',  ( 120.2841814775786276, 0.9020085738987339008, -11.91225656197089222 ) ) ;
#28764=CARTESIAN_POINT ( 'NONE',  ( 125.3328548109119964, -0.8288870151393684660, -10.36305467784094247 ) ) ;
#28765=CARTESIAN_POINT ( 'NONE',  ( 116.9373081442452929, -8.166667518702817929, -8.995218007635861213 ) ) ;
#28767=CARTESIAN_POINT ( 'NONE',  ( 112.0020881442453344, -9.565557343593413364, -10.61323700422348004 ) ) ;
#28769=CARTESIAN_POINT ( 'NONE',  ( 122.0994348109119585, -10.15424416112534978, -14.75197769757730093 ) ) ;
#28773=CARTESIAN_POINT ( 'NONE',  ( 116.1998614775786507, -10.63000616557722466, -14.87417383870573495 ) ) ;
#28777=EDGE_LOOP ( 'NONE', ( #42942, #17410, #29674, #31720 ) ) ;
#28778=CARTESIAN_POINT ( 'NONE',  ( 126.2940345447956503, -7.620160344469310232, -9.176220693874684642 ) ) ;
#28779=CARTESIAN_POINT ( 'NONE',  ( 117.4478481442453131, -9.565557343593413364, -10.61323700422348004 ) ) ;
#28780=CARTESIAN_POINT ( 'NONE',  ( 114.5547881442453217, -5.638512984488999180, -18.83840828888717311 ) ) ;
#28781=EDGE_CURVE ( 'NONE', #40512, #32536, #29358, .T. ) ;
#28783=CARTESIAN_POINT ( 'NONE',  ( 124.9924948109119924, -5.574606645277164318, -18.38911715685844683 ) ) ;
#28784=UNCERTAINTY_MEASURE_WITH_UNIT (LENGTH_MEASURE( 1.000000000000000082E-05 ), #24795, 'distance_accuracy_value', 'NONE');
#28785=CARTESIAN_POINT ( 'NONE',  ( 120.3976348109119812, -7.643976991954077427, -18.09477374809248928 ) ) ;
#28786=CARTESIAN_POINT ( 'NONE',  ( 117.5045748109119756, -9.859900752359374465, -12.68260735090039404 ) ) ;
#28791=CARTESIAN_POINT ( 'NONE',  ( 118.4122014775786340, -9.859900752359374465, -12.68260735090039404 ) ) ;
#28794=CARTESIAN_POINT ( 'NONE',  ( 114.3278814775786429, -10.30919188438810075, -12.61870101168855918 ) ) ;
#28796=CARTESIAN_POINT ( 'NONE',  ( 125.7866681442452688, -8.899110576539710493, -16.42337572283490132 ) ) ;
#28799=CARTESIAN_POINT ( 'NONE',  ( 124.0281414775786146, -7.643976991954077427, -18.09477374809248928 ) ) ;
#28800=CARTESIAN_POINT ( 'NONE',  ( 117.9016614775786280, -0.1624402480850797581, -16.17319339645315424 ) ) ;
#28804=CARTESIAN_POINT ( 'NONE',  ( 151.2860562277021472, -4.863998795839242995, -13.39321520033831447 ) ) ;
#28809=CARTESIAN_POINT ( 'NONE',  ( 125.6732148109119862, -9.859900752359378018, -12.68260735090039759 ) ) ;
#28810=CARTESIAN_POINT ( 'NONE',  ( 122.8368814775786291, -7.894159318335828068, -9.358103419637847864 ) ) ;
#28814=CARTESIAN_POINT ( 'NONE',  ( 121.1350814775786233, -9.859900752359378018, -12.68260735090039759 ) ) ;
#28818=CARTESIAN_POINT ( 'NONE',  ( 115.4056881442453459, -7.893985811506177619, -18.51759400769804742 ) ) ;
#28820=CARTESIAN_POINT ( 'NONE',  ( 117.1074881442453233, -10.63000616557722466, -14.87417383870573495 ) ) ;
#28823=CARTESIAN_POINT ( 'NONE',  ( 116.4267681442453153, -3.383040157471821630, -19.15922257007629170 ) ) ;
#28824=CARTESIAN_POINT ( 'NONE',  ( 118.0151148109119816, -10.63000616557722466, -14.87417383870573495 ) ) ;
#28825=CARTESIAN_POINT ( 'NONE',  ( 125.4463081442452932, -4.153390946401325223, -8.397313243818185668 ) ) ;
#28831=CARTESIAN_POINT ( 'NONE',  ( 120.6812681442452941, 0.1319031606808879209, -14.10382304977623669 ) ) ;
#28837=CARTESIAN_POINT ( 'NONE',  ( 113.9875214775786532, -8.899110576539710493, -16.42337572283490132 ) ) ;
#28838=CARTESIAN_POINT ( 'NONE',  ( 110.2184548109119788, -4.863998795839242995, -13.39321520033831447 ) ) ;
#28839=CARTESIAN_POINT ( 'NONE',  ( 122.6667014775786413, -7.893985811506177619, -18.51759400769804742 ) ) ;
#28840=CARTESIAN_POINT ( 'NONE',  ( 120.5110881442453206, -6.344957434206665248, -7.627207830600338134 ) ) ;
#28842=CARTESIAN_POINT ( 'NONE',  ( 119.7736414775786358, 0.1319031606808879209, -14.10382304977623669 ) ) ;
#28843=CARTESIAN_POINT ( 'NONE',  ( 111.7184548109119788, -9.261995988541697145, -16.69588392320189030 ) ) ;
#28844=CARTESIAN_POINT ( 'NONE',  ( 116.7671281442453335, -1.834011780172310813, -8.268836392978581529 ) ) ;
#28845=CARTESIAN_POINT ( 'NONE',  ( 120.6812681442452941, 0.1319031606808879209, -14.10382304977623669 ) ) ;
#28847=CARTESIAN_POINT ( 'NONE',  ( 116.4635497909088429, -1.016270020561755860, -17.26805140881366896 ) ) ;
#28848=AXIS2_PLACEMENT_3D ( 'NONE', #35899, #3990, #31587 ) ;
#28849=CARTESIAN_POINT ( 'NONE',  ( 119.7736414775786358, -10.30919188438810075, -12.61870101168855918 ) ) ;
#28850=CARTESIAN_POINT ( 'NONE',  ( 136.8967026949522676, 0.6524655654276926287, -12.96421432964295128 ) ) ;
#28855=CARTESIAN_POINT ( 'NONE',  ( 117.9583881442453048, -10.30919188438810075, -12.61870101168855918 ) ) ;
#28857=CARTESIAN_POINT ( 'NONE',  ( 112.3781902440515665, -2.467220198592768199, -17.83387418641523325 ) ) ;
#28858=CARTESIAN_POINT ( 'NONE',  ( 115.6325948109119821, -9.565557343593413364, -10.61323700422348004 ) ) ;
#28859=CARTESIAN_POINT ( 'NONE',  ( 126.2471382750653390, -0.7355600668381890861, -10.54709472444621099 ) ) ;
#28860=CARTESIAN_POINT ( 'NONE',  ( 117.6180281442453150, -8.899110576539721151, -16.42337572283488711 ) ) ;
#28862=CARTESIAN_POINT ( 'NONE',  ( 113.6471614775786492, -4.153390946401321671, -8.397313243818183892 ) ) ;
#28867=CARTESIAN_POINT ( 'NONE',  ( 118.0718414775786300, -9.261995988541697145, -16.69588392320189030 ) ) ;
#28868=CARTESIAN_POINT ( 'NONE',  ( 119.7736414775786358, 0.1319031606808879209, -14.10382304977623669 ) ) ;
#28869=CARTESIAN_POINT ( 'NONE',  ( 114.3278814775786429, 0.1319031606808879209, -14.10382304977623669 ) ) ;
#28871=CARTESIAN_POINT ( 'NONE',  ( 135.5886503745772984, -7.067465569328434505, -7.812523301970706768 ) ) ;
#28872=CARTESIAN_POINT ( 'NONE',  ( 122.3830681442452857, -8.166667518702819706, -8.995218007635861213 ) ) ;
#28874=CARTESIAN_POINT ( 'NONE',  ( 118.6391081442452986, -5.574606645277164318, -18.38911715685844683 ) ) ;
#28876=CARTESIAN_POINT ( 'NONE',  ( 117.5613014775786525, -10.15424416112533912, -14.75197769757731336 ) ) ;
#28879=CARTESIAN_POINT ( 'NONE',  ( 123.4608748109119745, 0.4262465694468514643, -12.03445270309931736 ) ) ;
#28880=CARTESIAN_POINT ( 'NONE',  ( 122.6099748109119929, -0.8288870151387760510, -10.36305467784173118 ) ) ;
#28881=CARTESIAN_POINT ( 'NONE',  ( 115.0086014775786509, -5.574606645277172312, -18.38911715685844683 ) ) ;
#28888=CARTESIAN_POINT ( 'NONE',  ( 116.8805814775786445, -6.344957434206662583, -7.627207830600332805 ) ) ;
#28889=CARTESIAN_POINT ( 'NONE',  ( 120.0572748109119772, -3.383040157471821630, -19.15922257007629170 ) ) ;
#28891=CARTESIAN_POINT ( 'NONE',  ( 111.8319081442453182, -5.638512984488999180, -18.83840828888717311 ) ) ;
#28893=CARTESIAN_POINT ( 'NONE',  ( 112.8721930757767495, -0.9924539043446216624, -17.29976612834909133 ) ) ;
#28894=CARTESIAN_POINT ( 'NONE',  ( 117.4478481442453131, 0.2603800115204892296, -16.42320221600525088 ) ) ;
#28895=CARTESIAN_POINT ( 'NONE',  ( 123.6877814775786533, -6.222761293078241884, -8.102969835052219238 ) ) ;
#28898=CARTESIAN_POINT ( 'NONE',  ( 123.8579614775786126, 0.5811942927096110934, -14.16772938898807510 ) ) ;
#28899=CARTESIAN_POINT ( 'NONE',  ( 122.0994348109119443, 0.9020085738987339008, -11.91225656197089222 ) ) ;
#28902=CARTESIAN_POINT ( 'NONE',  ( 117.7314814775786260, -5.574606645277164318, -18.38911715685844683 ) ) ;
#28908=CARTESIAN_POINT ( 'NONE',  ( 120.7947214775786193, -9.261995988541697145, -16.69588392320189030 ) ) ;
#28909=ORIENTED_EDGE ( 'NONE', *, *, #798, .T. ) ;
#28910=CARTESIAN_POINT ( 'NONE',  ( 124.9252281442453096, -8.862178061932084461, -16.39564131203287545 ) ) ;
#28913=CARTESIAN_POINT ( 'NONE',  ( 115.0653281442453277, -3.505236298600246325, -18.68346056562440793 ) ) ;
#28916=CARTESIAN_POINT ( 'NONE',  ( 123.0637881442452937, -8.899110576539710493, -16.42337572283490132 ) ) ;
#28917=EDGE_CURVE ( 'NONE', #2648, #28126, #1039, .T. ) ;
#28920=CARTESIAN_POINT ( 'NONE',  ( 123.0637881442452937, -8.899110576539710493, -16.42337572283490132 ) ) ;
#28923=CARTESIAN_POINT ( 'NONE',  ( 124.4252281442452812, -0.8288870151387760510, -10.36305467784173118 ) ) ;
#28924=CARTESIAN_POINT ( 'NONE',  ( 112.9097148109120070, 0.2603800115204892296, -16.42320221600525088 ) ) ;
#28925=CARTESIAN_POINT ( 'NONE',  ( 120.0005481442453146, -5.638512984488999180, -18.83840828888717311 ) ) ;
#28926=CARTESIAN_POINT ( 'NONE',  ( 113.4769814775786330, -10.63000616557722466, -14.87417383870573495 ) ) ;
#28928=CARTESIAN_POINT ( 'NONE',  ( 121.1350814775786233, -9.859900752359378018, -12.68260735090039759 ) ) ;
#28930=CARTESIAN_POINT ( 'NONE',  ( 121.2485348109119769, -0.4660016031367893996, -10.09054647747474043 ) ) ;
#28934=CARTESIAN_POINT ( 'NONE',  ( 138.2184548109120499, -3.542396227776595019, -16.40211655196756979 ) ) ;
#28937=CARTESIAN_POINT ( 'NONE',  ( 122.7234281442452755, -4.153390946401325223, -8.397313243818185668 ) ) ;
#28945=CARTESIAN_POINT ( 'NONE',  ( 115.9729548109119861, -6.344957434206662583, -7.627207830600332805 ) ) ;
#28947=CARTESIAN_POINT ( 'NONE',  ( 120.2274548109119934, -9.859900752359374465, -12.68260735090039404 ) ) ;
#28948=FACE_OUTER_BOUND ( 'NONE', #13649, .T. ) ;
#28955=EDGE_CURVE ( 'NONE', #19203, #29206, #26589, .T. ) ;
#28958=CARTESIAN_POINT ( 'NONE',  ( 122.0427081442452817, 0.5811942927096110934, -14.16772938898807510 ) ) ;
#28959=CARTESIAN_POINT ( 'NONE',  ( 136.9394333025971093, -9.868690179724596945, -15.68633195852948248 ) ) ;
#28960=ORIENTED_EDGE ( 'NONE', *, *, #1177, .F. ) ;
#28961=CARTESIAN_POINT ( 'NONE',  ( 112.2857214775786474, -4.089484607189486809, -7.948022111789456723 ) ) ;
#28962=CARTESIAN_POINT ( 'NONE',  ( 111.4915481442453142, -1.833838273342658365, -17.42832698103878286 ) ) ;
#28965=CARTESIAN_POINT ( 'NONE',  ( 121.9292548109119849, -7.894159318335828068, -9.358103419637847864 ) ) ;
#28967=CARTESIAN_POINT ( 'NONE',  ( 119.2631014775786298, 0.2603800115204892296, -16.42320221600525088 ) ) ;
#28969=ADVANCED_FACE ( 'NONE', ( #40271 ), #11708, .F. ) ;
#28973=CARTESIAN_POINT ( 'NONE',  ( 137.4945747550012811, -3.899949230086460883, -8.466937502284467953 ) ) ;
#28974=CARTESIAN_POINT ( 'NONE',  ( 112.1722681442453222, -8.899110576539710493, -16.42337572283490132 ) ) ;
#28977=CARTESIAN_POINT ( 'NONE',  ( 112.6828081442453282, -2.084020599724406786, -8.691656652584148546 ) ) ;
#28978=CARTESIAN_POINT ( 'NONE',  ( 112.1722681442453222, -0.4660016031367893996, -10.09054647747474043 ) ) ;
#28980=CARTESIAN_POINT ( 'NONE',  ( 125.1059481442452750, -1.833838273342660141, -17.42832698103878286 ) ) ;
#28981=CARTESIAN_POINT ( 'NONE',  ( 121.4187148109119789, -6.344957434206665248, -7.627207830600338134 ) ) ;
#28983=CARTESIAN_POINT ( 'NONE',  ( 126.5561942423968844, -8.545838888952497214, -17.02113326143807726 ) ) ;
#28987=CARTESIAN_POINT ( 'NONE',  ( 126.9932531981154966, -9.953270824051303478, -11.62590261691779858 ) ) ;
#28988=CARTESIAN_POINT ( 'NONE',  ( 115.5758681442453053, -1.561330072975668060, -17.79121239304076951 ) ) ;
#28990=CARTESIAN_POINT ( 'NONE',  ( 113.0798948109119948, -8.899110576539710493, -16.42337572283490132 ) ) ;
#28996=CARTESIAN_POINT ( 'NONE',  ( 114.9518748109119883, -1.834011780172310813, -8.268836392978581529 ) ) ;
#29001=CARTESIAN_POINT ( 'NONE',  ( 120.6812681442452941, 0.1319031606808879209, -14.10382304977623669 ) ) ;
#29002=CARTESIAN_POINT ( 'NONE',  ( 117.2209414775786485, -7.893985811506177619, -18.51759400769804742 ) ) ;
#29003=CARTESIAN_POINT ( 'NONE',  ( 111.8886348109120092, -3.383040157471821630, -19.15922257007629170 ) ) ;
#29004=CARTESIAN_POINT ( 'NONE',  ( 123.5176014775786228, -0.8288870151387760510, -10.36305467784173118 ) ) ;
#29005=CARTESIAN_POINT ( 'NONE',  ( 124.7088614775786226, -9.565557343593413364, -10.61323700422348004 ) ) ;
#29006=CARTESIAN_POINT ( 'NONE',  ( 114.6682414775786469, -7.894159318335828068, -9.358103419637847864 ) ) ;
#29010=CARTESIAN_POINT ( 'NONE',  ( 118.5823814775786360, -7.643976991954077427, -18.09477374809248928 ) ) ;
#29012=FACE_OUTER_BOUND ( 'NONE', #37926, .T. ) ;
#29013=EDGE_CURVE ( 'NONE', #21529, #15102, #13811, .T. ) ;
#29014=CARTESIAN_POINT ( 'NONE',  ( 116.4267681442453153, -3.383040157471821630, -19.15922257007629170 ) ) ;
#29016=CARTESIAN_POINT ( 'NONE',  ( 125.5030348109119558, -6.222761293078241884, -8.102969835052219238 ) ) ;
#29017=ORIENTED_EDGE ( 'NONE', *, *, #30672, .T. ) ;
#29019=CARTESIAN_POINT ( 'NONE',  ( 122.9503348109119827, -9.859900752359378018, -12.68260735090039759 ) ) ;
#29020=CARTESIAN_POINT ( 'NONE',  ( 115.8595014775786609, -7.643976991954077427, -18.09477374809248928 ) ) ;
#29024=CARTESIAN_POINT ( 'NONE',  ( 112.1719155697224295, -8.904739562214000870, -16.41571553851813547 ) ) ;
#29027=CARTESIAN_POINT ( 'NONE',  ( 112.2857214775786474, -4.089484607189486809, -7.948022111789456723 ) ) ;
#29028=CARTESIAN_POINT ( 'NONE',  ( 126.5808414775786446, -9.859900752359378018, -12.68260735090039759 ) ) ;
#29030=CARTESIAN_POINT ( 'NONE',  ( 121.8158014775786171, -4.153390946401325223, -8.397313243818185668 ) ) ;
#29033=CARTESIAN_POINT ( 'NONE',  ( 119.6034614775786196, -3.505236298600246325, -18.68346056562440793 ) ) ;
#29035=CARTESIAN_POINT ( 'NONE',  ( 114.2354127111058659, -1.267766418764742165, -16.93314635290707315 ) ) ;
#29037=CARTESIAN_POINT ( 'NONE',  ( 117.3343948109119737, -3.383040157471821630, -19.15922257007629170 ) ) ;
#29039=CARTESIAN_POINT ( 'NONE',  ( 116.4267681442453153, -3.383040157471821630, -19.15922257007629170 ) ) ;
#29042=CARTESIAN_POINT ( 'NONE',  ( 117.2209414775786485, -7.893985811506177619, -18.51759400769804742 ) ) ;
#29043=CARTESIAN_POINT ( 'NONE',  ( 118.6391081442452986, -4.089484607189486809, -7.948022111789456723 ) ) ;
#29044=CARTESIAN_POINT ( 'NONE',  ( 125.6164881442453094, -9.565557343593413364, -10.61323700422348004 ) ) ;
#29048=CARTESIAN_POINT ( 'NONE',  ( 112.2334103192116999, -2.378957183258581853, -17.95140958770220152 ) ) ;
#29050=CARTESIAN_POINT ( 'NONE',  ( 119.8870948109119752, -0.8288870151387760510, -10.36305467784173118 ) ) ;
#29051=AXIS2_PLACEMENT_3D ( 'NONE', #25016, #28672, #3590 ) ;
#29054=CARTESIAN_POINT ( 'NONE',  ( 113.0231681442453180, -10.15424416112533912, -14.75197769757731336 ) ) ;
#29056=CARTESIAN_POINT ( 'NONE',  ( 124.4252281442452812, -9.261995988541697145, -16.69588392320189030 ) ) ;
#29057=CARTESIAN_POINT ( 'NONE',  ( 121.2485348109119769, -0.4660016031367893996, -10.09054647747474043 ) ) ;
#29059=CARTESIAN_POINT ( 'NONE',  ( 119.2063748109119814, -7.894159318335828068, -9.358103419637847864 ) ) ;
#29060=CARTESIAN_POINT ( 'NONE',  ( 111.9453614775786434, -1.561330072975668060, -17.79121239304076596 ) ) ;
#29061=CARTESIAN_POINT ( 'NONE',  ( 122.7234281442452755, -5.638512984488999180, -18.83840828888717311 ) ) ;
#29062=CARTESIAN_POINT ( 'NONE',  ( 119.6601881442453106, -1.833838273342659253, -17.42832698103878286 ) ) ;
#29064=CARTESIAN_POINT ( 'NONE',  ( 124.8223148109119762, -10.15424416112533912, -14.75197769757731336 ) ) ;
#29065=CARTESIAN_POINT ( 'NONE',  ( 119.4900081442453086, -1.834011780172310813, -8.268836392978581529 ) ) ;
#29068=CARTESIAN_POINT ( 'NONE',  ( 126.2184548109119504, 0.09929810886256085212, -14.00506970868240231 ) ) ;
#29070=CARTESIAN_POINT ( 'NONE',  ( 117.1074881442453233, -10.63000616557722466, -14.87417383870573495 ) ) ;
#29073=CARTESIAN_POINT ( 'NONE',  ( 137.3527759848280141, -9.837515720139910158, -11.99256683774707177 ) ) ;
#29074=CARTESIAN_POINT ( 'NONE',  ( 116.0864081442453113, -0.1624402480850797581, -16.17319339645315424 ) ) ;
#29075=CARTESIAN_POINT ( 'NONE',  ( 111.6617281442453304, 0.4262465694468514643, -12.03445270309931736 ) ) ;
#29076=CARTESIAN_POINT ( 'NONE',  ( 126.3230600034097364, -0.6023121577465754273, -10.67916527035535168 ) ) ;
#29078=CARTESIAN_POINT ( 'NONE',  ( 113.4202548109119846, 0.1319031606808879209, -14.10382304977623669 ) ) ;
#29079=CARTESIAN_POINT ( 'NONE',  ( 114.9466624678160969, -1.149058757900091265, -17.09122335155388939 ) ) ;
#29082=CARTESIAN_POINT ( 'NONE',  ( 119.1496481442453046, -3.383040157471821630, -19.15922257007629170 ) ) ;
#29083=CARTESIAN_POINT ( 'NONE',  ( 124.3685014775786328, 0.4262465694468514643, -12.03445270309931736 ) ) ;
#29085=CARTESIAN_POINT ( 'NONE',  ( 137.0596819398186028, -7.194705560345089346, -8.499707714596844710 ) ) ;
#29088=CARTESIAN_POINT ( 'NONE',  ( 120.7947214775786193, -0.8288870151387760510, -10.36305467784173118 ) ) ;
#29089=( BOUNDED_CURVE ( )  B_SPLINE_CURVE ( 2, ( #9791, #34814, #31195, #403, #2932 ),
 .UNSPECIFIED., .F., .T. ) 
 B_SPLINE_CURVE_WITH_KNOTS ( ( 3, 2, 3 ),
 ( 0.8750000000000000000, 0.8828125000000000000, 0.8891217583431300087 ),
 .UNSPECIFIED. ) 
 CURVE ( )  GEOMETRIC_REPRESENTATION_ITEM ( )  RATIONAL_B_SPLINE_CURVE ( ( 0.9999999999999800160, 0.9238795325113059453, 1.000000000000000000, 0.9385262470929799372, 0.9763430640194590282 ) ) 
 REPRESENTATION_ITEM ( '' )  );
#29090=CARTESIAN_POINT ( 'NONE',  ( 121.1918081442452859, -10.15424416112533912, -14.75197769757731336 ) ) ;
#29091=CARTESIAN_POINT ( 'NONE',  ( 115.9162281442453093, -5.574606645277164318, -18.38911715685844683 ) ) ;
#29094=CARTESIAN_POINT ( 'NONE',  ( 124.1983214775786166, -1.833838273342659697, -17.42832698103878286 ) ) ;
#29095=CARTESIAN_POINT ( 'NONE',  ( 123.8012348109119642, -9.565557343593413364, -10.61323700422348004 ) ) ;
#29098=EDGE_CURVE ( 'NONE', #18562, #39160, #34317, .T. ) ;
#29103=CARTESIAN_POINT ( 'NONE',  ( 117.9583881442453048, -10.30919188438810075, -12.61870101168855918 ) ) ;
#29104=CARTESIAN_POINT ( 'NONE',  ( 119.8870948109119752, -9.261995988541697145, -16.69588392320189030 ) ) ;
#29106=CARTESIAN_POINT ( 'NONE',  ( 113.7038881442453402, -3.383040157471821630, -19.15922257007629170 ) ) ;
#29110=CARTESIAN_POINT ( 'NONE',  ( 116.7671281442453335, -1.834011780172310813, -8.268836392978581529 ) ) ;
#29112=CARTESIAN_POINT ( 'NONE',  ( 124.5954081442453116, -6.222761293078241884, -8.102969835052219238 ) ) ;
#29114=CARTESIAN_POINT ( 'NONE',  ( 113.8173414775786512, -9.565557343593413364, -10.61323700422348004 ) ) ;
#29115=CARTESIAN_POINT ( 'NONE',  ( 120.9081748109119872, -5.638512984488999180, -18.83840828888717311 ) ) ;
#29118=CARTESIAN_POINT ( 'NONE',  ( 115.7460481442453357, -10.15424416112533912, -14.75197769757731336 ) ) ;
#29124=CARTESIAN_POINT ( 'NONE',  ( 118.4122014775786340, 0.5811942927096110934, -14.16772938898807510 ) ) ;
#29129=CARTESIAN_POINT ( 'NONE',  ( 115.0086014775786509, -5.574606645277164318, -18.38911715685844683 ) ) ;
#29132=CARTESIAN_POINT ( 'NONE',  ( 123.9714148109119805, -8.899110576539710493, -16.42337572283490132 ) ) ;
#29134=CARTESIAN_POINT ( 'NONE',  ( 124.7655881442452852, -9.859900752359378018, -12.68260735090039759 ) ) ;
#29137=CARTESIAN_POINT ( 'NONE',  ( 119.0929214775786278, -4.153390946401325223, -8.397313243818185668 ) ) ;
#29138=CARTESIAN_POINT ( 'NONE',  ( 121.9292548109119849, -7.894159318335828068, -9.358103419637847864 ) ) ;
#29139=CARTESIAN_POINT ( 'NONE',  ( 113.7606148109119886, -1.561330072975668060, -17.79121239304076596 ) ) ;
#29140=CARTESIAN_POINT ( 'NONE',  ( 118.9794681442453026, -9.261995988541697145, -16.69588392320189030 ) ) ;
#29141=CARTESIAN_POINT ( 'NONE',  ( 112.9664414775786412, 0.5811942927096154232, -14.16772938898807155 ) ) ;
#29143=CARTESIAN_POINT ( 'NONE',  ( 122.9503348109119827, -9.859900752359378018, -12.68260735090039759 ) ) ;
#29145=CARTESIAN_POINT ( 'NONE',  ( 119.6601881442453106, -8.166667518702819706, -8.995218007635861213 ) ) ;
#29150=AXIS2_PLACEMENT_3D ( 'NONE', #45126, #6373, #7040 ) ;
#29154=CARTESIAN_POINT ( 'NONE',  ( 122.5532481442453019, 0.4262465694468514643, -12.03445270309931736 ) ) ;
#29159=CARTESIAN_POINT ( 'NONE',  ( 116.3133148109119759, -7.893985811506177619, -18.51759400769804742 ) ) ;
#29161=CARTESIAN_POINT ( 'NONE',  ( 119.0929214775786278, -4.153390946401325223, -8.397313243818185668 ) ) ;
#29163=CARTESIAN_POINT ( 'NONE',  ( 111.2184548109119788, -8.862178061932382889, -16.39564131203247399 ) ) ;
#29170=CARTESIAN_POINT ( 'NONE',  ( 120.9081748109119872, -5.638512984488999180, -18.83840828888717311 ) ) ;
#29173=CARTESIAN_POINT ( 'NONE',  ( 136.2315975805980486, -10.28294944029322444, -15.60456038644257148 ) ) ;
#29174=ORIENTED_EDGE ( 'NONE', *, *, #5828, .T. ) ;
#29175=CARTESIAN_POINT ( 'NONE',  ( 115.0653281442453277, -6.344957434206662583, -7.627207830600332805 ) ) ;
#29176=CARTESIAN_POINT ( 'NONE',  ( 125.9001214775786224, -4.089484607189486809, -7.948022111789456723 ) ) ;
#29178=CARTESIAN_POINT ( 'NONE',  ( 124.3117748109119844, 0.1319031606808879209, -14.10382304977623669 ) ) ;
#29181=CARTESIAN_POINT ( 'NONE',  ( 116.8805814775786445, -6.344957434206662583, -7.627207830600332805 ) ) ;
#29184=CARTESIAN_POINT ( 'NONE',  ( 111.6617281442453162, 0.4262465694468551280, -12.03445270309932269 ) ) ;
#29185=CARTESIAN_POINT ( 'NONE',  ( 137.1399781293984290, -5.107918420449511387, -8.041068576975341387 ) ) ;
#29186=CARTESIAN_POINT ( 'NONE',  ( 113.4769814775786330, 0.4262465694468514643, -12.03445270309931736 ) ) ;
#29188=FACE_OUTER_BOUND ( 'NONE', #16113, .T. ) ;
#29190=CARTESIAN_POINT ( 'NONE',  ( 112.9664414775786412, -9.859900752359374465, -12.68260735090039404 ) ) ;
#29191=CARTESIAN_POINT ( 'NONE',  ( 112.3424481442453384, -6.344957434206662583, -7.627207830600332805 ) ) ;
#29193=CARTESIAN_POINT ( 'NONE',  ( 124.3117748109119844, 0.1319031606808879209, -14.10382304977623669 ) ) ;
#29195=CARTESIAN_POINT ( 'NONE',  ( 118.2420214775786320, -3.383040157471821630, -19.15922257007629170 ) ) ;
#29198=CARTESIAN_POINT ( 'NONE',  ( 126.6211808763750213, -8.526882813983885256, -17.08637904477736669 ) ) ;
#29199=EDGE_CURVE ( 'NONE', #19714, #28588, #25899, .T. ) ;
#29204=CARTESIAN_POINT ( 'NONE',  ( 125.7194014775786286, -9.814174330883794539, -12.68911139247586739 ) ) ;
#29205=CARTESIAN_POINT ( 'NONE',  ( 114.6682414775786469, -1.561330072975668060, -17.79121239304076596 ) ) ;
#29206=VERTEX_POINT ( 'NONE', #35198 ) ;
#29207=CARTESIAN_POINT ( 'NONE',  ( 116.9373081442452929, -1.833838273342659253, -17.42832698103878286 ) ) ;
#29209=LINE ( 'NONE', #43118, #35776 ) ;
#29210=CARTESIAN_POINT ( 'NONE',  ( 125.9568481442452850, -6.344957434206665248, -7.627207830600338134 ) ) ;
#29211=DIRECTION ( 'NONE',  ( -1.000000000000000000, 0.000000000000000000, 0.000000000000000000 ) ) ;
#29212=CARTESIAN_POINT ( 'NONE',  ( 112.1722681442453222, -0.4660016031367893996, -10.09054647747474043 ) ) ;
#29213=CARTESIAN_POINT ( 'NONE',  ( 114.3846081442453197, -10.63000616557722466, -14.87417383870573495 ) ) ;
#29217=CARTESIAN_POINT ( 'NONE',  ( 124.6713397424434078, -0.9924539043446091169, -17.29976612834908423 ) ) ;
#29219=CARTESIAN_POINT ( 'NONE',  ( 119.0929214775786278, -4.153390946401325223, -8.397313243818185668 ) ) ;
#29220=CARTESIAN_POINT ( 'NONE',  ( 116.1998614775786507, -10.63000616557722466, -14.87417383870573495 ) ) ;
#29221=CARTESIAN_POINT ( 'NONE',  ( 112.1722681442453222, -0.4660016031367893996, -10.09054647747474043 ) ) ;
#29223=EDGE_CURVE ( 'NONE', #38146, #16801, #31793, .T. ) ;
#29224=CARTESIAN_POINT ( 'NONE',  ( 117.8659193777725278, -1.267766418764730840, -16.93314635290706605 ) ) ;
#29225=CARTESIAN_POINT ( 'NONE',  ( 123.0637881442452937, -8.899110576539710493, -16.42337572283490132 ) ) ;
#29226=CARTESIAN_POINT ( 'NONE',  ( 114.8384214775786489, -10.15424416112533912, -14.75197769757731336 ) ) ;
#29231=CARTESIAN_POINT ( 'NONE',  ( 121.9100498793805230, -2.191907684172563986, -18.20049396185734025 ) ) ;
#29232=CARTESIAN_POINT ( 'NONE',  ( 119.0361948109119652, -2.084020599724406786, -8.691656652584148546 ) ) ;
#29234=CARTESIAN_POINT ( 'NONE',  ( 126.9932531981142745, -9.712336270502818891, -15.74219525057805846 ) ) ;
#29235=CARTESIAN_POINT ( 'NONE',  ( 114.2711548109119803, -9.988377603198976828, -10.36322818467138340 ) ) ;
#29237=CARTESIAN_POINT ( 'NONE',  ( 118.9183259692789676, -1.179503403430467667, -17.05068175419387089 ) ) ;
#29241=CARTESIAN_POINT ( 'NONE',  ( 122.2128881442453263, -7.643976991954077427, -18.09477374809248928 ) ) ;
#29242=CARTESIAN_POINT ( 'NONE',  ( 117.7882081442453170, -3.505236298600246325, -18.68346056562440793 ) ) ;
#29244=CARTESIAN_POINT ( 'NONE',  ( 116.1431348109119881, 0.1319031606808870605, -14.10382304977625090 ) ) ;
#29250=CARTESIAN_POINT ( 'NONE',  ( 117.2776681442452968, -5.638512984488999180, -18.83840828888717311 ) ) ;
#29251=CARTESIAN_POINT ( 'NONE',  ( 126.0135748109119902, -1.833838273342660141, -17.42832698103878286 ) ) ;
#29252=CARTESIAN_POINT ( 'NONE',  ( 116.5402214775786405, -9.565557343593413364, -10.61323700422348004 ) ) ;
#29253=CARTESIAN_POINT ( 'NONE',  ( 123.0070614775786169, -10.15424416112533912, -14.75197769757731336 ) ) ;
#29255=VERTEX_POINT ( 'NONE', #38189 ) ;
#29256=CARTESIAN_POINT ( 'NONE',  ( 118.5256548109119876, -8.899110576539710493, -16.42337572283490132 ) ) ;
#29257=CARTESIAN_POINT ( 'NONE',  ( 125.3895814775786448, -2.084020599724406786, -8.691656652584148546 ) ) ;
#29261=CARTESIAN_POINT ( 'NONE',  ( 117.5045748109119756, 0.5811942927096110934, -14.16772938898807510 ) ) ;
#29263=CARTESIAN_POINT ( 'NONE',  ( 119.7169148109119874, -9.988377603198976828, -10.36322818467138340 ) ) ;
#29264=CARTESIAN_POINT ( 'NONE',  ( 115.2188909814547344, -2.395992375830784837, -17.92872468182854107 ) ) ;
#29266=CARTESIAN_POINT ( 'NONE',  ( 117.6180281442453150, -0.4660016031367893996, -10.09054647747474043 ) ) ;
#29267=CARTESIAN_POINT ( 'NONE',  ( 118.9794681442453026, -9.261995988541697145, -16.69588392320189030 ) ) ;
#29273=CARTESIAN_POINT ( 'NONE',  ( 121.9859814775786333, -9.565557343593413364, -10.61323700422348004 ) ) ;
#29276=CARTESIAN_POINT ( 'NONE',  ( 113.3068014775786594, -1.833838273342658809, -17.42832698103878286 ) ) ;
#29278=CARTESIAN_POINT ( 'NONE',  ( 113.7038881442453402, -6.222761293078241884, -8.102969835052219238 ) ) ;
#29279=CARTESIAN_POINT ( 'NONE',  ( 120.1707281442453166, 0.2603800115204892296, -16.42320221600525088 ) ) ;
#29282=CARTESIAN_POINT ( 'NONE',  ( 118.2987481442453088, -7.894159318335828068, -9.358103419637847864 ) ) ;
#29284=CARTESIAN_POINT ( 'NONE',  ( 116.9373081442452929, -8.166667518702817929, -8.995218007635861213 ) ) ;
#29285=CARTESIAN_POINT ( 'NONE',  ( 122.9503348109119827, 0.5811942927096110934, -14.16772938898807510 ) ) ;
#29286=CARTESIAN_POINT ( 'NONE',  ( 120.8514481442452961, -2.084020599724406786, -8.691656652584148546 ) ) ;
#29287=ORIENTED_EDGE ( 'NONE', *, *, #2498, .F. ) ;
#29289=CARTESIAN_POINT ( 'NONE',  ( 123.8012348109119642, -9.565557343593413364, -10.61323700422348004 ) ) ;
#29290=CARTESIAN_POINT ( 'NONE',  ( 120.5678148109119832, -8.166667518702819706, -8.995218007635861213 ) ) ;
#29292=CARTESIAN_POINT ( 'NONE',  ( 121.8158014775786171, -5.638512984488999180, -18.83840828888717311 ) ) ;
#29295=CARTESIAN_POINT ( 'NONE',  ( 127.9412782985066599, -3.042519830159750249, -14.56988733893606991 ) ) ;
#29299=CARTESIAN_POINT ( 'NONE',  ( 136.8192643132353510, -10.07312979839473499, -11.38871621322195971 ) ) ;
#29300=CARTESIAN_POINT ( 'NONE',  ( 114.5547881442453217, -4.153390946401321671, -8.397313243818183892 ) ) ;
#29301=CARTESIAN_POINT ( 'NONE',  ( 124.0281414775786146, -1.834011780172310813, -8.268836392978581529 ) ) ;
#29305=CARTESIAN_POINT ( 'NONE',  ( 114.8951481442453115, -8.899110576539710493, -16.42337572283490132 ) ) ;
#29310=CARTESIAN_POINT ( 'NONE',  ( 120.0005481442453146, -5.638512984488999180, -18.83840828888717311 ) ) ;
#29311=CARTESIAN_POINT ( 'NONE',  ( 121.7023481442452919, -0.8288870151387760510, -10.36305467784173118 ) ) ;
#29313=CARTESIAN_POINT ( 'NONE',  ( 137.5098831408921001, -7.763005863679194540, -9.317918806168908219 ) ) ;
#29316=CARTESIAN_POINT ( 'NONE',  ( 117.9583881442453048, 0.1319031606808879209, -14.10382304977623669 ) ) ;
#29317=EDGE_CURVE ( 'NONE', #20392, #18302, #4836, .T. ) ;
#29318=CARTESIAN_POINT ( 'NONE',  ( 120.2841814775786276, -10.15424416112533912, -14.75197769757731336 ) ) ;
#29319=CARTESIAN_POINT ( 'NONE',  ( 117.6180281442453150, -8.899110576539710493, -16.42337572283490132 ) ) ;
#29320=DIRECTION ( 'NONE',  ( 0.000000000000000000, 0.6004852223388327248, -0.7996358532186277346 ) ) ;
#29322=CARTESIAN_POINT ( 'NONE',  ( 125.1059481442452750, -1.833838273342660141, -17.42832698103878286 ) ) ;
#29323=CARTESIAN_POINT ( 'NONE',  ( 123.0637881442452937, -8.899110576539710493, -16.42337572283490132 ) ) ;
#29325=CARTESIAN_POINT ( 'NONE',  ( 112.6828081442453140, -2.084020599724394796, -8.691656652584146769 ) ) ;
#29330=CARTESIAN_POINT ( 'NONE',  ( 121.7590748109119687, -7.893985811506177619, -18.51759400769804742 ) ) ;
#29331=CARTESIAN_POINT ( 'NONE',  ( 117.8449348109119938, -8.166667518702817929, -8.995218007635861213 ) ) ;
#29333=CARTESIAN_POINT ( 'NONE',  ( 117.2776681442452968, -5.638512984488999180, -18.83840828888717311 ) ) ;
#29339=CARTESIAN_POINT ( 'NONE',  ( 119.6601881442453106, -8.166667518702819706, -8.995218007635861213 ) ) ;
#29341=CARTESIAN_POINT ( 'NONE',  ( 112.2857214775786474, -4.089484607189486809, -7.948022111789456723 ) ) ;
#29342=CARTESIAN_POINT ( 'NONE',  ( 114.0442481442453300, -7.643976991954077427, -18.09477374809248928 ) ) ;
#29343=CARTESIAN_POINT ( 'NONE',  ( 111.5482748109120053, -0.1624402480850797581, -16.17319339645315424 ) ) ;
#29346=CARTESIAN_POINT ( 'NONE',  ( 121.6456214775786293, 0.4262465694468514643, -12.03445270309931736 ) ) ;
#29348=CARTESIAN_POINT ( 'NONE',  ( 124.3344342554890716, -2.372251574601201174, -17.96033910819751611 ) ) ;
#29351=CARTESIAN_POINT ( 'NONE',  ( 121.7023481442452777, -9.261995988541697145, -16.69588392320189030 ) ) ;
#29353=CARTESIAN_POINT ( 'NONE',  ( 111.2647102085435193, -8.897589485953298905, -16.42540022429002633 ) ) ;
#29355=CARTESIAN_POINT ( 'NONE',  ( 119.0361948109119652, -2.084020599724406786, -8.691656652584148546 ) ) ;
#29358=( BOUNDED_CURVE ( )  B_SPLINE_CURVE ( 2, ( #23393, #33857, #44826, #37279, #34090, #16787, #20429, #13584, #16559, #27494, #4198, #38853, #24957, #39313, #773, #21761, #28163 ),
 .UNSPECIFIED., .F., .F. ) 
 B_SPLINE_CURVE_WITH_KNOTS ( ( 3, 2, 2, 2, 2, 2, 2, 2, 3 ),
 ( 0.3920046674808919662, 0.3984375000000000000, 0.4062500000000000000, 0.4140625000000000000, 0.4218750000000000000, 0.4296875000000000000, 0.4375000000000000000, 0.4453125000000000000, 0.4517453325190590174 ),
 .UNSPECIFIED. ) 
 CURVE ( )  GEOMETRIC_REPRESENTATION_ITEM ( )  RATIONAL_B_SPLINE_CURVE ( ( 0.9778625265006459788, 0.9373222120152210346, 1.000000000000000000, 0.9238795325112869605, 1.000000000000000000, 0.9238795325112869605, 1.000000000000000000, 0.9238795325112869605, 1.000000000000000000, 0.9238795325112869605, 1.000000000000000000, 0.9238795325112869605, 1.000000000000000000, 0.9238795325112869605, 1.000000000000000000, 0.9373222120157019832, 0.9778625265000240319 ) ) 
 REPRESENTATION_ITEM ( '' )  );
#29359=CARTESIAN_POINT ( 'NONE',  ( 124.8790414775786246, -8.899110576539710493, -16.42337572283490132 ) ) ;
#29362=CARTESIAN_POINT ( 'NONE',  ( 124.6521348109119884, -7.894159318335828068, -9.358103419637847864 ) ) ;
#29365=CARTESIAN_POINT ( 'NONE',  ( 115.9729548109119861, -3.505236298600246325, -18.68346056562440793 ) ) ;
#29366=CARTESIAN_POINT ( 'NONE',  ( 123.2339681442453241, -3.505236298600246325, -18.68346056562440793 ) ) ;
#29367=CARTESIAN_POINT ( 'NONE',  ( 119.0929214775786278, -5.638512984488999180, -18.83840828888717311 ) ) ;
#29368=CARTESIAN_POINT ( 'NONE',  ( 115.9162281442453235, -4.089484607189486809, -7.948022111789456723 ) ) ;
#29370=CARTESIAN_POINT ( 'NONE',  ( 125.2761281442453054, 0.4262465694468514643, -12.03445270309931736 ) ) ;
#29372=CARTESIAN_POINT ( 'NONE',  ( 120.2841814775786276, 0.9020085738987339008, -11.91225656197089222 ) ) ;
#29377=CARTESIAN_POINT ( 'NONE',  ( 112.2857214775786474, -5.574606645277164318, -18.38911715685844683 ) ) ;
#29380=ORIENTED_EDGE ( 'NONE', *, *, #20892, .F. ) ;
#29381=CARTESIAN_POINT ( 'NONE',  ( 126.2404814775786264, -0.8288870151387760510, -10.36305467784173118 ) ) ;
#29387=CARTESIAN_POINT ( 'NONE',  ( 113.9875214775786532, -0.4660016031367893996, -10.09054647747474043 ) ) ;
#29388=CARTESIAN_POINT ( 'NONE',  ( 126.1270281442452870, -10.30919188438810075, -12.61870101168855918 ) ) ;
#29389=CARTESIAN_POINT ( 'NONE',  ( 120.3409081442453044, -8.899110576539710493, -16.42337572283490132 ) ) ;
#29391=CARTESIAN_POINT ( 'NONE',  ( 113.3068014775786594, -1.833838273342658809, -17.42832698103878286 ) ) ;
#29395=CARTESIAN_POINT ( 'NONE',  ( 113.0231681442453322, 0.9020085738987339008, -11.91225656197089222 ) ) ;
#29398=CARTESIAN_POINT ( 'NONE',  ( 122.3830681442452857, -8.166667518702819706, -8.995218007635861213 ) ) ;
#29399=CARTESIAN_POINT ( 'NONE',  ( 136.1673833308560972, -10.30576297294811461, -15.60264770220974029 ) ) ;
#29401=CARTESIAN_POINT ( 'NONE',  ( 115.1220548109119761, -8.166667518702817929, -8.995218007635861213 ) ) ;
#29402=CARTESIAN_POINT ( 'NONE',  ( 125.2194014775786286, -10.30919188438810075, -12.61870101168855918 ) ) ;
#29404=CARTESIAN_POINT ( 'NONE',  ( 124.5386814775786206, -4.153390946401325223, -8.397313243818185668 ) ) ;
#29407=CARTESIAN_POINT ( 'NONE',  ( 116.5402214775786405, 0.2603800115204892296, -16.42320221600525088 ) ) ;
#29410=CARTESIAN_POINT ( 'NONE',  ( 111.7184548109119788, -0.8288870151387708329, -10.36305467784173828 ) ) ;
#29412=CARTESIAN_POINT ( 'NONE',  ( 116.0296814775786345, -1.833838273342658809, -17.42832698103878286 ) ) ;
#29415=CARTESIAN_POINT ( 'NONE',  ( 113.7606148109119886, -7.894159318335828068, -9.358103419637847864 ) ) ;
#29416=CARTESIAN_POINT ( 'NONE',  ( 126.4673881442452910, -7.894159318335828068, -9.358103419637847864 ) ) ;
#29418=CARTESIAN_POINT ( 'NONE',  ( 125.3328548109119964, -0.8288870151387760510, -10.36305467784173118 ) ) ;
#29420=CARTESIAN_POINT ( 'NONE',  ( 119.9438214775786378, -7.893985811506177619, -18.51759400769804742 ) ) ;
#29421=CARTESIAN_POINT ( 'NONE',  ( 120.2841814775786276, 0.9020085738987339008, -11.91225656197089222 ) ) ;
#29423=CARTESIAN_POINT ( 'NONE',  ( 117.7088220330015389, -1.172797794773247304, -17.05961127468924587 ) ) ;
#29427=CARTESIAN_POINT ( 'NONE',  ( 125.7761281442453196, -10.10582367741896093, -14.73954123521881066 ) ) ;
#29428=CARTESIAN_POINT ( 'NONE',  ( 115.9162281442453235, -4.089484607189486809, -7.948022111789456723 ) ) ;
#29433=CARTESIAN_POINT ( 'NONE',  ( 112.8529881442453302, -1.561330072975668060, -17.79121239304076596 ) ) ;
#29434=CARTESIAN_POINT ( 'NONE',  ( 120.0005481442453146, -5.638512984488999180, -18.83840828888717311 ) ) ;
#29436=CARTESIAN_POINT ( 'NONE',  ( 128.2184548109119930, -0.6896191363000483410, -17.70303589939592825 ) ) ;
#29439=CARTESIAN_POINT ( 'NONE',  ( 120.1140014775786398, -7.894159318335828068, -9.358103419637847864 ) ) ;
#29440=CARTESIAN_POINT ( 'NONE',  ( 117.9016614775786280, -9.988377603198976828, -10.36322818467138340 ) ) ;
#29444=CARTESIAN_POINT ( 'NONE',  ( 123.8012348109119642, -9.565557343593413364, -10.61323700422348004 ) ) ;
#29445=CARTESIAN_POINT ( 'NONE',  ( 115.0653281442453277, -3.505236298600246325, -18.68346056562440793 ) ) ;
#29446=ORIENTED_EDGE ( 'NONE', *, *, #40368, .F. ) ;
#29450=CARTESIAN_POINT ( 'NONE',  ( 118.3554748109119998, -9.565557343593413364, -10.61323700422348004 ) ) ;
#29453=CARTESIAN_POINT ( 'NONE',  ( 114.8951481442453115, -0.4660016031367893996, -10.09054647747474043 ) ) ;
#29457=CARTESIAN_POINT ( 'NONE',  ( 113.3635281442453504, -0.1624402480850797581, -16.17319339645315424 ) ) ;
#29459=VERTEX_POINT ( 'NONE', #24518 ) ;
#29460=CARTESIAN_POINT ( 'NONE',  ( 121.1918081442452859, -10.15424416112533912, -14.75197769757731336 ) ) ;
#29461=CARTESIAN_POINT ( 'NONE',  ( 122.5532481442453019, 0.4262465694468514643, -12.03445270309931736 ) ) ;
#29467=CARTESIAN_POINT ( 'NONE',  ( 115.1220548109119761, -8.166667518702817929, -8.995218007635861213 ) ) ;
#29469=CARTESIAN_POINT ( 'NONE',  ( 113.6471614775786492, -5.638512984488999180, -18.83840828888717311 ) ) ;
#29470=CARTESIAN_POINT ( 'NONE',  ( 116.4267681442453153, -6.222761293078241884, -8.102969835052219238 ) ) ;
#29471=CARTESIAN_POINT ( 'NONE',  ( 123.1205148109119563, -7.643976991954077427, -18.09477374809248928 ) ) ;
#29476=CARTESIAN_POINT ( 'NONE',  ( 121.1918081442452859, -10.15424416112533912, -14.75197769757731336 ) ) ;
#29482=CARTESIAN_POINT ( 'NONE',  ( 119.6034614775786196, -6.344957434206665248, -7.627207830600338134 ) ) ;
#29483=EDGE_LOOP ( 'NONE', ( #27380, #25366, #14466, #4465 ) ) ;
#29484=CARTESIAN_POINT ( 'NONE',  ( 119.7736414775786358, -10.30919188438810075, -12.61870101168855918 ) ) ;
#29487=CARTESIAN_POINT ( 'NONE',  ( 116.5969481442453031, 0.5811942927096154232, -14.16772938898807155 ) ) ;
#29488=CARTESIAN_POINT ( 'NONE',  ( 118.8660148109119774, -10.30919188438810075, -12.61870101168855918 ) ) ;
#29495=CARTESIAN_POINT ( 'NONE',  ( 120.5678148109119832, -1.833838273342659253, -17.42832698103878286 ) ) ;
#29498=CARTESIAN_POINT ( 'NONE',  ( 113.5904348109119866, -2.084020599724406786, -8.691656652584148546 ) ) ;
#29501=CARTESIAN_POINT ( 'NONE',  ( 113.7606148109119886, -7.894159318335828068, -9.358103419637847864 ) ) ;
#29502=CARTESIAN_POINT ( 'NONE',  ( 120.7947214775786193, -9.261995988541697145, -16.69588392320189030 ) ) ;
#29505=CARTESIAN_POINT ( 'NONE',  ( 118.4689281442453250, -10.15424416112533912, -14.75197769757731336 ) ) ;
#29506=CARTESIAN_POINT ( 'NONE',  ( 115.7460481442453357, 0.9020085738987339008, -11.91225656197089222 ) ) ;
#29507=CARTESIAN_POINT ( 'NONE',  ( 123.2339681442453241, -6.344957434206665248, -7.627207830600338134 ) ) ;
#29508=CARTESIAN_POINT ( 'NONE',  ( 120.9081748109119872, -4.153390946401325223, -8.397313243818185668 ) ) ;
#29510=CARTESIAN_POINT ( 'NONE',  ( 116.4244054349294686, -1.040089454026965399, -17.23633227186632766 ) ) ;
#29514=CARTESIAN_POINT ( 'NONE',  ( 120.1707281442453166, 0.2603800115204892296, -16.42320221600525088 ) ) ;
#29516=CARTESIAN_POINT ( 'NONE',  ( 122.5532481442453019, -10.63000616557722466, -14.87417383870573495 ) ) ;
#29518=AXIS2_PLACEMENT_3D ( 'NONE', #7576, #39494, #21718 ) ;
#29520=CARTESIAN_POINT ( 'NONE',  ( 118.8101210407382382, -2.419733177069661512, -17.89711025544711376 ) ) ;
#29524=CARTESIAN_POINT ( 'NONE',  ( 119.7736414775786358, 0.1319031606808879209, -14.10382304977623669 ) ) ;
#29525=CARTESIAN_POINT ( 'NONE',  ( 124.4252281442452812, -9.261995988541697145, -16.69588392320189030 ) ) ;
#29531=CARTESIAN_POINT ( 'NONE',  ( 117.1074881442453233, 0.4262465694468514643, -12.03445270309931736 ) ) ;
#29536=CARTESIAN_POINT ( 'NONE',  ( 122.0427081442452817, 0.5811942927096110934, -14.16772938898807510 ) ) ;
#29537=CARTESIAN_POINT ( 'NONE',  ( 122.4965214775786251, 0.1319031606808879209, -14.10382304977623669 ) ) ;
#29542=CARTESIAN_POINT ( 'NONE',  ( 121.3619881442452879, -5.574606645277164318, -18.38911715685844683 ) ) ;
#29543=CARTESIAN_POINT ( 'NONE',  ( 120.6812681442452941, 0.1319031606808879209, -14.10382304977623669 ) ) ;
#29544=CARTESIAN_POINT ( 'NONE',  ( 121.1918081442452859, -10.15424416112533912, -14.75197769757731336 ) ) ;
#29547=AXIS2_PLACEMENT_3D ( 'NONE', #11640, #31926, #39457 ) ;
#29553=CARTESIAN_POINT ( 'NONE',  ( 119.5467348109119712, -4.089484607189486809, -7.948022111789456723 ) ) ;
#29554=CARTESIAN_POINT ( 'NONE',  ( 116.8238548109119819, -4.089484607189486809, -7.948022111789456723 ) ) ;
#29556=CARTESIAN_POINT ( 'NONE',  ( 117.1074881442453233, -10.63000616557722466, -14.87417383870573495 ) ) ;
#29561=CARTESIAN_POINT ( 'NONE',  ( 122.8936081442453059, 0.2603800115204892296, -16.42320221600525088 ) ) ;
#29562=CARTESIAN_POINT ( 'NONE',  ( 120.1707281442453166, 0.2603800115204892296, -16.42320221600525088 ) ) ;
#29564=CARTESIAN_POINT ( 'NONE',  ( 126.5808414775786446, -9.859900752359378018, -12.68260735090039759 ) ) ;
#29565=CARTESIAN_POINT ( 'NONE',  ( 112.3991748109119868, -1.833838273342658809, -17.42832698103878286 ) ) ;
#29566=CARTESIAN_POINT ( 'NONE',  ( 112.1722681442453222, -8.899110576539710493, -16.42337572283490132 ) ) ;
#29568=CARTESIAN_POINT ( 'NONE',  ( 121.5888948109119809, 0.1319031606808879209, -14.10382304977623669 ) ) ;
#29571=CARTESIAN_POINT ( 'NONE',  ( 124.4129961498676948, -2.324775150319219108, -18.02356106541841996 ) ) ;
#29575=CARTESIAN_POINT ( 'NONE',  ( 121.3619881442452879, -4.089484607189486809, -7.948022111789456723 ) ) ;
#29580=CARTESIAN_POINT ( 'NONE',  ( 119.3765548109119834, -10.15424416112533912, -14.75197769757731336 ) ) ;
#29583=CARTESIAN_POINT ( 'NONE',  ( 124.5386814775786206, -4.153390946401325223, -8.397313243818185668 ) ) ;
#29585=CARTESIAN_POINT ( 'NONE',  ( 125.6164881442453094, -9.565557343593413364, -10.61323700422348004 ) ) ;
#29587=CARTESIAN_POINT ( 'NONE',  ( 122.4965214775786251, -10.30919188438810075, -12.61870101168855918 ) ) ;
#29588=CARTESIAN_POINT ( 'NONE',  ( 118.2420214775786320, -6.222761293078241884, -8.102969835052219238 ) ) ;
#29589=CARTESIAN_POINT ( 'NONE',  ( 122.0427081442452817, -9.859900752359378018, -12.68260735090039759 ) ) ;
#29591=CARTESIAN_POINT ( 'NONE',  ( 124.5386814775786206, -5.638512984488999180, -18.83840828888717311 ) ) ;
#29592=EDGE_CURVE ( 'NONE', #39160, #15102, #11001, .T. ) ;
#29593=CARTESIAN_POINT ( 'NONE',  ( 114.9518748109119883, -1.834011780172310813, -8.268836392978581529 ) ) ;
#29595=CARTESIAN_POINT ( 'NONE',  ( 124.6521348109119884, -7.894159318335828068, -9.358103419637847864 ) ) ;
#29596=CARTESIAN_POINT ( 'NONE',  ( 120.7947214775786193, -9.261995988541697145, -16.69588392320189030 ) ) ;
#29602=AXIS2_PLACEMENT_3D ( 'NONE', #23819, #6477, #40917 ) ;
#29603=CARTESIAN_POINT ( 'NONE',  ( 124.3685014775786328, -10.63000616557722466, -14.87417383870573495 ) ) ;
#29605=CARTESIAN_POINT ( 'NONE',  ( 124.5954081442453116, -6.222761293078241884, -8.102969835052219238 ) ) ;
#29610=AXIS2_PLACEMENT_3D ( 'NONE', #24563, #16893, #42793 ) ;
#29612=CARTESIAN_POINT ( 'NONE',  ( 114.1009748109119784, -4.089484607189486809, -7.948022111789456723 ) ) ;
#29614=CARTESIAN_POINT ( 'NONE',  ( 124.6521348109119884, -7.894159318335828068, -9.358103419637847864 ) ) ;
#29615=CARTESIAN_POINT ( 'NONE',  ( 114.8384214775786489, -10.15424416112533912, -14.75197769757731336 ) ) ;
#29616=CARTESIAN_POINT ( 'NONE',  ( 116.1265176481213928, -2.395992375830784837, -17.92872468182854107 ) ) ;
#29617=CARTESIAN_POINT ( 'NONE',  ( 124.0281414775786288, -1.834011780172276396, -8.268836392978611727 ) ) ;
#29618=CARTESIAN_POINT ( 'NONE',  ( 116.1431348109119881, -10.30919188438810075, -12.61870101168855918 ) ) ;
#29621=CARTESIAN_POINT ( 'NONE',  ( 122.5532481442453019, -10.63000616557722466, -14.87417383870573495 ) ) ;
#29625=CARTESIAN_POINT ( 'NONE',  ( 115.8595014775786609, -1.834011780172310813, -8.268836392978581529 ) ) ;
#29626=CARTESIAN_POINT ( 'NONE',  ( 114.4413348109119823, -0.8288870151387760510, -10.36305467784173118 ) ) ;
#29628=CARTESIAN_POINT ( 'NONE',  ( 126.4106614775786284, -6.222761293078241884, -8.102969835052219238 ) ) ;
#29630=CARTESIAN_POINT ( 'NONE',  ( 116.7671281442453335, -1.834011780172310813, -8.268836392978581529 ) ) ;
#29634=CARTESIAN_POINT ( 'NONE',  ( 111.9453614775786434, -7.894159318335820963, -9.358103419637842535 ) ) ;
#29635=CARTESIAN_POINT ( 'NONE',  ( 136.8611794030164788, -2.888169013652136741, -8.200740947275496850 ) ) ;
#29636=CARTESIAN_POINT ( 'NONE',  ( 112.7962614775786676, -6.222761293078241884, -8.102969835052219238 ) ) ;
#29640=CARTESIAN_POINT ( 'NONE',  ( 113.2500748109119968, -3.505236298600246325, -18.68346056562440793 ) ) ;
#29641=CARTESIAN_POINT ( 'NONE',  ( 111.9453614775786434, -1.561330072975668060, -17.79121239304076596 ) ) ;
#29643=CARTESIAN_POINT ( 'NONE',  ( 126.2972081442452890, -2.084020599724406786, -8.691656652584148546 ) ) ;
#29644=CARTESIAN_POINT ( 'NONE',  ( 112.3424481442453384, -3.505236298600246325, -18.68346056562440793 ) ) ;
#29645=CARTESIAN_POINT ( 'NONE',  ( 121.9859814775786333, 0.2603800115204892296, -16.42320221600525088 ) ) ;
#29646=CARTESIAN_POINT ( 'NONE',  ( 121.8158014775786171, -5.638512984488999180, -18.83840828888717311 ) ) ;
#29648=CARTESIAN_POINT ( 'NONE',  ( 127.0264730702694038, -8.469371566854281497, -17.41871083769240514 ) ) ;
#29654=CARTESIAN_POINT ( 'NONE',  ( 114.9518748109119883, -1.834011780172310813, -8.268836392978581529 ) ) ;
#29655=VERTEX_POINT ( 'NONE', #43193 ) ;
#29659=CARTESIAN_POINT ( 'NONE',  ( 112.8529881442453302, -7.894159318335828068, -9.358103419637847864 ) ) ;
#29660=CARTESIAN_POINT ( 'NONE',  ( 111.8886348109120092, -3.383040157471821630, -19.15922257007629170 ) ) ;
#29661=CARTESIAN_POINT ( 'NONE',  ( 118.8660148109119774, -10.30919188438810075, -12.61870101168855918 ) ) ;
#29666=CARTESIAN_POINT ( 'NONE',  ( 118.0718414775786442, -0.8288870151387760510, -10.36305467784173118 ) ) ;
#29667=CARTESIAN_POINT ( 'NONE',  ( 116.7671281442453335, -1.834011780172310813, -8.268836392978581529 ) ) ;
#29669=CARTESIAN_POINT ( 'NONE',  ( 114.7249681442453237, -9.565557343593413364, -10.61323700422348004 ) ) ;
#29670=CARTESIAN_POINT ( 'NONE',  ( 113.8173414775786512, 0.2603800115204892296, -16.42320221600525088 ) ) ;
#29672=CARTESIAN_POINT ( 'NONE',  ( 123.7445081442452874, -7.894159318335828068, -9.358103419637847864 ) ) ;
#29673=CARTESIAN_POINT ( 'NONE',  ( 120.7947214775786193, -0.8288870151387760510, -10.36305467784173118 ) ) ;
#29674=ORIENTED_EDGE ( 'NONE', *, *, #13860, .T. ) ;
#29676=CARTESIAN_POINT ( 'NONE',  ( 112.1155414775786454, 0.9020085738987339008, -11.91225656197089222 ) ) ;
#29677=CARTESIAN_POINT ( 'NONE',  ( 122.7234281442452755, -4.153390946401325223, -8.397313243818185668 ) ) ;
#29680=CARTESIAN_POINT ( 'NONE',  ( 115.9162281442453235, -4.089484607189486809, -7.948022111789456723 ) ) ;
#29683=CARTESIAN_POINT ( 'NONE',  ( 116.5402214775786405, -9.565557343593413364, -10.61323700422348004 ) ) ;
#29686=CARTESIAN_POINT ( 'NONE',  ( 120.4543614775786295, -5.574606645277164318, -18.38911715685844683 ) ) ;
#29687=CARTESIAN_POINT ( 'NONE',  ( 121.9292548109119849, -7.894159318335828068, -9.358103419637847864 ) ) ;
#29690=DIRECTION ( 'NONE',  ( 0.000000000000000000, 0.6004852223388321697, -0.7996358532186279566 ) ) ;
#29694=CARTESIAN_POINT ( 'NONE',  ( 115.9162281442453235, -4.089484607189486809, -7.948022111789456723 ) ) ;
#29695=CARTESIAN_POINT ( 'NONE',  ( 116.3700414775786527, -5.638512984488999180, -18.83840828888717311 ) ) ;
#29696=CARTESIAN_POINT ( 'NONE',  ( 117.6180281442453150, -8.899110576539710493, -16.42337572283490132 ) ) ;
#29697=CARTESIAN_POINT ( 'NONE',  ( 121.7023481442452777, -0.8288870151387760510, -10.36305467784173118 ) ) ;
#29698=CARTESIAN_POINT ( 'NONE',  ( 113.2500748109119968, -6.344957434206662583, -7.627207830600332805 ) ) ;
#29700=CARTESIAN_POINT ( 'NONE',  ( 120.3409081442453044, -8.899110576539710493, -16.42337572283490132 ) ) ;
#29701=DIRECTION ( 'NONE',  ( 1.000000000000000000, 0.000000000000000000, 0.000000000000000000 ) ) ;
#29705=CARTESIAN_POINT ( 'NONE',  ( 117.3911214775786505, -1.561330072975668504, -17.79121239304076951 ) ) ;
#29707=CARTESIAN_POINT ( 'NONE',  ( 120.7947214775786193, -9.261995988541697145, -16.69588392320189030 ) ) ;
#29710=CARTESIAN_POINT ( 'NONE',  ( 119.0929214775786278, -5.638512984488999180, -18.83840828888717311 ) ) ;
#29711=CARTESIAN_POINT ( 'NONE',  ( 116.7671281442453335, -1.834011780172310813, -8.268836392978581529 ) ) ;
#29717=CARTESIAN_POINT ( 'NONE',  ( 118.5256548109119876, -8.899110576539710493, -16.42337572283490132 ) ) ;
#29720=CARTESIAN_POINT ( 'NONE',  ( 117.6747548109119919, -7.643976991954077427, -18.09477374809248928 ) ) ;
#29723=CARTESIAN_POINT ( 'NONE',  ( 125.9001214775786224, -4.089484607189486809, -7.948022111789456723 ) ) ;
#29724=CARTESIAN_POINT ( 'NONE',  ( 124.5954081442453116, -3.383040157471821630, -19.15922257007629170 ) ) ;
#29726=CARTESIAN_POINT ( 'NONE',  ( 118.2420214775786320, -6.222761293078241884, -8.102969835052219238 ) ) ;
#29727=CARTESIAN_POINT ( 'NONE',  ( 115.5758681442453053, -1.561330072975668060, -17.79121239304076951 ) ) ;
#29728=CARTESIAN_POINT ( 'NONE',  ( 119.8870948109119752, -9.261995988541697145, -16.69588392320189030 ) ) ;
#29730=CARTESIAN_POINT ( 'NONE',  ( 122.6099748109119929, -0.8288870151387760510, -10.36305467784173118 ) ) ;
#29734=B_SPLINE_CURVE_WITH_KNOTS ( 'NONE', 3,
 ( #22347, #38995, #11422, #35559, #1141, #21449, #7764, #15277, #21672, #12092, #39677, #25548, #8217, #4103, #11867, #1367, #14837, #18924, #25997, #43324, #29185, #28747, #25329, #39221, #43097, #7986, #1581, #39901, #21895, #28973, #36016, #12769, #29863, #37372, #44238, #26894, #12998, #15960, #43779, #16187, #15733, #8662, #29635, #19597, #33481, #30312, #5679, #40814, #2260, #16643, #5234, #22564, #30092, #36907, #36468, #44008 ),
 .UNSPECIFIED., .F., .F.,
 ( 4, 2, 2, 2, 2, 2, 2, 1, 2, 2, 2, 2, 2, 2, 2, 2, 2, 2, 2, 2, 2, 1, 2, 2, 2, 2, 2, 2, 4 ),
 ( 0.000000000000000000, 0.06250000000003547163, 0.09375000000004662937, 0.1093750000000587308, 0.1250000000000708322, 0.1875000000001189049, 0.2187500000001370570, 0.2343750000001460498, 0.2421875000001448286, 0.2500000000001436073, 0.3125000000001424416, 0.3437500000001458278, 0.3593750000001435518, 0.3750000000001412759, 0.5000000000001461054, 0.5625000000001483258, 0.5937500000001509903, 0.6093750000001524336, 0.6250000000001537659, 0.6875000000001595390, 0.7187500000001625367, 0.7343750000001639799, 0.7421875000001597611, 0.7500000000001555422, 0.8125000000001221245, 0.8437500000001054712, 0.8593750000000912603, 0.8750000000000770495, 1.000000000000000000 ),
 .UNSPECIFIED. ) ;
#29735=CARTESIAN_POINT ( 'NONE',  ( 123.1772414775786189, -4.089484607189486809, -7.948022111789456723 ) ) ;
#29736=CARTESIAN_POINT ( 'NONE',  ( 112.1722681442453222, -8.899110576539710493, -16.42337572283490132 ) ) ;
#29737=CARTESIAN_POINT ( 'NONE',  ( 111.3213681442453264, -7.643976991954077427, -18.09477374809248928 ) ) ;
#29739=DIRECTION ( 'NONE',  ( 1.000000000000000000, 0.000000000000000000, 0.000000000000000000 ) ) ;
#29743=CARTESIAN_POINT ( 'NONE',  ( 136.8340972670076781, -10.06728345606325625, -11.39864759042615816 ) ) ;
#29744=CARTESIAN_POINT ( 'NONE',  ( 117.9583881442453048, 0.1319031606808879209, -14.10382304977623669 ) ) ;
#29745=CARTESIAN_POINT ( 'NONE',  ( 123.9146881442452894, 0.9020085738987339008, -11.91225656197089222 ) ) ;
#29746=CARTESIAN_POINT ( 'NONE',  ( 136.4689272580752686, -7.050714571525749541, -18.72418924296322729 ) ) ;
#29751=CARTESIAN_POINT ( 'NONE',  ( 115.7460481442453357, -10.15424416112533912, -14.75197769757731336 ) ) ;
#29757=CARTESIAN_POINT ( 'NONE',  ( 121.8725281442453223, -3.383040157471821630, -19.15922257007629170 ) ) ;
#29758=CARTESIAN_POINT ( 'NONE',  ( 123.5743281442453139, -2.084020599724406786, -8.691656652584148546 ) ) ;
#29761=CARTESIAN_POINT ( 'NONE',  ( 125.5030348109119558, -3.383040157471821630, -19.15922257007629170 ) ) ;
#29764=CARTESIAN_POINT ( 'NONE',  ( 121.7023481442452919, -0.8288870151387760510, -10.36305467784173118 ) ) ;
#29765=CARTESIAN_POINT ( 'NONE',  ( 121.3052614775786111, -7.643976991954077427, -18.09477374809248928 ) ) ;
#29775=CARTESIAN_POINT ( 'NONE',  ( 121.4187148109119789, -6.344957434206665248, -7.627207830600338134 ) ) ;
#29776=CARTESIAN_POINT ( 'NONE',  ( 121.6456214775786293, -10.63000616557722466, -14.87417383870573495 ) ) ;
#29778=CARTESIAN_POINT ( 'NONE',  ( 116.8238548109119819, -4.089484607189486809, -7.948022111789456723 ) ) ;
#29783=CARTESIAN_POINT ( 'NONE',  ( 123.3474214775786209, -9.988377603198976828, -10.36322818467138340 ) ) ;
#29784=CARTESIAN_POINT ( 'NONE',  ( 119.8870948109119752, -9.261995988541697145, -16.69588392320189030 ) ) ;
#29785=CARTESIAN_POINT ( 'NONE',  ( 111.7184548109119788, -9.261995988541697145, -16.69588392320189030 ) ) ;
#29787=CARTESIAN_POINT ( 'NONE',  ( 112.7962614775786676, -6.222761293078241884, -8.102969835052219238 ) ) ;
#29789=CARTESIAN_POINT ( 'NONE',  ( 113.7038881442453402, -6.222761293078241884, -8.102969835052219238 ) ) ;
#29790=CARTESIAN_POINT ( 'NONE',  ( 124.4819548109119722, -7.893985811506177619, -18.51759400769804742 ) ) ;
#29795=CARTESIAN_POINT ( 'NONE',  ( 119.4332814775786318, -8.899110576539710493, -16.42337572283490132 ) ) ;
#29797=CARTESIAN_POINT ( 'NONE',  ( 124.3737138206744959, -2.348512537728041583, -17.99195118506215962 ) ) ;
#29801=CARTESIAN_POINT ( 'NONE',  ( 121.8158014775786171, -5.638512984488999180, -18.83840828888717311 ) ) ;
#29805=CARTESIAN_POINT ( 'NONE',  ( 119.7169148109119874, -0.1624402480850797581, -16.17319339645315424 ) ) ;
#29808=CARTESIAN_POINT ( 'NONE',  ( 122.0427081442452817, -9.859900752359378018, -12.68260735090039759 ) ) ;
#29810=CARTESIAN_POINT ( 'NONE',  ( 135.5334395969766206, -4.108503626107443907, -19.33946713067309275 ) ) ;
#29812=CARTESIAN_POINT ( 'NONE',  ( 125.1059481442452750, -8.166667518702819706, -8.995218007635861213 ) ) ;
#29813=CARTESIAN_POINT ( 'NONE',  ( 118.0151148109119816, 0.4262465694468514643, -12.03445270309931736 ) ) ;
#29814=CARTESIAN_POINT ( 'NONE',  ( 122.3830681442452857, -1.833838273342659697, -17.42832698103878286 ) ) ;
#29815=VERTEX_POINT ( 'NONE', #20543 ) ;
#29816=CARTESIAN_POINT ( 'NONE',  ( 124.6521348109119884, -1.561330072975668948, -17.79121239304076951 ) ) ;
#29817=CARTESIAN_POINT ( 'NONE',  ( 116.2565881442452991, -9.261995988541697145, -16.69588392320189030 ) ) ;
#29819=CARTESIAN_POINT ( 'NONE',  ( 112.6828081442453282, -2.084020599724406786, -8.691656652584148546 ) ) ;
#29820=CARTESIAN_POINT ( 'NONE',  ( 124.8223148109119762, -10.15424416112533912, -14.75197769757731336 ) ) ;
#29821=CARTESIAN_POINT ( 'NONE',  ( 122.4397948109119767, -9.988377603198976828, -10.36322818467138340 ) ) ;
#29825=CARTESIAN_POINT ( 'NONE',  ( 113.4202548109119846, 0.1319031606808879209, -14.10382304977623669 ) ) ;
#29831=CARTESIAN_POINT ( 'NONE',  ( 125.5597614775786326, -7.894159318335828068, -9.358103419637847864 ) ) ;
#29839=CARTESIAN_POINT ( 'NONE',  ( 116.6536748109119941, 0.9020085738987339008, -11.91225656197089222 ) ) ;
#29840=CARTESIAN_POINT ( 'NONE',  ( 124.2550481442452792, -0.1624402480850797581, -16.17319339645315424 ) ) ;
#29841=CARTESIAN_POINT ( 'NONE',  ( 116.5402214775786405, -9.565557343593413364, -10.61323700422348004 ) ) ;
#29844=CARTESIAN_POINT ( 'NONE',  ( 114.7273308535611562, -2.239543233855025850, -18.13706010537467606 ) ) ;
#29845=CARTESIAN_POINT ( 'NONE',  ( 114.8384214775786489, 0.9020085738987339008, -11.91225656197089222 ) ) ;
#29849=CARTESIAN_POINT ( 'NONE',  ( 124.0281414775786146, -1.834011780172310813, -8.268836392978581529 ) ) ;
#29853=CARTESIAN_POINT ( 'NONE',  ( 114.6682414775786469, -1.561330072975668060, -17.79121239304076596 ) ) ;
#29854=CARTESIAN_POINT ( 'NONE',  ( 113.7038881442453402, -6.222761293078241884, -8.102969835052219238 ) ) ;
#29856=CARTESIAN_POINT ( 'NONE',  ( 111.7184548109119788, -9.261995988541697145, -16.69588392320189030 ) ) ;
#29858=CARTESIAN_POINT ( 'NONE',  ( 122.2696148109119889, -4.089484607189486809, -7.948022111789456723 ) ) ;
#29861=CARTESIAN_POINT ( 'NONE',  ( 115.6683931944929498, -1.036737761566197014, -17.24079555149560861 ) ) ;
#29863=CARTESIAN_POINT ( 'NONE',  ( 137.3930029278099312, -3.553605451871880039, -8.436688146991468074 ) ) ;
#29864=CARTESIAN_POINT ( 'NONE',  ( 112.7395348109119766, -4.153390946401321671, -8.397313243818183892 ) ) ;
#29867=CARTESIAN_POINT ( 'NONE',  ( 112.2289948109119848, -7.643976991954077427, -18.09477374809248928 ) ) ;
#29869=CARTESIAN_POINT ( 'NONE',  ( 112.9097148109120070, 0.2603800115204892296, -16.42320221600525088 ) ) ;
#29871=CARTESIAN_POINT ( 'NONE',  ( 126.5808414775786446, -9.859900752359378018, -12.68260735090039759 ) ) ;
#29872=CARTESIAN_POINT ( 'NONE',  ( 114.0442481442453300, -7.643976991954077427, -18.09477374809248928 ) ) ;
#29873=CARTESIAN_POINT ( 'NONE',  ( 124.5954081442453116, -3.383040157471821630, -19.15922257007629170 ) ) ;
#29874=CARTESIAN_POINT ( 'NONE',  ( 123.1772414775786189, -4.089484607189486809, -7.948022111789456723 ) ) ;
#29876=CARTESIAN_POINT ( 'NONE',  ( 114.9518748109119883, -1.834011780172310813, -8.268836392978581529 ) ) ;
#29881=CARTESIAN_POINT ( 'NONE',  ( 120.1707281442453166, 0.2603800115204892296, -16.42320221600525088 ) ) ;
#29883=CARTESIAN_POINT ( 'NONE',  ( 126.1270281442452870, -10.30919188438810075, -12.61870101168855918 ) ) ;
#29885=CARTESIAN_POINT ( 'NONE',  ( 119.5467348109119712, -5.574606645277192740, -18.38911715685844328 ) ) ;
#29886=CARTESIAN_POINT ( 'NONE',  ( 114.9518748109119883, -7.643976991954077427, -18.09477374809248928 ) ) ;
#29889=CARTESIAN_POINT ( 'NONE',  ( 121.0783548109119749, 0.2603800115204892296, -16.42320221600525088 ) ) ;
#29893=CARTESIAN_POINT ( 'NONE',  ( 121.3619881442452879, -5.574606645277164318, -18.38911715685844683 ) ) ;
#29894=CARTESIAN_POINT ( 'NONE',  ( 121.6456214775786293, 0.4262465694468514643, -12.03445270309931736 ) ) ;
#29895=CARTESIAN_POINT ( 'NONE',  ( 119.3765548109119834, 0.9020085738987339008, -11.91225656197089222 ) ) ;
#29896=CIRCLE ( 'NONE', #18239, 0.4999999999999999445 ) ;
#29898=CARTESIAN_POINT ( 'NONE',  ( 115.4056881442453459, -7.893985811506177619, -18.51759400769804742 ) ) ;
#29899=CARTESIAN_POINT ( 'NONE',  ( 135.3184548109119874, -7.252096815532139473, -18.89748516540533529 ) ) ;
#29901=CARTESIAN_POINT ( 'NONE',  ( 124.3685014775786328, 0.4262465694468514643, -12.03445270309931736 ) ) ;
#29902=CARTESIAN_POINT ( 'NONE',  ( 119.3198281442452924, -9.859900752359374465, -12.68260735090039404 ) ) ;
#29907=CARTESIAN_POINT ( 'NONE',  ( 112.8529881442453302, -1.561330072975668060, -17.79121239304076596 ) ) ;
#29908=CARTESIAN_POINT ( 'NONE',  ( 119.8870948109119752, -0.8288870151387760510, -10.36305467784173118 ) ) ;
#29912=CARTESIAN_POINT ( 'NONE',  ( 118.2987481442453088, -1.561330072975668504, -17.79121239304076951 ) ) ;
#29914=CARTESIAN_POINT ( 'NONE',  ( 114.4413348109119823, -0.8288870151387760510, -10.36305467784173118 ) ) ;
#29917=CARTESIAN_POINT ( 'NONE',  ( 124.4819548109119722, -2.084020599724406786, -8.691656652584148546 ) ) ;
#29918=CARTESIAN_POINT ( 'NONE',  ( 120.1140014775786398, -7.894159318335828068, -9.358103419637847864 ) ) ;
#29921=CARTESIAN_POINT ( 'NONE',  ( 118.8092881442453290, -9.988377603198976828, -10.36322818467138340 ) ) ;
#29925=CARTESIAN_POINT ( 'NONE',  ( 116.8805814775786445, -6.344957434206662583, -7.627207830600332805 ) ) ;
#29926=CARTESIAN_POINT ( 'NONE',  ( 116.7104014775786425, -0.4660016031367893996, -10.09054647747474043 ) ) ;
#29927=CARTESIAN_POINT ( 'NONE',  ( 115.8027748109119841, -8.899110576539710493, -16.42337572283490132 ) ) ;
#29928=CARTESIAN_POINT ( 'NONE',  ( 124.9924948109119924, -5.574606645277164318, -18.38911715685844683 ) ) ;
#29929=CARTESIAN_POINT ( 'NONE',  ( 113.7038881442453402, -3.383040157471821630, -19.15922257007629170 ) ) ;
#29931=CARTESIAN_POINT ( 'NONE',  ( 123.6310548109119765, -4.153390946401325223, -8.397313243818185668 ) ) ;
#29933=CARTESIAN_POINT ( 'NONE',  ( 114.1934435773848833, -2.467220198592768199, -17.83387418641523325 ) ) ;
#29937=CARTESIAN_POINT ( 'NONE',  ( 117.6747548109119919, -1.834011780172310813, -8.268836392978581529 ) ) ;
#29940=CARTESIAN_POINT ( 'NONE',  ( 121.4187148109119789, -6.344957434206665248, -7.627207830600338134 ) ) ;
#29943=CARTESIAN_POINT ( 'NONE',  ( 120.3409081442453044, -0.4660016031367893996, -10.09054647747474043 ) ) ;
#29944=CARTESIAN_POINT ( 'NONE',  ( 121.5888948109119809, -10.30919188438810075, -12.61870101168855918 ) ) ;
#29949=CARTESIAN_POINT ( 'NONE',  ( 113.0231681442453180, -10.15424416112533912, -14.75197769757731336 ) ) ;
#29950=CARTESIAN_POINT ( 'NONE',  ( 125.7299414775786346, -10.15424416112533912, -14.75197769757731336 ) ) ;
#29953=CARTESIAN_POINT ( 'NONE',  ( 119.4332814775786318, -8.899110576539710493, -16.42337572283490132 ) ) ;
#29956=CARTESIAN_POINT ( 'NONE',  ( 126.2404814775786264, -9.261995988541697145, -16.69588392320189030 ) ) ;
#29957=CARTESIAN_POINT ( 'NONE',  ( 121.9859814775786333, 0.2603800115204892296, -16.42320221600525088 ) ) ;
#29959=CARTESIAN_POINT ( 'NONE',  ( 122.3263414775786373, -3.505236298600246325, -18.68346056562440793 ) ) ;
#29960=CARTESIAN_POINT ( 'NONE',  ( 115.0086014775786509, -4.089484607189486809, -7.948022111789456723 ) ) ;
#29961=CARTESIAN_POINT ( 'NONE',  ( 121.8725281442453223, -3.383040157471821630, -19.15922257007629170 ) ) ;
#29963=CARTESIAN_POINT ( 'NONE',  ( 122.4397948109119767, -0.1624402480850797581, -16.17319339645315424 ) ) ;
#29967=CARTESIAN_POINT ( 'NONE',  ( 123.1205148109119563, -1.834011780172310813, -8.268836392978581529 ) ) ;
#29969=CARTESIAN_POINT ( 'NONE',  ( 124.4252281442452812, -9.261995988541697145, -16.69588392320189030 ) ) ;
#29972=CARTESIAN_POINT ( 'NONE',  ( 127.9617136114945879, -3.003383010795549701, -14.62204112140151047 ) ) ;
#29975=CARTESIAN_POINT ( 'NONE',  ( 119.2063748109119814, -7.894159318335828068, -9.358103419637847864 ) ) ;
#29976=CARTESIAN_POINT ( 'NONE',  ( 124.5386814775786206, -5.638512984488999180, -18.83840828888717311 ) ) ;
#29977=CARTESIAN_POINT ( 'NONE',  ( 126.9932531981088033, -0.01566132117990067310, -11.04423515009607470 ) ) ;
#29979=CARTESIAN_POINT ( 'NONE',  ( 115.7132342721482843, -2.287189184988710267, -18.07361239780447448 ) ) ;
#29980=CARTESIAN_POINT ( 'NONE',  ( 114.7816948109119863, -9.859900752359374465, -12.68260735090039404 ) ) ;
#29981=CARTESIAN_POINT ( 'NONE',  ( 113.1366214775786432, -7.643976991954077427, -18.09477374809248928 ) ) ;
#29984=CARTESIAN_POINT ( 'NONE',  ( 111.8319081442453182, -4.153390946401321671, -8.397313243818183892 ) ) ;
#29986=CARTESIAN_POINT ( 'NONE',  ( 121.9859814775786333, 0.2603800115204892296, -16.42320221600525088 ) ) ;
#29987=CARTESIAN_POINT ( 'NONE',  ( 121.0783548109119749, -9.565557343593413364, -10.61323700422348004 ) ) ;
#29992=CARTESIAN_POINT ( 'NONE',  ( 122.0427081442452817, -9.859900752359378018, -12.68260735090039759 ) ) ;
#29993=CARTESIAN_POINT ( 'NONE',  ( 118.9794681442453026, -0.8288870151387760510, -10.36305467784173118 ) ) ;
#30003=CARTESIAN_POINT ( 'NONE',  ( 120.5678148109119832, -8.166667518702819706, -8.995218007635861213 ) ) ;
#30004=CARTESIAN_POINT ( 'NONE',  ( 121.5888948109119809, -10.30919188438810075, -12.61870101168855918 ) ) ;
#30006=CARTESIAN_POINT ( 'NONE',  ( 117.0507614775786465, -10.30919188438810075, -12.61870101168855918 ) ) ;
#30007=CARTESIAN_POINT ( 'NONE',  ( 111.7184548109119788, -8.862178061932382889, -16.39564131203247399 ) ) ;
#30010=CARTESIAN_POINT ( 'NONE',  ( 124.7088614775786226, 0.2603800115204892296, -16.42320221600525088 ) ) ;
#30011=CARTESIAN_POINT ( 'NONE',  ( 121.1350814775786233, 0.5811942927096110934, -14.16772938898807510 ) ) ;
#30012=CARTESIAN_POINT ( 'NONE',  ( 112.2289948109119848, -1.834011780172310813, -8.268836392978581529 ) ) ;
#30013=CARTESIAN_POINT ( 'NONE',  ( 114.2144281442453178, -1.833838273342658809, -17.42832698103878286 ) ) ;
#30015=CARTESIAN_POINT ( 'NONE',  ( 114.8384214775786489, -10.15424416112533912, -14.75197769757731336 ) ) ;
#30016=CARTESIAN_POINT ( 'NONE',  ( 124.3117748109119844, -10.30919188438810075, -12.61870101168855918 ) ) ;
#30020=CARTESIAN_POINT ( 'NONE',  ( 120.2274548109119934, -9.859900752359378018, -12.68260735090039759 ) ) ;
#30023=VERTEX_POINT ( 'NONE', #23118 ) ;
#30027=CARTESIAN_POINT ( 'NONE',  ( 124.2550481442452792, -9.988377603198980381, -10.36322818467138518 ) ) ;
#30037=CARTESIAN_POINT ( 'NONE',  ( 125.9568481442452850, -6.344957434206665248, -7.627207830600338134 ) ) ;
#30038=CARTESIAN_POINT ( 'NONE',  ( 116.1431348109119881, 0.1319031606808879209, -14.10382304977623669 ) ) ;
#30042=CARTESIAN_POINT ( 'NONE',  ( 121.6456214775786293, -10.63000616557722466, -14.87417383870573495 ) ) ;
#30043=CARTESIAN_POINT ( 'NONE',  ( 116.7104014775786425, -0.4660016031367893996, -10.09054647747474043 ) ) ;
#30048=CARTESIAN_POINT ( 'NONE',  ( 123.3474214775786209, -0.1624402480850797581, -16.17319339645315424 ) ) ;
#30050=CARTESIAN_POINT ( 'NONE',  ( 124.4252281442452812, -9.261995988541697145, -16.69588392320189030 ) ) ;
#30054=CARTESIAN_POINT ( 'NONE',  ( 115.2355081442453155, 0.1319031606808879209, -14.10382304977623669 ) ) ;
#30056=CARTESIAN_POINT ( 'NONE',  ( 117.6747548109119919, -7.643976991954077427, -18.09477374809248928 ) ) ;
#30060=CARTESIAN_POINT ( 'NONE',  ( 122.6099748109119929, -0.8288870151387726093, -10.36305467784173651 ) ) ;
#30061=CARTESIAN_POINT ( 'NONE',  ( 126.1270281442452870, 0.1319031606808879209, -14.10382304977623669 ) ) ;
#30064=EDGE_LOOP ( 'NONE', ( #24637, #2353, #39252, #15532, #9312, #36623, #881 ) ) ;
#30070=CARTESIAN_POINT ( 'NONE',  ( 119.9438214775786378, -7.893985811506177619, -18.51759400769804742 ) ) ;
#30071=CARTESIAN_POINT ( 'NONE',  ( 124.0281414775786146, -7.643976991954077427, -18.09477374809248928 ) ) ;
#30072=CARTESIAN_POINT ( 'NONE',  ( 114.3846081442453197, 0.4262465694468514643, -12.03445270309931736 ) ) ;
#30074=CARTESIAN_POINT ( 'NONE',  ( 116.3176581477680145, -2.280480477428486363, -18.08254604495228435 ) ) ;
#30075=CARTESIAN_POINT ( 'NONE',  ( 124.5386814775786206, -5.638512984489033819, -18.83840828888716956 ) ) ;
#30076=CARTESIAN_POINT ( 'NONE',  ( 114.4980614775786592, -7.893985811506177619, -18.51759400769804742 ) ) ;
#30079=CARTESIAN_POINT ( 'NONE',  ( 125.1626748109119802, -9.988377603198980381, -10.36322818467138518 ) ) ;
#30081=CARTESIAN_POINT ( 'NONE',  ( 114.2711548109119803, -9.988377603198976828, -10.36322818467138340 ) ) ;
#30082=CARTESIAN_POINT ( 'NONE',  ( 115.5191414775786569, -6.222761293078241884, -8.102969835052219238 ) ) ;
#30085=CARTESIAN_POINT ( 'NONE',  ( 112.1155414775786454, 0.9020085738987339008, -11.91225656197089222 ) ) ;
#30086=VERTEX_POINT ( 'NONE', #7963 ) ;
#30088=CARTESIAN_POINT ( 'NONE',  ( 122.3830681442452857, -8.166667518702819706, -8.995218007635861213 ) ) ;
#30090=CARTESIAN_POINT ( 'NONE',  ( 115.9721219144190485, -1.220279397241700758, -16.99638242193885063 ) ) ;
#30092=CARTESIAN_POINT ( 'NONE',  ( 136.1332990479140506, -2.569798562088685845, -7.975597057175941806 ) ) ;
#30093=CARTESIAN_POINT ( 'NONE',  ( 114.2144281442453178, -1.833838273342658809, -17.42832698103878286 ) ) ;
#30096=CARTESIAN_POINT ( 'NONE',  ( 115.1220548109119761, -1.833838273342658809, -17.42832698103878286 ) ) ;
#30097=CARTESIAN_POINT ( 'NONE',  ( 115.1787814775786387, -9.988377603198976828, -10.36322818467138340 ) ) ;
#30099=CARTESIAN_POINT ( 'NONE',  ( 113.9307948109119906, 0.9020085738987339008, -11.91225656197089222 ) ) ;
#30100=CARTESIAN_POINT ( 'NONE',  ( 113.9307948109119764, -10.15424416112533912, -14.75197769757731336 ) ) ;
#30101=CARTESIAN_POINT ( 'NONE',  ( 121.7023481442452777, -9.261995988541697145, -16.69588392320189030 ) ) ;
#30103=CARTESIAN_POINT ( 'NONE',  ( 121.7023481442452777, -9.261995988541697145, -16.69588392320189030 ) ) ;
#30105=CARTESIAN_POINT ( 'NONE',  ( 112.7962614775786676, -3.383040157471821630, -19.15922257007629170 ) ) ;
#30110=CARTESIAN_POINT ( 'NONE',  ( 118.5256548109119876, -0.4660016031367893996, -10.09054647747474043 ) ) ;
#30116=CARTESIAN_POINT ( 'NONE',  ( 113.0798948109119948, -8.899110576539710493, -16.42337572283490132 ) ) ;
#30118=CARTESIAN_POINT ( 'NONE',  ( 118.8092881442453290, -9.988377603198976828, -10.36322818467138340 ) ) ;
#30122=ORIENTED_EDGE ( 'NONE', *, *, #44046, .T. ) ;
#30124=CARTESIAN_POINT ( 'NONE',  ( 123.1205148109119563, -7.643976991954077427, -18.09477374809248928 ) ) ;
#30126=CARTESIAN_POINT ( 'NONE',  ( 120.7947214775786193, -9.261995988541697145, -16.69588392320189030 ) ) ;
#30127=CARTESIAN_POINT ( 'NONE',  ( 112.4559014775786778, -0.1624402480850797581, -16.17319339645315424 ) ) ;
#30128=CARTESIAN_POINT ( 'NONE',  ( 117.0507614775786465, -10.30919188438810075, -12.61870101168855918 ) ) ;
#30130=CARTESIAN_POINT ( 'NONE',  ( 127.4620922276975534, -1.264427456653780091, -9.074754333436022335 ) ) ;
#30131=CARTESIAN_POINT ( 'NONE',  ( 118.1285681442453068, -2.084020599724406786, -8.691656652584148546 ) ) ;
#30133=CARTESIAN_POINT ( 'NONE',  ( 119.4332814775786318, -0.4660016031367946177, -10.09054647747473332 ) ) ;
#30135=CARTESIAN_POINT ( 'NONE',  ( 114.5547881442453217, -5.638512984488999180, -18.83840828888717311 ) ) ;
#30136=CARTESIAN_POINT ( 'NONE',  ( 121.7590748109119687, -2.084020599724406786, -8.691656652584148546 ) ) ;
#30139=CARTESIAN_POINT ( 'NONE',  ( 120.0005481442453146, -5.638512984488999180, -18.83840828888717311 ) ) ;
#30141=CARTESIAN_POINT ( 'NONE',  ( 115.7460481442453357, -10.15424416112533912, -14.75197769757731336 ) ) ;
#30144=CARTESIAN_POINT ( 'NONE',  ( 126.6375681442452930, -10.15424416112533912, -14.75197769757731336 ) ) ;
#30145=CARTESIAN_POINT ( 'NONE',  ( 121.9859814775786333, -9.565557343593413364, -10.61323700422348004 ) ) ;
#30147=EDGE_CURVE ( 'NONE', #32113, #45010, #9697, .T. ) ;
#30149=CARTESIAN_POINT ( 'NONE',  ( 118.7525614775786380, -8.166667518702819706, -8.995218007635861213 ) ) ;
#30151=CARTESIAN_POINT ( 'NONE',  ( 118.2420214775786320, -3.383040157471821630, -19.15922257007629170 ) ) ;
#30152=CARTESIAN_POINT ( 'NONE',  ( 114.6115148109119986, -3.383040157471821630, -19.15922257007629170 ) ) ;
#30153=CARTESIAN_POINT ( 'NONE',  ( 116.9940348109119839, -0.1624402480850797581, -16.17319339645315424 ) ) ;
#30154=CARTESIAN_POINT ( 'NONE',  ( 124.4819548109119722, -2.084020599724406786, -8.691656652584148546 ) ) ;
#30155=CARTESIAN_POINT ( 'NONE',  ( 114.1009748109119784, -4.089484607189486809, -7.948022111789456723 ) ) ;
#30157=CARTESIAN_POINT ( 'NONE',  ( 122.7801548109119665, -6.222761293078241884, -8.102969835052219238 ) ) ;
#30158=PLANE ( 'NONE',  #40952 ) ;
#30163=ADVANCED_FACE ( 'NONE', ( #28948 ), #23240, .T. ) ;
#30165=CARTESIAN_POINT ( 'NONE',  ( 123.2906948109119867, -8.166667518702819706, -8.995218007635861213 ) ) ;
#30167=CARTESIAN_POINT ( 'NONE',  ( 119.4900081442453086, -1.834011780172310813, -8.268836392978581529 ) ) ;
#30168=CARTESIAN_POINT ( 'NONE',  ( 113.2500748109119968, -3.505236298600246325, -18.68346056562440793 ) ) ;
#30170=CARTESIAN_POINT ( 'NONE',  ( 121.1350814775786233, 0.5811942927096110934, -14.16772938898807510 ) ) ;
#30171=CARTESIAN_POINT ( 'NONE',  ( 121.7023481442452777, -9.261995988541697145, -16.69588392320189030 ) ) ;
#30173=CARTESIAN_POINT ( 'NONE',  ( 125.6164881442453094, -9.565557343593413364, -10.61323700422348004 ) ) ;
#30176=ORIENTED_EDGE ( 'NONE', *, *, #16476, .T. ) ;
#30178=CARTESIAN_POINT ( 'NONE',  ( 118.4645848073892722, -1.081026697600512732, -17.18181821144401056 ) ) ;
#30179=CARTESIAN_POINT ( 'NONE',  ( 123.0637881442452937, -8.899110576539710493, -16.42337572283490132 ) ) ;
#30182=CARTESIAN_POINT ( 'NONE',  ( 117.5045748109119756, -9.859900752359374465, -12.68260735090039404 ) ) ;
#30185=CARTESIAN_POINT ( 'NONE',  ( 112.1155414775786454, -10.15424416112533912, -14.75197769757731336 ) ) ;
#30186=CARTESIAN_POINT ( 'NONE',  ( 122.8936081442453059, 0.2603800115204892296, -16.42320221600525088 ) ) ;
#30188=CARTESIAN_POINT ( 'NONE',  ( 123.4608748109119745, 0.4262465694468514643, -12.03445270309931736 ) ) ;
#30189=CARTESIAN_POINT ( 'NONE',  ( 114.4980614775786592, -7.893985811506177619, -18.51759400769804742 ) ) ;
#30190=CARTESIAN_POINT ( 'NONE',  ( 124.5386814775786206, -5.638512984488999180, -18.83840828888717311 ) ) ;
#30191=CARTESIAN_POINT ( 'NONE',  ( 124.5386814775786206, -4.153390946401325223, -8.397313243818185668 ) ) ;
#30192=ORIENTED_EDGE ( 'NONE', *, *, #32304, .F. ) ;
#30193=CARTESIAN_POINT ( 'NONE',  ( 123.3089807241438933, -2.443475742715334853, -17.86549347949429389 ) ) ;
#30194=CARTESIAN_POINT ( 'NONE',  ( 125.0492214775786266, -6.344957434206665248, -7.627207830600338134 ) ) ;
#30195=CARTESIAN_POINT ( 'NONE',  ( 114.3278814775786429, 0.1319031606808879209, -14.10382304977623669 ) ) ;
#30196=CARTESIAN_POINT ( 'NONE',  ( 111.4348214775786801, -3.505236298600246325, -18.68346056562440793 ) ) ;
#30199=ORIENTED_EDGE ( 'NONE', *, *, #21172, .F. ) ;
#30201=STYLED_ITEM('',(#45190),#36408);
#30204=CARTESIAN_POINT ( 'NONE',  ( 119.4332814775786318, -8.899110576539710493, -16.42337572283490132 ) ) ;
#30205=CARTESIAN_POINT ( 'NONE',  ( 112.5693548109119888, 0.4262465694468514643, -12.03445270309931736 ) ) ;
#30206=CARTESIAN_POINT ( 'NONE',  ( 126.8396850857285756, -0.1243826821608716021, -10.99732104622448681 ) ) ;
#30208=CARTESIAN_POINT ( 'NONE',  ( 115.6349575202278146, -2.239543233855044058, -18.13706010537467606 ) ) ;
#30209=CARTESIAN_POINT ( 'NONE',  ( 117.2209414775786485, -2.084020599724406786, -8.691656652584148546 ) ) ;
#30211=CARTESIAN_POINT ( 'NONE',  ( 113.2500748109119968, -3.505236298600246325, -18.68346056562440793 ) ) ;
#30215=CARTESIAN_POINT ( 'NONE',  ( 121.2485348109119769, -0.4660016031367893996, -10.09054647747474043 ) ) ;
#30217=CARTESIAN_POINT ( 'NONE',  ( 112.2289948109119848, -1.834011780172310813, -8.268836392978581529 ) ) ;
#30222=CARTESIAN_POINT ( 'NONE',  ( 125.1626748109119802, -0.1624402480850797581, -16.17319339645315424 ) ) ;
#30223=CARTESIAN_POINT ( 'NONE',  ( 119.5467348109119712, -5.574606645277164318, -18.38911715685844683 ) ) ;
#30224=CARTESIAN_POINT ( 'NONE',  ( 119.3722114740559448, -1.081026697600536046, -17.18181821144402832 ) ) ;
#30227=CARTESIAN_POINT ( 'NONE',  ( 112.7962614775786676, -6.222761293078241884, -8.102969835052219238 ) ) ;
#30231=CARTESIAN_POINT ( 'NONE',  ( 122.4397948109119767, -9.988377603198976828, -10.36322818467138340 ) ) ;
#30232=CARTESIAN_POINT ( 'NONE',  ( 122.3263414775786373, -6.344957434206665248, -7.627207830600338134 ) ) ;
#30234=CARTESIAN_POINT ( 'NONE',  ( 118.1285681442453068, -7.893985811506177619, -18.51759400769804742 ) ) ;
#30235=CARTESIAN_POINT ( 'NONE',  ( 113.1366214775786432, -1.834011780172310813, -8.268836392978581529 ) ) ;
#30237=CARTESIAN_POINT ( 'NONE',  ( 113.4202548109119846, 0.1319031606808879209, -14.10382304977623669 ) ) ;
#30239=CARTESIAN_POINT ( 'NONE',  ( 111.6050014775786536, 0.1319031606808879209, -14.10382304977623669 ) ) ;
#30240=CARTESIAN_POINT ( 'NONE',  ( 121.2485348109119769, -0.4660016031367893996, -10.09054647747474043 ) ) ;
#30241=CARTESIAN_POINT ( 'NONE',  ( 113.5904348109119866, -7.893985811506177619, -18.51759400769804742 ) ) ;
#30242=CARTESIAN_POINT ( 'NONE',  ( 113.1933481442453058, -5.574606645277164318, -18.38911715685844683 ) ) ;
#30244=CARTESIAN_POINT ( 'NONE',  ( 119.3198281442452924, -9.859900752359374465, -12.68260735090039404 ) ) ;
#30245=CARTESIAN_POINT ( 'NONE',  ( 111.6617281442453304, 0.4262465694468514643, -12.03445270309931736 ) ) ;
#30247=CARTESIAN_POINT ( 'NONE',  ( 121.4187148109119789, -3.505236298600246325, -18.68346056562440793 ) ) ;
#30251=CARTESIAN_POINT ( 'NONE',  ( 121.6456214775786293, -10.63000616557722466, -14.87417383870573495 ) ) ;
#30255=CARTESIAN_POINT ( 'NONE',  ( 112.6260814775786514, -9.261995988541698921, -16.69588392320189030 ) ) ;
#30259=CARTESIAN_POINT ( 'NONE',  ( 137.3872759786617053, -6.189116507261323008, -18.35186304430243709 ) ) ;
#30261=CARTESIAN_POINT ( 'NONE',  ( 125.0889430353348786, -2.469647041402692977, -17.83064248237198868 ) ) ;
#30263=CARTESIAN_POINT ( 'NONE',  ( 123.0637881442452937, -8.899110576539710493, -16.42337572283490132 ) ) ;
#30266=CARTESIAN_POINT ( 'NONE',  ( 123.4608748109119745, -10.63000616557722466, -14.87417383870573495 ) ) ;
#30267=CARTESIAN_POINT ( 'NONE',  ( 118.6958348109119754, -6.344957434206665248, -7.627207830600338134 ) ) ;
#30269=CARTESIAN_POINT ( 'NONE',  ( 113.1366214775786432, -7.643976991954077427, -18.09477374809248928 ) ) ;
#30271=CARTESIAN_POINT ( 'NONE',  ( 112.6260814775786514, -9.261995988541697145, -16.69588392320189030 ) ) ;
#30272=CARTESIAN_POINT ( 'NONE',  ( 122.9503348109119827, 0.5811942927096110934, -14.16772938898807510 ) ) ;
#30276=CARTESIAN_POINT ( 'NONE',  ( 117.5045748109119756, -9.859900752359374465, -12.68260735090039404 ) ) ;
#30277=CARTESIAN_POINT ( 'NONE',  ( 115.4624148109119943, -4.153390946401321671, -8.397313243818183892 ) ) ;
#30278=CARTESIAN_POINT ( 'NONE',  ( 136.7911968929755062, -2.114665601771191561, -18.30335334318372276 ) ) ;
#30282=CARTESIAN_POINT ( 'NONE',  ( 125.4463081442452932, -4.153390946401325223, -8.397313243818185668 ) ) ;
#30288=ORIENTED_EDGE ( 'NONE', *, *, #36815, .F. ) ;
#30289=CARTESIAN_POINT ( 'NONE',  ( 119.5467348109119712, -4.089484607189486809, -7.948022111789456723 ) ) ;
#30290=CARTESIAN_POINT ( 'NONE',  ( 125.0492214775786266, -3.505236298600246325, -18.68346056562440793 ) ) ;
#30291=CARTESIAN_POINT ( 'NONE',  ( 115.8027748109119841, -8.899110576539710493, -16.42337572283490132 ) ) ;
#30294=CARTESIAN_POINT ( 'NONE',  ( 120.2841814775786276, 0.9020085738987339008, -11.91225656197089222 ) ) ;
#30295=CARTESIAN_POINT ( 'NONE',  ( 114.9518748109119883, -1.834011780172310813, -8.268836392978581529 ) ) ;
#30297=CARTESIAN_POINT ( 'NONE',  ( 125.5030348109119558, -3.383040157471821630, -19.15922257007629170 ) ) ;
#30300=CARTESIAN_POINT ( 'NONE',  ( 119.5467348109119712, -4.089484607189486809, -7.948022111789456723 ) ) ;
#30302=CARTESIAN_POINT ( 'NONE',  ( 113.0231681442453180, -10.15424416112533912, -14.75197769757731336 ) ) ;
#30305=CARTESIAN_POINT ( 'NONE',  ( 113.8173414775786512, 0.2603800115204892296, -16.42320221600525088 ) ) ;
#30307=CARTESIAN_POINT ( 'NONE',  ( 119.9438214775786378, -7.893985811506177619, -18.51759400769804742 ) ) ;
#30311=CARTESIAN_POINT ( 'NONE',  ( 115.8027748109119841, -8.899110576539710493, -16.42337572283490132 ) ) ;
#30312=CARTESIAN_POINT ( 'NONE',  ( 136.7036351579039035, -2.784237195798857645, -8.139038447917522845 ) ) ;
#30313=CARTESIAN_POINT ( 'NONE',  ( 119.3765548109119834, -10.15424416112533912, -14.75197769757731336 ) ) ;
#30316=B_SPLINE_CURVE_WITH_KNOTS ( 'NONE', 3,
 ( #32415, #24912, #11908, #11235, #728, #39267, #39717, #35604, #4154, #29231 ),
 .UNSPECIFIED., .F., .F.,
 ( 4, 3, 3, 4 ),
 ( 0.000000000000000000, 0.0001671877548681280042, 0.0003343755096277710101, 0.0006463528481650629171 ),
 .UNSPECIFIED. ) ;
#30317=CARTESIAN_POINT ( 'NONE',  ( 115.8595014775786609, -7.643976991954077427, -18.09477374809248928 ) ) ;
#30318=CARTESIAN_POINT ( 'NONE',  ( 116.5402214775786405, 0.2603800115204892296, -16.42320221600525088 ) ) ;
#30320=CARTESIAN_POINT ( 'NONE',  ( 125.6732148109119862, -9.859900752359378018, -12.68260735090039759 ) ) ;
#30321=CARTESIAN_POINT ( 'NONE',  ( 115.9729548109119861, -3.505236298600246325, -18.68346056562440793 ) ) ;
#30322=CARTESIAN_POINT ( 'NONE',  ( 123.1772414775786189, -4.089484607189486809, -7.948022111789456723 ) ) ;
#30323=CARTESIAN_POINT ( 'NONE',  ( 121.9859814775786333, 0.2603800115204892296, -16.42320221600525088 ) ) ;
#30325=CARTESIAN_POINT ( 'NONE',  ( 113.0231681442453322, 0.9020085738987339008, -11.91225656197089222 ) ) ;
#30332=CARTESIAN_POINT ( 'NONE',  ( 120.3409081442453044, -0.4660016031367893996, -10.09054647747474043 ) ) ;
#30334=CARTESIAN_POINT ( 'NONE',  ( 125.6732148109119862, 0.5811942927096110934, -14.16772938898807510 ) ) ;
#30335=DIRECTION ( 'NONE',  ( 0.000000000000000000, 0.7996358532186282897, 0.6004852223388319477 ) ) ;
#30336=CARTESIAN_POINT ( 'NONE',  ( 114.4413348109119823, -0.8288870151387760510, -10.36305467784173118 ) ) ;
#30338=CARTESIAN_POINT ( 'NONE',  ( 124.7088614775786226, -9.565557343593420470, -10.61323700422348715 ) ) ;
#30340=CARTESIAN_POINT ( 'NONE',  ( 120.5110881442453206, -6.344957434206665248, -7.627207830600338134 ) ) ;
#30343=CARTESIAN_POINT ( 'NONE',  ( 119.3046025628257070, -2.263366209404225504, -18.10533625161308180 ) ) ;
#30345=CARTESIAN_POINT ( 'NONE',  ( 112.4559014775786494, -9.988377603198976828, -10.36322818467138340 ) ) ;
#30346=CARTESIAN_POINT ( 'NONE',  ( 122.0994348109119443, -10.15424416112533912, -14.75197769757731336 ) ) ;
#30347=CARTESIAN_POINT ( 'NONE',  ( 118.0718414775786300, -9.261995988541697145, -16.69588392320189030 ) ) ;
#30348=CARTESIAN_POINT ( 'NONE',  ( 113.1366214775786432, -7.643976991954077427, -18.09477374809248928 ) ) ;
#30349=CARTESIAN_POINT ( 'NONE',  ( 114.2711548109119803, -9.988377603198976828, -10.36322818467138340 ) ) ;
#30350=DIRECTION ( 'NONE',  ( 0.000000000000000000, 0.6004852223388321697, -0.7996358532186279566 ) ) ;
#30351=CARTESIAN_POINT ( 'NONE',  ( 125.7299414775786346, -10.15424416112533912, -14.75197769757731336 ) ) ;
#30352=CARTESIAN_POINT ( 'NONE',  ( 118.1852948109119836, -4.153390946401325223, -8.397313243818185668 ) ) ;
#30357=CARTESIAN_POINT ( 'NONE',  ( 112.0020881442453344, 0.2603800115204892296, -16.42320221600525088 ) ) ;
#30358=CARTESIAN_POINT ( 'NONE',  ( 122.0427081442452817, -9.859900752359378018, -12.68260735090039759 ) ) ;
#30364=CARTESIAN_POINT ( 'NONE',  ( 119.8303681442453126, -10.63000616557722466, -14.87417383870573495 ) ) ;
#30366=CARTESIAN_POINT ( 'NONE',  ( 116.3700414775786527, -4.153390946401321671, -8.397313243818183892 ) ) ;
#30369=CARTESIAN_POINT ( 'NONE',  ( 112.3991748109119868, -8.166667518702817929, -8.995218007635859436 ) ) ;
#30370=B_SPLINE_CURVE_WITH_KNOTS ( 'NONE', 3,
 ( #30557, #44478, #2282, #5702, #20531, #23043, #2966, #40376, #33503, #41068 ),
 .UNSPECIFIED., .F., .F.,
 ( 4, 3, 3, 4 ),
 ( 0.000000000000000000, 0.0001671877548681309858, 0.0003343755096277739917, 0.0006463528481650629171 ),
 .UNSPECIFIED. ) ;
#30371=CARTESIAN_POINT ( 'NONE',  ( 121.3052614775786111, -7.643976991954077427, -18.09477374809248928 ) ) ;
#30372=CARTESIAN_POINT ( 'NONE',  ( 135.3184548109119874, 0.6402711692277546218, -15.78131322003127579 ) ) ;
#30374=CARTESIAN_POINT ( 'NONE',  ( 119.6601881442453106, -8.166667518702819706, -8.995218007635861213 ) ) ;
#30376=CARTESIAN_POINT ( 'NONE',  ( 120.5678148109119832, -8.166667518702819706, -8.995218007635861213 ) ) ;
#30377=CARTESIAN_POINT ( 'NONE',  ( 114.7249681442453237, 0.2603800115204892296, -16.42320221600525088 ) ) ;
#30378=CARTESIAN_POINT ( 'NONE',  ( 119.6601881442453106, -1.833838273342659253, -17.42832698103878286 ) ) ;
#30379=CARTESIAN_POINT ( 'NONE',  ( 125.3328548109119964, -0.8288870151387760510, -10.36305467784173118 ) ) ;
#30382=CARTESIAN_POINT ( 'NONE',  ( 122.0427081442452817, -9.859900752359378018, -12.68260735090039759 ) ) ;
#30383=CARTESIAN_POINT ( 'NONE',  ( 126.2184548109119788, -4.863998795839242995, -13.39321520033831447 ) ) ;
#30389=CARTESIAN_POINT ( 'NONE',  ( 123.3474214775786209, -9.988377603198976828, -10.36322818467138340 ) ) ;
#30390=CARTESIAN_POINT ( 'NONE',  ( 124.6521348109119884, -7.894159318335828068, -9.358103419637847864 ) ) ;
#30392=CARTESIAN_POINT ( 'NONE',  ( 123.5743281442453139, -7.893985811506177619, -18.51759400769804742 ) ) ;
#30393=CARTESIAN_POINT ( 'NONE',  ( 112.1722681442453222, -8.899110576539710493, -16.42337572283490132 ) ) ;
#30395=CARTESIAN_POINT ( 'NONE',  ( 118.3554748109119998, 0.2603800115204892296, -16.42320221600525088 ) ) ;
#30396=CARTESIAN_POINT ( 'NONE',  ( 122.8368814775786291, -1.561330072975668948, -17.79121239304076951 ) ) ;
#30397=CARTESIAN_POINT ( 'NONE',  ( 111.2184548109119788, -8.862178061932382889, -16.39564131203247399 ) ) ;
#30398=CARTESIAN_POINT ( 'NONE',  ( 123.5743281442453139, -2.084020599724406786, -8.691656652584148546 ) ) ;
#30401=ORIENTED_EDGE ( 'NONE', *, *, #12622, .T. ) ;
#30404=CARTESIAN_POINT ( 'NONE',  ( 123.8012348109119642, -9.565557343593413364, -10.61323700422348004 ) ) ;
#30407=CARTESIAN_POINT ( 'NONE',  ( 118.9227414775786542, 0.4262465694468514643, -12.03445270309931736 ) ) ;
#30409=CARTESIAN_POINT ( 'NONE',  ( 117.5045748109119756, -9.859900752359374465, -12.68260735090039404 ) ) ;
#30410=CARTESIAN_POINT ( 'NONE',  ( 123.4608748109119745, -10.63000616557722466, -14.87417383870573495 ) ) ;
#30413=CARTESIAN_POINT ( 'NONE',  ( 123.8579614775786126, -9.859900752359378018, -12.68260735090039759 ) ) ;
#30414=CARTESIAN_POINT ( 'NONE',  ( 118.7525614775786380, -8.166667518702819706, -8.995218007635861213 ) ) ;
#30415=CARTESIAN_POINT ( 'NONE',  ( 124.9357681442453014, -1.834011780172310813, -8.268836392978581529 ) ) ;
#30416=CARTESIAN_POINT ( 'NONE',  ( 125.0492214775786266, -3.505236298600246325, -18.68346056562440793 ) ) ;
#30419=CARTESIAN_POINT ( 'NONE',  ( 125.3895814775786448, -7.893985811506177619, -18.51759400769804742 ) ) ;
#30420=CARTESIAN_POINT ( 'NONE',  ( 113.1933481442453058, -5.574606645277164318, -18.38911715685844683 ) ) ;
#30422=CARTESIAN_POINT ( 'NONE',  ( 123.5743281442453139, -7.893985811506177619, -18.51759400769804742 ) ) ;
#30430=CARTESIAN_POINT ( 'NONE',  ( 119.0361948109119652, -2.084020599724406786, -8.691656652584148546 ) ) ;
#30431=CARTESIAN_POINT ( 'NONE',  ( 112.4559014775786778, -0.1624402480850797581, -16.17319339645315424 ) ) ;
#30432=CARTESIAN_POINT ( 'NONE',  ( 125.2761281442452912, 0.4262465694468504651, -12.03445270309929604 ) ) ;
#30435=CARTESIAN_POINT ( 'NONE',  ( 120.1707281442453166, -9.565557343593413364, -10.61323700422348004 ) ) ;
#30438=CARTESIAN_POINT ( 'NONE',  ( 111.8886348109120092, -6.222761293078241884, -8.102969835052219238 ) ) ;
#30440=CARTESIAN_POINT ( 'NONE',  ( 123.4608748109119745, -10.63000616557722466, -14.87417383870573495 ) ) ;
#30441=CARTESIAN_POINT ( 'NONE',  ( 112.1155414775786454, 0.9020085738987339008, -11.91225656197089222 ) ) ;
#30443=CARTESIAN_POINT ( 'NONE',  ( 113.7038881442453402, -3.383040157471821630, -19.15922257007629170 ) ) ;
#30444=CARTESIAN_POINT ( 'NONE',  ( 113.6623870589982346, -1.063912429576153063, -17.20460841810474761 ) ) ;
#30446=CARTESIAN_POINT ( 'NONE',  ( 124.5386814775786206, -4.153390946401325223, -8.397313243818185668 ) ) ;
#30447=CARTESIAN_POINT ( 'NONE',  ( 120.9081748109119872, -4.153390946401325223, -8.397313243818185668 ) ) ;
#30452=CARTESIAN_POINT ( 'NONE',  ( 113.6471614775786492, -4.153390946401321671, -8.397313243818183892 ) ) ;
#30456=CARTESIAN_POINT ( 'NONE',  ( 124.5386814775786206, -5.638512984488999180, -18.83840828888717311 ) ) ;
#30457=CARTESIAN_POINT ( 'NONE',  ( 123.4041481442452834, -10.30919188438810075, -12.61870101168855918 ) ) ;
#30459=CARTESIAN_POINT ( 'NONE',  ( 121.8725281442453223, -3.383040157471821630, -19.15922257007629170 ) ) ;
#30460=CARTESIAN_POINT ( 'NONE',  ( 112.7395348109119766, -5.638512984488999180, -18.83840828888717311 ) ) ;
#30462=CARTESIAN_POINT ( 'NONE',  ( 115.0086014775786509, -5.574606645277164318, -18.38911715685844683 ) ) ;
#30463=CARTESIAN_POINT ( 'NONE',  ( 125.7299414775786346, 0.9020085738987339008, -11.91225656197089222 ) ) ;
#30464=CARTESIAN_POINT ( 'NONE',  ( 122.4397948109119767, -9.988377603198976828, -10.36322818467138340 ) ) ;
#30465=CARTESIAN_POINT ( 'NONE',  ( 114.2144281442453178, -8.166667518702817929, -8.995218007635859436 ) ) ;
#30466=CARTESIAN_POINT ( 'NONE',  ( 113.3068014775786594, -1.833838273342658809, -17.42832698103878286 ) ) ;
#30468=CARTESIAN_POINT ( 'NONE',  ( 116.9373081442452929, -1.833838273342659253, -17.42832698103878286 ) ) ;
#30472=CARTESIAN_POINT ( 'NONE',  ( 123.9714148109119805, -8.899110576539710493, -16.42337572283490132 ) ) ;
#30476=DIRECTION ( 'NONE',  ( 0.000000000000000000, 0.6004852223388321697, -0.7996358532186279566 ) ) ;
#30477=CARTESIAN_POINT ( 'NONE',  ( 126.1270281442452870, -10.30919188438810075, -12.61870101168855918 ) ) ;
#30479=CARTESIAN_POINT ( 'NONE',  ( 112.5693548109119888, -10.63000616557722466, -14.87417383870573495 ) ) ;
#30483=CARTESIAN_POINT ( 'NONE',  ( 115.4385020163423263, -1.087735405160632718, -17.17288456429612253 ) ) ;
#30484=CARTESIAN_POINT ( 'NONE',  ( 118.5823814775786360, -1.834011780172310813, -8.268836392978581529 ) ) ;
#30489=CARTESIAN_POINT ( 'NONE',  ( 121.3052614775786111, -7.643976991954077427, -18.09477374809248928 ) ) ;
#30492=CARTESIAN_POINT ( 'NONE',  ( 123.7445081442452874, -1.561330072975668948, -17.79121239304076951 ) ) ;
#30493=CARTESIAN_POINT ( 'NONE',  ( 120.9649014775786355, -3.383040157471821630, -19.15922257007629170 ) ) ;
#30495=CARTESIAN_POINT ( 'NONE',  ( 112.7962614775786676, -6.222761293078241884, -8.102969835052219238 ) ) ;
#30496=CARTESIAN_POINT ( 'NONE',  ( 123.3474214775786209, -9.988377603198976828, -10.36322818467138340 ) ) ;
#30500=CARTESIAN_POINT ( 'NONE',  ( 117.3911214775786505, -7.894159318335828068, -9.358103419637847864 ) ) ;
#30501=CARTESIAN_POINT ( 'NONE',  ( 118.2987481442453088, -7.894159318335828068, -9.358103419637847864 ) ) ;
#30506=CARTESIAN_POINT ( 'NONE',  ( 114.3278814775786429, -10.30919188438810075, -12.61870101168855918 ) ) ;
#30514=CARTESIAN_POINT ( 'NONE',  ( 116.7671281442453335, -1.834011780172310813, -8.268836392978581529 ) ) ;
#30515=CARTESIAN_POINT ( 'NONE',  ( 122.7801548109119665, -6.222761293078241884, -8.102969835052219238 ) ) ;
#30516=AXIS2_PLACEMENT_3D ( 'NONE', #8809, #12468, #25918 ) ;
#30517=CARTESIAN_POINT ( 'NONE',  ( 119.7736414775786358, 0.1319031606808879209, -14.10382304977623669 ) ) ;
#30520=CARTESIAN_POINT ( 'NONE',  ( 121.8725281442453223, -3.383040157471821630, -19.15922257007629170 ) ) ;
#30521=CARTESIAN_POINT ( 'NONE',  ( 118.8660148109119774, -10.30919188438810075, -12.61870101168855918 ) ) ;
#30523=CARTESIAN_POINT ( 'NONE',  ( 113.9307948109119764, -10.15424416112533912, -14.75197769757731336 ) ) ;
#30526=CARTESIAN_POINT ( 'NONE',  ( 117.0507614775786465, -10.30919188438810075, -12.61870101168855918 ) ) ;
#30527=CARTESIAN_POINT ( 'NONE',  ( 114.7249681442453237, -9.565557343593413364, -10.61323700422348004 ) ) ;
#30529=CARTESIAN_POINT ( 'NONE',  ( 112.4559014775786494, -9.988377603198976828, -10.36322818467138340 ) ) ;
#30531=CARTESIAN_POINT ( 'NONE',  ( 121.5888948109119809, -10.30919188438810075, -12.61870101168855918 ) ) ;
#30532=CARTESIAN_POINT ( 'NONE',  ( 138.2184548109119930, 0.7167481258041168424, -11.18974888642104659 ) ) ;
#30533=CARTESIAN_POINT ( 'NONE',  ( 112.7962614775786676, -6.222761293078241884, -8.102969835052219238 ) ) ;
#30535=CARTESIAN_POINT ( 'NONE',  ( 114.5547881442453217, -4.153390946401321671, -8.397313243818183892 ) ) ;
#30536=CARTESIAN_POINT ( 'NONE',  ( 123.5807492164245360, -4.317385761257377830, -15.37007627435306389 ) ) ;
#30537=CARTESIAN_POINT ( 'NONE',  ( 117.6180281442453150, -8.899110576539710493, -16.42337572283490132 ) ) ;
#30540=CARTESIAN_POINT ( 'NONE',  ( 114.0442481442453300, -7.643976991954077427, -18.09477374809248928 ) ) ;
#30541=CARTESIAN_POINT ( 'NONE',  ( 115.1220548109119761, -8.166667518702817929, -8.995218007635861213 ) ) ;
#30544=CARTESIAN_POINT ( 'NONE',  ( 112.2857214775786474, -4.089484607189486809, -7.948022111789456723 ) ) ;
#30545=CARTESIAN_POINT ( 'NONE',  ( 114.8951481442453115, -8.899110576539710493, -16.42337572283490132 ) ) ;
#30546=CARTESIAN_POINT ( 'NONE',  ( 123.4041481442452834, -10.30919188438810075, -12.61870101168855918 ) ) ;
#30547=CARTESIAN_POINT ( 'NONE',  ( 115.8595014775786609, -7.643976991954077427, -18.09477374809248928 ) ) ;
#30549=CARTESIAN_POINT ( 'NONE',  ( 112.4559014775786494, -9.988377603198976828, -10.36322818467138340 ) ) ;
#30554=CARTESIAN_POINT ( 'NONE',  ( 117.3343948109119737, -3.383040157471821630, -19.15922257007629170 ) ) ;
#30557=CARTESIAN_POINT ( 'NONE',  ( 120.5468302440515203, -2.467220198592778413, -17.83387418641524391 ) ) ;
#30558=CARTESIAN_POINT ( 'NONE',  ( 116.7671281442453335, -7.643976991954077427, -18.09477374809248928 ) ) ;
#30559=( BOUNDED_SURFACE ( )  B_SPLINE_SURFACE ( 1, 2, ( 
 ( #37750, #26591, #17019, #44608, #37518, #44833, #12922, #43923, #16565, #26818, #30689, #6520, #44157, #40730, #33863, #22937, #6290, #20211, #30460, #13372, #19745, #41191, #19975, #13143, #5825, #30235, #9265, #9486, #27276, #20435, #34319, #36830, #27046, #3093, #40504, #30911, #23400, #37285, #5600, #6054, #37054, #2633, #9718, #33400, #2174, #40964, #23632, #33631, #2405, #18122, #10395, #20876, #20660, #38407, #3753, #42079, #14477, #21541, #35201, #34536, #14033, #17675, #17237, #6750, #3536, #17451, #10618, #24520, #3315, #31571, #14253, #28170, #3976, #38859, #7178, #17898, #340, #10838, #34965, #45053, #24734, #41857, #38623, #27947, #32017, #21317, #42298, #13590, #11061, #24305, #27500, #7399, #31795, #4204, #31129, #41420, #10175, #13813, #24081, #21088, #24963, #567, #28386, #7627, #35428, #37974, #27724, #41640, #38192, #31346, #120, #6968, #34753, #18796, #43195, #8754, #32685, #4878, #19245, #25859, #1676, #8088, #36555, #35880, #8310, #15599, #36107, #11732, #25419, #22436, #8534, #39988, #28616, #1455, #5329, #780, #36329, #4650, #5099, #19014, #18350, #18572, #32464, #32900, #21990, #15375, #22211, #1013, #11286, #29279, #35661, #21767, #32242, #14929, #4433, #28840, #42751, #11515, #1239, #39764, #29502, #43417, #14702, #11960, #12183, #39320, #26084, #15151, #29057, #22659, #42965, #25645, #42525, #25194, #39092, #7861, #39548, #6001, #26769, #9899, #37699, #29957, #40450, #40220, #12869, #23343, #16511, #34043, #41139, #9663, #8985, #33577, #37227, #36777, #26312, #23121, #36998, #30186, #44104, #22883, #19924, #33810, #2581, #23582, #13315, #40679, #37465, #30410, #44331, #9430, #19465, #13091, #16284, #26989, #2352, #6471, #40909, #16740, #33128, #30635, #43872, #1897, #6238, #20160, #23811, #5548, #15825, #29724, #33348, #43638, #2811, #44551, #27222, #12412, #2122, #16051, #12644, #26540, #9212, #5769, #19690, #24249, #31076, #38569, #38353, #17623, #28331, #7129, #24461, #38803, #288, #21264, #27672, #11008, #10344, #27893, #35145 ),
 ( #31741, #6913, #17404, #3924, #45003, #41370, #42021, #17186, #34268, #21040, #3042, #10785, #31293, #10126, #17844, #67, #24907, #20382, #13979, #13763, #24682, #28116, #14421, #16964, #10565, #30858, #44781, #7347, #38141, #510, #42243, #37920, #20822, #34701, #13540, #41587, #34913, #41807, #20607, #27448, #3704, #24030, #6696, #34482, #3261, #3488, #31516, #14199, #22382, #36278, #21486, #42915, #5045, #21713, #18960, #21932, #42692, #32850, #35824, #42469, #29006, #36053, #35371, #29226, #1183, #25586, #15097, #29445, #12129, #4372, #14874, #14647, #32410, #11677, #4820, #8478, #15540, #43133, #28562, #8025, #39488, #11232, #724, #11461, #25365, #4598, #18519, #25140, #8253, #22159, #18743, #11903, #1619, #32634, #25804, #1400, #15316, #39714, #39034, #43360, #26032, #7573, #4149, #18067, #31958, #7805, #35600, #18291, #32186, #958, #28786, #39261, #30573, #33069, #44493, #8698, #1841, #22603, #23060, #23523, #26710, #30131, #30352, #9607, #9154, #2525, #40392, #37410, #12583, #43818, #5490, #13032, #12808, #37170, #2754, #40620, #44044, #13258, #19868, #40852, #2073, #39937, #29902, #2298, #6180, #9377, #16452, #20100, #33985, #23286, #36946, #26488, #5716, #19634, #16679, #5945, #12355, #26930, #36503, #33518, #16227, #5272, #19410, #15770, #44277, #36721, #19190, #33757, #29673, #43585, #26255, #40165, #8927, #22829, #33297, #15996, #10286, #3207, #11, #38514, #13486, #38082, #41312, #7291, #10507, #24632, #35086, #20323, #44726, #34646, #34207, #30801, #21208, #10072, #37859, #17350, #24408, #23973, #24191, #27832, #3432, #6860, #10733, #27388, #17788, #228, #38297, #451, #13708, #6635, #31240, #27615, #31460, #3866, #44949, #41528, #13923, #23751, #7076, #20986, #41743, #34859, #20547, #41966, #20767, #3647, #34426, #17132, #6415, #31682, #27162, #16909, #41084, #31019, #17566, #14142, #28057, #9840, #37641, #2981, #4767, #42190, #14367, #11849, #18904, #25531, #25082, #21431, #32793, #32358, #21654, #24853, #673, #22329, #7743, #28281, #10950 ) ),
 .UNSPECIFIED., .F., .F., .F. ) 
 B_SPLINE_SURFACE_WITH_KNOTS ( ( 2, 2 ),
 ( 3, 2, 2, 2, 2, 2, 2, 2, 2, 2, 2, 2, 2, 2, 2, 2, 2, 2, 2, 2, 2, 2, 2, 2, 2, 2, 2, 2, 2, 2, 2, 2, 2, 2, 2, 2, 2, 2, 2, 2, 2, 2, 2, 2, 2, 2, 2, 2, 2, 2, 2, 2, 2, 2, 2, 2, 2, 2, 2, 2, 2, 2, 2, 2, 2, 2, 2, 2, 2, 2, 2, 2, 2, 2, 2, 2, 2, 2, 2, 2, 2, 2, 2, 2, 2, 2, 2, 2, 2, 2, 2, 2, 2, 2, 2, 2, 2, 2, 2, 2, 2, 2, 2, 2, 2, 2, 2, 2, 2, 2, 2, 2, 2, 2, 2, 2, 2, 2, 2, 2, 2, 2, 2, 2, 2, 2, 2, 2, 3 ),
 ( 0.000000000000000000, 1.000000000000000000 ),
 ( 0.000000000000000000, 0.007812500000000000000, 0.01562500000000000000, 0.02343750000000000000, 0.03125000000000000000, 0.03906250000000000000, 0.04687500000000000000, 0.05468750000000000000, 0.06250000000000000000, 0.07031250000000000000, 0.07812500000000000000, 0.08593750000000000000, 0.09375000000000000000, 0.1015625000000000000, 0.1093750000000000000, 0.1171875000000000000, 0.1250000000000000000, 0.1328125000000000000, 0.1406250000000000000, 0.1484375000000000000, 0.1562500000000000000, 0.1640625000000000000, 0.1718750000000000000, 0.1796875000000000000, 0.1875000000000000000, 0.1953125000000000000, 0.2031250000000000000, 0.2109375000000000000, 0.2187500000000000000, 0.2265625000000000000, 0.2343750000000000000, 0.2421875000000000000, 0.2500000000000000000, 0.2578125000000000000, 0.2656250000000000000, 0.2734375000000000000, 0.2812500000000000000, 0.2890625000000000000, 0.2968750000000000000, 0.3046875000000000000, 0.3125000000000000000, 0.3203125000000000000, 0.3281250000000000000, 0.3359375000000000000, 0.3437500000000000000, 0.3515625000000000000, 0.3593750000000000000, 0.3671875000000000000, 0.3750000000000000000, 0.3828125000000000000, 0.3906250000000000000, 0.3984375000000000000, 0.4062500000000000000, 0.4140625000000000000, 0.4218750000000000000, 0.4296875000000000000, 0.4375000000000000000, 0.4453125000000000000, 0.4531250000000000000, 0.4609375000000000000, 0.4687500000000000000, 0.4765625000000000000, 0.4843750000000000000, 0.4921875000000000000, 0.5000000000000000000, 0.5078125000000000000, 0.5156250000000000000, 0.5234375000000000000, 0.5312500000000000000, 0.5390625000000000000, 0.5468750000000000000, 0.5546875000000000000, 0.5625000000000000000, 0.5703125000000000000, 0.5781250000000000000, 0.5859375000000000000, 0.5937500000000000000, 0.6015625000000000000, 0.6093750000000000000, 0.6171875000000000000, 0.6250000000000000000, 0.6328125000000000000, 0.6406250000000000000, 0.6484375000000000000, 0.6562500000000000000, 0.6640625000000000000, 0.6718750000000000000, 0.6796875000000000000, 0.6875000000000000000, 0.6953125000000000000, 0.7031250000000000000, 0.7109375000000000000, 0.7187500000000000000, 0.7265625000000000000, 0.7343750000000000000, 0.7421875000000000000, 0.7500000000000000000, 0.7578125000000000000, 0.7656250000000000000, 0.7734375000000000000, 0.7812500000000000000, 0.7890625000000000000, 0.7968750000000000000, 0.8046875000000000000, 0.8125000000000000000, 0.8203125000000000000, 0.8281250000000000000, 0.8359375000000000000, 0.8437500000000000000, 0.8515625000000000000, 0.8593750000000000000, 0.8671875000000000000, 0.8750000000000000000, 0.8828125000000000000, 0.8906250000000000000, 0.8984375000000000000, 0.9062500000000000000, 0.9140625000000000000, 0.9218750000000000000, 0.9296875000000000000, 0.9375000000000000000, 0.9453125000000000000, 0.9531250000000000000, 0.9609375000000000000, 0.9687500000000000000, 0.9765625000000000000, 0.9843750000000000000, 0.9921875000000000000, 1.000000000000000000 ),
 .UNSPECIFIED. ) 
 GEOMETRIC_REPRESENTATION_ITEM ( )  RATIONAL_B_SPLINE_SURFACE ( (
 ( 1.000000000000000000, 0.9238795325112869605, 1.000000000000000000, 0.9238795325112869605, 1.000000000000000000, 0.9238795325112869605, 1.000000000000000000, 0.9238795325112869605, 1.000000000000000000, 0.9238795325112869605, 1.000000000000000000, 0.9238795325112869605, 1.000000000000000000, 0.9238795325112869605, 1.000000000000000000, 0.9238795325112869605, 1.000000000000000000, 0.9238795325112869605, 1.000000000000000000, 0.9238795325112869605, 1.000000000000000000, 0.9238795325112869605, 1.000000000000000000, 0.9238795325112869605, 1.000000000000000000, 0.9238795325112869605, 1.000000000000000000, 0.9238795325112869605, 1.000000000000000000, 0.9238795325112869605, 1.000000000000000000, 0.9238795325112869605, 1.000000000000000000, 0.9238795325112869605, 1.000000000000000000, 0.9238795325112869605, 1.000000000000000000, 0.9238795325112869605, 1.000000000000000000, 0.9238795325112869605, 1.000000000000000000, 0.9238795325112869605, 1.000000000000000000, 0.9238795325112869605, 1.000000000000000000, 0.9238795325112869605, 1.000000000000000000, 0.9238795325112869605, 1.000000000000000000, 0.9238795325112869605, 1.000000000000000000, 0.9238795325112869605, 1.000000000000000000, 0.9238795325112869605, 1.000000000000000000, 0.9238795325112869605, 1.000000000000000000, 0.9238795325112869605, 1.000000000000000000, 0.9238795325112869605, 1.000000000000000000, 0.9238795325112869605, 1.000000000000000000, 0.9238795325112869605, 1.000000000000000000, 0.9238795325112869605, 1.000000000000000000, 0.9238795325112869605, 1.000000000000000000, 0.9238795325112869605, 1.000000000000000000, 0.9238795325112869605, 1.000000000000000000, 0.9238795325112869605, 1.000000000000000000, 0.9238795325112869605, 1.000000000000000000, 0.9238795325112869605, 1.000000000000000000, 0.9238795325112869605, 1.000000000000000000, 0.9238795325112869605, 1.000000000000000000, 0.9238795325112869605, 1.000000000000000000, 0.9238795325112869605, 1.000000000000000000, 0.9238795325112869605, 1.000000000000000000, 0.9238795325112869605, 1.000000000000000000, 0.9238795325112869605, 1.000000000000000000, 0.9238795325112869605, 1.000000000000000000, 0.9238795325112869605, 1.000000000000000000, 0.9238795325112869605, 1.000000000000000000, 0.9238795325112869605, 1.000000000000000000, 0.9238795325112869605, 1.000000000000000000, 0.9238795325112869605, 1.000000000000000000, 0.9238795325112869605, 1.000000000000000000, 0.9238795325112869605, 1.000000000000000000, 0.9238795325112869605, 1.000000000000000000, 0.9238795325112869605, 1.000000000000000000, 0.9238795325112869605, 1.000000000000000000, 0.9238795325112869605, 1.000000000000000000, 0.9238795325112869605, 1.000000000000000000, 0.9238795325112869605, 1.000000000000000000, 0.9238795325112869605, 1.000000000000000000, 0.9238795325112869605, 1.000000000000000000, 0.9238795325112869605, 1.000000000000000000, 0.9238795325112869605, 1.000000000000000000, 0.9238795325112869605, 1.000000000000000000, 0.9238795325112869605, 1.000000000000000000, 0.9238795325112869605, 1.000000000000000000, 0.9238795325112869605, 1.000000000000000000, 0.9238795325112869605, 1.000000000000000000, 0.9238795325112869605, 1.000000000000000000, 0.9238795325112869605, 1.000000000000000000, 0.9238795325112869605, 1.000000000000000000, 0.9238795325112869605, 1.000000000000000000, 0.9238795325112869605, 1.000000000000000000, 0.9238795325112869605, 1.000000000000000000, 0.9238795325112869605, 1.000000000000000000, 0.9238795325112869605, 1.000000000000000000, 0.9238795325112869605, 1.000000000000000000, 0.9238795325112869605, 1.000000000000000000, 0.9238795325112869605, 1.000000000000000000, 0.9238795325112869605, 1.000000000000000000, 0.9238795325112869605, 1.000000000000000000, 0.9238795325112869605, 1.000000000000000000, 0.9238795325112869605, 1.000000000000000000, 0.9238795325112869605, 1.000000000000000000, 0.9238795325112869605, 1.000000000000000000, 0.9238795325112869605, 1.000000000000000000, 0.9238795325112869605, 1.000000000000000000, 0.9238795325112869605, 1.000000000000000000, 0.9238795325112869605, 1.000000000000000000, 0.9238795325112869605, 1.000000000000000000, 0.9238795325112869605, 1.000000000000000000, 0.9238795325112869605, 1.000000000000000000, 0.9238795325112869605, 1.000000000000000000, 0.9238795325112869605, 1.000000000000000000, 0.9238795325112869605, 1.000000000000000000, 0.9238795325112869605, 1.000000000000000000, 0.9238795325112869605, 1.000000000000000000, 0.9238795325112869605, 1.000000000000000000, 0.9238795325112869605, 1.000000000000000000, 0.9238795325112869605, 1.000000000000000000, 0.9238795325112869605, 1.000000000000000000, 0.9238795325112869605, 1.000000000000000000, 0.9238795325112869605, 1.000000000000000000, 0.9238795325112869605, 1.000000000000000000, 0.9238795325112869605, 1.000000000000000000, 0.9238795325112869605, 1.000000000000000000, 0.9238795325112869605, 1.000000000000000000, 0.9238795325112869605, 1.000000000000000000, 0.9238795325112869605, 1.000000000000000000, 0.9238795325112869605, 1.000000000000000000, 0.9238795325112869605, 1.000000000000000000, 0.9238795325112869605, 1.000000000000000000, 0.9238795325112869605, 1.000000000000000000, 0.9238795325112869605, 1.000000000000000000, 0.9238795325112869605, 1.000000000000000000, 0.9238795325112869605, 1.000000000000000000, 0.9238795325112869605, 1.000000000000000000, 0.9238795325112869605, 1.000000000000000000, 0.9238795325112869605, 1.000000000000000000, 0.9238795325112869605, 1.000000000000000000, 0.9238795325112869605, 1.000000000000000000, 0.9238795325112869605, 1.000000000000000000, 0.9238795325112869605, 1.000000000000000000, 0.9238795325112869605, 1.000000000000000000, 0.9238795325112869605, 1.000000000000000000, 0.9238795325112869605, 1.000000000000000000, 0.9238795325112869605, 1.000000000000000000),
 ( 1.000000000000000000, 0.9238795325112869605, 1.000000000000000000, 0.9238795325112869605, 1.000000000000000000, 0.9238795325112869605, 1.000000000000000000, 0.9238795325112869605, 1.000000000000000000, 0.9238795325112869605, 1.000000000000000000, 0.9238795325112869605, 1.000000000000000000, 0.9238795325112869605, 1.000000000000000000, 0.9238795325112869605, 1.000000000000000000, 0.9238795325112869605, 1.000000000000000000, 0.9238795325112869605, 1.000000000000000000, 0.9238795325112869605, 1.000000000000000000, 0.9238795325112869605, 1.000000000000000000, 0.9238795325112869605, 1.000000000000000000, 0.9238795325112869605, 1.000000000000000000, 0.9238795325112869605, 1.000000000000000000, 0.9238795325112869605, 1.000000000000000000, 0.9238795325112869605, 1.000000000000000000, 0.9238795325112869605, 1.000000000000000000, 0.9238795325112869605, 1.000000000000000000, 0.9238795325112869605, 1.000000000000000000, 0.9238795325112869605, 1.000000000000000000, 0.9238795325112869605, 1.000000000000000000, 0.9238795325112869605, 1.000000000000000000, 0.9238795325112869605, 1.000000000000000000, 0.9238795325112869605, 1.000000000000000000, 0.9238795325112869605, 1.000000000000000000, 0.9238795325112869605, 1.000000000000000000, 0.9238795325112869605, 1.000000000000000000, 0.9238795325112869605, 1.000000000000000000, 0.9238795325112869605, 1.000000000000000000, 0.9238795325112869605, 1.000000000000000000, 0.9238795325112869605, 1.000000000000000000, 0.9238795325112869605, 1.000000000000000000, 0.9238795325112869605, 1.000000000000000000, 0.9238795325112869605, 1.000000000000000000, 0.9238795325112869605, 1.000000000000000000, 0.9238795325112869605, 1.000000000000000000, 0.9238795325112869605, 1.000000000000000000, 0.9238795325112869605, 1.000000000000000000, 0.9238795325112869605, 1.000000000000000000, 0.9238795325112869605, 1.000000000000000000, 0.9238795325112869605, 1.000000000000000000, 0.9238795325112869605, 1.000000000000000000, 0.9238795325112869605, 1.000000000000000000, 0.9238795325112869605, 1.000000000000000000, 0.9238795325112869605, 1.000000000000000000, 0.9238795325112869605, 1.000000000000000000, 0.9238795325112869605, 1.000000000000000000, 0.9238795325112869605, 1.000000000000000000, 0.9238795325112869605, 1.000000000000000000, 0.9238795325112869605, 1.000000000000000000, 0.9238795325112869605, 1.000000000000000000, 0.9238795325112869605, 1.000000000000000000, 0.9238795325112869605, 1.000000000000000000, 0.9238795325112869605, 1.000000000000000000, 0.9238795325112869605, 1.000000000000000000, 0.9238795325112869605, 1.000000000000000000, 0.9238795325112869605, 1.000000000000000000, 0.9238795325112869605, 1.000000000000000000, 0.9238795325112869605, 1.000000000000000000, 0.9238795325112869605, 1.000000000000000000, 0.9238795325112869605, 1.000000000000000000, 0.9238795325112869605, 1.000000000000000000, 0.9238795325112869605, 1.000000000000000000, 0.9238795325112869605, 1.000000000000000000, 0.9238795325112869605, 1.000000000000000000, 0.9238795325112869605, 1.000000000000000000, 0.9238795325112869605, 1.000000000000000000, 0.9238795325112869605, 1.000000000000000000, 0.9238795325112869605, 1.000000000000000000, 0.9238795325112869605, 1.000000000000000000, 0.9238795325112869605, 1.000000000000000000, 0.9238795325112869605, 1.000000000000000000, 0.9238795325112869605, 1.000000000000000000, 0.9238795325112869605, 1.000000000000000000, 0.9238795325112869605, 1.000000000000000000, 0.9238795325112869605, 1.000000000000000000, 0.9238795325112869605, 1.000000000000000000, 0.9238795325112869605, 1.000000000000000000, 0.9238795325112869605, 1.000000000000000000, 0.9238795325112869605, 1.000000000000000000, 0.9238795325112869605, 1.000000000000000000, 0.9238795325112869605, 1.000000000000000000, 0.9238795325112869605, 1.000000000000000000, 0.9238795325112869605, 1.000000000000000000, 0.9238795325112869605, 1.000000000000000000, 0.9238795325112869605, 1.000000000000000000, 0.9238795325112869605, 1.000000000000000000, 0.9238795325112869605, 1.000000000000000000, 0.9238795325112869605, 1.000000000000000000, 0.9238795325112869605, 1.000000000000000000, 0.9238795325112869605, 1.000000000000000000, 0.9238795325112869605, 1.000000000000000000, 0.9238795325112869605, 1.000000000000000000, 0.9238795325112869605, 1.000000000000000000, 0.9238795325112869605, 1.000000000000000000, 0.9238795325112869605, 1.000000000000000000, 0.9238795325112869605, 1.000000000000000000, 0.9238795325112869605, 1.000000000000000000, 0.9238795325112869605, 1.000000000000000000, 0.9238795325112869605, 1.000000000000000000, 0.9238795325112869605, 1.000000000000000000, 0.9238795325112869605, 1.000000000000000000, 0.9238795325112869605, 1.000000000000000000, 0.9238795325112869605, 1.000000000000000000, 0.9238795325112869605, 1.000000000000000000, 0.9238795325112869605, 1.000000000000000000, 0.9238795325112869605, 1.000000000000000000, 0.9238795325112869605, 1.000000000000000000, 0.9238795325112869605, 1.000000000000000000, 0.9238795325112869605, 1.000000000000000000, 0.9238795325112869605, 1.000000000000000000, 0.9238795325112869605, 1.000000000000000000, 0.9238795325112869605, 1.000000000000000000, 0.9238795325112869605, 1.000000000000000000, 0.9238795325112869605, 1.000000000000000000, 0.9238795325112869605, 1.000000000000000000, 0.9238795325112869605, 1.000000000000000000, 0.9238795325112869605, 1.000000000000000000, 0.9238795325112869605, 1.000000000000000000, 0.9238795325112869605, 1.000000000000000000, 0.9238795325112869605, 1.000000000000000000, 0.9238795325112869605, 1.000000000000000000, 0.9238795325112869605, 1.000000000000000000, 0.9238795325112869605, 1.000000000000000000, 0.9238795325112869605, 1.000000000000000000, 0.9238795325112869605, 1.000000000000000000, 0.9238795325112869605, 1.000000000000000000) ) ) 
 REPRESENTATION_ITEM ( '' )  SURFACE ( )  );
#30562=CARTESIAN_POINT ( 'NONE',  ( 124.3117748109119844, -10.30919188438810075, -12.61870101168855918 ) ) ;
#30564=CARTESIAN_POINT ( 'NONE',  ( 124.2916835400977504, -1.223627541775709870, -16.99192386690442902 ) ) ;
#30567=CARTESIAN_POINT ( 'NONE',  ( 123.8579614775786126, -9.859900752359378018, -12.68260735090039759 ) ) ;
#30568=CARTESIAN_POINT ( 'NONE',  ( 119.8870948109119752, -9.261995988541697145, -16.69588392320189030 ) ) ;
#30569=CARTESIAN_POINT ( 'NONE',  ( 112.2857214775786474, -5.574606645277164318, -18.38911715685844683 ) ) ;
#30570=CARTESIAN_POINT ( 'NONE',  ( 115.0086014775786509, -4.089484607189486809, -7.948022111789456723 ) ) ;
#30572=CARTESIAN_POINT ( 'NONE',  ( 125.3895814775786448, -2.084020599724406786, -8.691656652584148546 ) ) ;
#30573=CARTESIAN_POINT ( 'NONE',  ( 117.6180281442453150, -8.899110576539710493, -16.42337572283490132 ) ) ;
#30577=CARTESIAN_POINT ( 'NONE',  ( 115.2922348109119781, -10.63000616557722466, -14.87417383870573495 ) ) ;
#30578=CARTESIAN_POINT ( 'NONE',  ( 122.2128881442453263, -7.643976991954077427, -18.09477374809248928 ) ) ;
#30581=CARTESIAN_POINT ( 'NONE',  ( 136.9115742440200734, -1.268299463231087110, -9.195838862358661103 ) ) ;
#30582=CARTESIAN_POINT ( 'NONE',  ( 118.1285681442453068, -7.893985811506177619, -18.51759400769804742 ) ) ;
#30584=CARTESIAN_POINT ( 'NONE',  ( 114.8951481442453115, -8.899110576539710493, -16.42337572283490132 ) ) ;
#30589=CARTESIAN_POINT ( 'NONE',  ( 112.4559014775786494, -9.988377603198976828, -10.36322818467138340 ) ) ;
#30590=CARTESIAN_POINT ( 'NONE',  ( 125.3328548109119964, -0.8288870151387760510, -10.36305467784173118 ) ) ;
#30595=CARTESIAN_POINT ( 'NONE',  ( 122.6099748109119929, -9.261995988541697145, -16.69588392320189030 ) ) ;
#30596=CARTESIAN_POINT ( 'NONE',  ( 138.2184548109119930, 2.066246953222917959, -14.37896053134723040 ) ) ;
#30598=CARTESIAN_POINT ( 'NONE',  ( 121.0216281442452981, -1.561330072975668948, -17.79121239304076951 ) ) ;
#30599=CARTESIAN_POINT ( 'NONE',  ( 117.2776681442452968, -5.638512984488999180, -18.83840828888717311 ) ) ;
#30600=CARTESIAN_POINT ( 'NONE',  ( 118.0718414775786442, -0.8288870151387760510, -10.36305467784173118 ) ) ;
#30602=CARTESIAN_POINT ( 'NONE',  ( 112.5693548109119888, -10.63000616557722466, -14.87417383870573495 ) ) ;
#30604=CARTESIAN_POINT ( 'NONE',  ( 124.8223148109119762, -10.15424416112533912, -14.75197769757731336 ) ) ;
#30612=CARTESIAN_POINT ( 'NONE',  ( 121.4187148109119789, -6.344957434206665248, -7.627207830600338134 ) ) ;
#30613=CARTESIAN_POINT ( 'NONE',  ( 122.6099748109119929, -0.8288870151387760510, -10.36305467784173118 ) ) ;
#30614=ORIENTED_EDGE ( 'NONE', *, *, #35896, .F. ) ;
#30616=CARTESIAN_POINT ( 'NONE',  ( 123.2906948109119867, -8.166667518702819706, -8.995218007635861213 ) ) ;
#30617=CARTESIAN_POINT ( 'NONE',  ( 114.1009748109119784, -5.574606645277164318, -18.38911715685844683 ) ) ;
#30619=CARTESIAN_POINT ( 'NONE',  ( 120.8514481442452961, -7.893985811506177619, -18.51759400769804742 ) ) ;
#30622=CARTESIAN_POINT ( 'NONE',  ( 119.4332814775786318, -0.4660016031367893996, -10.09054647747474043 ) ) ;
#30624=CARTESIAN_POINT ( 'NONE',  ( 112.5126281442453120, -10.30919188438810075, -12.61870101168855918 ) ) ;
#30627=CARTESIAN_POINT ( 'NONE',  ( 124.6329298793804981, -2.191907684172563986, -18.20049396185734025 ) ) ;
#30628=CARTESIAN_POINT ( 'NONE',  ( 112.9664414775786412, -9.859900752359374465, -12.68260735090039404 ) ) ;
#30629=CARTESIAN_POINT ( 'NONE',  ( 125.1626748109119802, -0.1624402480850797581, -16.17319339645315424 ) ) ;
#30633=CARTESIAN_POINT ( 'NONE',  ( 121.1918081442452859, -10.15424416112533912, -14.75197769757731336 ) ) ;
#30634=CARTESIAN_POINT ( 'NONE',  ( 114.4980614775786734, -2.084020599724406786, -8.691656652584148546 ) ) ;
#30635=CARTESIAN_POINT ( 'NONE',  ( 124.1415948109119540, -6.344957434206665248, -7.627207830600338134 ) ) ;
#30637=CARTESIAN_POINT ( 'NONE',  ( 120.5110881442453206, -3.505236298600246325, -18.68346056562440793 ) ) ;
#30638=CARTESIAN_POINT ( 'NONE',  ( 119.0361948109119652, -7.893985811506177619, -18.51759400769804742 ) ) ;
#30639=CARTESIAN_POINT ( 'NONE',  ( 123.5743281442453139, -7.893985811506177619, -18.51759400769804742 ) ) ;
#30640=CARTESIAN_POINT ( 'NONE',  ( 125.2761281442453054, 0.4262465694468514643, -12.03445270309931736 ) ) ;
#30643=CARTESIAN_POINT ( 'NONE',  ( 122.8936081442453059, 0.2603800115204892296, -16.42320221600525088 ) ) ;
#30645=CARTESIAN_POINT ( 'NONE',  ( 115.0653281442453277, -3.505236298600246325, -18.68346056562440793 ) ) ;
#30647=CARTESIAN_POINT ( 'NONE',  ( 125.5030348109119558, -3.383040157471821630, -19.15922257007629170 ) ) ;
#30657=CARTESIAN_POINT ( 'NONE',  ( 123.9146881442452894, -10.15424416112533912, -14.75197769757731336 ) ) ;
#30658=CARTESIAN_POINT ( 'NONE',  ( 115.2922348109119781, 0.4262465694468514643, -12.03445270309931736 ) ) ;
#30659=CARTESIAN_POINT ( 'NONE',  ( 127.3434826497349377, 0.2239902821118424925, -11.13838800870225043 ) ) ;
#30660=ORIENTED_EDGE ( 'NONE', *, *, #33918, .T. ) ;
#30661=LINE ( 'NONE', #40935, #6944 ) ;
#30662=CARTESIAN_POINT ( 'NONE',  ( 121.4187148109119789, -3.505236298600246325, -18.68346056562440793 ) ) ;
#30663=CARTESIAN_POINT ( 'NONE',  ( 114.2711548109119803, -0.1624402480850797581, -16.17319339645315424 ) ) ;
#30664=CARTESIAN_POINT ( 'NONE',  ( 111.3780948109119890, -5.574606645277164318, -18.38911715685844683 ) ) ;
#30666=CARTESIAN_POINT ( 'NONE',  ( 125.4463081442452932, -5.638512984488999180, -18.83840828888717311 ) ) ;
#30667=CARTESIAN_POINT ( 'NONE',  ( 112.8529881442453302, -1.561330072975668060, -17.79121239304076596 ) ) ;
#30669=CARTESIAN_POINT ( 'NONE',  ( 112.5693548109119888, -10.63000616557722466, -14.87417383870573495 ) ) ;
#30670=CARTESIAN_POINT ( 'NONE',  ( 126.3509913982080946, 0.07182886583579818629, -14.53637278171945546 ) ) ;
#30672=EDGE_CURVE ( 'NONE', #42235, #2538, #6051, .T. ) ;
#30673=CARTESIAN_POINT ( 'NONE',  ( 123.9146881442452894, -10.15424416112533912, -14.75197769757731336 ) ) ;
#30674=CARTESIAN_POINT ( 'NONE',  ( 121.8725281442453223, -6.222761293078241884, -8.102969835052219238 ) ) ;
#30677=CARTESIAN_POINT ( 'NONE',  ( 111.9653064975817927, -2.215723800389698184, -18.16877924232191788 ) ) ;
#30681=CARTESIAN_POINT ( 'NONE',  ( 138.2184548109119930, -10.46144976836963814, -17.59661175671013922 ) ) ;
#30685=CARTESIAN_POINT ( 'NONE',  ( 125.6732148109119862, 0.5811942927096110934, -14.16772938898807510 ) ) ;
#30686=CARTESIAN_POINT ( 'NONE',  ( 123.6310548109119765, -5.638512984488999180, -18.83840828888717311 ) ) ;
#30688=CARTESIAN_POINT ( 'NONE',  ( 119.9438214775786378, -7.893985811506177619, -18.51759400769804742 ) ) ;
#30689=CARTESIAN_POINT ( 'NONE',  ( 112.2857214775786474, -4.089484607189486809, -7.948022111789456723 ) ) ;
#30691=CARTESIAN_POINT ( 'NONE',  ( 113.2500748109119968, -3.505236298600246325, -18.68346056562440793 ) ) ;
#30692=CARTESIAN_POINT ( 'NONE',  ( 111.4915481442453142, -1.833838273342658365, -17.42832698103878286 ) ) ;
#30694=CARTESIAN_POINT ( 'NONE',  ( 123.4041481442452834, -10.30919188438810075, -12.61870101168855918 ) ) ;
#30695=CARTESIAN_POINT ( 'NONE',  ( 115.2355081442453155, -10.30919188438810075, -12.61870101168855918 ) ) ;
#30696=CARTESIAN_POINT ( 'NONE',  ( 112.6828081442453282, -2.084020599724406786, -8.691656652584148546 ) ) ;
#30698=CARTESIAN_POINT ( 'NONE',  ( 117.7882081442453170, -3.505236298600246325, -18.68346056562440793 ) ) ;
#30700=CARTESIAN_POINT ( 'NONE',  ( 123.4041481442452834, 0.1319031606808879209, -14.10382304977623669 ) ) ;
#30707=CARTESIAN_POINT ( 'NONE',  ( 112.2289948109119848, -1.834011780172310813, -8.268836392978581529 ) ) ;
#30713=CARTESIAN_POINT ( 'NONE',  ( 117.1074881442453233, -10.63000616557722466, -14.87417383870573495 ) ) ;
#30714=CARTESIAN_POINT ( 'NONE',  ( 137.2687954574917910, -6.421912352659795431, -18.40503953683662175 ) ) ;
#30717=CARTESIAN_POINT ( 'NONE',  ( 124.8223148109119762, 0.9020085738987339008, -11.91225656197089222 ) ) ;
#30718=CARTESIAN_POINT ( 'NONE',  ( 121.9859814775786333, -9.565557343593413364, -10.61323700422348004 ) ) ;
#30719=ORIENTED_EDGE ( 'NONE', *, *, #30672, .F. ) ;
#30720=CARTESIAN_POINT ( 'NONE',  ( 126.0703014775786102, -9.988377603198980381, -10.36322818467138518 ) ) ;
#30721=CARTESIAN_POINT ( 'NONE',  ( 120.7379948109119709, -10.63000616557722466, -14.87417383870573495 ) ) ;
#30723=CARTESIAN_POINT ( 'NONE',  ( 115.9162281442453235, -5.574606645277164318, -18.38911715685844683 ) ) ;
#30724=CARTESIAN_POINT ( 'NONE',  ( 124.5386814775786206, -5.638512984488999180, -18.83840828888717311 ) ) ;
#30728=CARTESIAN_POINT ( 'NONE',  ( 115.5758681442453053, -7.894159318335828068, -9.358103419637847864 ) ) ;
#30729=CARTESIAN_POINT ( 'NONE',  ( 116.5969481442453031, -9.859900752359374465, -12.68260735090039404 ) ) ;
#30735=CARTESIAN_POINT ( 'NONE',  ( 114.4980614775786592, -7.893985811506177619, -18.51759400769804742 ) ) ;
#30743=CARTESIAN_POINT ( 'NONE',  ( 123.4608748109119745, -10.63000616557722466, -14.87417383870573495 ) ) ;
#30744=CARTESIAN_POINT ( 'NONE',  ( 113.1366214775786432, -1.834011780172310813, -8.268836392978581529 ) ) ;
#30745=CARTESIAN_POINT ( 'NONE',  ( 120.0572748109119772, -6.222761293078241884, -8.102969835052219238 ) ) ;
#30748=CARTESIAN_POINT ( 'NONE',  ( 120.9081748109119872, -5.638512984488999180, -18.83840828888717311 ) ) ;
#30749=CARTESIAN_POINT ( 'NONE',  ( 117.7314814775786260, -4.089484607189486809, -7.948022111789456723 ) ) ;
#30752=CARTESIAN_POINT ( 'NONE',  ( 112.6260814775786514, -0.8288870151387760510, -10.36305467784173118 ) ) ;
#30754=ORIENTED_EDGE ( 'NONE', *, *, #27562, .T. ) ;
#30755=CARTESIAN_POINT ( 'NONE',  ( 117.3911214775786505, -1.561330072975668504, -17.79121239304076951 ) ) ;
#30757=CARTESIAN_POINT ( 'NONE',  ( 115.0086014775786509, -4.089484607189486809, -7.948022111789456723 ) ) ;
#30759=CARTESIAN_POINT ( 'NONE',  ( 120.6245414775786458, -9.988377603198976828, -10.36322818467138340 ) ) ;
#30761=CARTESIAN_POINT ( 'NONE',  ( 113.7038881442453402, -6.222761293078241884, -8.102969835052219238 ) ) ;
#30763=CARTESIAN_POINT ( 'NONE',  ( 117.1074881442453233, 0.4262465694468514643, -12.03445270309931736 ) ) ;
#30766=CARTESIAN_POINT ( 'NONE',  ( 116.1998614775786507, 0.4262465694468514643, -12.03445270309931736 ) ) ;
#30768=CARTESIAN_POINT ( 'NONE',  ( 115.2922348109119781, 0.4262465694468514643, -12.03445270309931736 ) ) ;
#30769=CARTESIAN_POINT ( 'NONE',  ( 116.3133148109119759, -7.893985811506177619, -18.51759400769804742 ) ) ;
#30771=CARTESIAN_POINT ( 'NONE',  ( 114.3846081442453197, -10.63000616557722466, -14.87417383870573495 ) ) ;
#30772=CARTESIAN_POINT ( 'NONE',  ( 114.4980614775786734, -2.084020599724406786, -8.691656652584148546 ) ) ;
#30773=CARTESIAN_POINT ( 'NONE',  ( 112.1155414775786454, -10.15424416112533912, -14.75197769757731336 ) ) ;
#30775=CARTESIAN_POINT ( 'NONE',  ( 115.6893214775786447, -9.859900752359374465, -12.68260735090039404 ) ) ;
#30777=CARTESIAN_POINT ( 'NONE',  ( 114.4413348109119823, -9.261995988541697145, -16.69588392320189030 ) ) ;
#30784=CARTESIAN_POINT ( 'NONE',  ( 118.2420214775786320, -3.383040157471821630, -19.15922257007629170 ) ) ;
#30785=ORIENTED_EDGE ( 'NONE', *, *, #17538, .T. ) ;
#30787=CARTESIAN_POINT ( 'NONE',  ( 124.8790414775786246, -0.4660016031367893996, -10.09054647747473865 ) ) ;
#30788=CARTESIAN_POINT ( 'NONE',  ( 119.2063748109119814, -7.894159318335828068, -9.358103419637847864 ) ) ;
#30789=CARTESIAN_POINT ( 'NONE',  ( 124.4819548109119722, -2.084020599724378364, -8.691656652584169862 ) ) ;
#30790=CARTESIAN_POINT ( 'NONE',  ( 125.1059481442452750, -8.166667518702819706, -8.995218007635861213 ) ) ;
#30792=CARTESIAN_POINT ( 'NONE',  ( 124.4365102882354819, -1.135392229370316919, -17.10942237759952533 ) ) ;
#30794=CARTESIAN_POINT ( 'NONE',  ( 112.9664414775786412, 0.5811942927096154232, -14.16772938898807155 ) ) ;
#30795=CARTESIAN_POINT ( 'NONE',  ( 121.7590748109119687, -2.084020599724406786, -8.691656652584148546 ) ) ;
#30796=CARTESIAN_POINT ( 'NONE',  ( 118.6391081442452986, -4.089484607189486809, -7.948022111789456723 ) ) ;
#30797=CARTESIAN_POINT ( 'NONE',  ( 116.7671281442453335, -7.643976991954077427, -18.09477374809248928 ) ) ;
#30798=CARTESIAN_POINT ( 'NONE',  ( 119.6034614775786196, -6.344957434206665248, -7.627207830600338134 ) ) ;
#30801=CARTESIAN_POINT ( 'NONE',  ( 122.0994348109119443, -10.15424416112533912, -14.75197769757731336 ) ) ;
#30805=CARTESIAN_POINT ( 'NONE',  ( 118.6958348109119754, -6.344957434206665248, -7.627207830600338134 ) ) ;
#30806=B_SPLINE_CURVE_WITH_KNOTS ( 'NONE', 3,
 ( #18807, #22900, #36794, #43208, #15392, #5563, #33366, #29295, #43888, #33594, #39779, #29972, #22450, #26555, #2369 ),
 .UNSPECIFIED., .F., .F.,
 ( 4, 2, 2, 1, 1, 1, 2, 2, 4 ),
 ( 0.000000000000000000, 0.2500000000002625677, 0.3750000000004022338, 0.4375000000004654055, 0.4687500000004892753, 0.4843750000005023759, 0.4921875000005089817, 0.5000000000005155876, 1.000000000000000000 ),
 .UNSPECIFIED. ) ;
#30807=CARTESIAN_POINT ( 'NONE',  ( 125.1626748109119802, -0.1624402480850797581, -16.17319339645315424 ) ) ;
#30808=VERTEX_POINT ( 'NONE', #7557 ) ;
#30811=CARTESIAN_POINT ( 'NONE',  ( 119.3198281442452924, 0.5811942927096110934, -14.16772938898807510 ) ) ;
#30813=CARTESIAN_POINT ( 'NONE',  ( 118.0718414775786442, -0.8288870151387760510, -10.36305467784173118 ) ) ;
#30814=ORIENTED_EDGE ( 'NONE', *, *, #4404, .T. ) ;
#30817=CARTESIAN_POINT ( 'NONE',  ( 124.2550481442452792, -0.1624402480850797581, -16.17319339645315424 ) ) ;
#30818=CARTESIAN_POINT ( 'NONE',  ( 125.5597614775786326, -7.894159318335828068, -9.358103419637847864 ) ) ;
#30821=CARTESIAN_POINT ( 'NONE',  ( 120.2274548109119934, 0.5811942927096110934, -14.16772938898807510 ) ) ;
#30822=CARTESIAN_POINT ( 'NONE',  ( 111.7184548109119788, -9.244942279156937559, -16.71734234406761388 ) ) ;
#30824=CARTESIAN_POINT ( 'NONE',  ( 119.3198281442452924, 0.5811942927096110934, -14.16772938898807510 ) ) ;
#30825=CARTESIAN_POINT ( 'NONE',  ( 118.7525614775786380, -8.166667518702819706, -8.995218007635861213 ) ) ;
#30826=CARTESIAN_POINT ( 'NONE',  ( 121.0216281442452981, -7.894159318335828068, -9.358103419637847864 ) ) ;
#30829=CARTESIAN_POINT ( 'NONE',  ( 117.6180281442453150, -0.4660016031367893996, -10.09054647747474043 ) ) ;
#30830=ORIENTED_EDGE ( 'NONE', *, *, #19307, .T. ) ;
#30831=CARTESIAN_POINT ( 'NONE',  ( 123.7445081442452874, -7.894159318335828068, -9.358103419637847864 ) ) ;
#30836=CARTESIAN_POINT ( 'NONE',  ( 121.1350814775786233, 0.5811942927096110934, -14.16772938898807510 ) ) ;
#30837=CARTESIAN_POINT ( 'NONE',  ( 123.5176014775786228, -0.8288870151387760510, -10.36305467784173118 ) ) ;
#30839=CARTESIAN_POINT ( 'NONE',  ( 123.3474214775786209, -9.988377603198976828, -10.36322818467138340 ) ) ;
#30841=CARTESIAN_POINT ( 'NONE',  ( 113.1366214775786432, -7.643976991954077427, -18.09477374809248928 ) ) ;
#30843=CARTESIAN_POINT ( 'NONE',  ( 124.8223148109119762, 0.9020085738987339008, -11.91225656197089222 ) ) ;
#30844=CARTESIAN_POINT ( 'NONE',  ( 119.8303681442453126, -10.63000616557722466, -14.87417383870573495 ) ) ;
#30846=CARTESIAN_POINT ( 'NONE',  ( 112.8529881442453302, -1.561330072975668060, -17.79121239304076596 ) ) ;
#30851=CARTESIAN_POINT ( 'NONE',  ( 124.7895009388149248, -2.287189184988705826, -18.07361239780448159 ) ) ;
#30852=CARTESIAN_POINT ( 'NONE',  ( 113.4769814775786330, 0.4262465694468514643, -12.03445270309931736 ) ) ;
#30853=CARTESIAN_POINT ( 'NONE',  ( 124.0281414775786146, -7.643976991954077427, -18.09477374809248928 ) ) ;
#30856=CARTESIAN_POINT ( 'NONE',  ( 122.8368814775786291, -7.894159318335828068, -9.358103419637847864 ) ) ;
#30857=CARTESIAN_POINT ( 'NONE',  ( 115.2355081442453155, 0.1319031606808879209, -14.10382304977623669 ) ) ;
#30858=CARTESIAN_POINT ( 'NONE',  ( 112.6828081442453282, -2.084020599724406786, -8.691656652584148546 ) ) ;
#30861=CARTESIAN_POINT ( 'NONE',  ( 120.9081748109119872, -4.153390946401325223, -8.397313243818185668 ) ) ;
#30862=CARTESIAN_POINT ( 'NONE',  ( 117.9583881442453048, -10.30919188438810075, -12.61870101168855918 ) ) ;
#30868=CARTESIAN_POINT ( 'NONE',  ( 115.4056881442453459, -2.084020599724406786, -8.691656652584148546 ) ) ;
#30869=CARTESIAN_POINT ( 'NONE',  ( 113.7038881442453402, -6.222761293078241884, -8.102969835052219238 ) ) ;
#30871=CARTESIAN_POINT ( 'NONE',  ( 128.2184548109119930, -7.252096815532139473, -18.89748516540533529 ) ) ;
#30875=VERTEX_POINT ( 'NONE', #13964 ) ;
#30880=CARTESIAN_POINT ( 'NONE',  ( 124.7655881442452852, -9.859900752359378018, -12.68260735090039759 ) ) ;
#30881=CARTESIAN_POINT ( 'NONE',  ( 113.3068014775786594, -1.833838273342658809, -17.42832698103878286 ) ) ;
#30882=CARTESIAN_POINT ( 'NONE',  ( 125.5030348109119558, -6.222761293078236555, -8.102969835052215686 ) ) ;
#30887=CARTESIAN_POINT ( 'NONE',  ( 112.0126281442453120, -9.814174330883659536, -12.68911139247490105 ) ) ;
#30890=CARTESIAN_POINT ( 'NONE',  ( 124.7655881442452852, -9.859900752359378018, -12.68260735090039759 ) ) ;
#30892=CARTESIAN_POINT ( 'NONE',  ( 115.0653281442453277, -6.344957434206662583, -7.627207830600332805 ) ) ;
#30893=CARTESIAN_POINT ( 'NONE',  ( 126.9276200068715497, 0.2063212325922000601, -15.11478432700113395 ) ) ;
#30895=CARTESIAN_POINT ( 'NONE',  ( 125.6164881442453094, -9.565557343593413364, -10.61323700422348004 ) ) ;
#30896=CARTESIAN_POINT ( 'NONE',  ( 123.0637881442452937, -8.899110576539710493, -16.42337572283490132 ) ) ;
#30902=CARTESIAN_POINT ( 'NONE',  ( 112.5693548109119888, 0.4262465694468514643, -12.03445270309931736 ) ) ;
#30906=CARTESIAN_POINT ( 'NONE',  ( 124.7655881442452852, 0.5811942927096110934, -14.16772938898807510 ) ) ;
#30907=CARTESIAN_POINT ( 'NONE',  ( 125.2761281442453054, -10.63000616557722466, -14.87417383870573495 ) ) ;
#30910=CARTESIAN_POINT ( 'NONE',  ( 120.8514481442452961, -7.893985811506177619, -18.51759400769804742 ) ) ;
#30911=CARTESIAN_POINT ( 'NONE',  ( 113.7038881442453402, -3.383040157471821630, -19.15922257007629170 ) ) ;
#30913=CARTESIAN_POINT ( 'NONE',  ( 114.2711548109119803, -0.1624402480850797581, -16.17319339645315424 ) ) ;
#30914=EDGE_CURVE ( 'NONE', #11839, #30808, #12192, .T. ) ;
#30915=CARTESIAN_POINT ( 'NONE',  ( 125.8433948109119456, -1.834011780172310813, -8.268836392978581529 ) ) ;
#30916=CARTESIAN_POINT ( 'NONE',  ( 125.2194014775786286, -10.30919188438810075, -12.61870101168855918 ) ) ;
#30917=CARTESIAN_POINT ( 'NONE',  ( 113.7038881442453402, -3.383040157471821630, -19.15922257007629170 ) ) ;
#30919=CARTESIAN_POINT ( 'NONE',  ( 116.0864081442453113, -0.1624402480850797581, -16.17319339645315424 ) ) ;
#30921=CARTESIAN_POINT ( 'NONE',  ( 118.3554748109119998, -9.565557343593413364, -10.61323700422348004 ) ) ;
#30922=CARTESIAN_POINT ( 'NONE',  ( 125.4463081442452932, -4.153390946401325223, -8.397313243818185668 ) ) ;
#30933=B_SPLINE_CURVE_WITH_KNOTS ( 'NONE', 3,
 ( #14124, #3417, #31442, #41949, #6845, #20752, #34631, #17333, #31664, #657 ),
 .UNSPECIFIED., .F., .F.,
 ( 4, 3, 3, 4 ),
 ( 0.000000000000000000, 0.0001671877560958089928, 0.0003343755126086520144, 0.0006438490228507220145 ),
 .UNSPECIFIED. ) ;
#30935=CARTESIAN_POINT ( 'NONE',  ( 112.7395348109119766, -4.153390946401321671, -8.397313243818183892 ) ) ;
#30938=CARTESIAN_POINT ( 'NONE',  ( 116.9940348109119839, -9.988377603198976828, -10.36322818467138340 ) ) ;
#30939=CARTESIAN_POINT ( 'NONE',  ( 136.4340220207345169, -4.240043735563310712, -19.13645151290679536 ) ) ;
#30940=CARTESIAN_POINT ( 'NONE',  ( 111.2184548109119788, -4.863998795839242995, -13.39321520033831447 ) ) ;
#30942=CARTESIAN_POINT ( 'NONE',  ( 121.4187148109119789, -3.505236298600246325, -18.68346056562440793 ) ) ;
#30944=CARTESIAN_POINT ( 'NONE',  ( 136.5278073584882463, -9.320078359935157764, -9.779958153336949067 ) ) ;
#30945=CARTESIAN_POINT ( 'NONE',  ( 118.0718414775786300, -9.261995988541697145, -16.69588392320189030 ) ) ;
#30947=CARTESIAN_POINT ( 'NONE',  ( 116.0864081442453113, -0.1624402480850797581, -16.17319339645315424 ) ) ;
#30948=CARTESIAN_POINT ( 'NONE',  ( 114.1009748109119784, -5.574606645277164318, -18.38911715685844683 ) ) ;
#30953=CARTESIAN_POINT ( 'NONE',  ( 114.9518748109119883, -7.643976991954077427, -18.09477374809248928 ) ) ;
#30954=CARTESIAN_POINT ( 'NONE',  ( 120.1140014775786398, -7.894159318335828068, -9.358103419637847864 ) ) ;
#30959=CARTESIAN_POINT ( 'NONE',  ( 112.2857214775786474, -4.089484607189486809, -7.948022111789456723 ) ) ;
#30960=CARTESIAN_POINT ( 'NONE',  ( 115.4056881442453459, -7.893985811506177619, -18.51759400769804742 ) ) ;
#30963=ORIENTED_EDGE ( 'NONE', *, *, #3827, .T. ) ;
#30964=CARTESIAN_POINT ( 'NONE',  ( 123.4728812494079335, -2.843354789049347797, -14.83501475315878260 ) ) ;
#30967=CARTESIAN_POINT ( 'NONE',  ( 121.7590748109119687, -7.893985811506177619, -18.51759400769804742 ) ) ;
#30968=CARTESIAN_POINT ( 'NONE',  ( 111.7751814775786556, -7.893985811506177619, -18.51759400769804742 ) ) ;
#30969=CARTESIAN_POINT ( 'NONE',  ( 117.5613014775786525, -10.15424416112533912, -14.75197769757731336 ) ) ;
#30971=CARTESIAN_POINT ( 'NONE',  ( 122.3830681442452857, -8.166667518702819706, -8.995218007635861213 ) ) ;
#30972=CARTESIAN_POINT ( 'NONE',  ( 117.7882081442453170, -6.344957434206665248, -7.627207830600338134 ) ) ;
#30975=CARTESIAN_POINT ( 'NONE',  ( 111.5482748109120053, -0.1624402480850797581, -16.17319339645315424 ) ) ;
#30977=VERTEX_POINT ( 'NONE', #5475 ) ;
#30978=CARTESIAN_POINT ( 'NONE',  ( 119.0929214775786278, -5.638512984488999180, -18.83840828888717311 ) ) ;
#30980=CARTESIAN_POINT ( 'NONE',  ( 115.5758681442453053, -1.561330072975668060, -17.79121239304076951 ) ) ;
#30982=ORIENTED_EDGE ( 'NONE', *, *, #36698, .F. ) ;
#30989=CARTESIAN_POINT ( 'NONE',  ( 117.2776681442452968, -4.153390946401325223, -8.397313243818185668 ) ) ;
#30991=CARTESIAN_POINT ( 'NONE',  ( 116.9940348109119839, -0.1624402480850797581, -16.17319339645315424 ) ) ;
#30993=CARTESIAN_POINT ( 'NONE',  ( 117.5613014775786525, -10.15424416112533912, -14.75197769757731336 ) ) ;
#30995=CARTESIAN_POINT ( 'NONE',  ( 115.9162281442453235, -4.089484607189486809, -7.948022111789456723 ) ) ;
#30996=CARTESIAN_POINT ( 'NONE',  ( 111.6050014775786536, 0.1319031606808879209, -14.10382304977623669 ) ) ;
#30997=CARTESIAN_POINT ( 'NONE',  ( 118.0718414775786442, -0.8288870151387760510, -10.36305467784173118 ) ) ;
#30998=VERTEX_POINT ( 'NONE', #39474 ) ;
#30999=CARTESIAN_POINT ( 'NONE',  ( 117.2209414775786485, -7.893985811506177619, -18.51759400769804742 ) ) ;
#31003=CARTESIAN_POINT ( 'NONE',  ( 127.9650921473015330, -4.196254079835942008, -15.53128073880881388 ) ) ;
#31004=CARTESIAN_POINT ( 'NONE',  ( 121.1350814775786233, 0.5811942927096110934, -14.16772938898807510 ) ) ;
#31007=CARTESIAN_POINT ( 'NONE',  ( 119.4900081442453086, -7.643976991954077427, -18.09477374809248928 ) ) ;
#31008=CARTESIAN_POINT ( 'NONE',  ( 123.4041481442452834, -10.30919188438810075, -12.61870101168855918 ) ) ;
#31012=CARTESIAN_POINT ( 'NONE',  ( 111.9453614775786434, -1.561330072975668060, -17.79121239304076596 ) ) ;
#31013=CARTESIAN_POINT ( 'NONE',  ( 111.8886348109120092, -3.383040157471821630, -19.15922257007629170 ) ) ;
#31014=CARTESIAN_POINT ( 'NONE',  ( 123.4041481442452834, -10.30919188438810075, -12.61870101168855918 ) ) ;
#31015=CARTESIAN_POINT ( 'NONE',  ( 115.9162281442453235, -5.574606645277164318, -18.38911715685844683 ) ) ;
#31017=CARTESIAN_POINT ( 'NONE',  ( 118.7525614775786380, -8.166667518702819706, -8.995218007635861213 ) ) ;
#31019=CARTESIAN_POINT ( 'NONE',  ( 124.4819548109119722, -2.084020599724406786, -8.691656652584148546 ) ) ;
#31023=CARTESIAN_POINT ( 'NONE',  ( 117.9016614775786280, -9.988377603198976828, -10.36322818467138340 ) ) ;
#31024=CARTESIAN_POINT ( 'NONE',  ( 135.5837700375877262, -8.533490405816159807, -18.12891336820539934 ) ) ;
#31028=CARTESIAN_POINT ( 'NONE',  ( 121.9292548109119849, -1.561330072975668948, -17.79121239304076951 ) ) ;
#31030=CARTESIAN_POINT ( 'NONE',  ( 120.5110881442453206, -3.505236298600246325, -18.68346056562440793 ) ) ;
#31033=CARTESIAN_POINT ( 'NONE',  ( 114.3846081442453197, -10.63000616557722466, -14.87417383870573495 ) ) ;
#31039=CARTESIAN_POINT ( 'NONE',  ( 122.7234281442452755, -5.638512984488999180, -18.83840828888717311 ) ) ;
#31042=CARTESIAN_POINT ( 'NONE',  ( 121.5888948109119809, -10.30919188438810075, -12.61870101168855918 ) ) ;
#31043=CARTESIAN_POINT ( 'NONE',  ( 117.9583881442453048, -10.30919188438810075, -12.61870101168855918 ) ) ;
#31044=CARTESIAN_POINT ( 'NONE',  ( 117.9583881442453048, 0.1319031606808879209, -14.10382304977623669 ) ) ;
#31046=CARTESIAN_POINT ( 'NONE',  ( 116.1998614775786507, -10.63000616557722466, -14.87417383870573495 ) ) ;
#31049=CARTESIAN_POINT ( 'NONE',  ( 111.7184548109119788, -9.261995988541697145, -16.69588392320189030 ) ) ;
#31055=CARTESIAN_POINT ( 'NONE',  ( 122.9503348109119827, 0.5811942927096110934, -14.16772938898807510 ) ) ;
#31056=CARTESIAN_POINT ( 'NONE',  ( 112.0020881442453344, 0.2603800115204892296, -16.42320221600525088 ) ) ;
#31058=CARTESIAN_POINT ( 'NONE',  ( 125.7866681442452688, -0.4660016031367893996, -10.09054647747474043 ) ) ;
#31061=CARTESIAN_POINT ( 'NONE',  ( 123.6310548109119765, -5.638512984488999180, -18.83840828888717311 ) ) ;
#31064=CARTESIAN_POINT ( 'NONE',  ( 126.2972081442452890, -2.084020599724406786, -8.691656652584148546 ) ) ;
#31069=CARTESIAN_POINT ( 'NONE',  ( 114.2711548109119803, -0.1624402480850797581, -16.17319339645315424 ) ) ;
#31070=CARTESIAN_POINT ( 'NONE',  ( 125.7866681442452688, -8.899110576539710493, -16.42337572283490132 ) ) ;
#31074=CARTESIAN_POINT ( 'NONE',  ( 121.5888948109119809, 0.1319031606808879209, -14.10382304977623669 ) ) ;
#31075=CARTESIAN_POINT ( 'NONE',  ( 115.4624148109119943, -4.153390946401321671, -8.397313243818183892 ) ) ;
#31076=CARTESIAN_POINT ( 'NONE',  ( 125.4463081442452932, -5.638512984488999180, -18.83840828888717311 ) ) ;
#31079=CARTESIAN_POINT ( 'NONE',  ( 124.1415948109119540, -3.505236298600246325, -18.68346056562440793 ) ) ;
#31080=CARTESIAN_POINT ( 'NONE',  ( 118.4122014775786340, 0.5811942927096110934, -14.16772938898807510 ) ) ;
#31082=CARTESIAN_POINT ( 'NONE',  ( 113.1366214775786432, -7.643976991954077427, -18.09477374809248928 ) ) ;
#31087=CARTESIAN_POINT ( 'NONE',  ( 114.2144281442453178, -1.833838273342658809, -17.42832698103878286 ) ) ;
#31088=CARTESIAN_POINT ( 'NONE',  ( 115.4056881442453459, -2.084020599724406786, -8.691656652584148546 ) ) ;
#31090=CARTESIAN_POINT ( 'NONE',  ( 128.2184548109119930, -4.863998795839242995, -13.39321520033831447 ) ) ;
#31098=CARTESIAN_POINT ( 'NONE',  ( 123.6877814775786533, -6.222761293078241884, -8.102969835052219238 ) ) ;
#31099=CARTESIAN_POINT ( 'NONE',  ( 114.3846081442453197, 0.4262465694468514643, -12.03445270309931736 ) ) ;
#31100=CARTESIAN_POINT ( 'NONE',  ( 113.7606148109119886, -7.894159318335810305, -9.358103419637835430 ) ) ;
#31103=CARTESIAN_POINT ( 'NONE',  ( 116.3133148109120043, -2.084020599724406786, -8.691656652584148546 ) ) ;
#31106=CARTESIAN_POINT ( 'NONE',  ( 125.5597614775786326, -1.561330072975669392, -17.79121239304076951 ) ) ;
#31107=CARTESIAN_POINT ( 'NONE',  ( 125.5597614775786326, -7.894159318335828068, -9.358103419637847864 ) ) ;
#31109=CARTESIAN_POINT ( 'NONE',  ( 114.3846081442453197, -10.63000616557722466, -14.87417383870573495 ) ) ;
#31112=CARTESIAN_POINT ( 'NONE',  ( 126.1837548109119496, 0.4262465694468514643, -12.03445270309931736 ) ) ;
#31113=CARTESIAN_POINT ( 'NONE',  ( 126.5241148109119393, -9.565557343593413364, -10.61323700422348004 ) ) ;
#31115=CARTESIAN_POINT ( 'NONE',  ( 124.9357681442453014, -7.643976991954077427, -18.09477374809248928 ) ) ;
#31120=CARTESIAN_POINT ( 'NONE',  ( 116.3700414775786527, -4.153390946401321671, -8.397313243818183892 ) ) ;
#31124=CARTESIAN_POINT ( 'NONE',  ( 125.9001214775786224, -4.089484607189486809, -7.948022111789456723 ) ) ;
#31125=CARTESIAN_POINT ( 'NONE',  ( 112.2857214775786474, -5.574606645277164318, -18.38911715685844683 ) ) ;
#31127=CARTESIAN_POINT ( 'NONE',  ( 121.4754414775786131, -8.166667518702819706, -8.995218007635861213 ) ) ;
#31129=CARTESIAN_POINT ( 'NONE',  ( 117.0507614775786465, -10.30919188438810075, -12.61870101168855918 ) ) ;
#31131=CARTESIAN_POINT ( 'NONE',  ( 113.5904348109119866, -2.084020599724406786, -8.691656652584148546 ) ) ;
#31132=CARTESIAN_POINT ( 'NONE',  ( 122.3830681442452857, -8.166667518702819706, -8.995218007635861213 ) ) ;
#31133=CARTESIAN_POINT ( 'NONE',  ( 114.7816948109119863, 0.5811942927096154232, -14.16772938898807155 ) ) ;
#31134=CARTESIAN_POINT ( 'NONE',  ( 117.2209414775786485, -2.084020599724406786, -8.691656652584148546 ) ) ;
#31135=ORIENTED_EDGE ( 'NONE', *, *, #1608, .F. ) ;
#31136=CARTESIAN_POINT ( 'NONE',  ( 121.8725281442453223, -6.222761293078241884, -8.102969835052219238 ) ) ;
#31137=CARTESIAN_POINT ( 'NONE',  ( 115.8027748109119841, -0.4660016031367893996, -10.09054647747474043 ) ) ;
#31138=CARTESIAN_POINT ( 'NONE',  ( 124.8223148109119762, -10.15424416112533912, -14.75197769757731336 ) ) ;
#31144=CARTESIAN_POINT ( 'NONE',  ( 125.7299414775786346, 0.9020085738987339008, -11.91225656197089222 ) ) ;
#31147=CARTESIAN_POINT ( 'NONE',  ( 116.5402214775786405, 0.2603800115204892296, -16.42320221600525088 ) ) ;
#31149=CARTESIAN_POINT ( 'NONE',  ( 113.5904348109119866, -2.084020599724406786, -8.691656652584148546 ) ) ;
#31154=CARTESIAN_POINT ( 'NONE',  ( 119.1496481442453046, -3.383040157471821630, -19.15922257007629170 ) ) ;
#31155=CARTESIAN_POINT ( 'NONE',  ( 137.0897189579595192, -6.643744190842751252, -18.48770628774961367 ) ) ;
#31159=CARTESIAN_POINT ( 'NONE',  ( 118.7525614775786380, -8.166667518702801942, -8.995218007635848778 ) ) ;
#31160=CARTESIAN_POINT ( 'NONE',  ( 121.8158014775786171, -4.153390946401325223, -8.397313243818185668 ) ) ;
#31162=CARTESIAN_POINT ( 'NONE',  ( 125.9568481442452850, -6.344957434206665248, -7.627207830600338134 ) ) ;
#31163=CARTESIAN_POINT ( 'NONE',  ( 119.4332814775786318, -0.4660016031367893996, -10.09054647747474043 ) ) ;
#31165=CARTESIAN_POINT ( 'NONE',  ( 114.1577014775786552, -3.505236298600246325, -18.68346056562440793 ) ) ;
#31167=CARTESIAN_POINT ( 'NONE',  ( 113.5904348109119866, -2.084020599724406786, -8.691656652584148546 ) ) ;
#31171=CARTESIAN_POINT ( 'NONE',  ( 120.9081748109119872, -4.153390946401325223, -8.397313243818185668 ) ) ;
#31172=CARTESIAN_POINT ( 'NONE',  ( 120.3409081442453044, -8.899110576539710493, -16.42337572283490132 ) ) ;
#31178=CARTESIAN_POINT ( 'NONE',  ( 112.7962614775786676, -3.383040157471821630, -19.15922257007629170 ) ) ;
#31179=CARTESIAN_POINT ( 'NONE',  ( 114.6115148109119986, -3.383040157471821630, -19.15922257007629170 ) ) ;
#31181=EDGE_CURVE ( 'NONE', #39160, #21122, #29209, .T. ) ;
#31186=CARTESIAN_POINT ( 'NONE',  ( 123.5176014775786228, -9.261995988541697145, -16.69588392320189030 ) ) ;
#31187=CARTESIAN_POINT ( 'NONE',  ( 113.4202548109119846, -10.30919188438810075, -12.61870101168855918 ) ) ;
#31188=CARTESIAN_POINT ( 'NONE',  ( 117.7314814775786260, -5.574606645277164318, -18.38911715685844683 ) ) ;
#31189=B_SPLINE_CURVE_WITH_KNOTS ( 'NONE', 3,
 ( #41160, #22907, #9010, #6492, #44802, #6262, #5794, #2142, #13561, #27016, #2375, #5568, #26561, #3064, #16305, #36800, #19490, #12663, #19946, #20182, #34067, #12892, #44127, #26790, #9921, #40933 ),
 .UNSPECIFIED., .F., .F.,
 ( 4, 1, 1, 2, 2, 1, 1, 1, 2, 2, 2, 1, 1, 1, 2, 2, 4 ),
 ( 0.000000000000000000, 0.06249999999981883936, 0.09374999999972753739, 0.1093749999996763422, 0.1249999999996251332, 0.1874999999994354793, 0.2187499999993496314, 0.2343749999993062216, 0.2421874999992941757, 0.2499999999992821298, 0.3749999999993258171, 0.4374999999993480215, 0.4687499999993595123, 0.4843749999993777200, 0.4921874999993741118, 0.4999999999993705035, 1.000000000000000000 ),
 .UNSPECIFIED. ) ;
#31191=CARTESIAN_POINT ( 'NONE',  ( 121.9859814775786333, 0.2603800115204892296, -16.42320221600525088 ) ) ;
#31192=CARTESIAN_POINT ( 'NONE',  ( 117.6747548109119919, -1.834011780172310813, -8.268836392978581529 ) ) ;
#31194=CARTESIAN_POINT ( 'NONE',  ( 114.1009748109119784, -5.574606645277164318, -18.38911715685844683 ) ) ;
#31195=CARTESIAN_POINT ( 'NONE',  ( 124.9924948109119924, -5.574606645277184747, -18.38911715685844328 ) ) ;
#31197=CARTESIAN_POINT ( 'NONE',  ( 117.5045748109119756, 0.5811942927096110934, -14.16772938898807510 ) ) ;
#31199=CARTESIAN_POINT ( 'NONE',  ( 114.0442481442453300, -1.834011780172310813, -8.268836392978581529 ) ) ;
#31206=CARTESIAN_POINT ( 'NONE',  ( 115.9162281442453093, -5.574606645277164318, -18.38911715685844683 ) ) ;
#31208=CARTESIAN_POINT ( 'NONE',  ( 116.5402214775786405, -9.565557343593413364, -10.61323700422348004 ) ) ;
#31211=CARTESIAN_POINT ( 'NONE',  ( 117.7314814775786260, -5.574606645277164318, -18.38911715685844683 ) ) ;
#31213=CARTESIAN_POINT ( 'NONE',  ( 114.2144281442453178, -8.166667518702817929, -8.995218007635859436 ) ) ;
#31214=CARTESIAN_POINT ( 'NONE',  ( 115.5758681442453053, -7.894159318335828068, -9.358103419637847864 ) ) ;
#31216=CARTESIAN_POINT ( 'NONE',  ( 118.4689281442453392, 0.9020085738987339008, -11.91225656197089222 ) ) ;
#31219=CARTESIAN_POINT ( 'NONE',  ( 111.2184548109119788, -1.295815253274133161, -16.89579513612386563 ) ) ;
#31220=CARTESIAN_POINT ( 'NONE',  ( 112.1721994132789320, -8.900630651041904429, -16.42135045828372597 ) ) ;
#31221=CARTESIAN_POINT ( 'NONE',  ( 123.1205148109119563, -1.834011780172310813, -8.268836392978581529 ) ) ;
#31224=CARTESIAN_POINT ( 'NONE',  ( 118.9227414775786542, 0.4262465694468514643, -12.03445270309931736 ) ) ;
#31225=CARTESIAN_POINT ( 'NONE',  ( 115.7460481442453215, 0.9020085738987339008, -11.91225656197089222 ) ) ;
#31227=ADVANCED_FACE ( 'NONE', ( #26916 ), #10056, .T. ) ;
#31228=CARTESIAN_POINT ( 'NONE',  ( 123.1205148109119563, -1.834011780172310813, -8.268836392978581529 ) ) ;
#31230=CARTESIAN_POINT ( 'NONE',  ( 124.6321897909087966, -1.016270020561755860, -17.26805140881366896 ) ) ;
#31232=CARTESIAN_POINT ( 'NONE',  ( 112.3424481442453384, -6.344957434206662583, -7.627207830600332805 ) ) ;
#31233=CARTESIAN_POINT ( 'NONE',  ( 112.5693548109119888, -10.63000616557722466, -14.87417383870573495 ) ) ;
#31234=CARTESIAN_POINT ( 'NONE',  ( 124.5954081442453116, -3.383040157471821630, -19.15922257007629170 ) ) ;
#31235=CARTESIAN_POINT ( 'NONE',  ( 116.5969481442453031, -9.859900752359374465, -12.68260735090039404 ) ) ;
#31237=CARTESIAN_POINT ( 'NONE',  ( 119.9438214775786378, -7.893985811506177619, -18.51759400769804742 ) ) ;
#31240=CARTESIAN_POINT ( 'NONE',  ( 123.1772414775786189, -5.574606645277164318, -18.38911715685844683 ) ) ;
#31241=ORIENTED_EDGE ( 'NONE', *, *, #30914, .T. ) ;
#31243=CARTESIAN_POINT ( 'NONE',  ( 116.3700414775786527, -5.638512984488999180, -18.83840828888717311 ) ) ;
#31244=CARTESIAN_POINT ( 'NONE',  ( 136.0617147589325668, -8.510257085082880479, -18.03587336798454288 ) ) ;
#31245=VERTEX_POINT ( 'NONE', #37842 ) ;
#31247=CARTESIAN_POINT ( 'NONE',  ( 135.9373687278093996, -1.210166070096996505, -8.718225154784372322 ) ) ;
#31248=CARTESIAN_POINT ( 'NONE',  ( 121.7590748109119687, -7.893985811506177619, -18.51759400769804742 ) ) ;
#31250=CARTESIAN_POINT ( 'NONE',  ( 118.8660148109119774, 0.1319031606808879209, -14.10382304977623669 ) ) ;
#31251=ORIENTED_EDGE ( 'NONE', *, *, #38931, .F. ) ;
#31253=CARTESIAN_POINT ( 'NONE',  ( 114.1009748109119784, -4.089484607189486809, -7.948022111789456723 ) ) ;
#31254=CONICAL_SURFACE ( 'NONE', #31962, 3.499999999999999556, 1.325817663668031887 ) ;
#31255=CARTESIAN_POINT ( 'NONE',  ( 124.9357681442453014, -7.643976991954077427, -18.09477374809248928 ) ) ;
#31258=CARTESIAN_POINT ( 'NONE',  ( 120.9081748109119872, -5.638512984488999180, -18.83840828888717311 ) ) ;
#31261=CARTESIAN_POINT ( 'NONE',  ( 122.7801548109119665, -3.383040157471821630, -19.15922257007629170 ) ) ;
#31262=CARTESIAN_POINT ( 'NONE',  ( 120.1140014775786398, -1.561330072975668504, -17.79121239304076951 ) ) ;
#31263=CARTESIAN_POINT ( 'NONE',  ( 121.5321681442453183, -0.1624402480850797581, -16.17319339645315424 ) ) ;
#31265=CARTESIAN_POINT ( 'NONE',  ( 116.8238548109119819, -4.089484607189486809, -7.948022111789456723 ) ) ;
#31266=ORIENTED_EDGE ( 'NONE', *, *, #40378, .T. ) ;
#31272=CARTESIAN_POINT ( 'NONE',  ( 124.1983214775786166, -8.166667518702819706, -8.995218007635861213 ) ) ;
#31273=CARTESIAN_POINT ( 'NONE',  ( 125.5030348109119558, -6.222761293078241884, -8.102969835052219238 ) ) ;
#31275=CARTESIAN_POINT ( 'NONE',  ( 123.1205148109119563, -1.834011780172310813, -8.268836392978581529 ) ) ;
#31277=CARTESIAN_POINT ( 'NONE',  ( 122.2696148109119889, -5.574606645277198957, -18.38911715685844328 ) ) ;
#31278=CARTESIAN_POINT ( 'NONE',  ( 122.6667014775786413, -7.893985811506177619, -18.51759400769804742 ) ) ;
#31279=CARTESIAN_POINT ( 'NONE',  ( 124.1983214775786166, -8.166667518702819706, -8.995218007635861213 ) ) ;
#31281=CARTESIAN_POINT ( 'NONE',  ( 111.8319081442453182, -5.638512984488999180, -18.83840828888717311 ) ) ;
#31286=CARTESIAN_POINT ( 'NONE',  ( 116.7671281442453335, -7.643976991954077427, -18.09477374809248928 ) ) ;
#31287=CARTESIAN_POINT ( 'NONE',  ( 126.4673881442452910, -7.894159318335828068, -9.358103419637847864 ) ) ;
#31291=CARTESIAN_POINT ( 'NONE',  ( 120.4543614775786295, -5.574606645277164318, -18.38911715685844683 ) ) ;
#31292=CARTESIAN_POINT ( 'NONE',  ( 116.4267681442453153, -6.222761293078241884, -8.102969835052219238 ) ) ;
#31293=CARTESIAN_POINT ( 'NONE',  ( 111.9453614775786434, -7.894159318335828068, -9.358103419637847864 ) ) ;
#31294=EDGE_LOOP ( 'NONE', ( #26494, #35764, #41922, #16165 ) ) ;
#31295=CARTESIAN_POINT ( 'NONE',  ( 124.7088614775786226, -9.565557343593413364, -10.61323700422348004 ) ) ;
#31298=CARTESIAN_POINT ( 'NONE',  ( 112.6260814775786514, -0.8288870151387760510, -10.36305467784173118 ) ) ;
#31304=CARTESIAN_POINT ( 'NONE',  ( 120.2841814775786276, -10.15424416112533912, -14.75197769757731336 ) ) ;
#31305=CARTESIAN_POINT ( 'NONE',  ( 112.0588148109119828, -9.859900752359374465, -12.68260735090039404 ) ) ;
#31314=CARTESIAN_POINT ( 'NONE',  ( 123.0637881442452937, -8.899110576539710493, -16.42337572283490132 ) ) ;
#31315=CARTESIAN_POINT ( 'NONE',  ( 118.9227414775786542, 0.4262465694468514643, -12.03445270309931736 ) ) ;
#31316=CARTESIAN_POINT ( 'NONE',  ( 113.9307948109119764, -10.15424416112533912, -14.75197769757731336 ) ) ;
#31319=CARTESIAN_POINT ( 'NONE',  ( 114.5547881442453217, -4.153390946401321671, -8.397313243818183892 ) ) ;
#31320=CARTESIAN_POINT ( 'NONE',  ( 125.3895814775786448, -2.084020599724406786, -8.691656652584148546 ) ) ;
#31324=CARTESIAN_POINT ( 'NONE',  ( 115.3489614775786407, -9.261995988541697145, -16.69588392320189030 ) ) ;
#31327=CARTESIAN_POINT ( 'NONE',  ( 112.2289948109119848, -1.834011780172310813, -8.268836392978581529 ) ) ;
#31328=CARTESIAN_POINT ( 'NONE',  ( 113.7798197424434363, -0.9924539043446216624, -17.29976612834909133 ) ) ;
#31330=CARTESIAN_POINT ( 'NONE',  ( 111.9453614775786434, -1.561330072975668060, -17.79121239304076596 ) ) ;
#31331=CARTESIAN_POINT ( 'NONE',  ( 114.0442481442453300, -1.834011780172310813, -8.268836392978581529 ) ) ;
#31332=CARTESIAN_POINT ( 'NONE',  ( 123.3474214775786209, -0.1624402480850797581, -16.17319339645315424 ) ) ;
#31337=CARTESIAN_POINT ( 'NONE',  ( 117.9016614775786280, -0.1624402480850797581, -16.17319339645315424 ) ) ;
#31338=EDGE_CURVE ( 'NONE', #42698, #29255, #25984, .T. ) ;
#31343=CARTESIAN_POINT ( 'NONE',  ( 111.5482748109120053, -0.1624402480850797581, -16.17319339645315424 ) ) ;
#31344=CARTESIAN_POINT ( 'NONE',  ( 120.4994581469517101, -3.929494816604745200, -18.62311481910883870 ) ) ;
#31345=CARTESIAN_POINT ( 'NONE',  ( 121.0216281442452981, -1.561330072975668948, -17.79121239304076951 ) ) ;
#31346=CARTESIAN_POINT ( 'NONE',  ( 117.9016614775786280, -9.988377603198976828, -10.36322818467138340 ) ) ;
#31348=CARTESIAN_POINT ( 'NONE',  ( 113.5337081442453240, -0.8288870151387760510, -10.36305467784173118 ) ) ;
#31349=CARTESIAN_POINT ( 'NONE',  ( 122.3263414775786373, -6.344957434206665248, -7.627207830600338134 ) ) ;
#31351=CARTESIAN_POINT ( 'NONE',  ( 117.1074881442453233, -10.63000616557722466, -14.87417383870573495 ) ) ;
#31352=CARTESIAN_POINT ( 'NONE',  ( 116.4267681442453153, -6.222761293078241884, -8.102969835052219238 ) ) ;
#31354=CARTESIAN_POINT ( 'NONE',  ( 119.8303681442453126, 0.4262465694468514643, -12.03445270309931736 ) ) ;
#31356=AXIS2_PLACEMENT_3D ( 'NONE', #9034, #43242, #38185 ) ;
#31357=CARTESIAN_POINT ( 'NONE',  ( 116.3133148109119759, -7.893985811506177619, -18.51759400769804742 ) ) ;
#31358=CARTESIAN_POINT ( 'NONE',  ( 136.9165885681138377, 0.6403260112581466990, -12.97644181253951956 ) ) ;
#31365=CARTESIAN_POINT ( 'NONE',  ( 113.5337081442453240, -9.261995988541697145, -16.69588392320189030 ) ) ;
#31371=CARTESIAN_POINT ( 'NONE',  ( 116.4834948109119779, -1.561330072975668504, -17.79121239304076951 ) ) ;
#31374=CARTESIAN_POINT ( 'NONE',  ( 111.5098340574772777, -2.443475742715324639, -17.86549347949428679 ) ) ;
#31375=CARTESIAN_POINT ( 'NONE',  ( 118.3661624739652183, 0.3208234527006367798, -15.99825685930877839 ) ) ;
#31376=CARTESIAN_POINT ( 'NONE',  ( 123.3474214775786209, -0.1624402480850797581, -16.17319339645315424 ) ) ;
#31377=ORIENTED_EDGE ( 'NONE', *, *, #550, .F. ) ;
#31378=CARTESIAN_POINT ( 'NONE',  ( 135.3184548109119874, -9.609004340414083245, -9.721032963308941177 ) ) ;
#31379=CARTESIAN_POINT ( 'NONE',  ( 122.0994348109119443, 0.9020085738987339008, -11.91225656197089222 ) ) ;
#31381=CARTESIAN_POINT ( 'NONE',  ( 114.8384214775786489, -10.15424416112533912, -14.75197769757731336 ) ) ;
#31382=CARTESIAN_POINT ( 'NONE',  ( 126.0703014775786102, -9.988377603198980381, -10.36322818467138518 ) ) ;
#31385=CARTESIAN_POINT ( 'NONE',  ( 121.0216281442452981, -7.894159318335828068, -9.358103419637847864 ) ) ;
#31387=CARTESIAN_POINT ( 'NONE',  ( 121.2485348109119769, -8.899110576539710493, -16.42337572283490132 ) ) ;
#31393=CARTESIAN_POINT ( 'NONE',  ( 114.8951481442453115, -0.4660016031367893996, -10.09054647747474043 ) ) ;
#31394=CARTESIAN_POINT ( 'NONE',  ( 114.7249681442453237, 0.2603800115204892296, -16.42320221600525088 ) ) ;
#31398=CARTESIAN_POINT ( 'NONE',  ( 117.1030726359456224, -1.179503403430467667, -17.05068175419387089 ) ) ;
#31399=EDGE_CURVE ( 'NONE', #28588, #33070, #30370, .T. ) ;
#31400=CARTESIAN_POINT ( 'NONE',  ( 122.3830681442452857, -8.166667518702819706, -8.995218007635861213 ) ) ;
#31401=CARTESIAN_POINT ( 'NONE',  ( 114.5547881442453217, -5.638512984488999180, -18.83840828888717311 ) ) ;
#31402=CARTESIAN_POINT ( 'NONE',  ( 118.4689281442453392, -10.15424416112533912, -14.75197769757731336 ) ) ;
#31404=CARTESIAN_POINT ( 'NONE',  ( 111.6617281442453304, 0.4262465694468514643, -12.03445270309931736 ) ) ;
#31405=CARTESIAN_POINT ( 'NONE',  ( 117.0507614775786465, -10.30919188438810075, -12.61870101168855918 ) ) ;
#31409=CARTESIAN_POINT ( 'NONE',  ( 113.4202548109119846, 0.1319031606808879209, -14.10382304977623669 ) ) ;
#31412=CARTESIAN_POINT ( 'NONE',  ( 121.3619881442452879, -4.089484607189486809, -7.948022111789456723 ) ) ;
#31414=CARTESIAN_POINT ( 'NONE',  ( 116.5969481442453031, 0.5811942927096154232, -14.16772938898807155 ) ) ;
#31415=ORIENTED_EDGE ( 'NONE', *, *, #45118, .T. ) ;
#31418=CARTESIAN_POINT ( 'NONE',  ( 124.4819548109119722, -7.893985811506177619, -18.51759400769804742 ) ) ;
#31419=CARTESIAN_POINT ( 'NONE',  ( 122.6099748109119929, -9.261995988541706026, -16.69588392320187609 ) ) ;
#31421=EDGE_CURVE ( 'NONE', #37424, #10224, #12530, .T. ) ;
#31423=CARTESIAN_POINT ( 'NONE',  ( 120.6245414775786458, -0.1624402480850797581, -16.17319339645315424 ) ) ;
#31426=CARTESIAN_POINT ( 'NONE',  ( 120.5110881442453206, -3.505236298600246325, -18.68346056562440793 ) ) ;
#31428=CARTESIAN_POINT ( 'NONE',  ( 121.0783548109119749, -9.565557343593413364, -10.61323700422348004 ) ) ;
#31430=CARTESIAN_POINT ( 'NONE',  ( 117.5613014775786525, 0.9020085738987339008, -11.91225656197089222 ) ) ;
#31431=CARTESIAN_POINT ( 'NONE',  ( 123.2339681442453099, -6.344957434206645708, -7.627207830600334582 ) ) ;
#31432=CARTESIAN_POINT ( 'NONE',  ( 117.6180281442453150, -8.899110576539710493, -16.42337572283490132 ) ) ;
#31434=CARTESIAN_POINT ( 'NONE',  ( 116.9940348109119839, -9.988377603198976828, -10.36322818467138340 ) ) ;
#31436=CARTESIAN_POINT ( 'NONE',  ( 115.9162281442453235, -5.574606645277192740, -18.38911715685844328 ) ) ;
#31440=CARTESIAN_POINT ( 'NONE',  ( 123.2339681442453241, -6.344957434206665248, -7.627207830600338134 ) ) ;
#31442=CARTESIAN_POINT ( 'NONE',  ( 118.3578375202278181, -2.239543233855014748, -18.13706010537466895 ) ) ;
#31443=CARTESIAN_POINT ( 'NONE',  ( 117.6747548109119919, -7.643976991954077427, -18.09477374809248928 ) ) ;
#31446=CARTESIAN_POINT ( 'NONE',  ( 125.3328548109119964, -9.261995988541697145, -16.69588392320189030 ) ) ;
#31449=EDGE_CURVE ( 'NONE', #32536, #4879, #30933, .T. ) ;
#31451=CARTESIAN_POINT ( 'NONE',  ( 113.4202548109119846, -10.30919188438810075, -12.61870101168855918 ) ) ;
#31452=CARTESIAN_POINT ( 'NONE',  ( 112.8529881442453302, -1.561330072975668060, -17.79121239304076596 ) ) ;
#31453=CARTESIAN_POINT ( 'NONE',  ( 123.7445081442452874, -1.561330072975668948, -17.79121239304076951 ) ) ;
#31454=CARTESIAN_POINT ( 'NONE',  ( 118.0718414775786442, -0.8288870151387760510, -10.36305467784173118 ) ) ;
#31457=CARTESIAN_POINT ( 'NONE',  ( 117.6180281442453150, -0.4660016031367893996, -10.09054647747474043 ) ) ;
#31459=DIRECTION ( 'NONE',  ( -1.000000000000000000, 0.000000000000000000, 0.000000000000000000 ) ) ;
#31460=CARTESIAN_POINT ( 'NONE',  ( 123.2906948109119867, -1.833838273342659697, -17.42832698103878286 ) ) ;
#31461=ORIENTED_EDGE ( 'NONE', *, *, #27585, .T. ) ;
#31464=CARTESIAN_POINT ( 'NONE',  ( 116.5969481442453031, 0.5811942927096154232, -14.16772938898807155 ) ) ;
#31465=CARTESIAN_POINT ( 'NONE',  ( 136.6675107540889371, -8.468615216776449017, -17.76661867765510650 ) ) ;
#31467=CARTESIAN_POINT ( 'NONE',  ( 137.5098831408856768, -0.7887024016652356417, -10.49420813250452866 ) ) ;
#31468=CARTESIAN_POINT ( 'NONE',  ( 121.3052614775786111, -1.834011780172310813, -8.268836392978581529 ) ) ;
#31470=CARTESIAN_POINT ( 'NONE',  ( 121.0783548109119749, -9.565557343593413364, -10.61323700422348004 ) ) ;
#31472=VERTEX_POINT ( 'NONE', #35067 ) ;
#31473=CIRCLE ( 'NONE', #22752, 0.4999999999999999445 ) ;
#31474=CARTESIAN_POINT ( 'NONE',  ( 113.4769814775786330, -10.63000616557722466, -14.87417383870573495 ) ) ;
#31475=CARTESIAN_POINT ( 'NONE',  ( 124.5386814775786206, -4.153390946401325223, -8.397313243818185668 ) ) ;
#31476=CARTESIAN_POINT ( 'NONE',  ( 112.4925368734311206, -1.223627541775731631, -16.99192386690444323 ) ) ;
#31478=CARTESIAN_POINT ( 'NONE',  ( 113.7798197424434363, -0.9924539043446216624, -17.29976612834909133 ) ) ;
#31479=CARTESIAN_POINT ( 'NONE',  ( 123.6877814775786533, -3.383040157471821630, -19.15922257007629170 ) ) ;
#31483=CARTESIAN_POINT ( 'NONE',  ( 125.1626748109119802, -9.988377603198980381, -10.36322818467138518 ) ) ;
#31484=CARTESIAN_POINT ( 'NONE',  ( 122.7234281442452755, -5.638512984488999180, -18.83840828888717311 ) ) ;
#31485=CARTESIAN_POINT ( 'NONE',  ( 124.9924948109119924, -5.574606645277164318, -18.38911715685844683 ) ) ;
#31487=CARTESIAN_POINT ( 'NONE',  ( 120.3976348109119812, -7.643976991954077427, -18.09477374809248928 ) ) ;
#31488=CARTESIAN_POINT ( 'NONE',  ( 125.6059481442453318, -7.866424907534184996, -9.395035934245763443 ) ) ;
#31489=CARTESIAN_POINT ( 'NONE',  ( 115.6325948109119821, 0.2603800115204892296, -16.42320221600525088 ) ) ;
#31495=CARTESIAN_POINT ( 'NONE',  ( 124.5386814775786206, -5.638512984488999180, -18.83840828888717311 ) ) ;
#31496=CARTESIAN_POINT ( 'NONE',  ( 112.6260814775786514, -9.261995988541697145, -16.69588392320189030 ) ) ;
#31498=CARTESIAN_POINT ( 'NONE',  ( 114.4980614775786734, -2.084020599724406786, -8.691656652584148546 ) ) ;
#31500=CARTESIAN_POINT ( 'NONE',  ( 122.2128881442452979, -7.643976991954104960, -18.09477374809246442 ) ) ;
#31501=CARTESIAN_POINT ( 'NONE',  ( 124.0281414775786146, -1.834011780172310813, -8.268836392978581529 ) ) ;
#31502=CARTESIAN_POINT ( 'NONE',  ( 124.8790414775786246, -0.4660016031367893996, -10.09054647747474043 ) ) ;
#31504=CARTESIAN_POINT ( 'NONE',  ( 114.2711548109119803, -9.988377603198976828, -10.36322818467138340 ) ) ;
#31509=CARTESIAN_POINT ( 'NONE',  ( 116.0296814775786345, -1.833838273342658809, -17.42832698103878286 ) ) ;
#31511=CARTESIAN_POINT ( 'NONE',  ( 126.5808414775786446, -9.859900752359378018, -12.68260735090039759 ) ) ;
#31514=CARTESIAN_POINT ( 'NONE',  ( 120.0005481442453146, -4.153390946401325223, -8.397313243818185668 ) ) ;
#31515=CARTESIAN_POINT ( 'NONE',  ( 119.8870948109119752, -0.8288870151387760510, -10.36305467784173118 ) ) ;
#31516=CARTESIAN_POINT ( 'NONE',  ( 113.8740681442453138, -9.859900752359374465, -12.68260735090039404 ) ) ;
#31518=COLOUR_RGB ( '',0.7921568627450980005, 0.8196078431372548767, 0.9333333333333333481 ) ;
#31522=CARTESIAN_POINT ( 'NONE',  ( 113.7038881442453402, -6.222761293078241884, -8.102969835052219238 ) ) ;
#31525=EDGE_CURVE ( 'NONE', #19842, #37411, #33570, .T. ) ;
#31529=CARTESIAN_POINT ( 'NONE',  ( 116.9940348109119839, -0.1624402480850797581, -16.17319339645315424 ) ) ;
#31530=CARTESIAN_POINT ( 'NONE',  ( 114.2144281442453178, -1.833838273342658809, -17.42832698103878286 ) ) ;
#31531=CYLINDRICAL_SURFACE ( 'NONE', #3467, 2.999999999999998668 ) ;
#31535=CARTESIAN_POINT ( 'NONE',  ( 121.2607668052895491, -1.125321370491285444, -17.12283323191017814 ) ) ;
#31539=CARTESIAN_POINT ( 'NONE',  ( 113.1366214775786432, -1.834011780172310813, -8.268836392978581529 ) ) ;
#31540=CARTESIAN_POINT ( 'NONE',  ( 123.1205148109119563, -7.643976991954077427, -18.09477374809248928 ) ) ;
#31541=CARTESIAN_POINT ( 'NONE',  ( 115.9729548109119861, -3.505236298600246325, -18.68346056562440793 ) ) ;
#31542=DIRECTION ( 'NONE',  ( -1.000000000000000000, 0.000000000000000000, 0.000000000000000000 ) ) ;
#31545=CARTESIAN_POINT ( 'NONE',  ( 114.7249681442453237, -9.565557343593413364, -10.61323700422348004 ) ) ;
#31549=CARTESIAN_POINT ( 'NONE',  ( 125.7299414775786346, 0.9020085738987339008, -11.91225656197089222 ) ) ;
#31550=CARTESIAN_POINT ( 'NONE',  ( 116.3133148109119759, -7.893985811506177619, -18.51759400769804742 ) ) ;
#31552=CARTESIAN_POINT ( 'NONE',  ( 117.9583881442453048, -10.30919188438810075, -12.61870101168855918 ) ) ;
#31553=CARTESIAN_POINT ( 'NONE',  ( 114.2144281442453178, -8.166667518702809048, -8.995218007635852331 ) ) ;
#31555=CARTESIAN_POINT ( 'NONE',  ( 111.8886348109120092, -3.383040157471821630, -19.15922257007629170 ) ) ;
#31556=CARTESIAN_POINT ( 'NONE',  ( 115.1220548109119761, -8.166667518702817929, -8.995218007635861213 ) ) ;
#31557=CARTESIAN_POINT ( 'NONE',  ( 123.4608748109119745, 0.4262465694468514643, -12.03445270309931736 ) ) ;
#31561=CARTESIAN_POINT ( 'NONE',  ( 120.3531401386228907, -1.125321370491285444, -17.12283323191017814 ) ) ;
#31563=CARTESIAN_POINT ( 'NONE',  ( 115.3489614775786407, -0.8288870151387760510, -10.36305467784173118 ) ) ;
#31567=CARTESIAN_POINT ( 'NONE',  ( 121.4964260444391755, -1.267766418764731728, -16.93314635290706605 ) ) ;
#31568=CARTESIAN_POINT ( 'NONE',  ( 124.5954081442453116, -3.383040157471821630, -19.15922257007629170 ) ) ;
#31570=CARTESIAN_POINT ( 'NONE',  ( 125.1626748109119802, -9.988377603198980381, -10.36322818467138518 ) ) ;
#31571=CARTESIAN_POINT ( 'NONE',  ( 115.6325948109119821, 0.2603800115204892296, -16.42320221600525088 ) ) ;
#31574=CARTESIAN_POINT ( 'NONE',  ( 113.4202548109119846, 0.1319031606808879209, -14.10382304977623669 ) ) ;
#31576=CARTESIAN_POINT ( 'NONE',  ( 113.0231681442453322, 0.9020085738987339008, -11.91225656197089222 ) ) ;
#31577=CARTESIAN_POINT ( 'NONE',  ( 118.9794681442453026, -9.261995988541697145, -16.69588392320189030 ) ) ;
#31578=B_SPLINE_CURVE_WITH_KNOTS ( 'NONE', 3,
 ( #19147, #37130, #30090, #26215, #5677, #26890, #22787, #2032, #29861, #12541 ),
 .UNSPECIFIED., .F., .F.,
 ( 4, 3, 3, 4 ),
 ( 0.000000000000000000, 0.0001671877548681270013, 0.0003343755096277669986, 0.0006463528481650629171 ),
 .UNSPECIFIED. ) ;
#31579=CARTESIAN_POINT ( 'NONE',  ( 117.2776681442452968, -4.153390946401325223, -8.397313243818185668 ) ) ;
#31581=CARTESIAN_POINT ( 'NONE',  ( 122.7234281442452755, -4.153390946401325223, -8.397313243818185668 ) ) ;
#31583=CARTESIAN_POINT ( 'NONE',  ( 118.2987481442453088, -1.561330072975668504, -17.79121239304076951 ) ) ;
#31587=DIRECTION ( 'NONE',  ( 0.000000000000000000, -0.6004852223388321697, 0.7996358532186280677 ) ) ;
#31589=CARTESIAN_POINT ( 'NONE',  ( 114.0442481442453300, -1.834011780172310813, -8.268836392978581529 ) ) ;
#31591=CARTESIAN_POINT ( 'NONE',  ( 137.2865145795256581, -10.09372725149439276, -13.46056636665518091 ) ) ;
#31594=CARTESIAN_POINT ( 'NONE',  ( 128.2184548109119930, -4.863998795839242995, -13.39321520033831447 ) ) ;
#31596=CARTESIAN_POINT ( 'NONE',  ( 113.8173414775786512, -9.565557343593413364, -10.61323700422348004 ) ) ;
#31601=CARTESIAN_POINT ( 'NONE',  ( 116.4834948109119779, -1.561330072975668504, -17.79121239304076951 ) ) ;
#31602=LINE ( 'NONE', #14061, #33605 ) ;
#31603=CARTESIAN_POINT ( 'NONE',  ( 120.2841814775786276, -10.15424416112533912, -14.75197769757731336 ) ) ;
#31605=CARTESIAN_POINT ( 'NONE',  ( 136.6675107540776821, -9.237402273161876565, -9.788598779400610184 ) ) ;
#31606=CARTESIAN_POINT ( 'NONE',  ( 124.0848681442452772, -4.089484607189486809, -7.948022111789456723 ) ) ;
#31608=CARTESIAN_POINT ( 'NONE',  ( 114.9518748109119883, -7.643976991954077427, -18.09477374809248928 ) ) ;
#31609=CARTESIAN_POINT ( 'NONE',  ( 112.9097148109120070, -9.565557343593413364, -10.61323700422348004 ) ) ;
#31612=CARTESIAN_POINT ( 'NONE',  ( 119.6601881442453106, -1.833838273342659253, -17.42832698103878286 ) ) ;
#31613=CARTESIAN_POINT ( 'NONE',  ( 121.7590748109119687, -2.084020599724406786, -8.691656652584148546 ) ) ;
#31614=CARTESIAN_POINT ( 'NONE',  ( 114.3278814775786429, 0.1319031606808870605, -14.10382304977625090 ) ) ;
#31619=CARTESIAN_POINT ( 'NONE',  ( 116.7104014775786425, -0.4660016031367893996, -10.09054647747474043 ) ) ;
#31620=CARTESIAN_POINT ( 'NONE',  ( 115.6893214775786447, 0.5811942927096154232, -14.16772938898807155 ) ) ;
#31622=( BOUNDED_SURFACE ( )  B_SPLINE_SURFACE ( 1, 2, ( 
 ( #40848, #19863, #30569, #8923, #15992, #30127, #9603, #16222, #23518, #12804, #27158, #15147, #18568, #44040, #22825, #41080, #16448, #30348, #26926, #2521, #9373, #13255, #6175, #37406, #5712, #23746, #20096, #40388, #2750, #9836, #32460, #36716, #9149, #16673, #44489, #40616, #23055, #37637, #1235, #19406, #36942, #23282, #37166, #5941, #43813, #29669, #43581, #12351, #33752, #33293, #44272, #19630, #13028, #33514, #2294, #13481, #13918, #17127, #21201, #10725, #38078, #3860, #223, #17346, #17782, #14136, #31015, #28052, #41960, #37854, #24625, #24186, #27828, #20542, #31675, #7, #16905, #42183, #31235, #2977, #38508, #30797, #7285, #35079, #41739, #34421, #14361, #41524, #10943, #44722, #10503, #23968, #44945, #3202, #6629, #13703, #445, #3641, #27610, #28274, #24847, #6411, #38293, #20318, #31454, #27384, #10282, #6856, #20763, #34202, #24404, #41307, #10067, #7072, #34642, #3428, #20982, #34855, #17560, #42631, #1341, #25750, #29161, #25304, #43302, #15255, #14812, #11843, #32790, #38739, #667, #28725, #22325, #43075, #4538, #11395, #39656, #8419, #25075, #32125, #15036, #18462, #28947, #35536, #29389, #35307, #4079, #11614, #11171, #32352, #14583, #4761, #39196, #1118, #28501, #42855, #4308, #36221, #4986, #7962, #18899, #32574, #25525, #1562, #15485, #18230, #12071, #7508, #38968, #21423, #21873, #39429, #7737, #18003, #8194, #31901, #42407, #22102, #21647, #893, #35768, #35990, #18683, #33457, #40104, #33921, #15940, #30515, #22544, #16168, #43529, #19354, #8865, #26197, #22766, #19807, #23230, #12298, #44217, #33695, #2692, #12747, #40790, #5885, #33012, #36663, #26424, #5436, #8644, #30071, #44437, #25973, #19577, #29840, #16622, #15711, #33242, #43758, #12524, #2466, #29614, #16390, #40331, #37112, #1786, #26648, #9096, #30290, #40563, #37348, #2015, #22997, #36888, #12978, #5658, #26873, #2236, #39879, #36442, #5210, #43983, #9322, #19129, #9547, #23462, #6121, #20039, #3375, #7232, #45105, #3155, #34806, #13864, #24576, #20266, #10010, #24136 ),
 ( #23919, #30968, #6804, #27777, #27105, #23695, #21149, #31627, #28003, #38461, #37800, #41689, #170, #27334, #35022, #24354, #37581, #14086, #3805, #6576, #20713, #17730, #13204, #41252, #44891, #30744, #17295, #17075, #10451, #34592, #31187, #41027, #16852, #20493, #10229, #13651, #38242, #41909, #9780, #7021, #3592, #6354, #27557, #20932, #34373, #44668, #41470, #34152, #2922, #17503, #31401, #10673, #13430, #38029, #35714, #28446, #395, #28227, #38912, #25698, #7683, #25249, #17952, #21371, #18847, #21597, #4031, #1069, #839, #7912, #11339, #32302, #25019, #42133, #11790, #39147, #4711, #21819, #39379, #35484, #24793, #8146, #14758, #4932, #7451, #35254, #14308, #10893, #31851, #29110, #38686, #28674, #14982, #42577, #621, #14531, #18632, #39605, #32071, #4488, #18410, #28894, #11119, #8366, #42357, #4257, #42806, #18175, #11567, #22049, #35942, #25474, #32519, #1294, #15206, #43022, #22271, #36165, #15432, #44162, #26370, #37058, #12470, #26596, #12246, #12018, #40509, #33185, #37289, #39825, #8593, #32738, #6059, #5157, #16337, #1513, #1960, #2179, #15888, #25921, #29339, #5830, #12926, #19306, #29784, #43696, #33404, #43479, #26822, #29562, #43253, #5604, #22491, #36385, #9269, #23180, #40045, #19074, #32960, #40734, #1736, #26143, #16110, #19751, #19527, #15661, #30011, #8813, #30240, #22715, #9490, #33635, #36614, #5389, #40279, #9044, #43929, #22943, #36835, #23406, #12696, #2410, #124, #16797, #3320, #6972, #34100, #31349, #31132, #30464, #20881, #41860, #13379, #13595, #24524, #19979, #2868, #6524, #37522, #24084, #23868, #20664, #27504, #41423, #10622, #23636, #30694, #17025, #37754, #37979, #3539, #16569, #6753, #10399, #44384, #34324, #17241, #44612, #6295, #27280, #14036, #38411, #41644, #10178, #17454, #34539, #9955, #45056, #41195, #33868, #2637, #20440, #27953, #3097, #44839, #20215, #40969, #13147, #30916, #13816, #27727, #27051, #24309, #9724, #38195, #34756, #24737, #570, #21320, #7402, #35206, #1016, #4436, #38626, #25423, #14932, #15154 ) ),
 .UNSPECIFIED., .F., .F., .T. ) 
 B_SPLINE_SURFACE_WITH_KNOTS ( ( 2, 2 ),
 ( 3, 2, 2, 2, 2, 2, 2, 2, 2, 2, 2, 2, 2, 2, 2, 2, 2, 2, 2, 2, 2, 2, 2, 2, 2, 2, 2, 2, 2, 2, 2, 2, 2, 2, 2, 2, 2, 2, 2, 2, 2, 2, 2, 2, 2, 2, 2, 2, 2, 2, 2, 2, 2, 2, 2, 2, 2, 2, 2, 2, 2, 2, 2, 2, 2, 2, 2, 2, 2, 2, 2, 2, 2, 2, 2, 2, 2, 2, 2, 2, 2, 2, 2, 2, 2, 2, 2, 2, 2, 2, 2, 2, 2, 2, 2, 2, 2, 2, 2, 2, 2, 2, 2, 2, 2, 2, 2, 2, 2, 2, 2, 2, 2, 2, 2, 2, 2, 2, 2, 2, 2, 2, 2, 2, 2, 2, 2, 2, 3 ),
 ( 0.000000000000000000, 1.000000000000000000 ),
 ( 0.000000000000000000, 0.007812500000000000000, 0.01562500000000000000, 0.02343750000000000000, 0.03125000000000000000, 0.03906250000000000000, 0.04687500000000000000, 0.05468750000000000000, 0.06250000000000000000, 0.07031250000000000000, 0.07812500000000000000, 0.08593750000000000000, 0.09375000000000000000, 0.1015625000000000000, 0.1093750000000000000, 0.1171875000000000000, 0.1250000000000000000, 0.1328125000000000000, 0.1406250000000000000, 0.1484375000000000000, 0.1562500000000000000, 0.1640625000000000000, 0.1718750000000000000, 0.1796875000000000000, 0.1875000000000000000, 0.1953125000000000000, 0.2031250000000000000, 0.2109375000000000000, 0.2187500000000000000, 0.2265625000000000000, 0.2343750000000000000, 0.2421875000000000000, 0.2500000000000000000, 0.2578125000000000000, 0.2656250000000000000, 0.2734375000000000000, 0.2812500000000000000, 0.2890625000000000000, 0.2968750000000000000, 0.3046875000000000000, 0.3125000000000000000, 0.3203125000000000000, 0.3281250000000000000, 0.3359375000000000000, 0.3437500000000000000, 0.3515625000000000000, 0.3593750000000000000, 0.3671875000000000000, 0.3750000000000000000, 0.3828125000000000000, 0.3906250000000000000, 0.3984375000000000000, 0.4062500000000000000, 0.4140625000000000000, 0.4218750000000000000, 0.4296875000000000000, 0.4375000000000000000, 0.4453125000000000000, 0.4531250000000000000, 0.4609375000000000000, 0.4687500000000000000, 0.4765625000000000000, 0.4843750000000000000, 0.4921875000000000000, 0.5000000000000000000, 0.5078125000000000000, 0.5156250000000000000, 0.5234375000000000000, 0.5312500000000000000, 0.5390625000000000000, 0.5468750000000000000, 0.5546875000000000000, 0.5625000000000000000, 0.5703125000000000000, 0.5781250000000000000, 0.5859375000000000000, 0.5937500000000000000, 0.6015625000000000000, 0.6093750000000000000, 0.6171875000000000000, 0.6250000000000000000, 0.6328125000000000000, 0.6406250000000000000, 0.6484375000000000000, 0.6562500000000000000, 0.6640625000000000000, 0.6718750000000000000, 0.6796875000000000000, 0.6875000000000000000, 0.6953125000000000000, 0.7031250000000000000, 0.7109375000000000000, 0.7187500000000000000, 0.7265625000000000000, 0.7343750000000000000, 0.7421875000000000000, 0.7500000000000000000, 0.7578125000000000000, 0.7656250000000000000, 0.7734375000000000000, 0.7812500000000000000, 0.7890625000000000000, 0.7968750000000000000, 0.8046875000000000000, 0.8125000000000000000, 0.8203125000000000000, 0.8281250000000000000, 0.8359375000000000000, 0.8437500000000000000, 0.8515625000000000000, 0.8593750000000000000, 0.8671875000000000000, 0.8750000000000000000, 0.8828125000000000000, 0.8906250000000000000, 0.8984375000000000000, 0.9062500000000000000, 0.9140625000000000000, 0.9218750000000000000, 0.9296875000000000000, 0.9375000000000000000, 0.9453125000000000000, 0.9531250000000000000, 0.9609375000000000000, 0.9687500000000000000, 0.9765625000000000000, 0.9843750000000000000, 0.9921875000000000000, 1.000000000000000000 ),
 .UNSPECIFIED. ) 
 GEOMETRIC_REPRESENTATION_ITEM ( )  RATIONAL_B_SPLINE_SURFACE ( (
 ( 1.000000000000000000, 0.9238795325112869605, 1.000000000000000000, 0.9238795325112869605, 1.000000000000000000, 0.9238795325112869605, 1.000000000000000000, 0.9238795325112869605, 1.000000000000000000, 0.9238795325112869605, 1.000000000000000000, 0.9238795325112869605, 1.000000000000000000, 0.9238795325112869605, 1.000000000000000000, 0.9238795325112869605, 1.000000000000000000, 0.9238795325112869605, 1.000000000000000000, 0.9238795325112869605, 1.000000000000000000, 0.9238795325112869605, 1.000000000000000000, 0.9238795325112869605, 1.000000000000000000, 0.9238795325112869605, 1.000000000000000000, 0.9238795325112869605, 1.000000000000000000, 0.9238795325112869605, 1.000000000000000000, 0.9238795325112869605, 1.000000000000000000, 0.9238795325112869605, 1.000000000000000000, 0.9238795325112869605, 1.000000000000000000, 0.9238795325112869605, 1.000000000000000000, 0.9238795325112869605, 1.000000000000000000, 0.9238795325112869605, 1.000000000000000000, 0.9238795325112869605, 1.000000000000000000, 0.9238795325112869605, 1.000000000000000000, 0.9238795325112869605, 1.000000000000000000, 0.9238795325112869605, 1.000000000000000000, 0.9238795325112869605, 1.000000000000000000, 0.9238795325112869605, 1.000000000000000000, 0.9238795325112869605, 1.000000000000000000, 0.9238795325112869605, 1.000000000000000000, 0.9238795325112869605, 1.000000000000000000, 0.9238795325112869605, 1.000000000000000000, 0.9238795325112869605, 1.000000000000000000, 0.9238795325112869605, 1.000000000000000000, 0.9238795325112869605, 1.000000000000000000, 0.9238795325112869605, 1.000000000000000000, 0.9238795325112869605, 1.000000000000000000, 0.9238795325112869605, 1.000000000000000000, 0.9238795325112869605, 1.000000000000000000, 0.9238795325112869605, 1.000000000000000000, 0.9238795325112869605, 1.000000000000000000, 0.9238795325112869605, 1.000000000000000000, 0.9238795325112869605, 1.000000000000000000, 0.9238795325112869605, 1.000000000000000000, 0.9238795325112869605, 1.000000000000000000, 0.9238795325112869605, 1.000000000000000000, 0.9238795325112869605, 1.000000000000000000, 0.9238795325112869605, 1.000000000000000000, 0.9238795325112869605, 1.000000000000000000, 0.9238795325112869605, 1.000000000000000000, 0.9238795325112869605, 1.000000000000000000, 0.9238795325112869605, 1.000000000000000000, 0.9238795325112869605, 1.000000000000000000, 0.9238795325112869605, 1.000000000000000000, 0.9238795325112869605, 1.000000000000000000, 0.9238795325112869605, 1.000000000000000000, 0.9238795325112869605, 1.000000000000000000, 0.9238795325112869605, 1.000000000000000000, 0.9238795325112869605, 1.000000000000000000, 0.9238795325112869605, 1.000000000000000000, 0.9238795325112869605, 1.000000000000000000, 0.9238795325112869605, 1.000000000000000000, 0.9238795325112869605, 1.000000000000000000, 0.9238795325112869605, 1.000000000000000000, 0.9238795325112869605, 1.000000000000000000, 0.9238795325112869605, 1.000000000000000000, 0.9238795325112869605, 1.000000000000000000, 0.9238795325112869605, 1.000000000000000000, 0.9238795325112869605, 1.000000000000000000, 0.9238795325112869605, 1.000000000000000000, 0.9238795325112869605, 1.000000000000000000, 0.9238795325112869605, 1.000000000000000000, 0.9238795325112869605, 1.000000000000000000, 0.9238795325112869605, 1.000000000000000000, 0.9238795325112869605, 1.000000000000000000, 0.9238795325112869605, 1.000000000000000000, 0.9238795325112869605, 1.000000000000000000, 0.9238795325112869605, 1.000000000000000000, 0.9238795325112869605, 1.000000000000000000, 0.9238795325112869605, 1.000000000000000000, 0.9238795325112869605, 1.000000000000000000, 0.9238795325112869605, 1.000000000000000000, 0.9238795325112869605, 1.000000000000000000, 0.9238795325112869605, 1.000000000000000000, 0.9238795325112869605, 1.000000000000000000, 0.9238795325112869605, 1.000000000000000000, 0.9238795325112869605, 1.000000000000000000, 0.9238795325112869605, 1.000000000000000000, 0.9238795325112869605, 1.000000000000000000, 0.9238795325112869605, 1.000000000000000000, 0.9238795325112869605, 1.000000000000000000, 0.9238795325112869605, 1.000000000000000000, 0.9238795325112869605, 1.000000000000000000, 0.9238795325112869605, 1.000000000000000000, 0.9238795325112869605, 1.000000000000000000, 0.9238795325112869605, 1.000000000000000000, 0.9238795325112869605, 1.000000000000000000, 0.9238795325112869605, 1.000000000000000000, 0.9238795325112869605, 1.000000000000000000, 0.9238795325112869605, 1.000000000000000000, 0.9238795325112869605, 1.000000000000000000, 0.9238795325112869605, 1.000000000000000000, 0.9238795325112869605, 1.000000000000000000, 0.9238795325112869605, 1.000000000000000000, 0.9238795325112869605, 1.000000000000000000, 0.9238795325112869605, 1.000000000000000000, 0.9238795325112869605, 1.000000000000000000, 0.9238795325112869605, 1.000000000000000000, 0.9238795325112869605, 1.000000000000000000, 0.9238795325112869605, 1.000000000000000000, 0.9238795325112869605, 1.000000000000000000, 0.9238795325112869605, 1.000000000000000000, 0.9238795325112869605, 1.000000000000000000, 0.9238795325112869605, 1.000000000000000000, 0.9238795325112869605, 1.000000000000000000, 0.9238795325112869605, 1.000000000000000000, 0.9238795325112869605, 1.000000000000000000, 0.9238795325112869605, 1.000000000000000000, 0.9238795325112869605, 1.000000000000000000, 0.9238795325112869605, 1.000000000000000000, 0.9238795325112869605, 1.000000000000000000, 0.9238795325112869605, 1.000000000000000000, 0.9238795325112869605, 1.000000000000000000, 0.9238795325112869605, 1.000000000000000000, 0.9238795325112869605, 1.000000000000000000, 0.9238795325112869605, 1.000000000000000000, 0.9238795325112869605, 1.000000000000000000, 0.9238795325112869605, 1.000000000000000000, 0.9238795325112869605, 1.000000000000000000),
 ( 1.000000000000000000, 0.9238795325112869605, 1.000000000000000000, 0.9238795325112869605, 1.000000000000000000, 0.9238795325112869605, 1.000000000000000000, 0.9238795325112869605, 1.000000000000000000, 0.9238795325112869605, 1.000000000000000000, 0.9238795325112869605, 1.000000000000000000, 0.9238795325112869605, 1.000000000000000000, 0.9238795325112869605, 1.000000000000000000, 0.9238795325112869605, 1.000000000000000000, 0.9238795325112869605, 1.000000000000000000, 0.9238795325112869605, 1.000000000000000000, 0.9238795325112869605, 1.000000000000000000, 0.9238795325112869605, 1.000000000000000000, 0.9238795325112869605, 1.000000000000000000, 0.9238795325112869605, 1.000000000000000000, 0.9238795325112869605, 1.000000000000000000, 0.9238795325112869605, 1.000000000000000000, 0.9238795325112869605, 1.000000000000000000, 0.9238795325112869605, 1.000000000000000000, 0.9238795325112869605, 1.000000000000000000, 0.9238795325112869605, 1.000000000000000000, 0.9238795325112869605, 1.000000000000000000, 0.9238795325112869605, 1.000000000000000000, 0.9238795325112869605, 1.000000000000000000, 0.9238795325112869605, 1.000000000000000000, 0.9238795325112869605, 1.000000000000000000, 0.9238795325112869605, 1.000000000000000000, 0.9238795325112869605, 1.000000000000000000, 0.9238795325112869605, 1.000000000000000000, 0.9238795325112869605, 1.000000000000000000, 0.9238795325112869605, 1.000000000000000000, 0.9238795325112869605, 1.000000000000000000, 0.9238795325112869605, 1.000000000000000000, 0.9238795325112869605, 1.000000000000000000, 0.9238795325112869605, 1.000000000000000000, 0.9238795325112869605, 1.000000000000000000, 0.9238795325112869605, 1.000000000000000000, 0.9238795325112869605, 1.000000000000000000, 0.9238795325112869605, 1.000000000000000000, 0.9238795325112869605, 1.000000000000000000, 0.9238795325112869605, 1.000000000000000000, 0.9238795325112869605, 1.000000000000000000, 0.9238795325112869605, 1.000000000000000000, 0.9238795325112869605, 1.000000000000000000, 0.9238795325112869605, 1.000000000000000000, 0.9238795325112869605, 1.000000000000000000, 0.9238795325112869605, 1.000000000000000000, 0.9238795325112869605, 1.000000000000000000, 0.9238795325112869605, 1.000000000000000000, 0.9238795325112869605, 1.000000000000000000, 0.9238795325112869605, 1.000000000000000000, 0.9238795325112869605, 1.000000000000000000, 0.9238795325112869605, 1.000000000000000000, 0.9238795325112869605, 1.000000000000000000, 0.9238795325112869605, 1.000000000000000000, 0.9238795325112869605, 1.000000000000000000, 0.9238795325112869605, 1.000000000000000000, 0.9238795325112869605, 1.000000000000000000, 0.9238795325112869605, 1.000000000000000000, 0.9238795325112869605, 1.000000000000000000, 0.9238795325112869605, 1.000000000000000000, 0.9238795325112869605, 1.000000000000000000, 0.9238795325112869605, 1.000000000000000000, 0.9238795325112869605, 1.000000000000000000, 0.9238795325112869605, 1.000000000000000000, 0.9238795325112869605, 1.000000000000000000, 0.9238795325112869605, 1.000000000000000000, 0.9238795325112869605, 1.000000000000000000, 0.9238795325112869605, 1.000000000000000000, 0.9238795325112869605, 1.000000000000000000, 0.9238795325112869605, 1.000000000000000000, 0.9238795325112869605, 1.000000000000000000, 0.9238795325112869605, 1.000000000000000000, 0.9238795325112869605, 1.000000000000000000, 0.9238795325112869605, 1.000000000000000000, 0.9238795325112869605, 1.000000000000000000, 0.9238795325112869605, 1.000000000000000000, 0.9238795325112869605, 1.000000000000000000, 0.9238795325112869605, 1.000000000000000000, 0.9238795325112869605, 1.000000000000000000, 0.9238795325112869605, 1.000000000000000000, 0.9238795325112869605, 1.000000000000000000, 0.9238795325112869605, 1.000000000000000000, 0.9238795325112869605, 1.000000000000000000, 0.9238795325112869605, 1.000000000000000000, 0.9238795325112869605, 1.000000000000000000, 0.9238795325112869605, 1.000000000000000000, 0.9238795325112869605, 1.000000000000000000, 0.9238795325112869605, 1.000000000000000000, 0.9238795325112869605, 1.000000000000000000, 0.9238795325112869605, 1.000000000000000000, 0.9238795325112869605, 1.000000000000000000, 0.9238795325112869605, 1.000000000000000000, 0.9238795325112869605, 1.000000000000000000, 0.9238795325112869605, 1.000000000000000000, 0.9238795325112869605, 1.000000000000000000, 0.9238795325112869605, 1.000000000000000000, 0.9238795325112869605, 1.000000000000000000, 0.9238795325112869605, 1.000000000000000000, 0.9238795325112869605, 1.000000000000000000, 0.9238795325112869605, 1.000000000000000000, 0.9238795325112869605, 1.000000000000000000, 0.9238795325112869605, 1.000000000000000000, 0.9238795325112869605, 1.000000000000000000, 0.9238795325112869605, 1.000000000000000000, 0.9238795325112869605, 1.000000000000000000, 0.9238795325112869605, 1.000000000000000000, 0.9238795325112869605, 1.000000000000000000, 0.9238795325112869605, 1.000000000000000000, 0.9238795325112869605, 1.000000000000000000, 0.9238795325112869605, 1.000000000000000000, 0.9238795325112869605, 1.000000000000000000, 0.9238795325112869605, 1.000000000000000000, 0.9238795325112869605, 1.000000000000000000, 0.9238795325112869605, 1.000000000000000000, 0.9238795325112869605, 1.000000000000000000, 0.9238795325112869605, 1.000000000000000000, 0.9238795325112869605, 1.000000000000000000, 0.9238795325112869605, 1.000000000000000000, 0.9238795325112869605, 1.000000000000000000, 0.9238795325112869605, 1.000000000000000000, 0.9238795325112869605, 1.000000000000000000, 0.9238795325112869605, 1.000000000000000000, 0.9238795325112869605, 1.000000000000000000, 0.9238795325112869605, 1.000000000000000000, 0.9238795325112869605, 1.000000000000000000, 0.9238795325112869605, 1.000000000000000000, 0.9238795325112869605, 1.000000000000000000) ) ) 
 REPRESENTATION_ITEM ( '' )  SURFACE ( )  );
#31626=CARTESIAN_POINT ( 'NONE',  ( 123.8579614775786126, 0.5811942927096110934, -14.16772938898807510 ) ) ;
#31627=CARTESIAN_POINT ( 'NONE',  ( 112.1155414775786454, 0.9020085738987339008, -11.91225656197089222 ) ) ;
#31628=CARTESIAN_POINT ( 'NONE',  ( 123.1772414775786189, -5.574606645277164318, -18.38911715685844683 ) ) ;
#31629=( NAMED_UNIT ( * ) PLANE_ANGLE_UNIT ( ) SI_UNIT ( $, .RADIAN. ) );
#31630=CARTESIAN_POINT ( 'NONE',  ( 123.9714148109119805, -0.4660016031367893996, -10.09054647747474043 ) ) ;
#31631=CARTESIAN_POINT ( 'NONE',  ( 120.7947214775786193, -9.261995988541697145, -16.69588392320189030 ) ) ;
#31633=CARTESIAN_POINT ( 'NONE',  ( 116.8238548109119819, -5.574606645277164318, -18.38911715685844683 ) ) ;
#31636=CARTESIAN_POINT ( 'NONE',  ( 120.3409081442453044, -0.4660016031367893996, -10.09054647747474043 ) ) ;
#31638=CARTESIAN_POINT ( 'NONE',  ( 115.2355081442453155, -10.30919188438810075, -12.61870101168855918 ) ) ;
#31641=CARTESIAN_POINT ( 'NONE',  ( 125.6732148109119862, 0.5811942927096110934, -14.16772938898807510 ) ) ;
#31643=CARTESIAN_POINT ( 'NONE',  ( 116.6536748109119941, -10.15424416112533912, -14.75197769757731336 ) ) ;
#31645=CARTESIAN_POINT ( 'NONE',  ( 118.1852948109119836, -4.153390946401325223, -8.397313243818185668 ) ) ;
#31647=CARTESIAN_POINT ( 'NONE',  ( 122.2696148109119889, -5.574606645277164318, -18.38911715685844683 ) ) ;
#31651=CARTESIAN_POINT ( 'NONE',  ( 119.7169148109119874, -0.1624402480850797581, -16.17319339645315424 ) ) ;
#31653=CARTESIAN_POINT ( 'NONE',  ( 114.5547881442453217, -5.638512984488999180, -18.83840828888717311 ) ) ;
#31655=CARTESIAN_POINT ( 'NONE',  ( 120.5678148109119832, -1.833838273342659253, -17.42832698103878286 ) ) ;
#31657=CARTESIAN_POINT ( 'NONE',  ( 117.5045748109119756, 0.5811942927096110934, -14.16772938898807510 ) ) ;
#31659=LINE ( 'NONE', #28485, #7358 ) ;
#31662=CARTESIAN_POINT ( 'NONE',  ( 122.3830681442452857, -8.166667518702819706, -8.995218007635861213 ) ) ;
#31663=VERTEX_POINT ( 'NONE', #25292 ) ;
#31664=CARTESIAN_POINT ( 'NONE',  ( 118.6591994150595895, -2.423081321603731908, -17.89265170041263175 ) ) ;
#31665=CARTESIAN_POINT ( 'NONE',  ( 120.7947214775786193, -0.8288870151387760510, -10.36305467784173118 ) ) ;
#31672=CARTESIAN_POINT ( 'NONE',  ( 114.0442481442453300, -1.834011780172310813, -8.268836392978581529 ) ) ;
#31673=CARTESIAN_POINT ( 'NONE',  ( 125.9568481442452850, -3.505236298600246325, -18.68346056562440793 ) ) ;
#31674=CARTESIAN_POINT ( 'NONE',  ( 121.7023481442452777, -9.261995988541697145, -16.69588392320189030 ) ) ;
#31675=CARTESIAN_POINT ( 'NONE',  ( 116.3700414775786527, -4.153390946401321671, -8.397313243818183892 ) ) ;
#31678=CARTESIAN_POINT ( 'NONE',  ( 121.4754414775786131, -8.166667518702819706, -8.995218007635861213 ) ) ;
#31679=CARTESIAN_POINT ( 'NONE',  ( 123.4608748109119745, 0.4262465694468626776, -12.03445270309935111 ) ) ;
#31682=CARTESIAN_POINT ( 'NONE',  ( 124.2550481442452792, -0.1624402480850797581, -16.17319339645315424 ) ) ;
#31683=ORIENTED_EDGE ( 'NONE', *, *, #11469, .F. ) ;
#31687=CARTESIAN_POINT ( 'NONE',  ( 119.2631014775786298, 0.2603800115204892296, -16.42320221600525088 ) ) ;
#31688=CARTESIAN_POINT ( 'NONE',  ( 124.4819548109119722, -2.084020599724406786, -8.691656652584148546 ) ) ;
#31690=CARTESIAN_POINT ( 'NONE',  ( 136.1673833308536530, 0.5777653812705602077, -11.18378269846704853 ) ) ;
#31691=CARTESIAN_POINT ( 'NONE',  ( 120.9081748109119872, -5.638512984488999180, -18.83840828888717311 ) ) ;
#31694=CARTESIAN_POINT ( 'NONE',  ( 119.5467348109119712, -5.574606645277164318, -18.38911715685844683 ) ) ;
#31695=ORIENTED_EDGE ( 'NONE', *, *, #37297, .F. ) ;
#31696=CARTESIAN_POINT ( 'NONE',  ( 113.9307948109119906, 0.9020085738987339008, -11.91225656197089222 ) ) ;
#31698=CARTESIAN_POINT ( 'NONE',  ( 112.7547603923315762, -1.063912429576153063, -17.20460841810474761 ) ) ;
#31700=CARTESIAN_POINT ( 'NONE',  ( 124.5954081442453116, -3.383040157471821630, -19.15922257007629170 ) ) ;
#31704=CARTESIAN_POINT ( 'NONE',  ( 123.0070614775786169, 0.9020085738987339008, -11.91225656197089222 ) ) ;
#31705=CARTESIAN_POINT ( 'NONE',  ( 123.5176014775786228, -9.261995988541697145, -16.69588392320189030 ) ) ;
#31706=CARTESIAN_POINT ( 'NONE',  ( 123.4041481442452834, 0.1319031606808879209, -14.10382304977623669 ) ) ;
#31707=CARTESIAN_POINT ( 'NONE',  ( 119.9438214775786378, -2.084020599724406786, -8.691656652584148546 ) ) ;
#31709=CARTESIAN_POINT ( 'NONE',  ( 115.5758681442453053, -1.561330072975668060, -17.79121239304076951 ) ) ;
#31713=EDGE_CURVE ( 'NONE', #36520, #39978, #16483, .T. ) ;
#31714=CARTESIAN_POINT ( 'NONE',  ( 125.1521348109119742, -1.861572684144302992, -17.39139446643087084 ) ) ;
#31718=CARTESIAN_POINT ( 'NONE',  ( 125.7299414775786346, 0.9020085738987339008, -11.91225656197089222 ) ) ;
#31719=CARTESIAN_POINT ( 'NONE',  ( 112.6828081442453282, -7.893985811506177619, -18.51759400769804742 ) ) ;
#31720=ORIENTED_EDGE ( 'NONE', *, *, #43308, .F. ) ;
#31721=CARTESIAN_POINT ( 'NONE',  ( 114.4413348109119823, -0.8288870151387760510, -10.36305467784173118 ) ) ;
#31723=CARTESIAN_POINT ( 'NONE',  ( 125.2194014775786286, -10.30919188438810075, -12.61870101168855918 ) ) ;
#31724=CARTESIAN_POINT ( 'NONE',  ( 125.9001214775786224, -4.089484607189486809, -7.948022111789456723 ) ) ;
#31727=CARTESIAN_POINT ( 'NONE',  ( 115.4624148109119943, -5.638512984488999180, -18.83840828888717311 ) ) ;
#31733=CARTESIAN_POINT ( 'NONE',  ( 114.1009748109119784, -5.574606645277164318, -18.38911715685844683 ) ) ;
#31734=CARTESIAN_POINT ( 'NONE',  ( 111.8886348109120092, -3.383040157471821630, -19.15922257007629170 ) ) ;
#31738=EDGE_CURVE ( 'NONE', #17999, #34005, #35076, .T. ) ;
#31739=CARTESIAN_POINT ( 'NONE',  ( 124.1415948109119540, -3.505236298600246325, -18.68346056562440793 ) ) ;
#31740=CARTESIAN_POINT ( 'NONE',  ( 120.0005481442453146, -4.153390946401325223, -8.397313243818185668 ) ) ;
#31741=CARTESIAN_POINT ( 'NONE',  ( 111.2646414775786496, -8.899110576539710493, -16.42337572283490132 ) ) ;
#31743=ADVANCED_FACE ( 'NONE', ( #44305 ), #30158, .T. ) ;
#31745=CARTESIAN_POINT ( 'NONE',  ( 125.2194014775786286, 0.1319031606808879209, -14.10382304977623669 ) ) ;
#31748=CARTESIAN_POINT ( 'NONE',  ( 112.3424481442453384, -3.505236298600246325, -18.68346056562440793 ) ) ;
#31750=CARTESIAN_POINT ( 'NONE',  ( 126.2333338125929458, -8.954712395367375066, -16.28134568519805470 ) ) ;
#31754=CARTESIAN_POINT ( 'NONE',  ( 117.3911214775786505, -7.894159318335828068, -9.358103419637847864 ) ) ;
#31755=CARTESIAN_POINT ( 'NONE',  ( 112.8529881442453160, -7.894159318335828068, -9.358103419637847864 ) ) ;
#31763=CARTESIAN_POINT ( 'NONE',  ( 127.7425183523501744, 0.8652765085452543969, -12.77968882490997338 ) ) ;
#31764=CARTESIAN_POINT ( 'NONE',  ( 113.1366214775786432, -1.834011780172310813, -8.268836392978581529 ) ) ;
#31765=CARTESIAN_POINT ( 'NONE',  ( 118.1285681442453068, -2.084020599724406786, -8.691656652584148546 ) ) ;
#31766=PLANE ( 'NONE',  #24315 ) ;
#31768=CARTESIAN_POINT ( 'NONE',  ( 115.5191414775786569, -6.222761293078241884, -8.102969835052219238 ) ) ;
#31773=CARTESIAN_POINT ( 'NONE',  ( 116.3700414775786527, -5.638512984488999180, -18.83840828888717311 ) ) ;
#31775=CARTESIAN_POINT ( 'NONE',  ( 118.1285681442453068, -7.893985811506177619, -18.51759400769804742 ) ) ;
#31778=CARTESIAN_POINT ( 'NONE',  ( 114.3846081442453197, -10.63000616557722466, -14.87417383870573495 ) ) ;
#31779=CARTESIAN_POINT ( 'NONE',  ( 114.3846081442453197, -10.63000616557722466, -14.87417383870573495 ) ) ;
#31787=CARTESIAN_POINT ( 'NONE',  ( 115.8595014775786609, -7.643976991954077427, -18.09477374809248928 ) ) ;
#31789=CARTESIAN_POINT ( 'NONE',  ( 122.7777921015961198, -1.040089454026960292, -17.23633227186633476 ) ) ;
#31791=CARTESIAN_POINT ( 'NONE',  ( 126.3243314201107097, -4.538965831925366956, -8.350727740338225402 ) ) ;
#31792=CARTESIAN_POINT ( 'NONE',  ( 111.2646414775786496, -8.899110576539710493, -16.42337572283490132 ) ) ;
#31793=LINE ( 'NONE', #21315, #19708 ) ;
#31794=CARTESIAN_POINT ( 'NONE',  ( 124.3117748109119844, -10.30919188438810075, -12.61870101168855918 ) ) ;
#31795=CARTESIAN_POINT ( 'NONE',  ( 116.9373081442452929, -8.166667518702817929, -8.995218007635861213 ) ) ;
#31798=CARTESIAN_POINT ( 'NONE',  ( 116.4834948109119779, -7.894159318335828068, -9.358103419637847864 ) ) ;
#31800=CARTESIAN_POINT ( 'NONE',  ( 118.8092881442453290, -9.988377603198976828, -10.36322818467138340 ) ) ;
#31801=CARTESIAN_POINT ( 'NONE',  ( 117.5045748109119756, -9.859900752359374465, -12.68260735090039404 ) ) ;
#31803=EDGE_CURVE ( 'NONE', #28126, #39007, #41761, .T. ) ;
#31804=CARTESIAN_POINT ( 'NONE',  ( 121.2485348109119769, -8.899110576539710493, -16.42337572283490132 ) ) ;
#31805=CARTESIAN_POINT ( 'NONE',  ( 118.3554748109119998, 0.2603800115204892296, -16.42320221600525088 ) ) ;
#31806=CARTESIAN_POINT ( 'NONE',  ( 136.7878215370441524, 0.3576572923493759881, -15.41906115585400272 ) ) ;
#31812=CARTESIAN_POINT ( 'NONE',  ( 115.4624148109119943, -5.638512984488999180, -18.83840828888717311 ) ) ;
#31814=CARTESIAN_POINT ( 'NONE',  ( 113.9875214775786532, -8.899110576539710493, -16.42337572283490132 ) ) ;
#31821=CARTESIAN_POINT ( 'NONE',  ( 111.4705635773848940, -2.467220198592768199, -17.83387418641523325 ) ) ;
#31822=CARTESIAN_POINT ( 'NONE',  ( 116.0086969107182142, -2.467220198592777525, -17.83387418641524391 ) ) ;
#31823=CARTESIAN_POINT ( 'NONE',  ( 117.4478481442453131, 0.2603800115204892296, -16.42320221600525088 ) ) ;
#31825=CARTESIAN_POINT ( 'NONE',  ( 125.7866681442452688, -8.899110576539710493, -16.42337572283490132 ) ) ;
#31826=CARTESIAN_POINT ( 'NONE',  ( 120.5110881442453206, -3.505236298600246325, -18.68346056562440793 ) ) ;
#31827=CARTESIAN_POINT ( 'NONE',  ( 112.6828081442453282, -2.084020599724406786, -8.691656652584148546 ) ) ;
#31830=CARTESIAN_POINT ( 'NONE',  ( 122.3263414775786373, -6.344957434206665248, -7.627207830600338134 ) ) ;
#31832=CARTESIAN_POINT ( 'NONE',  ( 117.7314814775786260, -5.574606645277164318, -18.38911715685844683 ) ) ;
#31834=CARTESIAN_POINT ( 'NONE',  ( 111.6050014775786536, 0.1319031606808879209, -14.10382304977623669 ) ) ;
#31837=CARTESIAN_POINT ( 'NONE',  ( 120.2274548109119934, -9.859900752359374465, -12.68260735090039404 ) ) ;
#31838=CARTESIAN_POINT ( 'NONE',  ( 123.2906948109119867, -1.833838273342659697, -17.42832698103878286 ) ) ;
#31839=CARTESIAN_POINT ( 'NONE',  ( 114.3846081442453197, 0.4262465694468551280, -12.03445270309932269 ) ) ;
#31844=CARTESIAN_POINT ( 'NONE',  ( 119.2063748109119814, -1.561330072975668504, -17.79121239304076951 ) ) ;
#31845=CARTESIAN_POINT ( 'NONE',  ( 115.8595014775786609, -1.834011780172310813, -8.268836392978581529 ) ) ;
#31847=CARTESIAN_POINT ( 'NONE',  ( 114.7249681442453237, 0.2603800115204892296, -16.42320221600525088 ) ) ;
#31849=FACE_OUTER_BOUND ( 'NONE', #16162, .T. ) ;
#31850=CARTESIAN_POINT ( 'NONE',  ( 124.0281414775786146, -1.834011780172310813, -8.268836392978581529 ) ) ;
#31851=CARTESIAN_POINT ( 'NONE',  ( 116.7104014775786425, -0.4660016031367893996, -10.09054647747474043 ) ) ;
#31852=EDGE_CURVE ( 'NONE', #2648, #29655, #32015, .T. ) ;
#31853=CARTESIAN_POINT ( 'NONE',  ( 122.3830681442452857, -1.833838273342659697, -17.42832698103878286 ) ) ;
#31854=CARTESIAN_POINT ( 'NONE',  ( 124.5954081442453116, -3.383040157471821630, -19.15922257007629170 ) ) ;
#31855=CARTESIAN_POINT ( 'NONE',  ( 120.5110881442453206, -6.344957434206665248, -7.627207830600338134 ) ) ;
#31858=CARTESIAN_POINT ( 'NONE',  ( 115.6325948109119821, -9.565557343593413364, -10.61323700422348004 ) ) ;
#31862=CARTESIAN_POINT ( 'NONE',  ( 120.3976348109119812, -1.834011780172310813, -8.268836392978581529 ) ) ;
#31864=CARTESIAN_POINT ( 'NONE',  ( 120.9081748109119872, -5.638512984488999180, -18.83840828888717311 ) ) ;
#31867=CARTESIAN_POINT ( 'NONE',  ( 124.0281414775786146, -1.834011780172310813, -8.268836392978581529 ) ) ;
#31870=CARTESIAN_POINT ( 'NONE',  ( 122.0994348109119585, 0.9020085738987414503, -11.91225656197092242 ) ) ;
#31871=CARTESIAN_POINT ( 'NONE',  ( 116.5969481442453031, -9.859900752359374465, -12.68260735090039404 ) ) ;
#31872=CARTESIAN_POINT ( 'NONE',  ( 135.3184548109119874, -5.622599431619523358, -7.441364641445410655 ) ) ;
#31873=CARTESIAN_POINT ( 'NONE',  ( 119.3198281442452924, -9.859900752359374465, -12.68260735090039404 ) ) ;
#31875=CARTESIAN_POINT ( 'NONE',  ( 119.7169148109119874, -0.1624402480850797581, -16.17319339645315424 ) ) ;
#31877=CARTESIAN_POINT ( 'NONE',  ( 118.9227414775786542, 0.4262465694468514643, -12.03445270309931736 ) ) ;
#31878=CARTESIAN_POINT ( 'NONE',  ( 112.8529881442453302, -1.561330072975668060, -17.79121239304076596 ) ) ;
#31879=CARTESIAN_POINT ( 'NONE',  ( 118.3554748109119998, 0.2603800115204892296, -16.42320221600525088 ) ) ;
#31880=CARTESIAN_POINT ( 'NONE',  ( 112.2857214775786474, -4.089484607189486809, -7.948022111789456723 ) ) ;
#31882=CARTESIAN_POINT ( 'NONE',  ( 118.9227414775786542, 0.4262465694468514643, -12.03445270309931736 ) ) ;
#31884=CARTESIAN_POINT ( 'NONE',  ( 117.0507614775786465, -10.30919188438810075, -12.61870101168855918 ) ) ;
#31886=CARTESIAN_POINT ( 'NONE',  ( 115.4624148109119943, -4.153390946401313677, -8.397313243818183892 ) ) ;
#31887=DIRECTION ( 'NONE',  ( 0.000000000000000000, 0.6004852223388239540, -0.7996358532186341739 ) ) ;
#31889=CARTESIAN_POINT ( 'NONE',  ( 121.4187148109119789, -6.344957434206665248, -7.627207830600338134 ) ) ;
#31892=CARTESIAN_POINT ( 'NONE',  ( 120.2274548109119934, -9.859900752359374465, -12.68260735090039404 ) ) ;
#31898=CARTESIAN_POINT ( 'NONE',  ( 114.1009748109119784, -4.089484607189486809, -7.948022111789456723 ) ) ;
#31899=CARTESIAN_POINT ( 'NONE',  ( 124.7088614775786226, -9.565557343593413364, -10.61323700422348004 ) ) ;
#31901=CARTESIAN_POINT ( 'NONE',  ( 122.0994348109119443, -10.15424416112533912, -14.75197769757731336 ) ) ;
#31904=CARTESIAN_POINT ( 'NONE',  ( 124.1983214775786166, -8.166667518702819706, -8.995218007635861213 ) ) ;
#31905=CARTESIAN_POINT ( 'NONE',  ( 111.8886348109120092, -6.222761293078241884, -8.102969835052219238 ) ) ;
#31907=CARTESIAN_POINT ( 'NONE',  ( 125.1269327111056953, -1.267766418764818770, -16.93314635290698078 ) ) ;
#31908=CARTESIAN_POINT ( 'NONE',  ( 112.3424481442453384, -6.344957434206662583, -7.627207830600332805 ) ) ;
#31911=CARTESIAN_POINT ( 'NONE',  ( 121.6456214775786293, -10.63000616557722466, -14.87417383870573495 ) ) ;
#31914=CARTESIAN_POINT ( 'NONE',  ( 111.9453614775786434, -1.561330072975668060, -17.79121239304076596 ) ) ;
#31915=CARTESIAN_POINT ( 'NONE',  ( 123.5176014775786228, -9.261995988541697145, -16.69588392320189030 ) ) ;
#31917=CARTESIAN_POINT ( 'NONE',  ( 122.8368814775786291, -7.894159318335828068, -9.358103419637847864 ) ) ;
#31919=CARTESIAN_POINT ( 'NONE',  ( 113.1366214775786432, -1.834011780172310813, -8.268836392978581529 ) ) ;
#31920=B_SPLINE_CURVE_WITH_KNOTS ( 'NONE', 3,
 ( #37028, #26106, #30208, #9237, #29979, #43444, #44129, #33374, #4897, #12437 ),
 .UNSPECIFIED., .F., .F.,
 ( 4, 3, 3, 4 ),
 ( 0.000000000000000000, 0.0001671877560958114864, 0.0003343755126086554838, 0.0006438490228507209303 ),
 .UNSPECIFIED. ) ;
#31921=FACE_OUTER_BOUND ( 'NONE', #26500, .T. ) ;
#31923=CARTESIAN_POINT ( 'NONE',  ( 111.4441597945729541, -2.483185513731533511, -17.81261398230368798 ) ) ;
#31924=CARTESIAN_POINT ( 'NONE',  ( 111.7751814775786556, -2.084020599724406786, -8.691656652584148546 ) ) ;
#31926=DIRECTION ( 'NONE',  ( -1.000000000000000000, 0.000000000000000000, 0.000000000000000000 ) ) ;
#31927=CARTESIAN_POINT ( 'NONE',  ( 123.5743281442453139, -7.893985811506177619, -18.51759400769804742 ) ) ;
#31928=CARTESIAN_POINT ( 'NONE',  ( 122.5532481442453019, -10.63000616557722466, -14.87417383870573495 ) ) ;
#31929=CARTESIAN_POINT ( 'NONE',  ( 124.3117748109119844, 0.1319031606808879209, -14.10382304977623669 ) ) ;
#31930=CARTESIAN_POINT ( 'NONE',  ( 119.7736414775786358, 0.1319031606808879209, -14.10382304977623669 ) ) ;
#31932=CARTESIAN_POINT ( 'NONE',  ( 120.1140014775786398, -1.561330072975668504, -17.79121239304076951 ) ) ;
#31939=CARTESIAN_POINT ( 'NONE',  ( 124.5954081442453116, -3.383040157471821630, -19.15922257007629170 ) ) ;
#31940=CARTESIAN_POINT ( 'NONE',  ( 113.0231681442453322, 0.9020085738987339008, -11.91225656197089222 ) ) ;
#31942=CARTESIAN_POINT ( 'NONE',  ( 114.1009748109119784, -5.574606645277164318, -18.38911715685844683 ) ) ;
#31944=CARTESIAN_POINT ( 'NONE',  ( 119.0361948109119794, -2.084020599724404121, -8.691656652584155651 ) ) ;
#31946=CARTESIAN_POINT ( 'NONE',  ( 125.1626748109119802, -9.988377603198980381, -10.36322818467138518 ) ) ;
#31948=CARTESIAN_POINT ( 'NONE',  ( 117.9583881442453048, -10.30919188438810075, -12.61870101168855918 ) ) ;
#31952=CARTESIAN_POINT ( 'NONE',  ( 127.7429221096195420, -7.069607264515464173, -8.068942598320006709 ) ) ;
#31953=CARTESIAN_POINT ( 'NONE',  ( 114.9518748109119883, -7.643976991954077427, -18.09477374809248928 ) ) ;
#31954=CARTESIAN_POINT ( 'NONE',  ( 111.9453614775786434, -1.561330072975668060, -17.79121239304076596 ) ) ;
#31955=CARTESIAN_POINT ( 'NONE',  ( 111.7751814775786556, -7.893985811506177619, -18.51759400769804742 ) ) ;
#31956=CARTESIAN_POINT ( 'NONE',  ( 118.5256548109119876, -8.899110576539721151, -16.42337572283488711 ) ) ;
#31957=CARTESIAN_POINT ( 'NONE',  ( 118.6958348109119754, -3.505236298600246325, -18.68346056562440793 ) ) ;
#31958=CARTESIAN_POINT ( 'NONE',  ( 117.1642148109119859, -0.8288870151387760510, -10.36305467784173118 ) ) ;
#31962=AXIS2_PLACEMENT_3D ( 'NONE', #42574, #4256, #7230 ) ;
#31964=CARTESIAN_POINT ( 'NONE',  ( 115.6325948109119821, -9.565557343593413364, -10.61323700422348004 ) ) ;
#31965=EDGE_LOOP ( 'NONE', ( #7426, #40693, #7326, #2143 ) ) ;
#31972=CARTESIAN_POINT ( 'NONE',  ( 112.1722681442453222, -8.899110576539710493, -16.42337572283490132 ) ) ;
#31974=CARTESIAN_POINT ( 'NONE',  ( 118.1285681442453068, -2.084020599724406786, -8.691656652584148546 ) ) ;
#31975=CARTESIAN_POINT ( 'NONE',  ( 117.2776681442452968, -4.153390946401325223, -8.397313243818185668 ) ) ;
#31984=CARTESIAN_POINT ( 'NONE',  ( 112.9664414775786412, 0.5811942927096154232, -14.16772938898807155 ) ) ;
#31985=CARTESIAN_POINT ( 'NONE',  ( 116.9373081442452929, -1.833838273342659253, -17.42832698103878286 ) ) ;
#31990=CARTESIAN_POINT ( 'NONE',  ( 115.0653281442453277, -3.505236298600246325, -18.68346056562440793 ) ) ;
#31992=CARTESIAN_POINT ( 'NONE',  ( 125.1733191598100916, -1.295815253274133161, -16.89579513612386563 ) ) ;
#31994=CARTESIAN_POINT ( 'NONE',  ( 113.6471614775786492, -5.638512984488999180, -18.83840828888717311 ) ) ;
#31996=CARTESIAN_POINT ( 'NONE',  ( 118.6958348109119754, -6.344957434206665248, -7.627207830600338134 ) ) ;
#31999=CARTESIAN_POINT ( 'NONE',  ( 116.9940348109119839, -9.988377603198976828, -10.36322818467138340 ) ) ;
#32000=CARTESIAN_POINT ( 'NONE',  ( 112.3424481442453384, -6.344957434206662583, -7.627207830600332805 ) ) ;
#32001=CARTESIAN_POINT ( 'NONE',  ( 127.2313854076800794, -10.35564729092436309, -13.79736478706461433 ) ) ;
#32004=VERTEX_POINT ( 'NONE', #14561 ) ;
#32007=CARTESIAN_POINT ( 'NONE',  ( 116.0864081442453113, -0.1624402480850797581, -16.17319339645315424 ) ) ;
#32012=CARTESIAN_POINT ( 'NONE',  ( 127.1653849502323226, -5.235753722768803797, -7.932320622462421866 ) ) ;
#32013=CARTESIAN_POINT ( 'NONE',  ( 112.6260814775786514, -0.8288870151387760510, -10.36305467784173118 ) ) ;
#32014=DIRECTION ( 'NONE',  ( 0.000000000000000000, 0.6004852223388318366, -0.7996358532186281787 ) ) ;
#32015=( BOUNDED_CURVE ( )  B_SPLINE_CURVE ( 2, ( #12841, #27193, #9184, #14114, #37199, #9871, #3618, #31431, #41938, #198, #19661, #10701, #26740, #9404, #5972, #19896, #33783 ),
 .UNSPECIFIED., .F., .T. ) 
 B_SPLINE_CURVE_WITH_KNOTS ( ( 3, 2, 2, 2, 2, 2, 2, 2, 3 ),
 ( 0.7670046674808920217, 0.7734375000000000000, 0.7812500000000000000, 0.7890625000000000000, 0.7968750000000000000, 0.8046875000000000000, 0.8125000000000000000, 0.8203125000000000000, 0.8267453325190590174 ),
 .UNSPECIFIED. ) 
 CURVE ( )  GEOMETRIC_REPRESENTATION_ITEM ( )  RATIONAL_B_SPLINE_CURVE ( ( 0.9778625265006449796, 0.9373222120152220338, 1.000000000000000000, 0.9238795325112869605, 1.000000000000000000, 0.9238795325112869605, 1.000000000000000000, 0.9238795325112869605, 1.000000000000000000, 0.9238795325112869605, 1.000000000000000000, 0.9238795325112869605, 1.000000000000000000, 0.9238795325112869605, 1.000000000000000000, 0.9373222120157009840, 0.9778625265000250311 ) ) 
 REPRESENTATION_ITEM ( '' )  );
#32016=CARTESIAN_POINT ( 'NONE',  ( 124.1415948109119540, -6.344957434206665248, -7.627207830600338134 ) ) ;
#32017=CARTESIAN_POINT ( 'NONE',  ( 116.4834948109119779, -1.561330072975668504, -17.79121239304076951 ) ) ;
#32019=CARTESIAN_POINT ( 'NONE',  ( 116.1431348109119881, 0.1319031606808879209, -14.10382304977623669 ) ) ;
#32021=CARTESIAN_POINT ( 'NONE',  ( 116.8238548109119819, -4.089484607189486809, -7.948022111789456723 ) ) ;
#32022=CARTESIAN_POINT ( 'NONE',  ( 118.2987481442453088, -7.894159318335828068, -9.358103419637847864 ) ) ;
#32024=CARTESIAN_POINT ( 'NONE',  ( 121.0216281442452981, -7.894159318335828068, -9.358103419637847864 ) ) ;
#32025=CARTESIAN_POINT ( 'NONE',  ( 121.1918081442452859, 0.9020085738987339008, -11.91225656197089222 ) ) ;
#32033=CARTESIAN_POINT ( 'NONE',  ( 113.1933481442453058, -4.089484607189486809, -7.948022111789456723 ) ) ;
#32036=CARTESIAN_POINT ( 'NONE',  ( 116.3700414775786527, -4.153390946401321671, -8.397313243818183892 ) ) ;
#32039=DIRECTION ( 'NONE',  ( 0.000000000000000000, 0.6004852223388321697, -0.7996358532186279566 ) ) ;
#32041=CARTESIAN_POINT ( 'NONE',  ( 113.1933481442453058, -5.574606645277164318, -18.38911715685844683 ) ) ;
#32045=CARTESIAN_POINT ( 'NONE',  ( 118.7525614775786380, -8.166667518702819706, -8.995218007635861213 ) ) ;
#32046=CARTESIAN_POINT ( 'NONE',  ( 118.4122014775786340, -9.859900752359374465, -12.68260735090039404 ) ) ;
#32047=CARTESIAN_POINT ( 'NONE',  ( 125.8433948109119456, -1.834011780172310813, -8.268836392978581529 ) ) ;
#32051=CARTESIAN_POINT ( 'NONE',  ( 122.8936081442453059, 0.2603800115204892296, -16.42320221600525088 ) ) ;
#32053=CARTESIAN_POINT ( 'NONE',  ( 119.2063748109119814, -7.894159318335828068, -9.358103419637847864 ) ) ;
#32054=CARTESIAN_POINT ( 'NONE',  ( 117.9016614775786280, -0.1624402480850797581, -16.17319339645315424 ) ) ;
#32057=CARTESIAN_POINT ( 'NONE',  ( 121.7590748109119687, -2.084020599724406786, -8.691656652584148546 ) ) ;
#32058=CARTESIAN_POINT ( 'NONE',  ( 122.8368814775786291, -7.894159318335828068, -9.358103419637847864 ) ) ;
#32065=CARTESIAN_POINT ( 'NONE',  ( 118.5256548109119876, -0.4660016031367893996, -10.09054647747474043 ) ) ;
#32066=CARTESIAN_POINT ( 'NONE',  ( 118.1285681442453068, -7.893985811506177619, -18.51759400769804742 ) ) ;
#32071=CARTESIAN_POINT ( 'NONE',  ( 117.2776681442452968, -5.638512984488999180, -18.83840828888717311 ) ) ;
#32072=CARTESIAN_POINT ( 'NONE',  ( 121.9292548109119849, -7.894159318335828068, -9.358103419637847864 ) ) ;
#32075=CARTESIAN_POINT ( 'NONE',  ( 111.3780948109119890, -5.574606645277164318, -18.38911715685844683 ) ) ;
#32076=CARTESIAN_POINT ( 'NONE',  ( 121.9292548109119849, -1.561330072975668948, -17.79121239304076951 ) ) ;
#32078=CARTESIAN_POINT ( 'NONE',  ( 114.8951481442453115, -8.899110576539710493, -16.42337572283490132 ) ) ;
#32084=CARTESIAN_POINT ( 'NONE',  ( 119.6601881442453106, -8.166667518702819706, -8.995218007635861213 ) ) ;
#32088=CARTESIAN_POINT ( 'NONE',  ( 116.9940348109119839, -0.1624402480850797581, -16.17319339645315424 ) ) ;
#32089=( BOUNDED_SURFACE ( )  B_SPLINE_SURFACE ( 1, 2, ( 
 ( #40705, #27024, #30664, #34073, #40939, #20636, #16311, #34513, #16998, #41167, #29984, #30438, #12669, #40481, #2383, #44133, #23376 ),
 ( #9464, #13348, #37258, #6030, #19952, #2609, #9926, #44357, #13118, #16769, #27252, #37726, #20412, #34296, #30887, #17213, #3729 ) ),
 .UNSPECIFIED., .F., .F., .F. ) 
 B_SPLINE_SURFACE_WITH_KNOTS ( ( 2, 2 ),
 ( 3, 2, 2, 2, 2, 2, 2, 2, 3 ),
 ( 0.000000000000000000, 1.000000000000000000 ),
 ( 0.000000000000000000, 0.1250000000000000000, 0.2500000000000000000, 0.3750000000000000000, 0.5000000000000000000, 0.6250000000000000000, 0.7500000000000000000, 0.8750000000000000000, 1.000000000000000000 ),
 .UNSPECIFIED. ) 
 GEOMETRIC_REPRESENTATION_ITEM ( )  RATIONAL_B_SPLINE_SURFACE ( (
 ( 1.000000000000000000, 0.9238795325112869605, 1.000000000000000000, 0.9238795325112869605, 1.000000000000000000, 0.9238795325112869605, 1.000000000000000000, 0.9238795325112869605, 1.000000000000000000, 0.9238795325112869605, 1.000000000000000000, 0.9238795325112869605, 1.000000000000000000, 0.9238795325112869605, 1.000000000000000000, 0.9238795325112869605, 1.000000000000000000),
 ( 1.000000000000000000, 0.9238795325112869605, 1.000000000000000000, 0.9238795325112869605, 1.000000000000000000, 0.9238795325112869605, 1.000000000000000000, 0.9238795325112869605, 1.000000000000000000, 0.9238795325112869605, 1.000000000000000000, 0.9238795325112869605, 1.000000000000000000, 0.9238795325112869605, 1.000000000000000000, 0.9238795325112869605, 1.000000000000000000) ) ) 
 REPRESENTATION_ITEM ( '' )  SURFACE ( )  );
#32092=CARTESIAN_POINT ( 'NONE',  ( 118.9227414775786542, 0.4262465694468514643, -12.03445270309931736 ) ) ;
#32093=B_SPLINE_CURVE_WITH_KNOTS ( 'NONE', 3,
 ( #12198, #40001, #33140, #15841, #6252, #17415, #23594, #16752, #45016, #27685 ),
 .UNSPECIFIED., .F., .F.,
 ( 4, 3, 3, 4 ),
 ( 0.000000000000000000, 0.0001671877560958089928, 0.0003343755126086549959, 0.0006438490228507220145 ),
 .UNSPECIFIED. ) ;
#32094=CARTESIAN_POINT ( 'NONE',  ( 121.9100498793805230, -2.191907684172563986, -18.20049396185734025 ) ) ;
#32095=CARTESIAN_POINT ( 'NONE',  ( 121.5888948109119809, 0.1319031606808879209, -14.10382304977623669 ) ) ;
#32099=CARTESIAN_POINT ( 'NONE',  ( 118.4689281442453250, -10.15424416112533912, -14.75197769757731336 ) ) ;
#32101=CARTESIAN_POINT ( 'NONE',  ( 113.8173414775786512, 0.2603800115204892296, -16.42320221600525088 ) ) ;
#32102=CARTESIAN_POINT ( 'NONE',  ( 120.5110881442453206, -6.344957434206665248, -7.627207830600338134 ) ) ;
#32103=CARTESIAN_POINT ( 'NONE',  ( 125.6164881442453094, -9.565557343593413364, -10.61323700422348004 ) ) ;
#32105=CARTESIAN_POINT ( 'NONE',  ( 119.0929214775786278, -4.153390946401325223, -8.397313243818185668 ) ) ;
#32107=CARTESIAN_POINT ( 'NONE',  ( 120.9081748109119872, -5.638512984488999180, -18.83840828888717311 ) ) ;
#32112=CARTESIAN_POINT ( 'NONE',  ( 124.5386814775786206, -5.638512984488999180, -18.83840828888717311 ) ) ;
#32113=VERTEX_POINT ( 'NONE', #21627 ) ;
#32115=CARTESIAN_POINT ( 'NONE',  ( 123.1772414775786189, -5.574606645277164318, -18.38911715685844683 ) ) ;
#32121=CARTESIAN_POINT ( 'NONE',  ( 113.3635281442453504, -9.988377603198976828, -10.36322818467138340 ) ) ;
#32122=CARTESIAN_POINT ( 'NONE',  ( 115.2922348109119781, -10.63000616557722466, -14.87417383870573495 ) ) ;
#32125=CARTESIAN_POINT ( 'NONE',  ( 120.0572748109119772, -6.222761293078241884, -8.102969835052219238 ) ) ;
#32126=CARTESIAN_POINT ( 'NONE',  ( 112.4559014775786778, -0.1624402480850797581, -16.17319339645315424 ) ) ;
#32128=CARTESIAN_POINT ( 'NONE',  ( 123.8579614775786126, 0.5811942927096110934, -14.16772938898807510 ) ) ;
#32132=CARTESIAN_POINT ( 'NONE',  ( 112.1722681442453222, -0.4660016031367893996, -10.09054647747474043 ) ) ;
#32136=CARTESIAN_POINT ( 'NONE',  ( 119.4900081442453086, -1.834011780172310813, -8.268836392978581529 ) ) ;
#32141=CARTESIAN_POINT ( 'NONE',  ( 125.1626748109119802, -9.988377603198980381, -10.36322818467138518 ) ) ;
#32142=CARTESIAN_POINT ( 'NONE',  ( 128.2184548109119930, -4.105398160058917334, -19.34506575923121474 ) ) ;
#32143=CARTESIAN_POINT ( 'NONE',  ( 122.6667014775786413, -2.084020599724406786, -8.691656652584148546 ) ) ;
#32145=CARTESIAN_POINT ( 'NONE',  ( 118.9227414775786400, -10.63000616557722466, -14.87417383870573495 ) ) ;
#32149=CARTESIAN_POINT ( 'NONE',  ( 124.0848681442452772, -4.089484607189486809, -7.948022111789456723 ) ) ;
#32154=CARTESIAN_POINT ( 'NONE',  ( 123.1205148109119563, -1.834011780172310813, -8.268836392978581529 ) ) ;
#32155=CARTESIAN_POINT ( 'NONE',  ( 121.4187148109119789, -6.344957434206665248, -7.627207830600338134 ) ) ;
#32156=CARTESIAN_POINT ( 'NONE',  ( 122.3263414775786373, -3.505236298600246325, -18.68346056562440793 ) ) ;
#32158=CARTESIAN_POINT ( 'NONE',  ( 124.4819548109119722, -2.084020599724406786, -8.691656652584148546 ) ) ;
#32159=CARTESIAN_POINT ( 'NONE',  ( 113.3635281442453504, -0.1624402480850797581, -16.17319339645315424 ) ) ;
#32160=CARTESIAN_POINT ( 'NONE',  ( 119.7169148109119874, -9.988377603198976828, -10.36322818467138340 ) ) ;
#32168=CARTESIAN_POINT ( 'NONE',  ( 114.2144281442453178, -8.166667518702817929, -8.995218007635859436 ) ) ;
#32170=CARTESIAN_POINT ( 'NONE',  ( 112.3424481442453384, -3.505236298600246325, -18.68346056562440793 ) ) ;
#32176=CARTESIAN_POINT ( 'NONE',  ( 115.0653281442453277, -6.344957434206662583, -7.627207830600332805 ) ) ;
#32181=CARTESIAN_POINT ( 'NONE',  ( 118.5256548109119876, -8.899110576539710493, -16.42337572283490132 ) ) ;
#32182=CARTESIAN_POINT ( 'NONE',  ( 115.5758681442453053, -1.561330072975668060, -17.79121239304076951 ) ) ;
#32184=CARTESIAN_POINT ( 'NONE',  ( 118.0151148109119816, 0.4262465694468589028, -12.03445270309934578 ) ) ;
#32185=CARTESIAN_POINT ( 'NONE',  ( 118.1285681442453068, -2.084020599724406786, -8.691656652584148546 ) ) ;
#32186=CARTESIAN_POINT ( 'NONE',  ( 117.3911214775786505, -7.894159318335828068, -9.358103419637847864 ) ) ;
#32190=CARTESIAN_POINT ( 'NONE',  ( 119.2063748109119814, -7.894159318335828068, -9.358103419637847864 ) ) ;
#32193=CARTESIAN_POINT ( 'NONE',  ( 113.8740681442453138, 0.5811942927096154232, -14.16772938898807155 ) ) ;
#32195=CARTESIAN_POINT ( 'NONE',  ( 114.1009748109119784, -5.574606645277164318, -18.38911715685844683 ) ) ;
#32199=CARTESIAN_POINT ( 'NONE',  ( 117.5045748109119756, -9.859900752359374465, -12.68260735090039404 ) ) ;
#32200=CARTESIAN_POINT ( 'NONE',  ( 117.1074881442453233, 0.4262465694468514643, -12.03445270309931736 ) ) ;
#32209=CARTESIAN_POINT ( 'NONE',  ( 125.9568481442452850, -3.505236298600246325, -18.68346056562440793 ) ) ;
#32210=CARTESIAN_POINT ( 'NONE',  ( 118.4122014775786340, -9.859900752359374465, -12.68260735090039404 ) ) ;
#32213=CARTESIAN_POINT ( 'NONE',  ( 118.6391081442452986, -5.574606645277164318, -18.38911715685844683 ) ) ;
#32219=CARTESIAN_POINT ( 'NONE',  ( 114.1009748109119784, -4.089484607189486809, -7.948022111789456723 ) ) ;
#32220=VERTEX_POINT ( 'NONE', #35971 ) ;
#32221=CARTESIAN_POINT ( 'NONE',  ( 117.6747548109119919, -1.834011780172310813, -8.268836392978581529 ) ) ;
#32224=CARTESIAN_POINT ( 'NONE',  ( 115.2355081442453155, -10.30919188438810075, -12.61870101168855918 ) ) ;
#32225=CARTESIAN_POINT ( 'NONE',  ( 117.1074881442453233, -10.63000616557722466, -14.87417383870573495 ) ) ;
#32227=CARTESIAN_POINT ( 'NONE',  ( 127.0298367773221315, -10.26141744229719954, -13.69217050928270929 ) ) ;
#32234=CARTESIAN_POINT ( 'NONE',  ( 121.1350814775786233, -9.859900752359378018, -12.68260735090039759 ) ) ;
#32236=CARTESIAN_POINT ( 'NONE',  ( 122.5488326359456011, -1.179503403430467667, -17.05068175419387089 ) ) ;
#32238=CARTESIAN_POINT ( 'NONE',  ( 126.2184548109105435, -4.159894987975746972, -8.443039665293909479 ) ) ;
#32239=CARTESIAN_POINT ( 'NONE',  ( 112.9664414775786412, -9.859900752359374465, -12.68260735090039404 ) ) ;
#32241=CARTESIAN_POINT ( 'NONE',  ( 125.3328548109119964, -9.261995988541697145, -16.69588392320189030 ) ) ;
#32242=CARTESIAN_POINT ( 'NONE',  ( 120.3409081442453044, -0.4660016031367893996, -10.09054647747474043 ) ) ;
#32244=CARTESIAN_POINT ( 'NONE',  ( 119.4332814775786318, -8.899110576539710493, -16.42337572283490132 ) ) ;
#32245=FACE_OUTER_BOUND ( 'NONE', #40521, .T. ) ;
#32246=CARTESIAN_POINT ( 'NONE',  ( 119.5467348109119712, -4.089484607189486809, -7.948022111789456723 ) ) ;
#32247=CARTESIAN_POINT ( 'NONE',  ( 119.3198281442452924, -9.859900752359374465, -12.68260735090039404 ) ) ;
#32250=CARTESIAN_POINT ( 'NONE',  ( 124.1983214775786166, -1.833838273342659697, -17.42832698103878286 ) ) ;
#32253=CARTESIAN_POINT ( 'NONE',  ( 121.9292548109119849, -1.561330072975668948, -17.79121239304076951 ) ) ;
#32260=CARTESIAN_POINT ( 'NONE',  ( 118.3554748109119998, 0.2603800115204892296, -16.42320221600525088 ) ) ;
#32261=CARTESIAN_POINT ( 'NONE',  ( 137.3374356171263457, -9.844308156483171146, -11.96184393924012213 ) ) ;
#32262=CARTESIAN_POINT ( 'NONE',  ( 117.2209414775786485, -2.084020599724406786, -8.691656652584148546 ) ) ;
#32263=CARTESIAN_POINT ( 'NONE',  ( 126.2202699136542066, -0.8305752925518951058, -10.43662590553933889 ) ) ;
#32264=CARTESIAN_POINT ( 'NONE',  ( 117.3343948109119737, -6.222761293078222344, -8.102969835052219238 ) ) ;
#32266=CARTESIAN_POINT ( 'NONE',  ( 112.6260814775786514, -0.8288870151387760510, -10.36305467784173118 ) ) ;
#32269=CARTESIAN_POINT ( 'NONE',  ( 111.5883843147880725, -2.395992375830774179, -17.92872468182854462 ) ) ;
#32271=CARTESIAN_POINT ( 'NONE',  ( 117.5613014775786525, 0.9020085738987339008, -11.91225656197089222 ) ) ;
#32272=CARTESIAN_POINT ( 'NONE',  ( 118.5823814775786360, -7.643976991954077427, -18.09477374809248928 ) ) ;
#32273=CARTESIAN_POINT ( 'NONE',  ( 112.5693548109119888, 0.4262465694468514643, -12.03445270309931736 ) ) ;
#32275=CARTESIAN_POINT ( 'NONE',  ( 137.3802547664383269, -7.424459469978982540, -8.936682238071227857 ) ) ;
#32276=CARTESIAN_POINT ( 'NONE',  ( 123.4041481442452834, -10.30919188438810075, -12.61870101168855918 ) ) ;
#32278=CARTESIAN_POINT ( 'NONE',  ( 118.1285681442453068, -2.084020599724406786, -8.691656652584148546 ) ) ;
#32282=CARTESIAN_POINT ( 'NONE',  ( 115.8595014775786609, -7.643976991954077427, -18.09477374809248928 ) ) ;
#32286=CARTESIAN_POINT ( 'NONE',  ( 122.6667014775786413, -2.084020599724406786, -8.691656652584148546 ) ) ;
#32288=CARTESIAN_POINT ( 'NONE',  ( 124.5954081442453116, -6.222761293078241884, -8.102969835052219238 ) ) ;
#32295=CARTESIAN_POINT ( 'NONE',  ( 116.0864081442453113, -9.988377603198976828, -10.36322818467138340 ) ) ;
#32296=CARTESIAN_POINT ( 'NONE',  ( 120.0005481442453146, -5.638512984488999180, -18.83840828888717311 ) ) ;
#32298=CARTESIAN_POINT ( 'NONE',  ( 112.5126281442453120, -10.30919188438810075, -12.61870101168855918 ) ) ;
#32302=CARTESIAN_POINT ( 'NONE',  ( 115.7460481442453357, 0.9020085738987339008, -11.91225656197089222 ) ) ;
#32303=CARTESIAN_POINT ( 'NONE',  ( 123.4608748109119745, 0.4262465694468514643, -12.03445270309931736 ) ) ;
#32304=EDGE_CURVE ( 'NONE', #11237, #31245, #20569, .T. ) ;
#32305=CARTESIAN_POINT ( 'NONE',  ( 111.4348214775786801, -3.505236298600246325, -18.68346056562440793 ) ) ;
#32306=CARTESIAN_POINT ( 'NONE',  ( 120.4543614775786295, -4.089484607189486809, -7.948022111789456723 ) ) ;
#32310=CARTESIAN_POINT ( 'NONE',  ( 117.6747548109119919, -7.643976991954077427, -18.09477374809248928 ) ) ;
#32316=CARTESIAN_POINT ( 'NONE',  ( 119.8870948109119752, -9.261995988541697145, -16.69588392320189030 ) ) ;
#32320=CARTESIAN_POINT ( 'NONE',  ( 122.0427081442452817, 0.5811942927096049871, -14.16772938898809286 ) ) ;
#32321=CARTESIAN_POINT ( 'NONE',  ( 115.5191414775786569, -6.222761293078241884, -8.102969835052219238 ) ) ;
#32324=CARTESIAN_POINT ( 'NONE',  ( 119.2063748109119814, -7.894159318335828068, -9.358103419637847864 ) ) ;
#32326=CARTESIAN_POINT ( 'NONE',  ( 122.4965214775786251, 0.1319031606808879209, -14.10382304977623669 ) ) ;
#32328=CARTESIAN_POINT ( 'NONE',  ( 122.2696148109119889, -5.574606645277164318, -18.38911715685844683 ) ) ;
#32329=CARTESIAN_POINT ( 'NONE',  ( 112.5126281442453120, -10.30919188438810075, -12.61870101168855918 ) ) ;
#32330=CARTESIAN_POINT ( 'NONE',  ( 120.7947214775786193, -9.261995988541697145, -16.69588392320189030 ) ) ;
#32331=CARTESIAN_POINT ( 'NONE',  ( 113.5337081442453240, -9.261995988541697145, -16.69588392320189030 ) ) ;
#32333=CARTESIAN_POINT ( 'NONE',  ( 120.9081748109119872, -4.153390946401325223, -8.397313243818185668 ) ) ;
#32334=ORIENTED_EDGE ( 'NONE', *, *, #26825, .F. ) ;
#32335=CARTESIAN_POINT ( 'NONE',  ( 122.0994348109119443, 0.9020085738987339008, -11.91225656197089222 ) ) ;
#32340=CARTESIAN_POINT ( 'NONE',  ( 124.7088614775786226, 0.2603800115204892296, -16.42320221600525088 ) ) ;
#32342=CARTESIAN_POINT ( 'NONE',  ( 123.4608748109119745, 0.4262465694468514643, -12.03445270309931736 ) ) ;
#32350=CARTESIAN_POINT ( 'NONE',  ( 115.8027748109119841, -0.4660016031367893996, -10.09054647747474043 ) ) ;
#32351=CARTESIAN_POINT ( 'NONE',  ( 125.8433948109119456, -1.834011780172310813, -8.268836392978581529 ) ) ;
#32352=CARTESIAN_POINT ( 'NONE',  ( 120.6245414775786458, -0.1624402480850797581, -16.17319339645315424 ) ) ;
#32353=CARTESIAN_POINT ( 'NONE',  ( 127.0066334552993084, -3.087553896376482143, -8.300037743346093677 ) ) ;
#32355=CARTESIAN_POINT ( 'NONE',  ( 111.7184548109119788, -0.8288870151387760510, -10.36305467784173118 ) ) ;
#32357=CARTESIAN_POINT ( 'NONE',  ( 151.2860562277021472, -2.495269033102075262, -17.79652296963211455 ) ) ;
#32358=CARTESIAN_POINT ( 'NONE',  ( 125.3895814775786448, -2.084020599724406786, -8.691656652584148546 ) ) ;
#32361=CARTESIAN_POINT ( 'NONE',  ( 121.5321681442453183, -9.988377603198976828, -10.36322818467138340 ) ) ;
#32362=( BOUNDED_CURVE ( )  B_SPLINE_CURVE ( 2, ( #17860, #1416, #29244, #4840, #18759, #32649, #15335, #11694, #25604, #39508, #8270, #22174, #36069, #42121, #38670, #21584, #7669 ),
 .UNSPECIFIED., .F., .T. ) 
 B_SPLINE_CURVE_WITH_KNOTS ( ( 3, 2, 2, 2, 2, 2, 2, 2, 3 ),
 ( 0.3296282416568590001, 0.3359375000000000000, 0.3437500000000000000, 0.3515625000000000000, 0.3593750000000000000, 0.3671875000000000000, 0.3750000000000000000, 0.3828125000000000000, 0.3891217583431409999 ),
 .UNSPECIFIED. ) 
 CURVE ( )  GEOMETRIC_REPRESENTATION_ITEM ( )  RATIONAL_B_SPLINE_CURVE ( ( 0.9763430640195970289, 0.9385262470928680267, 1.000000000000000000, 0.9238795325112869605, 1.000000000000000000, 0.9238795325112869605, 1.000000000000000000, 0.9238795325112869605, 1.000000000000000000, 0.9238795325112869605, 1.000000000000000000, 0.9238795325112869605, 1.000000000000000000, 0.9238795325112869605, 1.000000000000000000, 0.9385262470928680267, 0.9763430640195970289 ) ) 
 REPRESENTATION_ITEM ( '' )  );
#32363=CARTESIAN_POINT ( 'NONE',  ( 137.3930029278097891, -9.295380705929696674, -15.97142107135823430 ) ) ;
#32366=CARTESIAN_POINT ( 'NONE',  ( 112.7395348109119766, -4.153390946401321671, -8.397313243818183892 ) ) ;
#32367=CARTESIAN_POINT ( 'NONE',  ( 127.0553483106875206, -4.550849702174990519, -18.80261012643152796 ) ) ;
#32368=CARTESIAN_POINT ( 'NONE',  ( 124.8790414775786246, -8.899110576539710493, -16.42337572283490132 ) ) ;
#32371=CARTESIAN_POINT ( 'NONE',  ( 119.4900081442453086, -1.834011780172310813, -8.268836392978581529 ) ) ;
#32376=CARTESIAN_POINT ( 'NONE',  ( 124.8790414775786246, -0.4660016031367893996, -10.09054647747474043 ) ) ;
#32379=CARTESIAN_POINT ( 'NONE',  ( 126.0135748109119902, -8.166667518702819706, -8.995218007635861213 ) ) ;
#32380=CARTESIAN_POINT ( 'NONE',  ( 124.5954081442453116, -6.222761293078241884, -8.102969835052219238 ) ) ;
#32382=CARTESIAN_POINT ( 'NONE',  ( 123.5176014775786228, -0.8288870151387760510, -10.36305467784173118 ) ) ;
#32384=CARTESIAN_POINT ( 'NONE',  ( 119.3765548109119834, 0.9020085738987339008, -11.91225656197089222 ) ) ;
#32386=CARTESIAN_POINT ( 'NONE',  ( 117.7873752477523794, -1.220279397241701647, -16.99638242193885418 ) ) ;
#32390=CARTESIAN_POINT ( 'NONE',  ( 126.3230600034178650, -9.796589426897714503, -12.29887078920687493 ) ) ;
#32391=CARTESIAN_POINT ( 'NONE',  ( 115.1220548109119761, -8.166667518702817929, -8.995218007635861213 ) ) ;
#32393=CARTESIAN_POINT ( 'NONE',  ( 113.7038881442453402, -6.222761293078241884, -8.102969835052219238 ) ) ;
#32395=CARTESIAN_POINT ( 'NONE',  ( 119.6392035773848761, -2.467220198592778413, -17.83387418641524391 ) ) ;
#32396=CARTESIAN_POINT ( 'NONE',  ( 112.5126281442453120, 0.1319031606808879209, -14.10382304977623669 ) ) ;
#32397=CARTESIAN_POINT ( 'NONE',  ( 122.8936081442453059, -9.565557343593390272, -10.61323700422343919 ) ) ;
#32399=CARTESIAN_POINT ( 'NONE',  ( 114.8384214775786489, 0.9020085738987339008, -11.91225656197089222 ) ) ;
#32404=CARTESIAN_POINT ( 'NONE',  ( 126.7702028005611368, -7.286025587178694529, -8.706033641032410841 ) ) ;
#32405=CARTESIAN_POINT ( 'NONE',  ( 120.6245414775786458, -0.1624402480850797581, -16.17319339645315424 ) ) ;
#32406=CARTESIAN_POINT ( 'NONE',  ( 114.7816948109119863, 0.5811942927096154232, -14.16772938898807155 ) ) ;
#32408=CARTESIAN_POINT ( 'NONE',  ( 117.9583881442453048, 0.1319031606808853119, -14.10382304977625800 ) ) ;
#32409=CARTESIAN_POINT ( 'NONE',  ( 120.3409081442453044, -8.899110576539710493, -16.42337572283490132 ) ) ;
#32410=CARTESIAN_POINT ( 'NONE',  ( 115.3489614775786407, -0.8288870151387760510, -10.36305467784173118 ) ) ;
#32415=CARTESIAN_POINT ( 'NONE',  ( 121.4544569107182070, -2.467220198592778413, -17.83387418641524391 ) ) ;
#32416=CARTESIAN_POINT ( 'NONE',  ( 119.3198281442452924, -9.859900752359374465, -12.68260735090039404 ) ) ;
#32419=CARTESIAN_POINT ( 'NONE',  ( 116.3700414775786527, -5.638512984488999180, -18.83840828888717311 ) ) ;
#32421=CARTESIAN_POINT ( 'NONE',  ( 119.0690086830089882, -1.087735405160626723, -17.17288456429612964 ) ) ;
#32424=CARTESIAN_POINT ( 'NONE',  ( 123.1205148109119563, -7.643976991954077427, -18.09477374809248928 ) ) ;
#32425=CARTESIAN_POINT ( 'NONE',  ( 115.9162281442453093, -5.574606645277164318, -18.38911715685844683 ) ) ;
#32427=CARTESIAN_POINT ( 'NONE',  ( 126.2184548109119788, -4.863998795839242995, -13.39321520033831447 ) ) ;
#32429=CARTESIAN_POINT ( 'NONE',  ( 112.1489877442403298, -8.920892194852200419, -16.35787768542246923 ) ) ;
#32433=CARTESIAN_POINT ( 'NONE',  ( 112.2289948109119848, -1.834011780172310813, -8.268836392978581529 ) ) ;
#32434=CARTESIAN_POINT ( 'NONE',  ( 126.6942948109119840, -8.899110576539710493, -16.42337572283490132 ) ) ;
#32435=CARTESIAN_POINT ( 'NONE',  ( 120.9081748109119872, -4.153390946401325223, -8.397313243818185668 ) ) ;
#32439=CARTESIAN_POINT ( 'NONE',  ( 118.2420214775786320, -6.222761293078241884, -8.102969835052219238 ) ) ;
#32441=CARTESIAN_POINT ( 'NONE',  ( 113.9264514740559520, -1.081026697600511843, -17.18181821144401056 ) ) ;
#32443=CARTESIAN_POINT ( 'NONE',  ( 118.6958348109119754, -6.344957434206665248, -7.627207830600338134 ) ) ;
#32444=EDGE_LOOP ( 'NONE', ( #24552, #11658, #38988, #4640 ) ) ;
#32445=CARTESIAN_POINT ( 'NONE',  ( 115.4624148109119943, -5.638512984488999180, -18.83840828888717311 ) ) ;
#32448=CARTESIAN_POINT ( 'NONE',  ( 117.4478481442453131, 0.2603800115204892296, -16.42320221600525088 ) ) ;
#32449=CARTESIAN_POINT ( 'NONE',  ( 117.5045748109119756, 0.5811942927096110934, -14.16772938898807510 ) ) ;
#32450=CARTESIAN_POINT ( 'NONE',  ( 127.0915067942372190, -10.29034310956583731, -13.72608135453547185 ) ) ;
#32456=CARTESIAN_POINT ( 'NONE',  ( 121.7023481442452919, -0.8288870151387760510, -10.36305467784173118 ) ) ;
#32460=CARTESIAN_POINT ( 'NONE',  ( 113.8740681442453138, -9.859900752359374465, -12.68260735090039404 ) ) ;
#32461=CARTESIAN_POINT ( 'NONE',  ( 113.1933481442453058, -5.574606645277164318, -18.38911715685844683 ) ) ;
#32463=CARTESIAN_POINT ( 'NONE',  ( 123.9146881442452894, 0.9020085738987339008, -11.91225656197089222 ) ) ;
#32464=CARTESIAN_POINT ( 'NONE',  ( 119.7736414775786358, -10.30919188438810075, -12.61870101168855918 ) ) ;
#32466=CARTESIAN_POINT ( 'NONE',  ( 119.3198281442452924, -9.859900752359374465, -12.68260735090039404 ) ) ;
#32467=CARTESIAN_POINT ( 'NONE',  ( 112.5693548109119888, -10.63000616557722466, -14.87417383870573495 ) ) ;
#32468=CARTESIAN_POINT ( 'NONE',  ( 120.0572748109119772, -3.383040157471821630, -19.15922257007629170 ) ) ;
#32469=CARTESIAN_POINT ( 'NONE',  ( 120.6245414775786458, -0.1624402480850797581, -16.17319339645315424 ) ) ;
#32471=CARTESIAN_POINT ( 'NONE',  ( 124.5386814775786206, -4.153390946401325223, -8.397313243818185668 ) ) ;
#32473=CARTESIAN_POINT ( 'NONE',  ( 119.7169148109119874, -9.988377603198976828, -10.36322818467138340 ) ) ;
#32475=CARTESIAN_POINT ( 'NONE',  ( 112.8529881442453302, -7.894159318335828068, -9.358103419637847864 ) ) ;
#32479=CARTESIAN_POINT ( 'NONE',  ( 119.8870948109119752, -9.261995988541697145, -16.69588392320189030 ) ) ;
#32481=CARTESIAN_POINT ( 'NONE',  ( 137.4478226697652303, -9.800447051581507196, -12.23758396775345858 ) ) ;
#32482=CARTESIAN_POINT ( 'NONE',  ( 114.3278814775786429, 0.1319031606808879209, -14.10382304977623669 ) ) ;
#32483=CARTESIAN_POINT ( 'NONE',  ( 112.0020881442453344, -9.565557343593413364, -10.61323700422348004 ) ) ;
#32484=CARTESIAN_POINT ( 'NONE',  ( 126.2940345447988761, -0.6470042893710473697, -10.63705365171230355 ) ) ;
#32487=CARTESIAN_POINT ( 'NONE',  ( 122.0274825628256963, -2.263366209404226392, -18.10533625161308180 ) ) ;
#32491=CARTESIAN_POINT ( 'NONE',  ( 120.7379948109119709, -10.63000616557722466, -14.87417383870573495 ) ) ;
#32492=CARTESIAN_POINT ( 'NONE',  ( 119.6034614775786196, -3.505236298600246325, -18.68346056562440793 ) ) ;
#32493=CARTESIAN_POINT ( 'NONE',  ( 114.2711548109119803, -0.1624402480850797581, -16.17319339645315424 ) ) ;
#32496=CARTESIAN_POINT ( 'NONE',  ( 125.7866681442452688, -0.4660016031367893996, -10.09054647747474043 ) ) ;
#32498=CARTESIAN_POINT ( 'NONE',  ( 118.4689281442453392, -10.15424416112533912, -14.75197769757731336 ) ) ;
#32499=EDGE_CURVE ( 'NONE', #43873, #34005, #38846, .T. ) ;
#32500=CARTESIAN_POINT ( 'NONE',  ( 119.9438214775786378, -2.084020599724406786, -8.691656652584148546 ) ) ;
#32501=CARTESIAN_POINT ( 'NONE',  ( 115.8027748109119841, -8.899110576539710493, -16.42337572283490132 ) ) ;
#32504=CARTESIAN_POINT ( 'NONE',  ( 124.9357681442453014, -7.643976991954077427, -18.09477374809248928 ) ) ;
#32505=CARTESIAN_POINT ( 'NONE',  ( 124.4252281442452812, -0.8288870151387760510, -10.36305467784173118 ) ) ;
#32512=CARTESIAN_POINT ( 'NONE',  ( 117.1074881442453233, -10.63000616557722466, -14.87417383870573495 ) ) ;
#32513=CARTESIAN_POINT ( 'NONE',  ( 117.2776681442452968, -5.638512984488999180, -18.83840828888717311 ) ) ;
#32514=DIRECTION ( 'NONE',  ( 1.000000000000000000, 0.000000000000000000, 0.000000000000000000 ) ) ;
#32515=CARTESIAN_POINT ( 'NONE',  ( 111.8886348109120092, -3.383040157471821630, -19.15922257007629170 ) ) ;
#32519=CARTESIAN_POINT ( 'NONE',  ( 118.0718414775786300, -9.261995988541697145, -16.69588392320189030 ) ) ;
#32520=CARTESIAN_POINT ( 'NONE',  ( 122.4397948109119767, -0.1624402480850797581, -16.17319339645315424 ) ) ;
#32522=CARTESIAN_POINT ( 'NONE',  ( 113.9875214775786532, -8.899110576539710493, -16.42337572283490132 ) ) ;
#32523=CARTESIAN_POINT ( 'NONE',  ( 122.5532481442453019, -10.63000616557722466, -14.87417383870573495 ) ) ;
#32527=CARTESIAN_POINT ( 'NONE',  ( 116.7104014775786425, -8.899110576539710493, -16.42337572283490132 ) ) ;
#32535=CARTESIAN_POINT ( 'NONE',  ( 120.6812681442452941, -10.30919188438810075, -12.61870101168855918 ) ) ;
#32536=VERTEX_POINT ( 'NONE', #41039 ) ;
#32540=CARTESIAN_POINT ( 'NONE',  ( 115.9729548109119861, -3.505236298600246325, -18.68346056562440793 ) ) ;
#32542=( BOUNDED_SURFACE ( )  B_SPLINE_SURFACE ( 1, 2, ( 
 ( #34330, #6301, #16575, #38578, #39043, #7814, #20446, #28569, #42252, #42031, #34106, #3103, #17030, #42478, #23641, #2643, #3932, #518, #2874, #17852, #14430, #13153, #27056, #16804, #44618, #13384, #41202, #9961, #43368, #8707, #8035, #15104, #43142, #32640, #11912, #18526, #12365, #18298, #32193, #39721, #18750, #25374, #22612, #4383, #39498, #29235, #28794, #25812, #8486, #14882, #33077, #15326, #19200, #15548, #1408, #1849, #29453, #1192, #12137, #26039, #21940, #39945, #8261, #22390, #35832, #15778, #36286, #966, #26265, #5054, #42700, #36510, #11470, #5284, #29680, #18969, #36060, #4829, #4606, #22165, #39272, #32858, #32419, #29014, #42924, #11687, #25593, #43592, #1628, #40172, #21722, #35609, #37650, #16236, #44503, #37179, #16004, #40403, #9384, #26496, #36731, #44286, #13494, #27399, #12820, #9851, #2766, #5952, #9164, #44053, #26718, #16690, #43826, #30582, #23294, #20109, #29912, #40862, #40627, #13266, #9615, #20335, #12592, #5723, #19876, #27172, #33765, #41093, #2533, #16917, #5497, #8936, #16460, #23068, #30811, #6189, #33995, #23760, #37420, #13039, #2991, #6425, #34218, #30364, #22840, #44735, #30139, #19418, #33304, #26938, #36952, #2306, #19641, #33528, #23534, #2080, #38521, #27623, #14375, #35093, #24863, #3441, #31691, #24416, #3215, #41537, #41755, #13716, #23983, #31468, #680, #14598, #20, #42197, #3876, #38307, #10300, #31248, #13933, #17798, #31028, #460, #10515, #7299, #17141, #28065, #27845, #28288, #41975, #7524, #44959, #38092, #7084, #10958, #20993, #38754, #34867, #4095, #37871, #41321, #3655, #24201, #18017, #21218, #21440, #35325, #24639, #240, #31915, #10080, #6647, #17576, #20555, #34436, #17360, #6868, #20776, #34656, #14150, #10740, #12082, #18911, #39446, #18477, #4998, #15495, #14829, #21886, #4776, #8207, #18697, #25321, #19140, #25090, #38984, #1355, #25539, #32141, #29402, #11187, #1132, #36005, #35552, #32586, #15268, #21664, #39893, #22115, #25988, #22338, #29176, #8654, #36233, #7978, #32804, #1574, #28739 ),
 ( #1797, #35782, #908, #43088, #28962, #11856, #25763, #39669, #4550, #8432, #43314, #7756, #22555, #36455, #42870, #4324, #18245, #5226, #33023, #15051, #28518, #42423, #11627, #42643, #11412, #39214, #32366, #40573, #43541, #8879, #16403, #30302, #26436, #15724, #33254, #33935, #15951, #40345, #19820, #26884, #23242, #12311, #5897, #29854, #37361, #36675, #23475, #44228, #19365, #43769, #36900, #43996, #37123, #26208, #40115, #2706, #29626, #16633, #22780, #5671, #40803, #30527, #19589, #5445, #6133, #20052, #33470, #2026, #12535, #9106, #23008, #2250, #2478, #16179, #33706, #30082, #12760, #26659, #9333, #12988, #9559, #36640, #2208, #29365, #26170, #32764, #30038, #11816, #1760, #5413, #36195, #19329, #33215, #22298, #40535, #22738, #26621, #22971, #40075, #9296, #36861, #8620, #5631, #19551, #15459, #33429, #15686, #1989, #43276, #23204, #15915, #39631, #19779, #8839, #25724, #16137, #8394, #43955, #12718, #29813, #43506, #12274, #12045, #29588, #4959, #43729, #1537, #22517, #25948, #39855, #36414, #37082, #26395, #5182, #5857, #33661, #2438, #19099, #29137, #12497, #32986, #43049, #18873, #40305, #9069, #37776, #27306, #6549, #13175, #12951, #23893, #34566, #16596, #13404, #20007, #17269, #44189, #34126, #20466, #23434, #34347, #3125, #9516, #27754, #9981, #13838, #10203, #41223, #41669, #24111, #40998, #38005, #6779, #2663, #20689, #2896, #17049, #30489, #10426, #30942, #26847, #6997, #44865, #40760, #3350, #37318, #31160, #45079, #13621, #30718, #44640, #44409, #16825, #6089, #27530, #33893, #9752, #27077, #23663, #37550, #24334, #41445, #6322, #38218, #20909, #34783, #20240, #16361, #30263, #10645, #34994, #4004, #21120, #31376, #38886, #8727, #22633, #7424, #5073, #43167, #595, #3778, #38655, #21345, #11936, #38437, #25832, #17926, #15349, #24550, #36083, #35229, #39740, #4854, #15572, #7207, #371, #14505, #8508, #28418, #22412, #42329, #12158, #147, #3566, #11090, #17702, #26061, #1429, #29257, #36305, #32661, #8284, #43391, #18990, #32878, #31825 ) ),
 .UNSPECIFIED., .F., .F., .T. ) 
 B_SPLINE_SURFACE_WITH_KNOTS ( ( 2, 2 ),
 ( 3, 2, 2, 2, 2, 2, 2, 2, 2, 2, 2, 2, 2, 2, 2, 2, 2, 2, 2, 2, 2, 2, 2, 2, 2, 2, 2, 2, 2, 2, 2, 2, 2, 2, 2, 2, 2, 2, 2, 2, 2, 2, 2, 2, 2, 2, 2, 2, 2, 2, 2, 2, 2, 2, 2, 2, 2, 2, 2, 2, 2, 2, 2, 2, 2, 2, 2, 2, 2, 2, 2, 2, 2, 2, 2, 2, 2, 2, 2, 2, 2, 2, 2, 2, 2, 2, 2, 2, 2, 2, 2, 2, 2, 2, 2, 2, 2, 2, 2, 2, 2, 2, 2, 2, 2, 2, 2, 2, 2, 2, 2, 2, 2, 2, 2, 2, 2, 2, 2, 2, 2, 2, 2, 2, 2, 2, 2, 2, 3 ),
 ( 0.000000000000000000, 1.000000000000000000 ),
 ( 0.000000000000000000, 0.007812500000000000000, 0.01562500000000000000, 0.02343750000000000000, 0.03125000000000000000, 0.03906250000000000000, 0.04687500000000000000, 0.05468750000000000000, 0.06250000000000000000, 0.07031250000000000000, 0.07812500000000000000, 0.08593750000000000000, 0.09375000000000000000, 0.1015625000000000000, 0.1093750000000000000, 0.1171875000000000000, 0.1250000000000000000, 0.1328125000000000000, 0.1406250000000000000, 0.1484375000000000000, 0.1562500000000000000, 0.1640625000000000000, 0.1718750000000000000, 0.1796875000000000000, 0.1875000000000000000, 0.1953125000000000000, 0.2031250000000000000, 0.2109375000000000000, 0.2187500000000000000, 0.2265625000000000000, 0.2343750000000000000, 0.2421875000000000000, 0.2500000000000000000, 0.2578125000000000000, 0.2656250000000000000, 0.2734375000000000000, 0.2812500000000000000, 0.2890625000000000000, 0.2968750000000000000, 0.3046875000000000000, 0.3125000000000000000, 0.3203125000000000000, 0.3281250000000000000, 0.3359375000000000000, 0.3437500000000000000, 0.3515625000000000000, 0.3593750000000000000, 0.3671875000000000000, 0.3750000000000000000, 0.3828125000000000000, 0.3906250000000000000, 0.3984375000000000000, 0.4062500000000000000, 0.4140625000000000000, 0.4218750000000000000, 0.4296875000000000000, 0.4375000000000000000, 0.4453125000000000000, 0.4531250000000000000, 0.4609375000000000000, 0.4687500000000000000, 0.4765625000000000000, 0.4843750000000000000, 0.4921875000000000000, 0.5000000000000000000, 0.5078125000000000000, 0.5156250000000000000, 0.5234375000000000000, 0.5312500000000000000, 0.5390625000000000000, 0.5468750000000000000, 0.5546875000000000000, 0.5625000000000000000, 0.5703125000000000000, 0.5781250000000000000, 0.5859375000000000000, 0.5937500000000000000, 0.6015625000000000000, 0.6093750000000000000, 0.6171875000000000000, 0.6250000000000000000, 0.6328125000000000000, 0.6406250000000000000, 0.6484375000000000000, 0.6562500000000000000, 0.6640625000000000000, 0.6718750000000000000, 0.6796875000000000000, 0.6875000000000000000, 0.6953125000000000000, 0.7031250000000000000, 0.7109375000000000000, 0.7187500000000000000, 0.7265625000000000000, 0.7343750000000000000, 0.7421875000000000000, 0.7500000000000000000, 0.7578125000000000000, 0.7656250000000000000, 0.7734375000000000000, 0.7812500000000000000, 0.7890625000000000000, 0.7968750000000000000, 0.8046875000000000000, 0.8125000000000000000, 0.8203125000000000000, 0.8281250000000000000, 0.8359375000000000000, 0.8437500000000000000, 0.8515625000000000000, 0.8593750000000000000, 0.8671875000000000000, 0.8750000000000000000, 0.8828125000000000000, 0.8906250000000000000, 0.8984375000000000000, 0.9062500000000000000, 0.9140625000000000000, 0.9218750000000000000, 0.9296875000000000000, 0.9375000000000000000, 0.9453125000000000000, 0.9531250000000000000, 0.9609375000000000000, 0.9687500000000000000, 0.9765625000000000000, 0.9843750000000000000, 0.9921875000000000000, 1.000000000000000000 ),
 .UNSPECIFIED. ) 
 GEOMETRIC_REPRESENTATION_ITEM ( )  RATIONAL_B_SPLINE_SURFACE ( (
 ( 1.000000000000000000, 0.9238795325112869605, 1.000000000000000000, 0.9238795325112869605, 1.000000000000000000, 0.9238795325112869605, 1.000000000000000000, 0.9238795325112869605, 1.000000000000000000, 0.9238795325112869605, 1.000000000000000000, 0.9238795325112869605, 1.000000000000000000, 0.9238795325112869605, 1.000000000000000000, 0.9238795325112869605, 1.000000000000000000, 0.9238795325112869605, 1.000000000000000000, 0.9238795325112869605, 1.000000000000000000, 0.9238795325112869605, 1.000000000000000000, 0.9238795325112869605, 1.000000000000000000, 0.9238795325112869605, 1.000000000000000000, 0.9238795325112869605, 1.000000000000000000, 0.9238795325112869605, 1.000000000000000000, 0.9238795325112869605, 1.000000000000000000, 0.9238795325112869605, 1.000000000000000000, 0.9238795325112869605, 1.000000000000000000, 0.9238795325112869605, 1.000000000000000000, 0.9238795325112869605, 1.000000000000000000, 0.9238795325112869605, 1.000000000000000000, 0.9238795325112869605, 1.000000000000000000, 0.9238795325112869605, 1.000000000000000000, 0.9238795325112869605, 1.000000000000000000, 0.9238795325112869605, 1.000000000000000000, 0.9238795325112869605, 1.000000000000000000, 0.9238795325112869605, 1.000000000000000000, 0.9238795325112869605, 1.000000000000000000, 0.9238795325112869605, 1.000000000000000000, 0.9238795325112869605, 1.000000000000000000, 0.9238795325112869605, 1.000000000000000000, 0.9238795325112869605, 1.000000000000000000, 0.9238795325112869605, 1.000000000000000000, 0.9238795325112869605, 1.000000000000000000, 0.9238795325112869605, 1.000000000000000000, 0.9238795325112869605, 1.000000000000000000, 0.9238795325112869605, 1.000000000000000000, 0.9238795325112869605, 1.000000000000000000, 0.9238795325112869605, 1.000000000000000000, 0.9238795325112869605, 1.000000000000000000, 0.9238795325112869605, 1.000000000000000000, 0.9238795325112869605, 1.000000000000000000, 0.9238795325112869605, 1.000000000000000000, 0.9238795325112869605, 1.000000000000000000, 0.9238795325112869605, 1.000000000000000000, 0.9238795325112869605, 1.000000000000000000, 0.9238795325112869605, 1.000000000000000000, 0.9238795325112869605, 1.000000000000000000, 0.9238795325112869605, 1.000000000000000000, 0.9238795325112869605, 1.000000000000000000, 0.9238795325112869605, 1.000000000000000000, 0.9238795325112869605, 1.000000000000000000, 0.9238795325112869605, 1.000000000000000000, 0.9238795325112869605, 1.000000000000000000, 0.9238795325112869605, 1.000000000000000000, 0.9238795325112869605, 1.000000000000000000, 0.9238795325112869605, 1.000000000000000000, 0.9238795325112869605, 1.000000000000000000, 0.9238795325112869605, 1.000000000000000000, 0.9238795325112869605, 1.000000000000000000, 0.9238795325112869605, 1.000000000000000000, 0.9238795325112869605, 1.000000000000000000, 0.9238795325112869605, 1.000000000000000000, 0.9238795325112869605, 1.000000000000000000, 0.9238795325112869605, 1.000000000000000000, 0.9238795325112869605, 1.000000000000000000, 0.9238795325112869605, 1.000000000000000000, 0.9238795325112869605, 1.000000000000000000, 0.9238795325112869605, 1.000000000000000000, 0.9238795325112869605, 1.000000000000000000, 0.9238795325112869605, 1.000000000000000000, 0.9238795325112869605, 1.000000000000000000, 0.9238795325112869605, 1.000000000000000000, 0.9238795325112869605, 1.000000000000000000, 0.9238795325112869605, 1.000000000000000000, 0.9238795325112869605, 1.000000000000000000, 0.9238795325112869605, 1.000000000000000000, 0.9238795325112869605, 1.000000000000000000, 0.9238795325112869605, 1.000000000000000000, 0.9238795325112869605, 1.000000000000000000, 0.9238795325112869605, 1.000000000000000000, 0.9238795325112869605, 1.000000000000000000, 0.9238795325112869605, 1.000000000000000000, 0.9238795325112869605, 1.000000000000000000, 0.9238795325112869605, 1.000000000000000000, 0.9238795325112869605, 1.000000000000000000, 0.9238795325112869605, 1.000000000000000000, 0.9238795325112869605, 1.000000000000000000, 0.9238795325112869605, 1.000000000000000000, 0.9238795325112869605, 1.000000000000000000, 0.9238795325112869605, 1.000000000000000000, 0.9238795325112869605, 1.000000000000000000, 0.9238795325112869605, 1.000000000000000000, 0.9238795325112869605, 1.000000000000000000, 0.9238795325112869605, 1.000000000000000000, 0.9238795325112869605, 1.000000000000000000, 0.9238795325112869605, 1.000000000000000000, 0.9238795325112869605, 1.000000000000000000, 0.9238795325112869605, 1.000000000000000000, 0.9238795325112869605, 1.000000000000000000, 0.9238795325112869605, 1.000000000000000000, 0.9238795325112869605, 1.000000000000000000, 0.9238795325112869605, 1.000000000000000000, 0.9238795325112869605, 1.000000000000000000, 0.9238795325112869605, 1.000000000000000000, 0.9238795325112869605, 1.000000000000000000, 0.9238795325112869605, 1.000000000000000000, 0.9238795325112869605, 1.000000000000000000, 0.9238795325112869605, 1.000000000000000000, 0.9238795325112869605, 1.000000000000000000, 0.9238795325112869605, 1.000000000000000000, 0.9238795325112869605, 1.000000000000000000, 0.9238795325112869605, 1.000000000000000000, 0.9238795325112869605, 1.000000000000000000, 0.9238795325112869605, 1.000000000000000000, 0.9238795325112869605, 1.000000000000000000, 0.9238795325112869605, 1.000000000000000000, 0.9238795325112869605, 1.000000000000000000, 0.9238795325112869605, 1.000000000000000000, 0.9238795325112869605, 1.000000000000000000, 0.9238795325112869605, 1.000000000000000000, 0.9238795325112869605, 1.000000000000000000, 0.9238795325112869605, 1.000000000000000000, 0.9238795325112869605, 1.000000000000000000, 0.9238795325112869605, 1.000000000000000000, 0.9238795325112869605, 1.000000000000000000, 0.9238795325112869605, 1.000000000000000000, 0.9238795325112869605, 1.000000000000000000),
 ( 1.000000000000000000, 0.9238795325112869605, 1.000000000000000000, 0.9238795325112869605, 1.000000000000000000, 0.9238795325112869605, 1.000000000000000000, 0.9238795325112869605, 1.000000000000000000, 0.9238795325112869605, 1.000000000000000000, 0.9238795325112869605, 1.000000000000000000, 0.9238795325112869605, 1.000000000000000000, 0.9238795325112869605, 1.000000000000000000, 0.9238795325112869605, 1.000000000000000000, 0.9238795325112869605, 1.000000000000000000, 0.9238795325112869605, 1.000000000000000000, 0.9238795325112869605, 1.000000000000000000, 0.9238795325112869605, 1.000000000000000000, 0.9238795325112869605, 1.000000000000000000, 0.9238795325112869605, 1.000000000000000000, 0.9238795325112869605, 1.000000000000000000, 0.9238795325112869605, 1.000000000000000000, 0.9238795325112869605, 1.000000000000000000, 0.9238795325112869605, 1.000000000000000000, 0.9238795325112869605, 1.000000000000000000, 0.9238795325112869605, 1.000000000000000000, 0.9238795325112869605, 1.000000000000000000, 0.9238795325112869605, 1.000000000000000000, 0.9238795325112869605, 1.000000000000000000, 0.9238795325112869605, 1.000000000000000000, 0.9238795325112869605, 1.000000000000000000, 0.9238795325112869605, 1.000000000000000000, 0.9238795325112869605, 1.000000000000000000, 0.9238795325112869605, 1.000000000000000000, 0.9238795325112869605, 1.000000000000000000, 0.9238795325112869605, 1.000000000000000000, 0.9238795325112869605, 1.000000000000000000, 0.9238795325112869605, 1.000000000000000000, 0.9238795325112869605, 1.000000000000000000, 0.9238795325112869605, 1.000000000000000000, 0.9238795325112869605, 1.000000000000000000, 0.9238795325112869605, 1.000000000000000000, 0.9238795325112869605, 1.000000000000000000, 0.9238795325112869605, 1.000000000000000000, 0.9238795325112869605, 1.000000000000000000, 0.9238795325112869605, 1.000000000000000000, 0.9238795325112869605, 1.000000000000000000, 0.9238795325112869605, 1.000000000000000000, 0.9238795325112869605, 1.000000000000000000, 0.9238795325112869605, 1.000000000000000000, 0.9238795325112869605, 1.000000000000000000, 0.9238795325112869605, 1.000000000000000000, 0.9238795325112869605, 1.000000000000000000, 0.9238795325112869605, 1.000000000000000000, 0.9238795325112869605, 1.000000000000000000, 0.9238795325112869605, 1.000000000000000000, 0.9238795325112869605, 1.000000000000000000, 0.9238795325112869605, 1.000000000000000000, 0.9238795325112869605, 1.000000000000000000, 0.9238795325112869605, 1.000000000000000000, 0.9238795325112869605, 1.000000000000000000, 0.9238795325112869605, 1.000000000000000000, 0.9238795325112869605, 1.000000000000000000, 0.9238795325112869605, 1.000000000000000000, 0.9238795325112869605, 1.000000000000000000, 0.9238795325112869605, 1.000000000000000000, 0.9238795325112869605, 1.000000000000000000, 0.9238795325112869605, 1.000000000000000000, 0.9238795325112869605, 1.000000000000000000, 0.9238795325112869605, 1.000000000000000000, 0.9238795325112869605, 1.000000000000000000, 0.9238795325112869605, 1.000000000000000000, 0.9238795325112869605, 1.000000000000000000, 0.9238795325112869605, 1.000000000000000000, 0.9238795325112869605, 1.000000000000000000, 0.9238795325112869605, 1.000000000000000000, 0.9238795325112869605, 1.000000000000000000, 0.9238795325112869605, 1.000000000000000000, 0.9238795325112869605, 1.000000000000000000, 0.9238795325112869605, 1.000000000000000000, 0.9238795325112869605, 1.000000000000000000, 0.9238795325112869605, 1.000000000000000000, 0.9238795325112869605, 1.000000000000000000, 0.9238795325112869605, 1.000000000000000000, 0.9238795325112869605, 1.000000000000000000, 0.9238795325112869605, 1.000000000000000000, 0.9238795325112869605, 1.000000000000000000, 0.9238795325112869605, 1.000000000000000000, 0.9238795325112869605, 1.000000000000000000, 0.9238795325112869605, 1.000000000000000000, 0.9238795325112869605, 1.000000000000000000, 0.9238795325112869605, 1.000000000000000000, 0.9238795325112869605, 1.000000000000000000, 0.9238795325112869605, 1.000000000000000000, 0.9238795325112869605, 1.000000000000000000, 0.9238795325112869605, 1.000000000000000000, 0.9238795325112869605, 1.000000000000000000, 0.9238795325112869605, 1.000000000000000000, 0.9238795325112869605, 1.000000000000000000, 0.9238795325112869605, 1.000000000000000000, 0.9238795325112869605, 1.000000000000000000, 0.9238795325112869605, 1.000000000000000000, 0.9238795325112869605, 1.000000000000000000, 0.9238795325112869605, 1.000000000000000000, 0.9238795325112869605, 1.000000000000000000, 0.9238795325112869605, 1.000000000000000000, 0.9238795325112869605, 1.000000000000000000, 0.9238795325112869605, 1.000000000000000000, 0.9238795325112869605, 1.000000000000000000, 0.9238795325112869605, 1.000000000000000000, 0.9238795325112869605, 1.000000000000000000, 0.9238795325112869605, 1.000000000000000000, 0.9238795325112869605, 1.000000000000000000, 0.9238795325112869605, 1.000000000000000000, 0.9238795325112869605, 1.000000000000000000, 0.9238795325112869605, 1.000000000000000000, 0.9238795325112869605, 1.000000000000000000, 0.9238795325112869605, 1.000000000000000000, 0.9238795325112869605, 1.000000000000000000, 0.9238795325112869605, 1.000000000000000000, 0.9238795325112869605, 1.000000000000000000, 0.9238795325112869605, 1.000000000000000000, 0.9238795325112869605, 1.000000000000000000, 0.9238795325112869605, 1.000000000000000000, 0.9238795325112869605, 1.000000000000000000, 0.9238795325112869605, 1.000000000000000000, 0.9238795325112869605, 1.000000000000000000, 0.9238795325112869605, 1.000000000000000000, 0.9238795325112869605, 1.000000000000000000, 0.9238795325112869605, 1.000000000000000000, 0.9238795325112869605, 1.000000000000000000, 0.9238795325112869605, 1.000000000000000000, 0.9238795325112869605, 1.000000000000000000) ) ) 
 REPRESENTATION_ITEM ( '' )  SURFACE ( )  );
#32543=CARTESIAN_POINT ( 'NONE',  ( 122.1561614775786353, -8.899110576539710493, -16.42337572283490132 ) ) ;
#32548=CARTESIAN_POINT ( 'NONE',  ( 123.7445081442452874, -7.894159318335828068, -9.358103419637847864 ) ) ;
#32550=CARTESIAN_POINT ( 'NONE',  ( 112.4559014775786494, -9.988377603198976828, -10.36322818467138340 ) ) ;
#32551=CARTESIAN_POINT ( 'NONE',  ( 121.0216281442452981, -1.561330072975668948, -17.79121239304076951 ) ) ;
#32552=CARTESIAN_POINT ( 'NONE',  ( 125.7866681442452688, -8.899110576539710493, -16.42337572283490132 ) ) ;
#32556=CARTESIAN_POINT ( 'NONE',  ( 120.5110881442453206, -3.505236298600246325, -18.68346056562440793 ) ) ;
#32558=CARTESIAN_POINT ( 'NONE',  ( 118.9794681442453026, -9.261995988541697145, -16.69588392320189030 ) ) ;
#32561=CARTESIAN_POINT ( 'NONE',  ( 114.1577014775786552, -3.505236298600246325, -18.68346056562440793 ) ) ;
#32563=CARTESIAN_POINT ( 'NONE',  ( 125.3328548109119964, -9.261995988541697145, -16.69588392320189030 ) ) ;
#32565=CARTESIAN_POINT ( 'NONE',  ( 121.9859814775786333, -9.565557343593413364, -10.61323700422348004 ) ) ;
#32572=CARTESIAN_POINT ( 'NONE',  ( 113.7038881442453402, -3.383040157471821630, -19.15922257007629170 ) ) ;
#32574=CARTESIAN_POINT ( 'NONE',  ( 121.3052614775786111, -7.643976991954077427, -18.09477374809248928 ) ) ;
#32576=CARTESIAN_POINT ( 'NONE',  ( 123.7445081442452874, -7.894159318335831621, -9.358103419637849640 ) ) ;
#32577=CARTESIAN_POINT ( 'NONE',  ( 124.5847204811916669, -3.807985514183276354, -19.09877912889402651 ) ) ;
#32582=CARTESIAN_POINT ( 'NONE',  ( 120.5678148109119832, -8.166667518702819706, -8.995218007635861213 ) ) ;
#32586=CARTESIAN_POINT ( 'NONE',  ( 125.5030348109119558, -3.383040157471821630, -19.15922257007629170 ) ) ;
#32589=CARTESIAN_POINT ( 'NONE',  ( 125.1059481442452750, -1.833838273342660141, -17.42832698103878286 ) ) ;
#32591=CARTESIAN_POINT ( 'NONE',  ( 117.3911214775786505, -1.561330072975668504, -17.79121239304076951 ) ) ;
#32597=CARTESIAN_POINT ( 'NONE',  ( 124.4252281442452812, -9.261995988541697145, -16.69588392320189030 ) ) ;
#32600=CARTESIAN_POINT ( 'NONE',  ( 113.1366214775786432, -7.643976991954077427, -18.09477374809248928 ) ) ;
#32602=CARTESIAN_POINT ( 'NONE',  ( 125.3895814775786448, -2.084020599724406786, -8.691656652584148546 ) ) ;
#32604=CARTESIAN_POINT ( 'NONE',  ( 123.0070614775786169, -10.15424416112533912, -14.75197769757731336 ) ) ;
#32605=CARTESIAN_POINT ( 'NONE',  ( 113.5904348109119866, -2.084020599724406786, -8.691656652584148546 ) ) ;
#32606=CARTESIAN_POINT ( 'NONE',  ( 121.0216281442452981, -1.561330072975668948, -17.79121239304076951 ) ) ;
#32614=CARTESIAN_POINT ( 'NONE',  ( 126.2333338125945517, -9.798786772754054297, -12.54286052501422688 ) ) ;
#32615=CARTESIAN_POINT ( 'NONE',  ( 113.6471614775786492, -5.638512984488999180, -18.83840828888717311 ) ) ;
#32616=ORIENTED_EDGE ( 'NONE', *, *, #39615, .T. ) ;
#32617=CARTESIAN_POINT ( 'NONE',  ( 116.6536748109119941, -10.15424416112533912, -14.75197769757731336 ) ) ;
#32622=CARTESIAN_POINT ( 'NONE',  ( 123.2223381469516568, -3.929494816604741203, -18.62311481910882804 ) ) ;
#32624=CARTESIAN_POINT ( 'NONE',  ( 115.8595014775786609, -1.834011780172310813, -8.268836392978581529 ) ) ;
#32629=CARTESIAN_POINT ( 'NONE',  ( 117.3343948109119737, -6.222761293078241884, -8.102969835052219238 ) ) ;
#32630=CARTESIAN_POINT ( 'NONE',  ( 115.5191414775786569, -3.383040157471821630, -19.15922257007629170 ) ) ;
#32632=CARTESIAN_POINT ( 'NONE',  ( 125.2761281442453054, 0.4262465694468514643, -12.03445270309931736 ) ) ;
#32633=CARTESIAN_POINT ( 'NONE',  ( 124.9357681442453014, -7.643976991954077427, -18.09477374809248928 ) ) ;
#32634=CARTESIAN_POINT ( 'NONE',  ( 116.5402214775786405, -9.565557343593413364, -10.61323700422348004 ) ) ;
#32635=ORIENTED_EDGE ( 'NONE', *, *, #27585, .F. ) ;
#32638=CARTESIAN_POINT ( 'NONE',  ( 119.4332814775786318, -8.899110576539710493, -16.42337572283490132 ) ) ;
#32640=CARTESIAN_POINT ( 'NONE',  ( 113.5904348109119866, -7.893985811506177619, -18.51759400769804742 ) ) ;
#32642=CARTESIAN_POINT ( 'NONE',  ( 114.3278814775786429, 0.1319031606808879209, -14.10382304977623669 ) ) ;
#32645=CARTESIAN_POINT ( 'NONE',  ( 121.4754414775786131, -1.833838273342659697, -17.42832698103878286 ) ) ;
#32646=CARTESIAN_POINT ( 'NONE',  ( 115.9729548109119861, -3.505236298600246325, -18.68346056562440793 ) ) ;
#32647=CARTESIAN_POINT ( 'NONE',  ( 110.8846310998092264, -2.698019154030093514, -17.52653087006472177 ) ) ;
#32649=CARTESIAN_POINT ( 'NONE',  ( 116.3133148109120043, -2.084020599724407230, -8.691656652584150322 ) ) ;
#32654=CARTESIAN_POINT ( 'NONE',  ( 116.7104014775786425, -0.4660016031367893996, -10.09054647747474043 ) ) ;
#32655=CARTESIAN_POINT ( 'NONE',  ( 112.6828081442453282, -7.893985811506177619, -18.51759400769804742 ) ) ;
#32656=CARTESIAN_POINT ( 'NONE',  ( 116.8238548109119819, -5.574606645277164318, -18.38911715685844683 ) ) ;
#32657=CARTESIAN_POINT ( 'NONE',  ( 120.3976348109119812, -7.643976991954077427, -18.09477374809248928 ) ) ;
#32660=CARTESIAN_POINT ( 'NONE',  ( 118.4122014775786340, -9.859900752359374465, -12.68260735090039404 ) ) ;
#32661=CARTESIAN_POINT ( 'NONE',  ( 125.5030348109119558, -6.222761293078241884, -8.102969835052219238 ) ) ;
#32666=CARTESIAN_POINT ( 'NONE',  ( 116.9940348109119839, -9.988377603198976828, -10.36322818467138340 ) ) ;
#32667=VERTEX_POINT ( 'NONE', #3817 ) ;
#32668=CARTESIAN_POINT ( 'NONE',  ( 121.8725281442453223, -3.383040157471821630, -19.15922257007629170 ) ) ;
#32671=CARTESIAN_POINT ( 'NONE',  ( 117.5613014775786525, 0.9020085738987339008, -11.91225656197089222 ) ) ;
#32672=CARTESIAN_POINT ( 'NONE',  ( 116.4834948109119779, -1.561330072975668504, -17.79121239304076951 ) ) ;
#32673=CARTESIAN_POINT ( 'NONE',  ( 126.3115243456358883, -9.898515367256928599, -13.04493836775356463 ) ) ;
#32679=CARTESIAN_POINT ( 'NONE',  ( 118.5823814775786360, -7.643976991954077427, -18.09477374809248928 ) ) ;
#32682=CARTESIAN_POINT ( 'NONE',  ( 113.8173414775786512, -9.565557343593413364, -10.61323700422348004 ) ) ;
#32684=CARTESIAN_POINT ( 'NONE',  ( 112.3424481442453384, -3.505236298600246325, -18.68346056562440793 ) ) ;
#32685=CARTESIAN_POINT ( 'NONE',  ( 118.2987481442453088, -1.561330072975668504, -17.79121239304076951 ) ) ;
#32687=CARTESIAN_POINT ( 'NONE',  ( 117.3343948109119737, -6.222761293078241884, -8.102969835052219238 ) ) ;
#32688=CARTESIAN_POINT ( 'NONE',  ( 116.3700414775786527, -5.638512984488999180, -18.83840828888717311 ) ) ;
#32689=CARTESIAN_POINT ( 'NONE',  ( 119.7169148109119874, -9.988377603198976828, -10.36322818467138340 ) ) ;
#32691=CARTESIAN_POINT ( 'NONE',  ( 121.3052614775786111, -7.643976991954077427, -18.09477374809248928 ) ) ;
#32692=ORIENTED_EDGE ( 'NONE', *, *, #44046, .F. ) ;
#32693=CARTESIAN_POINT ( 'NONE',  ( 123.4041481442452834, 0.1319031606808879209, -14.10382304977623669 ) ) ;
#32694=CARTESIAN_POINT ( 'NONE',  ( 118.6958348109119754, -6.344957434206665248, -7.627207830600338134 ) ) ;
#32696=CARTESIAN_POINT ( 'NONE',  ( 120.2841814775786276, 0.9020085738987339008, -11.91225656197089222 ) ) ;
#32697=CARTESIAN_POINT ( 'NONE',  ( 151.2860562277021472, -1.295815253274133161, -16.89579513612386563 ) ) ;
#32701=AXIS2_PLACEMENT_3D ( 'NONE', #1220, #8292, #22419 ) ;
#32702=CARTESIAN_POINT ( 'NONE',  ( 135.5886503745816469, -10.36823017854120543, -11.00515641294314584 ) ) ;
#32703=CARTESIAN_POINT ( 'NONE',  ( 114.4413348109119823, -0.8288870151387760510, -10.36305467784173118 ) ) ;
#32704=CARTESIAN_POINT ( 'NONE',  ( 124.2550481442452792, -9.988377603198980381, -10.36322818467138518 ) ) ;
#32707=CARTESIAN_POINT ( 'NONE',  ( 114.7249681442453237, -9.565557343593413364, -10.61323700422348004 ) ) ;
#32708=CARTESIAN_POINT ( 'NONE',  ( 114.9859420330015354, -1.172797794773246416, -17.05961127468924587 ) ) ;
#32711=CARTESIAN_POINT ( 'NONE',  ( 118.2420214775786320, -3.383040157471821630, -19.15922257007629170 ) ) ;
#32713=CARTESIAN_POINT ( 'NONE',  ( 121.3619881442452879, -5.574606645277164318, -18.38911715685844683 ) ) ;
#32715=CARTESIAN_POINT ( 'NONE',  ( 136.2632467228178825, -7.076446026251988819, -7.986235859556298777 ) ) ;
#32718=CARTESIAN_POINT ( 'NONE',  ( 119.6034614775786196, -3.505236298600246325, -18.68346056562440793 ) ) ;
#32719=CARTESIAN_POINT ( 'NONE',  ( 120.9081748109119872, -4.153390946401325223, -8.397313243818185668 ) ) ;
#32720=CARTESIAN_POINT ( 'NONE',  ( 117.2776681442452968, -4.153390946401325223, -8.397313243818185668 ) ) ;
#32723=CARTESIAN_POINT ( 'NONE',  ( 123.1205148109119563, -7.643976991954077427, -18.09477374809248928 ) ) ;
#32724=CARTESIAN_POINT ( 'NONE',  ( 125.2761281442453054, 0.4262465694468514643, -12.03445270309931736 ) ) ;
#32726=CARTESIAN_POINT ( 'NONE',  ( 112.4201593777725208, -1.267766418764741276, -16.93314635290707315 ) ) ;
#32729=FACE_OUTER_BOUND ( 'NONE', #40738, .T. ) ;
#32731=CARTESIAN_POINT ( 'NONE',  ( 119.4332814775786318, -0.4660016031367893996, -10.09054647747474043 ) ) ;
#32732=CARTESIAN_POINT ( 'NONE',  ( 117.2209414775786485, -7.893985811506177619, -18.51759400769804742 ) ) ;
#32734=CARTESIAN_POINT ( 'NONE',  ( 116.0864081442453113, -9.988377603198976828, -10.36322818467138340 ) ) ;
#32738=CARTESIAN_POINT ( 'NONE',  ( 119.1496481442453046, -3.383040157471821630, -19.15922257007629170 ) ) ;
#32740=CARTESIAN_POINT ( 'NONE',  ( 111.8886348109120092, -3.383040157471821630, -19.15922257007629170 ) ) ;
#32742=CARTESIAN_POINT ( 'NONE',  ( 113.0231681442453180, -10.15424416112533912, -14.75197769757731336 ) ) ;
#32743=CARTESIAN_POINT ( 'NONE',  ( 111.3213681442453264, -7.643976991954077427, -18.09477374809248928 ) ) ;
#32745=CARTESIAN_POINT ( 'NONE',  ( 118.2987481442453088, -7.894159318335828068, -9.358103419637847864 ) ) ;
#32751=CARTESIAN_POINT ( 'NONE',  ( 122.0427081442452817, 0.5811942927096110934, -14.16772938898807510 ) ) ;
#32752=EDGE_LOOP ( 'NONE', ( #26722, #28555, #33646, #36479 ) ) ;
#32754=CARTESIAN_POINT ( 'NONE',  ( 111.4705635773848940, -2.467220198592768199, -17.83387418641523325 ) ) ;
#32756=CARTESIAN_POINT ( 'NONE',  ( 119.2063748109119814, -7.894159318335828068, -9.358103419637847864 ) ) ;
#32759=CARTESIAN_POINT ( 'NONE',  ( 125.1626748109119802, -0.1624402480850797581, -16.17319339645315424 ) ) ;
#32761=CARTESIAN_POINT ( 'NONE',  ( 123.7445081442452874, -7.894159318335828068, -9.358103419637847864 ) ) ;
#32764=CARTESIAN_POINT ( 'NONE',  ( 116.0864081442453113, -0.1624402480850797581, -16.17319339645315424 ) ) ;
#32765=CARTESIAN_POINT ( 'NONE',  ( 121.9859814775786333, -9.565557343593413364, -10.61323700422348004 ) ) ;
#32766=CARTESIAN_POINT ( 'NONE',  ( 117.9016614775786280, -9.988377603198976828, -10.36322818467138340 ) ) ;
#32767=CARTESIAN_POINT ( 'NONE',  ( 117.3343948109119737, -3.383040157471821630, -19.15922257007629170 ) ) ;
#32769=CARTESIAN_POINT ( 'NONE',  ( 125.6732148109119862, -9.859900752359378018, -12.68260735090039759 ) ) ;
#32771=CARTESIAN_POINT ( 'NONE',  ( 121.4187148109119789, -6.344957434206665248, -7.627207830600338134 ) ) ;
#32775=CARTESIAN_POINT ( 'NONE',  ( 112.8529881442453302, -7.894159318335828068, -9.358103419637847864 ) ) ;
#32777=CARTESIAN_POINT ( 'NONE',  ( 138.2184548109119930, -3.657522433324904565, -16.24880879654457289 ) ) ;
#32779=ORIENTED_EDGE ( 'NONE', *, *, #17770, .T. ) ;
#32781=CARTESIAN_POINT ( 'NONE',  ( 125.3328548109119964, -0.8288870151387760510, -10.36305467784173118 ) ) ;
#32784=CARTESIAN_POINT ( 'NONE',  ( 111.7289948109119990, -2.109465145232937378, -8.734689011829464889 ) ) ;
#32788=CARTESIAN_POINT ( 'NONE',  ( 115.1787814775786387, -9.988377603198976828, -10.36322818467138340 ) ) ;
#32790=CARTESIAN_POINT ( 'NONE',  ( 119.4332814775786318, -8.899110576539710493, -16.42337572283490132 ) ) ;
#32791=CARTESIAN_POINT ( 'NONE',  ( 115.3489614775786407, -0.8288870151387760510, -10.36305467784173118 ) ) ;
#32793=CARTESIAN_POINT ( 'NONE',  ( 125.3328548109119964, -0.8288870151387760510, -10.36305467784173118 ) ) ;
#32796=CARTESIAN_POINT ( 'NONE',  ( 123.0070614775786169, 0.9020085738987339008, -11.91225656197089222 ) ) ;
#32800=( BOUNDED_SURFACE ( )  B_SPLINE_SURFACE ( 1, 2, ( 
 ( #22574, #11876, #35797, #29644, #11647, #12327, #18263, #22355, #25337, #39462, #4569, #7995, #18493, #43558, #5016, #22132, #26226, #7775, #21682, #32821, #35570, #32159, #42661, #36025, #4793, #32605, #927, #11432, #44698, #13458, #33726, #30100, #16881, #29872, #12552, #44016, #12778, #2724, #40135, #2496, #26680, #30772, #43787, #26459, #40591, #9350, #16650, #40361, #30545, #23260, #6151, #2045, #26904, #37143, #44466, #40824, #6386, #15969, #36916, #5917, #13231, #19839, #27132, #16425, #2954, #36692, #8900, #30321, #9125, #22798, #37381, #20071, #41056, #23495, #44247, #34179, #9813, #23722, #13005, #5462, #37612, #16196, #20294, #33957, #19382, #33270, #9579, #23029, #5687, #19606, #33490, #2268, #14956, #14283, #21346, #4233, #38887, #18151, #24765, #18601, #24551, #38438, #814, #372, #21571, #3779, #39121, #596, #35458, #34995, #32046, #38656, #42781, #32272, #14506, #25449, #21794, #7656, #39351, #35688, #7425, #4463, #18384, #28202, #1040, #28419, #14733, #42109, #8119, #28645, #7208, #32492, #42551, #21121, #28868, #17703, #11542, #22020, #11313, #10870, #35914, #17927, #1267, #31603, #25223, #35230, #4005, #31826, #42330, #11091, #4680, #7888, #24992, #27980, #41884, #10646, #1936, #29987, #40254, #22241, #1485, #15633, #32713, #42995, #5364, #19723, #15407, #8566, #29311, #43224, #11991, #9020, #12445, #25893, #33381, #22918, #23153, #15862, #43904, #36810, #36137, #39797, #29537, #22466, #11762, #19281, #33609, #15180, #8786, #5132, #37035, #4905, #36360, #19048, #32935, #5578, #18821, #19502, #43453, #26346, #1710, #29758, #12218, #2152, #43670, #26571, #26116, #40021, #22692, #16082, #36589, #12673, #33160, #5804, #25672, #29083, #40485, #9244, #39577, #8340, #44812, #10154, #30890, #37730, #41618, #34516, #37954, #34076, #6948, #24062, #23612, #20639, #13570, #3294, #45031, #41170, #31107, #6728, #13351, #37498, #17217, #13791, #33844, #40942, #23843, #27255, #6500, #44360, #38169, #44137, #12902, #20415, #19955, #9930, #23379, #27480, #20192 ),
 ( #20853, #27703, #34299, #10374, #3072, #6272, #17001, #30441, #2386, #30217, #9698, #24283, #2843, #41399, #2613, #37261, #16314, #16772, #6033, #26798, #30667, #40708, #9467, #16545, #27027, #13121, #44588, #28362, #39070, #14456, #7605, #25172, #99, #3954, #31994, #14231, #38383, #28147, #992, #8064, #11264, #42275, #32219, #38836, #24711, #24940, #17654, #34731, #17431, #42057, #14907, #10815, #11038, #7156, #10596, #3514, #38600, #21067, #35406, #35177, #21519, #544, #4181, #7377, #31324, #28818, #18098, #7839, #756, #28593, #21293, #14012, #42504, #17876, #39296, #41836, #24499, #27927, #34945, #3731, #18326, #31550, #31773, #14679, #21745, #318, #35635, #4411, #42728, #11493, #25398, #22416, #22639, #32666, #2102, #18776, #35856, #39969, #4630, #29037, #29705, #43618, #29261, #21969, #8289, #29937, #36087, #15355, #5310, #40199, #8732, #18551, #19226, #1434, #5525, #42946, #19445, #12392, #39527, #43172, #39745, #15577, #36536, #32443, #1217, #16030, #40430, #36757, #43851, #11941, #33106, #8965, #4858, #33328, #1877, #15804, #25837, #15131, #12623, #29482, #26521, #11711, #8512, #36309, #22191, #26065, #5079, #26291, #43395, #12163, #25622, #18994, #32882, #1656, #22864, #27200, #37897, #5746, #13518, #40886, #6675, #3019, #20137, #20582, #16941, #33788, #30836, #44759, #40654, #27427, #26966, #30612, #23320, #34461, #2791, #19667, #44983, #34023, #33554, #41349, #2332, #10105, #24009, #16718, #37205, #17166, #44311, #13741, #16262, #44529, #26748, #2560, #5978, #9409, #19903, #3240, #6452, #16489, #31055, #27650, #9191, #41118, #23097, #34247, #30165, #30389, #9640, #13066, #36978, #13292, #44082, #12847, #9877, #23562, #37443, #6215, #23787, #37677, #20360, #4125, #31272, #18045, #42001, #7552, #3468, #28311, #31495, #31939, #42223, #7784, #17383, #38332, #7323, #705, #38548, #14625, #35120, #4351, #38117, #41565, #21243, #45, #18271, #38781, #21467, #28543, #24888, #31718, #35578, #42447, #11213, #28092, #936, #25118, #17602, #39014, #35350 ) ),
 .UNSPECIFIED., .F., .F., .F. ) 
 B_SPLINE_SURFACE_WITH_KNOTS ( ( 2, 2 ),
 ( 3, 2, 2, 2, 2, 2, 2, 2, 2, 2, 2, 2, 2, 2, 2, 2, 2, 2, 2, 2, 2, 2, 2, 2, 2, 2, 2, 2, 2, 2, 2, 2, 2, 2, 2, 2, 2, 2, 2, 2, 2, 2, 2, 2, 2, 2, 2, 2, 2, 2, 2, 2, 2, 2, 2, 2, 2, 2, 2, 2, 2, 2, 2, 2, 2, 2, 2, 2, 2, 2, 2, 2, 2, 2, 2, 2, 2, 2, 2, 2, 2, 2, 2, 2, 2, 2, 2, 2, 2, 2, 2, 2, 2, 2, 2, 2, 2, 2, 2, 2, 2, 2, 2, 2, 2, 2, 2, 2, 2, 2, 2, 2, 2, 2, 2, 2, 2, 2, 2, 2, 2, 2, 2, 2, 2, 2, 2, 2, 3 ),
 ( 0.000000000000000000, 1.000000000000000000 ),
 ( 0.000000000000000000, 0.007812500000000000000, 0.01562500000000000000, 0.02343750000000000000, 0.03125000000000000000, 0.03906250000000000000, 0.04687500000000000000, 0.05468750000000000000, 0.06250000000000000000, 0.07031250000000000000, 0.07812500000000000000, 0.08593750000000000000, 0.09375000000000000000, 0.1015625000000000000, 0.1093750000000000000, 0.1171875000000000000, 0.1250000000000000000, 0.1328125000000000000, 0.1406250000000000000, 0.1484375000000000000, 0.1562500000000000000, 0.1640625000000000000, 0.1718750000000000000, 0.1796875000000000000, 0.1875000000000000000, 0.1953125000000000000, 0.2031250000000000000, 0.2109375000000000000, 0.2187500000000000000, 0.2265625000000000000, 0.2343750000000000000, 0.2421875000000000000, 0.2500000000000000000, 0.2578125000000000000, 0.2656250000000000000, 0.2734375000000000000, 0.2812500000000000000, 0.2890625000000000000, 0.2968750000000000000, 0.3046875000000000000, 0.3125000000000000000, 0.3203125000000000000, 0.3281250000000000000, 0.3359375000000000000, 0.3437500000000000000, 0.3515625000000000000, 0.3593750000000000000, 0.3671875000000000000, 0.3750000000000000000, 0.3828125000000000000, 0.3906250000000000000, 0.3984375000000000000, 0.4062500000000000000, 0.4140625000000000000, 0.4218750000000000000, 0.4296875000000000000, 0.4375000000000000000, 0.4453125000000000000, 0.4531250000000000000, 0.4609375000000000000, 0.4687500000000000000, 0.4765625000000000000, 0.4843750000000000000, 0.4921875000000000000, 0.5000000000000000000, 0.5078125000000000000, 0.5156250000000000000, 0.5234375000000000000, 0.5312500000000000000, 0.5390625000000000000, 0.5468750000000000000, 0.5546875000000000000, 0.5625000000000000000, 0.5703125000000000000, 0.5781250000000000000, 0.5859375000000000000, 0.5937500000000000000, 0.6015625000000000000, 0.6093750000000000000, 0.6171875000000000000, 0.6250000000000000000, 0.6328125000000000000, 0.6406250000000000000, 0.6484375000000000000, 0.6562500000000000000, 0.6640625000000000000, 0.6718750000000000000, 0.6796875000000000000, 0.6875000000000000000, 0.6953125000000000000, 0.7031250000000000000, 0.7109375000000000000, 0.7187500000000000000, 0.7265625000000000000, 0.7343750000000000000, 0.7421875000000000000, 0.7500000000000000000, 0.7578125000000000000, 0.7656250000000000000, 0.7734375000000000000, 0.7812500000000000000, 0.7890625000000000000, 0.7968750000000000000, 0.8046875000000000000, 0.8125000000000000000, 0.8203125000000000000, 0.8281250000000000000, 0.8359375000000000000, 0.8437500000000000000, 0.8515625000000000000, 0.8593750000000000000, 0.8671875000000000000, 0.8750000000000000000, 0.8828125000000000000, 0.8906250000000000000, 0.8984375000000000000, 0.9062500000000000000, 0.9140625000000000000, 0.9218750000000000000, 0.9296875000000000000, 0.9375000000000000000, 0.9453125000000000000, 0.9531250000000000000, 0.9609375000000000000, 0.9687500000000000000, 0.9765625000000000000, 0.9843750000000000000, 0.9921875000000000000, 1.000000000000000000 ),
 .UNSPECIFIED. ) 
 GEOMETRIC_REPRESENTATION_ITEM ( )  RATIONAL_B_SPLINE_SURFACE ( (
 ( 1.000000000000000000, 0.9238795325112869605, 1.000000000000000000, 0.9238795325112869605, 1.000000000000000000, 0.9238795325112869605, 1.000000000000000000, 0.9238795325112869605, 1.000000000000000000, 0.9238795325112869605, 1.000000000000000000, 0.9238795325112869605, 1.000000000000000000, 0.9238795325112869605, 1.000000000000000000, 0.9238795325112869605, 1.000000000000000000, 0.9238795325112869605, 1.000000000000000000, 0.9238795325112869605, 1.000000000000000000, 0.9238795325112869605, 1.000000000000000000, 0.9238795325112869605, 1.000000000000000000, 0.9238795325112869605, 1.000000000000000000, 0.9238795325112869605, 1.000000000000000000, 0.9238795325112869605, 1.000000000000000000, 0.9238795325112869605, 1.000000000000000000, 0.9238795325112869605, 1.000000000000000000, 0.9238795325112869605, 1.000000000000000000, 0.9238795325112869605, 1.000000000000000000, 0.9238795325112869605, 1.000000000000000000, 0.9238795325112869605, 1.000000000000000000, 0.9238795325112869605, 1.000000000000000000, 0.9238795325112869605, 1.000000000000000000, 0.9238795325112869605, 1.000000000000000000, 0.9238795325112869605, 1.000000000000000000, 0.9238795325112869605, 1.000000000000000000, 0.9238795325112869605, 1.000000000000000000, 0.9238795325112869605, 1.000000000000000000, 0.9238795325112869605, 1.000000000000000000, 0.9238795325112869605, 1.000000000000000000, 0.9238795325112869605, 1.000000000000000000, 0.9238795325112869605, 1.000000000000000000, 0.9238795325112869605, 1.000000000000000000, 0.9238795325112869605, 1.000000000000000000, 0.9238795325112869605, 1.000000000000000000, 0.9238795325112869605, 1.000000000000000000, 0.9238795325112869605, 1.000000000000000000, 0.9238795325112869605, 1.000000000000000000, 0.9238795325112869605, 1.000000000000000000, 0.9238795325112869605, 1.000000000000000000, 0.9238795325112869605, 1.000000000000000000, 0.9238795325112869605, 1.000000000000000000, 0.9238795325112869605, 1.000000000000000000, 0.9238795325112869605, 1.000000000000000000, 0.9238795325112869605, 1.000000000000000000, 0.9238795325112869605, 1.000000000000000000, 0.9238795325112869605, 1.000000000000000000, 0.9238795325112869605, 1.000000000000000000, 0.9238795325112869605, 1.000000000000000000, 0.9238795325112869605, 1.000000000000000000, 0.9238795325112869605, 1.000000000000000000, 0.9238795325112869605, 1.000000000000000000, 0.9238795325112869605, 1.000000000000000000, 0.9238795325112869605, 1.000000000000000000, 0.9238795325112869605, 1.000000000000000000, 0.9238795325112869605, 1.000000000000000000, 0.9238795325112869605, 1.000000000000000000, 0.9238795325112869605, 1.000000000000000000, 0.9238795325112869605, 1.000000000000000000, 0.9238795325112869605, 1.000000000000000000, 0.9238795325112869605, 1.000000000000000000, 0.9238795325112869605, 1.000000000000000000, 0.9238795325112869605, 1.000000000000000000, 0.9238795325112869605, 1.000000000000000000, 0.9238795325112869605, 1.000000000000000000, 0.9238795325112869605, 1.000000000000000000, 0.9238795325112869605, 1.000000000000000000, 0.9238795325112869605, 1.000000000000000000, 0.9238795325112869605, 1.000000000000000000, 0.9238795325112869605, 1.000000000000000000, 0.9238795325112869605, 1.000000000000000000, 0.9238795325112869605, 1.000000000000000000, 0.9238795325112869605, 1.000000000000000000, 0.9238795325112869605, 1.000000000000000000, 0.9238795325112869605, 1.000000000000000000, 0.9238795325112869605, 1.000000000000000000, 0.9238795325112869605, 1.000000000000000000, 0.9238795325112869605, 1.000000000000000000, 0.9238795325112869605, 1.000000000000000000, 0.9238795325112869605, 1.000000000000000000, 0.9238795325112869605, 1.000000000000000000, 0.9238795325112869605, 1.000000000000000000, 0.9238795325112869605, 1.000000000000000000, 0.9238795325112869605, 1.000000000000000000, 0.9238795325112869605, 1.000000000000000000, 0.9238795325112869605, 1.000000000000000000, 0.9238795325112869605, 1.000000000000000000, 0.9238795325112869605, 1.000000000000000000, 0.9238795325112869605, 1.000000000000000000, 0.9238795325112869605, 1.000000000000000000, 0.9238795325112869605, 1.000000000000000000, 0.9238795325112869605, 1.000000000000000000, 0.9238795325112869605, 1.000000000000000000, 0.9238795325112869605, 1.000000000000000000, 0.9238795325112869605, 1.000000000000000000, 0.9238795325112869605, 1.000000000000000000, 0.9238795325112869605, 1.000000000000000000, 0.9238795325112869605, 1.000000000000000000, 0.9238795325112869605, 1.000000000000000000, 0.9238795325112869605, 1.000000000000000000, 0.9238795325112869605, 1.000000000000000000, 0.9238795325112869605, 1.000000000000000000, 0.9238795325112869605, 1.000000000000000000, 0.9238795325112869605, 1.000000000000000000, 0.9238795325112869605, 1.000000000000000000, 0.9238795325112869605, 1.000000000000000000, 0.9238795325112869605, 1.000000000000000000, 0.9238795325112869605, 1.000000000000000000, 0.9238795325112869605, 1.000000000000000000, 0.9238795325112869605, 1.000000000000000000, 0.9238795325112869605, 1.000000000000000000, 0.9238795325112869605, 1.000000000000000000, 0.9238795325112869605, 1.000000000000000000, 0.9238795325112869605, 1.000000000000000000, 0.9238795325112869605, 1.000000000000000000, 0.9238795325112869605, 1.000000000000000000, 0.9238795325112869605, 1.000000000000000000, 0.9238795325112869605, 1.000000000000000000, 0.9238795325112869605, 1.000000000000000000, 0.9238795325112869605, 1.000000000000000000, 0.9238795325112869605, 1.000000000000000000, 0.9238795325112869605, 1.000000000000000000, 0.9238795325112869605, 1.000000000000000000, 0.9238795325112869605, 1.000000000000000000, 0.9238795325112869605, 1.000000000000000000, 0.9238795325112869605, 1.000000000000000000, 0.9238795325112869605, 1.000000000000000000, 0.9238795325112869605, 1.000000000000000000),
 ( 1.000000000000000000, 0.9238795325112869605, 1.000000000000000000, 0.9238795325112869605, 1.000000000000000000, 0.9238795325112869605, 1.000000000000000000, 0.9238795325112869605, 1.000000000000000000, 0.9238795325112869605, 1.000000000000000000, 0.9238795325112869605, 1.000000000000000000, 0.9238795325112869605, 1.000000000000000000, 0.9238795325112869605, 1.000000000000000000, 0.9238795325112869605, 1.000000000000000000, 0.9238795325112869605, 1.000000000000000000, 0.9238795325112869605, 1.000000000000000000, 0.9238795325112869605, 1.000000000000000000, 0.9238795325112869605, 1.000000000000000000, 0.9238795325112869605, 1.000000000000000000, 0.9238795325112869605, 1.000000000000000000, 0.9238795325112869605, 1.000000000000000000, 0.9238795325112869605, 1.000000000000000000, 0.9238795325112869605, 1.000000000000000000, 0.9238795325112869605, 1.000000000000000000, 0.9238795325112869605, 1.000000000000000000, 0.9238795325112869605, 1.000000000000000000, 0.9238795325112869605, 1.000000000000000000, 0.9238795325112869605, 1.000000000000000000, 0.9238795325112869605, 1.000000000000000000, 0.9238795325112869605, 1.000000000000000000, 0.9238795325112869605, 1.000000000000000000, 0.9238795325112869605, 1.000000000000000000, 0.9238795325112869605, 1.000000000000000000, 0.9238795325112869605, 1.000000000000000000, 0.9238795325112869605, 1.000000000000000000, 0.9238795325112869605, 1.000000000000000000, 0.9238795325112869605, 1.000000000000000000, 0.9238795325112869605, 1.000000000000000000, 0.9238795325112869605, 1.000000000000000000, 0.9238795325112869605, 1.000000000000000000, 0.9238795325112869605, 1.000000000000000000, 0.9238795325112869605, 1.000000000000000000, 0.9238795325112869605, 1.000000000000000000, 0.9238795325112869605, 1.000000000000000000, 0.9238795325112869605, 1.000000000000000000, 0.9238795325112869605, 1.000000000000000000, 0.9238795325112869605, 1.000000000000000000, 0.9238795325112869605, 1.000000000000000000, 0.9238795325112869605, 1.000000000000000000, 0.9238795325112869605, 1.000000000000000000, 0.9238795325112869605, 1.000000000000000000, 0.9238795325112869605, 1.000000000000000000, 0.9238795325112869605, 1.000000000000000000, 0.9238795325112869605, 1.000000000000000000, 0.9238795325112869605, 1.000000000000000000, 0.9238795325112869605, 1.000000000000000000, 0.9238795325112869605, 1.000000000000000000, 0.9238795325112869605, 1.000000000000000000, 0.9238795325112869605, 1.000000000000000000, 0.9238795325112869605, 1.000000000000000000, 0.9238795325112869605, 1.000000000000000000, 0.9238795325112869605, 1.000000000000000000, 0.9238795325112869605, 1.000000000000000000, 0.9238795325112869605, 1.000000000000000000, 0.9238795325112869605, 1.000000000000000000, 0.9238795325112869605, 1.000000000000000000, 0.9238795325112869605, 1.000000000000000000, 0.9238795325112869605, 1.000000000000000000, 0.9238795325112869605, 1.000000000000000000, 0.9238795325112869605, 1.000000000000000000, 0.9238795325112869605, 1.000000000000000000, 0.9238795325112869605, 1.000000000000000000, 0.9238795325112869605, 1.000000000000000000, 0.9238795325112869605, 1.000000000000000000, 0.9238795325112869605, 1.000000000000000000, 0.9238795325112869605, 1.000000000000000000, 0.9238795325112869605, 1.000000000000000000, 0.9238795325112869605, 1.000000000000000000, 0.9238795325112869605, 1.000000000000000000, 0.9238795325112869605, 1.000000000000000000, 0.9238795325112869605, 1.000000000000000000, 0.9238795325112869605, 1.000000000000000000, 0.9238795325112869605, 1.000000000000000000, 0.9238795325112869605, 1.000000000000000000, 0.9238795325112869605, 1.000000000000000000, 0.9238795325112869605, 1.000000000000000000, 0.9238795325112869605, 1.000000000000000000, 0.9238795325112869605, 1.000000000000000000, 0.9238795325112869605, 1.000000000000000000, 0.9238795325112869605, 1.000000000000000000, 0.9238795325112869605, 1.000000000000000000, 0.9238795325112869605, 1.000000000000000000, 0.9238795325112869605, 1.000000000000000000, 0.9238795325112869605, 1.000000000000000000, 0.9238795325112869605, 1.000000000000000000, 0.9238795325112869605, 1.000000000000000000, 0.9238795325112869605, 1.000000000000000000, 0.9238795325112869605, 1.000000000000000000, 0.9238795325112869605, 1.000000000000000000, 0.9238795325112869605, 1.000000000000000000, 0.9238795325112869605, 1.000000000000000000, 0.9238795325112869605, 1.000000000000000000, 0.9238795325112869605, 1.000000000000000000, 0.9238795325112869605, 1.000000000000000000, 0.9238795325112869605, 1.000000000000000000, 0.9238795325112869605, 1.000000000000000000, 0.9238795325112869605, 1.000000000000000000, 0.9238795325112869605, 1.000000000000000000, 0.9238795325112869605, 1.000000000000000000, 0.9238795325112869605, 1.000000000000000000, 0.9238795325112869605, 1.000000000000000000, 0.9238795325112869605, 1.000000000000000000, 0.9238795325112869605, 1.000000000000000000, 0.9238795325112869605, 1.000000000000000000, 0.9238795325112869605, 1.000000000000000000, 0.9238795325112869605, 1.000000000000000000, 0.9238795325112869605, 1.000000000000000000, 0.9238795325112869605, 1.000000000000000000, 0.9238795325112869605, 1.000000000000000000, 0.9238795325112869605, 1.000000000000000000, 0.9238795325112869605, 1.000000000000000000, 0.9238795325112869605, 1.000000000000000000, 0.9238795325112869605, 1.000000000000000000, 0.9238795325112869605, 1.000000000000000000, 0.9238795325112869605, 1.000000000000000000, 0.9238795325112869605, 1.000000000000000000, 0.9238795325112869605, 1.000000000000000000, 0.9238795325112869605, 1.000000000000000000, 0.9238795325112869605, 1.000000000000000000, 0.9238795325112869605, 1.000000000000000000, 0.9238795325112869605, 1.000000000000000000, 0.9238795325112869605, 1.000000000000000000, 0.9238795325112869605, 1.000000000000000000) ) ) 
 REPRESENTATION_ITEM ( '' )  SURFACE ( )  );
#32801=CARTESIAN_POINT ( 'NONE',  ( 112.6260814775786514, -9.261995988541697145, -16.69588392320189030 ) ) ;
#32804=CARTESIAN_POINT ( 'NONE',  ( 126.1270281442452870, -10.30919188438810075, -12.61870101168855918 ) ) ;
#32806=CARTESIAN_POINT ( 'NONE',  ( 125.2761281442453054, 0.4262465694468514643, -12.03445270309931736 ) ) ;
#32808=CARTESIAN_POINT ( 'NONE',  ( 118.6958348109119754, -6.344957434206665248, -7.627207830600338134 ) ) ;
#32813=CARTESIAN_POINT ( 'NONE',  ( 111.4321701211256652, -2.490435581280318278, -17.80295943339125486 ) ) ;
#32814=CARTESIAN_POINT ( 'NONE',  ( 112.5126281442453120, 0.1319031606808879209, -14.10382304977623669 ) ) ;
#32817=CARTESIAN_POINT ( 'NONE',  ( 113.6471614775786492, -4.153390946401321671, -8.397313243818183892 ) ) ;
#32818=CARTESIAN_POINT ( 'NONE',  ( 125.7299414775786346, -10.15424416112533912, -14.75197769757731336 ) ) ;
#32820=CARTESIAN_POINT ( 'NONE',  ( 125.2194014775786286, 0.1319031606808879209, -14.10382304977623669 ) ) ;
#32821=CARTESIAN_POINT ( 'NONE',  ( 113.2500748109119968, -3.505236298600246325, -18.68346056562440793 ) ) ;
#32822=CARTESIAN_POINT ( 'NONE',  ( 119.0929214775786278, -5.638512984488999180, -18.83840828888717311 ) ) ;
#32823=CARTESIAN_POINT ( 'NONE',  ( 121.5888948109119809, -10.30919188438810075, -12.61870101168855918 ) ) ;
#32831=CARTESIAN_POINT ( 'NONE',  ( 126.8396850857652396, -9.909566493429444733, -11.73595350948055582 ) ) ;
#32832=CARTESIAN_POINT ( 'NONE',  ( 116.0864081442453113, -9.988377603198976828, -10.36322818467138340 ) ) ;
#32838=CARTESIAN_POINT ( 'NONE',  ( 112.7395348109119766, -5.638512984488999180, -18.83840828888717311 ) ) ;
#32839=CARTESIAN_POINT ( 'NONE',  ( 121.1350814775786233, 0.5811942927096110934, -14.16772938898807510 ) ) ;
#32843=ORIENTED_EDGE ( 'NONE', *, *, #2498, .T. ) ;
#32844=CARTESIAN_POINT ( 'NONE',  ( 121.1918081442452859, -10.15424416112535155, -14.75197769757726185 ) ) ;
#32845=CARTESIAN_POINT ( 'NONE',  ( 118.4689281442453392, -10.15424416112533912, -14.75197769757731336 ) ) ;
#32846=CARTESIAN_POINT ( 'NONE',  ( 117.5613014775786525, 0.9020085738987339008, -11.91225656197089222 ) ) ;
#32847=CARTESIAN_POINT ( 'NONE',  ( 112.2857214775786474, -4.089484607189486809, -7.948022111789456723 ) ) ;
#32849=CARTESIAN_POINT ( 'NONE',  ( 125.0492214775786266, -3.505236298600246325, -18.68346056562440793 ) ) ;
#32850=CARTESIAN_POINT ( 'NONE',  ( 114.4980614775786734, -2.084020599724406786, -8.691656652584148546 ) ) ;
#32854=CARTESIAN_POINT ( 'NONE',  ( 117.3911214775786505, -7.894159318335828068, -9.358103419637847864 ) ) ;
#32858=CARTESIAN_POINT ( 'NONE',  ( 116.3133148109119759, -7.893985811506177619, -18.51759400769804742 ) ) ;
#32860=CARTESIAN_POINT ( 'NONE',  ( 113.3068014775786594, -1.833838273342658809, -17.42832698103878286 ) ) ;
#32863=CARTESIAN_POINT ( 'NONE',  ( 122.0427081442452817, -9.859900752359378018, -12.68260735090039759 ) ) ;
#32865=CARTESIAN_POINT ( 'NONE',  ( 117.0507614775786465, 0.1319031606808879209, -14.10382304977623669 ) ) ;
#32871=CARTESIAN_POINT ( 'NONE',  ( 117.6747548109119919, -1.834011780172310813, -8.268836392978581529 ) ) ;
#32872=CARTESIAN_POINT ( 'NONE',  ( 115.9162281442453235, -4.089484607189486809, -7.948022111789456723 ) ) ;
#32873=CARTESIAN_POINT ( 'NONE',  ( 116.9373081442452929, -1.833838273342659253, -17.42832698103878286 ) ) ;
#32874=CARTESIAN_POINT ( 'NONE',  ( 121.7590748109119687, -2.084020599724406786, -8.691656652584148546 ) ) ;
#32877=CARTESIAN_POINT ( 'NONE',  ( 120.7947214775786193, -0.8288870151387760510, -10.36305467784173118 ) ) ;
#32878=CARTESIAN_POINT ( 'NONE',  ( 125.7299414775786346, -10.15424416112533912, -14.75197769757731336 ) ) ;
#32880=CARTESIAN_POINT ( 'NONE',  ( 135.3184548109119874, 0.7167481258041168424, -11.18974888642104659 ) ) ;
#32882=CARTESIAN_POINT ( 'NONE',  ( 120.3409081442453044, -0.4660016031367893996, -10.09054647747474043 ) ) ;
#32884=CARTESIAN_POINT ( 'NONE',  ( 121.4754414775786131, -8.166667518702819706, -8.995218007635861213 ) ) ;
#32887=CARTESIAN_POINT ( 'NONE',  ( 116.0296814775786345, -8.166667518702817929, -8.995218007635861213 ) ) ;
#32888=CARTESIAN_POINT ( 'NONE',  ( 119.0361948109119652, -7.893985811506177619, -18.51759400769804742 ) ) ;
#32893=CARTESIAN_POINT ( 'NONE',  ( 119.8303681442453126, 0.4262465694468514643, -12.03445270309931736 ) ) ;
#32896=CARTESIAN_POINT ( 'NONE',  ( 115.1787814775786387, -0.1624402480850797581, -16.17319339645315424 ) ) ;
#32899=CARTESIAN_POINT ( 'NONE',  ( 112.9664414775786412, -9.859900752359374465, -12.68260735090039404 ) ) ;
#32900=CARTESIAN_POINT ( 'NONE',  ( 119.8303681442453126, -10.63000616557722466, -14.87417383870573495 ) ) ;
#32903=CARTESIAN_POINT ( 'NONE',  ( 119.2631014775786298, -9.565557343593413364, -10.61323700422348004 ) ) ;
#32905=CARTESIAN_POINT ( 'NONE',  ( 113.8173414775786512, 0.2603800115204892296, -16.42320221600525088 ) ) ;
#32906=CARTESIAN_POINT ( 'NONE',  ( 122.1561614775786353, -0.4660016031367893996, -10.09054647747474043 ) ) ;
#32907=CARTESIAN_POINT ( 'NONE',  ( 120.5110881442453206, -3.505236298600246325, -18.68346056562440793 ) ) ;
#32908=ORIENTED_EDGE ( 'NONE', *, *, #26446, .T. ) ;
#32909=CARTESIAN_POINT ( 'NONE',  ( 125.6164881442453094, -9.565557343593413364, -10.61323700422348004 ) ) ;
#32910=CARTESIAN_POINT ( 'NONE',  ( 118.8660148109119774, -10.30919188438810075, -12.61870101168855918 ) ) ;
#32911=CARTESIAN_POINT ( 'NONE',  ( 113.0231681442453180, -10.15424416112533912, -14.75197769757731336 ) ) ;
#32912=CARTESIAN_POINT ( 'NONE',  ( 122.4397948109119767, -9.988377603198976828, -10.36322818467138340 ) ) ;
#32917=CARTESIAN_POINT ( 'NONE',  ( 118.9672361498677162, -2.324775150319212891, -18.02356106541841640 ) ) ;
#32921=CARTESIAN_POINT ( 'NONE',  ( 137.4282737236217145, -9.806850323706933992, -12.17485108655606929 ) ) ;
#32922=CARTESIAN_POINT ( 'NONE',  ( 119.2631014775786298, -9.565557343593413364, -10.61323700422348004 ) ) ;
#32923=CARTESIAN_POINT ( 'NONE',  ( 123.8012348109119642, 0.2603800115204892296, -16.42320221600525088 ) ) ;
#32928=CARTESIAN_POINT ( 'NONE',  ( 115.4056881442453459, -2.084020599724406786, -8.691656652584148546 ) ) ;
#32932=CARTESIAN_POINT ( 'NONE',  ( 123.7637130757767352, -0.9924539043446216624, -17.29976612834909133 ) ) ;
#32934=CARTESIAN_POINT ( 'NONE',  ( 122.9503348109119827, 0.5811942927096110934, -14.16772938898807510 ) ) ;
#32935=CARTESIAN_POINT ( 'NONE',  ( 123.1772414775786189, -5.574606645277164318, -18.38911715685844683 ) ) ;
#32939=CARTESIAN_POINT ( 'NONE',  ( 124.0281414775786146, -7.643976991954077427, -18.09477374809248928 ) ) ;
#32940=CARTESIAN_POINT ( 'NONE',  ( 123.4041481442452834, 0.1319031606808879209, -14.10382304977623669 ) ) ;
#32941=CARTESIAN_POINT ( 'NONE',  ( 116.9940348109119839, -0.1624402480850797581, -16.17319339645315424 ) ) ;
#32946=CARTESIAN_POINT ( 'NONE',  ( 151.2860562277021472, -4.863998795839242995, -13.39321520033831447 ) ) ;
#32950=CARTESIAN_POINT ( 'NONE',  ( 120.5110881442453206, -6.344957434206665248, -7.627207830600338134 ) ) ;
#32951=CARTESIAN_POINT ( 'NONE',  ( 117.5613014775786525, 0.9020085738987339008, -11.91225656197089222 ) ) ;
#32953=CARTESIAN_POINT ( 'NONE',  ( 117.6180281442453150, -0.4660016031367893996, -10.09054647747474043 ) ) ;
#32958=CARTESIAN_POINT ( 'NONE',  ( 122.0427081442452817, 0.5811942927096110934, -14.16772938898807510 ) ) ;
#32959=VECTOR ( 'NONE', #11272, 1000.000000000000000 ) ;
#32960=CARTESIAN_POINT ( 'NONE',  ( 120.6812681442452941, -10.30919188438810075, -12.61870101168855918 ) ) ;
#32961=CARTESIAN_POINT ( 'NONE',  ( 123.8579614775786126, -9.859900752359378018, -12.68260735090039759 ) ) ;
#32963=CARTESIAN_POINT ( 'NONE',  ( 113.8740681442453138, -9.859900752359374465, -12.68260735090039404 ) ) ;
#32964=CARTESIAN_POINT ( 'NONE',  ( 111.8886348109120092, -6.222761293078241884, -8.102969835052219238 ) ) ;
#32968=CARTESIAN_POINT ( 'NONE',  ( 120.1140014775786398, -7.894159318335828068, -9.358103419637847864 ) ) ;
#32972=CARTESIAN_POINT ( 'NONE',  ( 122.7801548109119665, -3.383040157471821630, -19.15922257007629170 ) ) ;
#32976=CARTESIAN_POINT ( 'NONE',  ( 118.4122014775786340, -9.859900752359374465, -12.68260735090039404 ) ) ;
#32978=CARTESIAN_POINT ( 'NONE',  ( 124.1773369107181821, -2.467220198592779301, -17.83387418641524391 ) ) ;
#32979=CARTESIAN_POINT ( 'NONE',  ( 124.5954081442453116, -6.222761293078241884, -8.102969835052219238 ) ) ;
#32980=CARTESIAN_POINT ( 'NONE',  ( 111.9645664091100912, -0.9924539043446216624, -17.29976612834909133 ) ) ;
#32982=CARTESIAN_POINT ( 'NONE',  ( 125.4463081442452932, -4.153390946401325223, -8.397313243818185668 ) ) ;
#32985=CARTESIAN_POINT ( 'NONE',  ( 121.1918081442452859, 0.9020085738987339008, -11.91225656197089222 ) ) ;
#32986=CARTESIAN_POINT ( 'NONE',  ( 119.2063748109119814, -7.894159318335828068, -9.358103419637847864 ) ) ;
#32987=CARTESIAN_POINT ( 'NONE',  ( 121.7023481442452777, -0.8288870151387760510, -10.36305467784173118 ) ) ;
#32988=ORIENTED_EDGE ( 'NONE', *, *, #42307, .T. ) ;
#32989=CARTESIAN_POINT ( 'NONE',  ( 123.8012348109119642, 0.2603800115204892296, -16.42320221600525088 ) ) ;
#32990=CARTESIAN_POINT ( 'NONE',  ( 117.1642148109119859, -9.261995988541697145, -16.69588392320189030 ) ) ;
#32992=DIRECTION ( 'NONE',  ( 0.000000000000000000, 0.6004852223388321697, -0.7996358532186279566 ) ) ;
#32993=CARTESIAN_POINT ( 'NONE',  ( 123.2906948109119867, -1.833838273342659697, -17.42832698103878286 ) ) ;
#32994=CARTESIAN_POINT ( 'NONE',  ( 119.9438214775786378, -7.893985811506177619, -18.51759400769804742 ) ) ;
#32999=CARTESIAN_POINT ( 'NONE',  ( 114.7249681442453237, -9.565557343593413364, -10.61323700422348004 ) ) ;
#33000=CARTESIAN_POINT ( 'NONE',  ( 137.5143514225471222, -2.492992885558165561, -17.79955400039792934 ) ) ;
#33001=CARTESIAN_POINT ( 'NONE',  ( 124.8790414775786246, -0.4660016031367893996, -10.09054647747474043 ) ) ;
#33003=CARTESIAN_POINT ( 'NONE',  ( 123.9714148109119805, -8.899110576539710493, -16.42337572283490132 ) ) ;
#33009=CARTESIAN_POINT ( 'NONE',  ( 115.7460481442453357, 0.9020085738987339008, -11.91225656197089222 ) ) ;
#33010=CARTESIAN_POINT ( 'NONE',  ( 113.1366214775786432, -1.834011780172310591, -8.268836392978581529 ) ) ;
#33012=CARTESIAN_POINT ( 'NONE',  ( 123.7445081442452874, -7.894159318335828068, -9.358103419637847864 ) ) ;
#33013=CARTESIAN_POINT ( 'NONE',  ( 114.2711548109119803, -0.1624402480850797581, -16.17319339645315424 ) ) ;
#33015=CARTESIAN_POINT ( 'NONE',  ( 123.8579614775786126, 0.5811942927096084288, -14.16772938898809642 ) ) ;
#33016=CARTESIAN_POINT ( 'NONE',  ( 113.6471614775786492, -5.638512984488999180, -18.83840828888717311 ) ) ;
#33019=CARTESIAN_POINT ( 'NONE',  ( 124.8790414775786246, -0.4660016031367893996, -10.09054647747474043 ) ) ;
#33022=CARTESIAN_POINT ( 'NONE',  ( 114.0442481442453300, -1.834011780172310813, -8.268836392978581529 ) ) ;
#33023=CARTESIAN_POINT ( 'NONE',  ( 112.2857214775786474, -5.574606645277164318, -18.38911715685844683 ) ) ;
#33025=CARTESIAN_POINT ( 'NONE',  ( 112.8529881442453302, -1.561330072975668060, -17.79121239304076596 ) ) ;
#33028=CARTESIAN_POINT ( 'NONE',  ( 118.1285681442453068, -7.893985811506177619, -18.51759400769804742 ) ) ;
#33032=CARTESIAN_POINT ( 'NONE',  ( 123.6431847287616534, -4.480430082091682920, -15.15308252923503751 ) ) ;
#33033=CARTESIAN_POINT ( 'NONE',  ( 114.8384214775786489, -10.15424416112533912, -14.75197769757731336 ) ) ;
#33036=CARTESIAN_POINT ( 'NONE',  ( 111.7751814775786556, -2.084020599724406786, -8.691656652584148546 ) ) ;
#33037=CARTESIAN_POINT ( 'NONE',  ( 112.6260814775786514, -9.261995988541697145, -16.69588392320189030 ) ) ;
#33039=CARTESIAN_POINT ( 'NONE',  ( 122.8936081442453059, -9.565557343593413364, -10.61323700422348004 ) ) ;
#33041=CARTESIAN_POINT ( 'NONE',  ( 124.1415948109119540, -6.344957434206665248, -7.627207830600338134 ) ) ;
#33043=CARTESIAN_POINT ( 'NONE',  ( 121.3052614775786111, -1.834011780172310813, -8.268836392978581529 ) ) ;
#33045=CARTESIAN_POINT ( 'NONE',  ( 127.0553483106877621, -8.467588782543378656, -17.43966488234757506 ) ) ;
#33049=CARTESIAN_POINT ( 'NONE',  ( 127.0066334553000615, -9.957176252831715146, -11.61677030087517792 ) ) ;
#33050=CARTESIAN_POINT ( 'NONE',  ( 114.4980614775786592, -7.893985811506177619, -18.51759400769804742 ) ) ;
#33054=CARTESIAN_POINT ( 'NONE',  ( 115.4056881442453459, -2.084020599724406786, -8.691656652584148546 ) ) ;
#33056=CARTESIAN_POINT ( 'NONE',  ( 112.8337832127138682, -2.191907684172563986, -18.20049396185734025 ) ) ;
#33057=CARTESIAN_POINT ( 'NONE',  ( 120.3976348109119812, -1.834011780172310813, -8.268836392978581529 ) ) ;
#33061=CARTESIAN_POINT ( 'NONE',  ( 120.7379948109119709, 0.4262465694468476896, -12.03445270309931381 ) ) ;
#33062=CARTESIAN_POINT ( 'NONE',  ( 117.7314814775786260, -5.574606645277164318, -18.38911715685844683 ) ) ;
#33063=CARTESIAN_POINT ( 'NONE',  ( 115.3489614775786407, -9.261995988541697145, -16.69588392320189030 ) ) ;
#33065=CARTESIAN_POINT ( 'NONE',  ( 115.7460481442453357, 0.9020085738987339008, -11.91225656197089222 ) ) ;
#33066=FACE_OUTER_BOUND ( 'NONE', #26827, .T. ) ;
#33068=CARTESIAN_POINT ( 'NONE',  ( 122.8936081442453059, -9.565557343593413364, -10.61323700422348004 ) ) ;
#33069=CARTESIAN_POINT ( 'NONE',  ( 117.6747548109119919, -7.643976991954077427, -18.09477374809248928 ) ) ;
#33070=VERTEX_POINT ( 'NONE', #5617 ) ;
#33073=CARTESIAN_POINT ( 'NONE',  ( 113.8740681442453138, 0.5811942927096154232, -14.16772938898807155 ) ) ;
#33074=CARTESIAN_POINT ( 'NONE',  ( 116.1431348109119881, 0.1319031606808879209, -14.10382304977623669 ) ) ;
#33077=CARTESIAN_POINT ( 'NONE',  ( 114.5547881442453217, -5.638512984488999180, -18.83840828888717311 ) ) ;
#33080=CARTESIAN_POINT ( 'NONE',  ( 114.4980614775786734, -2.084020599724406786, -8.691656652584148546 ) ) ;
#33084=CARTESIAN_POINT ( 'NONE',  ( 121.2485348109119769, -8.899110576539710493, -16.42337572283490132 ) ) ;
#33085=CARTESIAN_POINT ( 'NONE',  ( 121.0783548109119749, -9.565557343593413364, -10.61323700422348004 ) ) ;
#33093=CARTESIAN_POINT ( 'NONE',  ( 116.5402214775786405, 0.2603800115204892296, -16.42320221600525088 ) ) ;
#33094=CARTESIAN_POINT ( 'NONE',  ( 116.1998614775786507, -10.63000616557722466, -14.87417383870573495 ) ) ;
#33095=CARTESIAN_POINT ( 'NONE',  ( 117.5045748109119756, -9.859900752359374465, -12.68260735090039404 ) ) ;
#33096=CARTESIAN_POINT ( 'NONE',  ( 121.5321681442453183, -0.1624402480850797581, -16.17319339645315424 ) ) ;
#33099=CARTESIAN_POINT ( 'NONE',  ( 120.5678148109119832, -1.833838273342659253, -17.42832698103878286 ) ) ;
#33104=CARTESIAN_POINT ( 'NONE',  ( 113.8531398611596046, -1.036737761566196570, -17.24079555149560505 ) ) ;
#33106=CARTESIAN_POINT ( 'NONE',  ( 119.0929214775786278, -5.638512984488999180, -18.83840828888717311 ) ) ;
#33107=ORIENTED_EDGE ( 'NONE', *, *, #11905, .F. ) ;
#33109=CARTESIAN_POINT ( 'NONE',  ( 122.4397948109119767, -9.988377603198976828, -10.36322818467138340 ) ) ;
#33112=CARTESIAN_POINT ( 'NONE',  ( 119.7169148109119874, -9.988377603198976828, -10.36322818467138340 ) ) ;
#33113=ADVANCED_FACE ( 'NONE', ( #20453 ), #9692, .T. ) ;
#33115=CARTESIAN_POINT ( 'NONE',  ( 118.2987481442453088, -1.561330072975668504, -17.79121239304076951 ) ) ;
#33121=CARTESIAN_POINT ( 'NONE',  ( 121.2485348109119769, -8.899110576539710493, -16.42337572283490132 ) ) ;
#33124=CARTESIAN_POINT ( 'NONE',  ( 117.0507614775786465, 0.1319031606808879209, -14.10382304977623669 ) ) ;
#33127=CARTESIAN_POINT ( 'NONE',  ( 112.0020881442453344, -9.565557343593413364, -10.61323700422348004 ) ) ;
#33128=CARTESIAN_POINT ( 'NONE',  ( 124.0848681442452772, -4.089484607189486809, -7.948022111789456723 ) ) ;
#33129=ORIENTED_EDGE ( 'NONE', *, *, #29317, .T. ) ;
#33130=CARTESIAN_POINT ( 'NONE',  ( 117.2776681442452968, -4.153390946401325223, -8.397313243818185668 ) ) ;
#33131=CARTESIAN_POINT ( 'NONE',  ( 113.8740681442453138, 0.5811942927096154232, -14.16772938898807155 ) ) ;
#33132=CARTESIAN_POINT ( 'NONE',  ( 122.2696148109119889, -4.089484607189486809, -7.948022111789456723 ) ) ;
#33133=CARTESIAN_POINT ( 'NONE',  ( 122.0427081442452817, -9.859900752359378018, -12.68260735090039759 ) ) ;
#33135=CARTESIAN_POINT ( 'NONE',  ( 124.6521348109119884, -7.894159318335828068, -9.358103419637847864 ) ) ;
#33137=CARTESIAN_POINT ( 'NONE',  ( 123.8012348109119642, 0.2603800115204892296, -16.42320221600525088 ) ) ;
#33139=CARTESIAN_POINT ( 'NONE',  ( 125.7299414775786346, 0.9020085738987339008, -11.91225656197089222 ) ) ;
#33140=CARTESIAN_POINT ( 'NONE',  ( 117.4502108535611313, -2.239543233855014748, -18.13706010537466895 ) ) ;
#33142=FACE_OUTER_BOUND ( 'NONE', #10903, .T. ) ;
#33143=CARTESIAN_POINT ( 'NONE',  ( 137.9312451099349914, -1.677599621188868406, -16.38739216894681050 ) ) ;
#33146=CARTESIAN_POINT ( 'NONE',  ( 123.2184548109119788, -4.863998795839242995, -13.39321520033831447 ) ) ;
#33147=CARTESIAN_POINT ( 'NONE',  ( 120.1707281442453166, -9.565557343593413364, -10.61323700422348004 ) ) ;
#33148=CARTESIAN_POINT ( 'NONE',  ( 125.5030348109119558, -3.383040157471821630, -19.15922257007629170 ) ) ;
#33153=CARTESIAN_POINT ( 'NONE',  ( 115.5191414775786569, -6.222761293078241884, -8.102969835052219238 ) ) ;
#33154=CARTESIAN_POINT ( 'NONE',  ( 113.5947781477680110, -2.280480477428486363, -18.08254604495228435 ) ) ;
#33158=CARTESIAN_POINT ( 'NONE',  ( 121.1918081442452859, 0.9020085738987339008, -11.91225656197089222 ) ) ;
#33160=CARTESIAN_POINT ( 'NONE',  ( 124.1983214775786166, -1.833838273342659697, -17.42832698103878286 ) ) ;
#33161=ORIENTED_EDGE ( 'NONE', *, *, #767, .F. ) ;
#33163=CARTESIAN_POINT ( 'NONE',  ( 126.2275303246284608, 0.07306257752206567202, -14.21277131990163767 ) ) ;
#33166=CARTESIAN_POINT ( 'NONE',  ( 120.4543614775786295, -5.574606645277164318, -18.38911715685844683 ) ) ;
#33167=CARTESIAN_POINT ( 'NONE',  ( 120.7379948109119709, 0.4262465694468514643, -12.03445270309931736 ) ) ;
#33171=EDGE_CURVE ( 'NONE', #29815, #12393, #34113, .T. ) ;
#33175=CARTESIAN_POINT ( 'NONE',  ( 119.7169148109119874, -9.988377603198976828, -10.36322818467138340 ) ) ;
#33176=CARTESIAN_POINT ( 'NONE',  ( 123.8012348109119642, 0.2603800115204892296, -16.42320221600525088 ) ) ;
#33179=CARTESIAN_POINT ( 'NONE',  ( 115.0653281442453277, -6.344957434206662583, -7.627207830600332805 ) ) ;
#33184=CARTESIAN_POINT ( 'NONE',  ( 124.4819548109119722, -7.893985811506177619, -18.51759400769804742 ) ) ;
#33185=CARTESIAN_POINT ( 'NONE',  ( 118.9227414775786400, -10.63000616557722466, -14.87417383870573495 ) ) ;
#33187=CARTESIAN_POINT ( 'NONE',  ( 126.6942948109119840, -8.899110576539710493, -16.42337572283490132 ) ) ;
#33190=CARTESIAN_POINT ( 'NONE',  ( 112.2857214775786474, -5.574606645277164318, -18.38911715685844683 ) ) ;
#33191=CARTESIAN_POINT ( 'NONE',  ( 125.6732148109119862, 0.5811942927096110934, -14.16772938898807510 ) ) ;
#33193=CARTESIAN_POINT ( 'NONE',  ( 118.8660148109119774, 0.1319031606808879209, -14.10382304977623669 ) ) ;
#33200=CARTESIAN_POINT ( 'NONE',  ( 121.3052614775786111, -1.834011780172310813, -8.268836392978581529 ) ) ;
#33205=CARTESIAN_POINT ( 'NONE',  ( 117.7882081442453170, -3.505236298600246325, -18.68346056562440793 ) ) ;
#33208=CARTESIAN_POINT ( 'NONE',  ( 124.4819548109119722, -2.084020599724406786, -8.691656652584148546 ) ) ;
#33214=CARTESIAN_POINT ( 'NONE',  ( 124.3685014775786328, -10.63000616557722466, -14.87417383870573495 ) ) ;
#33215=CARTESIAN_POINT ( 'NONE',  ( 116.4834948109119779, -7.894159318335828068, -9.358103419637847864 ) ) ;
#33216=CARTESIAN_POINT ( 'NONE',  ( 123.6877814775786533, -6.222761293078241884, -8.102969835052219238 ) ) ;
#33218=CARTESIAN_POINT ( 'NONE',  ( 122.1561614775786353, -0.4660016031367893996, -10.09054647747474043 ) ) ;
#33219=CARTESIAN_POINT ( 'NONE',  ( 114.8384214775786489, 0.9020085738987339008, -11.91225656197089222 ) ) ;
#33221=CYLINDRICAL_SURFACE ( 'NONE', #27768, 1.999999999999998890 ) ;
#33222=CARTESIAN_POINT ( 'NONE',  ( 123.6877814775786533, -6.222761293078241884, -8.102969835052219238 ) ) ;
#33223=CARTESIAN_POINT ( 'NONE',  ( 124.7088614775786226, 0.2603800115204892296, -16.42320221600525088 ) ) ;
#33227=CARTESIAN_POINT ( 'NONE',  ( 113.8740681442453138, -9.859900752359374465, -12.68260735090039404 ) ) ;
#33228=EDGE_CURVE ( 'NONE', #24205, #17200, #26340, .T. ) ;
#33233=CARTESIAN_POINT ( 'NONE',  ( 126.1837548109119496, 0.4262465694468514643, -12.03445270309931736 ) ) ;
#33241=CARTESIAN_POINT ( 'NONE',  ( 118.8660148109119774, -10.30919188438810075, -12.61870101168855918 ) ) ;
#33242=CARTESIAN_POINT ( 'NONE',  ( 124.4252281442452812, -0.8288870151387760510, -10.36305467784173118 ) ) ;
#33243=CARTESIAN_POINT ( 'NONE',  ( 116.3700414775786527, -4.153390946401321671, -8.397313243818183892 ) ) ;
#33245=CARTESIAN_POINT ( 'NONE',  ( 124.2550481442452792, -9.988377603198980381, -10.36322818467138518 ) ) ;
#33246=CARTESIAN_POINT ( 'NONE',  ( 115.2355081442453155, -10.30919188438810075, -12.61870101168855918 ) ) ;
#33250=CARTESIAN_POINT ( 'NONE',  ( 123.9714148109119805, -0.4660016031367893996, -10.09054647747474043 ) ) ;
#33253=CARTESIAN_POINT ( 'NONE',  ( 115.1787814775786387, -9.988377603198976828, -10.36322818467138340 ) ) ;
#33254=CARTESIAN_POINT ( 'NONE',  ( 113.1933481442453058, -5.574606645277164318, -18.38911715685844683 ) ) ;
#33256=CARTESIAN_POINT ( 'NONE',  ( 126.2972081442452890, -2.084020599724406786, -8.691656652584148546 ) ) ;
#33257=ORIENTED_EDGE ( 'NONE', *, *, #35618, .F. ) ;
#33258=CARTESIAN_POINT ( 'NONE',  ( 122.7234281442452755, -5.638512984488999180, -18.83840828888717311 ) ) ;
#33259=AXIS2_PLACEMENT_3D ( 'NONE', #8485, #42922, #11686 ) ;
#33262=DIRECTION ( 'NONE',  ( 1.000000000000000000, 0.000000000000000000, 0.000000000000000000 ) ) ;
#33263=CARTESIAN_POINT ( 'NONE',  ( 113.5337081442453240, -0.8288870151387760510, -10.36305467784173118 ) ) ;
#33266=CARTESIAN_POINT ( 'NONE',  ( 125.7299414775786346, 0.9020085738987339008, -11.91225656197089222 ) ) ;
#33267=CARTESIAN_POINT ( 'NONE',  ( 112.0020881442453344, 0.2603800115204892296, -16.42320221600525088 ) ) ;
#33269=CARTESIAN_POINT ( 'NONE',  ( 113.0798948109119948, -0.4660016031367893996, -10.09054647747474043 ) ) ;
#33270=CARTESIAN_POINT ( 'NONE',  ( 116.9940348109119839, -0.1624402480850797581, -16.17319339645315424 ) ) ;
#33271=CARTESIAN_POINT ( 'NONE',  ( 124.3685014775786328, -10.63000616557722466, -14.87417383870573495 ) ) ;
#33273=CARTESIAN_POINT ( 'NONE',  ( 121.1918081442452859, 0.9020085738987339008, -11.91225656197089222 ) ) ;
#33274=ORIENTED_EDGE ( 'NONE', *, *, #33228, .F. ) ;
#33275=CARTESIAN_POINT ( 'NONE',  ( 117.6302601386228730, -1.125321370491268125, -17.12283323191015327 ) ) ;
#33279=CARTESIAN_POINT ( 'NONE',  ( 126.6390922358717717, -9.857170889351081655, -11.90331356446383282 ) ) ;
#33280=CARTESIAN_POINT ( 'NONE',  ( 119.8303681442453126, -10.63000616557722466, -14.87417383870573495 ) ) ;
#33282=CARTESIAN_POINT ( 'NONE',  ( 124.9357681442453014, -1.834011780172310813, -8.268836392978581529 ) ) ;
#33285=CARTESIAN_POINT ( 'NONE',  ( 113.7606148109119886, -7.894159318335828068, -9.358103419637847864 ) ) ;
#33286=CARTESIAN_POINT ( 'NONE',  ( 118.9227414775786400, -10.63000616557722466, -14.87417383870573495 ) ) ;
#33290=CARTESIAN_POINT ( 'NONE',  ( 121.0216281442452981, -7.894159318335803199, -9.358103419637831877 ) ) ;
#33291=CARTESIAN_POINT ( 'NONE',  ( 122.1561614775786353, -8.899110576539710493, -16.42337572283490132 ) ) ;
#33292=CARTESIAN_POINT ( 'NONE',  ( 120.3976348109119812, -1.834011780172310813, -8.268836392978581529 ) ) ;
#33293=CARTESIAN_POINT ( 'NONE',  ( 114.9518748109119883, -7.643976991954077427, -18.09477374809248928 ) ) ;
#33294=CARTESIAN_POINT ( 'NONE',  ( 116.1431348109119881, -10.30919188438810075, -12.61870101168855918 ) ) ;
#33296=CARTESIAN_POINT ( 'NONE',  ( 123.2339681442453241, -3.505236298600246325, -18.68346056562440793 ) ) ;
#33297=CARTESIAN_POINT ( 'NONE',  ( 121.1350814775786233, -9.859900752359378018, -12.68260735090039759 ) ) ;
#33299=CARTESIAN_POINT ( 'NONE',  ( 119.2255797424434149, -0.9924539043446216624, -17.29976612834909133 ) ) ;
#33300=CARTESIAN_POINT ( 'NONE',  ( 112.5126281442453120, -10.30919188438810075, -12.61870101168855918 ) ) ;
#33301=CARTESIAN_POINT ( 'NONE',  ( 120.2274548109119934, -9.859900752359378018, -12.68260735090039759 ) ) ;
#33304=CARTESIAN_POINT ( 'NONE',  ( 120.1140014775786398, -1.561330072975668504, -17.79121239304076951 ) ) ;
#33307=CARTESIAN_POINT ( 'NONE',  ( 116.4267681442453153, -6.222761293078241884, -8.102969835052219238 ) ) ;
#33308=ORIENTED_EDGE ( 'NONE', *, *, #3698, .T. ) ;
#33310=CARTESIAN_POINT ( 'NONE',  ( 125.7866681442452688, -8.899110576539710493, -16.42337572283490132 ) ) ;
#33311=CARTESIAN_POINT ( 'NONE',  ( 122.2128881442453263, -7.643976991954077427, -18.09477374809248928 ) ) ;
#33314=CARTESIAN_POINT ( 'NONE',  ( 117.1642148109119859, -9.261995988541697145, -16.69588392320189030 ) ) ;
#33317=CARTESIAN_POINT ( 'NONE',  ( 114.5547881442453217, -5.638512984488999180, -18.83840828888717311 ) ) ;
#33318=CARTESIAN_POINT ( 'NONE',  ( 114.3278814775786429, -10.30919188438810075, -12.61870101168855918 ) ) ;
#33319=CARTESIAN_POINT ( 'NONE',  ( 117.8449348109119938, -1.833838273342659253, -17.42832698103878286 ) ) ;
#33320=CARTESIAN_POINT ( 'NONE',  ( 124.7655881442452852, -9.859900752359378018, -12.68260735090039759 ) ) ;
#33323=CARTESIAN_POINT ( 'NONE',  ( 124.5954081442453116, -6.222761293078241884, -8.102969835052219238 ) ) ;
#33324=CARTESIAN_POINT ( 'NONE',  ( 114.0486636525450450, -2.378957183258581853, -17.95140958770220152 ) ) ;
#33328=CARTESIAN_POINT ( 'NONE',  ( 119.2631014775786298, 0.2603800115204892296, -16.42320221600525088 ) ) ;
#33330=CARTESIAN_POINT ( 'NONE',  ( 120.9081748109119872, -5.638512984488999180, -18.83840828888717311 ) ) ;
#33333=CARTESIAN_POINT ( 'NONE',  ( 119.6601881442453106, -8.166667518702819706, -8.995218007635861213 ) ) ;
#33334=CARTESIAN_POINT ( 'NONE',  ( 120.9081748109119872, -5.638512984488999180, -18.83840828888717311 ) ) ;
#33341=CARTESIAN_POINT ( 'NONE',  ( 123.4041481442452834, 0.1319031606808879209, -14.10382304977623669 ) ) ;
#33344=CARTESIAN_POINT ( 'NONE',  ( 116.8238548109119819, -5.574606645277164318, -18.38911715685844683 ) ) ;
#33347=CARTESIAN_POINT ( 'NONE',  ( 125.8433948109119456, -1.834011780172310813, -8.268836392978581529 ) ) ;
#33348=CARTESIAN_POINT ( 'NONE',  ( 124.6521348109119884, -1.561330072975668948, -17.79121239304076951 ) ) ;
#33351=CARTESIAN_POINT ( 'NONE',  ( 120.9649014775786355, -6.222761293078241884, -8.102969835052219238 ) ) ;
#33352=CARTESIAN_POINT ( 'NONE',  ( 116.5402214775786405, 0.2603800115204892296, -16.42320221600525088 ) ) ;
#33353=CARTESIAN_POINT ( 'NONE',  ( 122.3830681442452857, -8.166667518702819706, -8.995218007635861213 ) ) ;
#33355=CARTESIAN_POINT ( 'NONE',  ( 124.3685014775786328, 0.4262465694468514643, -12.03445270309931736 ) ) ;
#33358=CARTESIAN_POINT ( 'NONE',  ( 124.9357681442453014, -1.834011780172310813, -8.268836392978581529 ) ) ;
#33360=CARTESIAN_POINT ( 'NONE',  ( 123.8579614775786126, 0.5811942927096110934, -14.16772938898807510 ) ) ;
#33366=CARTESIAN_POINT ( 'NONE',  ( 127.9202185846628481, -3.082963570468182812, -14.51592808579281701 ) ) ;
#33370=CARTESIAN_POINT ( 'NONE',  ( 117.9016614775786280, -0.1624402480850797581, -16.17319339645315424 ) ) ;
#33371=CARTESIAN_POINT ( 'NONE',  ( 111.3213681442453264, -7.643976991954077427, -18.09477374809248928 ) ) ;
#33374=CARTESIAN_POINT ( 'NONE',  ( 115.8639169858783617, -2.378957183258571639, -17.95140958770219086 ) ) ;
#33375=CARTESIAN_POINT ( 'NONE',  ( 116.7104014775786425, -8.899110576539710493, -16.42337572283490132 ) ) ;
#33378=CARTESIAN_POINT ( 'NONE',  ( 123.9103448073892508, -1.081026697600536046, -17.18181821144402832 ) ) ;
#33380=CARTESIAN_POINT ( 'NONE',  ( 123.2906948109119867, -8.166667518702819706, -8.995218007635861213 ) ) ;
#33381=CARTESIAN_POINT ( 'NONE',  ( 122.0427081442452817, -9.859900752359378018, -12.68260735090039759 ) ) ;
#33383=CYLINDRICAL_SURFACE ( 'NONE', #11312, 5.999999999999997335 ) ;
#33386=CARTESIAN_POINT ( 'NONE',  ( 122.0994348109119443, -10.15424416112533912, -14.75197769757731336 ) ) ;
#33387=CARTESIAN_POINT ( 'NONE',  ( 120.9649014775786355, -6.222761293078241884, -8.102969835052219238 ) ) ;
#33396=CARTESIAN_POINT ( 'NONE',  ( 120.4543614775786295, -4.089484607189486809, -7.948022111789456723 ) ) ;
#33397=CARTESIAN_POINT ( 'NONE',  ( 122.6099748109119929, -9.261995988541697145, -16.69588392320189030 ) ) ;
#33399=CARTESIAN_POINT ( 'NONE',  ( 115.0086014775786509, -4.089484607189486809, -7.948022111789456723 ) ) ;
#33400=CARTESIAN_POINT ( 'NONE',  ( 114.1577014775786552, -6.344957434206662583, -7.627207830600332805 ) ) ;
#33403=CARTESIAN_POINT ( 'NONE',  ( 112.2289948109119848, -7.643976991954077427, -18.09477374809248928 ) ) ;
#33404=CARTESIAN_POINT ( 'NONE',  ( 120.0005481442453146, -5.638512984488999180, -18.83840828888717311 ) ) ;
#33405=CARTESIAN_POINT ( 'NONE',  ( 112.0020881442453344, 0.2603800115204892296, -16.42320221600525088 ) ) ;
#33406=CARTESIAN_POINT ( 'NONE',  ( 114.0442481442453300, -7.643976991954077427, -18.09477374809248928 ) ) ;
#33408=CARTESIAN_POINT ( 'NONE',  ( 112.5126281442453120, 0.1319031606808879209, -14.10382304977623669 ) ) ;
#33409=CARTESIAN_POINT ( 'NONE',  ( 125.2194014775786286, -10.30919188438810075, -12.61870101168855918 ) ) ;
#33411=CARTESIAN_POINT ( 'NONE',  ( 118.4689281442453250, -10.15424416112533912, -14.75197769757731336 ) ) ;
#33418=CARTESIAN_POINT ( 'NONE',  ( 121.5321681442453183, -9.988377603198976828, -10.36322818467138340 ) ) ;
#33426=CARTESIAN_POINT ( 'NONE',  ( 124.1983214775786166, -1.833838273342659697, -17.42832698103878286 ) ) ;
#33428=CARTESIAN_POINT ( 'NONE',  ( 124.5386814775786206, -5.638512984488999180, -18.83840828888717311 ) ) ;
#33429=CARTESIAN_POINT ( 'NONE',  ( 117.2209414775786485, -2.084020599724406786, -8.691656652584148546 ) ) ;
#33432=CARTESIAN_POINT ( 'NONE',  ( 123.1205148109119563, -1.834011780172310813, -8.268836392978581529 ) ) ;
#33433=CARTESIAN_POINT ( 'NONE',  ( 115.9729548109119861, -6.344957434206662583, -7.627207830600332805 ) ) ;
#33435=DIRECTION ( 'NONE',  ( 1.000000000000000000, 0.000000000000000000, 0.000000000000000000 ) ) ;
#33436=CARTESIAN_POINT ( 'NONE',  ( 123.1772414775786189, -5.574606645277164318, -18.38911715685844683 ) ) ;
#33437=CARTESIAN_POINT ( 'NONE',  ( 124.0281414775786146, -1.834011780172310813, -8.268836392978581529 ) ) ;
#33441=CARTESIAN_POINT ( 'NONE',  ( 114.3278814775786429, 0.1319031606808879209, -14.10382304977623669 ) ) ;
#33442=CARTESIAN_POINT ( 'NONE',  ( 115.8027748109119841, -8.899110576539710493, -16.42337572283490132 ) ) ;
#33448=CARTESIAN_POINT ( 'NONE',  ( 125.9001214775786224, -5.574606645277164318, -18.38911715685844683 ) ) ;
#33455=CARTESIAN_POINT ( 'NONE',  ( 119.0361948109119652, -7.893985811506177619, -18.51759400769804742 ) ) ;
#33457=CARTESIAN_POINT ( 'NONE',  ( 122.5532481442453019, 0.4262465694468514643, -12.03445270309931736 ) ) ;
#33458=CARTESIAN_POINT ( 'NONE',  ( 114.3278814775786429, 0.1319031606808879209, -14.10382304977623669 ) ) ;
#33463=CARTESIAN_POINT ( 'NONE',  ( 114.5547881442453217, -5.638512984488999180, -18.83840828888717311 ) ) ;
#33466=CARTESIAN_POINT ( 'NONE',  ( 122.8368814775786291, -1.561330072975668948, -17.79121239304076951 ) ) ;
#33469=CARTESIAN_POINT ( 'NONE',  ( 113.5904348109119866, -7.893985811506177619, -18.51759400769804742 ) ) ;
#33470=CARTESIAN_POINT ( 'NONE',  ( 115.0086014775786509, -5.574606645277164318, -18.38911715685844683 ) ) ;
#33471=CARTESIAN_POINT ( 'NONE',  ( 126.2184548109120072, -5.454730531075203004, -18.35951656919957742 ) ) ;
#33472=CARTESIAN_POINT ( 'NONE',  ( 125.3895814775786448, -2.084020599724406786, -8.691656652584148546 ) ) ;
#33474=CARTESIAN_POINT ( 'NONE',  ( 123.0070614775786169, 0.9020085738987339008, -11.91225656197089222 ) ) ;
#33481=CARTESIAN_POINT ( 'NONE',  ( 136.8192643132354931, -2.859499808723217296, -8.184084197783032977 ) ) ;
#33482=CARTESIAN_POINT ( 'NONE',  ( 112.9664414775786412, -9.859900752359374465, -12.68260735090039404 ) ) ;
#33486=CARTESIAN_POINT ( 'NONE',  ( 114.5547881442453217, -4.153390946401321671, -8.397313243818183892 ) ) ;
#33487=CARTESIAN_POINT ( 'NONE',  ( 111.8886348109120092, -3.383040157471821630, -19.15922257007629170 ) ) ;
#33489=CARTESIAN_POINT ( 'NONE',  ( 126.4673881442452910, -7.894159318335828068, -9.358103419637847864 ) ) ;
#33490=CARTESIAN_POINT ( 'NONE',  ( 117.2776681442452968, -4.153390946401321671, -8.397313243818183892 ) ) ;
#33491=CARTESIAN_POINT ( 'NONE',  ( 124.8790414775786246, -0.4660016031367893996, -10.09054647747474043 ) ) ;
#33492=CARTESIAN_POINT ( 'NONE',  ( 122.9503348109119827, 0.5811942927096110934, -14.16772938898807510 ) ) ;
#33494=CARTESIAN_POINT ( 'NONE',  ( 113.2500748109119968, -6.344957434206662583, -7.627207830600332805 ) ) ;
#33499=CARTESIAN_POINT ( 'NONE',  ( 119.7736414775786358, -10.30919188438810075, -12.61870101168855918 ) ) ;
#33501=CARTESIAN_POINT ( 'NONE',  ( 124.7088614775786226, 0.2603800115204892296, -16.42320221600525088 ) ) ;
#33503=CARTESIAN_POINT ( 'NONE',  ( 120.9291030939976821, -2.236191541394346061, -18.14152338500401029 ) ) ;
#33504=CARTESIAN_POINT ( 'NONE',  ( 113.9307948109119764, -10.15424416112533912, -14.75197769757731336 ) ) ;
#33506=CARTESIAN_POINT ( 'NONE',  ( 118.6391081442452986, -4.089484607189486809, -7.948022111789456723 ) ) ;
#33510=CARTESIAN_POINT ( 'NONE',  ( 120.6812681442452941, 0.1319031606808905299, -14.10382304977622248 ) ) ;
#33511=CARTESIAN_POINT ( 'NONE',  ( 123.0070614775786169, -10.15424416112533912, -14.75197769757731336 ) ) ;
#33512=CARTESIAN_POINT ( 'NONE',  ( 120.0572748109119772, -3.383040157471821630, -19.15922257007629170 ) ) ;
#33514=CARTESIAN_POINT ( 'NONE',  ( 115.1787814775786387, -0.1624402480850797581, -16.17319339645315424 ) ) ;
#33515=CARTESIAN_POINT ( 'NONE',  ( 116.7104014775786425, -0.4660016031367893996, -10.09054647747474043 ) ) ;
#33517=CARTESIAN_POINT ( 'NONE',  ( 126.8137406967790071, -1.239144018213914622, -9.529331767162547706 ) ) ;
#33518=CARTESIAN_POINT ( 'NONE',  ( 120.2841814775786276, -10.15424416112533912, -14.75197769757731336 ) ) ;
#33520=CARTESIAN_POINT ( 'NONE',  ( 119.6034614775786196, -6.344957434206651037, -7.627207830600339911 ) ) ;
#33522=CARTESIAN_POINT ( 'NONE',  ( 112.3424481442453384, -6.344957434206662583, -7.627207830600332805 ) ) ;
#33523=CARTESIAN_POINT ( 'NONE',  ( 121.7023481442452777, -0.8288870151387760510, -10.36305467784173118 ) ) ;
#33528=CARTESIAN_POINT ( 'NONE',  ( 120.3976348109119812, -1.834011780172310813, -8.268836392978581529 ) ) ;
#33530=CARTESIAN_POINT ( 'NONE',  ( 114.7249681442453237, -9.565557343593413364, -10.61323700422348004 ) ) ;
#33533=CARTESIAN_POINT ( 'NONE',  ( 126.4673881442452910, -7.894159318335828068, -9.358103419637847864 ) ) ;
#33535=CARTESIAN_POINT ( 'NONE',  ( 121.1918081442452859, -10.15424416112533912, -14.75197769757731336 ) ) ;
#33538=CARTESIAN_POINT ( 'NONE',  ( 120.1140014775786398, -1.561330072975668504, -17.79121239304076951 ) ) ;
#33541=CARTESIAN_POINT ( 'NONE',  ( 117.9016614775786280, -9.988377603198976828, -10.36322818467138340 ) ) ;
#33542=CARTESIAN_POINT ( 'NONE',  ( 116.9373081442452929, -8.166667518702817929, -8.995218007635861213 ) ) ;
#33543=CARTESIAN_POINT ( 'NONE',  ( 115.5191414775786569, -6.222761293078241884, -8.102969835052219238 ) ) ;
#33544=CARTESIAN_POINT ( 'NONE',  ( 124.8790414775786246, -8.899110576539710493, -16.42337572283490132 ) ) ;
#33545=CARTESIAN_POINT ( 'NONE',  ( 111.7751814775786556, -7.893985811506177619, -18.51759400769804742 ) ) ;
#33547=CARTESIAN_POINT ( 'NONE',  ( 124.6521348109119884, -7.894159318335828068, -9.358103419637847864 ) ) ;
#33554=CARTESIAN_POINT ( 'NONE',  ( 121.8158014775786171, -5.638512984488999180, -18.83840828888717311 ) ) ;
#33557=CARTESIAN_POINT ( 'NONE',  ( 121.5321681442453183, -9.988377603198976828, -10.36322818467138340 ) ) ;
#33560=CARTESIAN_POINT ( 'NONE',  ( 119.3765548109119834, 0.9020085738987339008, -11.91225656197089222 ) ) ;
#33561=CARTESIAN_POINT ( 'NONE',  ( 122.0427081442452817, 0.5811942927096110934, -14.16772938898807510 ) ) ;
#33563=CARTESIAN_POINT ( 'NONE',  ( 123.9146881442452894, -10.15424416112533912, -14.75197769757731336 ) ) ;
#33568=CARTESIAN_POINT ( 'NONE',  ( 114.6490365460471992, -2.191907684172563986, -18.20049396185734025 ) ) ;
#33569=CARTESIAN_POINT ( 'NONE',  ( 123.4608748109119745, 0.4262465694468514643, -12.03445270309931736 ) ) ;
#33570=B_SPLINE_CURVE_WITH_KNOTS ( 'NONE', 3,
 ( #14573, #10491, #13905, #35295, #42172, #27814, #41728, #24393, #38281, #7061, #433, #42395, #17548, #34843, #20971, #10932, #38725, #28041, #14349, #3848, #17768, #10713, #17992, #38497, #11159, #38957, #7725, #24176, #7274, #28263, #44933 ),
 .UNSPECIFIED., .F., .F.,
 ( 4, 2, 2, 1, 1, 1, 2, 2, 2, 1, 1, 1, 2, 2, 2, 1, 2, 2, 4 ),
 ( 0.000000000000000000, 0.2499999999999587552, 0.3749999999999381606, 0.4374999999999273914, 0.4687499999999356626, 0.4843749999999260036, 0.4921874999999357181, 0.4999999999999454880, 0.6250000000000111022, 0.6875000000000333067, 0.7187500000000436318, 0.7343750000000371925, 0.7421875000000338618, 0.7500000000000305311, 0.8125000000000198730, 0.8437500000000134337, 0.8593750000000098810, 0.8750000000000063283, 1.000000000000000000 ),
 .UNSPECIFIED. ) ;
#33573=CARTESIAN_POINT ( 'NONE',  ( 116.2565881442453133, -0.8288870151387760510, -10.36305467784173118 ) ) ;
#33576=CARTESIAN_POINT ( 'NONE',  ( 113.3635281442453504, -0.1624402480850797581, -16.17319339645315424 ) ) ;
#33577=CARTESIAN_POINT ( 'NONE',  ( 122.5532481442453019, -10.63000616557722466, -14.87417383870573495 ) ) ;
#33579=CARTESIAN_POINT ( 'NONE',  ( 121.2485348109119769, -8.899110576539710493, -16.42337572283490132 ) ) ;
#33580=CARTESIAN_POINT ( 'NONE',  ( 116.0864081442453113, -9.988377603198976828, -10.36322818467138340 ) ) ;
#33582=CARTESIAN_POINT ( 'NONE',  ( 125.3328548109119964, -9.261995988541697145, -16.69588392320189030 ) ) ;
#33584=CARTESIAN_POINT ( 'NONE',  ( 123.5176014775786228, -0.8288870151387760510, -10.36305467784173118 ) ) ;
#33586=CARTESIAN_POINT ( 'NONE',  ( 123.6519830939976572, -2.236191541394346061, -18.14152338500401029 ) ) ;
#33588=CARTESIAN_POINT ( 'NONE',  ( 124.1415948109119540, -6.344957434206665248, -7.627207830600338134 ) ) ;
#33589=CARTESIAN_POINT ( 'NONE',  ( 113.5337081442453240, -0.8288870151387760510, -10.36305467784173118 ) ) ;
#33590=CARTESIAN_POINT ( 'NONE',  ( 126.0135748109119902, -8.166667518702819706, -8.995218007635861213 ) ) ;
#33594=CARTESIAN_POINT ( 'NONE',  ( 127.9566280595583692, -3.013114159214123511, -14.60907972933637566 ) ) ;
#33597=CARTESIAN_POINT ( 'NONE',  ( 119.4900081442453086, -7.643976991954077427, -18.09477374809248928 ) ) ;
#33598=CARTESIAN_POINT ( 'NONE',  ( 112.7962614775786676, -6.222761293078241884, -8.102969835052219238 ) ) ;
#33599=CARTESIAN_POINT ( 'NONE',  ( 127.0150841466615930, -0.0006450967245569220066, -11.05022577389757465 ) ) ;
#33602=CARTESIAN_POINT ( 'NONE',  ( 115.3489614775786407, -0.8288870151387760510, -10.36305467784173118 ) ) ;
#33605=VECTOR ( 'NONE', #22186, 1000.000000000000000 ) ;
#33608=CARTESIAN_POINT ( 'NONE',  ( 124.1983214775786166, -8.166667518702819706, -8.995218007635861213 ) ) ;
#33609=CARTESIAN_POINT ( 'NONE',  ( 122.7234281442452755, -4.153390946401325223, -8.397313243818185668 ) ) ;
#33614=CARTESIAN_POINT ( 'NONE',  ( 126.6375681442452930, -10.15424416112533912, -14.75197769757731336 ) ) ;
#33615=CARTESIAN_POINT ( 'NONE',  ( 118.5256548109119876, -8.899110576539710493, -16.42337572283490132 ) ) ;
#33620=CARTESIAN_POINT ( 'NONE',  ( 112.2857214775786474, -5.574606645277172312, -18.38911715685844683 ) ) ;
#33621=CARTESIAN_POINT ( 'NONE',  ( 114.6115148109119986, -6.222761293078241884, -8.102969835052219238 ) ) ;
#33625=CARTESIAN_POINT ( 'NONE',  ( 122.3263414775786373, -6.344957434206665248, -7.627207830600338134 ) ) ;
#33626=CARTESIAN_POINT ( 'NONE',  ( 123.1772414775786189, -4.089484607189486809, -7.948022111789456723 ) ) ;
#33628=CARTESIAN_POINT ( 'NONE',  ( 117.5045748109119756, 0.5811942927096110934, -14.16772938898807510 ) ) ;
#33631=CARTESIAN_POINT ( 'NONE',  ( 114.3846081442453197, -10.63000616557722466, -14.87417383870573495 ) ) ;
#33633=CARTESIAN_POINT ( 'NONE',  ( 114.7816948109119863, -9.859900752359374465, -12.68260735090039404 ) ) ;
#33634=CARTESIAN_POINT ( 'NONE',  ( 113.0798948109119948, -8.899110576539710493, -16.42337572283490132 ) ) ;
#33635=CARTESIAN_POINT ( 'NONE',  ( 121.4187148109119789, -6.344957434206665248, -7.627207830600338134 ) ) ;
#33636=CARTESIAN_POINT ( 'NONE',  ( 124.7088614775786226, -9.565557343593413364, -10.61323700422348004 ) ) ;
#33637=CARTESIAN_POINT ( 'NONE',  ( 113.3635281442453504, -0.1624402480850797581, -16.17319339645315424 ) ) ;
#33639=CARTESIAN_POINT ( 'NONE',  ( 118.8660148109119774, 0.1319031606808879209, -14.10382304977623669 ) ) ;
#33640=CARTESIAN_POINT ( 'NONE',  ( 124.1983214775786166, -8.166667518702819706, -8.995218007635861213 ) ) ;
#33644=CARTESIAN_POINT ( 'NONE',  ( 119.2631014775786298, -9.565557343593413364, -10.61323700422348004 ) ) ;
#33645=CARTESIAN_POINT ( 'NONE',  ( 128.2184548109119930, -4.105398160058917334, -19.34506575923121474 ) ) ;
#33646=ORIENTED_EDGE ( 'NONE', *, *, #26167, .F. ) ;
#33648=CARTESIAN_POINT ( 'NONE',  ( 122.7234281442452755, -5.638512984488999180, -18.83840828888717311 ) ) ;
#33652=CARTESIAN_POINT ( 'NONE',  ( 112.5693548109119888, -10.63000616557722466, -14.87417383870573495 ) ) ;
#33657=CARTESIAN_POINT ( 'NONE',  ( 137.5058127635946335, -5.720712770326367824, -18.32462370007482377 ) ) ;
#33659=CARTESIAN_POINT ( 'NONE',  ( 125.1008810305878001, -2.476927793680328449, -17.82094707215535578 ) ) ;
#33661=CARTESIAN_POINT ( 'NONE',  ( 118.9227414775786542, 0.4262465694468514643, -12.03445270309931736 ) ) ;
#33664=CARTESIAN_POINT ( 'NONE',  ( 124.1415948109119540, -6.344957434206665248, -7.627207830600338134 ) ) ;
#33665=CARTESIAN_POINT ( 'NONE',  ( 115.2355081442453155, -10.30919188438810075, -12.61870101168855918 ) ) ;
#33667=CARTESIAN_POINT ( 'NONE',  ( 125.1309504620138284, -2.495269033102075262, -17.79652296963211455 ) ) ;
#33668=CARTESIAN_POINT ( 'NONE',  ( 122.6667014775786413, -2.084020599724406786, -8.691656652584148546 ) ) ;
#33669=EDGE_CURVE ( 'NONE', #25347, #22341, #44118, .T. ) ;
#33671=CARTESIAN_POINT ( 'NONE',  ( 125.9001214775786224, -4.089484607189486809, -7.948022111789456723 ) ) ;
#33675=CARTESIAN_POINT ( 'NONE',  ( 115.8027748109119841, -8.899110576539710493, -16.42337572283490132 ) ) ;
#33677=CARTESIAN_POINT ( 'NONE',  ( 116.0296814775786345, -1.833838273342658809, -17.42832698103878286 ) ) ;
#33683=CARTESIAN_POINT ( 'NONE',  ( 124.1983214775786166, -1.833838273342659697, -17.42832698103878286 ) ) ;
#33690=CARTESIAN_POINT ( 'NONE',  ( 123.5827482314454926, -3.123236290774572321, -14.46231915649883959 ) ) ;
#33694=CARTESIAN_POINT ( 'NONE',  ( 119.4900081442453086, -1.834011780172310813, -8.268836392978581529 ) ) ;
#33695=CARTESIAN_POINT ( 'NONE',  ( 123.4608748109119745, 0.4262465694468514643, -12.03445270309931736 ) ) ;
#33696=CARTESIAN_POINT ( 'NONE',  ( 115.6893214775786447, -9.859900752359374465, -12.68260735090039404 ) ) ;
#33699=CARTESIAN_POINT ( 'NONE',  ( 122.9503348109119827, 0.5811942927096110934, -14.16772938898807510 ) ) ;
#33700=CARTESIAN_POINT ( 'NONE',  ( 114.6682414775786469, -1.561330072975668060, -17.79121239304076596 ) ) ;
#33702=CARTESIAN_POINT ( 'NONE',  ( 125.7299414775786346, 0.9020085738987339008, -11.91225656197089222 ) ) ;
#33704=ORIENTED_EDGE ( 'NONE', *, *, #38175, .T. ) ;
#33705=CARTESIAN_POINT ( 'NONE',  ( 114.7249681442453237, 0.2603800115204892296, -16.42320221600525088 ) ) ;
#33706=CARTESIAN_POINT ( 'NONE',  ( 115.4624148109119943, -4.153390946401321671, -8.397313243818183892 ) ) ;
#33709=CARTESIAN_POINT ( 'NONE',  ( 113.6471614775786492, -5.638512984488999180, -18.83840828888717311 ) ) ;
#33710=ORIENTED_EDGE ( 'NONE', *, *, #41595, .T. ) ;
#33712=CARTESIAN_POINT ( 'NONE',  ( 121.3619881442452879, -4.089484607189486809, -7.948022111789456723 ) ) ;
#33715=CARTESIAN_POINT ( 'NONE',  ( 124.8179714740559234, -1.081026697600536934, -17.18181821144403187 ) ) ;
#33716=CARTESIAN_POINT ( 'NONE',  ( 116.6536748109119941, -10.15424416112533912, -14.75197769757731336 ) ) ;
#33718=CARTESIAN_POINT ( 'NONE',  ( 115.4624148109119943, -4.153390946401321671, -8.397313243818183892 ) ) ;
#33722=CARTESIAN_POINT ( 'NONE',  ( 115.4624148109119943, -4.153390946401321671, -8.397313243818183892 ) ) ;
#33723=CARTESIAN_POINT ( 'NONE',  ( 116.3700414775786527, -5.638512984488999180, -18.83840828888717311 ) ) ;
#33725=CARTESIAN_POINT ( 'NONE',  ( 126.0135748109119902, -1.833838273342660141, -17.42832698103878286 ) ) ;
#33726=CARTESIAN_POINT ( 'NONE',  ( 113.8740681442453138, -9.859900752359374465, -12.68260735090039404 ) ) ;
#33727=CARTESIAN_POINT ( 'NONE',  ( 124.9924948109119924, -4.089484607189486809, -7.948022111789456723 ) ) ;
#33728=ADVANCED_FACE ( 'NONE', ( #33142 ), #2381, .T. ) ;
#33729=CARTESIAN_POINT ( 'NONE',  ( 121.0216281442452981, -1.561330072975668948, -17.79121239304076951 ) ) ;
#33731=CARTESIAN_POINT ( 'NONE',  ( 113.1933481442453058, -4.089484607189486809, -7.948022111789456723 ) ) ;
#33735=CARTESIAN_POINT ( 'NONE',  ( 128.1232624476561739, -3.897116775730919080, -15.92989199573930925 ) ) ;
#33736=CARTESIAN_POINT ( 'NONE',  ( 118.7525614775786380, -8.166667518702819706, -8.995218007635861213 ) ) ;
#33738=CARTESIAN_POINT ( 'NONE',  ( 125.2194014775786286, -10.30919188438810075, -12.61870101168855918 ) ) ;
#33740=CARTESIAN_POINT ( 'NONE',  ( 114.4980614775786734, -2.084020599724406786, -8.691656652584148546 ) ) ;
#33741=( BOUNDED_CURVE ( )  B_SPLINE_CURVE ( 2, ( #19676, #14351, #13079, #31225, #16270, #38283, #6226, #33798, #10493, #9651, #7063, #8216, #20973, #42174, #34845, #24616, #17550 ),
 .UNSPECIFIED., .F., .T. ) 
 B_SPLINE_CURVE_WITH_KNOTS ( ( 3, 2, 2, 2, 2, 2, 2, 2, 3 ),
 ( 0.2670046674808919662, 0.2734375000000000000, 0.2812500000000000000, 0.2890625000000000000, 0.2968750000000000000, 0.3046875000000000000, 0.3125000000000000000, 0.3203125000000000000, 0.3267453325190585178 ),
 .UNSPECIFIED. ) 
 CURVE ( )  GEOMETRIC_REPRESENTATION_ITEM ( )  RATIONAL_B_SPLINE_CURVE ( ( 0.9778625265006459788, 0.9373222120152210346, 1.000000000000000000, 0.9238795325112869605, 1.000000000000000000, 0.9238795325112869605, 1.000000000000000000, 0.9238795325112869605, 1.000000000000000000, 0.9238795325112869605, 1.000000000000000000, 0.9238795325112869605, 1.000000000000000000, 0.9238795325112869605, 1.000000000000000000, 0.9373222120157019832, 0.9778625265000240319 ) ) 
 REPRESENTATION_ITEM ( '' )  );
#33743=CARTESIAN_POINT ( 'NONE',  ( 120.4543614775786295, -4.089484607189486809, -7.948022111789456723 ) ) ;
#33749=CARTESIAN_POINT ( 'NONE',  ( 123.6310548109119765, -4.153390946401325223, -8.397313243818185668 ) ) ;
#33751=CARTESIAN_POINT ( 'NONE',  ( 121.0216281442452981, -1.561330072975668948, -17.79121239304076951 ) ) ;
#33752=CARTESIAN_POINT ( 'NONE',  ( 114.8951481442453115, -8.899110576539710493, -16.42337572283490132 ) ) ;
#33753=CARTESIAN_POINT ( 'NONE',  ( 115.1787814775786387, -9.988377603198976828, -10.36322818467138340 ) ) ;
#33756=CARTESIAN_POINT ( 'NONE',  ( 127.0298367773230979, -1.258840796252208127, -9.365270548298379794 ) ) ;
#33757=CARTESIAN_POINT ( 'NONE',  ( 120.7379948109119709, 0.4262465694468514643, -12.03445270309931736 ) ) ;
#33761=CARTESIAN_POINT ( 'NONE',  ( 113.1933481442453058, -4.089484607189486809, -7.948022111789456723 ) ) ;
#33762=CARTESIAN_POINT ( 'NONE',  ( 119.6601881442453106, -1.833838273342659253, -17.42832698103878286 ) ) ;
#33765=CARTESIAN_POINT ( 'NONE',  ( 118.8660148109119774, -10.30919188438810075, -12.61870101168855918 ) ) ;
#33767=CARTESIAN_POINT ( 'NONE',  ( 117.7314814775786260, -5.574606645277164318, -18.38911715685844683 ) ) ;
#33770=CARTESIAN_POINT ( 'NONE',  ( 112.2289948109119848, -1.834011780172310813, -8.268836392978581529 ) ) ;
#33771=CARTESIAN_POINT ( 'NONE',  ( 121.4754414775786131, -1.833838273342659697, -17.42832698103878286 ) ) ;
#33774=CARTESIAN_POINT ( 'NONE',  ( 118.1285681442453068, -7.893985811506177619, -18.51759400769804742 ) ) ;
#33776=CARTESIAN_POINT ( 'NONE',  ( 120.9649014775786355, -3.383040157471821630, -19.15922257007629170 ) ) ;
#33777=CARTESIAN_POINT ( 'NONE',  ( 115.6325948109119821, 0.2603800115204892296, -16.42320221600525088 ) ) ;
#33778=CARTESIAN_POINT ( 'NONE',  ( 119.4332814775786318, -8.899110576539710493, -16.42337572283490132 ) ) ;
#33779=CARTESIAN_POINT ( 'NONE',  ( 123.9714148109119805, -8.899110576539710493, -16.42337572283490132 ) ) ;
#33780=FACE_OUTER_BOUND ( 'NONE', #19572, .T. ) ;
#33782=CARTESIAN_POINT ( 'NONE',  ( 124.7655881442452852, -9.859900752359378018, -12.68260735090039759 ) ) ;
#33783=CARTESIAN_POINT ( 'NONE',  ( 123.7253032127138397, -2.191907684172563986, -18.20049396185734025 ) ) ;
#33784=CARTESIAN_POINT ( 'NONE',  ( 125.8328548109119964, -8.862178061931794915, -16.39564131203325559 ) ) ;
#33788=CARTESIAN_POINT ( 'NONE',  ( 121.0783548109119749, 0.2603800115204892296, -16.42320221600525088 ) ) ;
#33789=CARTESIAN_POINT ( 'NONE',  ( 123.8579614775786126, -9.859900752359378018, -12.68260735090039759 ) ) ;
#33791=CARTESIAN_POINT ( 'NONE',  ( 124.9924948109119924, -4.089484607189486809, -7.948022111789456723 ) ) ;
#33792=CARTESIAN_POINT ( 'NONE',  ( 113.8740681442453138, -9.859900752359374465, -12.68260735090039404 ) ) ;
#33794=CARTESIAN_POINT ( 'NONE',  ( 120.6245414775786458, -9.988377603198976828, -10.36322818467138340 ) ) ;
#33795=CARTESIAN_POINT ( 'NONE',  ( 122.4965214775786251, -10.30919188438810075, -12.61870101168855918 ) ) ;
#33797=CARTESIAN_POINT ( 'NONE',  ( 122.3263414775786373, -3.505236298600246325, -18.68346056562440793 ) ) ;
#33798=CARTESIAN_POINT ( 'NONE',  ( 115.9729548109120003, -6.344957434206662583, -7.627207830600333693 ) ) ;
#33802=CARTESIAN_POINT ( 'NONE',  ( 112.3991748109119868, -1.833838273342658809, -17.42832698103878286 ) ) ;
#33803=CARTESIAN_POINT ( 'NONE',  ( 123.6877814775786533, -6.222761293078241884, -8.102969835052219238 ) ) ;
#33807=CARTESIAN_POINT ( 'NONE',  ( 117.2776681442452968, -4.153390946401325223, -8.397313243818185668 ) ) ;
#33809=CARTESIAN_POINT ( 'NONE',  ( 114.8384214775786489, -10.15424416112533912, -14.75197769757731336 ) ) ;
#33810=CARTESIAN_POINT ( 'NONE',  ( 123.1205148109119563, -1.834011780172310813, -8.268836392978581529 ) ) ;
#33813=CARTESIAN_POINT ( 'NONE',  ( 121.8725281442453223, -6.222761293078241884, -8.102969835052219238 ) ) ;
#33814=CARTESIAN_POINT ( 'NONE',  ( 117.5613014775786525, 0.9020085738987339008, -11.91225656197089222 ) ) ;
#33815=CARTESIAN_POINT ( 'NONE',  ( 125.2194014775786286, -10.30919188438810075, -12.61870101168855918 ) ) ;
#33816=CARTESIAN_POINT ( 'NONE',  ( 124.9357681442453014, -7.643976991954077427, -18.09477374809248928 ) ) ;
#33819=CARTESIAN_POINT ( 'NONE',  ( 124.9924948109119924, -4.089484607189486809, -7.948022111789456723 ) ) ;
#33821=CARTESIAN_POINT ( 'NONE',  ( 115.9162281442453235, -5.574606645277164318, -18.38911715685844683 ) ) ;
#33822=( BOUNDED_CURVE ( )  B_SPLINE_CURVE ( 2, ( #18688, #4990, #33015, #15715, #40107, #29617, #26651, #18902, #9326, #33245, #43986, #43532, #39884, #8647, #30075, #32577, #25754 ),
 .UNSPECIFIED., .F., .F. ) 
 B_SPLINE_CURVE_WITH_KNOTS ( ( 3, 2, 2, 2, 2, 2, 2, 2, 3 ),
 ( 0.8295046674808920217, 0.8359375000000000000, 0.8437500000000000000, 0.8515625000000000000, 0.8593750000000000000, 0.8671875000000000000, 0.8750000000000000000, 0.8828125000000000000, 0.8892453325190590174 ),
 .UNSPECIFIED. ) 
 CURVE ( )  GEOMETRIC_REPRESENTATION_ITEM ( )  RATIONAL_B_SPLINE_CURVE ( ( 0.9778625265006459788, 0.9373222120152210346, 1.000000000000000000, 0.9238795325112869605, 1.000000000000000000, 0.9238795325112869605, 1.000000000000000000, 0.9238795325112869605, 1.000000000000000000, 0.9238795325112869605, 1.000000000000000000, 0.9238795325112869605, 1.000000000000000000, 0.9238795325112869605, 1.000000000000000000, 0.9373222120156999848, 0.9778625265000260303 ) ) 
 REPRESENTATION_ITEM ( '' )  );
#33823=CARTESIAN_POINT ( 'NONE',  ( 123.9146881442452894, 0.9020085738987339008, -11.91225656197089222 ) ) ;
#33828=B_SPLINE_CURVE_WITH_KNOTS ( 'NONE', 3,
 ( #11194, #3884, #249, #31698, #916, #39453, #7763, #28294, #31476, #17805 ),
 .UNSPECIFIED., .F., .F.,
 ( 4, 3, 3, 4 ),
 ( 0.000000000000000000, 0.0001671877560958099957, 0.0003343755126086554838, 0.0006438490228505469159 ),
 .UNSPECIFIED. ) ;
#33831=CARTESIAN_POINT ( 'NONE',  ( 117.8632207241439289, -2.443475742715334853, -17.86549347949429389 ) ) ;
#33832=CARTESIAN_POINT ( 'NONE',  ( 117.6747548109119919, -7.643976991954077427, -18.09477374809248928 ) ) ;
#33833=CARTESIAN_POINT ( 'NONE',  ( 115.8027748109119841, -8.899110576539710493, -16.42337572283490132 ) ) ;
#33834=CARTESIAN_POINT ( 'NONE',  ( 127.0066334552966651, -0.006442243401518138457, -11.04793111752537094 ) ) ;
#33835=ORIENTED_EDGE ( 'NONE', *, *, #5573, .T. ) ;
#33837=CARTESIAN_POINT ( 'NONE',  ( 118.9227414775786542, 0.4262465694468514643, -12.03445270309931736 ) ) ;
#33839=CARTESIAN_POINT ( 'NONE',  ( 113.3635281442453504, -0.1624402480850797581, -16.17319339645315424 ) ) ;
#33843=CARTESIAN_POINT ( 'NONE',  ( 122.6099748109119929, -9.261995988541697145, -16.69588392320189030 ) ) ;
#33844=CARTESIAN_POINT ( 'NONE',  ( 125.9001214775786224, -5.574606645277164318, -18.38911715685844683 ) ) ;
#33845=ORIENTED_EDGE ( 'NONE', *, *, #7441, .F. ) ;
#33847=CARTESIAN_POINT ( 'NONE',  ( 113.3277860444392076, -1.267766418764742165, -16.93314635290707315 ) ) ;
#33849=CARTESIAN_POINT ( 'NONE',  ( 111.8319081442453182, -5.638512984488999180, -18.83840828888717311 ) ) ;
#33850=CARTESIAN_POINT ( 'NONE',  ( 119.7736414775786358, 0.1319031606808879209, -14.10382304977623669 ) ) ;
#33855=CARTESIAN_POINT ( 'NONE',  ( 112.8529881442453302, -7.894159318335828068, -9.358103419637847864 ) ) ;
#33857=CARTESIAN_POINT ( 'NONE',  ( 117.4585358072985315, 0.3208234527006367798, -15.99825685930877839 ) ) ;
#33859=CARTESIAN_POINT ( 'NONE',  ( 125.5597614775786326, -1.561330072975669392, -17.79121239304076951 ) ) ;
#33860=CARTESIAN_POINT ( 'NONE',  ( 122.8936081442453059, 0.2603800115204892296, -16.42320221600525088 ) ) ;
#33862=CARTESIAN_POINT ( 'NONE',  ( 121.2485348109119769, -0.4660016031367893996, -10.09054647747474043 ) ) ;
#33863=CARTESIAN_POINT ( 'NONE',  ( 112.5126281442453120, -10.30919188438810075, -12.61870101168855918 ) ) ;
#33865=CARTESIAN_POINT ( 'NONE',  ( 114.5547881442453217, -4.153390946401321671, -8.397313243818183892 ) ) ;
#33867=CARTESIAN_POINT ( 'NONE',  ( 111.4348214775786801, -3.505236298600246325, -18.68346056562440793 ) ) ;
#33868=CARTESIAN_POINT ( 'NONE',  ( 124.7088614775786226, 0.2603800115204892296, -16.42320221600525088 ) ) ;
#33869=CARTESIAN_POINT ( 'NONE',  ( 115.6325948109119821, 0.2603800115204892296, -16.42320221600525088 ) ) ;
#33870=CARTESIAN_POINT ( 'NONE',  ( 113.0798948109119948, -8.899110576539710493, -16.42337572283490132 ) ) ;
#33872=CARTESIAN_POINT ( 'NONE',  ( 116.3133148109120043, -2.084020599724406786, -8.691656652584148546 ) ) ;
#33874=FACE_OUTER_BOUND ( 'NONE', #28777, .T. ) ;
#33876=CARTESIAN_POINT ( 'NONE',  ( 123.3474214775786209, -0.1624402480850797581, -16.17319339645315424 ) ) ;
#33881=CARTESIAN_POINT ( 'NONE',  ( 125.6164881442453094, 0.2603800115204892296, -16.42320221600525088 ) ) ;
#33883=CARTESIAN_POINT ( 'NONE',  ( 112.5126281442453120, -10.30919188438810075, -12.61870101168855918 ) ) ;
#33888=DIRECTION ( 'NONE',  ( -1.000000000000000000, 0.000000000000000000, 0.000000000000000000 ) ) ;
#33889=CARTESIAN_POINT ( 'NONE',  ( 137.4419881480160370, -6.036542153170629810, -18.33154758575252430 ) ) ;
#33891=DIRECTION ( 'NONE',  ( 0.000000000000000000, 0.6004852223388321697, -0.7996358532186279566 ) ) ;
#33892=CARTESIAN_POINT ( 'NONE',  ( 124.9357681442453014, -1.834011780172310813, -8.268836392978581529 ) ) ;
#33893=CARTESIAN_POINT ( 'NONE',  ( 122.3263414775786373, -3.505236298600246325, -18.68346056562440793 ) ) ;
#33895=ORIENTED_EDGE ( 'NONE', *, *, #40728, .T. ) ;
#33896=CARTESIAN_POINT ( 'NONE',  ( 123.5176014775786228, -9.261995988541697145, -16.69588392320189030 ) ) ;
#33897=CARTESIAN_POINT ( 'NONE',  ( 120.8514481442452961, -7.893985811506177619, -18.51759400769804742 ) ) ;
#33898=CARTESIAN_POINT ( 'NONE',  ( 126.1270281442452870, -10.30919188438810075, -12.61870101168855918 ) ) ;
#33899=CARTESIAN_POINT ( 'NONE',  ( 113.4769814775786614, -10.63000616557722466, -14.87417383870573495 ) ) ;
#33900=CARTESIAN_POINT ( 'NONE',  ( 126.5241148109119393, -9.565557343593413364, -10.61323700422348004 ) ) ;
#33901=CARTESIAN_POINT ( 'NONE',  ( 125.0492214775786266, -6.344957434206665248, -7.627207830600338134 ) ) ;
#33905=CARTESIAN_POINT ( 'NONE',  ( 115.5191414775786569, -6.222761293078241884, -8.102969835052219238 ) ) ;
#33906=CARTESIAN_POINT ( 'NONE',  ( 118.2420214775786320, -6.222761293078241884, -8.102969835052219238 ) ) ;
#33911=CARTESIAN_POINT ( 'NONE',  ( 113.7606148109119886, -1.561330072975668060, -17.79121239304076596 ) ) ;
#33916=CARTESIAN_POINT ( 'NONE',  ( 123.3152181068994651, -2.449738653808077427, -15.35887260493897344 ) ) ;
#33918=EDGE_CURVE ( 'NONE', #43250, #34606, #6028, .T. ) ;
#33919=VERTEX_POINT ( 'NONE', #7362 ) ;
#33920=CARTESIAN_POINT ( 'NONE',  ( 117.7882081442453170, -6.344957434206665248, -7.627207830600338134 ) ) ;
#33921=CARTESIAN_POINT ( 'NONE',  ( 122.6667014775786413, -2.084020599724406786, -8.691656652584148546 ) ) ;
#33922=CARTESIAN_POINT ( 'NONE',  ( 119.4900081442453086, -7.643976991954077427, -18.09477374809248928 ) ) ;
#33925=CARTESIAN_POINT ( 'NONE',  ( 120.9649014775786355, -3.383040157471821630, -19.15922257007629170 ) ) ;
#33926=EDGE_CURVE ( 'NONE', #20193, #44110, #32362, .T. ) ;
#33927=CARTESIAN_POINT ( 'NONE',  ( 119.5467348109119712, -4.089484607189486809, -7.948022111789456723 ) ) ;
#33930=CARTESIAN_POINT ( 'NONE',  ( 111.6617281442453304, 0.4262465694468514643, -12.03445270309931736 ) ) ;
#33931=B_SPLINE_CURVE_WITH_KNOTS ( 'NONE', 3,
 ( #1930, #15627, #15857, #19042, #36131, #2146, #12212, #33154, #22461, #39347 ),
 .UNSPECIFIED., .F., .F.,
 ( 4, 3, 3, 4 ),
 ( 0.000000000000000000, 0.0001671877548681235048, 0.0003343755096277620112, 0.0006463528481650609656 ),
 .UNSPECIFIED. ) ;
#33934=CARTESIAN_POINT ( 'NONE',  ( 116.1998614775786507, -10.63000616557722466, -14.87417383870573495 ) ) ;
#33935=CARTESIAN_POINT ( 'NONE',  ( 113.2500748109119968, -3.505236298600246325, -18.68346056562440793 ) ) ;
#33938=CARTESIAN_POINT ( 'NONE',  ( 113.8740681442453138, 0.5811942927096154232, -14.16772938898807155 ) ) ;
#33940=CARTESIAN_POINT ( 'NONE',  ( 120.7947214775786193, -9.261995988541697145, -16.69588392320189030 ) ) ;
#33942=CARTESIAN_POINT ( 'NONE',  ( 113.5337081442453240, -0.8288870151387760510, -10.36305467784173118 ) ) ;
#33945=CARTESIAN_POINT ( 'NONE',  ( 151.2860562277021472, -4.863998795839242995, -13.39321520033831447 ) ) ;
#33946=CARTESIAN_POINT ( 'NONE',  ( 117.5613014775786525, -10.15424416112533912, -14.75197769757731336 ) ) ;
#33947=ADVANCED_FACE ( 'NONE', ( #10881 ), #10659, .T. ) ;
#33949=CARTESIAN_POINT ( 'NONE',  ( 123.6834074775628380, -4.587599304697977054, -15.01040869781757081 ) ) ;
#33950=CARTESIAN_POINT ( 'NONE',  ( 116.7104014775786425, -8.899110576539710493, -16.42337572283490132 ) ) ;
#33952=VECTOR ( 'NONE', #10557, 1000.000000000000000 ) ;
#33953=CARTESIAN_POINT ( 'NONE',  ( 114.3278814775786429, 0.1319031606808879209, -14.10382304977623669 ) ) ;
#33954=CARTESIAN_POINT ( 'NONE',  ( 115.4056881442453459, -7.893985811506177619, -18.51759400769804742 ) ) ;
#33956=CARTESIAN_POINT ( 'NONE',  ( 113.0231681442453322, 0.9020085738987339008, -11.91225656197089222 ) ) ;
#33957=CARTESIAN_POINT ( 'NONE',  ( 116.8805814775786445, -3.505236298600246325, -18.68346056562440793 ) ) ;
#33958=CARTESIAN_POINT ( 'NONE',  ( 122.6667014775786413, -7.893985811506177619, -18.51759400769804742 ) ) ;
#33959=CARTESIAN_POINT ( 'NONE',  ( 116.8805814775786445, -3.505236298600246325, -18.68346056562440793 ) ) ;
#33961=CARTESIAN_POINT ( 'NONE',  ( 113.1366214775786432, -1.834011780172310813, -8.268836392978581529 ) ) ;
#33967=CARTESIAN_POINT ( 'NONE',  ( 120.4543614775786295, -4.089484607189486809, -7.948022111789456723 ) ) ;
#33969=CARTESIAN_POINT ( 'NONE',  ( 124.5954081442453116, -3.383040157471821630, -19.15922257007629170 ) ) ;
#33971=CARTESIAN_POINT ( 'NONE',  ( 114.5547881442453217, -4.153390946401321671, -8.397313243818183892 ) ) ;
#33973=VECTOR ( 'NONE', #6138, 1000.000000000000000 ) ;
#33974=CARTESIAN_POINT ( 'NONE',  ( 123.8579614775786126, 0.5811942927096110934, -14.16772938898807510 ) ) ;
#33979=CARTESIAN_POINT ( 'NONE',  ( 124.0281414775786146, -7.643976991954077427, -18.09477374809248928 ) ) ;
#33980=CARTESIAN_POINT ( 'NONE',  ( 118.1285681442453068, -7.893985811506177619, -18.51759400769804742 ) ) ;
#33982=CARTESIAN_POINT ( 'NONE',  ( 116.7671281442453335, -1.834011780172310813, -8.268836392978581529 ) ) ;
#33984=CARTESIAN_POINT ( 'NONE',  ( 125.5030348109119558, -6.222761293078241884, -8.102969835052219238 ) ) ;
#33985=CARTESIAN_POINT ( 'NONE',  ( 119.6601881442453106, -1.833838273342659253, -17.42832698103878286 ) ) ;
#33987=EDGE_CURVE ( 'NONE', #29206, #38146, #7055, .T. ) ;
#33988=CARTESIAN_POINT ( 'NONE',  ( 120.0005481442453146, -5.638512984489026714, -18.83840828888716956 ) ) ;
#33990=CARTESIAN_POINT ( 'NONE',  ( 113.4202548109119846, -10.30919188438810075, -12.61870101168855918 ) ) ;
#33991=CARTESIAN_POINT ( 'NONE',  ( 121.1918081442452859, -10.15424416112533912, -14.75197769757731336 ) ) ;
#33994=CARTESIAN_POINT ( 'NONE',  ( 136.7478768735744552, -1.263210933052332230, -9.073952808020385064 ) ) ;
#33995=CARTESIAN_POINT ( 'NONE',  ( 119.4332814775786318, -0.4660016031367893996, -10.09054647747474043 ) ) ;
#33997=CARTESIAN_POINT ( 'NONE',  ( 115.5191414775786569, -6.222761293078241884, -8.102969835052219238 ) ) ;
#34000=ORIENTED_EDGE ( 'NONE', *, *, #9401, .T. ) ;
#34001=CARTESIAN_POINT ( 'NONE',  ( 125.1626748109119802, -0.1624402480850797581, -16.17319339645315424 ) ) ;
#34002=CARTESIAN_POINT ( 'NONE',  ( 122.4965214775786251, 0.1319031606808879209, -14.10382304977623669 ) ) ;
#34005=VERTEX_POINT ( 'NONE', #11326 ) ;
#34006=CARTESIAN_POINT ( 'NONE',  ( 122.3830681442452857, -8.166667518702819706, -8.995218007635861213 ) ) ;
#34008=CARTESIAN_POINT ( 'NONE',  ( 120.6812681442452941, -10.30919188438810075, -12.61870101168855918 ) ) ;
#34009=CARTESIAN_POINT ( 'NONE',  ( 117.6180281442453150, -0.4660016031367893996, -10.09054647747474043 ) ) ;
#34010=CARTESIAN_POINT ( 'NONE',  ( 119.8303681442453126, 0.4262465694468514643, -12.03445270309931736 ) ) ;
#34011=EDGE_CURVE ( 'NONE', #17200, #40452, #9068, .T. ) ;
#34013=CARTESIAN_POINT ( 'NONE',  ( 124.3117748109119844, 0.1319031606808879209, -14.10382304977623669 ) ) ;
#34014=CARTESIAN_POINT ( 'NONE',  ( 112.5126281442453120, -10.30919188438810075, -12.61870101168855918 ) ) ;
#34016=CARTESIAN_POINT ( 'NONE',  ( 124.9357681442453014, -7.643976991954077427, -18.09477374809248928 ) ) ;
#34023=CARTESIAN_POINT ( 'NONE',  ( 121.7590748109119687, -7.893985811506177619, -18.51759400769804742 ) ) ;
#34024=CARTESIAN_POINT ( 'NONE',  ( 121.1918081442452859, -10.15424416112533912, -14.75197769757731336 ) ) ;
#34026=CARTESIAN_POINT ( 'NONE',  ( 124.2550481442452792, -9.988377603198980381, -10.36322818467138518 ) ) ;
#34027=CARTESIAN_POINT ( 'NONE',  ( 113.0231681442453180, -10.15424416112533912, -14.75197769757731336 ) ) ;
#34028=CARTESIAN_POINT ( 'NONE',  ( 121.5437981415388862, -0.1020945015694968705, -15.74893487844867757 ) ) ;
#34029=CARTESIAN_POINT ( 'NONE',  ( 120.7379948109119709, -10.63000616557722466, -14.87417383870573495 ) ) ;
#34030=CARTESIAN_POINT ( 'NONE',  ( 120.5110881442453206, -6.344957434206665248, -7.627207830600338134 ) ) ;
#34032=CARTESIAN_POINT ( 'NONE',  ( 126.0703014775786102, -0.1624402480850797581, -16.17319339645315424 ) ) ;
#34034=ORIENTED_EDGE ( 'NONE', *, *, #2161, .F. ) ;
#34035=LINE ( 'NONE', #17397, #21559 ) ;
#34036=CARTESIAN_POINT ( 'NONE',  ( 118.6950019144190520, -1.220279397241701647, -16.99638242193885418 ) ) ;
#34037=CARTESIAN_POINT ( 'NONE',  ( 124.3117748109119844, 0.1319031606808879209, -14.10382304977623669 ) ) ;
#34040=CARTESIAN_POINT ( 'NONE',  ( 118.4689281442453250, -10.15424416112533912, -14.75197769757731336 ) ) ;
#34042=CARTESIAN_POINT ( 'NONE',  ( 117.7314814775786260, -5.574606645277164318, -18.38911715685844683 ) ) ;
#34043=CARTESIAN_POINT ( 'NONE',  ( 122.3263414775786373, -6.344957434206665248, -7.627207830600338134 ) ) ;
#34044=EDGE_LOOP ( 'NONE', ( #15569, #35916, #26489, #42804 ) ) ;
#34046=CARTESIAN_POINT ( 'NONE',  ( 120.7947214775786193, -0.8288870151387760510, -10.36305467784173118 ) ) ;
#34047=CARTESIAN_POINT ( 'NONE',  ( 120.0005481442453146, -5.638512984488999180, -18.83840828888717311 ) ) ;
#34048=CARTESIAN_POINT ( 'NONE',  ( 124.8223148109119762, 0.9020085738987339008, -11.91225656197089222 ) ) ;
#34049=CARTESIAN_POINT ( 'NONE',  ( 124.2550481442452792, -0.1624402480850797581, -16.17319339645315424 ) ) ;
#34050=VERTEX_POINT ( 'NONE', #26127 ) ;
#34053=CARTESIAN_POINT ( 'NONE',  ( 125.2194014775786286, -10.30919188438810075, -12.61870101168855918 ) ) ;
#34054=CARTESIAN_POINT ( 'NONE',  ( 114.1577014775786552, -3.505236298600246325, -18.68346056562440793 ) ) ;
#34056=CARTESIAN_POINT ( 'NONE',  ( 125.2761281442453054, -10.63000616557722466, -14.87417383870573495 ) ) ;
#34065=CARTESIAN_POINT ( 'NONE',  ( 123.3474214775786209, -0.1624402480850797581, -16.17319339645315424 ) ) ;
#34066=CARTESIAN_POINT ( 'NONE',  ( 114.7816948109119863, -9.859900752359374465, -12.68260735090039404 ) ) ;
#34067=CARTESIAN_POINT ( 'NONE',  ( 126.7858337141697689, -6.477483175330938536, -18.42452263347122354 ) ) ;
#34070=CARTESIAN_POINT ( 'NONE',  ( 118.9794681442453026, -0.8288870151387760510, -10.36305467784173118 ) ) ;
#34071=CARTESIAN_POINT ( 'NONE',  ( 114.1577014775786552, -3.505236298600246325, -18.68346056562440793 ) ) ;
#34073=CARTESIAN_POINT ( 'NONE',  ( 111.4348214775786801, -3.505236298600246325, -18.68346056562440793 ) ) ;
#34075=CARTESIAN_POINT ( 'NONE',  ( 125.1626748109119802, -9.988377603198980381, -10.36322818467138518 ) ) ;
#34076=CARTESIAN_POINT ( 'NONE',  ( 125.0492214775786266, -3.505236298600246325, -18.68346056562440793 ) ) ;
#34078=CARTESIAN_POINT ( 'NONE',  ( 112.8529881442453302, -1.561330072975668060, -17.79121239304076596 ) ) ;
#34081=CARTESIAN_POINT ( 'NONE',  ( 123.6310548109119765, -4.153390946401325223, -8.397313243818185668 ) ) ;
#34082=CARTESIAN_POINT ( 'NONE',  ( 119.2631014775786298, -9.565557343593413364, -10.61323700422348004 ) ) ;
#34087=CARTESIAN_POINT ( 'NONE',  ( 112.8529881442453302, -7.894159318335819187, -9.358103419637840759 ) ) ;
#34090=CARTESIAN_POINT ( 'NONE',  ( 117.6180281442453150, -0.4660016031367954503, -10.09054647747473155 ) ) ;
#34092=CARTESIAN_POINT ( 'NONE',  ( 123.9146881442452894, 0.9020085738987339008, -11.91225656197089222 ) ) ;
#34093=CARTESIAN_POINT ( 'NONE',  ( 121.9292548109119849, -1.561330072975668948, -17.79121239304076951 ) ) ;
#34095=CARTESIAN_POINT ( 'NONE',  ( 118.5823814775786360, -1.834011780172310813, -8.268836392978581529 ) ) ;
#34098=CARTESIAN_POINT ( 'NONE',  ( 115.0653281442453277, -3.505236298600246325, -18.68346056562440793 ) ) ;
#34099=CARTESIAN_POINT ( 'NONE',  ( 112.0020881442453344, -9.565557343593413364, -10.61323700422348004 ) ) ;
#34100=CARTESIAN_POINT ( 'NONE',  ( 122.2696148109119889, -4.089484607189486809, -7.948022111789456723 ) ) ;
#34101=CARTESIAN_POINT ( 'NONE',  ( 112.7395348109119766, -5.638512984488999180, -18.83840828888717311 ) ) ;
#34102=( BOUNDED_CURVE ( )  B_SPLINE_CURVE ( 2, ( #29353, #39844, #35957, #5171, #32754 ),
 .UNSPECIFIED., .F., .T. ) 
 B_SPLINE_CURVE_WITH_KNOTS ( ( 3, 2, 3 ),
 ( 5.122041608693530667E-06, 0.007812500000000000000, 0.01412175834311804080 ),
 .UNSPECIFIED. ) 
 CURVE ( )  GEOMETRIC_REPRESENTATION_ITEM ( )  RATIONAL_B_SPLINE_CURVE ( ( 0.9999002530354920149, 0.9239294387131110620, 1.000000000000000000, 0.9385262470930929579, 0.9763430640193200283 ) ) 
 REPRESENTATION_ITEM ( '' )  );
#34103=CARTESIAN_POINT ( 'NONE',  ( 111.4348214775786801, -3.505236298600246325, -18.68346056562440793 ) ) ;
#34105=CARTESIAN_POINT ( 'NONE',  ( 118.2420214775786320, -6.222761293078241884, -8.102969835052219238 ) ) ;
#34106=CARTESIAN_POINT ( 'NONE',  ( 112.2857214775786474, -4.089484607189486809, -7.948022111789456723 ) ) ;
#34108=CARTESIAN_POINT ( 'NONE',  ( 124.6521348109119884, -7.894159318335828068, -9.358103419637847864 ) ) ;
#34113=LINE ( 'NONE', #45065, #7492 ) ;
#34114=CARTESIAN_POINT ( 'NONE',  ( 125.0492214775786266, -6.344957434206665248, -7.627207830600338134 ) ) ;
#34122=CARTESIAN_POINT ( 'NONE',  ( 119.6034614775786196, -6.344957434206665248, -7.627207830600338134 ) ) ;
#34125=CARTESIAN_POINT ( 'NONE',  ( 125.7866681442452688, -0.4660016031367893996, -10.09054647747474043 ) ) ;
#34126=CARTESIAN_POINT ( 'NONE',  ( 120.1707281442453166, -9.565557343593413364, -10.61323700422348004 ) ) ;
#34129=CARTESIAN_POINT ( 'NONE',  ( 125.3328548109119964, -9.261995988541697145, -16.69588392320189030 ) ) ;
#34130=CARTESIAN_POINT ( 'NONE',  ( 121.0783548109119749, 0.2603800115204892296, -16.42320221600525088 ) ) ;
#34132=CARTESIAN_POINT ( 'NONE',  ( 116.1431348109119881, 0.1319031606808879209, -14.10382304977623669 ) ) ;
#34133=CARTESIAN_POINT ( 'NONE',  ( 123.9714148109119805, -0.4660016031367893996, -10.09054647747474043 ) ) ;
#34137=CARTESIAN_POINT ( 'NONE',  ( 115.4624148109119943, -4.153390946401321671, -8.397313243818183892 ) ) ;
#34138=CARTESIAN_POINT ( 'NONE',  ( 115.1787814775786387, -0.1624402480850797581, -16.17319339645315424 ) ) ;
#34142=CARTESIAN_POINT ( 'NONE',  ( 111.5125327111057345, -1.267766418764825875, -16.93314635290698789 ) ) ;
#34143=CARTESIAN_POINT ( 'NONE',  ( 114.5547881442453217, -5.638512984488999180, -18.83840828888717311 ) ) ;
#34144=CARTESIAN_POINT ( 'NONE',  ( 112.8729331642484510, -2.215723800389698184, -18.16877924232191788 ) ) ;
#34151=CARTESIAN_POINT ( 'NONE',  ( 116.8238548109119819, -4.089484607189486809, -7.948022111789456723 ) ) ;
#34152=CARTESIAN_POINT ( 'NONE',  ( 114.3846081442453197, -10.63000616557722466, -14.87417383870573495 ) ) ;
#34154=CARTESIAN_POINT ( 'NONE',  ( 118.8660148109119774, 0.1319031606808879209, -14.10382304977623669 ) ) ;
#34156=CARTESIAN_POINT ( 'NONE',  ( 120.2274548109119934, 0.5811942927096110934, -14.16772938898807510 ) ) ;
#34157=CARTESIAN_POINT ( 'NONE',  ( 118.0718414775786300, -9.261995988541697145, -16.69588392320189030 ) ) ;
#34159=CARTESIAN_POINT ( 'NONE',  ( 112.2857214775786474, -5.574606645277164318, -18.38911715685844683 ) ) ;
#34161=ORIENTED_EDGE ( 'NONE', *, *, #1470, .T. ) ;
#34162=CARTESIAN_POINT ( 'NONE',  ( 119.3765548109119834, 0.9020085738987339008, -11.91225656197089222 ) ) ;
#34164=CARTESIAN_POINT ( 'NONE',  ( 113.9875214775786532, -0.4660016031367893996, -10.09054647747474043 ) ) ;
#34166=CARTESIAN_POINT ( 'NONE',  ( 121.9292548109119849, -1.561330072975668948, -17.79121239304076951 ) ) ;
#34167=CARTESIAN_POINT ( 'NONE',  ( 110.2184548109119788, -6.243778871467079661, -12.80482167309617125 ) ) ;
#34170=CARTESIAN_POINT ( 'NONE',  ( 116.7671281442453335, -7.643976991954077427, -18.09477374809248928 ) ) ;
#34172=CARTESIAN_POINT ( 'NONE',  ( 117.2209414775786485, -2.084020599724406786, -8.691656652584148546 ) ) ;
#34174=CARTESIAN_POINT ( 'NONE',  ( 116.1431348109119881, 0.1319031606808879209, -14.10382304977623669 ) ) ;
#34175=CARTESIAN_POINT ( 'NONE',  ( 115.3489614775786407, -9.261995988541697145, -16.69588392320189030 ) ) ;
#34178=CARTESIAN_POINT ( 'NONE',  ( 113.3635281442453504, -9.988377603198976828, -10.36322818467138340 ) ) ;
#34179=CARTESIAN_POINT ( 'NONE',  ( 116.4267681442453153, -6.222761293078241884, -8.102969835052219238 ) ) ;
#34180=CARTESIAN_POINT ( 'NONE',  ( 113.4769814775786330, 0.4262465694468514643, -12.03445270309931736 ) ) ;
#34181=CARTESIAN_POINT ( 'NONE',  ( 116.2565881442453133, -0.8288870151387760510, -10.36305467784173118 ) ) ;
#34183=CARTESIAN_POINT ( 'NONE',  ( 112.5126281442453120, -10.30919188438810075, -12.61870101168855918 ) ) ;
#34189=CARTESIAN_POINT ( 'NONE',  ( 117.4478481442453131, 0.2603800115204892296, -16.42320221600525088 ) ) ;
#34192=CARTESIAN_POINT ( 'NONE',  ( 124.9924948109119924, -4.089484607189473486, -7.948022111789465605 ) ) ;
#34193=CARTESIAN_POINT ( 'NONE',  ( 118.9794681442453026, -0.8288870151387760510, -10.36305467784173118 ) ) ;
#34194=CARTESIAN_POINT ( 'NONE',  ( 128.2184548109119930, 1.087851763053662602, -12.63461456455805276 ) ) ;
#34195=CARTESIAN_POINT ( 'NONE',  ( 123.9146881442452894, 0.9020085738987339008, -11.91225656197089222 ) ) ;
#34200=CARTESIAN_POINT ( 'NONE',  ( 120.7947214775786193, -0.8288870151387760510, -10.36305467784173118 ) ) ;
#34201=CARTESIAN_POINT ( 'NONE',  ( 119.6601881442453106, -8.166667518702819706, -8.995218007635861213 ) ) ;
#34202=CARTESIAN_POINT ( 'NONE',  ( 118.3554748109119998, -9.565557343593413364, -10.61323700422348004 ) ) ;
#34203=CARTESIAN_POINT ( 'NONE',  ( 118.9794681442453026, -9.261995988541697145, -16.69588392320189030 ) ) ;
#34207=CARTESIAN_POINT ( 'NONE',  ( 122.0427081442452817, -9.859900752359378018, -12.68260735090039759 ) ) ;
#34208=ORIENTED_EDGE ( 'NONE', *, *, #33926, .F. ) ;
#34213=CARTESIAN_POINT ( 'NONE',  ( 117.1074881442453233, -10.63000616557722466, -14.87417383870573495 ) ) ;
#34214=CARTESIAN_POINT ( 'NONE',  ( 121.3052614775786111, -7.643976991954077427, -18.09477374809248928 ) ) ;
#34217=CARTESIAN_POINT ( 'NONE',  ( 137.1886586612299652, -0.1096322012115264061, -11.00619489583255906 ) ) ;
#34218=CARTESIAN_POINT ( 'NONE',  ( 119.7736414775786358, -10.30919188438810075, -12.61870101168855918 ) ) ;
#34220=CARTESIAN_POINT ( 'NONE',  ( 121.1350814775786233, -9.859900752359378018, -12.68260735090039759 ) ) ;
#34221=ORIENTED_EDGE ( 'NONE', *, *, #2130, .F. ) ;
#34224=CARTESIAN_POINT ( 'NONE',  ( 124.9357681442453014, -7.643976991954077427, -18.09477374809248928 ) ) ;
#34225=CARTESIAN_POINT ( 'NONE',  ( 125.2761281442453054, 0.4262465694468514643, -12.03445270309931736 ) ) ;
#34229=CARTESIAN_POINT ( 'NONE',  ( 120.4543614775786295, -4.089484607189486809, -7.948022111789456723 ) ) ;
#34233=CARTESIAN_POINT ( 'NONE',  ( 120.6245414775786458, -9.988377603198976828, -10.36322818467138340 ) ) ;
#34234=CARTESIAN_POINT ( 'NONE',  ( 117.4478481442453131, 0.2603800115204892296, -16.42320221600525088 ) ) ;
#34235=CARTESIAN_POINT ( 'NONE',  ( 120.7947214775786193, -0.8288870151387760510, -10.36305467784173118 ) ) ;
#34237=CARTESIAN_POINT ( 'NONE',  ( 117.4478481442453131, 0.2603800115204892296, -16.42320221600525088 ) ) ;
#34240=CARTESIAN_POINT ( 'NONE',  ( 123.8579614775786126, -9.859900752359378018, -12.68260735090039759 ) ) ;
#34247=CARTESIAN_POINT ( 'NONE',  ( 123.2339681442453241, -6.344957434206665248, -7.627207830600338134 ) ) ;
#34248=CARTESIAN_POINT ( 'NONE',  ( 122.7234281442452755, -4.153390946401325223, -8.397313243818185668 ) ) ;
#34249=ORIENTED_EDGE ( 'NONE', *, *, #12793, .T. ) ;
#34250=CARTESIAN_POINT ( 'NONE',  ( 124.3117748109119844, -10.30919188438810075, -12.61870101168855918 ) ) ;
#34251=CARTESIAN_POINT ( 'NONE',  ( 112.3424481442453384, -3.505236298600246325, -18.68346056562440793 ) ) ;
#34253=CARTESIAN_POINT ( 'NONE',  ( 121.9292548109119849, -1.561330072975668948, -17.79121239304076951 ) ) ;
#34254=CARTESIAN_POINT ( 'NONE',  ( 120.1140014775786398, -1.561330072975668504, -17.79121239304076951 ) ) ;
#34256=CARTESIAN_POINT ( 'NONE',  ( 125.9568481442452850, -3.505236298600246325, -18.68346056562440793 ) ) ;
#34257=CARTESIAN_POINT ( 'NONE',  ( 111.7184548109119788, -9.261995988541697145, -16.69588392320189030 ) ) ;
#34260=DIRECTION ( 'NONE',  ( 1.000000000000000000, 0.000000000000000000, 0.000000000000000000 ) ) ;
#34261=CARTESIAN_POINT ( 'NONE',  ( 113.2500748109119968, -3.505236298600246325, -18.68346056562440793 ) ) ;
#34262=CARTESIAN_POINT ( 'NONE',  ( 122.2128881442453263, -7.643976991954077427, -18.09477374809248928 ) ) ;
#34265=AXIS2_PLACEMENT_3D ( 'NONE', #30596, #44513, #37663 ) ;
#34266=CARTESIAN_POINT ( 'NONE',  ( 123.0637881442452937, -8.899110576539710493, -16.42337572283490132 ) ) ;
#34267=CARTESIAN_POINT ( 'NONE',  ( 114.7249681442453237, -9.565557343593413364, -10.61323700422348004 ) ) ;
#34268=CARTESIAN_POINT ( 'NONE',  ( 111.7184548109119788, -0.8288870151387760510, -10.36305467784173118 ) ) ;
#34271=CARTESIAN_POINT ( 'NONE',  ( 122.6667014775786413, -2.084020599724406786, -8.691656652584148546 ) ) ;
#34272=CARTESIAN_POINT ( 'NONE',  ( 118.4689281442453392, 0.9020085738987339008, -11.91225656197089222 ) ) ;
#34278=CARTESIAN_POINT ( 'NONE',  ( 116.0296814775786345, -1.833838273342658809, -17.42832698103878286 ) ) ;
#34279=CARTESIAN_POINT ( 'NONE',  ( 113.8173414775786512, -9.565557343593413364, -10.61323700422348004 ) ) ;
#34280=( BOUNDED_SURFACE ( )  B_SPLINE_SURFACE ( 1, 2, ( 
 ( #30393, #13523, #27204, #34251, #5750, #6219, #26751, #41122, #2335, #3024, #43854, #16947, #40433, #23566, #9413, #34027, #26970, #30841, #19670, #30168, #44764, #23324, #37210, #37447, #9644, #9881, #5982, #2795, #44315, #19907, #33792, #2564, #13071, #20142, #30617, #44534, #13296, #23791, #8503, #22407, #36077, #2322, #19215, #26735, #12608, #19656, #15343, #8955, #36300, #26510, #25827, #36966, #8279, #8722, #22855, #22628, #1423, #4848, #40418, #33543, #39960, #5299, #18984, #16019, #29927, #36526, #5068, #22181, #26281, #18767, #5737, #43841, #9178, #23085, #15566, #29470, #15794, #29252, #1642, #36746, #16250, #40189, #32656, #5514, #32873, #30153, #43161, #44069, #12835, #39734, #43385, #26056, #12153, #11929, #33095, #1865, #29696, #43607, #12383, #19434, #33319, #2093, #31044, #27188, #30600, #19891, #6203, #34672, #9866, #20573, #27640, #16931, #23550, #44974, #20792, #23775, #36, #13509, #2548, #13948, #13282, #24216, #3231, #37667, #26954, #16475, #34450, #13055, #33778, #23999, #37887, #20125, #30378, #41108, #44517, #34010, #40876, #44300, #13731, #6442, #2781, #37193, #40643, #9629, #37433, #16706, #23309, #3458, #20351, #9398, #41554, #6882, #34235, #41337, #3009, #10314, #30826, #38107, #5967, #44750, #10096, #27417, #6663, #17157, #17375, #31263, #14389, #24877, #38538, #35567, #4340, #28301, #24653, #41771, #694, #10531, #11429, #18260, #924, #32156, #35111, #3892, #35339, #34883, #21232, #11201, #14843, #14614, #24430, #25106, #7313, #25334, #3671, #39227, #28753, #255, #17812, #476, #31706, #38322, #42213, #42658, #7992, #10974, #7539, #38769, #21900, #10755, #35794, #21456, #4111, #7099, #18032, #4566, #31929, #7772, #18490, #28531, #42437, #32380, #1147, #39002, #27861, #21679, #17592, #21009, #31485, #14164, #28082, #41990, #1372, #22129, #8897, #32602, #8223, #43555, #12323, #25777, #39459, #32818, #18931, #39684, #15284, #36022, #5459, #36473, #26223, #9122, #36913, #42883, #15064, #15739, #29416, #19379, #18711, #12099, #26003 ),
 ( #19156, #4790, #43330, #33487, #29641, #33267, #8668, #5013, #28978, #23026, #5240, #29191, #40132, #2042, #8449, #22352, #33037, #43103, #36246, #5684, #1812, #29869, #22795, #11873, #1588, #15509, #39907, #11644, #36689, #19603, #25553, #22571, #15965, #43784, #12549, #26456, #40358, #6148, #10039, #7206, #37609, #23719, #16193, #37826, #13455, #16422, #370, #2951, #14281, #9347, #44244, #13228, #23946, #44463, #21119, #41053, #10868, #44013, #2265, #6383, #30541, #30097, #9810, #20291, #34175, #33954, #24763, #16878, #13002, #27129, #38654, #3777, #27359, #26900, #40821, #12775, #17701, #9576, #23492, #7423, #28200, #30769, #33723, #34993, #31601, #30318, #42105, #21344, #44695, #26677, #20068, #40588, #41279, #23256, #2721, #37140, #5914, #19836, #2493, #37378, #16647, #31823, #14955, #32271, #813, #594, #18150, #35228, #18820, #39796, #18383, #28417, #28867, #7886, #15176, #32711, #25891, #42779, #4003, #36136, #35457, #24990, #4462, #1484, #32045, #14504, #8339, #8118, #22239, #25448, #42550, #29082, #17925, #42328, #35913, #39350, #11089, #1038, #11541, #11311, #38885, #8565, #7654, #4231, #14732, #21570, #29310, #22019, #28644, #39576, #15406, #25221, #4679, #39120, #4904, #21793, #43223, #35687, #18600, #32491, #1266, #42994, #11761, #11990, #25671, #9019, #19501, #33158, #30215, #44135, #22917, #19280, #36359, #40483, #5130, #6032, #12901, #40707, #26797, #29757, #43669, #29986, #29536, #15861, #5803, #9466, #9243, #19047, #19722, #1935, #19954, #43452, #33843, #23378, #40020, #12444, #40252, #26345, #32934, #36809, #37260, #2611, #5577, #2151, #33380, #16544, #5363, #30440, #16081, #43903, #1709, #12671, #44359, #26570, #2385, #13120, #23152, #37034, #27026, #40941, #33608, #22465, #16313, #12217, #15632, #26114, #8785, #22690, #36588, #41169, #16771, #3513, #27254, #2841, #38168, #6947, #20414, #34075, #27479, #13568, #34298, #9928, #30666, #97, #31106, #20851, #3730, #31549, #37497, #9696, #10373, #24061, #14011, #13350, #6727, #20638, #44587 ) ),
 .UNSPECIFIED., .F., .F., .F. ) 
 B_SPLINE_SURFACE_WITH_KNOTS ( ( 2, 2 ),
 ( 3, 2, 2, 2, 2, 2, 2, 2, 2, 2, 2, 2, 2, 2, 2, 2, 2, 2, 2, 2, 2, 2, 2, 2, 2, 2, 2, 2, 2, 2, 2, 2, 2, 2, 2, 2, 2, 2, 2, 2, 2, 2, 2, 2, 2, 2, 2, 2, 2, 2, 2, 2, 2, 2, 2, 2, 2, 2, 2, 2, 2, 2, 2, 2, 2, 2, 2, 2, 2, 2, 2, 2, 2, 2, 2, 2, 2, 2, 2, 2, 2, 2, 2, 2, 2, 2, 2, 2, 2, 2, 2, 2, 2, 2, 2, 2, 2, 2, 2, 2, 2, 2, 2, 2, 2, 2, 2, 2, 2, 2, 2, 2, 2, 2, 2, 2, 2, 2, 2, 2, 2, 2, 2, 2, 2, 2, 2, 2, 3 ),
 ( 0.000000000000000000, 1.000000000000000000 ),
 ( 0.000000000000000000, 0.007812500000000000000, 0.01562500000000000000, 0.02343750000000000000, 0.03125000000000000000, 0.03906250000000000000, 0.04687500000000000000, 0.05468750000000000000, 0.06250000000000000000, 0.07031250000000000000, 0.07812500000000000000, 0.08593750000000000000, 0.09375000000000000000, 0.1015625000000000000, 0.1093750000000000000, 0.1171875000000000000, 0.1250000000000000000, 0.1328125000000000000, 0.1406250000000000000, 0.1484375000000000000, 0.1562500000000000000, 0.1640625000000000000, 0.1718750000000000000, 0.1796875000000000000, 0.1875000000000000000, 0.1953125000000000000, 0.2031250000000000000, 0.2109375000000000000, 0.2187500000000000000, 0.2265625000000000000, 0.2343750000000000000, 0.2421875000000000000, 0.2500000000000000000, 0.2578125000000000000, 0.2656250000000000000, 0.2734375000000000000, 0.2812500000000000000, 0.2890625000000000000, 0.2968750000000000000, 0.3046875000000000000, 0.3125000000000000000, 0.3203125000000000000, 0.3281250000000000000, 0.3359375000000000000, 0.3437500000000000000, 0.3515625000000000000, 0.3593750000000000000, 0.3671875000000000000, 0.3750000000000000000, 0.3828125000000000000, 0.3906250000000000000, 0.3984375000000000000, 0.4062500000000000000, 0.4140625000000000000, 0.4218750000000000000, 0.4296875000000000000, 0.4375000000000000000, 0.4453125000000000000, 0.4531250000000000000, 0.4609375000000000000, 0.4687500000000000000, 0.4765625000000000000, 0.4843750000000000000, 0.4921875000000000000, 0.5000000000000000000, 0.5078125000000000000, 0.5156250000000000000, 0.5234375000000000000, 0.5312500000000000000, 0.5390625000000000000, 0.5468750000000000000, 0.5546875000000000000, 0.5625000000000000000, 0.5703125000000000000, 0.5781250000000000000, 0.5859375000000000000, 0.5937500000000000000, 0.6015625000000000000, 0.6093750000000000000, 0.6171875000000000000, 0.6250000000000000000, 0.6328125000000000000, 0.6406250000000000000, 0.6484375000000000000, 0.6562500000000000000, 0.6640625000000000000, 0.6718750000000000000, 0.6796875000000000000, 0.6875000000000000000, 0.6953125000000000000, 0.7031250000000000000, 0.7109375000000000000, 0.7187500000000000000, 0.7265625000000000000, 0.7343750000000000000, 0.7421875000000000000, 0.7500000000000000000, 0.7578125000000000000, 0.7656250000000000000, 0.7734375000000000000, 0.7812500000000000000, 0.7890625000000000000, 0.7968750000000000000, 0.8046875000000000000, 0.8125000000000000000, 0.8203125000000000000, 0.8281250000000000000, 0.8359375000000000000, 0.8437500000000000000, 0.8515625000000000000, 0.8593750000000000000, 0.8671875000000000000, 0.8750000000000000000, 0.8828125000000000000, 0.8906250000000000000, 0.8984375000000000000, 0.9062500000000000000, 0.9140625000000000000, 0.9218750000000000000, 0.9296875000000000000, 0.9375000000000000000, 0.9453125000000000000, 0.9531250000000000000, 0.9609375000000000000, 0.9687500000000000000, 0.9765625000000000000, 0.9843750000000000000, 0.9921875000000000000, 1.000000000000000000 ),
 .UNSPECIFIED. ) 
 GEOMETRIC_REPRESENTATION_ITEM ( )  RATIONAL_B_SPLINE_SURFACE ( (
 ( 1.000000000000000000, 0.9238795325112869605, 1.000000000000000000, 0.9238795325112869605, 1.000000000000000000, 0.9238795325112869605, 1.000000000000000000, 0.9238795325112869605, 1.000000000000000000, 0.9238795325112869605, 1.000000000000000000, 0.9238795325112869605, 1.000000000000000000, 0.9238795325112869605, 1.000000000000000000, 0.9238795325112869605, 1.000000000000000000, 0.9238795325112869605, 1.000000000000000000, 0.9238795325112869605, 1.000000000000000000, 0.9238795325112869605, 1.000000000000000000, 0.9238795325112869605, 1.000000000000000000, 0.9238795325112869605, 1.000000000000000000, 0.9238795325112869605, 1.000000000000000000, 0.9238795325112869605, 1.000000000000000000, 0.9238795325112869605, 1.000000000000000000, 0.9238795325112869605, 1.000000000000000000, 0.9238795325112869605, 1.000000000000000000, 0.9238795325112869605, 1.000000000000000000, 0.9238795325112869605, 1.000000000000000000, 0.9238795325112869605, 1.000000000000000000, 0.9238795325112869605, 1.000000000000000000, 0.9238795325112869605, 1.000000000000000000, 0.9238795325112869605, 1.000000000000000000, 0.9238795325112869605, 1.000000000000000000, 0.9238795325112869605, 1.000000000000000000, 0.9238795325112869605, 1.000000000000000000, 0.9238795325112869605, 1.000000000000000000, 0.9238795325112869605, 1.000000000000000000, 0.9238795325112869605, 1.000000000000000000, 0.9238795325112869605, 1.000000000000000000, 0.9238795325112869605, 1.000000000000000000, 0.9238795325112869605, 1.000000000000000000, 0.9238795325112869605, 1.000000000000000000, 0.9238795325112869605, 1.000000000000000000, 0.9238795325112869605, 1.000000000000000000, 0.9238795325112869605, 1.000000000000000000, 0.9238795325112869605, 1.000000000000000000, 0.9238795325112869605, 1.000000000000000000, 0.9238795325112869605, 1.000000000000000000, 0.9238795325112869605, 1.000000000000000000, 0.9238795325112869605, 1.000000000000000000, 0.9238795325112869605, 1.000000000000000000, 0.9238795325112869605, 1.000000000000000000, 0.9238795325112869605, 1.000000000000000000, 0.9238795325112869605, 1.000000000000000000, 0.9238795325112869605, 1.000000000000000000, 0.9238795325112869605, 1.000000000000000000, 0.9238795325112869605, 1.000000000000000000, 0.9238795325112869605, 1.000000000000000000, 0.9238795325112869605, 1.000000000000000000, 0.9238795325112869605, 1.000000000000000000, 0.9238795325112869605, 1.000000000000000000, 0.9238795325112869605, 1.000000000000000000, 0.9238795325112869605, 1.000000000000000000, 0.9238795325112869605, 1.000000000000000000, 0.9238795325112869605, 1.000000000000000000, 0.9238795325112869605, 1.000000000000000000, 0.9238795325112869605, 1.000000000000000000, 0.9238795325112869605, 1.000000000000000000, 0.9238795325112869605, 1.000000000000000000, 0.9238795325112869605, 1.000000000000000000, 0.9238795325112869605, 1.000000000000000000, 0.9238795325112869605, 1.000000000000000000, 0.9238795325112869605, 1.000000000000000000, 0.9238795325112869605, 1.000000000000000000, 0.9238795325112869605, 1.000000000000000000, 0.9238795325112869605, 1.000000000000000000, 0.9238795325112869605, 1.000000000000000000, 0.9238795325112869605, 1.000000000000000000, 0.9238795325112869605, 1.000000000000000000, 0.9238795325112869605, 1.000000000000000000, 0.9238795325112869605, 1.000000000000000000, 0.9238795325112869605, 1.000000000000000000, 0.9238795325112869605, 1.000000000000000000, 0.9238795325112869605, 1.000000000000000000, 0.9238795325112869605, 1.000000000000000000, 0.9238795325112869605, 1.000000000000000000, 0.9238795325112869605, 1.000000000000000000, 0.9238795325112869605, 1.000000000000000000, 0.9238795325112869605, 1.000000000000000000, 0.9238795325112869605, 1.000000000000000000, 0.9238795325112869605, 1.000000000000000000, 0.9238795325112869605, 1.000000000000000000, 0.9238795325112869605, 1.000000000000000000, 0.9238795325112869605, 1.000000000000000000, 0.9238795325112869605, 1.000000000000000000, 0.9238795325112869605, 1.000000000000000000, 0.9238795325112869605, 1.000000000000000000, 0.9238795325112869605, 1.000000000000000000, 0.9238795325112869605, 1.000000000000000000, 0.9238795325112869605, 1.000000000000000000, 0.9238795325112869605, 1.000000000000000000, 0.9238795325112869605, 1.000000000000000000, 0.9238795325112869605, 1.000000000000000000, 0.9238795325112869605, 1.000000000000000000, 0.9238795325112869605, 1.000000000000000000, 0.9238795325112869605, 1.000000000000000000, 0.9238795325112869605, 1.000000000000000000, 0.9238795325112869605, 1.000000000000000000, 0.9238795325112869605, 1.000000000000000000, 0.9238795325112869605, 1.000000000000000000, 0.9238795325112869605, 1.000000000000000000, 0.9238795325112869605, 1.000000000000000000, 0.9238795325112869605, 1.000000000000000000, 0.9238795325112869605, 1.000000000000000000, 0.9238795325112869605, 1.000000000000000000, 0.9238795325112869605, 1.000000000000000000, 0.9238795325112869605, 1.000000000000000000, 0.9238795325112869605, 1.000000000000000000, 0.9238795325112869605, 1.000000000000000000, 0.9238795325112869605, 1.000000000000000000, 0.9238795325112869605, 1.000000000000000000, 0.9238795325112869605, 1.000000000000000000, 0.9238795325112869605, 1.000000000000000000, 0.9238795325112869605, 1.000000000000000000, 0.9238795325112869605, 1.000000000000000000, 0.9238795325112869605, 1.000000000000000000, 0.9238795325112869605, 1.000000000000000000, 0.9238795325112869605, 1.000000000000000000, 0.9238795325112869605, 1.000000000000000000, 0.9238795325112869605, 1.000000000000000000, 0.9238795325112869605, 1.000000000000000000, 0.9238795325112869605, 1.000000000000000000, 0.9238795325112869605, 1.000000000000000000, 0.9238795325112869605, 1.000000000000000000, 0.9238795325112869605, 1.000000000000000000, 0.9238795325112869605, 1.000000000000000000),
 ( 1.000000000000000000, 0.9238795325112869605, 1.000000000000000000, 0.9238795325112869605, 1.000000000000000000, 0.9238795325112869605, 1.000000000000000000, 0.9238795325112869605, 1.000000000000000000, 0.9238795325112869605, 1.000000000000000000, 0.9238795325112869605, 1.000000000000000000, 0.9238795325112869605, 1.000000000000000000, 0.9238795325112869605, 1.000000000000000000, 0.9238795325112869605, 1.000000000000000000, 0.9238795325112869605, 1.000000000000000000, 0.9238795325112869605, 1.000000000000000000, 0.9238795325112869605, 1.000000000000000000, 0.9238795325112869605, 1.000000000000000000, 0.9238795325112869605, 1.000000000000000000, 0.9238795325112869605, 1.000000000000000000, 0.9238795325112869605, 1.000000000000000000, 0.9238795325112869605, 1.000000000000000000, 0.9238795325112869605, 1.000000000000000000, 0.9238795325112869605, 1.000000000000000000, 0.9238795325112869605, 1.000000000000000000, 0.9238795325112869605, 1.000000000000000000, 0.9238795325112869605, 1.000000000000000000, 0.9238795325112869605, 1.000000000000000000, 0.9238795325112869605, 1.000000000000000000, 0.9238795325112869605, 1.000000000000000000, 0.9238795325112869605, 1.000000000000000000, 0.9238795325112869605, 1.000000000000000000, 0.9238795325112869605, 1.000000000000000000, 0.9238795325112869605, 1.000000000000000000, 0.9238795325112869605, 1.000000000000000000, 0.9238795325112869605, 1.000000000000000000, 0.9238795325112869605, 1.000000000000000000, 0.9238795325112869605, 1.000000000000000000, 0.9238795325112869605, 1.000000000000000000, 0.9238795325112869605, 1.000000000000000000, 0.9238795325112869605, 1.000000000000000000, 0.9238795325112869605, 1.000000000000000000, 0.9238795325112869605, 1.000000000000000000, 0.9238795325112869605, 1.000000000000000000, 0.9238795325112869605, 1.000000000000000000, 0.9238795325112869605, 1.000000000000000000, 0.9238795325112869605, 1.000000000000000000, 0.9238795325112869605, 1.000000000000000000, 0.9238795325112869605, 1.000000000000000000, 0.9238795325112869605, 1.000000000000000000, 0.9238795325112869605, 1.000000000000000000, 0.9238795325112869605, 1.000000000000000000, 0.9238795325112869605, 1.000000000000000000, 0.9238795325112869605, 1.000000000000000000, 0.9238795325112869605, 1.000000000000000000, 0.9238795325112869605, 1.000000000000000000, 0.9238795325112869605, 1.000000000000000000, 0.9238795325112869605, 1.000000000000000000, 0.9238795325112869605, 1.000000000000000000, 0.9238795325112869605, 1.000000000000000000, 0.9238795325112869605, 1.000000000000000000, 0.9238795325112869605, 1.000000000000000000, 0.9238795325112869605, 1.000000000000000000, 0.9238795325112869605, 1.000000000000000000, 0.9238795325112869605, 1.000000000000000000, 0.9238795325112869605, 1.000000000000000000, 0.9238795325112869605, 1.000000000000000000, 0.9238795325112869605, 1.000000000000000000, 0.9238795325112869605, 1.000000000000000000, 0.9238795325112869605, 1.000000000000000000, 0.9238795325112869605, 1.000000000000000000, 0.9238795325112869605, 1.000000000000000000, 0.9238795325112869605, 1.000000000000000000, 0.9238795325112869605, 1.000000000000000000, 0.9238795325112869605, 1.000000000000000000, 0.9238795325112869605, 1.000000000000000000, 0.9238795325112869605, 1.000000000000000000, 0.9238795325112869605, 1.000000000000000000, 0.9238795325112869605, 1.000000000000000000, 0.9238795325112869605, 1.000000000000000000, 0.9238795325112869605, 1.000000000000000000, 0.9238795325112869605, 1.000000000000000000, 0.9238795325112869605, 1.000000000000000000, 0.9238795325112869605, 1.000000000000000000, 0.9238795325112869605, 1.000000000000000000, 0.9238795325112869605, 1.000000000000000000, 0.9238795325112869605, 1.000000000000000000, 0.9238795325112869605, 1.000000000000000000, 0.9238795325112869605, 1.000000000000000000, 0.9238795325112869605, 1.000000000000000000, 0.9238795325112869605, 1.000000000000000000, 0.9238795325112869605, 1.000000000000000000, 0.9238795325112869605, 1.000000000000000000, 0.9238795325112869605, 1.000000000000000000, 0.9238795325112869605, 1.000000000000000000, 0.9238795325112869605, 1.000000000000000000, 0.9238795325112869605, 1.000000000000000000, 0.9238795325112869605, 1.000000000000000000, 0.9238795325112869605, 1.000000000000000000, 0.9238795325112869605, 1.000000000000000000, 0.9238795325112869605, 1.000000000000000000, 0.9238795325112869605, 1.000000000000000000, 0.9238795325112869605, 1.000000000000000000, 0.9238795325112869605, 1.000000000000000000, 0.9238795325112869605, 1.000000000000000000, 0.9238795325112869605, 1.000000000000000000, 0.9238795325112869605, 1.000000000000000000, 0.9238795325112869605, 1.000000000000000000, 0.9238795325112869605, 1.000000000000000000, 0.9238795325112869605, 1.000000000000000000, 0.9238795325112869605, 1.000000000000000000, 0.9238795325112869605, 1.000000000000000000, 0.9238795325112869605, 1.000000000000000000, 0.9238795325112869605, 1.000000000000000000, 0.9238795325112869605, 1.000000000000000000, 0.9238795325112869605, 1.000000000000000000, 0.9238795325112869605, 1.000000000000000000, 0.9238795325112869605, 1.000000000000000000, 0.9238795325112869605, 1.000000000000000000, 0.9238795325112869605, 1.000000000000000000, 0.9238795325112869605, 1.000000000000000000, 0.9238795325112869605, 1.000000000000000000, 0.9238795325112869605, 1.000000000000000000, 0.9238795325112869605, 1.000000000000000000, 0.9238795325112869605, 1.000000000000000000, 0.9238795325112869605, 1.000000000000000000, 0.9238795325112869605, 1.000000000000000000, 0.9238795325112869605, 1.000000000000000000, 0.9238795325112869605, 1.000000000000000000, 0.9238795325112869605, 1.000000000000000000, 0.9238795325112869605, 1.000000000000000000, 0.9238795325112869605, 1.000000000000000000, 0.9238795325112869605, 1.000000000000000000) ) ) 
 REPRESENTATION_ITEM ( '' )  SURFACE ( )  );
#34281=DIRECTION ( 'NONE',  ( 1.000000000000000000, 0.000000000000000000, 0.000000000000000000 ) ) ;
#34289=CARTESIAN_POINT ( 'NONE',  ( 123.4041481442452834, 0.1319031606808879209, -14.10382304977623669 ) ) ;
#34290=CARTESIAN_POINT ( 'NONE',  ( 112.5126281442453120, 0.1319031606808879209, -14.10382304977623669 ) ) ;
#34291=CARTESIAN_POINT ( 'NONE',  ( 128.2184548109119930, 0.7167481258041193959, -11.18974888642105014 ) ) ;
#34292=ORIENTED_EDGE ( 'NONE', *, *, #31738, .T. ) ;
#34296=CARTESIAN_POINT ( 'NONE',  ( 111.9559014775786494, -9.522524984348097021, -10.63868154973201108 ) ) ;
#34298=CARTESIAN_POINT ( 'NONE',  ( 125.3328548109119964, -9.261995988541697145, -16.69588392320189030 ) ) ;
#34299=CARTESIAN_POINT ( 'NONE',  ( 111.8319081442453182, -5.638512984488999180, -18.83840828888717311 ) ) ;
#34301=CARTESIAN_POINT ( 'NONE',  ( 114.6115148109119986, -3.383040157471821630, -19.15922257007629170 ) ) ;
#34302=CARTESIAN_POINT ( 'NONE',  ( 113.4001635400977790, -1.223627541775725636, -16.99192386690445034 ) ) ;
#34305=CARTESIAN_POINT ( 'NONE',  ( 123.8012348109119642, -9.565557343593413364, -10.61323700422348004 ) ) ;
#34306=CARTESIAN_POINT ( 'NONE',  ( 122.8936081442453059, -9.565557343593413364, -10.61323700422348004 ) ) ;
#34315=CARTESIAN_POINT ( 'NONE',  ( 124.0848681442452772, -4.089484607189486809, -7.948022111789456723 ) ) ;
#34316=CARTESIAN_POINT ( 'NONE',  ( 111.7184548109119788, -0.8288870151387760510, -10.36305467784173118 ) ) ;
#34317=LINE ( 'NONE', #41188, #37173 ) ;
#34318=CARTESIAN_POINT ( 'NONE',  ( 120.6812681442452941, -10.30919188438810075, -12.61870101168855918 ) ) ;
#34319=CARTESIAN_POINT ( 'NONE',  ( 113.4202548109119846, -10.30919188438810075, -12.61870101168855918 ) ) ;
#34321=CARTESIAN_POINT ( 'NONE',  ( 114.2144281442453178, -1.833838273342658809, -17.42832698103878286 ) ) ;
#34322=CARTESIAN_POINT ( 'NONE',  ( 125.6732148109119862, 0.5811942927096110934, -14.16772938898807510 ) ) ;
#34324=CARTESIAN_POINT ( 'NONE',  ( 123.9146881442452894, 0.9020085738987339008, -11.91225656197089222 ) ) ;
#34325=CARTESIAN_POINT ( 'NONE',  ( 113.2500748109119968, -6.344957434206662583, -7.627207830600332805 ) ) ;
#34326=CARTESIAN_POINT ( 'NONE',  ( 113.5337081442453240, -0.8288870151387760510, -10.36305467784173118 ) ) ;
#34328=EDGE_CURVE ( 'NONE', #34005, #21889, #39834, .T. ) ;
#34329=CARTESIAN_POINT ( 'NONE',  ( 116.1998614775786507, 0.4262465694468514643, -12.03445270309931736 ) ) ;
#34330=CARTESIAN_POINT ( 'NONE',  ( 111.7184548109119788, -9.261995988541697145, -16.69588392320189030 ) ) ;
#34331=CARTESIAN_POINT ( 'NONE',  ( 125.2194014775786286, 0.1319031606808879209, -14.10382304977623669 ) ) ;
#34338=CARTESIAN_POINT ( 'NONE',  ( 115.1430393777725385, -1.267766418764730840, -16.93314635290706605 ) ) ;
#34343=CARTESIAN_POINT ( 'NONE',  ( 119.9438214775786378, -7.893985811506177619, -18.51759400769804742 ) ) ;
#34344=CARTESIAN_POINT ( 'NONE',  ( 137.0337503232511267, -6.699180850412786548, -18.51269755244290494 ) ) ;
#34347=CARTESIAN_POINT ( 'NONE',  ( 120.3409081442453044, -8.899110576539710493, -16.42337572283490132 ) ) ;
#34348=ORIENTED_EDGE ( 'NONE', *, *, #43308, .T. ) ;
#34349=CARTESIAN_POINT ( 'NONE',  ( 126.2404814775786264, -9.261995988541697145, -16.69588392320189030 ) ) ;
#34350=CARTESIAN_POINT ( 'NONE',  ( 118.7525614775786380, -8.166667518702819706, -8.995218007635861213 ) ) ;
#34352=CARTESIAN_POINT ( 'NONE',  ( 115.8595014775786609, -7.643976991954077427, -18.09477374809248928 ) ) ;
#34353=CARTESIAN_POINT ( 'NONE',  ( 112.2857214775786474, -5.574606645277164318, -18.38911715685844683 ) ) ;
#34357=CARTESIAN_POINT ( 'NONE',  ( 118.0718414775786442, -0.8288870151387760510, -10.36305467784173118 ) ) ;
#34358=CARTESIAN_POINT ( 'NONE',  ( 119.6034614775786196, -3.505236298600246325, -18.68346056562440793 ) ) ;
#34364=CARTESIAN_POINT ( 'NONE',  ( 115.4056881442453459, -7.893985811506177619, -18.51759400769804742 ) ) ;
#34365=CARTESIAN_POINT ( 'NONE',  ( 111.7751814775786556, -7.893985811506177619, -18.51759400769804742 ) ) ;
#34371=CARTESIAN_POINT ( 'NONE',  ( 120.8514481442452961, -7.893985811506177619, -18.51759400769804742 ) ) ;
#34373=CARTESIAN_POINT ( 'NONE',  ( 114.2144281442453178, -8.166667518702817929, -8.995218007635859436 ) ) ;
#34375=CARTESIAN_POINT ( 'NONE',  ( 118.5823814775786360, -7.643976991954077427, -18.09477374809248928 ) ) ;
#34377=CARTESIAN_POINT ( 'NONE',  ( 120.4543614775786295, -4.089484607189486809, -7.948022111789456723 ) ) ;
#34378=CARTESIAN_POINT ( 'NONE',  ( 118.5256548109119876, -0.4660016031367893996, -10.09054647747474043 ) ) ;
#34380=CARTESIAN_POINT ( 'NONE',  ( 111.4348214775786801, -3.505236298600246325, -18.68346056562440793 ) ) ;
#34383=CARTESIAN_POINT ( 'NONE',  ( 118.9794681442453026, -9.261995988541697145, -16.69588392320189030 ) ) ;
#34385=CARTESIAN_POINT ( 'NONE',  ( 114.5547881442453217, -5.638512984488999180, -18.83840828888717311 ) ) ;
#34387=CARTESIAN_POINT ( 'NONE',  ( 125.4463081442452932, -5.638512984488999180, -18.83840828888717311 ) ) ;
#34388=EDGE_CURVE ( 'NONE', #29815, #38024, #23056, .T. ) ;
#34390=CARTESIAN_POINT ( 'NONE',  ( 112.4559014775786778, -0.1624402480850797581, -16.17319339645315424 ) ) ;
#34392=CARTESIAN_POINT ( 'NONE',  ( 116.1431348109119881, 0.1319031606808879209, -14.10382304977623669 ) ) ;
#34394=CARTESIAN_POINT ( 'NONE',  ( 117.9016614775786280, -0.1624402480850797581, -16.17319339645315424 ) ) ;
#34397=CARTESIAN_POINT ( 'NONE',  ( 116.3700414775786527, -4.153390946401321671, -8.397313243818183892 ) ) ;
#34399=CARTESIAN_POINT ( 'NONE',  ( 115.6893214775786447, 0.5811942927096154232, -14.16772938898807155 ) ) ;
#34400=CARTESIAN_POINT ( 'NONE',  ( 125.6732148109119862, 0.5811942927096110934, -14.16772938898807510 ) ) ;
#34401=CARTESIAN_POINT ( 'NONE',  ( 118.4122014775786340, -9.859900752359374465, -12.68260735090039404 ) ) ;
#34403=CARTESIAN_POINT ( 'NONE',  ( 116.7671281442453335, -1.834011780172310813, -8.268836392978581529 ) ) ;
#34407=FACE_OUTER_BOUND ( 'NONE', #30064, .T. ) ;
#34409=CARTESIAN_POINT ( 'NONE',  ( 123.5176014775786228, -9.261995988541697145, -16.69588392320189030 ) ) ;
#34412=CARTESIAN_POINT ( 'NONE',  ( 118.1285681442453068, -2.084020599724406786, -8.691656652584148546 ) ) ;
#34413=CARTESIAN_POINT ( 'NONE',  ( 127.8924691488521574, 0.9350681874800557125, -12.72727887896535925 ) ) ;
#34414=CARTESIAN_POINT ( 'NONE',  ( 123.0070614775786169, 0.9020085738987339008, -11.91225656197089222 ) ) ;
#34418=CARTESIAN_POINT ( 'NONE',  ( 111.8319081442453182, -5.638512984488999180, -18.83840828888717311 ) ) ;
#34419=CARTESIAN_POINT ( 'NONE',  ( 111.7184548109119788, -9.261995988541697145, -16.69588392320189030 ) ) ;
#34420=CARTESIAN_POINT ( 'NONE',  ( 122.5532481442453019, -10.63000616557722466, -14.87417383870573495 ) ) ;
#34421=CARTESIAN_POINT ( 'NONE',  ( 116.9940348109119839, -0.1624402480850797581, -16.17319339645315424 ) ) ;
#34423=CARTESIAN_POINT ( 'NONE',  ( 119.4900081442453086, -1.834011780172310813, -8.268836392978581529 ) ) ;
#34425=CARTESIAN_POINT ( 'NONE',  ( 126.3115243456358883, -1.057789078141782690, -10.07954330274492882 ) ) ;
#34426=CARTESIAN_POINT ( 'NONE',  ( 124.0848681442452772, -5.574606645277164318, -18.38911715685844683 ) ) ;
#34431=CARTESIAN_POINT ( 'NONE',  ( 118.0151148109119816, -10.63000616557722466, -14.87417383870573495 ) ) ;
#34432=CARTESIAN_POINT ( 'NONE',  ( 124.8790414775786246, -8.899110576539710493, -16.42337572283490132 ) ) ;
#34436=CARTESIAN_POINT ( 'NONE',  ( 123.8012348109119642, 0.2603800115204892296, -16.42320221600525088 ) ) ;
#34438=CARTESIAN_POINT ( 'NONE',  ( 119.2063748109119814, -7.894159318335828068, -9.358103419637847864 ) ) ;
#34441=CARTESIAN_POINT ( 'NONE',  ( 114.9518748109119883, -1.834011780172310813, -8.268836392978581529 ) ) ;
#34442=CARTESIAN_POINT ( 'NONE',  ( 124.3117748109119844, 0.1319031606808879209, -14.10382304977623669 ) ) ;
#34444=DIRECTION ( 'NONE',  ( 1.000000000000000000, 0.000000000000000000, 0.000000000000000000 ) ) ;
#34445=CARTESIAN_POINT ( 'NONE',  ( 122.0994348109119443, 0.9020085738987339008, -11.91225656197089222 ) ) ;
#34446=CARTESIAN_POINT ( 'NONE',  ( 111.4159584094731059, -9.013377521824503802, -16.52270977695948417 ) ) ;
#34448=CARTESIAN_POINT ( 'NONE',  ( 121.4187148109119789, -6.344957434206665248, -7.627207830600338134 ) ) ;
#34449=CARTESIAN_POINT ( 'NONE',  ( 118.4122014775786340, 0.5811942927096110934, -14.16772938898807510 ) ) ;
#34450=CARTESIAN_POINT ( 'NONE',  ( 119.3198281442452924, -9.859900752359374465, -12.68260735090039404 ) ) ;
#34452=CARTESIAN_POINT ( 'NONE',  ( 116.7671281442453335, -1.834011780172310813, -8.268836392978581529 ) ) ;
#34455=CARTESIAN_POINT ( 'NONE',  ( 126.5808414775786446, -9.859900752359378018, -12.68260735090039759 ) ) ;
#34457=CARTESIAN_POINT ( 'NONE',  ( 125.6626748109119802, -9.522524984348629928, -10.63868154973292413 ) ) ;
#34461=CARTESIAN_POINT ( 'NONE',  ( 121.5321681442453183, -9.988377603198976828, -10.36322818467138340 ) ) ;
#34462=CARTESIAN_POINT ( 'NONE',  ( 122.1561614775786353, -8.899110576539710493, -16.42337572283490132 ) ) ;
#34464=CARTESIAN_POINT ( 'NONE',  ( 123.7445081442452874, -1.561330072975668948, -17.79121239304076951 ) ) ;
#34467=CARTESIAN_POINT ( 'NONE',  ( 125.1626748109119802, -9.988377603198980381, -10.36322818467138518 ) ) ;
#34470=CARTESIAN_POINT ( 'NONE',  ( 114.0442481442453300, -1.834011780172310813, -8.268836392978581529 ) ) ;
#34476=CARTESIAN_POINT ( 'NONE',  ( 112.6260814775786514, -0.8288870151387760510, -10.36305467784173118 ) ) ;
#34477=CARTESIAN_POINT ( 'NONE',  ( 112.2857214775786474, -4.089484607189486809, -7.948022111789456723 ) ) ;
#34480=CARTESIAN_POINT ( 'NONE',  ( 122.4965214775786251, 0.1319031606808879209, -14.10382304977623669 ) ) ;
#34481=CARTESIAN_POINT ( 'NONE',  ( 114.5547881442453217, -4.153390946401321671, -8.397313243818183892 ) ) ;
#34482=CARTESIAN_POINT ( 'NONE',  ( 113.7038881442453402, -6.222761293078241884, -8.102969835052219238 ) ) ;
#34485=CARTESIAN_POINT ( 'NONE',  ( 124.9357681442453014, -7.643976991954077427, -18.09477374809248928 ) ) ;
#34486=CARTESIAN_POINT ( 'NONE',  ( 119.3198281442452924, 0.5811942927096110934, -14.16772938898807510 ) ) ;
#34487=CARTESIAN_POINT ( 'NONE',  ( 125.7866681442452688, -8.899110576539710493, -16.42337572283490132 ) ) ;
#34488=CARTESIAN_POINT ( 'NONE',  ( 115.4624148109119943, -4.153390946401321671, -8.397313243818183892 ) ) ;
#34490=CARTESIAN_POINT ( 'NONE',  ( 126.9276200068663343, -9.666589674469316051, -15.76113967148663697 ) ) ;
#34494=CARTESIAN_POINT ( 'NONE',  ( 115.2355081442453155, 0.1319031606808879209, -14.10382304977623669 ) ) ;
#34495=CARTESIAN_POINT ( 'NONE',  ( 114.9518748109119883, -7.643976991954077427, -18.09477374809248928 ) ) ;
#34496=CARTESIAN_POINT ( 'NONE',  ( 115.2355081442453155, -10.30919188438809542, -12.61870101168854852 ) ) ;
#34505=CARTESIAN_POINT ( 'NONE',  ( 122.7234281442452755, -4.153390946401325223, -8.397313243818185668 ) ) ;
#34506=CARTESIAN_POINT ( 'NONE',  ( 113.5337081442453240, -0.8288870151387760510, -10.36305467784173118 ) ) ;
#34513=CARTESIAN_POINT ( 'NONE',  ( 111.6617281442453304, 0.4262465694468514643, -12.03445270309931736 ) ) ;
#34516=CARTESIAN_POINT ( 'NONE',  ( 124.9357681442453014, -7.643976991954077427, -18.09477374809248928 ) ) ;
#34518=CARTESIAN_POINT ( 'NONE',  ( 114.3278814775786429, -10.30919188438810075, -12.61870101168855918 ) ) ;
#34519=CARTESIAN_POINT ( 'NONE',  ( 126.4599182912957644, 0.09025682329171769158, -14.68838553235235445 ) ) ;
#34521=CARTESIAN_POINT ( 'NONE',  ( 124.0281414775786146, -7.643976991954077427, -18.09477374809248928 ) ) ;
#34522=CARTESIAN_POINT ( 'NONE',  ( 122.0427081442452817, -9.859900752359378018, -12.68260735090039759 ) ) ;
#34528=CARTESIAN_POINT ( 'NONE',  ( 114.4413348109119823, -0.8288870151387760510, -10.36305467784173118 ) ) ;
#34530=CARTESIAN_POINT ( 'NONE',  ( 111.7184544649789331, -9.256331613732484698, -16.70304772739236654 ) ) ;
#34532=CARTESIAN_POINT ( 'NONE',  ( 125.7866681442452688, -0.4660016031367893996, -10.09054647747474043 ) ) ;
#34533=CARTESIAN_POINT ( 'NONE',  ( 126.0703014775786102, -9.988377603198980381, -10.36322818467138518 ) ) ;
#34535=CARTESIAN_POINT ( 'NONE',  ( 121.9292548109119849, -1.561330072975668948, -17.79121239304076951 ) ) ;
#34536=CARTESIAN_POINT ( 'NONE',  ( 115.0653281442453277, -6.344957434206662583, -7.627207830600332805 ) ) ;
#34538=CARTESIAN_POINT ( 'NONE',  ( 114.4413348109119823, -0.8288870151387760510, -10.36305467784173118 ) ) ;
#34539=CARTESIAN_POINT ( 'NONE',  ( 124.4819548109119722, -7.893985811506177619, -18.51759400769804742 ) ) ;
#34540=CARTESIAN_POINT ( 'NONE',  ( 112.6260814775786514, -9.261995988541697145, -16.69588392320189030 ) ) ;
#34541=CARTESIAN_POINT ( 'NONE',  ( 117.1074881442453233, 0.4262465694468514643, -12.03445270309931736 ) ) ;
#34543=CARTESIAN_POINT ( 'NONE',  ( 118.8092881442453290, -0.1624402480850797581, -16.17319339645315424 ) ) ;
#34546=CARTESIAN_POINT ( 'NONE',  ( 116.5402214775786405, 0.2603800115204892296, -16.42320221600525088 ) ) ;
#34547=CARTESIAN_POINT ( 'NONE',  ( 122.6099748109119929, -0.8288870151387760510, -10.36305467784173118 ) ) ;
#34555=CARTESIAN_POINT ( 'NONE',  ( 116.3133148109119759, -7.893985811506177619, -18.51759400769804742 ) ) ;
#34557=CARTESIAN_POINT ( 'NONE',  ( 113.0798948109119948, -8.899110576539710493, -16.42337572283490132 ) ) ;
#34559=ADVANCED_FACE ( 'NONE', ( #40720 ), #26721, .T. ) ;
#34562=CARTESIAN_POINT ( 'NONE',  ( 118.6391081442452986, -4.089484607189486809, -7.948022111789456723 ) ) ;
#34563=CARTESIAN_POINT ( 'NONE',  ( 136.6493356239704156, -4.310644207877323275, -19.04512585373862876 ) ) ;
#34566=CARTESIAN_POINT ( 'NONE',  ( 119.8303681442453126, 0.4262465694468514643, -12.03445270309931736 ) ) ;
#34570=CARTESIAN_POINT ( 'NONE',  ( 117.6180281442453150, -0.4660016031367893996, -10.09054647747474043 ) ) ;
#34572=CARTESIAN_POINT ( 'NONE',  ( 117.2776681442452968, -4.153390946401321671, -8.397313243818183892 ) ) ;
#34573=CARTESIAN_POINT ( 'NONE',  ( 112.4559014775786778, -0.1624402480850797581, -16.17319339645315424 ) ) ;
#34578=CARTESIAN_POINT ( 'NONE',  ( 115.1787814775786387, -0.1624402480850797581, -16.17319339645315424 ) ) ;
#34579=CARTESIAN_POINT ( 'NONE',  ( 120.6245414775786458, -0.1624402480850797581, -16.17319339645315424 ) ) ;
#34584=CARTESIAN_POINT ( 'NONE',  ( 114.7816948109119863, 0.5811942927096154232, -14.16772938898807155 ) ) ;
#34585=CARTESIAN_POINT ( 'NONE',  ( 113.9875214775786532, -0.4660016031367893996, -10.09054647747474043 ) ) ;
#34589=VECTOR ( 'NONE', #13785, 1000.000000000000000 ) ;
#34590=ORIENTED_EDGE ( 'NONE', *, *, #44253, .T. ) ;
#34591=CARTESIAN_POINT ( 'NONE',  ( 123.0637881442452937, -0.4660016031367893996, -10.09054647747474043 ) ) ;
#34592=CARTESIAN_POINT ( 'NONE',  ( 113.3635281442453504, -9.988377603198976828, -10.36322818467138340 ) ) ;
#34593=CARTESIAN_POINT ( 'NONE',  ( 119.8870948109119752, -0.8288870151387760510, -10.36305467784173118 ) ) ;
#34596=CARTESIAN_POINT ( 'NONE',  ( 121.8158014775786171, -5.638512984488999180, -18.83840828888717311 ) ) ;
#34597=CARTESIAN_POINT ( 'NONE',  ( 117.8449348109119938, -8.166667518702817929, -8.995218007635861213 ) ) ;
#34599=CARTESIAN_POINT ( 'NONE',  ( 113.8173414775786512, -9.565557343593413364, -10.61323700422348004 ) ) ;
#34602=CARTESIAN_POINT ( 'NONE',  ( 117.2209414775786485, -7.893985811506177619, -18.51759400769804742 ) ) ;
#34605=CARTESIAN_POINT ( 'NONE',  ( 115.8595014775786609, -1.834011780172310813, -8.268836392978581529 ) ) ;
#34606=VERTEX_POINT ( 'NONE', #37508 ) ;
#34608=CARTESIAN_POINT ( 'NONE',  ( 124.1415948109119540, -6.344957434206665248, -7.627207830600338134 ) ) ;
#34611=CARTESIAN_POINT ( 'NONE',  ( 124.6713397424434078, -0.9924539043446091169, -17.29976612834908423 ) ) ;
#34612=CARTESIAN_POINT ( 'NONE',  ( 116.5969481442453031, -9.859900752359374465, -12.68260735090039404 ) ) ;
#34614=CARTESIAN_POINT ( 'NONE',  ( 117.5045748109119756, -9.859900752359374465, -12.68260735090039404 ) ) ;
#34617=CARTESIAN_POINT ( 'NONE',  ( 120.5110881442453206, -3.505236298600246325, -18.68346056562440793 ) ) ;
#34619=CARTESIAN_POINT ( 'NONE',  ( 116.7671281442453335, -1.834011780172310813, -8.268836392978581529 ) ) ;
#34620=CARTESIAN_POINT ( 'NONE',  ( 112.9097148109120070, -9.565557343593413364, -10.61323700422348004 ) ) ;
#34621=CARTESIAN_POINT ( 'NONE',  ( 117.4478481442453131, -9.565557343593413364, -10.61323700422348004 ) ) ;
#34622=ORIENTED_EDGE ( 'NONE', *, *, #20874, .F. ) ;
#34623=CARTESIAN_POINT ( 'NONE',  ( 115.9729548109119861, -6.344957434206662583, -7.627207830600332805 ) ) ;
#34629=CARTESIAN_POINT ( 'NONE',  ( 121.7023481442452777, -9.261995988541697145, -16.69588392320189030 ) ) ;
#34630=EDGE_LOOP ( 'NONE', ( #33895, #7950, #37176, #8704, #31377 ) ) ;
#34631=CARTESIAN_POINT ( 'NONE',  ( 118.5143726669217585, -2.334846009198389805, -18.01015021110788439 ) ) ;
#34632=CARTESIAN_POINT ( 'NONE',  ( 118.4689281442453392, -10.15424416112533912, -14.75197769757731336 ) ) ;
#34635=CARTESIAN_POINT ( 'NONE',  ( 121.9292548109119849, -1.561330072975668948, -17.79121239304076951 ) ) ;
#34637=DIRECTION ( 'NONE',  ( 1.000000000000000000, 0.000000000000000000, 0.000000000000000000 ) ) ;
#34639=CARTESIAN_POINT ( 'NONE',  ( 111.8319081442453182, -5.638512984488999180, -18.83840828888717311 ) ) ;
#34640=CARTESIAN_POINT ( 'NONE',  ( 112.3991748109119868, -8.166667518702817929, -8.995218007635859436 ) ) ;
#34641=CARTESIAN_POINT ( 'NONE',  ( 124.4252281442452812, -9.261995988541697145, -16.69588392320189030 ) ) ;
#34642=CARTESIAN_POINT ( 'NONE',  ( 118.6391081442452986, -5.574606645277164318, -18.38911715685844683 ) ) ;
#34644=CARTESIAN_POINT ( 'NONE',  ( 120.8514481442452961, -7.893985811506177619, -18.51759400769804742 ) ) ;
#34646=CARTESIAN_POINT ( 'NONE',  ( 121.9859814775786333, -9.565557343593413364, -10.61323700422348004 ) ) ;
#34651=CARTESIAN_POINT ( 'NONE',  ( 116.1998614775786507, -10.63000616557722466, -14.87417383870573495 ) ) ;
#34652=CARTESIAN_POINT ( 'NONE',  ( 123.2906948109119867, -1.833838273342659697, -17.42832698103878286 ) ) ;
#34656=CARTESIAN_POINT ( 'NONE',  ( 124.0281414775786146, -1.834011780172310813, -8.268836392978581529 ) ) ;
#34658=CARTESIAN_POINT ( 'NONE',  ( 120.8514481442452961, -2.084020599724406786, -8.691656652584148546 ) ) ;
#34661=CARTESIAN_POINT ( 'NONE',  ( 115.4056881442453459, -7.893985811506177619, -18.51759400769804742 ) ) ;
#34662=CARTESIAN_POINT ( 'NONE',  ( 125.4463081442452932, -4.153390946401325223, -8.397313243818185668 ) ) ;
#34666=CARTESIAN_POINT ( 'NONE',  ( 122.2696148109119889, -4.089484607189486809, -7.948022111789456723 ) ) ;
#34669=CARTESIAN_POINT ( 'NONE',  ( 116.9948677074048931, -2.419733177069680607, -17.89711025544712442 ) ) ;
#34670=CARTESIAN_POINT ( 'NONE',  ( 120.3409081442453044, -0.4660016031367893996, -10.09054647747474043 ) ) ;
#34671=CARTESIAN_POINT ( 'NONE',  ( 119.0929214775786278, -5.638512984488999180, -18.83840828888717311 ) ) ;
#34672=CARTESIAN_POINT ( 'NONE',  ( 118.2420214775786320, -6.222761293078241884, -8.102969835052219238 ) ) ;
#34674=CARTESIAN_POINT ( 'NONE',  ( 115.2922348109119781, -10.63000616557722466, -14.87417383870573495 ) ) ;
#34681=CARTESIAN_POINT ( 'NONE',  ( 113.3635281442453504, -9.988377603198976828, -10.36322818467138340 ) ) ;
#34683=CARTESIAN_POINT ( 'NONE',  ( 124.5386814775786206, -5.638512984488999180, -18.83840828888717311 ) ) ;
#34686=CARTESIAN_POINT ( 'NONE',  ( 123.9146881442452894, 0.9020085738987339008, -11.91225656197089222 ) ) ;
#34687=CARTESIAN_POINT ( 'NONE',  ( 124.5954081442453116, -3.383040157471821630, -19.15922257007629170 ) ) ;
#34689=CARTESIAN_POINT ( 'NONE',  ( 113.5337081442453240, -9.261995988541697145, -16.69588392320189030 ) ) ;
#34694=CARTESIAN_POINT ( 'NONE',  ( 113.8173414775786512, -9.565557343593413364, -10.61323700422348004 ) ) ;
#34695=CARTESIAN_POINT ( 'NONE',  ( 113.7038881442453402, -3.383040157471821630, -19.15922257007629170 ) ) ;
#34696=VECTOR ( 'NONE', #517, 1000.000000000000114 ) ;
#34699=CARTESIAN_POINT ( 'NONE',  ( 119.8303681442453126, 0.4262465694468514643, -12.03445270309931736 ) ) ;
#34700=CARTESIAN_POINT ( 'NONE',  ( 115.5758681442453053, -7.894159318335828068, -9.358103419637847864 ) ) ;
#34701=CARTESIAN_POINT ( 'NONE',  ( 113.1366214775786432, -7.643976991954077427, -18.09477374809248928 ) ) ;
#34706=CARTESIAN_POINT ( 'NONE',  ( 115.6893214775786447, -9.859900752359374465, -12.68260735090039404 ) ) ;
#34711=CARTESIAN_POINT ( 'NONE',  ( 118.8092881442453290, -0.1624402480850797581, -16.17319339645315424 ) ) ;
#34713=CARTESIAN_POINT ( 'NONE',  ( 113.1366214775786432, -7.643976991954077427, -18.09477374809248928 ) ) ;
#34722=CARTESIAN_POINT ( 'NONE',  ( 124.4819548109119722, -2.084020599724406786, -8.691656652584148546 ) ) ;
#34723=CARTESIAN_POINT ( 'NONE',  ( 117.7882081442453170, -3.505236298600246325, -18.68346056562440793 ) ) ;
#34724=CARTESIAN_POINT ( 'NONE',  ( 119.6811727111058588, -1.267766418764730840, -16.93314635290706605 ) ) ;
#34727=CARTESIAN_POINT ( 'NONE',  ( 115.2355081442453155, 0.1319031606808879209, -14.10382304977623669 ) ) ;
#34730=CARTESIAN_POINT ( 'NONE',  ( 116.8011953663348805, -1.172797794773246416, -17.05961127468924587 ) ) ;
#34731=CARTESIAN_POINT ( 'NONE',  ( 114.3846081442453197, -10.63000616557722466, -14.87417383870573495 ) ) ;
#34732=ORIENTED_EDGE ( 'NONE', *, *, #37000, .F. ) ;
#34733=CARTESIAN_POINT ( 'NONE',  ( 115.3489614775786407, -9.261995988541697145, -16.69588392320189030 ) ) ;
#34736=CARTESIAN_POINT ( 'NONE',  ( 113.2500748109119968, -6.344957434206662583, -7.627207830600332805 ) ) ;
#34737=CARTESIAN_POINT ( 'NONE',  ( 113.1933481442453058, -4.089484607189486809, -7.948022111789456723 ) ) ;
#34739=CARTESIAN_POINT ( 'NONE',  ( 125.0492214775786266, -3.505236298600246325, -18.68346056562440793 ) ) ;
#34740=EDGE_CURVE ( 'NONE', #40113, #8883, #11075, .T. ) ;
#34743=CARTESIAN_POINT ( 'NONE',  ( 120.2798381407226032, -1.081026697600536046, -17.18181821144402832 ) ) ;
#34745=CARTESIAN_POINT ( 'NONE',  ( 118.2420214775786320, -6.222761293078241884, -8.102969835052219238 ) ) ;
#34749=CARTESIAN_POINT ( 'NONE',  ( 123.3474214775786209, -9.988377603198976828, -10.36322818467138340 ) ) ;
#34750=CARTESIAN_POINT ( 'NONE',  ( 125.7299414775786346, 0.9020085738987339008, -11.91225656197089222 ) ) ;
#34751=CARTESIAN_POINT ( 'NONE',  ( 119.8870948109119752, -0.8288870151387535135, -10.36305467784176138 ) ) ;
#34752=CARTESIAN_POINT ( 'NONE',  ( 120.6245414775786458, -9.988377603198976828, -10.36322818467138340 ) ) ;
#34753=CARTESIAN_POINT ( 'NONE',  ( 118.0718414775786300, -9.261995988541697145, -16.69588392320189030 ) ) ;
#34755=CARTESIAN_POINT ( 'NONE',  ( 116.0864081442453113, -0.1624402480850797581, -16.17319339645315424 ) ) ;
#34756=CARTESIAN_POINT ( 'NONE',  ( 125.6164881442453094, 0.2603800115204892296, -16.42320221600525088 ) ) ;
#34757=CARTESIAN_POINT ( 'NONE',  ( 113.1933481442453058, -4.089484607189486809, -7.948022111789456723 ) ) ;
#34759=CARTESIAN_POINT ( 'NONE',  ( 114.6115148109119986, -6.222761293078241884, -8.102969835052219238 ) ) ;
#34762=CARTESIAN_POINT ( 'NONE',  ( 121.0783548109119749, -9.565557343593413364, -10.61323700422348004 ) ) ;
#34764=EDGE_CURVE ( 'NONE', #11839, #19331, #9960, .T. ) ;
#34765=CARTESIAN_POINT ( 'NONE',  ( 118.2420214775786320, -3.383040157471821630, -19.15922257007629170 ) ) ;
#34766=DIRECTION ( 'NONE',  ( 0.000000000000000000, 0.6004852223388321697, -0.7996358532186279566 ) ) ;
#34768=ORIENTED_EDGE ( 'NONE', *, *, #10847, .T. ) ;
#34772=CARTESIAN_POINT ( 'NONE',  ( 115.9162281442453235, -4.089484607189486809, -7.948022111789456723 ) ) ;
#34773=CARTESIAN_POINT ( 'NONE',  ( 136.5278073585146217, -10.56988143321154539, -13.98918071750362735 ) ) ;
#34778=CARTESIAN_POINT ( 'NONE',  ( 118.8660148109119774, -10.30919188438810075, -12.61870101168855918 ) ) ;
#34781=CARTESIAN_POINT ( 'NONE',  ( 111.7062228165344067, -2.324775150319231098, -18.02356106541843062 ) ) ;
#34783=CARTESIAN_POINT ( 'NONE',  ( 122.8936081442453059, -9.565557343593413364, -10.61323700422348004 ) ) ;
#34786=CARTESIAN_POINT ( 'NONE',  ( 119.8870948109119752, -9.261995988541697145, -16.69588392320189030 ) ) ;
#34788=CARTESIAN_POINT ( 'NONE',  ( 115.8027748109119841, -8.899110576539710493, -16.42337572283490132 ) ) ;
#34789=CARTESIAN_POINT ( 'NONE',  ( 111.4915481442453142, -1.833838273342658365, -17.42832698103878286 ) ) ;
#34793=CARTESIAN_POINT ( 'NONE',  ( 118.6958348109119754, -3.505236298600246325, -18.68346056562440793 ) ) ;
#34794=CARTESIAN_POINT ( 'NONE',  ( 120.9649014775786355, -6.222761293078241884, -8.102969835052219238 ) ) ;
#34799=CARTESIAN_POINT ( 'NONE',  ( 112.7395348109119766, -5.638512984488999180, -18.83840828888717311 ) ) ;
#34800=CARTESIAN_POINT ( 'NONE',  ( 116.1998614775786507, -10.63000616557722466, -14.87417383870573495 ) ) ;
#34805=CARTESIAN_POINT ( 'NONE',  ( 120.5678148109119832, -8.166667518702819706, -8.995218007635861213 ) ) ;
#34806=CARTESIAN_POINT ( 'NONE',  ( 126.4106614775786284, -6.222761293078241884, -8.102969835052219238 ) ) ;
#34807=CARTESIAN_POINT ( 'NONE',  ( 117.3911214775786505, -7.894159318335828068, -9.358103419637847864 ) ) ;
#34808=CARTESIAN_POINT ( 'NONE',  ( 124.0281414775786146, -1.834011780172310813, -8.268836392978581529 ) ) ;
#34809=CARTESIAN_POINT ( 'NONE',  ( 119.8870948109119752, -9.261995988541697145, -16.69588392320189030 ) ) ;
#34810=EDGE_CURVE ( 'NONE', #12347, #36520, #25255, .T. ) ;
#34813=CARTESIAN_POINT ( 'NONE',  ( 113.0231681442453180, -10.15424416112533912, -14.75197769757731336 ) ) ;
#34814=CARTESIAN_POINT ( 'NONE',  ( 124.9357681442453156, -7.643976991953527644, -18.09477374809256034 ) ) ;
#34816=ADVANCED_FACE ( 'NONE', ( #5993 ), #10541, .T. ) ;
#34817=CARTESIAN_POINT ( 'NONE',  ( 122.6667014775786413, -7.893985811506177619, -18.51759400769804742 ) ) ;
#34819=CARTESIAN_POINT ( 'NONE',  ( 116.4834948109119779, -1.561330072975668504, -17.79121239304076951 ) ) ;
#34822=CARTESIAN_POINT ( 'NONE',  ( 124.7655881442452852, 0.5811942927096110934, -14.16772938898807510 ) ) ;
#34823=CARTESIAN_POINT ( 'NONE',  ( 122.3830681442452857, -8.166667518702830364, -8.995218007635870094 ) ) ;
#34825=CARTESIAN_POINT ( 'NONE',  ( 128.2184548109119930, -0.6896191363000483410, -17.70303589939592825 ) ) ;
#34826=CARTESIAN_POINT ( 'NONE',  ( 120.5110881442453206, -3.505236298600246325, -18.68346056562440793 ) ) ;
#34828=CARTESIAN_POINT ( 'NONE',  ( 120.0572748109119772, -6.222761293078241884, -8.102969835052219238 ) ) ;
#34830=CARTESIAN_POINT ( 'NONE',  ( 120.3976348109119812, -7.643976991954077427, -18.09477374809248928 ) ) ;
#34832=CARTESIAN_POINT ( 'NONE',  ( 117.3911214775786505, -1.561330072975668504, -17.79121239304076951 ) ) ;
#34834=CARTESIAN_POINT ( 'NONE',  ( 115.1787814775786387, -0.1624402480850797581, -16.17319339645315424 ) ) ;
#34836=CARTESIAN_POINT ( 'NONE',  ( 115.4056881442453459, -7.893985811506177619, -18.51759400769804742 ) ) ;
#34840=CARTESIAN_POINT ( 'NONE',  ( 127.7816961174390258, -4.552121613038932146, -15.05751623555017993 ) ) ;
#34841=CARTESIAN_POINT ( 'NONE',  ( 121.7590748109119687, -7.893985811506177619, -18.51759400769804742 ) ) ;
#34843=CARTESIAN_POINT ( 'NONE',  ( 126.8137406967828582, -8.727882229017838611, -9.768360422713213254 ) ) ;
#34844=CARTESIAN_POINT ( 'NONE',  ( 116.5402214775786405, -9.565557343593413364, -10.61323700422348004 ) ) ;
#34845=CARTESIAN_POINT ( 'NONE',  ( 116.3700414775786527, -5.638512984489023161, -18.83840828888716601 ) ) ;
#34848=CARTESIAN_POINT ( 'NONE',  ( 124.1983214775786166, -8.166667518702819706, -8.995218007635861213 ) ) ;
#34850=CARTESIAN_POINT ( 'NONE',  ( 124.2193060444391790, -1.267766418764731728, -16.93314635290706605 ) ) ;
#34851=ORIENTED_EDGE ( 'NONE', *, *, #10825, .F. ) ;
#34852=CARTESIAN_POINT ( 'NONE',  ( 115.6325948109119821, 0.2603800115204892296, -16.42320221600525088 ) ) ;
#34853=CARTESIAN_POINT ( 'NONE',  ( 125.6164881442453094, -9.565557343593413364, -10.61323700422348004 ) ) ;
#34854=CARTESIAN_POINT ( 'NONE',  ( 122.7234281442452755, -5.638512984488999180, -18.83840828888717311 ) ) ;
#34855=CARTESIAN_POINT ( 'NONE',  ( 118.8092881442453290, -0.1624402480850797581, -16.17319339645315424 ) ) ;
#34857=CARTESIAN_POINT ( 'NONE',  ( 118.1852948109119836, -5.638512984488999180, -18.83840828888717311 ) ) ;
#34858=CARTESIAN_POINT ( 'NONE',  ( 119.6811727111058588, -1.267766418764730840, -16.93314635290706605 ) ) ;
#34859=CARTESIAN_POINT ( 'NONE',  ( 123.8012348109119642, -9.565557343593413364, -10.61323700422348004 ) ) ;
#34862=CARTESIAN_POINT ( 'NONE',  ( 115.6325948109119821, 0.2603800115204892296, -16.42320221600525088 ) ) ;
#34864=CARTESIAN_POINT ( 'NONE',  ( 124.7655881442452852, -9.859900752359378018, -12.68260735090039759 ) ) ;
#34866=CARTESIAN_POINT ( 'NONE',  ( 136.2267163768073601, -1.228667602531395620, -8.800274834874135976 ) ) ;
#34867=CARTESIAN_POINT ( 'NONE',  ( 122.8368814775786291, -1.561330072975668948, -17.79121239304076951 ) ) ;
#34869=CARTESIAN_POINT ( 'NONE',  ( 118.6391081442452986, -5.574606645277164318, -18.38911715685844683 ) ) ;
#34872=CARTESIAN_POINT ( 'NONE',  ( 115.0086014775786509, -4.089484607189486809, -7.948022111789456723 ) ) ;
#34874=CARTESIAN_POINT ( 'NONE',  ( 123.8012348109119642, -9.565557343593413364, -10.61323700422348004 ) ) ;
#34876=CARTESIAN_POINT ( 'NONE',  ( 120.2274548109119934, 0.5811942927096084288, -14.16772938898808931 ) ) ;
#34878=CARTESIAN_POINT ( 'NONE',  ( 121.1918081442452859, 0.9020085738987339008, -11.91225656197089222 ) ) ;
#34880=CARTESIAN_POINT ( 'NONE',  ( 116.9555940574772706, -2.443475742715334853, -17.86549347949429389 ) ) ;
#34881=CARTESIAN_POINT ( 'NONE',  ( 122.6667014775786413, -7.893985811506177619, -18.51759400769804742 ) ) ;
#34882=CARTESIAN_POINT ( 'NONE',  ( 118.9794681442453026, -9.261995988541697145, -16.69588392320189030 ) ) ;
#34883=CARTESIAN_POINT ( 'NONE',  ( 122.5532481442453019, 0.4262465694468514643, -12.03445270309931736 ) ) ;
#34884=CARTESIAN_POINT ( 'NONE',  ( 120.0005481442453146, -4.153390946401325223, -8.397313243818185668 ) ) ;
#34885=CARTESIAN_POINT ( 'NONE',  ( 128.2184548109119930, -5.622599431619523358, -7.441364641445410655 ) ) ;
#34886=CARTESIAN_POINT ( 'NONE',  ( 116.4834948109119779, -1.561330072975668504, -17.79121239304076951 ) ) ;
#34892=CARTESIAN_POINT ( 'NONE',  ( 125.1521348109119742, -1.861572684144302992, -17.39139446643087084 ) ) ;
#34893=CARTESIAN_POINT ( 'NONE',  ( 124.9357681442453014, -7.643976991954077427, -18.09477374809248928 ) ) ;
#34895=CARTESIAN_POINT ( 'NONE',  ( 114.0442481442453300, -7.643976991954077427, -18.09477374809248928 ) ) ;
#34898=CARTESIAN_POINT ( 'NONE',  ( 121.8725281442453223, -3.383040157471821630, -19.15922257007629170 ) ) ;
#34899=CARTESIAN_POINT ( 'NONE',  ( 123.2339681442453241, -6.344957434206665248, -7.627207830600338134 ) ) ;
#34901=CARTESIAN_POINT ( 'NONE',  ( 113.8740681442453138, 0.5811942927096154232, -14.16772938898807155 ) ) ;
#34906=CARTESIAN_POINT ( 'NONE',  ( 113.5904348109119866, -2.084020599724406786, -8.691656652584148546 ) ) ;
#34907=CARTESIAN_POINT ( 'NONE',  ( 113.6471614775786492, -5.638512984488999180, -18.83840828888717311 ) ) ;
#34911=CARTESIAN_POINT ( 'NONE',  ( 121.6456214775786293, 0.4262465694468514643, -12.03445270309931736 ) ) ;
#34912=CARTESIAN_POINT ( 'NONE',  ( 118.9227414775786542, 0.4262465694468514643, -12.03445270309931736 ) ) ;
#34913=CARTESIAN_POINT ( 'NONE',  ( 113.3068014775786594, -1.833838273342658809, -17.42832698103878286 ) ) ;
#34916=CIRCLE ( 'NONE', #37943, 3.099999999999998757 ) ;
#34919=CARTESIAN_POINT ( 'NONE',  ( 114.4413348109119823, -0.8288870151387760510, -10.36305467784173118 ) ) ;
#34926=CARTESIAN_POINT ( 'NONE',  ( 120.3976348109119812, -7.643976991954077427, -18.09477374809248928 ) ) ;
#34927=CARTESIAN_POINT ( 'NONE',  ( 113.3068014775786594, -1.833838273342658809, -17.42832698103878286 ) ) ;
#34928=CARTESIAN_POINT ( 'NONE',  ( 115.0086014775786509, -4.089484607189486809, -7.948022111789456723 ) ) ;
#34931=DIRECTION ( 'NONE',  ( 0.000000000000000000, 0.6004852223388321697, -0.7996358532186279566 ) ) ;
#34935=CARTESIAN_POINT ( 'NONE',  ( 112.7962614775786676, -3.383040157471821630, -19.15922257007629170 ) ) ;
#34936=CARTESIAN_POINT ( 'NONE',  ( 122.3263414775786373, -3.505236298600246325, -18.68346056562440793 ) ) ;
#34937=CARTESIAN_POINT ( 'NONE',  ( 118.5256548109119876, -8.899110576539710493, -16.42337572283490132 ) ) ;
#34938=CARTESIAN_POINT ( 'NONE',  ( 119.7535502067644444, -1.223627541775746730, -16.99192386690446810 ) ) ;
#34940=CARTESIAN_POINT ( 'NONE',  ( 115.7460481442453357, -10.15424416112533912, -14.75197769757731336 ) ) ;
#34945=CARTESIAN_POINT ( 'NONE',  ( 116.1431348109119881, -10.30919188438810075, -12.61870101168855918 ) ) ;
#34948=CARTESIAN_POINT ( 'NONE',  ( 113.2500748109119968, -6.344957434206662583, -7.627207830600332805 ) ) ;
#34950=CARTESIAN_POINT ( 'NONE',  ( 112.6828081442453282, -7.893985811506177619, -18.51759400769804742 ) ) ;
#34951=CARTESIAN_POINT ( 'NONE',  ( 114.9518748109119883, -1.834011780172310813, -8.268836392978581529 ) ) ;
#34952=CARTESIAN_POINT ( 'NONE',  ( 124.4252281442452812, -0.8288870151387760510, -10.36305467784173118 ) ) ;
#34955=CARTESIAN_POINT ( 'NONE',  ( 117.2776681442452968, -5.638512984489023161, -18.83840828888716601 ) ) ;
#34957=CARTESIAN_POINT ( 'NONE',  ( 115.5191414775786569, -6.222761293078241884, -8.102969835052219238 ) ) ;
#34961=CARTESIAN_POINT ( 'NONE',  ( 127.0298367773237089, -5.162954104783970877, -7.995796553879564783 ) ) ;
#34962=CARTESIAN_POINT ( 'NONE',  ( 126.2404814775786264, -9.261995988541697145, -16.69588392320189030 ) ) ;
#34964=CARTESIAN_POINT ( 'NONE',  ( 123.5176014775786228, -9.261995988541697145, -16.69588392320189030 ) ) ;
#34965=CARTESIAN_POINT ( 'NONE',  ( 116.1431348109119881, -10.30919188438810075, -12.61870101168855918 ) ) ;
#34967=CARTESIAN_POINT ( 'NONE',  ( 114.7816948109119863, -9.859900752359374465, -12.68260735090039404 ) ) ;
#34970=CARTESIAN_POINT ( 'NONE',  ( 116.5969481442453031, 0.5811942927096154232, -14.16772938898807155 ) ) ;
#34971=CARTESIAN_POINT ( 'NONE',  ( 116.7104014775786425, -8.899110576539710493, -16.42337572283490132 ) ) ;
#34973=CARTESIAN_POINT ( 'NONE',  ( 119.9438214775786378, -2.084020599724406786, -8.691656652584148546 ) ) ;
#34974=VECTOR ( 'NONE', #32514, 1000.000000000000000 ) ;
#34975=CARTESIAN_POINT ( 'NONE',  ( 117.9016614775786280, -9.988377603198976828, -10.36322818467138340 ) ) ;
#34976=CARTESIAN_POINT ( 'NONE',  ( 137.4406106298543193, 0.07373545144022489173, -14.57874919129496583 ) ) ;
#34982=CARTESIAN_POINT ( 'NONE',  ( 113.0231681442453322, 0.9020085738987339008, -11.91225656197089222 ) ) ;
#34983=CARTESIAN_POINT ( 'NONE',  ( 137.1799701741867921, -10.18481525785750819, -13.59600295436091066 ) ) ;
#34984=CARTESIAN_POINT ( 'NONE',  ( 113.8173414775786512, -9.565557343593413364, -10.61323700422348004 ) ) ;
#34988=CARTESIAN_POINT ( 'NONE',  ( 122.3620835773848654, -2.467220198592778413, -17.83387418641524391 ) ) ;
#34991=DIRECTION ( 'NONE',  ( 1.000000000000000000, 0.000000000000000000, 0.000000000000000000 ) ) ;
#34993=CARTESIAN_POINT ( 'NONE',  ( 116.4267681442453153, -3.383040157471821630, -19.15922257007629170 ) ) ;
#34994=CARTESIAN_POINT ( 'NONE',  ( 123.1772414775786189, -5.574606645277164318, -18.38911715685844683 ) ) ;
#34995=CARTESIAN_POINT ( 'NONE',  ( 118.3554748109119998, -9.565557343593413364, -10.61323700422348004 ) ) ;
#34997=CARTESIAN_POINT ( 'NONE',  ( 136.3514896075744218, -9.407894941071146988, -9.767453091696252088 ) ) ;
#34998=CARTESIAN_POINT ( 'NONE',  ( 123.9714148109119805, -0.4660016031367893996, -10.09054647747474043 ) ) ;
#35000=CARTESIAN_POINT ( 'NONE',  ( 113.9875214775786532, -8.899110576539710493, -16.42337572283490132 ) ) ;
#35002=CARTESIAN_POINT ( 'NONE',  ( 111.8886348109120092, -6.222761293078241884, -8.102969835052219238 ) ) ;
#35005=CARTESIAN_POINT ( 'NONE',  ( 119.2631014775786298, -9.565557343593413364, -10.61323700422348004 ) ) ;
#35007=CARTESIAN_POINT ( 'NONE',  ( 120.5110881442453206, -3.505236298600246325, -18.68346056562440793 ) ) ;
#35015=CARTESIAN_POINT ( 'NONE',  ( 118.4689281442453392, 0.9020085738987339008, -11.91225656197089222 ) ) ;
#35016=CARTESIAN_POINT ( 'NONE',  ( 113.4202548109119846, -10.30919188438810075, -12.61870101168855918 ) ) ;
#35021=CARTESIAN_POINT ( 'NONE',  ( 123.6310548109119765, -5.638512984488999180, -18.83840828888717311 ) ) ;
#35022=CARTESIAN_POINT ( 'NONE',  ( 112.5126281442453120, -10.30919188438810075, -12.61870101168855918 ) ) ;
#35023=CARTESIAN_POINT ( 'NONE',  ( 121.4754414775786131, -1.833838273342659697, -17.42832698103878286 ) ) ;
#35025=CARTESIAN_POINT ( 'NONE',  ( 123.7445081442452874, -1.561330072975668948, -17.79121239304076951 ) ) ;
#35026=CARTESIAN_POINT ( 'NONE',  ( 120.6245414775786458, -9.988377603198976828, -10.36322818467138340 ) ) ;
#35030=CARTESIAN_POINT ( 'NONE',  ( 117.0507614775786465, 0.1319031606808879209, -14.10382304977623669 ) ) ;
#35033=CARTESIAN_POINT ( 'NONE',  ( 121.0783548109119749, 0.2603800115204892296, -16.42320221600525088 ) ) ;
#35037=CARTESIAN_POINT ( 'NONE',  ( 116.7104014775786425, -0.4660016031367893996, -10.09054647747474043 ) ) ;
#35038=ORIENTED_EDGE ( 'NONE', *, *, #11170, .F. ) ;
#35041=CARTESIAN_POINT ( 'NONE',  ( 125.9001214775786224, -4.089484607189486809, -7.948022111789456723 ) ) ;
#35042=CARTESIAN_POINT ( 'NONE',  ( 122.8176765460471955, -2.191907684172563986, -18.20049396185734025 ) ) ;
#35043=CARTESIAN_POINT ( 'NONE',  ( 116.0864081442453113, -0.1624402480850797581, -16.17319339645315424 ) ) ;
#35045=CARTESIAN_POINT ( 'NONE',  ( 120.4543614775786295, -5.574606645277164318, -18.38911715685844683 ) ) ;
#35048=CARTESIAN_POINT ( 'NONE',  ( 122.3263414775786373, -3.505236298600246325, -18.68346056562440793 ) ) ;
#35050=CARTESIAN_POINT ( 'NONE',  ( 118.1852948109119836, -4.153390946401325223, -8.397313243818185668 ) ) ;
#35053=CARTESIAN_POINT ( 'NONE',  ( 115.7460481442453357, 0.9020085738987339008, -11.91225656197089222 ) ) ;
#35057=CARTESIAN_POINT ( 'NONE',  ( 122.0994348109119443, -10.15424416112533912, -14.75197769757731336 ) ) ;
#35059=CARTESIAN_POINT ( 'NONE',  ( 117.7314814775786260, -4.089484607189486809, -7.948022111789456723 ) ) ;
#35061=CARTESIAN_POINT ( 'NONE',  ( 115.4056881442453317, -2.084020599724388578, -8.691656652584157428 ) ) ;
#35065=CARTESIAN_POINT ( 'NONE',  ( 121.6456214775786293, -10.63000616557722466, -14.87417383870573495 ) ) ;
#35067=CARTESIAN_POINT ( 'NONE',  ( 128.2184548109119930, -10.81584935473217080, -14.15181583611863303 ) ) ;
#35068=CARTESIAN_POINT ( 'NONE',  ( 117.5045748109119756, -9.859900752359374465, -12.68260735090039404 ) ) ;
#35075=CARTESIAN_POINT ( 'NONE',  ( 115.0653281442453277, -6.344957434206662583, -7.627207830600332805 ) ) ;
#35076=CIRCLE ( 'NONE', #15448, 4.999999999999998224 ) ;
#35077=CARTESIAN_POINT ( 'NONE',  ( 111.9453614775786434, -1.561330072975668060, -17.79121239304076596 ) ) ;
#35078=CARTESIAN_POINT ( 'NONE',  ( 122.9503348109119827, 0.5811942927096110934, -14.16772938898807510 ) ) ;
#35079=CARTESIAN_POINT ( 'NONE',  ( 116.8805814775786445, -3.505236298600246325, -18.68346056562440793 ) ) ;
#35082=CARTESIAN_POINT ( 'NONE',  ( 120.7947214775786193, -9.261995988541697145, -16.69588392320189030 ) ) ;
#35083=CARTESIAN_POINT ( 'NONE',  ( 111.5020881442453202, -0.2054726073303936307, -16.14774885094461965 ) ) ;
#35086=CARTESIAN_POINT ( 'NONE',  ( 121.8158014775786171, -4.153390946401325223, -8.397313243818185668 ) ) ;
#35087=EDGE_LOOP ( 'NONE', ( #29287, #30192, #40119, #12 ) ) ;
#35089=CARTESIAN_POINT ( 'NONE',  ( 116.5402214775786405, 0.2603800115204892296, -16.42320221600525088 ) ) ;
#35090=CARTESIAN_POINT ( 'NONE',  ( 125.3895814775786448, -2.084020599724406786, -8.691656652584148546 ) ) ;
#35092=CARTESIAN_POINT ( 'NONE',  ( 136.2315975805936148, 0.5549518486163793618, -11.18187001423429727 ) ) ;
#35093=CARTESIAN_POINT ( 'NONE',  ( 120.7379948109119709, -10.63000616557722466, -14.87417383870573495 ) ) ;
#35096=CARTESIAN_POINT ( 'NONE',  ( 119.3765548109119834, -10.15424416112533912, -14.75197769757731336 ) ) ;
#35097=ORIENTED_EDGE ( 'NONE', *, *, #19220, .T. ) ;
#35099=CARTESIAN_POINT ( 'NONE',  ( 114.4980614775786592, -7.893985811506177619, -18.51759400769804742 ) ) ;
#35100=CARTESIAN_POINT ( 'NONE',  ( 123.9146881442452894, -10.15424416112533912, -14.75197769757731336 ) ) ;
#35104=CARTESIAN_POINT ( 'NONE',  ( 124.9924948109119924, -4.089484607189486809, -7.948022111789456723 ) ) ;
#35109=CARTESIAN_POINT ( 'NONE',  ( 123.9146881442452894, 0.9020085738987339008, -11.91225656197089222 ) ) ;
#35110=CARTESIAN_POINT ( 'NONE',  ( 122.3830681442452857, -8.166667518702819706, -8.995218007635861213 ) ) ;
#35111=CARTESIAN_POINT ( 'NONE',  ( 122.3830681442452857, -1.833838273342659697, -17.42832698103878286 ) ) ;
#35112=CARTESIAN_POINT ( 'NONE',  ( 120.6245414775786458, -0.1624402480850797581, -16.17319339645315424 ) ) ;
#35114=CARTESIAN_POINT ( 'NONE',  ( 115.9729548109119861, -6.344957434206662583, -7.627207830600332805 ) ) ;
#35115=VERTEX_POINT ( 'NONE', #44402 ) ;
#35120=CARTESIAN_POINT ( 'NONE',  ( 125.1059481442452750, -8.166667518702819706, -8.995218007635861213 ) ) ;
#35121=CARTESIAN_POINT ( 'NONE',  ( 125.9568481442452850, -3.505236298600246325, -18.68346056562440793 ) ) ;
#35123=CARTESIAN_POINT ( 'NONE',  ( 113.8740681442453138, -9.859900752359374465, -12.68260735090039404 ) ) ;
#35127=CARTESIAN_POINT ( 'NONE',  ( 123.6877814775786533, -3.383040157471821630, -19.15922257007629170 ) ) ;
#35128=CARTESIAN_POINT ( 'NONE',  ( 125.4463081442452932, -5.638512984488999180, -18.83840828888717311 ) ) ;
#35130=CARTESIAN_POINT ( 'NONE',  ( 116.1431348109119881, -10.30919188438810075, -12.61870101168855918 ) ) ;
#35136=CARTESIAN_POINT ( 'NONE',  ( 115.4056881442453459, -2.084020599724406786, -8.691656652584148546 ) ) ;
#35138=CARTESIAN_POINT ( 'NONE',  ( 113.4769814775786330, -10.63000616557722466, -14.87417383870573495 ) ) ;
#35139=B_SPLINE_CURVE_WITH_KNOTS ( 'NONE', 3,
 ( #39282, #8047, #35844, #4617, #18538, #32429, #10581, #24481, #11922, #36521, #22176, #29024, #25822 ),
 .UNSPECIFIED., .F., .F.,
 ( 4, 3, 3, 3, 4 ),
 ( 1.568264261493034943E-06, 2.784814680393055196E-05, 5.575405619718069985E-05, 9.782819182226189052E-05, 0.0001187612790815211953 ),
 .UNSPECIFIED. ) ;
#35142=CARTESIAN_POINT ( 'NONE',  ( 120.7947214775786193, -0.8288870151387760510, -10.36305467784173118 ) ) ;
#35143=UNCERTAINTY_MEASURE_WITH_UNIT (LENGTH_MEASURE( 1.000000000000000082E-05 ), #10523, 'distance_accuracy_value', 'NONE');
#35144=CARTESIAN_POINT ( 'NONE',  ( 120.6812681442452941, 0.1319031606808879209, -14.10382304977623669 ) ) ;
#35145=CARTESIAN_POINT ( 'NONE',  ( 126.2404814775786264, -9.261995988541697145, -16.69588392320189030 ) ) ;
#35147=STYLED_ITEM ( 'NONE', ( #7235 ), #24824 ) ;
#35148=CARTESIAN_POINT ( 'NONE',  ( 124.4252281442452812, -0.8288870151387760510, -10.36305467784173118 ) ) ;
#35150=CARTESIAN_POINT ( 'NONE',  ( 113.4769814775786330, 0.4262465694468514643, -12.03445270309931736 ) ) ;
#35151=ORIENTED_EDGE ( 'NONE', *, *, #9703, .T. ) ;
#35152=CARTESIAN_POINT ( 'NONE',  ( 126.3999550322210155, -9.219482243445801473, -16.02874797595598366 ) ) ;
#35155=ORIENTED_EDGE ( 'NONE', *, *, #40638, .T. ) ;
#35156=CARTESIAN_POINT ( 'NONE',  ( 117.6747548109119919, -7.643976991954077427, -18.09477374809248928 ) ) ;
#35157=CARTESIAN_POINT ( 'NONE',  ( 114.7816948109119863, -9.859900752359374465, -12.68260735090039404 ) ) ;
#35167=CARTESIAN_POINT ( 'NONE',  ( 113.6471614775786492, -5.638512984488999180, -18.83840828888717311 ) ) ;
#35168=CARTESIAN_POINT ( 'NONE',  ( 124.9357681442453014, -7.643976991954077427, -18.09477374809248928 ) ) ;
#35169=CARTESIAN_POINT ( 'NONE',  ( 116.1431348109119881, 0.1319031606808879209, -14.10382304977623669 ) ) ;
#35172=CARTESIAN_POINT ( 'NONE',  ( 117.7314814775786260, -5.574606645277164318, -18.38911715685844683 ) ) ;
#35177=CARTESIAN_POINT ( 'NONE',  ( 115.0653281442453277, -6.344957434206662583, -7.627207830600332805 ) ) ;
#35179=CARTESIAN_POINT ( 'NONE',  ( 116.9373081442452929, -8.166667518702817929, -8.995218007635861213 ) ) ;
#35180=CARTESIAN_POINT ( 'NONE',  ( 114.2711548109119946, -9.988377603198976828, -10.36322818467138340 ) ) ;
#35182=CARTESIAN_POINT ( 'NONE',  ( 112.1155414775786454, 0.9020085738987339008, -11.91225656197089222 ) ) ;
#35183=CARTESIAN_POINT ( 'NONE',  ( 113.3635281442453504, -9.988377603198976828, -10.36322818467138340 ) ) ;
#35191=CARTESIAN_POINT ( 'NONE',  ( 115.9162281442453235, -5.574606645277164318, -18.38911715685844683 ) ) ;
#35194=CARTESIAN_POINT ( 'NONE',  ( 122.8169364575754798, -1.016270020561755860, -17.26805140881366896 ) ) ;
#35196=CARTESIAN_POINT ( 'NONE',  ( 127.2313854077063979, -5.268148382571362198, -7.901566705240425925 ) ) ;
#35197=CARTESIAN_POINT ( 'NONE',  ( 125.4463081442452932, -5.638512984488999180, -18.83840828888717311 ) ) ;
#35198=CARTESIAN_POINT ( 'NONE',  ( 138.2184548109119930, -2.520019956603805511, -15.26558354049377009 ) ) ;
#35199=( BOUNDED_SURFACE ( )  B_SPLINE_SURFACE ( 1, 2, ( 
 ( #38971, #11617, #35993, #42411, #11175, #11398, #21204, #18465, #32355, #25307, #22105, #31905, #4764, #18233, #39201, #4082, #7740 ),
 ( #29163, #43077, #24850, #7288, #21651, #35083, #35542, #3863, #17785, #14364, #28278, #38742, #21427, #7512, #35311, #670, #2468 ) ),
 .UNSPECIFIED., .F., .F., .T. ) 
 B_SPLINE_SURFACE_WITH_KNOTS ( ( 2, 2 ),
 ( 3, 2, 2, 2, 2, 2, 2, 2, 3 ),
 ( 0.000000000000000000, 1.000000000000000000 ),
 ( 0.000000000000000000, 0.1250000000000000000, 0.2500000000000000000, 0.3750000000000000000, 0.5000000000000000000, 0.6250000000000000000, 0.7500000000000000000, 0.8750000000000000000, 1.000000000000000000 ),
 .UNSPECIFIED. ) 
 GEOMETRIC_REPRESENTATION_ITEM ( )  RATIONAL_B_SPLINE_SURFACE ( (
 ( 1.000000000000000000, 0.9238795325112869605, 1.000000000000000000, 0.9238795325112869605, 1.000000000000000000, 0.9238795325112869605, 1.000000000000000000, 0.9238795325112869605, 1.000000000000000000, 0.9238795325112869605, 1.000000000000000000, 0.9238795325112869605, 1.000000000000000000, 0.9238795325112869605, 1.000000000000000000, 0.9238795325112869605, 1.000000000000000000),
 ( 1.000000000000000000, 0.9238795325112869605, 1.000000000000000000, 0.9238795325112869605, 1.000000000000000000, 0.9238795325112869605, 1.000000000000000000, 0.9238795325112869605, 1.000000000000000000, 0.9238795325112869605, 1.000000000000000000, 0.9238795325112869605, 1.000000000000000000, 0.9238795325112869605, 1.000000000000000000, 0.9238795325112869605, 1.000000000000000000) ) ) 
 REPRESENTATION_ITEM ( '' )  SURFACE ( )  );
#35200=CARTESIAN_POINT ( 'NONE',  ( 124.7088614775786226, 0.2603800115204892296, -16.42320221600525088 ) ) ;
#35201=CARTESIAN_POINT ( 'NONE',  ( 115.0086014775786509, -4.089484607189486809, -7.948022111789456723 ) ) ;
#35204=CARTESIAN_POINT ( 'NONE',  ( 115.6893214775786447, -9.859900752359374465, -12.68260735090039404 ) ) ;
#35206=CARTESIAN_POINT ( 'NONE',  ( 125.9001214775786224, -4.089484607189486809, -7.948022111789456723 ) ) ;
#35207=CARTESIAN_POINT ( 'NONE',  ( 119.1496481442453046, -3.383040157471821630, -19.15922257007629170 ) ) ;
#35209=CARTESIAN_POINT ( 'NONE',  ( 116.6536748109119941, -10.15424416112533912, -14.75197769757731336 ) ) ;
#35211=CARTESIAN_POINT ( 'NONE',  ( 119.8870948109119752, -0.8288870151387760510, -10.36305467784173118 ) ) ;
#35213=CARTESIAN_POINT ( 'NONE',  ( 116.5969481442453031, 0.5811942927096154232, -14.16772938898807155 ) ) ;
#35214=CARTESIAN_POINT ( 'NONE',  ( 136.1682244357625109, 0.5463004873506387415, -15.67897323516908159 ) ) ;
#35217=FACE_OUTER_BOUND ( 'NONE', #10483, .T. ) ;
#35219=CARTESIAN_POINT ( 'NONE',  ( 116.1431348109119881, -10.30919188438810075, -12.61870101168855918 ) ) ;
#35220=CARTESIAN_POINT ( 'NONE',  ( 136.0320772899216877, -10.73234492129708428, -14.10229740280723476 ) ) ;
#35223=CARTESIAN_POINT ( 'NONE',  ( 117.5613014775786525, -10.15424416112534267, -14.75197769757730804 ) ) ;
#35225=CARTESIAN_POINT ( 'NONE',  ( 113.4769814775786330, 0.4262465694468514643, -12.03445270309931736 ) ) ;
#35226=CARTESIAN_POINT ( 'NONE',  ( 111.9261565460472099, -2.191907684172563986, -18.20049396185734025 ) ) ;
#35227=CARTESIAN_POINT ( 'NONE',  ( 118.5823814775786502, -1.834011780172310591, -8.268836392978581529 ) ) ;
#35228=CARTESIAN_POINT ( 'NONE',  ( 117.7882081442453170, -6.344957434206665248, -7.627207830600338134 ) ) ;
#35229=CARTESIAN_POINT ( 'NONE',  ( 124.3685014775786328, 0.4262465694468514643, -12.03445270309931736 ) ) ;
#35230=CARTESIAN_POINT ( 'NONE',  ( 120.3976348109119812, -7.643976991954077427, -18.09477374809248928 ) ) ;
#35232=CARTESIAN_POINT ( 'NONE',  ( 136.2315975805923074, -7.075343981943422733, -7.974264555883486594 ) ) ;
#35233=CARTESIAN_POINT ( 'NONE',  ( 121.8158014775786171, -5.638512984488999180, -18.83840828888717311 ) ) ;
#35235=CARTESIAN_POINT ( 'NONE',  ( 120.5678148109119832, -1.833838273342659253, -17.42832698103878286 ) ) ;
#35236=CARTESIAN_POINT ( 'NONE',  ( 114.0442481442453300, -7.643976991954077427, -18.09477374809248928 ) ) ;
#35239=CARTESIAN_POINT ( 'NONE',  ( 119.3198281442452924, -9.859900752359374465, -12.68260735090039404 ) ) ;
#35240=CARTESIAN_POINT ( 'NONE',  ( 121.8158014775786171, -4.153390946401325223, -8.397313243818185668 ) ) ;
#35241=DIRECTION ( 'NONE',  ( 0.000000000000000000, 0.6004852223388321697, -0.7996358532186279566 ) ) ;
#35246=CARTESIAN_POINT ( 'NONE',  ( 119.0361948109119652, -7.893985811506177619, -18.51759400769804742 ) ) ;
#35247=CARTESIAN_POINT ( 'NONE',  ( 113.7038881442453402, -3.383040157471821630, -19.15922257007629170 ) ) ;
#35249=CARTESIAN_POINT ( 'NONE',  ( 114.5547881442453217, -5.638512984488999180, -18.83840828888717311 ) ) ;
#35252=AXIS2_PLACEMENT_3D ( 'NONE', #26796, #9465, #19721 ) ;
#35253=CARTESIAN_POINT ( 'NONE',  ( 121.2485348109119769, -0.4660016031367893996, -10.09054647747474043 ) ) ;
#35254=CARTESIAN_POINT ( 'NONE',  ( 116.5402214775786405, 0.2603800115204892296, -16.42320221600525088 ) ) ;
#35255=CARTESIAN_POINT ( 'NONE',  ( 122.0427081442452817, -9.859900752359378018, -12.68260735090039759 ) ) ;
#35256=CARTESIAN_POINT ( 'NONE',  ( 111.8319081442453182, -4.153390946401321671, -8.397313243818183892 ) ) ;
#35257=CARTESIAN_POINT ( 'NONE',  ( 123.3474214775786209, -9.988377603198976828, -10.36322818467138340 ) ) ;
#35260=CARTESIAN_POINT ( 'NONE',  ( 117.4478481442453131, -9.565557343593413364, -10.61323700422348004 ) ) ;
#35263=CARTESIAN_POINT ( 'NONE',  ( 120.9649014775786355, -3.383040157471821630, -19.15922257007629170 ) ) ;
#35266=CARTESIAN_POINT ( 'NONE',  ( 120.8514481442452961, -7.893985811506177619, -18.51759400769804742 ) ) ;
#35269=CARTESIAN_POINT ( 'NONE',  ( 124.7088614775786226, 0.2603800115204892296, -16.42320221600525088 ) ) ;
#35270=CARTESIAN_POINT ( 'NONE',  ( 119.9481648144346622, -2.280480477428469488, -18.08254604495227014 ) ) ;
#35271=CARTESIAN_POINT ( 'NONE',  ( 117.0507614775786465, 0.1319031606808879209, -14.10382304977623669 ) ) ;
#35274=CARTESIAN_POINT ( 'NONE',  ( 120.8514481442452961, -2.084020599724406786, -8.691656652584148546 ) ) ;
#35275=CARTESIAN_POINT ( 'NONE',  ( 121.7590748109119687, -7.893985811506158079, -18.51759400769805453 ) ) ;
#35276=CARTESIAN_POINT ( 'NONE',  ( 121.5321681442453183, -0.1624402480850797581, -16.17319339645315424 ) ) ;
#35279=CARTESIAN_POINT ( 'NONE',  ( 117.6747548109119919, -7.643976991954077427, -18.09477374809248928 ) ) ;
#35281=CARTESIAN_POINT ( 'NONE',  ( 115.0086014775786509, -4.089484607189486809, -7.948022111789456723 ) ) ;
#35282=CARTESIAN_POINT ( 'NONE',  ( 125.3895814775786448, -2.084020599724406786, -8.691656652584148546 ) ) ;
#35285=CARTESIAN_POINT ( 'NONE',  ( 119.2063748109119814, -7.894159318335828068, -9.358103419637847864 ) ) ;
#35287=CARTESIAN_POINT ( 'NONE',  ( 116.6536748109119941, 0.9020085738987339008, -11.91225656197089222 ) ) ;
#35293=CARTESIAN_POINT ( 'NONE',  ( 121.0216281442452981, -1.561330072975668948, -17.79121239304076951 ) ) ;
#35295=CARTESIAN_POINT ( 'NONE',  ( 127.4620922276975818, -9.182459662741596418, -9.793643861152926178 ) ) ;
#35296=CARTESIAN_POINT ( 'NONE',  ( 122.0427081442452817, -9.859900752359378018, -12.68260735090039759 ) ) ;
#35300=CARTESIAN_POINT ( 'NONE',  ( 125.6732148109119862, 0.5811942927096110934, -14.16772938898807510 ) ) ;
#35304=CARTESIAN_POINT ( 'NONE',  ( 114.3846081442453197, -10.63000616557722466, -14.87417383870573495 ) ) ;
#35305=CARTESIAN_POINT ( 'NONE',  ( 126.0135748109119902, -1.833838273342660141, -17.42832698103878286 ) ) ;
#35306=CARTESIAN_POINT ( 'NONE',  ( 124.5386814775786206, -5.638512984488999180, -18.83840828888717311 ) ) ;
#35307=CARTESIAN_POINT ( 'NONE',  ( 120.3976348109119812, -7.643976991954077427, -18.09477374809248928 ) ) ;
#35308=CARTESIAN_POINT ( 'NONE',  ( 126.3509913982043571, -3.720841214467113911, -8.457387538663136084 ) ) ;
#35310=CARTESIAN_POINT ( 'NONE',  ( 122.2696148109119889, -4.089484607189486809, -7.948022111789456723 ) ) ;
#35311=CARTESIAN_POINT ( 'NONE',  ( 112.0126281442453120, -9.814174330883659536, -12.68911139247490105 ) ) ;
#35314=CARTESIAN_POINT ( 'NONE',  ( 112.0588148109119828, 0.5811942927096154232, -14.16772938898807155 ) ) ;
#35316=CIRCLE ( 'NONE', #22967, 3.499999999999998668 ) ;
#35318=CARTESIAN_POINT ( 'NONE',  ( 120.4543614775786295, -4.089484607189486809, -7.948022111789456723 ) ) ;
#35319=CARTESIAN_POINT ( 'NONE',  ( 135.3184548109119874, -10.44474571748257041, -15.59668151425567650 ) ) ;
#35325=CARTESIAN_POINT ( 'NONE',  ( 123.3474214775786209, -9.988377603198976828, -10.36322818467138340 ) ) ;
#35328=CARTESIAN_POINT ( 'NONE',  ( 122.2696148109119889, -5.574606645277164318, -18.38911715685844683 ) ) ;
#35329=ORIENTED_EDGE ( 'NONE', *, *, #23091, .T. ) ;
#35330=CARTESIAN_POINT ( 'NONE',  ( 114.6115148109119986, -3.383040157471821630, -19.15922257007629170 ) ) ;
#35334=CARTESIAN_POINT ( 'NONE',  ( 124.3117748109119844, -10.30919188438810075, -12.61870101168855918 ) ) ;
#35337=CARTESIAN_POINT ( 'NONE',  ( 122.2128881442453263, -1.834011780172310813, -8.268836392978581529 ) ) ;
#35338=CARTESIAN_POINT ( 'NONE',  ( 121.5888948109119809, -10.30919188438810075, -12.61870101168855918 ) ) ;
#35339=CARTESIAN_POINT ( 'NONE',  ( 122.4965214775786251, 0.1319031606808879209, -14.10382304977623669 ) ) ;
#35340=CARTESIAN_POINT ( 'NONE',  ( 118.6958348109119754, -3.505236298600246325, -18.68346056562440793 ) ) ;
#35342=CARTESIAN_POINT ( 'NONE',  ( 118.5256548109119876, -0.4660016031367893996, -10.09054647747474043 ) ) ;
#35350=CARTESIAN_POINT ( 'NONE',  ( 126.2404814775786264, -9.261995988541697145, -16.69588392320189030 ) ) ;
#35351=CARTESIAN_POINT ( 'NONE',  ( 112.9097148109120070, 0.2603800115204892296, -16.42320221600525088 ) ) ;
#35353=CARTESIAN_POINT ( 'NONE',  ( 112.9097148109120070, -9.565557343593413364, -10.61323700422348004 ) ) ;
#35355=CARTESIAN_POINT ( 'NONE',  ( 119.1496481442453046, -6.222761293078222344, -8.102969835052219238 ) ) ;
#35356=CARTESIAN_POINT ( 'NONE',  ( 111.2646872982215029, -8.898115269823104967, -16.42473896082089269 ) ) ;
#35357=CARTESIAN_POINT ( 'NONE',  ( 123.3474214775786209, -9.988377603198976828, -10.36322818467138340 ) ) ;
#35360=CARTESIAN_POINT ( 'NONE',  ( 117.7882081442453170, -6.344957434206665248, -7.627207830600338134 ) ) ;
#35364=ORIENTED_EDGE ( 'NONE', *, *, #2472, .T. ) ;
#35366=CARTESIAN_POINT ( 'NONE',  ( 116.1431348109119881, 0.1319031606808879209, -14.10382304977623669 ) ) ;
#35367=CARTESIAN_POINT ( 'NONE',  ( 126.3539348109119800, -4.153390946401325223, -8.397313243818185668 ) ) ;
#35368=CARTESIAN_POINT ( 'NONE',  ( 112.9664414775786412, 0.5811942927096154232, -14.16772938898807155 ) ) ;
#35369=CARTESIAN_POINT ( 'NONE',  ( 124.1983214775786166, -1.833838273342659697, -17.42832698103878286 ) ) ;
#35370=CARTESIAN_POINT ( 'NONE',  ( 119.4332814775786318, -8.899110576539710493, -16.42337572283490132 ) ) ;
#35371=CARTESIAN_POINT ( 'NONE',  ( 114.7816948109119863, -9.859900752359374465, -12.68260735090039404 ) ) ;
#35373=CARTESIAN_POINT ( 'NONE',  ( 125.6164881442453094, -9.565557343593413364, -10.61323700422348004 ) ) ;
#35376=CARTESIAN_POINT ( 'NONE',  ( 114.0442481442453300, -7.643976991954077427, -18.09477374809248928 ) ) ;
#35382=CARTESIAN_POINT ( 'NONE',  ( 123.4608748109119745, 0.4262465694468514643, -12.03445270309931736 ) ) ;
#35383=AXIS2_PLACEMENT_3D ( 'NONE', #38941, #21174, #28026 ) ;
#35386=CARTESIAN_POINT ( 'NONE',  ( 118.0718414775786442, -0.8288870151387760510, -10.36305467784173118 ) ) ;
#35387=CARTESIAN_POINT ( 'NONE',  ( 118.2987481442453088, -7.894159318335828068, -9.358103419637847864 ) ) ;
#35393=CARTESIAN_POINT ( 'NONE',  ( 121.1141531944929284, -1.036737761566197014, -17.24079555149560861 ) ) ;
#35396=CARTESIAN_POINT ( 'NONE',  ( 113.0231681442453322, 0.9020085738987339008, -11.91225656197089222 ) ) ;
#35397=CARTESIAN_POINT ( 'NONE',  ( 113.3068014775786594, -8.166667518702817929, -8.995218007635859436 ) ) ;
#35398=CARTESIAN_POINT ( 'NONE',  ( 116.7671281442453335, -7.643976991954077427, -18.09477374809248928 ) ) ;
#35399=CARTESIAN_POINT ( 'NONE',  ( 128.2184548109119930, -10.44474571748257041, -15.59668151425567650 ) ) ;
#35400=ORIENTED_EDGE ( 'NONE', *, *, #3827, .F. ) ;
#35401=CARTESIAN_POINT ( 'NONE',  ( 114.4413348109119823, -0.8288870151387760510, -10.36305467784173118 ) ) ;
#35406=CARTESIAN_POINT ( 'NONE',  ( 115.0086014775786509, -4.089484607189486809, -7.948022111789456723 ) ) ;
#35408=CARTESIAN_POINT ( 'NONE',  ( 116.7104014775786425, -0.4660016031367893996, -10.09054647747474043 ) ) ;
#35411=CARTESIAN_POINT ( 'NONE',  ( 114.3278814775786429, -10.30919188438810075, -12.61870101168855918 ) ) ;
#35412=CARTESIAN_POINT ( 'NONE',  ( 113.5904348109119866, -7.893985811506177619, -18.51759400769804742 ) ) ;
#35420=CARTESIAN_POINT ( 'NONE',  ( 116.9373081442452929, -1.833838273342659253, -17.42832698103878286 ) ) ;
#35424=CARTESIAN_POINT ( 'NONE',  ( 127.3669547543521929, -5.331670183757885262, -7.838481523644200699 ) ) ;
#35425=CARTESIAN_POINT ( 'NONE',  ( 116.0864081442453113, -0.1624402480850797581, -16.17319339645315424 ) ) ;
#35426=CARTESIAN_POINT ( 'NONE',  ( 135.4185995790644483, 1.087834318095270758, -12.63462434935058276 ) ) ;
#35427=CARTESIAN_POINT ( 'NONE',  ( 122.4397948109119767, -9.988377603198976828, -10.36322818467138340 ) ) ;
#35428=CARTESIAN_POINT ( 'NONE',  ( 117.6180281442453150, -0.4660016031367893996, -10.09054647747474043 ) ) ;
#35429=ADVANCED_FACE ( 'NONE', ( #38429 ), #2942, .T. ) ;
#35432=CARTESIAN_POINT ( 'NONE',  ( 114.1577014775786552, -3.505236298600246325, -18.68346056562440793 ) ) ;
#35433=CARTESIAN_POINT ( 'NONE',  ( 112.3991748109119868, -8.166667518702817929, -8.995218007635859436 ) ) ;
#35434=CARTESIAN_POINT ( 'NONE',  ( 117.2776681442452968, -5.638512984488999180, -18.83840828888717311 ) ) ;
#35435=CARTESIAN_POINT ( 'NONE',  ( 115.1220548109119761, -1.833838273342658809, -17.42832698103878286 ) ) ;
#35437=CARTESIAN_POINT ( 'NONE',  ( 122.1561614775786353, -8.899110576539710493, -16.42337572283490132 ) ) ;
#35438=CARTESIAN_POINT ( 'NONE',  ( 117.4478481442453131, 0.2603800115204892296, -16.42320221600525088 ) ) ;
#35439=CARTESIAN_POINT ( 'NONE',  ( 136.6755514030890026, 0.3990558587189101947, -15.48381416683688094 ) ) ;
#35446=CARTESIAN_POINT ( 'NONE',  ( 115.8595014775786609, -1.834011780172310813, -8.268836392978581529 ) ) ;
#35447=CARTESIAN_POINT ( 'NONE',  ( 135.7778351054948587, -10.78233002638890348, -14.13261394578744579 ) ) ;
#35448=CARTESIAN_POINT ( 'NONE',  ( 114.0442481442453300, -7.643976991954077427, -18.09477374809248928 ) ) ;
#35450=CARTESIAN_POINT ( 'NONE',  ( 117.1642148109119859, -0.8288870151387769392, -10.36305467784172940 ) ) ;
#35457=CARTESIAN_POINT ( 'NONE',  ( 118.5256548109119876, -0.4660016031367893996, -10.09054647747474043 ) ) ;
#35458=CARTESIAN_POINT ( 'NONE',  ( 118.2987481442453088, -7.894159318335828068, -9.358103419637847864 ) ) ;
#35459=CARTESIAN_POINT ( 'NONE',  ( 112.4559014775786778, -0.1624402480850797581, -16.17319339645315424 ) ) ;
#35460=VERTEX_POINT ( 'NONE', #26620 ) ;
#35462=CARTESIAN_POINT ( 'NONE',  ( 122.6099748109119929, -9.261995988541697145, -16.69588392320189030 ) ) ;
#35464=CARTESIAN_POINT ( 'NONE',  ( 118.3554748109119998, -9.565557343593413364, -10.61323700422348004 ) ) ;
#35466=CARTESIAN_POINT ( 'NONE',  ( 116.6536748109119941, -10.15424416112533912, -14.75197769757731336 ) ) ;
#35469=CARTESIAN_POINT ( 'NONE',  ( 121.5888948109119809, 0.1319031606808879209, -14.10382304977623669 ) ) ;
#35470=CARTESIAN_POINT ( 'NONE',  ( 125.3328548109119964, -0.8288870151387760510, -10.36305467784173118 ) ) ;
#35477=CARTESIAN_POINT ( 'NONE',  ( 116.8238548109119819, -4.089484607189486809, -7.948022111789456723 ) ) ;
#35478=CARTESIAN_POINT ( 'NONE',  ( 114.6682414775786469, -1.561330072975668060, -17.79121239304076596 ) ) ;
#35480=CARTESIAN_POINT ( 'NONE',  ( 114.2144281442453178, -8.166667518702817929, -8.995218007635859436 ) ) ;
#35483=CARTESIAN_POINT ( 'NONE',  ( 124.5386814775786206, -5.638512984488999180, -18.83840828888717311 ) ) ;
#35484=CARTESIAN_POINT ( 'NONE',  ( 116.1998614775786507, -10.63000616557722466, -14.87417383870573495 ) ) ;
#35485=CARTESIAN_POINT ( 'NONE',  ( 121.1350814775786233, -9.859900752359378018, -12.68260735090039759 ) ) ;
#35487=CARTESIAN_POINT ( 'NONE',  ( 123.8012348109119642, 0.2603800115204892296, -16.42320221600525088 ) ) ;
#35488=CARTESIAN_POINT ( 'NONE',  ( 122.4965214775786251, -10.30919188438810075, -12.61870101168855918 ) ) ;
#35492=CARTESIAN_POINT ( 'NONE',  ( 117.3911214775786505, -7.894159318335828068, -9.358103419637847864 ) ) ;
#35496=CARTESIAN_POINT ( 'NONE',  ( 120.4543614775786295, -4.089484607189486809, -7.948022111789456723 ) ) ;
#35498=CARTESIAN_POINT ( 'NONE',  ( 120.1140014775786398, -1.561330072975668504, -17.79121239304076951 ) ) ;
#35499=ORIENTED_EDGE ( 'NONE', *, *, #22969, .F. ) ;
#35503=CARTESIAN_POINT ( 'NONE',  ( 119.6392035773848761, -2.467220198592778413, -17.83387418641524391 ) ) ;
#35504=CARTESIAN_POINT ( 'NONE',  ( 116.8238548109119819, -5.574606645277164318, -18.38911715685844683 ) ) ;
#35507=CARTESIAN_POINT ( 'NONE',  ( 119.3765548109119834, -10.15424416112533912, -14.75197769757731336 ) ) ;
#35509=CARTESIAN_POINT ( 'NONE',  ( 120.1707281442453166, -9.565557343593413364, -10.61323700422348004 ) ) ;
#35511=CARTESIAN_POINT ( 'NONE',  ( 118.0151148109119816, 0.4262465694468514643, -12.03445270309931736 ) ) ;
#35512=CARTESIAN_POINT ( 'NONE',  ( 111.9453614775786434, -1.561330072975668060, -17.79121239304076596 ) ) ;
#35513=CARTESIAN_POINT ( 'NONE',  ( 117.9583881442453048, -10.30919188438810075, -12.61870101168855918 ) ) ;
#35514=CARTESIAN_POINT ( 'NONE',  ( 113.1366214775786432, -1.834011780172310813, -8.268836392978581529 ) ) ;
#35516=CARTESIAN_POINT ( 'NONE',  ( 120.3976348109119812, -7.643976991954077427, -18.09477374809248928 ) ) ;
#35518=CARTESIAN_POINT ( 'NONE',  ( 121.8725281442453223, -3.383040157471821630, -19.15922257007629170 ) ) ;
#35521=CARTESIAN_POINT ( 'NONE',  ( 128.2184548109119930, 1.087851763053662602, -12.63461456455805276 ) ) ;
#35523=CARTESIAN_POINT ( 'NONE',  ( 124.7655881442452852, 0.5811942927096110934, -14.16772938898807510 ) ) ;
#35527=CARTESIAN_POINT ( 'NONE',  ( 120.1140014775786398, -7.894159318335828068, -9.358103419637847864 ) ) ;
#35530=CARTESIAN_POINT ( 'NONE',  ( 114.6490365460471992, -2.191907684172563986, -18.20049396185734025 ) ) ;
#35533=CARTESIAN_POINT ( 'NONE',  ( 114.4980614775786592, -7.893985811506177619, -18.51759400769804742 ) ) ;
#35534=CARTESIAN_POINT ( 'NONE',  ( 114.4980614775786592, -7.893985811506177619, -18.51759400769804742 ) ) ;
#35536=CARTESIAN_POINT ( 'NONE',  ( 120.2841814775786276, -10.15424416112533912, -14.75197769757731336 ) ) ;
#35538=CARTESIAN_POINT ( 'NONE',  ( 112.3424481442453384, -3.505236298600246325, -18.68346056562440793 ) ) ;
#35541=CARTESIAN_POINT ( 'NONE',  ( 121.9859814775786333, 0.2603800115204892296, -16.42320221600525088 ) ) ;
#35542=CARTESIAN_POINT ( 'NONE',  ( 111.5588148109119828, 0.08617673920517221475, -14.09731900820172967 ) ) ;
#35548=CARTESIAN_POINT ( 'NONE',  ( 118.9794681442453026, -9.261995988541697145, -16.69588392320189030 ) ) ;
#35549=CARTESIAN_POINT ( 'NONE',  ( 136.5935259641917412, -10.11762552186683450, -15.62548657175932476 ) ) ;
#35551=CARTESIAN_POINT ( 'NONE',  ( 136.2632467228194173, 0.5429805449437086207, -11.18076796992574806 ) ) ;
#35552=CARTESIAN_POINT ( 'NONE',  ( 125.4463081442452932, -5.638512984488999180, -18.83840828888717311 ) ) ;
#35554=CARTESIAN_POINT ( 'NONE',  ( 124.4252281442452812, -0.8288870151387760510, -10.36305467784173118 ) ) ;
#35556=CARTESIAN_POINT ( 'NONE',  ( 119.8303681442453126, -10.63000616557722466, -14.87417383870573495 ) ) ;
#35558=CARTESIAN_POINT ( 'NONE',  ( 120.5678148109119832, -8.166667518702801942, -8.995218007635848778 ) ) ;
#35559=CARTESIAN_POINT ( 'NONE',  ( 135.7778351054869859, -5.603397541288348549, -7.474883969788649551 ) ) ;
#35561=CARTESIAN_POINT ( 'NONE',  ( 126.2404814775786264, -9.261995988541697145, -16.69588392320189030 ) ) ;
#35565=CARTESIAN_POINT ( 'NONE',  ( 124.9924948109119924, -4.089484607189486809, -7.948022111789456723 ) ) ;
#35566=CARTESIAN_POINT ( 'NONE',  ( 121.9859814775786333, 0.2603800115204892296, -16.42320221600525088 ) ) ;
#35567=CARTESIAN_POINT ( 'NONE',  ( 121.7590748109119687, -2.084020599724406786, -8.691656652584148546 ) ) ;
#35569=CARTESIAN_POINT ( 'NONE',  ( 122.7801548109119665, -6.222761293078241884, -8.102969835052219238 ) ) ;
#35570=CARTESIAN_POINT ( 'NONE',  ( 113.3068014775786594, -1.833838273342658809, -17.42832698103878286 ) ) ;
#35571=CARTESIAN_POINT ( 'NONE',  ( 121.2485348109119769, -0.4660016031367893996, -10.09054647747474043 ) ) ;
#35578=CARTESIAN_POINT ( 'NONE',  ( 125.7866681442452688, -0.4660016031367893996, -10.09054647747474043 ) ) ;
#35579=CARTESIAN_POINT ( 'NONE',  ( 113.0798948109119948, -0.4660016031367893996, -10.09054647747474043 ) ) ;
#35582=CARTESIAN_POINT ( 'NONE',  ( 114.2144281442453178, -1.833838273342658809, -17.42832698103878286 ) ) ;
#35590=CARTESIAN_POINT ( 'NONE',  ( 115.0086014775786509, -4.089484607189486809, -7.948022111789456723 ) ) ;
#35593=EDGE_LOOP ( 'NONE', ( #20183, #44739, #10738, #976, #21706 ) ) ;
#35595=CARTESIAN_POINT ( 'NONE',  ( 115.5191414775786569, -6.222761293078241884, -8.102969835052219238 ) ) ;
#35596=CARTESIAN_POINT ( 'NONE',  ( 117.6180281442453150, -0.4660016031367893996, -10.09054647747474043 ) ) ;
#35597=CARTESIAN_POINT ( 'NONE',  ( 125.4463081442452932, -4.153390946401325223, -8.397313243818185668 ) ) ;
#35599=CARTESIAN_POINT ( 'NONE',  ( 119.8303681442453126, 0.4262465694468514643, -12.03445270309931736 ) ) ;
#35600=CARTESIAN_POINT ( 'NONE',  ( 117.2776681442452968, -4.153390946401325223, -8.397313243818185668 ) ) ;
#35601=VERTEX_POINT ( 'NONE', #31822 ) ;
#35603=CIRCLE ( 'NONE', #30516, 2.999999999999998668 ) ;
#35604=CARTESIAN_POINT ( 'NONE',  ( 121.7634181477679789, -2.280480477428469488, -18.08254604495227014 ) ) ;
#35605=CARTESIAN_POINT ( 'NONE',  ( 116.3133148109120043, -2.084020599724406786, -8.691656652584148546 ) ) ;
#35609=CARTESIAN_POINT ( 'NONE',  ( 116.8805814775786445, -6.344957434206662583, -7.627207830600332805 ) ) ;
#35615=CARTESIAN_POINT ( 'NONE',  ( 118.9227414775786542, 0.4262465694468514643, -12.03445270309931736 ) ) ;
#35616=CARTESIAN_POINT ( 'NONE',  ( 119.1496481442453046, -6.222761293078241884, -8.102969835052219238 ) ) ;
#35618=EDGE_CURVE ( 'NONE', #19331, #19315, #4398, .T. ) ;
#35625=CARTESIAN_POINT ( 'NONE',  ( 113.5904348109119866, -7.893985811506177619, -18.51759400769804742 ) ) ;
#35626=CARTESIAN_POINT ( 'NONE',  ( 126.5241148109119393, -9.565557343593413364, -10.61323700422348004 ) ) ;
#35627=CARTESIAN_POINT ( 'NONE',  ( 117.8449348109119938, -1.833838273342659253, -17.42832698103878286 ) ) ;
#35630=CARTESIAN_POINT ( 'NONE',  ( 118.6958348109119754, -3.505236298600246325, -18.68346056562440793 ) ) ;
#35635=CARTESIAN_POINT ( 'NONE',  ( 116.5969481442453031, 0.5811942927096154232, -14.16772938898807155 ) ) ;
#35638=CARTESIAN_POINT ( 'NONE',  ( 117.2209414775786485, -7.893985811506177619, -18.51759400769804742 ) ) ;
#35639=CARTESIAN_POINT ( 'NONE',  ( 114.4413348109119823, -9.261995988541698921, -16.69588392320188674 ) ) ;
#35641=CARTESIAN_POINT ( 'NONE',  ( 116.4834948109119779, -1.561330072975668504, -17.79121239304076951 ) ) ;
#35644=CARTESIAN_POINT ( 'NONE',  ( 115.1787814775786387, -9.988377603198976828, -10.36322818467138340 ) ) ;
#35651=CARTESIAN_POINT ( 'NONE',  ( 117.3911214775786505, -7.894159318335828068, -9.358103419637847864 ) ) ;
#35657=CARTESIAN_POINT ( 'NONE',  ( 115.4624148109119943, -4.153390946401321671, -8.397313243818183892 ) ) ;
#35659=B_SPLINE_CURVE_WITH_KNOTS ( 'NONE', 3,
 ( #15516, #4796, #32386, #42666, #29423, #19386, #33275, #5247, #18718, #19164 ),
 .UNSPECIFIED., .F., .F.,
 ( 4, 3, 3, 4 ),
 ( 0.000000000000000000, 0.0001671877548681254834, 0.0003343755096277640170, 0.0006463528481650629171 ),
 .UNSPECIFIED. ) ;
#35660=CARTESIAN_POINT ( 'NONE',  ( 124.9924948109119924, -4.089484607189486809, -7.948022111789456723 ) ) ;
#35661=CARTESIAN_POINT ( 'NONE',  ( 120.2274548109119934, 0.5811942927096110934, -14.16772938898807510 ) ) ;
#35663=CARTESIAN_POINT ( 'NONE',  ( 119.3765548109119834, -10.15424416112533912, -14.75197769757731336 ) ) ;
#35665=CARTESIAN_POINT ( 'NONE',  ( 118.7525614775786380, -8.166667518702819706, -8.995218007635861213 ) ) ;
#35666=CARTESIAN_POINT ( 'NONE',  ( 118.1285681442453068, -2.084020599724406786, -8.691656652584148546 ) ) ;
#35668=CARTESIAN_POINT ( 'NONE',  ( 120.9649014775786355, -6.222761293078241884, -8.102969835052219238 ) ) ;
#35669=CARTESIAN_POINT ( 'NONE',  ( 121.5321681442453183, -9.988377603198976828, -10.36322818467138340 ) ) ;
#35675=CARTESIAN_POINT ( 'NONE',  ( 118.0151148109119816, -10.63000616557722466, -14.87417383870573495 ) ) ;
#35676=AXIS2_PLACEMENT_3D ( 'NONE', #38997, #28297, #920 ) ;
#35678=CARTESIAN_POINT ( 'NONE',  ( 115.6893214775786447, -9.859900752359374465, -12.68260735090039404 ) ) ;
#35683=CARTESIAN_POINT ( 'NONE',  ( 122.0666209388149355, -2.287189184988711155, -18.07361239780447448 ) ) ;
#35687=CARTESIAN_POINT ( 'NONE',  ( 120.6245414775786458, -9.988377603198976828, -10.36322818467138340 ) ) ;
#35688=CARTESIAN_POINT ( 'NONE',  ( 118.9227414775786542, 0.4262465694468514643, -12.03445270309931736 ) ) ;
#35689=CARTESIAN_POINT ( 'NONE',  ( 111.7751814775786556, -2.084020599724406786, -8.691656652584148546 ) ) ;
#35692=CARTESIAN_POINT ( 'NONE',  ( 122.5532481442453019, -10.63000616557722466, -14.87417383870573495 ) ) ;
#35694=CARTESIAN_POINT ( 'NONE',  ( 119.0929214775786278, -4.153390946401325223, -8.397313243818185668 ) ) ;
#35695=CARTESIAN_POINT ( 'NONE',  ( 115.4624148109119943, -4.153390946401321671, -8.397313243818183892 ) ) ;
#35698=CARTESIAN_POINT ( 'NONE',  ( 120.0005481442453146, -4.153390946401325223, -8.397313243818185668 ) ) ;
#35699=CARTESIAN_POINT ( 'NONE',  ( 123.4608748109119745, 0.4262465694468514643, -12.03445270309931736 ) ) ;
#35706=CARTESIAN_POINT ( 'NONE',  ( 116.3133148109119759, -7.893985811506177619, -18.51759400769804742 ) ) ;
#35707=CARTESIAN_POINT ( 'NONE',  ( 117.1642148109119859, -9.261995988541697145, -16.69588392320189030 ) ) ;
#35710=CARTESIAN_POINT ( 'NONE',  ( 113.1366214775786432, -1.834011780172310813, -8.268836392978581529 ) ) ;
#35712=CARTESIAN_POINT ( 'NONE',  ( 117.2537553496756715, -1.087735405160632718, -17.17288456429612253 ) ) ;
#35714=CARTESIAN_POINT ( 'NONE',  ( 114.7816948109119863, 0.5811942927096154232, -14.16772938898807155 ) ) ;
#35715=CARTESIAN_POINT ( 'NONE',  ( 122.7234281442452755, -4.153390946401325223, -8.397313243818185668 ) ) ;
#35717=B_SPLINE_CURVE_WITH_KNOTS ( 'NONE', 3,
 ( #39105, #8103, #42538, #14490, #28185, #25657, #42314, #14268, #42092, #10855, #7875, #11073, #24750, #21783, #18586, #581, #28404, #11299, #38638, #24977, #15163, #1252, #7193, #7642, #18368, #18135, #7411, #21331, #29068, #42979 ),
 .UNSPECIFIED., .F., .F.,
 ( 4, 2, 2, 1, 1, 1, 2, 2, 2, 1, 1, 1, 2, 2, 1, 1, 2, 2, 4 ),
 ( 0.000000000000000000, 0.2499999999999678590, 0.3749999999999364952, 0.4374999999999213407, 0.4687499999999293343, 0.4843749999999326650, 0.4921874999999179545, 0.4999999999999032441, 0.6249999999998178124, 0.6874999999997751798, 0.7187499999997664091, 0.7343749999997620792, 0.7421874999997711830, 0.7499999999997802869, 0.8124999999998421263, 0.8437499999998633315, 0.8593749999998809841, 0.8749999999998986366, 1.000000000000000000 ),
 .UNSPECIFIED. ) ;
#35719=CARTESIAN_POINT ( 'NONE',  ( 111.9453614775786434, -7.894159318335828068, -9.358103419637847864 ) ) ;
#35720=CARTESIAN_POINT ( 'NONE',  ( 123.6310548109119765, -5.638512984488999180, -18.83840828888717311 ) ) ;
#35722=CARTESIAN_POINT ( 'NONE',  ( 117.9016614775786280, -0.1624402480850797581, -16.17319339645315424 ) ) ;
#35727=CARTESIAN_POINT ( 'NONE',  ( 119.4900081442453086, -1.834011780172310813, -8.268836392978581529 ) ) ;
#35733=CARTESIAN_POINT ( 'NONE',  ( 114.7249681442453237, -9.565557343593413364, -10.61323700422348004 ) ) ;
#35734=CARTESIAN_POINT ( 'NONE',  ( 126.8848614667774939, -1.093441926320177338, -17.16528547817962291 ) ) ;
#35735=CARTESIAN_POINT ( 'NONE',  ( 123.7644531642484225, -2.215723800389698184, -18.16877924232191788 ) ) ;
#35737=CARTESIAN_POINT ( 'NONE',  ( 120.3976348109119812, -7.643976991954077427, -18.09477374809248928 ) ) ;
#35739=CARTESIAN_POINT ( 'NONE',  ( 122.6099748109119929, -0.8288870151387760510, -10.36305467784173118 ) ) ;
#35742=CARTESIAN_POINT ( 'NONE',  ( 124.1415948109119540, -3.505236298600246325, -18.68346056562440793 ) ) ;
#35744=CARTESIAN_POINT ( 'NONE',  ( 112.2857214775786474, -4.089484607189486809, -7.948022111789456723 ) ) ;
#35745=CARTESIAN_POINT ( 'NONE',  ( 118.2420214775786320, -3.383040157471821630, -19.15922257007629170 ) ) ;
#35746=CARTESIAN_POINT ( 'NONE',  ( 112.5126281442453120, -10.30919188438810075, -12.61870101168855918 ) ) ;
#35748=CARTESIAN_POINT ( 'NONE',  ( 119.4332814775786318, -8.899110576539710493, -16.42337572283490132 ) ) ;
#35750=CARTESIAN_POINT ( 'NONE',  ( 120.7379948109119709, -10.63000616557722466, -14.87417383870573495 ) ) ;
#35755=CARTESIAN_POINT ( 'NONE',  ( 118.7735460444391862, -1.267766418764730840, -16.93314635290706605 ) ) ;
#35756=CARTESIAN_POINT ( 'NONE',  ( 124.4819548109119722, -7.893985811506177619, -18.51759400769804742 ) ) ;
#35757=ORIENTED_EDGE ( 'NONE', *, *, #12253, .T. ) ;
#35759=CARTESIAN_POINT ( 'NONE',  ( 120.8514481442452961, -2.084020599724406786, -8.691656652584148546 ) ) ;
#35764=ORIENTED_EDGE ( 'NONE', *, *, #31449, .T. ) ;
#35765=CARTESIAN_POINT ( 'NONE',  ( 115.5758681442453053, -1.561330072975668060, -17.79121239304076951 ) ) ;
#35768=CARTESIAN_POINT ( 'NONE',  ( 122.3830681442452857, -1.833838273342659697, -17.42832698103878286 ) ) ;
#35769=CARTESIAN_POINT ( 'NONE',  ( 126.2940345447970998, -3.831033905170792675, -8.462449267509514428 ) ) ;
#35770=CARTESIAN_POINT ( 'NONE',  ( 121.9292548109119849, -1.561330072975668948, -17.79121239304076951 ) ) ;
#35774=ORIENTED_EDGE ( 'NONE', *, *, #10847, .F. ) ;
#35776=VECTOR ( 'NONE', #13017, 1000.000000000000000 ) ;
#35778=CARTESIAN_POINT ( 'NONE',  ( 119.7736414775786358, -10.30919188438810075, -12.61870101168855918 ) ) ;
#35779=CARTESIAN_POINT ( 'NONE',  ( 137.4443952029541549, -8.589549469794567571, -16.85306431102494074 ) ) ;
#35781=CARTESIAN_POINT ( 'NONE',  ( 112.2289948109119848, -1.834011780172310813, -8.268836392978581529 ) ) ;
#35782=CARTESIAN_POINT ( 'NONE',  ( 111.3213681442453264, -7.643976991954077427, -18.09477374809248928 ) ) ;
#35783=CARTESIAN_POINT ( 'NONE',  ( 127.2313854076960808, -4.459849209109382429, -18.88486369543121413 ) ) ;
#35784=CARTESIAN_POINT ( 'NONE',  ( 123.7445081442452874, -7.894159318335828068, -9.358103419637847864 ) ) ;
#35786=CARTESIAN_POINT ( 'NONE',  ( 117.1642148109119859, -9.261995988541697145, -16.69588392320189030 ) ) ;
#35790=CARTESIAN_POINT ( 'NONE',  ( 111.8319081442453182, -4.153390946401321671, -8.397313243818183892 ) ) ;
#35793=CARTESIAN_POINT ( 'NONE',  ( 121.8725281442453223, -3.383040157471821630, -19.15922257007629170 ) ) ;
#35794=CARTESIAN_POINT ( 'NONE',  ( 123.9714148109119805, -8.899110576539710493, -16.42337572283490132 ) ) ;
#35796=CARTESIAN_POINT ( 'NONE',  ( 122.4965214775786251, 0.1319031606808879209, -14.10382304977623669 ) ) ;
#35797=CARTESIAN_POINT ( 'NONE',  ( 112.2857214775786474, -5.574606645277164318, -18.38911715685844683 ) ) ;
#35798=CARTESIAN_POINT ( 'NONE',  ( 118.1285681442453068, -7.893985811506177619, -18.51759400769804742 ) ) ;
#35801=CARTESIAN_POINT ( 'NONE',  ( 126.3115243456364709, -8.670208513534547023, -16.70688709793458671 ) ) ;
#35805=CARTESIAN_POINT ( 'NONE',  ( 125.1059481442453034, -1.833838273341870773, -17.42832698103818956 ) ) ;
#35806=CARTESIAN_POINT ( 'NONE',  ( 113.4202548109119846, -10.30919188438810075, -12.61870101168855918 ) ) ;
#35808=CARTESIAN_POINT ( 'NONE',  ( 111.8886348109120092, -6.222761293078241884, -8.102969835052219238 ) ) ;
#35811=CARTESIAN_POINT ( 'NONE',  ( 112.3424481442453384, -3.505236298600246325, -18.68346056562440793 ) ) ;
#35812=CARTESIAN_POINT ( 'NONE',  ( 122.7234281442452755, -4.153390946401307460, -8.397313243818183892 ) ) ;
#35814=CARTESIAN_POINT ( 'NONE',  ( 115.1787814775786387, -9.988377603198976828, -10.36322818467138340 ) ) ;
#35818=CARTESIAN_POINT ( 'NONE',  ( 126.6390922358795734, -7.341185092770153631, -8.808989803355210313 ) ) ;
#35819=CARTESIAN_POINT ( 'NONE',  ( 117.2209414775786485, -2.084020599724406786, -8.691656652584148546 ) ) ;
#35820=CARTESIAN_POINT ( 'NONE',  ( 115.8027748109119841, -0.4660016031367893996, -10.09054647747474043 ) ) ;
#35822=CARTESIAN_POINT ( 'NONE',  ( 123.7445081442452874, -7.894159318335828068, -9.358103419637847864 ) ) ;
#35823=CARTESIAN_POINT ( 'NONE',  ( 120.7379948109119709, 0.4262465694468514643, -12.03445270309931736 ) ) ;
#35824=CARTESIAN_POINT ( 'NONE',  ( 114.5547881442453217, -4.153390946401321671, -8.397313243818183892 ) ) ;
#35829=CARTESIAN_POINT ( 'NONE',  ( 116.4834948109119779, -7.894159318335828068, -9.358103419637847864 ) ) ;
#35831=CARTESIAN_POINT ( 'NONE',  ( 128.2184548109119930, -10.44474571748257041, -15.59668151425567650 ) ) ;
#35832=CARTESIAN_POINT ( 'NONE',  ( 115.3489614775786407, -9.261995988541697145, -16.69588392320189030 ) ) ;
#35834=CARTESIAN_POINT ( 'NONE',  ( 113.4769814775786330, 0.4262465694468514643, -12.03445270309931736 ) ) ;
#35838=CARTESIAN_POINT ( 'NONE',  ( 123.2906948109119867, -1.833838273342659697, -17.42832698103878286 ) ) ;
#35839=CARTESIAN_POINT ( 'NONE',  ( 117.3343948109119737, -6.222761293078241884, -8.102969835052219238 ) ) ;
#35844=CARTESIAN_POINT ( 'NONE',  ( 112.1344032980735363, -8.920344330785875187, -16.33470576110396522 ) ) ;
#35846=CARTESIAN_POINT ( 'NONE',  ( 112.9097148109120070, 0.2603800115204892296, -16.42320221600525088 ) ) ;
#35847=CARTESIAN_POINT ( 'NONE',  ( 112.3424481442453384, -6.344957434206662583, -7.627207830600332805 ) ) ;
#35848=CARTESIAN_POINT ( 'NONE',  ( 121.5888948109119809, 0.1319031606808879209, -14.10382304977623669 ) ) ;
#35851=CARTESIAN_POINT ( 'NONE',  ( 121.5321681442453183, -0.1624402480850797581, -16.17319339645315424 ) ) ;
#35856=CARTESIAN_POINT ( 'NONE',  ( 117.1642148109119859, -9.261995988541697145, -16.69588392320189030 ) ) ;
#35858=CARTESIAN_POINT ( 'NONE',  ( 116.5969481442453031, 0.5811942927096154232, -14.16772938898807155 ) ) ;
#35859=CARTESIAN_POINT ( 'NONE',  ( 115.1796143740715763, -2.419733177069680607, -17.89711025544712442 ) ) ;
#35861=CARTESIAN_POINT ( 'NONE',  ( 115.2922348109119781, -10.63000616557722466, -14.87417383870573495 ) ) ;
#35862=CARTESIAN_POINT ( 'NONE',  ( 117.3911214775786505, -1.561330072975668504, -17.79121239304076951 ) ) ;
#35864=CARTESIAN_POINT ( 'NONE',  ( 126.5254139958964572, -10.01703884201283223, -13.32492638032154098 ) ) ;
#35868=ORIENTED_EDGE ( 'NONE', *, *, #22583, .F. ) ;
#35870=DIRECTION ( 'NONE',  ( -0.2425356250363335242, -0.5825562349001200957, 0.7757607258473654399 ) ) ;
#35872=CARTESIAN_POINT ( 'NONE',  ( 120.3976348109119812, -7.643976991954077427, -18.09477374809248928 ) ) ;
#35876=CARTESIAN_POINT ( 'NONE',  ( 112.7395348109119766, -4.153390946401321671, -8.397313243818183892 ) ) ;
#35879=CARTESIAN_POINT ( 'NONE',  ( 123.4608748109119745, -10.63000616557722466, -14.87417383870573495 ) ) ;
#35880=CARTESIAN_POINT ( 'NONE',  ( 118.6958348109119754, -6.344957434206665248, -7.627207830600338134 ) ) ;
#35883=CARTESIAN_POINT ( 'NONE',  ( 117.5045748109119756, -9.859900752359374465, -12.68260735090039404 ) ) ;
#35885=CARTESIAN_POINT ( 'NONE',  ( 119.7736414775786358, -10.30919188438810075, -12.61870101168855918 ) ) ;
#35886=CARTESIAN_POINT ( 'NONE',  ( 120.7947214775786193, -0.8288870151387760510, -10.36305467784173118 ) ) ;
#35888=CARTESIAN_POINT ( 'NONE',  ( 116.3069962859068909, -1.111561923218680858, -17.14115599315434935 ) ) ;
#35892=CARTESIAN_POINT ( 'NONE',  ( 119.0929214775786278, -5.638512984488999180, -18.83840828888717311 ) ) ;
#35896=EDGE_CURVE ( 'NONE', #43873, #31663, #17801, .T. ) ;
#35899=CARTESIAN_POINT ( 'NONE',  ( 138.2184548109119930, -5.849744126848086090, -20.32346094940048786 ) ) ;
#35902=CARTESIAN_POINT ( 'NONE',  ( 117.5045748109119756, 0.5811942927096110934, -14.16772938898807510 ) ) ;
#35903=CARTESIAN_POINT ( 'NONE',  ( 136.3568202015727024, -10.22787683451856999, -11.16363433356868562 ) ) ;
#35904=CARTESIAN_POINT ( 'NONE',  ( 116.1998614775786507, 0.4262465694468514643, -12.03445270309931736 ) ) ;
#35905=CARTESIAN_POINT ( 'NONE',  ( 124.5954081442453116, -3.383040157471821630, -19.15922257007629170 ) ) ;
#35909=CARTESIAN_POINT ( 'NONE',  ( 114.2144281442453178, -1.833838273342658809, -17.42832698103878286 ) ) ;
#35913=CARTESIAN_POINT ( 'NONE',  ( 119.3198281442452924, 0.5811942927096110934, -14.16772938898807510 ) ) ;
#35914=CARTESIAN_POINT ( 'NONE',  ( 120.1140014775786398, -7.894159318335828068, -9.358103419637847864 ) ) ;
#35915=CARTESIAN_POINT ( 'NONE',  ( 113.9875214775786532, -8.899110576539710493, -16.42337572283490132 ) ) ;
#35916=ORIENTED_EDGE ( 'NONE', *, *, #11278, .T. ) ;
#35918=CARTESIAN_POINT ( 'NONE',  ( 122.8368814775786291, -1.561330072975668948, -17.79121239304076951 ) ) ;
#35920=CARTESIAN_POINT ( 'NONE',  ( 120.0572748109119772, -6.222761293078241884, -8.102969835052219238 ) ) ;
#35921=CARTESIAN_POINT ( 'NONE',  ( 123.0070614775786169, -10.15424416112533912, -14.75197769757731336 ) ) ;
#35923=CARTESIAN_POINT ( 'NONE',  ( 116.0296814775786345, -1.833838273342658809, -17.42832698103878286 ) ) ;
#35926=CARTESIAN_POINT ( 'NONE',  ( 124.4819548109119722, -2.084020599724406786, -8.691656652584148546 ) ) ;
#35928=CARTESIAN_POINT ( 'NONE',  ( 124.0281414775786146, -7.643976991954077427, -18.09477374809248928 ) ) ;
#35934=CARTESIAN_POINT ( 'NONE',  ( 116.6536748109119941, 0.9020085738987339008, -11.91225656197089222 ) ) ;
#35935=CARTESIAN_POINT ( 'NONE',  ( 120.2274548109119934, 0.5811942927096110934, -14.16772938898807510 ) ) ;
#35937=CARTESIAN_POINT ( 'NONE',  ( 113.4769814775786330, -10.63000616557722466, -14.87417383870573495 ) ) ;
#35942=CARTESIAN_POINT ( 'NONE',  ( 117.9583881442453048, -10.30919188438810075, -12.61870101168855918 ) ) ;
#35943=CARTESIAN_POINT ( 'NONE',  ( 121.7590748109119687, -2.084020599724406786, -8.691656652584148546 ) ) ;
#35945=CARTESIAN_POINT ( 'NONE',  ( 113.4769814775786330, 0.4262465694468514643, -12.03445270309931736 ) ) ;
#35946=CARTESIAN_POINT ( 'NONE',  ( 122.2128881442453263, -1.834011780172310813, -8.268836392978581529 ) ) ;
#35948=CARTESIAN_POINT ( 'NONE',  ( 116.5969481442453031, -9.859900752359374465, -12.68260735090039404 ) ) ;
#35954=CARTESIAN_POINT ( 'NONE',  ( 118.2987481442453088, -1.561330072975668504, -17.79121239304076951 ) ) ;
#35957=CARTESIAN_POINT ( 'NONE',  ( 111.3780948109119890, -5.574606645277172312, -18.38911715685844683 ) ) ;
#35959=CARTESIAN_POINT ( 'NONE',  ( 115.1787814775786387, -0.1624402480850797581, -16.17319339645315424 ) ) ;
#35963=CARTESIAN_POINT ( 'NONE',  ( 122.2128881442453263, -7.643976991954077427, -18.09477374809248928 ) ) ;
#35965=CARTESIAN_POINT ( 'NONE',  ( 123.8012348109119642, -9.565557343593413364, -10.61323700422348004 ) ) ;
#35967=CARTESIAN_POINT ( 'NONE',  ( 121.6456214775786293, 0.4262465694468514643, -12.03445270309931736 ) ) ;
#35968=CARTESIAN_POINT ( 'NONE',  ( 114.2711548109119803, -9.988377603198976828, -10.36322818467138340 ) ) ;
#35969=CARTESIAN_POINT ( 'NONE',  ( 121.1350814775786233, 0.5811942927096110934, -14.16772938898807510 ) ) ;
#35970=CARTESIAN_POINT ( 'NONE',  ( 113.8740681442453138, 0.5811942927096154232, -14.16772938898807155 ) ) ;
#35971=CARTESIAN_POINT ( 'NONE',  ( 135.3184548109119874, -2.475900776146298110, -7.888945235271312306 ) ) ;
#35972=CARTESIAN_POINT ( 'NONE',  ( 122.2128881442453263, -7.643976991954077427, -18.09477374809248928 ) ) ;
#35974=CARTESIAN_POINT ( 'NONE',  ( 120.6812681442452941, -10.30919188438810075, -12.61870101168855918 ) ) ;
#35977=CARTESIAN_POINT ( 'NONE',  ( 113.5337081442453240, -0.8288870151387760510, -10.36305467784173118 ) ) ;
#35981=CARTESIAN_POINT ( 'NONE',  ( 121.0216281442452981, -7.894159318335828068, -9.358103419637847864 ) ) ;
#35985=CIRCLE ( 'NONE', #28007, 5.999999999999997335 ) ;
#35988=CARTESIAN_POINT ( 'NONE',  ( 115.9162281442453235, -4.089484607189486809, -7.948022111789456723 ) ) ;
#35990=CARTESIAN_POINT ( 'NONE',  ( 122.4397948109119767, -0.1624402480850797581, -16.17319339645315424 ) ) ;
#35991=CARTESIAN_POINT ( 'NONE',  ( 112.9097148109120070, -9.565557343593413364, -10.61323700422348004 ) ) ;
#35993=CARTESIAN_POINT ( 'NONE',  ( 111.3780948109119890, -5.574606645277164318, -18.38911715685844683 ) ) ;
#35996=CARTESIAN_POINT ( 'NONE',  ( 111.7751814775786556, -7.893985811506177619, -18.51759400769804742 ) ) ;
#35997=ORIENTED_EDGE ( 'NONE', *, *, #44845, .F. ) ;
#35998=EDGE_CURVE ( 'NONE', #29655, #10303, #4493, .T. ) ;
#36000=CARTESIAN_POINT ( 'NONE',  ( 119.7169148109119874, -9.988377603198976828, -10.36322818467138340 ) ) ;
#36001=CARTESIAN_POINT ( 'NONE',  ( 137.2618751061035880, -9.521150726106348827, -15.82766067591523651 ) ) ;
#36004=CARTESIAN_POINT ( 'NONE',  ( 136.5935259641839252, 0.3896279301912132786, -11.16094382891788861 ) ) ;
#36005=CARTESIAN_POINT ( 'NONE',  ( 125.3895814775786448, -7.893985811506177619, -18.51759400769804742 ) ) ;
#36007=CARTESIAN_POINT ( 'NONE',  ( 124.1415948109119540, -3.505236298600246325, -18.68346056562440793 ) ) ;
#36008=B_SPLINE_CURVE_WITH_KNOTS ( 'NONE', 3,
 ( #18535, #32647, #11247, #974 ),
 .UNSPECIFIED., .F., .F.,
 ( 4, 4 ),
 ( 0.005429436266171680341, 0.006853839515878830564 ),
 .UNSPECIFIED. ) ;
#36011=CARTESIAN_POINT ( 'NONE',  ( 119.7736414775786358, -10.30919188438810075, -12.61870101168855918 ) ) ;
#36014=CARTESIAN_POINT ( 'NONE',  ( 116.6599933359170507, -2.311015703046737535, -18.04188382666267998 ) ) ;
#36016=CARTESIAN_POINT ( 'NONE',  ( 137.4478226697684136, -3.708367563260872579, -8.456766944596608937 ) ) ;
#36018=CARTESIAN_POINT ( 'NONE',  ( 112.3424481442453384, -3.505236298600246325, -18.68346056562440793 ) ) ;
#36021=CARTESIAN_POINT ( 'NONE',  ( 111.5482748109120053, -0.1624402480850797581, -16.17319339645315424 ) ) ;
#36022=CARTESIAN_POINT ( 'NONE',  ( 125.9568481442452850, -3.505236298600246325, -18.68346056562440793 ) ) ;
#36024=CARTESIAN_POINT ( 'NONE',  ( 122.5532481442453019, 0.4262465694468514643, -12.03445270309931736 ) ) ;
#36025=CARTESIAN_POINT ( 'NONE',  ( 113.4769814775786330, 0.4262465694468514643, -12.03445270309931736 ) ) ;
#36026=CARTESIAN_POINT ( 'NONE',  ( 120.0005481442453146, -5.638512984488999180, -18.83840828888717311 ) ) ;
#36028=CARTESIAN_POINT ( 'NONE',  ( 126.2455040230441341, -8.733555821824001697, -16.58294173486839540 ) ) ;
#36032=CARTESIAN_POINT ( 'NONE',  ( 125.2761281442453338, 0.4262465694465857324, -12.03445270309828175 ) ) ;
#36033=CARTESIAN_POINT ( 'NONE',  ( 115.9729548109119861, -6.344957434206662583, -7.627207830600332805 ) ) ;
#36035=CARTESIAN_POINT ( 'NONE',  ( 115.2355081442453155, 0.1319031606808879209, -14.10382304977623669 ) ) ;
#36038=CARTESIAN_POINT ( 'NONE',  ( 126.2404814775786264, -9.261995988541697145, -16.69588392320189030 ) ) ;
#36041=CARTESIAN_POINT ( 'NONE',  ( 115.4056881442453459, -7.893985811506177619, -18.51759400769804742 ) ) ;
#36046=CARTESIAN_POINT ( 'NONE',  ( 128.2184548109119930, -7.067465109756605912, -7.812468278694988832 ) ) ;
#36047=CARTESIAN_POINT ( 'NONE',  ( 119.4900081442453086, -7.643976991954077427, -18.09477374809248928 ) ) ;
#36048=CARTESIAN_POINT ( 'NONE',  ( 114.6682414775786469, -1.561330072975668060, -17.79121239304076596 ) ) ;
#36049=CARTESIAN_POINT ( 'NONE',  ( 113.4202548109119846, -10.30919188438810075, -12.61870101168855918 ) ) ;
#36050=CARTESIAN_POINT ( 'NONE',  ( 125.6732148109119862, -9.859900752359378018, -12.68260735090039759 ) ) ;
#36052=CARTESIAN_POINT ( 'NONE',  ( 123.5176014775786228, -0.8288870151387760510, -10.36305467784173118 ) ) ;
#36053=CARTESIAN_POINT ( 'NONE',  ( 114.7249681442453237, -9.565557343593413364, -10.61323700422348004 ) ) ;
#36057=CARTESIAN_POINT ( 'NONE',  ( 117.1074881442453233, 0.4262465694468514643, -12.03445270309931736 ) ) ;
#36060=CARTESIAN_POINT ( 'NONE',  ( 116.0296814775786345, -8.166667518702817929, -8.995218007635861213 ) ) ;
#36062=CARTESIAN_POINT ( 'NONE',  ( 112.9097148109120070, -9.565557343593413364, -10.61323700422348004 ) ) ;
#36065=CARTESIAN_POINT ( 'NONE',  ( 121.3619881442452879, -5.574606645277164318, -18.38911715685844683 ) ) ;
#36066=EDGE_CURVE ( 'NONE', #3495, #32667, #36008, .T. ) ;
#36067=CARTESIAN_POINT ( 'NONE',  ( 118.9227414775786542, 0.4262465694468514643, -12.03445270309931736 ) ) ;
#36069=CARTESIAN_POINT ( 'NONE',  ( 116.7104014775786425, -8.899110576539721151, -16.42337572283488711 ) ) ;
#36071=CARTESIAN_POINT ( 'NONE',  ( 128.2184548109119930, -4.863998795839242995, -13.39321520033831447 ) ) ;
#36075=CARTESIAN_POINT ( 'NONE',  ( 114.8951481442453115, -0.4660016031367893996, -10.09054647747474043 ) ) ;
#36076=CARTESIAN_POINT ( 'NONE',  ( 112.5126281442453120, -10.30919188438810075, -12.61870101168855918 ) ) ;
#36077=CARTESIAN_POINT ( 'NONE',  ( 114.4413348109119823, -0.8288870151387760510, -10.36305467784173118 ) ) ;
#36078=CARTESIAN_POINT ( 'NONE',  ( 121.9292548109119849, -7.894159318335828068, -9.358103419637847864 ) ) ;
#36082=CARTESIAN_POINT ( 'NONE',  ( 120.7379948109119709, 0.4262465694468514643, -12.03445270309931736 ) ) ;
#36083=CARTESIAN_POINT ( 'NONE',  ( 124.3117748109119844, 0.1319031606808879209, -14.10382304977623669 ) ) ;
#36085=CARTESIAN_POINT ( 'NONE',  ( 117.8239502440515452, -2.467220198592778413, -17.83387418641524391 ) ) ;
#36087=CARTESIAN_POINT ( 'NONE',  ( 117.7314814775786260, -4.089484607189486809, -7.948022111789456723 ) ) ;
#36089=CARTESIAN_POINT ( 'NONE',  ( 117.8449348109119938, -8.166667518702817929, -8.995218007635861213 ) ) ;
#36090=CARTESIAN_POINT ( 'NONE',  ( 115.2974471540078554, -2.348512537728063787, -17.99195118506216318 ) ) ;
#36092=CARTESIAN_POINT ( 'NONE',  ( 116.1431348109119881, -10.30919188438810075, -12.61870101168855918 ) ) ;
#36093=CARTESIAN_POINT ( 'NONE',  ( 117.7882081442453170, -6.344957434206665248, -7.627207830600338134 ) ) ;
#36094=CARTESIAN_POINT ( 'NONE',  ( 126.9115046738313879, -10.20580091807491030, -13.62532772550883919 ) ) ;
#36098=CARTESIAN_POINT ( 'NONE',  ( 112.4201593777725208, -1.267766418764741276, -16.93314635290707315 ) ) ;
#36100=CARTESIAN_POINT ( 'NONE',  ( 119.7736414775786358, 0.1319031606808879209, -14.10382304977623669 ) ) ;
#36104=CARTESIAN_POINT ( 'NONE',  ( 114.7816948109119863, -9.859900752359374465, -12.68260735090039404 ) ) ;
#36106=CARTESIAN_POINT ( 'NONE',  ( 112.2289948109119848, -7.643976991954077427, -18.09477374809248928 ) ) ;
#36107=CARTESIAN_POINT ( 'NONE',  ( 118.8660148109119774, -10.30919188438810075, -12.61870101168855918 ) ) ;
#36110=CARTESIAN_POINT ( 'NONE',  ( 118.1285681442453068, -2.084020599724406786, -8.691656652584148546 ) ) ;
#36111=CARTESIAN_POINT ( 'NONE',  ( 114.8951481442453115, -0.4660016031367893996, -10.09054647747474043 ) ) ;
#36112=CARTESIAN_POINT ( 'NONE',  ( 121.7023481442452777, -9.261995988541697145, -16.69588392320189030 ) ) ;
#36113=CARTESIAN_POINT ( 'NONE',  ( 120.2274548109119934, -9.859900752359378018, -12.68260735090039759 ) ) ;
#36115=CARTESIAN_POINT ( 'NONE',  ( 124.7088614775786226, -9.565557343593413364, -10.61323700422348004 ) ) ;
#36117=CARTESIAN_POINT ( 'NONE',  ( 122.0427081442452817, 0.5811942927096110934, -14.16772938898807510 ) ) ;
#36120=CARTESIAN_POINT ( 'NONE',  ( 138.1238347578285754, -2.002283765726665887, -15.95502668635790222 ) ) ;
#36125=CARTESIAN_POINT ( 'NONE',  ( 115.5758681442453053, -7.894159318335828068, -9.358103419637847864 ) ) ;
#36126=CARTESIAN_POINT ( 'NONE',  ( 124.4819548109119722, -7.893985811506177619, -18.51759400769804742 ) ) ;
#36130=CARTESIAN_POINT ( 'NONE',  ( 116.7671281442453335, -7.643976991954077427, -18.09477374809248928 ) ) ;
#36131=CARTESIAN_POINT ( 'NONE',  ( 113.4429142554890859, -2.372251574601226043, -17.96033910819752322 ) ) ;
#36136=CARTESIAN_POINT ( 'NONE',  ( 118.4689281442453392, 0.9020085738987339008, -11.91225656197089222 ) ) ;
#36137=CARTESIAN_POINT ( 'NONE',  ( 122.3830681442452857, -1.833838273342659697, -17.42832698103878286 ) ) ;
#36139=CARTESIAN_POINT ( 'NONE',  ( 137.0105207745575342, -8.969470875690532807, -9.795839679219671581 ) ) ;
#36140=CARTESIAN_POINT ( 'NONE',  ( 125.6164881442453094, 0.2603800115204892296, -16.42320221600525088 ) ) ;
#36142=CARTESIAN_POINT ( 'NONE',  ( 120.9081748109119872, -4.153390946401325223, -8.397313243818185668 ) ) ;
#36143=CARTESIAN_POINT ( 'NONE',  ( 120.3409081442453044, -8.899110576539710493, -16.42337572283490132 ) ) ;
#36145=CARTESIAN_POINT ( 'NONE',  ( 117.1642148109119859, -0.8288870151387760510, -10.36305467784173118 ) ) ;
#36148=CARTESIAN_POINT ( 'NONE',  ( 122.8368814775786291, -7.894159318335828068, -9.358103419637847864 ) ) ;
#36149=CARTESIAN_POINT ( 'NONE',  ( 125.2194014775786286, 0.1319031606808879209, -14.10382304977623669 ) ) ;
#36156=CARTESIAN_POINT ( 'NONE',  ( 122.6099748109119929, -9.261995988541697145, -16.69588392320189030 ) ) ;
#36157=CARTESIAN_POINT ( 'NONE',  ( 118.4122014775786340, 0.5811942927096110934, -14.16772938898807510 ) ) ;
#36159=CARTESIAN_POINT ( 'NONE',  ( 113.2500748109119968, -6.344957434206662583, -7.627207830600332805 ) ) ;
#36165=CARTESIAN_POINT ( 'NONE',  ( 118.3554748109119998, 0.2603800115204892296, -16.42320221600525088 ) ) ;
#36166=CARTESIAN_POINT ( 'NONE',  ( 126.0135748109119902, -1.833838273342660141, -17.42832698103878286 ) ) ;
#36169=CARTESIAN_POINT ( 'NONE',  ( 115.4624148109119943, -4.153390946401321671, -8.397313243818183892 ) ) ;
#36170=CARTESIAN_POINT ( 'NONE',  ( 125.4463081442452932, -5.638512984488999180, -18.83840828888717311 ) ) ;
#36173=CARTESIAN_POINT ( 'NONE',  ( 120.7379948109119709, 0.4262465694468514643, -12.03445270309931736 ) ) ;
#36179=CARTESIAN_POINT ( 'NONE',  ( 118.6391081442452986, -4.089484607189486809, -7.948022111789456723 ) ) ;
#36185=CARTESIAN_POINT ( 'NONE',  ( 118.3554748109119998, -9.565557343593413364, -10.61323700422348004 ) ) ;
#36188=CARTESIAN_POINT ( 'NONE',  ( 124.6521348109119884, -7.894159318335828068, -9.358103419637847864 ) ) ;
#36195=CARTESIAN_POINT ( 'NONE',  ( 116.3700414775786527, -4.153390946401321671, -8.397313243818183892 ) ) ;
#36196=CARTESIAN_POINT ( 'NONE',  ( 124.6521348109119884, -7.894159318335828068, -9.358103419637847864 ) ) ;
#36197=CARTESIAN_POINT ( 'NONE',  ( 112.5693548109119888, -10.63000616557722466, -14.87417383870573495 ) ) ;
#36198=CARTESIAN_POINT ( 'NONE',  ( 119.9438214775786378, -7.893985811506177619, -18.51759400769804742 ) ) ;
#36199=CARTESIAN_POINT ( 'NONE',  ( 117.1074881442453233, -10.63000616557722466, -14.87417383870573495 ) ) ;
#36201=CARTESIAN_POINT ( 'NONE',  ( 123.0070614775786169, -10.15424416112533912, -14.75197769757731336 ) ) ;
#36203=CARTESIAN_POINT ( 'NONE',  ( 121.0216281442452981, -1.561330072975668948, -17.79121239304076951 ) ) ;
#36209=CARTESIAN_POINT ( 'NONE',  ( 124.4252281442452812, -9.261995988541697145, -16.69588392320189030 ) ) ;
#36210=ORIENTED_EDGE ( 'NONE', *, *, #34328, .T. ) ;
#36211=CARTESIAN_POINT ( 'NONE',  ( 122.4965214775786251, 0.1319031606808879209, -14.10382304977623669 ) ) ;
#36216=CARTESIAN_POINT ( 'NONE',  ( 111.8991748109119868, -7.866424907533402511, -9.395035934245173692 ) ) ;
#36219=CARTESIAN_POINT ( 'NONE',  ( 114.8951481442453115, -0.4660016031367893996, -10.09054647747474043 ) ) ;
#36221=CARTESIAN_POINT ( 'NONE',  ( 121.0783548109119749, -9.565557343593413364, -10.61323700422348004 ) ) ;
#36222=CARTESIAN_POINT ( 'NONE',  ( 113.4202548109119846, 0.1319031606808879209, -14.10382304977623669 ) ) ;
#36228=CIRCLE ( 'NONE', #7829, 4.999999999999998224 ) ;
#36229=CARTESIAN_POINT ( 'NONE',  ( 120.0572748109119772, -3.383040157471821630, -19.15922257007629170 ) ) ;
#36230=CARTESIAN_POINT ( 'NONE',  ( 137.2352176311256073, -8.497078852651583247, -17.21982894588502333 ) ) ;
#36232=CARTESIAN_POINT ( 'NONE',  ( 113.8173414775786512, 0.2603800115204892296, -16.42320221600525088 ) ) ;
#36233=CARTESIAN_POINT ( 'NONE',  ( 126.0135748109119902, -8.166667518702819706, -8.995218007635861213 ) ) ;
#36235=CARTESIAN_POINT ( 'NONE',  ( 124.4819548109119722, -2.084020599724406786, -8.691656652584148546 ) ) ;
#36237=CARTESIAN_POINT ( 'NONE',  ( 119.3198281442452924, 0.5811942927096110934, -14.16772938898807510 ) ) ;
#36241=CARTESIAN_POINT ( 'NONE',  ( 111.4281736080169054, -2.492852297122321037, -17.79974121491989436 ) ) ;
#36242=CARTESIAN_POINT ( 'NONE',  ( 114.5547881442453217, -4.153390946401321671, -8.397313243818183892 ) ) ;
#36245=CARTESIAN_POINT ( 'NONE',  ( 126.1837548109119211, -10.63000616557722466, -14.87417383870573495 ) ) ;
#36246=CARTESIAN_POINT ( 'NONE',  ( 112.7395348109119766, -5.638512984488999180, -18.83840828888717311 ) ) ;
#36248=CARTESIAN_POINT ( 'NONE',  ( 123.2906948109119867, -1.833838273342659697, -17.42832698103878286 ) ) ;
#36250=CARTESIAN_POINT ( 'NONE',  ( 119.3198281442452924, 0.5811942927096110934, -14.16772938898807510 ) ) ;
#36252=CARTESIAN_POINT ( 'NONE',  ( 120.6245414775786458, -9.988377603198976828, -10.36322818467138340 ) ) ;
#36253=ORIENTED_EDGE ( 'NONE', *, *, #13141, .F. ) ;
#36259=CARTESIAN_POINT ( 'NONE',  ( 135.3184548109119874, -8.536181032868617180, -18.13822074491315561 ) ) ;
#36260=CARTESIAN_POINT ( 'NONE',  ( 114.2711548109119803, -9.988377603198976828, -10.36322818467138340 ) ) ;
#36266=CARTESIAN_POINT ( 'NONE',  ( 112.6260814775786514, -9.261995988541697145, -16.69588392320189030 ) ) ;
#36267=CARTESIAN_POINT ( 'NONE',  ( 119.4332814775786318, -0.4660016031367893996, -10.09054647747474043 ) ) ;
#36272=CARTESIAN_POINT ( 'NONE',  ( 119.1496481442453046, -6.222761293078241884, -8.102969835052219238 ) ) ;
#36273=CARTESIAN_POINT ( 'NONE',  ( 116.4834948109119779, -1.561330072975668504, -17.79121239304076951 ) ) ;
#36274=CARTESIAN_POINT ( 'NONE',  ( 112.0020881442453344, 0.2603800115204892296, -16.42320221600525088 ) ) ;
#36275=CARTESIAN_POINT ( 'NONE',  ( 123.6877814775786533, -6.222761293078241884, -8.102969835052219238 ) ) ;
#36277=CARTESIAN_POINT ( 'NONE',  ( 122.9503348109119827, -9.859900752359378018, -12.68260735090039759 ) ) ;
#36278=CARTESIAN_POINT ( 'NONE',  ( 114.0442481442453300, -7.643976991954077427, -18.09477374809248928 ) ) ;
#36282=CARTESIAN_POINT ( 'NONE',  ( 117.8449348109119938, -1.833838273342659253, -17.42832698103878286 ) ) ;
#36283=ORIENTED_EDGE ( 'NONE', *, *, #16530, .F. ) ;
#36285=B_SPLINE_CURVE_WITH_KNOTS ( 'NONE', 3,
 ( #19359, #39660, #29844, #40566, #43761, #1345, #12527, #9099, #8422, #22328 ),
 .UNSPECIFIED., .F., .F.,
 ( 4, 3, 3, 4 ),
 ( 0.000000000000000000, 0.0001671877560958109985, 0.0003343755126086574896, 0.0006438490228507209303 ),
 .UNSPECIFIED. ) ;
#36286=CARTESIAN_POINT ( 'NONE',  ( 115.4624148109119943, -5.638512984488999180, -18.83840828888717311 ) ) ;
#36288=CARTESIAN_POINT ( 'NONE',  ( 112.8529881442453302, -7.894159318335828068, -9.358103419637847864 ) ) ;
#36291=CARTESIAN_POINT ( 'NONE',  ( 121.1350814775786233, -9.859900752359378018, -12.68260735090039759 ) ) ;
#36292=CARTESIAN_POINT ( 'NONE',  ( 117.9583881442453048, 0.1319031606808879209, -14.10382304977623669 ) ) ;
#36298=CARTESIAN_POINT ( 'NONE',  ( 116.3700414775786527, -5.638512984488999180, -18.83840828888717311 ) ) ;
#36299=CARTESIAN_POINT ( 'NONE',  ( 115.7460481442453357, 0.9020085738987339008, -11.91225656197089222 ) ) ;
#36300=CARTESIAN_POINT ( 'NONE',  ( 114.8951481442453115, -8.899110576539710493, -16.42337572283490132 ) ) ;
#36301=CARTESIAN_POINT ( 'NONE',  ( 121.0783548109119749, -9.565557343593413364, -10.61323700422348004 ) ) ;
#36304=CARTESIAN_POINT ( 'NONE',  ( 118.0718414775786442, -0.8288870151387760510, -10.36305467784173118 ) ) ;
#36305=CARTESIAN_POINT ( 'NONE',  ( 125.4463081442452932, -4.153390946401325223, -8.397313243818185668 ) ) ;
#36309=CARTESIAN_POINT ( 'NONE',  ( 119.8303681442453126, -10.63000616557722466, -14.87417383870573495 ) ) ;
#36310=ORIENTED_EDGE ( 'NONE', *, *, #797, .T. ) ;
#36311=CARTESIAN_POINT ( 'NONE',  ( 120.1140014775786398, -1.561330072975668504, -17.79121239304076951 ) ) ;
#36314=CARTESIAN_POINT ( 'NONE',  ( 114.6115148109119986, -3.383040157471821630, -19.15922257007629170 ) ) ;
#36315=CARTESIAN_POINT ( 'NONE',  ( 119.3198281442452924, 0.5811942927096110934, -14.16772938898807510 ) ) ;
#36321=CARTESIAN_POINT ( 'NONE',  ( 119.1496481442453046, -6.222761293078241884, -8.102969835052219238 ) ) ;
#36325=CARTESIAN_POINT ( 'NONE',  ( 113.4202548109119846, 0.1319031606808879209, -14.10382304977623669 ) ) ;
#36328=CARTESIAN_POINT ( 'NONE',  ( 113.0231681442453180, -10.15424416112533912, -14.75197769757731336 ) ) ;
#36329=CARTESIAN_POINT ( 'NONE',  ( 119.4332814775786318, -0.4660016031367893996, -10.09054647747474043 ) ) ;
#36331=CARTESIAN_POINT ( 'NONE',  ( 118.6391081442452986, -5.574606645277164318, -18.38911715685844683 ) ) ;
#36332=CARTESIAN_POINT ( 'NONE',  ( 114.6115148109119986, -3.383040157471821630, -19.15922257007629170 ) ) ;
#36333=CARTESIAN_POINT ( 'NONE',  ( 123.0637881442452937, -0.4660016031367893996, -10.09054647747474043 ) ) ;
#36334=CARTESIAN_POINT ( 'NONE',  ( 121.5321681442453183, -0.1624402480850797581, -16.17319339645315424 ) ) ;
#36336=CARTESIAN_POINT ( 'NONE',  ( 125.1059481442452750, -1.833838273342660141, -17.42832698103878286 ) ) ;
#36337=CARTESIAN_POINT ( 'NONE',  ( 118.8092881442453290, -9.988377603198976828, -10.36322818467138340 ) ) ;
#36338=CARTESIAN_POINT ( 'NONE',  ( 112.5693548109119888, 0.4262465694468514643, -12.03445270309931736 ) ) ;
#36339=CARTESIAN_POINT ( 'NONE',  ( 122.2128881442453263, -1.834011780172310813, -8.268836392978581529 ) ) ;
#36342=CARTESIAN_POINT ( 'NONE',  ( 135.7012255816029551, -0.6896191363000495622, -17.70303589939592825 ) ) ;
#36347=CARTESIAN_POINT ( 'NONE',  ( 136.2632467228252438, -10.25174699308209547, -11.13433988238026728 ) ) ;
#36348=CARTESIAN_POINT ( 'NONE',  ( 116.5402214775786405, -9.565557343593413364, -10.61323700422348004 ) ) ;
#36349=CARTESIAN_POINT ( 'NONE',  ( 112.2289948109119848, -7.643976991954077427, -18.09477374809248928 ) ) ;
#36354=CARTESIAN_POINT ( 'NONE',  ( 117.0507614775786465, 0.1319031606808879209, -14.10382304977623669 ) ) ;
#36355=CARTESIAN_POINT ( 'NONE',  ( 115.1430393777725385, -1.267766418764730840, -16.93314635290706605 ) ) ;
#36359=CARTESIAN_POINT ( 'NONE',  ( 121.4754414775786131, -8.166667518702819706, -8.995218007635861213 ) ) ;
#36360=CARTESIAN_POINT ( 'NONE',  ( 123.0637881442452937, -8.899110576539710493, -16.42337572283490132 ) ) ;
#36365=CARTESIAN_POINT ( 'NONE',  ( 122.2128881442453263, -7.643976991954077427, -18.09477374809248928 ) ) ;
#36367=CARTESIAN_POINT ( 'NONE',  ( 122.5532481442453019, 0.4262465694468514643, -12.03445270309931736 ) ) ;
#36368=CARTESIAN_POINT ( 'NONE',  ( 115.4056881442453459, -2.084020599724406786, -8.691656652584148546 ) ) ;
#36371=CARTESIAN_POINT ( 'NONE',  ( 124.0281414775786146, -7.643976991954077427, -18.09477374809248928 ) ) ;
#36372=CARTESIAN_POINT ( 'NONE',  ( 122.8936081442453059, -9.565557343593413364, -10.61323700422348004 ) ) ;
#36378=CARTESIAN_POINT ( 'NONE',  ( 122.2128881442453263, -1.834011780172310813, -8.268836392978581529 ) ) ;
#36379=CARTESIAN_POINT ( 'NONE',  ( 119.0361948109119652, -7.893985811506177619, -18.51759400769804742 ) ) ;
#36381=CARTESIAN_POINT ( 'NONE',  ( 114.9518748109119883, -1.834011780172310813, -8.268836392978581529 ) ) ;
#36385=CARTESIAN_POINT ( 'NONE',  ( 120.3976348109119812, -1.834011780172310813, -8.268836392978581529 ) ) ;
#36387=CARTESIAN_POINT ( 'NONE',  ( 125.0492214775786266, -3.505236298600246325, -18.68346056562440793 ) ) ;
#36389=CARTESIAN_POINT ( 'NONE',  ( 112.7962614775786676, -6.222761293078241884, -8.102969835052219238 ) ) ;
#36390=CARTESIAN_POINT ( 'NONE',  ( 112.0020881442453344, -9.565557343593413364, -10.61323700422348004 ) ) ;
#36393=CARTESIAN_POINT ( 'NONE',  ( 119.8870948109119752, -0.8288870151387760510, -10.36305467784173118 ) ) ;
#36399=CARTESIAN_POINT ( 'NONE',  ( 123.5743281442453139, -7.893985811506177619, -18.51759400769804742 ) ) ;
#36403=CARTESIAN_POINT ( 'NONE',  ( 119.2631014775786298, -9.565557343593413364, -10.61323700422348004 ) ) ;
#36406=CARTESIAN_POINT ( 'NONE',  ( 122.3830681442452857, -1.833838273342659697, -17.42832698103878286 ) ) ;
#36408=MANIFOLD_SOLID_BREP ( 'NONE', #42527 ) ;
#36410=CARTESIAN_POINT ( 'NONE',  ( 124.0281414775786146, -7.643976991954077427, -18.09477374809248928 ) ) ;
#36412=CARTESIAN_POINT ( 'NONE',  ( 123.0070614775786169, 0.9020085738987339008, -11.91225656197089222 ) ) ;
#36414=CARTESIAN_POINT ( 'NONE',  ( 118.6391081442452986, -5.574606645277164318, -18.38911715685844683 ) ) ;
#36416=CARTESIAN_POINT ( 'NONE',  ( 124.8223148109119762, -10.15424416112533912, -14.75197769757731336 ) ) ;
#36417=CARTESIAN_POINT ( 'NONE',  ( 122.9503348109119827, 0.5811942927096110934, -14.16772938898807510 ) ) ;
#36418=CARTESIAN_POINT ( 'NONE',  ( 115.4624148109119943, -5.638512984488999180, -18.83840828888717311 ) ) ;
#36420=CARTESIAN_POINT ( 'NONE',  ( 113.4202548109119846, -10.30919188438809542, -12.61870101168854852 ) ) ;
#36421=CARTESIAN_POINT ( 'NONE',  ( 125.8433948109119456, -7.643976991954077427, -18.09477374809248928 ) ) ;
#36423=CARTESIAN_POINT ( 'NONE',  ( 119.4900081442453086, -1.834011780172310813, -8.268836392978581529 ) ) ;
#36427=CARTESIAN_POINT ( 'NONE',  ( 114.1009748109119784, -5.574606645277164318, -18.38911715685844683 ) ) ;
#36433=CARTESIAN_POINT ( 'NONE',  ( 124.6521348109119884, -7.894159318335828068, -9.358103419637847864 ) ) ;
#36440=CARTESIAN_POINT ( 'NONE',  ( 114.8384214775786489, 0.9020085738987339008, -11.91225656197089222 ) ) ;
#36441=CARTESIAN_POINT ( 'NONE',  ( 125.6164881442453094, 0.2603800115204892296, -16.42320221600525088 ) ) ;
#36442=CARTESIAN_POINT ( 'NONE',  ( 125.6732148109119862, -9.859900752359378018, -12.68260735090039759 ) ) ;
#36443=CARTESIAN_POINT ( 'NONE',  ( 115.0653281442453277, -3.505236298600246325, -18.68346056562440793 ) ) ;
#36444=CARTESIAN_POINT ( 'NONE',  ( 128.2184548109119930, -9.609004340414083245, -9.721032963308941177 ) ) ;
#36447=CARTESIAN_POINT ( 'NONE',  ( 115.8595014775786609, -1.834011780172310813, -8.268836392978581529 ) ) ;
#36451=CARTESIAN_POINT ( 'NONE',  ( 124.3685014775786328, -10.63000616557722466, -14.87417383870573495 ) ) ;
#36453=ORIENTED_EDGE ( 'NONE', *, *, #33171, .T. ) ;
#36454=CARTESIAN_POINT ( 'NONE',  ( 115.7460481442453357, 0.9020085738987339008, -11.91225656197089222 ) ) ;
#36455=CARTESIAN_POINT ( 'NONE',  ( 112.0020881442453344, -9.565557343593413364, -10.61323700422348004 ) ) ;
#36458=CARTESIAN_POINT ( 'NONE',  ( 126.1270281442452870, 0.1319031606808879209, -14.10382304977623669 ) ) ;
#36460=CARTESIAN_POINT ( 'NONE',  ( 117.6180281442453150, -0.4660016031367893996, -10.09054647747474043 ) ) ;
#36468=CARTESIAN_POINT ( 'NONE',  ( 135.5886503745646792, -2.475940008444037943, -7.888983817636334273 ) ) ;
#36469=CARTESIAN_POINT ( 'NONE',  ( 113.9307948109119764, -10.15424416112533912, -14.75197769757731336 ) ) ;
#36472=CARTESIAN_POINT ( 'NONE',  ( 111.8886348109120092, -6.222761293078241884, -8.102969835052219238 ) ) ;
#36473=CARTESIAN_POINT ( 'NONE',  ( 126.0703014775786102, -0.1624402480850797581, -16.17319339645315424 ) ) ;
#36475=CARTESIAN_POINT ( 'NONE',  ( 122.3263414775786373, -3.505236298600246325, -18.68346056562440793 ) ) ;
#36477=CARTESIAN_POINT ( 'NONE',  ( 123.1205148109119563, -1.834011780172310813, -8.268836392978581529 ) ) ;
#36478=CARTESIAN_POINT ( 'NONE',  ( 122.0427081442452817, 0.5811942927096110934, -14.16772938898807510 ) ) ;
#36479=ORIENTED_EDGE ( 'NONE', *, *, #23681, .T. ) ;
#36485=CARTESIAN_POINT ( 'NONE',  ( 125.1626748109119802, -0.1624402480845399399, -16.17319339645223053 ) ) ;
#36486=CARTESIAN_POINT ( 'NONE',  ( 116.4267681442453153, -3.383040157471821630, -19.15922257007629170 ) ) ;
#36487=ORIENTED_EDGE ( 'NONE', *, *, #26957, .T. ) ;
#36490=CARTESIAN_POINT ( 'NONE',  ( 116.0864081442453113, -0.1624402480850797581, -16.17319339645315424 ) ) ;
#36491=CARTESIAN_POINT ( 'NONE',  ( 122.8959708535611242, -2.239543233855044946, -18.13706010537467606 ) ) ;
#36492=CARTESIAN_POINT ( 'NONE',  ( 118.5823814775786360, -1.834011780172310813, -8.268836392978581529 ) ) ;
#36494=CARTESIAN_POINT ( 'NONE',  ( 119.2263198309151164, -2.215723800389698184, -18.16877924232191788 ) ) ;
#36498=CARTESIAN_POINT ( 'NONE',  ( 120.2274548109119934, -9.859900752359374465, -12.68260735090039404 ) ) ;
#36499=CARTESIAN_POINT ( 'NONE',  ( 114.9518748109119883, -1.834011780172310813, -8.268836392978581529 ) ) ;
#36500=CARTESIAN_POINT ( 'NONE',  ( 117.1642148109119859, -9.261995988541697145, -16.69588392320189030 ) ) ;
#36502=CARTESIAN_POINT ( 'NONE',  ( 121.8725281442453223, -6.222761293078241884, -8.102969835052219238 ) ) ;
#36503=CARTESIAN_POINT ( 'NONE',  ( 120.2274548109119934, -9.859900752359378018, -12.68260735090039759 ) ) ;
#36506=CARTESIAN_POINT ( 'NONE',  ( 111.7184548109119788, -9.261995988541697145, -16.69588392320189030 ) ) ;
#36507=CARTESIAN_POINT ( 'NONE',  ( 116.6536748109119941, -10.15424416112533912, -14.75197769757731336 ) ) ;
#36510=CARTESIAN_POINT ( 'NONE',  ( 115.7460481442453357, 0.9020085738987339008, -11.91225656197089222 ) ) ;
#36512=CARTESIAN_POINT ( 'NONE',  ( 114.0442481442453300, -7.643976991954077427, -18.09477374809248928 ) ) ;
#36517=CARTESIAN_POINT ( 'NONE',  ( 121.4187148109119789, -3.505236298600246325, -18.68346056562440793 ) ) ;
#36518=CARTESIAN_POINT ( 'NONE',  ( 122.7801548109119665, -6.222761293078241884, -8.102969835052219238 ) ) ;
#36520=VERTEX_POINT ( 'NONE', #30372 ) ;
#36521=CARTESIAN_POINT ( 'NONE',  ( 112.1691149257650579, -8.910908836065232208, -16.40337021355369629 ) ) ;
#36524=CARTESIAN_POINT ( 'NONE',  ( 116.1431348109119881, -10.30919188438810075, -12.61870101168855918 ) ) ;
#36525=CARTESIAN_POINT ( 'NONE',  ( 116.1431348109119881, -10.30919188438810075, -12.61870101168855918 ) ) ;
#36526=CARTESIAN_POINT ( 'NONE',  ( 115.8595014775786609, -7.643976991954077427, -18.09477374809248928 ) ) ;
#36528=CARTESIAN_POINT ( 'NONE',  ( 120.8514481442452961, -2.084020599724406786, -8.691656652584148546 ) ) ;
#36531=CARTESIAN_POINT ( 'NONE',  ( 119.4332814775786318, -8.899110576539710493, -16.42337572283490132 ) ) ;
#36532=CARTESIAN_POINT ( 'NONE',  ( 128.2184548109119930, -4.863998795839242995, -13.39321520033831447 ) ) ;
#36536=CARTESIAN_POINT ( 'NONE',  ( 118.6391081442452986, -4.089484607189486809, -7.948022111789456723 ) ) ;
#36538=CARTESIAN_POINT ( 'NONE',  ( 122.4965214775786251, -10.30919188438810075, -12.61870101168855918 ) ) ;
#36541=CARTESIAN_POINT ( 'NONE',  ( 118.6391081442452986, -4.089484607189486809, -7.948022111789456723 ) ) ;
#36542=CARTESIAN_POINT ( 'NONE',  ( 117.9016614775786280, -9.988377603198976828, -10.36322818467138340 ) ) ;
#36545=ORIENTED_EDGE ( 'NONE', *, *, #20500, .F. ) ;
#36546=FACE_OUTER_BOUND ( 'NONE', #12258, .T. ) ;
#36548=CARTESIAN_POINT ( 'NONE',  ( 120.8514481442452961, -2.084020599724406786, -8.691656652584148546 ) ) ;
#36551=CARTESIAN_POINT ( 'NONE',  ( 116.7671281442453335, -7.643976991954077427, -18.09477374809248928 ) ) ;
#36554=CARTESIAN_POINT ( 'NONE',  ( 112.6260814775786514, -0.8288870151387760510, -10.36305467784173118 ) ) ;
#36555=CARTESIAN_POINT ( 'NONE',  ( 118.6391081442452986, -4.089484607189486809, -7.948022111789456723 ) ) ;
#36557=CARTESIAN_POINT ( 'NONE',  ( 119.0929214775786278, -4.153390946401325223, -8.397313243818185668 ) ) ;
#36559=CARTESIAN_POINT ( 'NONE',  ( 114.6682414775786469, -1.561330072975668060, -17.79121239304076596 ) ) ;
#36560=CARTESIAN_POINT ( 'NONE',  ( 120.7379948109119709, -10.63000616557722466, -14.87417383870573495 ) ) ;
#36561=CARTESIAN_POINT ( 'NONE',  ( 123.3474214775786209, -0.1624402480850797581, -16.17319339645315424 ) ) ;
#36563=CARTESIAN_POINT ( 'NONE',  ( 116.1954459692789641, -1.179503403430490538, -17.05068175419388865 ) ) ;
#36565=CARTESIAN_POINT ( 'NONE',  ( 119.2631014775786298, 0.2603800115204892296, -16.42320221600525088 ) ) ;
#36566=CARTESIAN_POINT ( 'NONE',  ( 112.3991748109119868, -1.833838273342658809, -17.42832698103878286 ) ) ;
#36567=CARTESIAN_POINT ( 'NONE',  ( 124.9357681442453014, -1.834011780172310813, -8.268836392978581529 ) ) ;
#36572=AXIS2_PLACEMENT_3D ( 'NONE', #17478, #39965, #1651 ) ;
#36575=CARTESIAN_POINT ( 'NONE',  ( 135.8497638153382070, -10.33978686199914598, -11.03243195220415451 ) ) ;
#36576=CARTESIAN_POINT ( 'NONE',  ( 119.8870948109119752, -0.8288870151387760510, -10.36305467784173118 ) ) ;
#36577=CARTESIAN_POINT ( 'NONE',  ( 125.9001214775786224, -4.089484607189486809, -7.948022111789456723 ) ) ;
#36580=CARTESIAN_POINT ( 'NONE',  ( 112.1237736387913770, -8.918551276432252095, -16.31957112036458568 ) ) ;
#36582=CARTESIAN_POINT ( 'NONE',  ( 117.6180281442453150, -8.899110576539710493, -16.42337572283490132 ) ) ;
#36588=CARTESIAN_POINT ( 'NONE',  ( 124.6521348109119884, -1.561330072975668948, -17.79121239304076951 ) ) ;
#36589=CARTESIAN_POINT ( 'NONE',  ( 124.0848681442452772, -5.574606645277164318, -18.38911715685844683 ) ) ;
#36591=FACE_OUTER_BOUND ( 'NONE', #4502, .T. ) ;
#36592=CARTESIAN_POINT ( 'NONE',  ( 125.3895814775786448, -7.893985811506177619, -18.51759400769804742 ) ) ;
#36594=CARTESIAN_POINT ( 'NONE',  ( 120.3976348109119812, -7.643976991954077427, -18.09477374809248928 ) ) ;
#36595=CARTESIAN_POINT ( 'NONE',  ( 119.1496481442453046, -6.222761293078241884, -8.102969835052219238 ) ) ;
#36596=CARTESIAN_POINT ( 'NONE',  ( 119.2255797424434149, -0.9924539043446216624, -17.29976612834909133 ) ) ;
#36605=CARTESIAN_POINT ( 'NONE',  ( 121.3619881442452879, -4.089484607189486809, -7.948022111789456723 ) ) ;
#36606=CARTESIAN_POINT ( 'NONE',  ( 122.5532481442453019, -10.63000616557722466, -14.87417383870573495 ) ) ;
#36608=CARTESIAN_POINT ( 'NONE',  ( 117.9016614775786280, -9.988377603198976828, -10.36322818467138340 ) ) ;
#36612=CARTESIAN_POINT ( 'NONE',  ( 124.3685014775786328, -10.63000616557722466, -14.87417383870573495 ) ) ;
#36614=CARTESIAN_POINT ( 'NONE',  ( 121.4754414775786131, -8.166667518702819706, -8.995218007635861213 ) ) ;
#36615=CARTESIAN_POINT ( 'NONE',  ( 125.9001214775786224, -5.574606645277164318, -18.38911715685844683 ) ) ;
#36616=CARTESIAN_POINT ( 'NONE',  ( 114.7816948109119863, -9.859900752359374465, -12.68260735090039404 ) ) ;
#36617=CARTESIAN_POINT ( 'NONE',  ( 124.6521348109119884, -1.561330072975668948, -17.79121239304076951 ) ) ;
#36620=CARTESIAN_POINT ( 'NONE',  ( 118.4122014775786340, -9.859900752359374465, -12.68260735090039404 ) ) ;
#36623=ORIENTED_EDGE ( 'NONE', *, *, #28663, .F. ) ;
#36625=CARTESIAN_POINT ( 'NONE',  ( 121.4187148109119789, -6.344957434206665248, -7.627207830600338134 ) ) ;
#36630=CARTESIAN_POINT ( 'NONE',  ( 118.9794681442453026, -0.8288870151387760510, -10.36305467784173118 ) ) ;
#36633=CARTESIAN_POINT ( 'NONE',  ( 122.7234281442452755, -4.153390946401325223, -8.397313243818185668 ) ) ;
#36634=CARTESIAN_POINT ( 'NONE',  ( 123.6854187682627781, -1.040089454026960292, -17.23633227186633476 ) ) ;
#36639=CARTESIAN_POINT ( 'NONE',  ( 121.1350814775786233, 0.5811942927096110934, -14.16772938898807510 ) ) ;
#36640=CARTESIAN_POINT ( 'NONE',  ( 115.8595014775786609, -7.643976991954077427, -18.09477374809248928 ) ) ;
#36641=CARTESIAN_POINT ( 'NONE',  ( 121.5321681442453183, -0.1624402480850797581, -16.17319339645315424 ) ) ;
#36643=CARTESIAN_POINT ( 'NONE',  ( 123.3474214775786209, -9.988377603198976828, -10.36322818467138340 ) ) ;
#36644=CARTESIAN_POINT ( 'NONE',  ( 114.3846081442453197, -10.63000616557722466, -14.87417383870573495 ) ) ;
#36646=CARTESIAN_POINT ( 'NONE',  ( 112.5126281442453120, 0.1319031606808879209, -14.10382304977623669 ) ) ;
#36647=CARTESIAN_POINT ( 'NONE',  ( 124.3117748109119844, 0.1319031606808879209, -14.10382304977623669 ) ) ;
#36648=CARTESIAN_POINT ( 'NONE',  ( 124.4819548109119722, -7.893985811506177619, -18.51759400769804742 ) ) ;
#36656=CARTESIAN_POINT ( 'NONE',  ( 125.7866681442452688, -8.899110576539710493, -16.42337572283490132 ) ) ;
#36662=CARTESIAN_POINT ( 'NONE',  ( 118.3554748109119998, 0.2603800115204892296, -16.42320221600525088 ) ) ;
#36663=CARTESIAN_POINT ( 'NONE',  ( 123.8012348109119642, -9.565557343593413364, -10.61323700422348004 ) ) ;
#36664=CARTESIAN_POINT ( 'NONE',  ( 116.1998614775786507, 0.4262465694468514643, -12.03445270309931736 ) ) ;
#36669=CARTESIAN_POINT ( 'NONE',  ( 115.8027748109119841, -0.4660016031367893996, -10.09054647747474043 ) ) ;
#36671=CARTESIAN_POINT ( 'NONE',  ( 123.5176014775786228, -9.261995988541697145, -16.69588392320189030 ) ) ;
#36674=CARTESIAN_POINT ( 'NONE',  ( 113.3068014775786594, -8.166667518702817929, -8.995218007635859436 ) ) ;
#36675=CARTESIAN_POINT ( 'NONE',  ( 113.8173414775786512, -9.565557343593413364, -10.61323700422348004 ) ) ;
#36677=CARTESIAN_POINT ( 'NONE',  ( 126.0135748109119902, -1.833838273342660141, -17.42832698103878286 ) ) ;
#36679=CARTESIAN_POINT ( 'NONE',  ( 122.7801548109119665, -3.383040157471821630, -19.15922257007629170 ) ) ;
#36682=DIRECTION ( 'NONE',  ( 1.000000000000000000, 0.000000000000000000, 0.000000000000000000 ) ) ;
#36683=CARTESIAN_POINT ( 'NONE',  ( 123.2184548109119788, -3.410847707154505137, -16.57729307524250828 ) ) ;
#36684=CARTESIAN_POINT ( 'NONE',  ( 115.2922348109119781, 0.4262465694468514643, -12.03445270309931736 ) ) ;
#36685=EDGE_CURVE ( 'NONE', #40611, #41698, #33828, .T. ) ;
#36688=CARTESIAN_POINT ( 'NONE',  ( 111.8319081442453182, -4.153390946401321671, -8.397313243818183892 ) ) ;
#36689=CARTESIAN_POINT ( 'NONE',  ( 113.3068014775786594, -8.166667518702817929, -8.995218007635859436 ) ) ;
#36691=CARTESIAN_POINT ( 'NONE',  ( 125.9001214775786224, -5.574606645277164318, -18.38911715685844683 ) ) ;
#36692=CARTESIAN_POINT ( 'NONE',  ( 115.8595014775786609, -7.643976991954077427, -18.09477374809248928 ) ) ;
#36693=CARTESIAN_POINT ( 'NONE',  ( 122.1561614775786353, -0.4660016031367893996, -10.09054647747474043 ) ) ;
#36695=CARTESIAN_POINT ( 'NONE',  ( 120.6812681442452941, -10.30919188438810075, -12.61870101168855918 ) ) ;
#36697=CARTESIAN_POINT ( 'NONE',  ( 126.5254139959020847, -8.556035843926350637, -16.98867727300566699 ) ) ;
#36698=EDGE_CURVE ( 'NONE', #37016, #33070, #5856, .T. ) ;
#36702=CARTESIAN_POINT ( 'NONE',  ( 125.4463081442453500, -4.153390946402302220, -8.397313243818043560 ) ) ;
#36703=CARTESIAN_POINT ( 'NONE',  ( 113.5904348109119866, -7.893985811506177619, -18.51759400769804742 ) ) ;
#36705=CARTESIAN_POINT ( 'NONE',  ( 126.2404814775786264, -9.261995988541697145, -16.69588392320189030 ) ) ;
#36708=CARTESIAN_POINT ( 'NONE',  ( 114.0442481442453300, -7.643976991954077427, -18.09477374809248928 ) ) ;
#36709=CARTESIAN_POINT ( 'NONE',  ( 119.2631014775786298, 0.2603800115204892296, -16.42320221600525088 ) ) ;
#36714=CARTESIAN_POINT ( 'NONE',  ( 121.7023481442452919, -0.8288870151387760510, -10.36305467784173118 ) ) ;
#36715=CARTESIAN_POINT ( 'NONE',  ( 119.3198281442452924, 0.5811942927096110934, -14.16772938898807510 ) ) ;
#36716=CARTESIAN_POINT ( 'NONE',  ( 113.9307948109119764, -10.15424416112533912, -14.75197769757731336 ) ) ;
#36717=CARTESIAN_POINT ( 'NONE',  ( 115.2922348109119781, -10.63000616557722466, -14.87417383870573495 ) ) ;
#36719=CARTESIAN_POINT ( 'NONE',  ( 136.0073873814629337, -7.187683303096414456, -18.83671677009607848 ) ) ;
#36720=CARTESIAN_POINT ( 'NONE',  ( 122.2128881442453263, -7.643976991954077427, -18.09477374809248928 ) ) ;
#36721=CARTESIAN_POINT ( 'NONE',  ( 120.6245414775786458, -0.1624402480850797581, -16.17319339645315424 ) ) ;
#36727=CARTESIAN_POINT ( 'NONE',  ( 111.7751814775786556, -7.893985811506177619, -18.51759400769804742 ) ) ;
#36728=CARTESIAN_POINT ( 'NONE',  ( 123.1205148109119563, -7.643976991954077427, -18.09477374809248928 ) ) ;
#36731=CARTESIAN_POINT ( 'NONE',  ( 117.3911214775786505, -1.561330072975668504, -17.79121239304076951 ) ) ;
#36734=CARTESIAN_POINT ( 'NONE',  ( 117.7882081442453170, -3.505236298600246325, -18.68346056562440793 ) ) ;
#36737=CARTESIAN_POINT ( 'NONE',  ( 121.7023481442452919, -0.8288870151387760510, -10.36305467784173118 ) ) ;
#36738=CARTESIAN_POINT ( 'NONE',  ( 121.7590748109119687, -2.084020599724406786, -8.691656652584148546 ) ) ;
#36742=CARTESIAN_POINT ( 'NONE',  ( 117.9016614775786280, -9.988377603198976828, -10.36322818467138340 ) ) ;
#36744=CARTESIAN_POINT ( 'NONE',  ( 116.3133148109119759, -7.893985811506177619, -18.51759400769804742 ) ) ;
#36745=CARTESIAN_POINT ( 'NONE',  ( 116.5402214775786405, 0.2603800115204892296, -16.42320221600525088 ) ) ;
#36746=CARTESIAN_POINT ( 'NONE',  ( 116.6536748109119941, -10.15424416112533912, -14.75197769757731336 ) ) ;
#36747=CARTESIAN_POINT ( 'NONE',  ( 119.5467348109119712, -5.574606645277164318, -18.38911715685844683 ) ) ;
#36750=CARTESIAN_POINT ( 'NONE',  ( 122.0994348109119443, -10.15424416112533912, -14.75197769757731336 ) ) ;
#36752=CARTESIAN_POINT ( 'NONE',  ( 113.8979809388149533, -2.287189184988692059, -18.07361239780447448 ) ) ;
#36757=CARTESIAN_POINT ( 'NONE',  ( 118.9227414775786400, -10.63000616557722466, -14.87417383870573495 ) ) ;
#36758=ORIENTED_EDGE ( 'NONE', *, *, #23941, .T. ) ;
#36759=CARTESIAN_POINT ( 'NONE',  ( 121.9859814775786333, 0.2603800115204892296, -16.42320221600525088 ) ) ;
#36762=CARTESIAN_POINT ( 'NONE',  ( 120.7947214775786193, -9.261995988541697145, -16.69588392320189030 ) ) ;
#36763=CARTESIAN_POINT ( 'NONE',  ( 116.2565881442452991, -9.261995988541697145, -16.69588392320189030 ) ) ;
#36766=CARTESIAN_POINT ( 'NONE',  ( 114.2354127111058659, -1.267766418764742165, -16.93314635290707315 ) ) ;
#36770=CARTESIAN_POINT ( 'NONE',  ( 121.4754414775786131, -1.833838273342659697, -17.42832698103878286 ) ) ;
#36773=CARTESIAN_POINT ( 'NONE',  ( 119.6034614775786196, -3.505236298600246325, -18.68346056562440793 ) ) ;
#36776=CARTESIAN_POINT ( 'NONE',  ( 113.2500748109119968, -3.505236298600246325, -18.68346056562440793 ) ) ;
#36777=CARTESIAN_POINT ( 'NONE',  ( 122.6667014775786413, -7.893985811506177619, -18.51759400769804742 ) ) ;
#36780=CARTESIAN_POINT ( 'NONE',  ( 120.4543614775786295, -5.574606645277164318, -18.38911715685844683 ) ) ;
#36781=CARTESIAN_POINT ( 'NONE',  ( 115.1787814775786387, -9.988377603198976828, -10.36322818467138340 ) ) ;
#36782=CARTESIAN_POINT ( 'NONE',  ( 121.4754414775786131, -8.166667518702819706, -8.995218007635861213 ) ) ;
#36783=CARTESIAN_POINT ( 'NONE',  ( 123.6310548109119765, -4.153390946401325223, -8.397313243818185668 ) ) ;
#36786=CARTESIAN_POINT ( 'NONE',  ( 123.5176014775786228, -0.8288870151387760510, -10.36305467784173118 ) ) ;
#36788=CARTESIAN_POINT ( 'NONE',  ( 124.8223148109119762, 0.9020085738987339008, -11.91225656197089222 ) ) ;
#36790=CARTESIAN_POINT ( 'NONE',  ( 111.3780948109119890, -5.574606645277164318, -18.38911715685844683 ) ) ;
#36791=B_SPLINE_CURVE_WITH_KNOTS ( 'NONE', 3,
 ( #27020, #10146, #41614, #2835 ),
 .UNSPECIFIED., .F., .F.,
 ( 4, 4 ),
 ( 0.005938763149045529939, 0.008179074650722518991 ),
 .UNSPECIFIED. ) ;
#36794=CARTESIAN_POINT ( 'NONE',  ( 127.7862423803841381, -3.345148870660049845, -14.16624594358310141 ) ) ;
#36797=CARTESIAN_POINT ( 'NONE',  ( 117.2985964273310060, -2.236191541394345172, -18.14152338500401029 ) ) ;
#36798=CARTESIAN_POINT ( 'NONE',  ( 120.4543614775786295, -5.574606645277164318, -18.38911715685844683 ) ) ;
#36799=CARTESIAN_POINT ( 'NONE',  ( 123.7445081442452874, -1.561330072975668948, -17.79121239304076951 ) ) ;
#36800=CARTESIAN_POINT ( 'NONE',  ( 126.5177454662631220, -6.230080189768934851, -18.35871718775414152 ) ) ;
#36804=CARTESIAN_POINT ( 'NONE',  ( 117.2776681442452968, -4.153390946401321671, -8.397313243818183892 ) ) ;
#36807=CARTESIAN_POINT ( 'NONE',  ( 124.1800355643466673, -1.244021962887375432, -16.96476564598603431 ) ) ;
#36809=CARTESIAN_POINT ( 'NONE',  ( 123.0070614775786169, 0.9020085738987339008, -11.91225656197089222 ) ) ;
#36810=CARTESIAN_POINT ( 'NONE',  ( 122.3263414775786373, -3.505236298600246325, -18.68346056562440793 ) ) ;
#36813=CARTESIAN_POINT ( 'NONE',  ( 124.9924948109119924, -4.089484607189486809, -7.948022111789456723 ) ) ;
#36815=EDGE_CURVE ( 'NONE', #27848, #11611, #12273, .T. ) ;
#36816=CARTESIAN_POINT ( 'NONE',  ( 121.9859814775786333, -9.565557343593413364, -10.61323700422348004 ) ) ;
#36817=CARTESIAN_POINT ( 'NONE',  ( 119.3765548109119834, -10.15424416112533912, -14.75197769757731336 ) ) ;
#36826=CARTESIAN_POINT ( 'NONE',  ( 119.9438214775786378, -7.893985811506177619, -18.51759400769804742 ) ) ;
#36827=CARTESIAN_POINT ( 'NONE',  ( 121.0216281442452981, -1.561330072975668948, -17.79121239304076951 ) ) ;
#36829=CARTESIAN_POINT ( 'NONE',  ( 116.8805814775786445, -6.344957434206662583, -7.627207830600332805 ) ) ;
#36830=CARTESIAN_POINT ( 'NONE',  ( 113.4769814775786330, -10.63000616557722466, -14.87417383870573495 ) ) ;
#36834=CARTESIAN_POINT ( 'NONE',  ( 121.6456214775786293, -10.63000616557722466, -14.87417383870573495 ) ) ;
#36835=CARTESIAN_POINT ( 'NONE',  ( 121.8158014775786171, -5.638512984488999180, -18.83840828888717311 ) ) ;
#36837=CARTESIAN_POINT ( 'NONE',  ( 111.9453614775786434, -1.561330072975668060, -17.79121239304076596 ) ) ;
#36839=CARTESIAN_POINT ( 'NONE',  ( 111.6617281442453304, 0.4262465694468514643, -12.03445270309931736 ) ) ;
#36840=CARTESIAN_POINT ( 'NONE',  ( 115.7460481442453357, -10.15424416112533912, -14.75197769757731336 ) ) ;
#36841=CARTESIAN_POINT ( 'NONE',  ( 124.5954081442453116, -3.383040157471821630, -19.15922257007629170 ) ) ;
#36843=CARTESIAN_POINT ( 'NONE',  ( 119.6034614775786196, -3.505236298600246325, -18.68346056562440793 ) ) ;
#36849=CARTESIAN_POINT ( 'NONE',  ( 124.1415948109119540, -6.344957434206665248, -7.627207830600338134 ) ) ;
#36850=VECTOR ( 'NONE', #37607, 1000.000000000000000 ) ;
#36855=CARTESIAN_POINT ( 'NONE',  ( 124.9357681442453014, -7.643976991954077427, -18.09477374809248928 ) ) ;
#36860=CARTESIAN_POINT ( 'NONE',  ( 125.6164881442453094, 0.2603800115204892296, -16.42320221600525088 ) ) ;
#36861=CARTESIAN_POINT ( 'NONE',  ( 116.9373081442452929, -1.833838273342659253, -17.42832698103878286 ) ) ;
#36864=CARTESIAN_POINT ( 'NONE',  ( 124.8790414775786246, -0.4660016031367893996, -10.09054647747474043 ) ) ;
#36865=CARTESIAN_POINT ( 'NONE',  ( 116.9940348109119839, -9.988377603198976828, -10.36322818467138340 ) ) ;
#36867=CARTESIAN_POINT ( 'NONE',  ( 113.7038881442453402, -6.222761293078241884, -8.102969835052219238 ) ) ;
#36868=CARTESIAN_POINT ( 'NONE',  ( 124.8790414775786246, -8.899110576539710493, -16.42337572283490132 ) ) ;
#36869=CARTESIAN_POINT ( 'NONE',  ( 122.7801548109119665, -3.383040157471821630, -19.15922257007629170 ) ) ;
#36874=CARTESIAN_POINT ( 'NONE',  ( 117.5613014775786525, -10.15424416112533912, -14.75197769757731336 ) ) ;
#36879=CARTESIAN_POINT ( 'NONE',  ( 124.3117748109119844, 0.1319031606808879209, -14.10382304977623669 ) ) ;
#36887=CARTESIAN_POINT ( 'NONE',  ( 118.2420214775786320, -3.383040157471821630, -19.15922257007629170 ) ) ;
#36888=CARTESIAN_POINT ( 'NONE',  ( 125.3328548109119964, -0.8288870151387760510, -10.36305467784173118 ) ) ;
#36890=CARTESIAN_POINT ( 'NONE',  ( 113.2500748109119968, -3.505236298600246325, -18.68346056562440793 ) ) ;
#36893=CARTESIAN_POINT ( 'NONE',  ( 116.2565881442452991, -9.261995988541697145, -16.69588392320189030 ) ) ;
#36896=CARTESIAN_POINT ( 'NONE',  ( 125.9568481442452850, -6.344957434206665248, -7.627207830600338134 ) ) ;
#36899=CARTESIAN_POINT ( 'NONE',  ( 115.2355081442453155, -10.30919188438810075, -12.61870101168855918 ) ) ;
#36900=CARTESIAN_POINT ( 'NONE',  ( 114.1009748109119784, -5.574606645277164318, -18.38911715685844683 ) ) ;
#36901=CARTESIAN_POINT ( 'NONE',  ( 126.3539348109119800, -4.153390946401325223, -8.397313243818185668 ) ) ;
#36903=CARTESIAN_POINT ( 'NONE',  ( 121.7023481442452777, -9.261995988541697145, -16.69588392320189030 ) ) ;
#36907=CARTESIAN_POINT ( 'NONE',  ( 135.8497638153212108, -2.503215547705048394, -7.917427134178404380 ) ) ;
#36908=CARTESIAN_POINT ( 'NONE',  ( 113.3068014775786594, -1.833838273342658809, -17.42832698103878286 ) ) ;
#36912=CARTESIAN_POINT ( 'NONE',  ( 116.9940348109119839, -0.1624402480850797581, -16.17319339645315424 ) ) ;
#36913=CARTESIAN_POINT ( 'NONE',  ( 126.2404814775786264, -0.8288870151387760510, -10.36305467784173118 ) ) ;
#36915=CARTESIAN_POINT ( 'NONE',  ( 111.7751814775786556, -7.893985811506177619, -18.51759400769804742 ) ) ;
#36916=CARTESIAN_POINT ( 'NONE',  ( 115.4624148109119943, -4.153390946401321671, -8.397313243818183892 ) ) ;
#36917=CARTESIAN_POINT ( 'NONE',  ( 122.7234281442452755, -5.638512984488999180, -18.83840828888717311 ) ) ;
#36919=CARTESIAN_POINT ( 'NONE',  ( 120.7379948109119709, -10.63000616557722466, -14.87417383870573495 ) ) ;
#36921=CARTESIAN_POINT ( 'NONE',  ( 114.3846081442453197, -10.63000616557722466, -14.87417383870573495 ) ) ;
#36926=CARTESIAN_POINT ( 'NONE',  ( 118.1852948109119836, -5.638512984488999180, -18.83840828888717311 ) ) ;
#36930=CARTESIAN_POINT ( 'NONE',  ( 125.2761281442453196, -10.63000616557728506, -14.87417383870603160 ) ) ;
#36931=CARTESIAN_POINT ( 'NONE',  ( 115.2355081442453155, 0.1319031606808879209, -14.10382304977623669 ) ) ;
#36932=( BOUNDED_CURVE ( )  B_SPLINE_CURVE ( 2, ( #41082, #37639, #6413, #31679, #4313, #14816, #7967, #25528, #32576, #1120, #448, #25079, #28728 ),
 .UNSPECIFIED., .F., .F. ) 
 B_SPLINE_CURVE_WITH_KNOTS ( ( 3, 2, 2, 2, 2, 2, 3 ),
 ( 0.8296282416568590001, 0.8359375000000000000, 0.8437500000000000000, 0.8515625000000000000, 0.8593750000000000000, 0.8671875000000000000, 0.8750000000000000000 ),
 .UNSPECIFIED. ) 
 CURVE ( )  GEOMETRIC_REPRESENTATION_ITEM ( )  RATIONAL_B_SPLINE_CURVE ( ( 0.9763430640195970289, 0.9385262470928680267, 1.000000000000000000, 0.9238795325112869605, 1.000000000000000000, 0.9238795325112869605, 1.000000000000000000, 0.9238795325112869605, 1.000000000000000000, 0.9238795325112869605, 1.000000000000000000, 0.9238795325112869605, 1.000000000000000000 ) ) 
 REPRESENTATION_ITEM ( '' )  );
#36934=CARTESIAN_POINT ( 'NONE',  ( 120.7379948109119709, -10.63000616557722466, -14.87417383870573495 ) ) ;
#36939=CARTESIAN_POINT ( 'NONE',  ( 120.9649014775786355, -6.222761293078241884, -8.102969835052219238 ) ) ;
#36940=CARTESIAN_POINT ( 'NONE',  ( 119.8303681442453126, -10.63000616557722466, -14.87417383870573495 ) ) ;
#36942=CARTESIAN_POINT ( 'NONE',  ( 114.4413348109119823, -0.8288870151387760510, -10.36305467784173118 ) ) ;
#36943=CARTESIAN_POINT ( 'NONE',  ( 116.3133148109119759, -7.893985811506177619, -18.51759400769804742 ) ) ;
#36944=DIRECTION ( 'NONE',  ( -0.7071067811865480168, -0.5654279342906962658, -0.4246071727182139655 ) ) ;
#36945=CARTESIAN_POINT ( 'NONE',  ( 121.9859814775786333, -9.565557343593413364, -10.61323700422348004 ) ) ;
#36946=CARTESIAN_POINT ( 'NONE',  ( 119.7736414775786358, 0.1319031606808879209, -14.10382304977623669 ) ) ;
#36948=CARTESIAN_POINT ( 'NONE',  ( 113.7606148109119886, -1.561330072975668060, -17.79121239304076596 ) ) ;
#36949=CARTESIAN_POINT ( 'NONE',  ( 119.6034614775786196, -3.505236298600246325, -18.68346056562440793 ) ) ;
#36950=EDGE_LOOP ( 'NONE', ( #9219, #28158, #20877, #26237 ) ) ;
#36952=CARTESIAN_POINT ( 'NONE',  ( 120.2274548109119934, 0.5811942927096110934, -14.16772938898807510 ) ) ;
#36954=CARTESIAN_POINT ( 'NONE',  ( 116.0296814775786345, -1.833838273342658809, -17.42832698103878286 ) ) ;
#36957=CARTESIAN_POINT ( 'NONE',  ( 124.9924948109119924, -5.574606645277164318, -18.38911715685844683 ) ) ;
#36958=CARTESIAN_POINT ( 'NONE',  ( 121.0216281442452981, -7.894159318335828068, -9.358103419637847864 ) ) ;
#36960=ORIENTED_EDGE ( 'NONE', *, *, #3633, .T. ) ;
#36961=CARTESIAN_POINT ( 'NONE',  ( 116.9373081442452929, -8.166667518702817929, -8.995218007635861213 ) ) ;
#36964=CARTESIAN_POINT ( 'NONE',  ( 116.0864081442453113, -9.988377603198976828, -10.36322818467138340 ) ) ;
#36965=CARTESIAN_POINT ( 'NONE',  ( 115.5191414775786569, -3.383040157471821630, -19.15922257007629170 ) ) ;
#36966=CARTESIAN_POINT ( 'NONE',  ( 115.0653281442453277, -3.505236298600246325, -18.68346056562440793 ) ) ;
#36967=CARTESIAN_POINT ( 'NONE',  ( 123.8579614775786126, -9.859900752359378018, -12.68260735090039759 ) ) ;
#36968=CARTESIAN_POINT ( 'NONE',  ( 113.9307948109119906, 0.9020085738987339008, -11.91225656197089222 ) ) ;
#36972=CARTESIAN_POINT ( 'NONE',  ( 124.1415948109119540, -3.505236298600246325, -18.68346056562440793 ) ) ;
#36973=CARTESIAN_POINT ( 'NONE',  ( 122.3647822310133364, -1.244021962887374544, -16.96476564598603076 ) ) ;
#36978=CARTESIAN_POINT ( 'NONE',  ( 123.5176014775786228, -9.261995988541697145, -16.69588392320189030 ) ) ;
#36980=CARTESIAN_POINT ( 'NONE',  ( 120.2274548109119934, 0.5811942927096110934, -14.16772938898807510 ) ) ;
#36981=DIRECTION ( 'NONE',  ( 1.000000000000000000, 0.000000000000000000, 0.000000000000000000 ) ) ;
#36983=CARTESIAN_POINT ( 'NONE',  ( 118.4122014775786340, 0.5811942927096110934, -14.16772938898807510 ) ) ;
#36984=CARTESIAN_POINT ( 'NONE',  ( 122.2128881442453263, -1.834011780172310813, -8.268836392978581529 ) ) ;
#36990=CARTESIAN_POINT ( 'NONE',  ( 114.5757164273310167, -2.236191541394345172, -18.14152338500401029 ) ) ;
#36991=CARTESIAN_POINT ( 'NONE',  ( 123.6310548109119765, -4.153390946401325223, -8.397313243818185668 ) ) ;
#36994=CARTESIAN_POINT ( 'NONE',  ( 117.3911214775786505, -7.894159318335828068, -9.358103419637847864 ) ) ;
#36997=CARTESIAN_POINT ( 'NONE',  ( 111.3780948109119890, -5.574606645277164318, -18.38911715685844683 ) ) ;
#36998=CARTESIAN_POINT ( 'NONE',  ( 122.8368814775786291, -1.561330072975668948, -17.79121239304076951 ) ) ;
#37000=EDGE_CURVE ( 'NONE', #37411, #2634, #1800, .T. ) ;
#37001=CARTESIAN_POINT ( 'NONE',  ( 123.1205148109119563, -7.643976991954077427, -18.09477374809248928 ) ) ;
#37002=CARTESIAN_POINT ( 'NONE',  ( 115.6325948109119821, 0.2603800115204892296, -16.42320221600525088 ) ) ;
#37003=CARTESIAN_POINT ( 'NONE',  ( 124.5954081442453116, -3.383040157471821630, -19.15922257007629170 ) ) ;
#37004=CARTESIAN_POINT ( 'NONE',  ( 123.0637881442452937, -8.899110576539710493, -16.42337572283490132 ) ) ;
#37009=CARTESIAN_POINT ( 'NONE',  ( 122.3263414775786373, -6.344957434206665248, -7.627207830600338134 ) ) ;
#37010=CARTESIAN_POINT ( 'NONE',  ( 113.9875214775786532, -8.899110576539710493, -16.42337572283490132 ) ) ;
#37012=CARTESIAN_POINT ( 'NONE',  ( 123.5176014775786228, -9.261995988541697145, -16.69588392320189030 ) ) ;
#37014=B_SPLINE_CURVE_WITH_KNOTS ( 'NONE', 3,
 ( #31821, #31374, #10424, #32269, #1036, #42103, #34781, #38435, #145, #35226 ),
 .UNSPECIFIED., .F., .F.,
 ( 4, 3, 3, 4 ),
 ( 0.000000000000000000, 0.0001671877548681249956, 0.0003343755096277680285, 0.0006463528481650609656 ),
 .UNSPECIFIED. ) ;
#37016=VERTEX_POINT ( 'NONE', #8661 ) ;
#37021=EDGE_CURVE ( 'NONE', #44717, #42698, #26742, .T. ) ;
#37022=CARTESIAN_POINT ( 'NONE',  ( 118.6391081442452986, -5.574606645277164318, -18.38911715685844683 ) ) ;
#37023=CARTESIAN_POINT ( 'NONE',  ( 115.1220548109119761, -1.833838273342658809, -17.42832698103878286 ) ) ;
#37026=EDGE_CURVE ( 'NONE', #43860, #40595, #43317, .T. ) ;
#37028=CARTESIAN_POINT ( 'NONE',  ( 115.5566632127138575, -2.191907684172563986, -18.20049396185734025 ) ) ;
#37029=CARTESIAN_POINT ( 'NONE',  ( 114.6115148109119986, -6.222761293078241884, -8.102969835052219238 ) ) ;
#37030=FACE_OUTER_BOUND ( 'NONE', #31294, .T. ) ;
#37034=CARTESIAN_POINT ( 'NONE',  ( 124.0281414775786146, -1.834011780172310813, -8.268836392978581529 ) ) ;
#37035=CARTESIAN_POINT ( 'NONE',  ( 122.9503348109119827, -9.859900752359378018, -12.68260735090039759 ) ) ;
#37036=ORIENTED_EDGE ( 'NONE', *, *, #39291, .T. ) ;
#37037=CARTESIAN_POINT ( 'NONE',  ( 135.3184548109119874, -10.36826876090623450, -11.00511718064541178 ) ) ;
#37038=CARTESIAN_POINT ( 'NONE',  ( 126.9733055311793066, 0.2194708681666166783, -15.14682149785671150 ) ) ;
#37040=CARTESIAN_POINT ( 'NONE',  ( 124.9924948109119924, -5.574606645277164318, -18.38911715685844683 ) ) ;
#37041=CARTESIAN_POINT ( 'NONE',  ( 118.4689281442453250, -10.15424416112533912, -14.75197769757731336 ) ) ;
#37046=CARTESIAN_POINT ( 'NONE',  ( 114.3846081442453197, 0.4262465694468514643, -12.03445270309931736 ) ) ;
#37050=CARTESIAN_POINT ( 'NONE',  ( 122.2696148109119889, -4.089484607189486809, -7.948022111789456723 ) ) ;
#37051=CARTESIAN_POINT ( 'NONE',  ( 121.8725281442453223, -3.383040157471821630, -19.15922257007629170 ) ) ;
#37052=CARTESIAN_POINT ( 'NONE',  ( 119.7285448082055836, -0.1020945015694968705, -15.74893487844867757 ) ) ;
#37053=CARTESIAN_POINT ( 'NONE',  ( 115.5191414775786569, -3.383040157471821630, -19.15922257007629170 ) ) ;
#37054=CARTESIAN_POINT ( 'NONE',  ( 113.9875214775786532, -0.4660016031367893996, -10.09054647747474043 ) ) ;
#37056=CARTESIAN_POINT ( 'NONE',  ( 113.1933481442453058, -5.574606645277164318, -18.38911715685844683 ) ) ;
#37057=CARTESIAN_POINT ( 'NONE',  ( 112.5693548109119888, 0.4262465694468514643, -12.03445270309931736 ) ) ;
#37058=CARTESIAN_POINT ( 'NONE',  ( 118.5823814775786360, -1.834011780172310813, -8.268836392978581529 ) ) ;
#37059=CARTESIAN_POINT ( 'NONE',  ( 125.1059481442452750, -1.833838273342660141, -17.42832698103878286 ) ) ;
#37060=CARTESIAN_POINT ( 'NONE',  ( 111.4915481442453142, -1.833838273342658365, -17.42832698103878286 ) ) ;
#37062=CARTESIAN_POINT ( 'NONE',  ( 116.7104014775786425, -8.899110576539710493, -16.42337572283490132 ) ) ;
#37063=CARTESIAN_POINT ( 'NONE',  ( 124.9357681442453014, -1.834011780172310813, -8.268836392978581529 ) ) ;
#37065=CARTESIAN_POINT ( 'NONE',  ( 121.2485348109119769, -8.899110576539710493, -16.42337572283490132 ) ) ;
#37067=CARTESIAN_POINT ( 'NONE',  ( 124.2951576481213607, -2.395992375830759524, -17.92872468182853396 ) ) ;
#37072=CARTESIAN_POINT ( 'NONE',  ( 124.7088614775786226, 0.2603800115204892296, -16.42320221600525088 ) ) ;
#37079=CARTESIAN_POINT ( 'NONE',  ( 137.0714388877963188, -6.662488778310335036, -18.49593449032493808 ) ) ;
#37081=CARTESIAN_POINT ( 'NONE',  ( 125.8433948109119456, -1.834011780172310813, -8.268836392978581529 ) ) ;
#37082=CARTESIAN_POINT ( 'NONE',  ( 118.6958348109119754, -3.505236298600246325, -18.68346056562440793 ) ) ;
#37083=LINE ( 'NONE', #20008, #37896 ) ;
#37085=CARTESIAN_POINT ( 'NONE',  ( 124.4252281442452812, -9.261995988541697145, -16.69588392320189030 ) ) ;
#37087=CARTESIAN_POINT ( 'NONE',  ( 116.1998614775786507, -10.63000616557722466, -14.87417383870573495 ) ) ;
#37089=CARTESIAN_POINT ( 'NONE',  ( 112.6260814775786514, -0.8288870151387760510, -10.36305467784173118 ) ) ;
#37090=CARTESIAN_POINT ( 'NONE',  ( 122.8936081442453059, -9.565557343593413364, -10.61323700422348004 ) ) ;
#37091=CARTESIAN_POINT ( 'NONE',  ( 124.6521348109119884, -1.561330072975668948, -17.79121239304076951 ) ) ;
#37095=CARTESIAN_POINT ( 'NONE',  ( 118.1285681442453068, -2.084020599724406786, -8.691656652584148546 ) ) ;
#37096=CARTESIAN_POINT ( 'NONE',  ( 116.5402214775786405, -9.565557343593413364, -10.61323700422348004 ) ) ;
#37101=DIRECTION ( 'NONE',  ( 0.000000000000000000, -0.6004852223388321697, 0.7996358532186280677 ) ) ;
#37102=CARTESIAN_POINT ( 'NONE',  ( 126.5808414775786446, -9.859900752359378018, -12.68260735090039759 ) ) ;
#37108=CARTESIAN_POINT ( 'NONE',  ( 111.4886568738142074, -1.282328013897791052, -16.91375541185598053 ) ) ;
#37110=CARTESIAN_POINT ( 'NONE',  ( 117.5613014775786525, 0.9020085738987339008, -11.91225656197089222 ) ) ;
#37112=CARTESIAN_POINT ( 'NONE',  ( 124.8223148109119762, -10.15424416112533912, -14.75197769757731336 ) ) ;
#37113=CARTESIAN_POINT ( 'NONE',  ( 114.1009748109119784, -5.574606645277164318, -18.38911715685844683 ) ) ;
#37116=CARTESIAN_POINT ( 'NONE',  ( 121.5321681442453183, -9.988377603198976828, -10.36322818467138340 ) ) ;
#37117=CARTESIAN_POINT ( 'NONE',  ( 112.9664414775786412, 0.5811942927096154232, -14.16772938898807155 ) ) ;
#37119=CARTESIAN_POINT ( 'NONE',  ( 124.9357681442453014, -1.834011780172310813, -8.268836392978581529 ) ) ;
#37122=CARTESIAN_POINT ( 'NONE',  ( 114.8951481442453115, -0.4660016031367893996, -10.09054647747474043 ) ) ;
#37123=CARTESIAN_POINT ( 'NONE',  ( 114.2144281442453178, -1.833838273342658809, -17.42832698103878286 ) ) ;
#37124=CARTESIAN_POINT ( 'NONE',  ( 126.6211808763464717, -4.842587725348250771, -18.59472652668980430 ) ) ;
#37125=CARTESIAN_POINT ( 'NONE',  ( 113.5904348109119866, -7.893985811506177619, -18.51759400769804742 ) ) ;
#37127=CARTESIAN_POINT ( 'NONE',  ( 123.4608748109119745, -10.63000616557722466, -14.87417383870573495 ) ) ;
#37130=CARTESIAN_POINT ( 'NONE',  ( 116.0113955643466852, -1.244021962887374544, -16.96476564598603076 ) ) ;
#37132=CARTESIAN_POINT ( 'NONE',  ( 115.0086014775786509, -5.574606645277164318, -18.38911715685844683 ) ) ;
#37133=CARTESIAN_POINT ( 'NONE',  ( 123.5140266804501152, -4.146825303465054624, -15.59726675418158948 ) ) ;
#37134=CARTESIAN_POINT ( 'NONE',  ( 115.0653281442453277, -3.505236298600246325, -18.68346056562440793 ) ) ;
#37139=CARTESIAN_POINT ( 'NONE',  ( 115.9729548109119861, -3.505236298600246325, -18.68346056562440793 ) ) ;
#37140=CARTESIAN_POINT ( 'NONE',  ( 117.1074881442453233, -10.63000616557722466, -14.87417383870573495 ) ) ;
#37142=CARTESIAN_POINT ( 'NONE',  ( 125.7866681442452688, -8.899110576539710493, -16.42337572283490132 ) ) ;
#37143=CARTESIAN_POINT ( 'NONE',  ( 115.1787814775786387, -0.1624402480850797581, -16.17319339645315424 ) ) ;
#37144=CARTESIAN_POINT ( 'NONE',  ( 123.0637881442452937, -0.4660016031367893996, -10.09054647747474043 ) ) ;
#37145=CARTESIAN_POINT ( 'NONE',  ( 123.2339681442453241, -6.344957434206665248, -7.627207830600338134 ) ) ;
#37151=CARTESIAN_POINT ( 'NONE',  ( 120.5110881442453206, -6.344957434206665248, -7.627207830600338134 ) ) ;
#37155=CARTESIAN_POINT ( 'NONE',  ( 112.7395348109119766, -4.153390946401321671, -8.397313243818183892 ) ) ;
#37157=CARTESIAN_POINT ( 'NONE',  ( 119.0361948109119652, -7.893985811506177619, -18.51759400769804742 ) ) ;
#37159=CARTESIAN_POINT ( 'NONE',  ( 119.2654641868944765, -2.239543233855044058, -18.13706010537467606 ) ) ;
#37162=CARTESIAN_POINT ( 'NONE',  ( 123.3474214775786209, -0.1624402480850797581, -16.17319339645315424 ) ) ;
#37163=CARTESIAN_POINT ( 'NONE',  ( 119.4332814775786318, -0.4660016031367893996, -10.09054647747474043 ) ) ;
#37166=CARTESIAN_POINT ( 'NONE',  ( 114.5547881442453217, -4.153390946401321671, -8.397313243818183892 ) ) ;
#37167=CARTESIAN_POINT ( 'NONE',  ( 116.8238548109119819, -4.089484607189486809, -7.948022111789456723 ) ) ;
#37168=CARTESIAN_POINT ( 'NONE',  ( 117.9382968734310992, -1.223627541775731631, -16.99192386690444323 ) ) ;
#37169=CARTESIAN_POINT ( 'NONE',  ( 126.2184548109090940, -8.862178061931365036, -16.39564131203211517 ) ) ;
#37170=CARTESIAN_POINT ( 'NONE',  ( 118.8092881442453290, -0.1624402480850797581, -16.17319339645315424 ) ) ;
#37172=CARTESIAN_POINT ( 'NONE',  ( 119.8870948109119752, -9.261995988541704250, -16.69588392320187964 ) ) ;
#37173=VECTOR ( 'NONE', #23629, 1000.000000000000000 ) ;
#37174=CARTESIAN_POINT ( 'NONE',  ( 114.9518748109119883, -1.834011780172310813, -8.268836392978581529 ) ) ;
#37175=CARTESIAN_POINT ( 'NONE',  ( 120.9081748109119872, -4.153390946401325223, -8.397313243818185668 ) ) ;
#37176=ORIENTED_EDGE ( 'NONE', *, *, #42558, .F. ) ;
#37179=CARTESIAN_POINT ( 'NONE',  ( 117.1074881442453233, -10.63000616557722466, -14.87417383870573495 ) ) ;
#37181=CARTESIAN_POINT ( 'NONE',  ( 115.8595014775786609, -7.643976991954077427, -18.09477374809248928 ) ) ;
#37182=ORIENTED_EDGE ( 'NONE', *, *, #3077, .T. ) ;
#37184=CARTESIAN_POINT ( 'NONE',  ( 125.3328548109119964, -0.8288870151387760510, -10.36305467784173118 ) ) ;
#37185=CARTESIAN_POINT ( 'NONE',  ( 120.4543614775786295, -5.574606645277164318, -18.38911715685844683 ) ) ;
#37188=CARTESIAN_POINT ( 'NONE',  ( 117.6747548109119919, -1.834011780172310813, -8.268836392978581529 ) ) ;
#37191=CARTESIAN_POINT ( 'NONE',  ( 121.3052614775786111, -1.834011780172310813, -8.268836392978581529 ) ) ;
#37192=CARTESIAN_POINT ( 'NONE',  ( 115.1787814775786387, -9.988377603198976828, -10.36322818467138340 ) ) ;
#37193=CARTESIAN_POINT ( 'NONE',  ( 120.1707281442453166, -9.565557343593413364, -10.61323700422348004 ) ) ;
#37195=CARTESIAN_POINT ( 'NONE',  ( 123.6877814775786533, -6.222761293078241884, -8.102969835052219238 ) ) ;
#37198=CARTESIAN_POINT ( 'NONE',  ( 122.3263414775786373, -3.505236298600246325, -18.68346056562440793 ) ) ;
#37199=CARTESIAN_POINT ( 'NONE',  ( 123.0637881442452937, -0.4660016031367911205, -10.09054647747473688 ) ) ;
#37205=CARTESIAN_POINT ( 'NONE',  ( 122.1561614775786353, -0.4660016031367893996, -10.09054647747474043 ) ) ;
#37206=CARTESIAN_POINT ( 'NONE',  ( 124.7088614775786226, -9.565557343593413364, -10.61323700422348004 ) ) ;
#37208=AXIS2_PLACEMENT_3D ( 'NONE', #14604, #28524, #42429 ) ;
#37209=CARTESIAN_POINT ( 'NONE',  ( 124.6521348109119884, -1.561330072975668948, -17.79121239304076951 ) ) ;
#37210=CARTESIAN_POINT ( 'NONE',  ( 113.4202548109119846, 0.1319031606808879209, -14.10382304977623669 ) ) ;
#37212=CARTESIAN_POINT ( 'NONE',  ( 119.4900081442453086, -1.834011780172310813, -8.268836392978581529 ) ) ;
#37213=CARTESIAN_POINT ( 'NONE',  ( 119.8870948109119752, -9.261995988541697145, -16.69588392320189030 ) ) ;
#37215=CARTESIAN_POINT ( 'NONE',  ( 123.9714148109119805, -8.899110576539710493, -16.42337572283490132 ) ) ;
#37221=CARTESIAN_POINT ( 'NONE',  ( 124.8790414775786246, -8.899110576539710493, -16.42337572283490132 ) ) ;
#37224=CARTESIAN_POINT ( 'NONE',  ( 118.3554748109119998, -9.565557343593413364, -10.61323700422348004 ) ) ;
#37226=CARTESIAN_POINT ( 'NONE',  ( 117.2776681442452968, -4.153390946401325223, -8.397313243818185668 ) ) ;
#37227=CARTESIAN_POINT ( 'NONE',  ( 122.6099748109119929, -9.261995988541697145, -16.69588392320189030 ) ) ;
#37229=CARTESIAN_POINT ( 'NONE',  ( 123.6877814775786533, -6.222761293078241884, -8.102969835052219238 ) ) ;
#37230=CARTESIAN_POINT ( 'NONE',  ( 117.2776681442452968, -5.638512984488999180, -18.83840828888717311 ) ) ;
#37232=CARTESIAN_POINT ( 'NONE',  ( 124.8790414775786246, -0.4660016031367893996, -10.09054647747474043 ) ) ;
#37233=CARTESIAN_POINT ( 'NONE',  ( 122.3263414775786373, -3.505236298600246325, -18.68346056562440793 ) ) ;
#37238=CARTESIAN_POINT ( 'NONE',  ( 124.4252281442452812, -9.261995988541697145, -16.69588392320189030 ) ) ;
#37239=CARTESIAN_POINT ( 'NONE',  ( 114.7249681442453237, -9.565557343593413364, -10.61323700422348004 ) ) ;
#37240=B_SPLINE_CURVE_WITH_KNOTS ( 'NONE', 3,
 ( #1985, #18871, #29810, #26617, #40531, #6084, #16592, #17266, #20686, #37545, #40757, #30939, #44862, #37315, #24107, #34563, #2892, #45075, #27073, #6776, #41218, #9513, #16358, #3122, #26844, #2434, #37773, #6546, #20004, #33657, #40995, #13171, #33889, #23430, #30259, #13617, #30714, #20462, #3346, #31155, #37079, #34344, #13835, #27750, #16821, #23201 ),
 .UNSPECIFIED., .F., .F.,
 ( 4, 2, 2, 2, 2, 2, 2, 2, 2, 2, 2, 2, 2, 2, 2, 2, 2, 2, 2, 2, 2, 2, 4 ),
 ( 0.000000000000000000, 0.06249999999998258338, 0.09374999999996579125, 0.1249999999999489853, 0.1874999999999005518, 0.2187499999998762656, 0.2343749999998641920, 0.2499999999998521183, 0.3124999999998443467, 0.3437499999998468447, 0.3749999999998493982, 0.4374999999998543943, 0.4687499999998612776, 0.4999999999998682165, 0.6249999999998880895, 0.6874999999998981925, 0.7187499999999032996, 0.7499999999999082956, 0.8124999999999186207, 0.8437499999999280575, 0.8593749999999329425, 0.8749999999999378275, 1.000000000000000000 ),
 .UNSPECIFIED. ) ;
#37241=CARTESIAN_POINT ( 'NONE',  ( 111.7751814775786556, -2.084020599724406786, -8.691656652584148546 ) ) ;
#37248=CARTESIAN_POINT ( 'NONE',  ( 121.1918081442452859, -10.15424416112533912, -14.75197769757731336 ) ) ;
#37249=CARTESIAN_POINT ( 'NONE',  ( 115.4624148109119943, -4.153390946401321671, -8.397313243818183892 ) ) ;
#37253=CARTESIAN_POINT ( 'NONE',  ( 121.0783548109119749, -9.565557343593413364, -10.61323700422348004 ) ) ;
#37254=CARTESIAN_POINT ( 'NONE',  ( 112.4559014775786778, -0.1624402480850797581, -16.17319339645315424 ) ) ;
#37258=CARTESIAN_POINT ( 'NONE',  ( 111.3319081442453182, -5.568102603702657305, -18.34339073538273013 ) ) ;
#37260=CARTESIAN_POINT ( 'NONE',  ( 123.0637881442452937, -0.4660016031367893996, -10.09054647747474043 ) ) ;
#37261=CARTESIAN_POINT ( 'NONE',  ( 112.5693548109119888, -10.63000616557722466, -14.87417383870573495 ) ) ;
#37265=CARTESIAN_POINT ( 'NONE',  ( 126.6390922358748270, 0.1291732976736364169, -14.88311683621468795 ) ) ;
#37269=CARTESIAN_POINT ( 'NONE',  ( 126.1270281442452870, 0.1319031606808879209, -14.10382304977623669 ) ) ;
#37270=CARTESIAN_POINT ( 'NONE',  ( 120.8514481442452961, -2.084020599724406786, -8.691656652584148546 ) ) ;
#37277=CARTESIAN_POINT ( 'NONE',  ( 114.3278814775786429, 0.1319031606808879209, -14.10382304977623669 ) ) ;
#37279=CARTESIAN_POINT ( 'NONE',  ( 117.5613014775786525, 0.9020085738987385637, -11.91225656197091887 ) ) ;
#37281=CARTESIAN_POINT ( 'NONE',  ( 124.0281414775786146, -1.834011780172310813, -8.268836392978581529 ) ) ;
#37282=CARTESIAN_POINT ( 'NONE',  ( 122.8368814775786291, -1.561330072975668948, -17.79121239304076951 ) ) ;
#37284=CARTESIAN_POINT ( 'NONE',  ( 115.9162281442453235, -4.089484607189486809, -7.948022111789456723 ) ) ;
#37285=CARTESIAN_POINT ( 'NONE',  ( 113.8173414775786512, 0.2603800115204892296, -16.42320221600525088 ) ) ;
#37287=CARTESIAN_POINT ( 'NONE',  ( 113.5337081442453240, -0.8288870151387760510, -10.36305467784173118 ) ) ;
#37288=CARTESIAN_POINT ( 'NONE',  ( 112.4559014775786778, -0.1624402480850797581, -16.17319339645315424 ) ) ;
#37289=CARTESIAN_POINT ( 'NONE',  ( 118.9794681442453026, -9.261995988541697145, -16.69588392320189030 ) ) ;
#37290=CARTESIAN_POINT ( 'NONE',  ( 115.1220548109119761, -8.166667518702817929, -8.995218007635861213 ) ) ;
#37292=CARTESIAN_POINT ( 'NONE',  ( 111.6050014775786536, 0.1319031606808879209, -14.10382304977623669 ) ) ;
#37295=CARTESIAN_POINT ( 'NONE',  ( 116.2565881442453133, -0.8288870151387760510, -10.36305467784173118 ) ) ;
#37296=CARTESIAN_POINT ( 'NONE',  ( 115.7460481442453357, -10.15424416112533912, -14.75197769757731336 ) ) ;
#37297=EDGE_CURVE ( 'NONE', #20751, #6914, #27843, .T. ) ;
#37303=CARTESIAN_POINT ( 'NONE',  ( 123.6310548109119765, -4.153390946401325223, -8.397313243818185668 ) ) ;
#37308=CARTESIAN_POINT ( 'NONE',  ( 122.1561614775786353, -0.4660016031367893996, -10.09054647747474043 ) ) ;
#37310=CARTESIAN_POINT ( 'NONE',  ( 111.7751814775786556, -7.893985811506177619, -18.51759400769804742 ) ) ;
#37315=CARTESIAN_POINT ( 'NONE',  ( 136.5048557854543674, -4.261492763881302714, -19.10789423623526417 ) ) ;
#37317=CARTESIAN_POINT ( 'NONE',  ( 126.2404814775786264, -9.261995988541697145, -16.69588392320189030 ) ) ;
#37318=CARTESIAN_POINT ( 'NONE',  ( 121.7590748109119687, -2.084020599724406786, -8.691656652584148546 ) ) ;
#37321=CARTESIAN_POINT ( 'NONE',  ( 122.4397948109119767, -9.988377603198976828, -10.36322818467138340 ) ) ;
#37322=CARTESIAN_POINT ( 'NONE',  ( 118.1852948109119836, -5.638512984488999180, -18.83840828888717311 ) ) ;
#37324=CARTESIAN_POINT ( 'NONE',  ( 113.7606148109119886, -7.894159318335828068, -9.358103419637847864 ) ) ;
#37325=CARTESIAN_POINT ( 'NONE',  ( 113.1933481442453058, -4.089484607189486809, -7.948022111789456723 ) ) ;
#37327=CARTESIAN_POINT ( 'NONE',  ( 123.0637881442452937, -0.4660016031367893996, -10.09054647747474043 ) ) ;
#37332=CARTESIAN_POINT ( 'NONE',  ( 116.5969481442453031, -9.859900752359374465, -12.68260735090039404 ) ) ;
#37333=CARTESIAN_POINT ( 'NONE',  ( 116.7671281442453335, -7.643976991954077427, -18.09477374809248928 ) ) ;
#37338=CARTESIAN_POINT ( 'NONE',  ( 114.2711548109119803, -9.988377603198976828, -10.36322818467138340 ) ) ;
#37342=VERTEX_POINT ( 'NONE', #14330 ) ;
#37343=CARTESIAN_POINT ( 'NONE',  ( 123.4286749921664352, -2.732273803890511665, -14.98280307987510085 ) ) ;
#37345=ORIENTED_EDGE ( 'NONE', *, *, #18214, .F. ) ;
#37347=CARTESIAN_POINT ( 'NONE',  ( 116.9940348109119839, -9.988377603198976828, -10.36322818467138340 ) ) ;
#37348=CARTESIAN_POINT ( 'NONE',  ( 125.1626748109119802, -0.1624402480850797581, -16.17319339645315424 ) ) ;
#37349=CARTESIAN_POINT ( 'NONE',  ( 117.6747548109119919, -7.643976991954077427, -18.09477374809248928 ) ) ;
#37352=CARTESIAN_POINT ( 'NONE',  ( 121.3052614775786111, -1.834011780172310813, -8.268836392978581529 ) ) ;
#37353=CARTESIAN_POINT ( 'NONE',  ( 115.5191414775786569, -3.383040157471821630, -19.15922257007629170 ) ) ;
#37356=CARTESIAN_POINT ( 'NONE',  ( 111.7184548109119788, -0.8288870151387760510, -10.36305467784173118 ) ) ;
#37360=CARTESIAN_POINT ( 'NONE',  ( 118.0718414775786300, -9.261995988541697145, -16.69588392320189030 ) ) ;
#37361=CARTESIAN_POINT ( 'NONE',  ( 113.7606148109119886, -7.894159318335828068, -9.358103419637847864 ) ) ;
#37362=CARTESIAN_POINT ( 'NONE',  ( 126.3975136127248362, -5.074220342508069415, -18.47877043462501234 ) ) ;
#37363=CARTESIAN_POINT ( 'NONE',  ( 112.7962614775786676, -3.383040157471821630, -19.15922257007629170 ) ) ;
#37366=CARTESIAN_POINT ( 'NONE',  ( 122.0427081442452817, 0.5811942927096110934, -14.16772938898807510 ) ) ;
#37368=CARTESIAN_POINT ( 'NONE',  ( 113.0798948109119948, -8.899110576539710493, -16.42337572283490132 ) ) ;
#37371=CARTESIAN_POINT ( 'NONE',  ( 116.9940348109119839, -0.1624402480850797581, -16.17319339645315424 ) ) ;
#37372=CARTESIAN_POINT ( 'NONE',  ( 137.3802547664384122, -3.523273223278070354, -8.431451416491041684 ) ) ;
#37373=CARTESIAN_POINT ( 'NONE',  ( 117.9583881442453048, 0.1319031606808879209, -14.10382304977623669 ) ) ;
#37377=CARTESIAN_POINT ( 'NONE',  ( 116.7104014775786425, -8.899110576539710493, -16.42337572283490132 ) ) ;
#37378=CARTESIAN_POINT ( 'NONE',  ( 117.3343948109119737, -3.383040157471821630, -19.15922257007629170 ) ) ;
#37380=CARTESIAN_POINT ( 'NONE',  ( 112.7962614775786676, -3.383040157471821630, -19.15922257007629170 ) ) ;
#37381=CARTESIAN_POINT ( 'NONE',  ( 116.1431348109119881, 0.1319031606808879209, -14.10382304977623669 ) ) ;
#37382=CARTESIAN_POINT ( 'NONE',  ( 121.5888948109119809, -10.30919188438810075, -12.61870101168855918 ) ) ;
#37383=CARTESIAN_POINT ( 'NONE',  ( 115.4056881442453459, -2.084020599724406786, -8.691656652584148546 ) ) ;
#37384=ORIENTED_EDGE ( 'NONE', *, *, #19307, .F. ) ;
#37385=CARTESIAN_POINT ( 'NONE',  ( 113.7606148109119886, -1.561330072975668060, -17.79121239304076596 ) ) ;
#37389=CARTESIAN_POINT ( 'NONE',  ( 127.9950210827190631, -4.139185286760726612, -15.60733003398113361 ) ) ;
#37390=CARTESIAN_POINT ( 'NONE',  ( 120.0005481442453146, -5.638512984488999180, -18.83840828888717311 ) ) ;
#37392=CARTESIAN_POINT ( 'NONE',  ( 126.0135748109119902, -8.166667518702819706, -8.995218007635861213 ) ) ;
#37393=CARTESIAN_POINT ( 'NONE',  ( 125.0492214775786266, -6.344957434206642155, -7.627207830600332805 ) ) ;
#37394=CARTESIAN_POINT ( 'NONE',  ( 115.9162281442453235, -5.574606645277164318, -18.38911715685844683 ) ) ;
#37395=CARTESIAN_POINT ( 'NONE',  ( 124.3685014775786186, 0.4262465694468523525, -12.03445270309933690 ) ) ;
#37397=CARTESIAN_POINT ( 'NONE',  ( 124.6521348109119884, -1.561330072975668948, -17.79121239304076951 ) ) ;
#37402=CARTESIAN_POINT ( 'NONE',  ( 112.5693548109119888, -10.63000616557722466, -14.87417383870573495 ) ) ;
#37403=CARTESIAN_POINT ( 'NONE',  ( 123.1772414775786189, -5.574606645277164318, -18.38911715685844683 ) ) ;
#37405=CARTESIAN_POINT ( 'NONE',  ( 119.4900081442453086, -1.834011780172310813, -8.268836392978581529 ) ) ;
#37406=CARTESIAN_POINT ( 'NONE',  ( 113.4769814775786330, 0.4262465694468514643, -12.03445270309931736 ) ) ;
#37407=CARTESIAN_POINT ( 'NONE',  ( 116.3700414775786527, -5.638512984488999180, -18.83840828888717311 ) ) ;
#37409=CARTESIAN_POINT ( 'NONE',  ( 127.0915067942438839, -1.262365849409121221, -9.320838424185609483 ) ) ;
#37410=CARTESIAN_POINT ( 'NONE',  ( 118.4689281442453250, -10.15424416112533912, -14.75197769757731336 ) ) ;
#37411=VERTEX_POINT ( 'NONE', #10912 ) ;
#37412=CARTESIAN_POINT ( 'NONE',  ( 119.3765548109119550, 0.9020085738987385637, -11.91225656197091887 ) ) ;
#37415=CARTESIAN_POINT ( 'NONE',  ( 115.0653281442453277, -6.344957434206662583, -7.627207830600332805 ) ) ;
#37416=CARTESIAN_POINT ( 'NONE',  ( 122.3263414775786373, -3.505236298600246325, -18.68346056562440793 ) ) ;
#37419=CARTESIAN_POINT ( 'NONE',  ( 137.4282737236158027, -0.5073614352806926631, -10.75960489339085768 ) ) ;
#37420=CARTESIAN_POINT ( 'NONE',  ( 119.5467348109119712, -4.089484607189486809, -7.948022111789456723 ) ) ;
#37422=CARTESIAN_POINT ( 'NONE',  ( 114.6682414775786469, -7.894159318335828068, -9.358103419637847864 ) ) ;
#37424=VERTEX_POINT ( 'NONE', #31872 ) ;
#37425=CARTESIAN_POINT ( 'NONE',  ( 125.7299414775786346, -10.15424416112533912, -14.75197769757731336 ) ) ;
#37426=CARTESIAN_POINT ( 'NONE',  ( 121.8725281442453223, -6.222761293078241884, -8.102969835052219238 ) ) ;
#37429=CARTESIAN_POINT ( 'NONE',  ( 123.7445081442452874, -1.561330072975668948, -17.79121239304076951 ) ) ;
#37430=CARTESIAN_POINT ( 'NONE',  ( 112.1721994132789320, -8.900630651041904429, -16.42135045828372597 ) ) ;
#37431=CARTESIAN_POINT ( 'NONE',  ( 118.1852948109119836, -5.638512984488999180, -18.83840828888717311 ) ) ;
#37432=CARTESIAN_POINT ( 'NONE',  ( 119.0361948109119652, -7.893985811506177619, -18.51759400769804742 ) ) ;
#37433=CARTESIAN_POINT ( 'NONE',  ( 120.3409081442453044, -8.899110576539710493, -16.42337572283490132 ) ) ;
#37435=CARTESIAN_POINT ( 'NONE',  ( 112.0378865278262737, -1.036737761566193239, -17.24079555149560505 ) ) ;
#37437=CARTESIAN_POINT ( 'NONE',  ( 122.8936081442453059, -9.565557343593413364, -10.61323700422348004 ) ) ;
#37443=CARTESIAN_POINT ( 'NONE',  ( 123.8579614775786126, 0.5811942927096110934, -14.16772938898807510 ) ) ;
#37444=CARTESIAN_POINT ( 'NONE',  ( 124.0848681442452772, -5.574606645277164318, -18.38911715685844683 ) ) ;
#37446=CARTESIAN_POINT ( 'NONE',  ( 124.5954081442453116, -3.383040157471821630, -19.15922257007629170 ) ) ;
#37447=CARTESIAN_POINT ( 'NONE',  ( 113.4769814775786330, 0.4262465694468514643, -12.03445270309931736 ) ) ;
#37449=CARTESIAN_POINT ( 'NONE',  ( 121.7023481442452777, -9.261995988541697145, -16.69588392320189030 ) ) ;
#37450=CARTESIAN_POINT ( 'NONE',  ( 121.0216281442452981, -1.561330072975668948, -17.79121239304076951 ) ) ;
#37452=CARTESIAN_POINT ( 'NONE',  ( 125.7866681442452688, -8.899110576539710493, -16.42337572283490132 ) ) ;
#37457=CARTESIAN_POINT ( 'NONE',  ( 124.6720798309150808, -2.215723800389698184, -18.16877924232191788 ) ) ;
#37458=CARTESIAN_POINT ( 'NONE',  ( 114.5024048144346693, -2.280480477428486363, -18.08254604495228435 ) ) ;
#37459=CARTESIAN_POINT ( 'NONE',  ( 123.9714148109119805, -8.899110576539710493, -16.42337572283490132 ) ) ;
#37462=CARTESIAN_POINT ( 'NONE',  ( 119.0361948109119652, -2.084020599724406786, -8.691656652584148546 ) ) ;
#37464=CARTESIAN_POINT ( 'NONE',  ( 117.7882081442453170, -3.505236298600246325, -18.68346056562440793 ) ) ;
#37465=CARTESIAN_POINT ( 'NONE',  ( 123.4041481442452834, -10.30919188438810075, -12.61870101168855918 ) ) ;
#37468=CARTESIAN_POINT ( 'NONE',  ( 123.0637881442452937, -8.899110576539710493, -16.42337572283490132 ) ) ;
#37469=CARTESIAN_POINT ( 'NONE',  ( 119.8303681442453126, -10.63000616557722466, -14.87417383870573495 ) ) ;
#37470=CARTESIAN_POINT ( 'NONE',  ( 124.9924948109119924, -4.089484607189486809, -7.948022111789456723 ) ) ;
#37472=CARTESIAN_POINT ( 'NONE',  ( 122.8936081442453059, -9.565557343593413364, -10.61323700422348004 ) ) ;
#37475=CARTESIAN_POINT ( 'NONE',  ( 124.3685014775786328, -10.63000616557722466, -14.87417383870573495 ) ) ;
#37476=CARTESIAN_POINT ( 'NONE',  ( 116.3700414775786527, -4.153390946401321671, -8.397313243818183892 ) ) ;
#37477=CARTESIAN_POINT ( 'NONE',  ( 123.4608748109119745, -10.63000616557722466, -14.87417383870573495 ) ) ;
#37479=FACE_OUTER_BOUND ( 'NONE', #31965, .T. ) ;
#37486=CARTESIAN_POINT ( 'NONE',  ( 122.5532481442453019, 0.4262465694468514643, -12.03445270309931736 ) ) ;
#37487=CARTESIAN_POINT ( 'NONE',  ( 113.2500748109119968, -3.505236298600246325, -18.68346056562440793 ) ) ;
#37488=CARTESIAN_POINT ( 'NONE',  ( 125.3328548109119964, -0.8288870151387812690, -10.36305467784172407 ) ) ;
#37491=CARTESIAN_POINT ( 'NONE',  ( 120.6812681442452941, 0.1319031606808879209, -14.10382304977623669 ) ) ;
#37497=CARTESIAN_POINT ( 'NONE',  ( 125.7866681442452688, -0.4660016031367893996, -10.09054647747474043 ) ) ;
#37498=CARTESIAN_POINT ( 'NONE',  ( 125.7299414775786346, -10.15424416112533912, -14.75197769757731336 ) ) ;
#37500=CARTESIAN_POINT ( 'NONE',  ( 113.5904348109119866, -7.893985811506177619, -18.51759400769804742 ) ) ;
#37503=CARTESIAN_POINT ( 'NONE',  ( 124.3117748109119844, 0.1319031606808879209, -14.10382304977623669 ) ) ;
#37504=CARTESIAN_POINT ( 'NONE',  ( 121.5888948109119809, 0.1319031606808879209, -14.10382304977623669 ) ) ;
#37508=CARTESIAN_POINT ( 'NONE',  ( 126.2184548109105435, -0.8658195297460520301, -10.39078908864422246 ) ) ;
#37509=CYLINDRICAL_SURFACE ( 'NONE', #9536, 1.999999999999998890 ) ;
#37513=CARTESIAN_POINT ( 'NONE',  ( 124.1983214775786166, -8.166667518702819706, -8.995218007635861213 ) ) ;
#37514=CARTESIAN_POINT ( 'NONE',  ( 122.9503348109119827, 0.5811942927096110934, -14.16772938898807510 ) ) ;
#37516=CARTESIAN_POINT ( 'NONE',  ( 119.4332814775786318, -0.4660016031367893996, -10.09054647747474043 ) ) ;
#37517=B_SPLINE_CURVE_WITH_KNOTS ( 'NONE', 3,
 ( #31378, #23666, #21123, #17271, #45081, #20468, #3127, #149, #27982, #24553, #34997, #30944, #17705, #31605, #4683, #25674, #39579, #24767, #817, #36139, #15409, #8122, #18387, #4008, #14509, #22243, #42333, #38890, #29313, #4466, #7659, #7891, #11545, #32275, #21797, #8342, #11094, #1487, #29085, #22023, #10872, #14736, #11316, #42997, #7427, #42554, #21348, #25226, #28648, #32715, #35232, #1270, #17930, #599, #28871, #25452 ),
 .UNSPECIFIED., .F., .F.,
 ( 4, 2, 2, 2, 2, 2, 2, 1, 2, 2, 2, 2, 2, 2, 2, 2, 2, 2, 2, 2, 2, 1, 2, 2, 2, 2, 2, 2, 4 ),
 ( 0.000000000000000000, 0.06250000000001540434, 0.09375000000001655620, 0.1093750000000236755, 0.1250000000000308087, 0.1875000000000596467, 0.2187500000000681954, 0.2343750000000779099, 0.2421875000000825451, 0.2500000000000871525, 0.3125000000001046940, 0.3437500000001088019, 0.3593750000001146860, 0.3750000000001205147, 0.5000000000001594280, 0.5625000000001791900, 0.5937500000001889600, 0.6093750000001936229, 0.6250000000001982858, 0.6875000000002169376, 0.7187500000002267075, 0.7343750000002317035, 0.7421875000002340350, 0.7500000000002362555, 0.8125000000001991740, 0.8437500000001806333, 0.8593750000001714184, 0.8750000000001620926, 1.000000000000000000 ),
 .UNSPECIFIED. ) ;
#37518=CARTESIAN_POINT ( 'NONE',  ( 111.9453614775786434, -1.561330072975668060, -17.79121239304076596 ) ) ;
#37520=CARTESIAN_POINT ( 'NONE',  ( 114.6682414775786469, -7.894159318335828068, -9.358103419637847864 ) ) ;
#37521=CARTESIAN_POINT ( 'NONE',  ( 124.6521348109119884, -1.561330072975668948, -17.79121239304076951 ) ) ;
#37522=CARTESIAN_POINT ( 'NONE',  ( 122.9503348109119827, 0.5811942927096110934, -14.16772938898807510 ) ) ;
#37523=CARTESIAN_POINT ( 'NONE',  ( 114.3846081442453197, -10.63000616557722466, -14.87417383870573495 ) ) ;
#37525=CARTESIAN_POINT ( 'NONE',  ( 114.3846081442453197, 0.4262465694468514643, -12.03445270309931736 ) ) ;
#37527=CARTESIAN_POINT ( 'NONE',  ( 117.7314814775786260, -5.574606645277164318, -18.38911715685844683 ) ) ;
#37531=CARTESIAN_POINT ( 'NONE',  ( 122.4397948109119767, -0.1624402480850797581, -16.17319339645315424 ) ) ;
#37537=CARTESIAN_POINT ( 'NONE',  ( 125.2194014775786286, -10.30919188438810075, -12.61870101168855918 ) ) ;
#37543=CARTESIAN_POINT ( 'NONE',  ( 123.1153024678160932, -1.149058757900107697, -17.09122335155391781 ) ) ;
#37544=CARTESIAN_POINT ( 'NONE',  ( 119.2063748109119814, -1.561330072975668504, -17.79121239304076951 ) ) ;
#37545=CARTESIAN_POINT ( 'NONE',  ( 136.3130839835673100, -4.208110519389379967, -19.18091293523846019 ) ) ;
#37550=CARTESIAN_POINT ( 'NONE',  ( 122.5532481442453019, 0.4262465694468514643, -12.03445270309931736 ) ) ;
#37555=CARTESIAN_POINT ( 'NONE',  ( 119.7736414775786358, -10.30919188438810075, -12.61870101168855918 ) ) ;
#37557=CARTESIAN_POINT ( 'NONE',  ( 115.7460481442453357, -10.15424416112533912, -14.75197769757731336 ) ) ;
#37561=CARTESIAN_POINT ( 'NONE',  ( 123.1772414775786189, -4.089484607189486809, -7.948022111789456723 ) ) ;
#37565=CARTESIAN_POINT ( 'NONE',  ( 115.6325948109119821, -9.565557343593413364, -10.61323700422348004 ) ) ;
#37566=CARTESIAN_POINT ( 'NONE',  ( 116.7104014775786425, -8.899110576539710493, -16.42337572283490132 ) ) ;
#37572=CARTESIAN_POINT ( 'NONE',  ( 114.4413348109119823, -9.261995988541697145, -16.69588392320189030 ) ) ;
#37573=CARTESIAN_POINT ( 'NONE',  ( 122.8568264975817499, -2.215723800389698184, -18.16877924232191788 ) ) ;
#37579=EDGE_LOOP ( 'NONE', ( #31241, #29174, #12611, #39754 ) ) ;
#37580=CARTESIAN_POINT ( 'NONE',  ( 118.0718414775786300, -9.261995988541697145, -16.69588392320189030 ) ) ;
#37581=CARTESIAN_POINT ( 'NONE',  ( 112.6260814775786514, -9.261995988541697145, -16.69588392320189030 ) ) ;
#37582=CARTESIAN_POINT ( 'NONE',  ( 116.7104014775786425, -8.899110576539710493, -16.42337572283490132 ) ) ;
#37585=CARTESIAN_POINT ( 'NONE',  ( 122.8936081442453059, 0.2603800115204892296, -16.42320221600525088 ) ) ;
#37586=CARTESIAN_POINT ( 'NONE',  ( 117.3911214775786505, -1.561330072975668504, -17.79121239304076951 ) ) ;
#37590=CARTESIAN_POINT ( 'NONE',  ( 114.4980614775786734, -2.084020599724406786, -8.691656652584148546 ) ) ;
#37593=CARTESIAN_POINT ( 'NONE',  ( 119.1496481442453046, -3.383040157471821630, -19.15922257007629170 ) ) ;
#37597=EDGE_CURVE ( 'NONE', #1633, #6756, #13743, .T. ) ;
#37598=CARTESIAN_POINT ( 'NONE',  ( 116.7671281442453335, -1.834011780172310813, -8.268836392978581529 ) ) ;
#37600=CARTESIAN_POINT ( 'NONE',  ( 120.5110881442453206, -6.344957434206665248, -7.627207830600338134 ) ) ;
#37602=CARTESIAN_POINT ( 'NONE',  ( 112.5126281442453120, 0.1319031606808879209, -14.10382304977623669 ) ) ;
#37604=CARTESIAN_POINT ( 'NONE',  ( 114.6682414775786469, -7.894159318335828068, -9.358103419637847864 ) ) ;
#37606=CARTESIAN_POINT ( 'NONE',  ( 119.0361948109119652, -2.084020599724406786, -8.691656652584148546 ) ) ;
#37607=DIRECTION ( 'NONE',  ( -1.000000000000000000, 0.000000000000000000, 0.000000000000000000 ) ) ;
#37608=CARTESIAN_POINT ( 'NONE',  ( 113.9875214775786532, -8.899110576539710493, -16.42337572283490132 ) ) ;
#37609=CARTESIAN_POINT ( 'NONE',  ( 113.9875214775786532, -0.4660016031367893996, -10.09054647747474043 ) ) ;
#37611=CARTESIAN_POINT ( 'NONE',  ( 112.3424481442453384, -6.344957434206662583, -7.627207830600332805 ) ) ;
#37612=CARTESIAN_POINT ( 'NONE',  ( 116.7104014775786425, -8.899110576539710493, -16.42337572283490132 ) ) ;
#37613=CARTESIAN_POINT ( 'NONE',  ( 113.3068014775786594, -1.833838273342658809, -17.42832698103878286 ) ) ;
#37615=CARTESIAN_POINT ( 'NONE',  ( 118.1285681442453068, -2.084020599724406786, -8.691656652584148546 ) ) ;
#37623=CARTESIAN_POINT ( 'NONE',  ( 118.5823814775786360, -1.834011780172310813, -8.268836392978581529 ) ) ;
#37625=CARTESIAN_POINT ( 'NONE',  ( 125.9568481442452850, -6.344957434206665248, -7.627207830600338134 ) ) ;
#37627=CARTESIAN_POINT ( 'NONE',  ( 116.2565881442453133, -0.8288870151387760510, -10.36305467784173118 ) ) ;
#37630=CARTESIAN_POINT ( 'NONE',  ( 124.3685014775786328, -10.63000616557722466, -14.87417383870573495 ) ) ;
#37634=CARTESIAN_POINT ( 'NONE',  ( 111.8779471478583929, -3.807985514183284348, -19.09877912889400875 ) ) ;
#37635=CARTESIAN_POINT ( 'NONE',  ( 122.9503348109119827, -9.859900752359378018, -12.68260735090039759 ) ) ;
#37636=CARTESIAN_POINT ( 'NONE',  ( 121.3052614775786111, -1.834011780172310813, -8.268836392978581529 ) ) ;
#37637=CARTESIAN_POINT ( 'NONE',  ( 114.2711548109119803, -0.1624402480850797581, -16.17319339645315424 ) ) ;
#37638=CARTESIAN_POINT ( 'NONE',  ( 118.5256548109119876, -0.4660016031367893996, -10.09054647747474043 ) ) ;
#37639=CARTESIAN_POINT ( 'NONE',  ( 123.3590514748722455, -0.1020945015695005759, -15.74893487844868112 ) ) ;
#37640=CARTESIAN_POINT ( 'NONE',  ( 126.5041214912225627, -1.164387443341326378, -9.820872858089868984 ) ) ;
#37641=CARTESIAN_POINT ( 'NONE',  ( 124.7655881442452852, -9.859900752359378018, -12.68260735090039759 ) ) ;
#37645=CARTESIAN_POINT ( 'NONE',  ( 117.8449348109119938, -8.166667518702817929, -8.995218007635861213 ) ) ;
#37646=CARTESIAN_POINT ( 'NONE',  ( 121.6456214775786293, 0.4262465694468514643, -12.03445270309931736 ) ) ;
#37650=CARTESIAN_POINT ( 'NONE',  ( 116.9373081442452929, -8.166667518702817929, -8.995218007635861213 ) ) ;
#37652=CARTESIAN_POINT ( 'NONE',  ( 115.9729548109119861, -3.505236298600246325, -18.68346056562440793 ) ) ;
#37654=ORIENTED_EDGE ( 'NONE', *, *, #1684, .F. ) ;
#37656=CARTESIAN_POINT ( 'NONE',  ( 126.0703014775786102, -0.1624402480850797581, -16.17319339645315424 ) ) ;
#37662=CARTESIAN_POINT ( 'NONE',  ( 121.4754414775786131, -8.166667518702819706, -8.995218007635861213 ) ) ;
#37663=DIRECTION ( 'NONE',  ( 0.000000000000000000, -0.6004852223388322807, 0.7996358532186280677 ) ) ;
#37665=CARTESIAN_POINT ( 'NONE',  ( 120.2841814775786276, 0.9020085738987339008, -11.91225656197089222 ) ) ;
#37666=CARTESIAN_POINT ( 'NONE',  ( 120.6812681442452941, -10.30919188438810075, -12.61870101168855918 ) ) ;
#37667=CARTESIAN_POINT ( 'NONE',  ( 119.1496481442453046, -6.222761293078241884, -8.102969835052219238 ) ) ;
#37668=CARTESIAN_POINT ( 'NONE',  ( 124.5954081442453116, -6.222761293078241884, -8.102969835052219238 ) ) ;
#37669=CARTESIAN_POINT ( 'NONE',  ( 113.3635281442453504, -9.988377603198976828, -10.36322818467138340 ) ) ;
#37671=CARTESIAN_POINT ( 'NONE',  ( 123.4041481442452834, 0.1319031606808879209, -14.10382304977623669 ) ) ;
#37672=CARTESIAN_POINT ( 'NONE',  ( 125.3790414775786388, -0.8658195297466895202, -10.39078908864337514 ) ) ;
#37677=CARTESIAN_POINT ( 'NONE',  ( 124.0281414775786146, -1.834011780172310813, -8.268836392978581529 ) ) ;
#37678=CARTESIAN_POINT ( 'NONE',  ( 123.4041481442452834, 0.1319031606808879209, -14.10382304977623669 ) ) ;
#37680=CARTESIAN_POINT ( 'NONE',  ( 125.8433948109119456, -1.834011780172310813, -8.268836392978581529 ) ) ;
#37684=CARTESIAN_POINT ( 'NONE',  ( 124.7088614775786226, 0.2603800115204892296, -16.42320221600525088 ) ) ;
#37685=CARTESIAN_POINT ( 'NONE',  ( 120.6245414775786458, -9.988377603198976828, -10.36322818467138340 ) ) ;
#37687=CARTESIAN_POINT ( 'NONE',  ( 113.1933481442453058, -4.089484607189486809, -7.948022111789456723 ) ) ;
#37691=CARTESIAN_POINT ( 'NONE',  ( 124.8677593335883955, -2.334846009198413341, -18.01015021110790215 ) ) ;
#37692=CARTESIAN_POINT ( 'NONE',  ( 112.7962614775786676, -6.222761293078241884, -8.102969835052219238 ) ) ;
#37693=CARTESIAN_POINT ( 'NONE',  ( 125.5597614775786326, -7.894159318335828068, -9.358103419637847864 ) ) ;
#37696=CARTESIAN_POINT ( 'NONE',  ( 122.8936081442453059, -9.565557343593413364, -10.61323700422348004 ) ) ;
#37698=CARTESIAN_POINT ( 'NONE',  ( 115.2922348109119781, 0.4262465694468514643, -12.03445270309931736 ) ) ;
#37699=CARTESIAN_POINT ( 'NONE',  ( 121.9292548109119849, -1.561330072975668948, -17.79121239304076951 ) ) ;
#37702=CARTESIAN_POINT ( 'NONE',  ( 121.7023481442452777, -0.8288870151387760510, -10.36305467784173118 ) ) ;
#37703=CARTESIAN_POINT ( 'NONE',  ( 118.9227414775786400, -10.63000616557722466, -14.87417383870573495 ) ) ;
#37704=CARTESIAN_POINT ( 'NONE',  ( 124.2550481442452792, -9.988377603198980381, -10.36322818467138518 ) ) ;
#37707=CARTESIAN_POINT ( 'NONE',  ( 123.3482543740715442, -2.419733177069661512, -17.89711025544711376 ) ) ;
#37708=CARTESIAN_POINT ( 'NONE',  ( 122.8368814775786291, -1.561330072975668948, -17.79121239304076951 ) ) ;
#37709=CARTESIAN_POINT ( 'NONE',  ( 116.5402214775786405, -9.565557343593413364, -10.61323700422348004 ) ) ;
#37710=AXIS2_PLACEMENT_3D ( 'NONE', #18096, #24281, #38167 ) ;
#37711=CARTESIAN_POINT ( 'NONE',  ( 115.1220548109119761, -1.833838273342658809, -17.42832698103878286 ) ) ;
#37718=CARTESIAN_POINT ( 'NONE',  ( 117.9024943740715656, -2.419733177069680607, -17.89711025544712442 ) ) ;
#37719=CARTESIAN_POINT ( 'NONE',  ( 122.9503348109119827, -9.859900752359378018, -12.68260735090039759 ) ) ;
#37720=CARTESIAN_POINT ( 'NONE',  ( 112.7395348109119766, -4.153390946401321671, -8.397313243818183892 ) ) ;
#37721=CARTESIAN_POINT ( 'NONE',  ( 126.9276200068485991, -0.06140791722303787920, -11.02529072918189534 ) ) ;
#37722=ORIENTED_EDGE ( 'NONE', *, *, #5477, .T. ) ;
#37724=CARTESIAN_POINT ( 'NONE',  ( 113.1933481442453058, -5.574606645277164318, -18.38911715685844683 ) ) ;
#37726=CARTESIAN_POINT ( 'NONE',  ( 111.8424481442453242, -6.210324830718715994, -8.151390318758327425 ) ) ;
#37730=CARTESIAN_POINT ( 'NONE',  ( 124.8223148109119762, -10.15424416112533912, -14.75197769757731336 ) ) ;
#37732=CARTESIAN_POINT ( 'NONE',  ( 113.0798948109119948, -0.4660016031367893996, -10.09054647747474043 ) ) ;
#37733=CARTESIAN_POINT ( 'NONE',  ( 127.0066334553003315, 0.2291786611533031814, -15.16966009980168906 ) ) ;
#37735=CARTESIAN_POINT ( 'NONE',  ( 124.4819548109119722, -2.084020599724406786, -8.691656652584148546 ) ) ;
#37736=CARTESIAN_POINT ( 'NONE',  ( 122.7234281442452755, -4.153390946401325223, -8.397313243818185668 ) ) ;
#37741=CARTESIAN_POINT ( 'NONE',  ( 113.7038881442453402, -6.222761293078241884, -8.102969835052219238 ) ) ;
#37746=CARTESIAN_POINT ( 'NONE',  ( 123.2339681442453241, -6.344957434206665248, -7.627207830600338134 ) ) ;
#37747=CARTESIAN_POINT ( 'NONE',  ( 124.8790414775786246, -0.4660016031367893996, -10.09054647747474043 ) ) ;
#37749=CARTESIAN_POINT ( 'NONE',  ( 120.0572748109119772, -3.383040157471821630, -19.15922257007629170 ) ) ;
#37750=CARTESIAN_POINT ( 'NONE',  ( 111.7184548109119788, -9.261995988541697145, -16.69588392320189030 ) ) ;
#37752=CARTESIAN_POINT ( 'NONE',  ( 113.3068014775786594, -1.833838273342658809, -17.42832698103878286 ) ) ;
#37753=CARTESIAN_POINT ( 'NONE',  ( 125.3328548109119964, -9.261995988541697145, -16.69588392320189030 ) ) ;
#37754=CARTESIAN_POINT ( 'NONE',  ( 123.5176014775786228, -9.261995988541697145, -16.69588392320189030 ) ) ;
#37755=CARTESIAN_POINT ( 'NONE',  ( 114.8951481442453115, -0.4660016031367893996, -10.09054647747474043 ) ) ;
#37756=CARTESIAN_POINT ( 'NONE',  ( 112.7395348109119766, -4.153390946401321671, -8.397313243818183892 ) ) ;
#37758=CARTESIAN_POINT ( 'NONE',  ( 118.6958348109119754, -3.505236298600246325, -18.68346056562440793 ) ) ;
#37761=CARTESIAN_POINT ( 'NONE',  ( 124.4252281442452812, -0.8288870151387760510, -10.36305467784173118 ) ) ;
#37766=CARTESIAN_POINT ( 'NONE',  ( 125.3328548109119964, -9.261995988541697145, -16.69588392320189030 ) ) ;
#37771=CARTESIAN_POINT ( 'NONE',  ( 115.2154168734311241, -1.223627541775731631, -16.99192386690444323 ) ) ;
#37772=CARTESIAN_POINT ( 'NONE',  ( 116.5969481442453031, 0.5811942927096154232, -14.16772938898807155 ) ) ;
#37773=CARTESIAN_POINT ( 'NONE',  ( 137.3803399967318910, -4.959070169535716666, -18.53201221635876905 ) ) ;
#37775=CARTESIAN_POINT ( 'NONE',  ( 124.7088614775786226, 0.2603800115204892296, -16.42320221600525088 ) ) ;
#37776=CARTESIAN_POINT ( 'NONE',  ( 119.4900081442453086, -7.643976991954077427, -18.09477374809248928 ) ) ;
#37779=CARTESIAN_POINT ( 'NONE',  ( 118.9227414775786400, -10.63000616557722466, -14.87417383870573495 ) ) ;
#37781=CARTESIAN_POINT ( 'NONE',  ( 116.1998614775786507, 0.4262465694468514643, -12.03445270309931736 ) ) ;
#37782=CARTESIAN_POINT ( 'NONE',  ( 111.7184548109119788, -0.8288870151387760510, -10.36305467784173118 ) ) ;
#37786=CARTESIAN_POINT ( 'NONE',  ( 118.0151148109119816, 0.4262465694468514643, -12.03445270309931736 ) ) ;
#37787=CARTESIAN_POINT ( 'NONE',  ( 118.6391081442452986, -5.574606645277164318, -18.38911715685844683 ) ) ;
#37793=CARTESIAN_POINT ( 'NONE',  ( 114.2144281442453178, -8.166667518702817929, -8.995218007635859436 ) ) ;
#37794=DIRECTION ( 'NONE',  ( -1.000000000000000000, 0.000000000000000000, 0.000000000000000000 ) ) ;
#37797=DIRECTION ( 'NONE',  ( -1.000000000000000000, 0.000000000000000000, 0.000000000000000000 ) ) ;
#37799=CARTESIAN_POINT ( 'NONE',  ( 121.8725281442453223, -3.383040157471821630, -19.15922257007629170 ) ) ;
#37800=CARTESIAN_POINT ( 'NONE',  ( 112.2857214775786474, -4.089484607189486809, -7.948022111789456723 ) ) ;
#37801=CARTESIAN_POINT ( 'NONE',  ( 117.4478481442453131, -9.565557343593413364, -10.61323700422348004 ) ) ;
#37805=CARTESIAN_POINT ( 'NONE',  ( 121.0783548109119749, 0.2603800115204892296, -16.42320221600525088 ) ) ;
#37806=CARTESIAN_POINT ( 'NONE',  ( 119.7736414775786358, -10.30919188438810075, -12.61870101168855918 ) ) ;
#37808=CARTESIAN_POINT ( 'NONE',  ( 113.5904348109119866, -2.084020599724406786, -8.691656652584148546 ) ) ;
#37811=CARTESIAN_POINT ( 'NONE',  ( 118.1852948109119836, -5.638512984488999180, -18.83840828888717311 ) ) ;
#37814=CARTESIAN_POINT ( 'NONE',  ( 117.2776681442452968, -5.638512984488999180, -18.83840828888717311 ) ) ;
#37815=ORIENTED_EDGE ( 'NONE', *, *, #18587, .T. ) ;
#37816=CARTESIAN_POINT ( 'NONE',  ( 124.1983214775786166, -8.166667518702819706, -8.995218007635861213 ) ) ;
#37817=LINE ( 'NONE', #30532, #33973 ) ;
#37818=CARTESIAN_POINT ( 'NONE',  ( 113.8740681442453138, -9.859900752359374465, -12.68260735090039404 ) ) ;
#37820=CARTESIAN_POINT ( 'NONE',  ( 115.2355081442453155, 0.1319031606808879209, -14.10382304977623669 ) ) ;
#37822=CARTESIAN_POINT ( 'NONE',  ( 119.1496481442453046, -6.222761293078241884, -8.102969835052219238 ) ) ;
#37825=CARTESIAN_POINT ( 'NONE',  ( 115.3489614775786407, -0.8288870151387760510, -10.36305467784173118 ) ) ;
#37826=CARTESIAN_POINT ( 'NONE',  ( 114.1577014775786552, -6.344957434206662583, -7.627207830600332805 ) ) ;
#37829=CARTESIAN_POINT ( 'NONE',  ( 114.1009748109119784, -4.089484607189486809, -7.948022111789456723 ) ) ;
#37830=CARTESIAN_POINT ( 'NONE',  ( 113.1366214775786432, -7.643976991954077427, -18.09477374809248928 ) ) ;
#37831=CARTESIAN_POINT ( 'NONE',  ( 118.4689281442453392, -10.15424416112533912, -14.75197769757731336 ) ) ;
#37833=CARTESIAN_POINT ( 'NONE',  ( 114.8384214775786489, 0.9020085738987339008, -11.91225656197089222 ) ) ;
#37839=CARTESIAN_POINT ( 'NONE',  ( 123.0070614775786169, 0.9020085738987339008, -11.91225656197089222 ) ) ;
#37842=CARTESIAN_POINT ( 'NONE',  ( 135.3184548109119874, -7.252096815532139473, -18.89748516540533529 ) ) ;
#37843=CARTESIAN_POINT ( 'NONE',  ( 119.7169148109119874, -0.1624402480850797581, -16.17319339645315424 ) ) ;
#37846=CARTESIAN_POINT ( 'NONE',  ( 122.6099748109119929, -9.261995988541697145, -16.69588392320189030 ) ) ;
#37852=CARTESIAN_POINT ( 'NONE',  ( 126.1270281442452870, 0.1319031606808879209, -14.10382304977623669 ) ) ;
#37853=CARTESIAN_POINT ( 'NONE',  ( 122.3830681442452857, -8.166667518702819706, -8.995218007635861213 ) ) ;
#37854=CARTESIAN_POINT ( 'NONE',  ( 116.0864081442453113, -0.1624402480850797581, -16.17319339645315424 ) ) ;
#37856=CARTESIAN_POINT ( 'NONE',  ( 119.7736414775786358, -10.30919188438810075, -12.61870101168855918 ) ) ;
#37858=CARTESIAN_POINT ( 'NONE',  ( 126.3243314201119603, -1.068588705931508676, -10.05747113621685429 ) ) ;
#37859=CARTESIAN_POINT ( 'NONE',  ( 122.2696148109119889, -5.574606645277164318, -18.38911715685844683 ) ) ;
#37863=CARTESIAN_POINT ( 'NONE',  ( 116.9940348109119839, -9.988377603198976828, -10.36322818467138340 ) ) ;
#37864=CARTESIAN_POINT ( 'NONE',  ( 124.5954081442453116, -6.222761293078241884, -8.102969835052219238 ) ) ;
#37868=CARTESIAN_POINT ( 'NONE',  ( 136.3514896075954539, -1.238236687199658181, -8.849319055121297239 ) ) ;
#37870=EDGE_CURVE ( 'NONE', #38570, #41059, #17498, .T. ) ;
#37871=CARTESIAN_POINT ( 'NONE',  ( 122.9503348109119827, 0.5811942927096110934, -14.16772938898807510 ) ) ;
#37873=CARTESIAN_POINT ( 'NONE',  ( 120.3409081442453044, -8.899110576539710493, -16.42337572283490132 ) ) ;
#37877=CARTESIAN_POINT ( 'NONE',  ( 124.8790414775786246, -8.899110576539710493, -16.42337572283490132 ) ) ;
#37882=CARTESIAN_POINT ( 'NONE',  ( 121.2485348109119769, -0.4660016031367893996, -10.09054647747474043 ) ) ;
#37883=FACE_OUTER_BOUND ( 'NONE', #7554, .T. ) ;
#37884=CARTESIAN_POINT ( 'NONE',  ( 138.2184548109119930, -3.719473736431747390, -16.16631137400202078 ) ) ;
#37885=CARTESIAN_POINT ( 'NONE',  ( 118.1285681442453068, -7.893985811506177619, -18.51759400769804742 ) ) ;
#37886=CARTESIAN_POINT ( 'NONE',  ( 117.9016614775786280, -9.988377603198976828, -10.36322818467138340 ) ) ;
#37887=CARTESIAN_POINT ( 'NONE',  ( 119.5467348109119712, -5.574606645277164318, -18.38911715685844683 ) ) ;
#37888=CARTESIAN_POINT ( 'NONE',  ( 123.2906948109119867, -1.833838273342659697, -17.42832698103878286 ) ) ;
#37889=CARTESIAN_POINT ( 'NONE',  ( 116.0864081442453113, -9.988377603198976828, -10.36322818467138340 ) ) ;
#37891=CARTESIAN_POINT ( 'NONE',  ( 125.8433948109119456, -7.643976991954077427, -18.09477374809248928 ) ) ;
#37892=CARTESIAN_POINT ( 'NONE',  ( 125.0954081442453401, -3.517672760958747702, -18.63504008191803152 ) ) ;
#37896=VECTOR ( 'NONE', #5858, 1000.000000000000000 ) ;
#37897=CARTESIAN_POINT ( 'NONE',  ( 120.5678148109119832, -8.166667518702819706, -8.995218007635861213 ) ) ;
#37898=CARTESIAN_POINT ( 'NONE',  ( 123.9146881442452894, -10.15424416112533912, -14.75197769757731336 ) ) ;
#37900=CARTESIAN_POINT ( 'NONE',  ( 124.3685014775786328, -10.63000616557722466, -14.87417383870573495 ) ) ;
#37903=CARTESIAN_POINT ( 'NONE',  ( 124.4819548109119722, -7.893985811506177619, -18.51759400769804742 ) ) ;
#37904=CARTESIAN_POINT ( 'NONE',  ( 119.4900081442453086, -1.834011780172310813, -8.268836392978581529 ) ) ;
#37906=CARTESIAN_POINT ( 'NONE',  ( 113.4202548109119846, -10.30919188438810075, -12.61870101168855918 ) ) ;
#37909=ORIENTED_EDGE ( 'NONE', *, *, #23332, .F. ) ;
#37910=CARTESIAN_POINT ( 'NONE',  ( 125.0125860817262122, -2.423081321603731908, -17.89265170041263175 ) ) ;
#37912=CARTESIAN_POINT ( 'NONE',  ( 114.3505409221557443, -2.372251574601226043, -17.96033910819752322 ) ) ;
#37913=CARTESIAN_POINT ( 'NONE',  ( 112.0020881442453344, 0.2603800115204892296, -16.42320221600525088 ) ) ;
#37917=CARTESIAN_POINT ( 'NONE',  ( 120.0572748109119772, -6.222761293078241884, -8.102969835052219238 ) ) ;
#37919=CARTESIAN_POINT ( 'NONE',  ( 115.9729548109119861, -3.505236298600246325, -18.68346056562440793 ) ) ;
#37920=CARTESIAN_POINT ( 'NONE',  ( 113.0231681442453180, -10.15424416112533912, -14.75197769757731336 ) ) ;
#37924=CARTESIAN_POINT ( 'NONE',  ( 119.4900081442453086, -1.834011780172310813, -8.268836392978581529 ) ) ;
#37926=EDGE_LOOP ( 'NONE', ( #32616, #17637, #21594, #15552 ) ) ;
#37927=CARTESIAN_POINT ( 'NONE',  ( 126.2597653975841325, -9.021097607470126789, -16.20867439364996088 ) ) ;
#37928=EDGE_CURVE ( 'NONE', #21122, #35115, #35316, .T. ) ;
#37932=CARTESIAN_POINT ( 'NONE',  ( 113.2500748109119968, -3.505236298600246325, -18.68346056562440793 ) ) ;
#37933=CARTESIAN_POINT ( 'NONE',  ( 115.3489614775786407, -0.8288870151387760510, -10.36305467784173118 ) ) ;
#37943=AXIS2_PLACEMENT_3D ( 'NONE', #40082, #5637, #2214 ) ;
#37944=CARTESIAN_POINT ( 'NONE',  ( 124.7088614775786226, -9.565557343593413364, -10.61323700422348004 ) ) ;
#37945=CARTESIAN_POINT ( 'NONE',  ( 113.0798948109119948, -8.899110576539710493, -16.42337572283490132 ) ) ;
#37946=CARTESIAN_POINT ( 'NONE',  ( 120.0549121015961163, -1.040089454026960292, -17.23633227186633476 ) ) ;
#37949=CARTESIAN_POINT ( 'NONE',  ( 112.3424481442453384, -3.505236298600246325, -18.68346056562440793 ) ) ;
#37951=FACE_OUTER_BOUND ( 'NONE', #41979, .T. ) ;
#37954=CARTESIAN_POINT ( 'NONE',  ( 124.9924948109119924, -5.574606645277164318, -18.38911715685844683 ) ) ;
#37956=CARTESIAN_POINT ( 'NONE',  ( 113.6471614775786492, -5.638512984488999180, -18.83840828888717311 ) ) ;
#37957=CARTESIAN_POINT ( 'NONE',  ( 126.5621572004088051, 0.1111755995133630603, -14.80766266791229135 ) ) ;
#37959=CARTESIAN_POINT ( 'NONE',  ( 126.2404814775786264, -0.8288870151387760510, -10.36305467784173118 ) ) ;
#37960=CARTESIAN_POINT ( 'NONE',  ( 124.4819548109119722, -2.084020599724406786, -8.691656652584148546 ) ) ;
#37966=CARTESIAN_POINT ( 'NONE',  ( 114.1577014775786552, -3.505236298600246325, -18.68346056562440793 ) ) ;
#37970=CARTESIAN_POINT ( 'NONE',  ( 123.6310548109119765, -5.638512984488999180, -18.83840828888717311 ) ) ;
#37971=CARTESIAN_POINT ( 'NONE',  ( 112.2289948109119848, -7.643976991954077427, -18.09477374809248928 ) ) ;
#37973=CARTESIAN_POINT ( 'NONE',  ( 120.7947214775786193, -9.261995988541697145, -16.69588392320189030 ) ) ;
#37974=CARTESIAN_POINT ( 'NONE',  ( 117.6747548109119919, -1.834011780172310813, -8.268836392978581529 ) ) ;
#37977=CARTESIAN_POINT ( 'NONE',  ( 111.7751814775786556, -2.084020599724406786, -8.691656652584148546 ) ) ;
#37979=CARTESIAN_POINT ( 'NONE',  ( 123.5743281442453139, -7.893985811506177619, -18.51759400769804742 ) ) ;
#37980=CARTESIAN_POINT ( 'NONE',  ( 114.0442481442453300, -1.834011780172310813, -8.268836392978581529 ) ) ;
#37981=CARTESIAN_POINT ( 'NONE',  ( 116.9373081442452929, -1.833838273342659253, -17.42832698103878286 ) ) ;
#37983=CARTESIAN_POINT ( 'NONE',  ( 119.0361948109119652, -2.084020599724406786, -8.691656652584148546 ) ) ;
#37984=CARTESIAN_POINT ( 'NONE',  ( 117.6180281442453150, -0.4660016031367893996, -10.09054647747474043 ) ) ;
#37986=CARTESIAN_POINT ( 'NONE',  ( 123.5176014775786228, -0.8288870151387760510, -10.36305467784173118 ) ) ;
#37991=CARTESIAN_POINT ( 'NONE',  ( 125.7866681442452688, -0.4660016031367893996, -10.09054647747474043 ) ) ;
#37994=CARTESIAN_POINT ( 'NONE',  ( 117.3719165460472027, -2.191907684172563986, -18.20049396185734025 ) ) ;
#37998=CARTESIAN_POINT ( 'NONE',  ( 115.3993696192402325, -1.111561923218680858, -17.14115599315434935 ) ) ;
#37999=CARTESIAN_POINT ( 'NONE',  ( 117.8449348109119938, -8.166667518702817929, -8.995218007635861213 ) ) ;
#38005=CARTESIAN_POINT ( 'NONE',  ( 120.9649014775786355, -6.222761293078241884, -8.102969835052219238 ) ) ;
#38007=CARTESIAN_POINT ( 'NONE',  ( 125.3895814775786448, -7.893985811506177619, -18.51759400769804742 ) ) ;
#38008=CARTESIAN_POINT ( 'NONE',  ( 117.5613014775786525, 0.9020085738987339008, -11.91225656197089222 ) ) ;
#38010=CARTESIAN_POINT ( 'NONE',  ( 117.1642148109119859, -0.8288870151387760510, -10.36305467784173118 ) ) ;
#38011=CARTESIAN_POINT ( 'NONE',  ( 126.0135748109119902, -8.166667518702819706, -8.995218007635861213 ) ) ;
#38015=CARTESIAN_POINT ( 'NONE',  ( 118.4122014775786340, -9.859900752359374465, -12.68260735090039404 ) ) ;
#38016=CARTESIAN_POINT ( 'NONE',  ( 120.5678148109119832, -1.833838273342659253, -17.42832698103878286 ) ) ;
#38021=CARTESIAN_POINT ( 'NONE',  ( 115.5191414775786569, -3.383040157471821630, -19.15922257007629170 ) ) ;
#38022=CARTESIAN_POINT ( 'NONE',  ( 113.0231681442453322, 0.9020085738987339008, -11.91225656197089222 ) ) ;
#38024=VERTEX_POINT ( 'NONE', #28857 ) ;
#38025=CARTESIAN_POINT ( 'NONE',  ( 123.6451722564640079, -3.285188920618888897, -14.24668229758334803 ) ) ;
#38027=CARTESIAN_POINT ( 'NONE',  ( 121.0783548109119749, 0.2603800115204892296, -16.42320221600525088 ) ) ;
#38029=CARTESIAN_POINT ( 'NONE',  ( 114.7249681442453237, 0.2603800115204892296, -16.42320221600525088 ) ) ;
#38030=CARTESIAN_POINT ( 'NONE',  ( 117.6180281442453150, -8.899110576539710493, -16.42337572283490132 ) ) ;
#38032=CARTESIAN_POINT ( 'NONE',  ( 123.6310548109119765, -5.638512984488999180, -18.83840828888717311 ) ) ;
#38033=CARTESIAN_POINT ( 'NONE',  ( 118.4689281442453392, 0.9020085738987339008, -11.91225656197089222 ) ) ;
#38037=CARTESIAN_POINT ( 'NONE',  ( 112.2289948109119848, -7.643976991954077427, -18.09477374809248928 ) ) ;
#38040=CARTESIAN_POINT ( 'NONE',  ( 117.3343948109119737, -3.383040157471821630, -19.15922257007629170 ) ) ;
#38042=CARTESIAN_POINT ( 'NONE',  ( 116.4267681442453153, -3.383040157471821630, -19.15922257007629170 ) ) ;
#38045=CARTESIAN_POINT ( 'NONE',  ( 123.9146881442452894, 0.9020085738987339008, -11.91225656197089222 ) ) ;
#38047=CARTESIAN_POINT ( 'NONE',  ( 113.4769814775786330, 0.4262465694468514643, -12.03445270309931736 ) ) ;
#38049=CARTESIAN_POINT ( 'NONE',  ( 116.1998614775786507, 0.4262465694468514643, -12.03445270309931736 ) ) ;
#38051=CARTESIAN_POINT ( 'NONE',  ( 116.0864081442453113, -0.1624402480850797581, -16.17319339645315424 ) ) ;
#38054=CARTESIAN_POINT ( 'NONE',  ( 120.0572748109119772, -6.222761293078241884, -8.102969835052219238 ) ) ;
#38056=CARTESIAN_POINT ( 'NONE',  ( 116.4267681442453153, -3.383040157471821630, -19.15922257007629170 ) ) ;
#38057=CARTESIAN_POINT ( 'NONE',  ( 112.3991748109119868, -1.833838273342658809, -17.42832698103878286 ) ) ;
#38058=CARTESIAN_POINT ( 'NONE',  ( 115.9729548109119861, -3.505236298600246325, -18.68346056562440793 ) ) ;
#38060=CARTESIAN_POINT ( 'NONE',  ( 118.2987481442453088, -1.561330072975668504, -17.79121239304076951 ) ) ;
#38066=CARTESIAN_POINT ( 'NONE',  ( 122.0427081442452817, 0.5811942927096110934, -14.16772938898807510 ) ) ;
#38069=CARTESIAN_POINT ( 'NONE',  ( 118.0718414775786442, -0.8288870151387760510, -10.36305467784173118 ) ) ;
#38071=CARTESIAN_POINT ( 'NONE',  ( 124.4819548109119722, -7.893985811506177619, -18.51759400769804742 ) ) ;
#38076=CARTESIAN_POINT ( 'NONE',  ( 126.2972081442452890, -2.084020599724406786, -8.691656652584148546 ) ) ;
#38077=CARTESIAN_POINT ( 'NONE',  ( 122.8368814775786291, -1.561330072975668948, -17.79121239304076951 ) ) ;
#38078=CARTESIAN_POINT ( 'NONE',  ( 115.5758681442453053, -7.894159318335828068, -9.358103419637847864 ) ) ;
#38080=CARTESIAN_POINT ( 'NONE',  ( 120.5678148109119832, -8.166667518702819706, -8.995218007635861213 ) ) ;
#38082=CARTESIAN_POINT ( 'NONE',  ( 121.5321681442453183, -0.1624402480850797581, -16.17319339645315424 ) ) ;
#38087=CARTESIAN_POINT ( 'NONE',  ( 116.0864081442453113, -9.988377603198976828, -10.36322818467138340 ) ) ;
#38088=CARTESIAN_POINT ( 'NONE',  ( 124.3685014775786328, 0.4262465694468514643, -12.03445270309931736 ) ) ;
#38092=CARTESIAN_POINT ( 'NONE',  ( 122.5532481442453019, -10.63000616557722466, -14.87417383870573495 ) ) ;
#38094=CARTESIAN_POINT ( 'NONE',  ( 121.0216281442452981, -7.894159318335828068, -9.358103419637847864 ) ) ;
#38099=CARTESIAN_POINT ( 'NONE',  ( 115.1787814775786387, -9.988377603198976828, -10.36322818467138340 ) ) ;
#38100=CARTESIAN_POINT ( 'NONE',  ( 123.5176014775786228, -0.8288870151387760510, -10.36305467784173118 ) ) ;
#38103=CARTESIAN_POINT ( 'NONE',  ( 122.4965214775786251, -10.30919188438810075, -12.61870101168855918 ) ) ;
#38104=CARTESIAN_POINT ( 'NONE',  ( 111.3403343090046889, -8.955484211904590097, -16.47405415812863083 ) ) ;
#38105=CARTESIAN_POINT ( 'NONE',  ( 118.3554748109119998, 0.2603800115204892296, -16.42320221600525088 ) ) ;
#38106=CARTESIAN_POINT ( 'NONE',  ( 119.6601881442453106, -8.166667518702819706, -8.995218007635861213 ) ) ;
#38107=CARTESIAN_POINT ( 'NONE',  ( 121.0783548109119749, -9.565557343593413364, -10.61323700422348004 ) ) ;
#38109=CARTESIAN_POINT ( 'NONE',  ( 117.1074881442453233, -10.63000616557722466, -14.87417383870573495 ) ) ;
#38117=CARTESIAN_POINT ( 'NONE',  ( 125.2194014775786286, -10.30919188438810075, -12.61870101168855918 ) ) ;
#38118=CARTESIAN_POINT ( 'NONE',  ( 113.2500748109119968, -6.344957434206662583, -7.627207830600332805 ) ) ;
#38119=VERTEX_POINT ( 'NONE', #10528 ) ;
#38121=CARTESIAN_POINT ( 'NONE',  ( 111.2646414775786496, -8.899110576539710493, -16.42337572283490132 ) ) ;
#38124=CARTESIAN_POINT ( 'NONE',  ( 123.4041481442452834, -10.30919188438810075, -12.61870101168855918 ) ) ;
#38127=CARTESIAN_POINT ( 'NONE',  ( 124.7655881442452852, 0.5811942927096110934, -14.16772938898807510 ) ) ;
#38129=CARTESIAN_POINT ( 'NONE',  ( 112.7962614775786676, -3.383040157471821630, -19.15922257007629170 ) ) ;
#38135=CARTESIAN_POINT ( 'NONE',  ( 114.3278814775786429, 0.1319031606808879209, -14.10382304977623669 ) ) ;
#38136=CARTESIAN_POINT ( 'NONE',  ( 112.7395348109119766, -5.638512984488999180, -18.83840828888717311 ) ) ;
#38139=CARTESIAN_POINT ( 'NONE',  ( 120.2274548109119934, -9.859900752359378018, -12.68260735090039759 ) ) ;
#38140=CARTESIAN_POINT ( 'NONE',  ( 116.7104014775786425, -8.899110576539710493, -16.42337572283490132 ) ) ;
#38141=CARTESIAN_POINT ( 'NONE',  ( 112.8529881442453160, -7.894159318335828068, -9.358103419637847864 ) ) ;
#38145=CARTESIAN_POINT ( 'NONE',  ( 114.7249681442453237, -9.565557343593413364, -10.61323700422348004 ) ) ;
#38146=VERTEX_POINT ( 'NONE', #37884 ) ;
#38151=CARTESIAN_POINT ( 'NONE',  ( 117.1642148109119859, -0.8288870151387760510, -10.36305467784173118 ) ) ;
#38152=CARTESIAN_POINT ( 'NONE',  ( 114.7249681442453237, -9.565557343593413364, -10.61323700422348004 ) ) ;
#38153=DIRECTION ( 'NONE',  ( 1.000000000000000000, 0.000000000000000000, 0.000000000000000000 ) ) ;
#38160=CARTESIAN_POINT ( 'NONE',  ( 117.9810475888224062, -2.372251574601226043, -17.96033910819752322 ) ) ;
#38161=CARTESIAN_POINT ( 'NONE',  ( 124.0848681442452772, -5.574606645277164318, -18.38911715685844683 ) ) ;
#38162=CARTESIAN_POINT ( 'NONE',  ( 118.6391081442452986, -5.574606645277164318, -18.38911715685844683 ) ) ;
#38163=CARTESIAN_POINT ( 'NONE',  ( 119.9766353496756608, -1.087735405160626723, -17.17288456429612964 ) ) ;
#38165=CARTESIAN_POINT ( 'NONE',  ( 126.2184548109119788, -4.863998795839242995, -13.39321520033831447 ) ) ;
#38166=CARTESIAN_POINT ( 'NONE',  ( 115.9729548109119861, -3.505236298600246325, -18.68346056562440793 ) ) ;
#38167=DIRECTION ( 'NONE',  ( 0.000000000000000000, 0.6004852223388321697, -0.7996358532186279566 ) ) ;
#38168=CARTESIAN_POINT ( 'NONE',  ( 124.9924948109119924, -4.089484607189486809, -7.948022111789456723 ) ) ;
#38169=CARTESIAN_POINT ( 'NONE',  ( 126.2404814775786264, -0.8288870151387760510, -10.36305467784173118 ) ) ;
#38171=CARTESIAN_POINT ( 'NONE',  ( 115.2355081442453155, -10.30919188438810075, -12.61870101168855918 ) ) ;
#38174=CARTESIAN_POINT ( 'NONE',  ( 113.0231681442453322, 0.9020085738987339008, -11.91225656197089222 ) ) ;
#38175=EDGE_CURVE ( 'NONE', #44110, #6291, #44169, .T. ) ;
#38176=CARTESIAN_POINT ( 'NONE',  ( 113.0231681442453322, 0.9020085738987339008, -11.91225656197089222 ) ) ;
#38177=CARTESIAN_POINT ( 'NONE',  ( 125.2761281442453054, 0.4262465694468514643, -12.03445270309931736 ) ) ;
#38178=VECTOR ( 'NONE', #33262, 1000.000000000000000 ) ;
#38183=CARTESIAN_POINT ( 'NONE',  ( 118.1285681442453068, -2.084020599724406786, -8.691656652584148546 ) ) ;
#38185=DIRECTION ( 'NONE',  ( 0.000000000000000000, 0.6004852223388321697, -0.7996358532186279566 ) ) ;
#38188=CARTESIAN_POINT ( 'NONE',  ( 124.4819548109119722, -7.893985811506177619, -18.51759400769804742 ) ) ;
#38189=CARTESIAN_POINT ( 'NONE',  ( 125.3328548109119964, -9.261995988541379177, -16.69588392320231307 ) ) ;
#38191=CARTESIAN_POINT ( 'NONE',  ( 118.9227414775786400, -10.63000616557722466, -14.87417383870573495 ) ) ;
#38192=CARTESIAN_POINT ( 'NONE',  ( 117.8449348109119938, -8.166667518702817929, -8.995218007635861213 ) ) ;
#38194=CARTESIAN_POINT ( 'NONE',  ( 115.4624148109119943, -4.153390946401321671, -8.397313243818183892 ) ) ;
#38195=CARTESIAN_POINT ( 'NONE',  ( 125.5597614775786326, -1.561330072975669392, -17.79121239304076951 ) ) ;
#38196=CARTESIAN_POINT ( 'NONE',  ( 113.9875214775786532, -0.4660016031367893996, -10.09054647747474043 ) ) ;
#38197=CARTESIAN_POINT ( 'NONE',  ( 117.3911214775786505, -7.894159318335828068, -9.358103419637847864 ) ) ;
#38199=CARTESIAN_POINT ( 'NONE',  ( 120.2841814775786276, -10.15424416112533912, -14.75197769757731336 ) ) ;
#38201=CARTESIAN_POINT ( 'NONE',  ( 116.4267681442453153, -3.383040157471821630, -19.15922257007629170 ) ) ;
#38205=CARTESIAN_POINT ( 'NONE',  ( 114.6874464091100947, -0.9924539043446216624, -17.29976612834909133 ) ) ;
#38208=CARTESIAN_POINT ( 'NONE',  ( 114.7249681442453237, 0.2603800115204892296, -16.42320221600525088 ) ) ;
#38215=CARTESIAN_POINT ( 'NONE',  ( 118.4689281442453392, 0.9020085738987339008, -11.91225656197089222 ) ) ;
#38218=CARTESIAN_POINT ( 'NONE',  ( 122.7801548109119665, -6.222761293078241884, -8.102969835052219238 ) ) ;
#38220=CARTESIAN_POINT ( 'NONE',  ( 125.9001214775786224, -4.089484607189486809, -7.948022111789456723 ) ) ;
#38221=CARTESIAN_POINT ( 'NONE',  ( 118.5823814775786360, -1.834011780172310813, -8.268836392978581529 ) ) ;
#38223=CARTESIAN_POINT ( 'NONE',  ( 114.6682414775786469, -7.894159318335828068, -9.358103419637847864 ) ) ;
#38224=CARTESIAN_POINT ( 'NONE',  ( 112.1155414775786454, -10.15424416112533912, -14.75197769757731336 ) ) ;
#38227=CARTESIAN_POINT ( 'NONE',  ( 120.8514481442452961, -2.084020599724406786, -8.691656652584148546 ) ) ;
#38228=CARTESIAN_POINT ( 'NONE',  ( 122.0994348109119443, -10.15424416112533912, -14.75197769757731336 ) ) ;
#38235=CARTESIAN_POINT ( 'NONE',  ( 113.9307948109119906, 0.9020085738987339008, -11.91225656197089222 ) ) ;
#38236=CARTESIAN_POINT ( 'NONE',  ( 113.3635281442453504, -9.988377603198976828, -10.36322818467138340 ) ) ;
#38239=CARTESIAN_POINT ( 'NONE',  ( 116.9582927111058552, -1.267766418764730840, -16.93314635290706605 ) ) ;
#38241=CARTESIAN_POINT ( 'NONE',  ( 120.3409081442453044, -0.4660016031367893996, -10.09054647747474043 ) ) ;
#38242=CARTESIAN_POINT ( 'NONE',  ( 113.7606148109119886, -1.561330072975668060, -17.79121239304076596 ) ) ;
#38243=CARTESIAN_POINT ( 'NONE',  ( 116.9373081442452929, -1.833838273342659253, -17.42832698103878286 ) ) ;
#38245=CARTESIAN_POINT ( 'NONE',  ( 125.6732148109119862, 0.5811942927096110934, -14.16772938898807510 ) ) ;
#38246=CARTESIAN_POINT ( 'NONE',  ( 118.5823814775786360, -1.834011780172310813, -8.268836392978581529 ) ) ;
#38248=CARTESIAN_POINT ( 'NONE',  ( 112.4559014775786778, -0.1624402480850797581, -16.17319339645315424 ) ) ;
#38251=CARTESIAN_POINT ( 'NONE',  ( 119.4332814775786318, -0.4660016031367893996, -10.09054647747474043 ) ) ;
#38253=CARTESIAN_POINT ( 'NONE',  ( 114.7816948109119863, 0.5811942927096154232, -14.16772938898807155 ) ) ;
#38257=CARTESIAN_POINT ( 'NONE',  ( 125.3328548109119964, -9.261995988541697145, -16.69588392320189030 ) ) ;
#38258=CARTESIAN_POINT ( 'NONE',  ( 128.2184548109119930, -4.863998795839242995, -13.39321520033831447 ) ) ;
#38261=CARTESIAN_POINT ( 'NONE',  ( 120.1140014775786398, -7.894159318335828068, -9.358103419637847864 ) ) ;
#38262=CARTESIAN_POINT ( 'NONE',  ( 120.0947965460471920, -2.191907684172563986, -18.20049396185734025 ) ) ;
#38264=CARTESIAN_POINT ( 'NONE',  ( 119.3198281442452924, -9.859900752359374465, -12.68260735090039404 ) ) ;
#38266=CARTESIAN_POINT ( 'NONE',  ( 120.8514481442452961, -2.084020599724406786, -8.691656652584148546 ) ) ;
#38268=CARTESIAN_POINT ( 'NONE',  ( 116.7104014775786425, -0.4660016031367893996, -10.09054647747474043 ) ) ;
#38270=CARTESIAN_POINT ( 'NONE',  ( 116.3133148109120043, -2.084020599724406786, -8.691656652584148546 ) ) ;
#38272=CARTESIAN_POINT ( 'NONE',  ( 115.8027748109119841, -0.4660016031367893996, -10.09054647747474043 ) ) ;
#38279=CARTESIAN_POINT ( 'NONE',  ( 122.7234281442452755, -5.638512984488999180, -18.83840828888717311 ) ) ;
#38281=CARTESIAN_POINT ( 'NONE',  ( 127.0553483106876484, -8.910448477848374793, -9.789625213634170819 ) ) ;
#38282=CARTESIAN_POINT ( 'NONE',  ( 117.1074881442453233, 0.4262465694468514643, -12.03445270309931736 ) ) ;
#38283=CARTESIAN_POINT ( 'NONE',  ( 115.8595014775786609, -1.834011780172301043, -8.268836392978595740 ) ) ;
#38285=CARTESIAN_POINT ( 'NONE',  ( 123.7445081442452874, -1.561330072975668948, -17.79121239304076951 ) ) ;
#38291=CARTESIAN_POINT ( 'NONE',  ( 125.3328548109119964, -0.8288870151387760510, -10.36305467784173118 ) ) ;
#38292=CARTESIAN_POINT ( 'NONE',  ( 122.6667014775786413, -7.893985811506177619, -18.51759400769804742 ) ) ;
#38293=CARTESIAN_POINT ( 'NONE',  ( 117.9583881442453048, 0.1319031606808879209, -14.10382304977623669 ) ) ;
#38295=CARTESIAN_POINT ( 'NONE',  ( 117.7882081442453170, -6.344957434206665248, -7.627207830600338134 ) ) ;
#38297=CARTESIAN_POINT ( 'NONE',  ( 122.9503348109119827, -9.859900752359378018, -12.68260735090039759 ) ) ;
#38301=CARTESIAN_POINT ( 'NONE',  ( 118.4689281442453392, 0.9020085738987339008, -11.91225656197089222 ) ) ;
#38302=CARTESIAN_POINT ( 'NONE',  ( 123.4041481442452834, 0.1319031606808879209, -14.10382304977623669 ) ) ;
#38307=CARTESIAN_POINT ( 'NONE',  ( 121.6456214775786293, -10.63000616557722466, -14.87417383870573495 ) ) ;
#38309=CARTESIAN_POINT ( 'NONE',  ( 119.8303681442453126, 0.4262465694468514643, -12.03445270309931736 ) ) ;
#38312=CARTESIAN_POINT ( 'NONE',  ( 115.1220548109119761, -8.166667518702817929, -8.995218007635861213 ) ) ;
#38313=CARTESIAN_POINT ( 'NONE',  ( 125.5030348109119558, -6.222761293078241884, -8.102969835052219238 ) ) ;
#38316=CARTESIAN_POINT ( 'NONE',  ( 123.4608748109119745, -10.63000616557722466, -14.87417383870573495 ) ) ;
#38320=CARTESIAN_POINT ( 'NONE',  ( 122.7234281442452755, -5.638512984488999180, -18.83840828888717311 ) ) ;
#38321=CARTESIAN_POINT ( 'NONE',  ( 120.0005481442453146, -5.638512984488999180, -18.83840828888717311 ) ) ;
#38322=CARTESIAN_POINT ( 'NONE',  ( 123.4608748109119745, 0.4262465694468514643, -12.03445270309931736 ) ) ;
#38323=CARTESIAN_POINT ( 'NONE',  ( 121.6456214775786293, 0.4262465694468514643, -12.03445270309931736 ) ) ;
#38325=CARTESIAN_POINT ( 'NONE',  ( 116.4267681442453153, -3.383040157471821630, -19.15922257007629170 ) ) ;
#38328=CARTESIAN_POINT ( 'NONE',  ( 125.2655881442453278, 0.08617673920530924403, -14.09731900820076334 ) ) ;
#38332=CARTESIAN_POINT ( 'NONE',  ( 124.8223148109119762, 0.9020085738987339008, -11.91225656197089222 ) ) ;
#38333=CARTESIAN_POINT ( 'NONE',  ( 111.7184548109119788, -9.261995988541697145, -16.69588392320189030 ) ) ;
#38335=CARTESIAN_POINT ( 'NONE',  ( 113.3068014775786594, -1.833838273342658809, -17.42832698103878286 ) ) ;
#38338=CARTESIAN_POINT ( 'NONE',  ( 124.4252281442452812, -9.261995988541697145, -16.69588392320189030 ) ) ;
#38341=CARTESIAN_POINT ( 'NONE',  ( 112.7395348109119766, -5.638512984488999180, -18.83840828888717311 ) ) ;
#38346=CARTESIAN_POINT ( 'NONE',  ( 116.9373081442452929, -1.833838273342659253, -17.42832698103878286 ) ) ;
#38347=CARTESIAN_POINT ( 'NONE',  ( 113.2500748109119968, -6.344957434206662583, -7.627207830600332805 ) ) ;
#38351=CARTESIAN_POINT ( 'NONE',  ( 122.0427081442452817, -9.859900752359378018, -12.68260735090039759 ) ) ;
#38352=CARTESIAN_POINT ( 'NONE',  ( 120.1707281442453166, -9.565557343593413364, -10.61323700422348004 ) ) ;
#38353=CARTESIAN_POINT ( 'NONE',  ( 125.5597614775786326, -1.561330072975669392, -17.79121239304076951 ) ) ;
#38356=CARTESIAN_POINT ( 'NONE',  ( 125.1626748109119802, -0.1624402480850797581, -16.17319339645315424 ) ) ;
#38358=CARTESIAN_POINT ( 'NONE',  ( 114.1009748109119784, -5.574606645277164318, -18.38911715685844683 ) ) ;
#38360=CARTESIAN_POINT ( 'NONE',  ( 126.6390922358648368, -9.448224192814040023, -15.87040149726915139 ) ) ;
#38364=CARTESIAN_POINT ( 'NONE',  ( 119.5467348109119712, -5.574606645277164318, -18.38911715685844683 ) ) ;
#38365=CARTESIAN_POINT ( 'NONE',  ( 113.2500748109119968, -3.505236298600246325, -18.68346056562440793 ) ) ;
#38366=DIRECTION ( 'NONE',  ( 0.000000000000000000, 0.7996358532185066093, 0.6004852223389939292 ) ) ;
#38367=ADVANCED_FACE ( 'NONE', ( #25551 ), #26618, .F. ) ;
#38370=CARTESIAN_POINT ( 'NONE',  ( 121.4571555643466922, -1.244021962887374544, -16.96476564598603076 ) ) ;
#38375=CARTESIAN_POINT ( 'NONE',  ( 122.0994348109119443, -10.15424416112533912, -14.75197769757731336 ) ) ;
#38376=CARTESIAN_POINT ( 'NONE',  ( 116.7104014775786425, -8.899110576539710493, -16.42337572283490132 ) ) ;
#38377=CARTESIAN_POINT ( 'NONE',  ( 114.0442481442453300, -7.643976991954099631, -18.09477374809247152 ) ) ;
#38379=CARTESIAN_POINT ( 'NONE',  ( 117.6747548109119919, -7.643976991954077427, -18.09477374809248928 ) ) ;
#38380=CARTESIAN_POINT ( 'NONE',  ( 125.0492214775786266, -3.505236298600246325, -18.68346056562440793 ) ) ;
#38383=CARTESIAN_POINT ( 'NONE',  ( 113.7606148109119886, -1.561330072975668060, -17.79121239304076596 ) ) ;
#38385=CARTESIAN_POINT ( 'NONE',  ( 115.2922348109119781, -10.63000616557722466, -14.87417383870573495 ) ) ;
#38388=CARTESIAN_POINT ( 'NONE',  ( 113.1366214775786432, -1.834011780172310813, -8.268836392978581529 ) ) ;
#38389=CARTESIAN_POINT ( 'NONE',  ( 113.4769814775786330, -10.63000616557722466, -14.87417383870573495 ) ) ;
#38391=CARTESIAN_POINT ( 'NONE',  ( 122.6099748109119929, -0.8288870151387760510, -10.36305467784173118 ) ) ;
#38395=CARTESIAN_POINT ( 'NONE',  ( 111.9261565460472099, -2.191907684172563986, -18.20049396185734025 ) ) ;
#38397=CARTESIAN_POINT ( 'NONE',  ( 116.1431348109119881, 0.1319031606808879209, -14.10382304977623669 ) ) ;
#38402=CARTESIAN_POINT ( 'NONE',  ( 126.1837548109119211, -10.63000616557722466, -14.87417383870573495 ) ) ;
#38406=CARTESIAN_POINT ( 'NONE',  ( 119.6601881442453106, -8.166667518702819706, -8.995218007635861213 ) ) ;
#38407=CARTESIAN_POINT ( 'NONE',  ( 114.7249681442453237, 0.2603800115204892296, -16.42320221600525088 ) ) ;
#38410=CARTESIAN_POINT ( 'NONE',  ( 114.6115148109119986, -6.222761293078241884, -8.102969835052219238 ) ) ;
#38411=CARTESIAN_POINT ( 'NONE',  ( 124.2550481442452792, -9.988377603198980381, -10.36322818467138518 ) ) ;
#38412=CARTESIAN_POINT ( 'NONE',  ( 116.9373081442452929, -8.166667518702817929, -8.995218007635861213 ) ) ;
#38414=CARTESIAN_POINT ( 'NONE',  ( 116.1431348109119881, 0.1319031606808879209, -14.10382304977623669 ) ) ;
#38416=CARTESIAN_POINT ( 'NONE',  ( 122.5532481442453019, 0.4262465694468514643, -12.03445270309931736 ) ) ;
#38418=CARTESIAN_POINT ( 'NONE',  ( 117.3911214775786505, -1.561330072975668504, -17.79121239304076951 ) ) ;
#38419=CARTESIAN_POINT ( 'NONE',  ( 137.4696151216520263, 0.06564595942581503973, -14.47274270616910563 ) ) ;
#38425=CARTESIAN_POINT ( 'NONE',  ( 124.9357681442453014, -1.834011780172310813, -8.268836392978581529 ) ) ;
#38427=CARTESIAN_POINT ( 'NONE',  ( 114.3278814775786429, -10.30919188438810075, -12.61870101168855918 ) ) ;
#38428=CARTESIAN_POINT ( 'NONE',  ( 136.7860375664301387, -10.44385780544745401, -13.88278873169130456 ) ) ;
#38429=FACE_OUTER_BOUND ( 'NONE', #4498, .T. ) ;
#38433=CARTESIAN_POINT ( 'NONE',  ( 118.8092881442453290, -9.988377603198976828, -10.36322818467138340 ) ) ;
#38435=CARTESIAN_POINT ( 'NONE',  ( 111.7795248144346800, -2.280480477428481922, -18.08254604495228079 ) ) ;
#38436=CARTESIAN_POINT ( 'NONE',  ( 119.1389604811917025, -3.807985514183269693, -19.09877912889401230 ) ) ;
#38437=CARTESIAN_POINT ( 'NONE',  ( 124.0281414775786146, -7.643976991954077427, -18.09477374809248928 ) ) ;
#38438=CARTESIAN_POINT ( 'NONE',  ( 117.9016614775786280, -0.1624402480850797581, -16.17319339645315424 ) ) ;
#38441=CARTESIAN_POINT ( 'NONE',  ( 123.1205148109119563, -1.834011780172310813, -8.268836392978581529 ) ) ;
#38443=CARTESIAN_POINT ( 'NONE',  ( 114.2711548109119803, -0.1624402480850797581, -16.17319339645315424 ) ) ;
#38444=CARTESIAN_POINT ( 'NONE',  ( 112.7395348109119766, -4.153390946401321671, -8.397313243818183892 ) ) ;
#38447=CARTESIAN_POINT ( 'NONE',  ( 120.6812681442452941, 0.1319031606808879209, -14.10382304977623669 ) ) ;
#38448=CARTESIAN_POINT ( 'NONE',  ( 120.8514481442452961, -2.084020599724406786, -8.691656652584148546 ) ) ;
#38454=CARTESIAN_POINT ( 'NONE',  ( 118.2420214775786320, -3.383040157471821630, -19.15922257007629170 ) ) ;
#38455=CARTESIAN_POINT ( 'NONE',  ( 113.5904348109119866, -7.893985811506177619, -18.51759400769804742 ) ) ;
#38459=CARTESIAN_POINT ( 'NONE',  ( 113.2099653070359011, -1.196538596002804766, -17.02799684832027438 ) ) ;
#38460=CARTESIAN_POINT ( 'NONE',  ( 121.1350814775786233, 0.5811942927096110934, -14.16772938898807510 ) ) ;
#38461=CARTESIAN_POINT ( 'NONE',  ( 112.2289948109119848, -1.834011780172310813, -8.268836392978581529 ) ) ;
#38462=CARTESIAN_POINT ( 'NONE',  ( 123.5176014775786228, -0.8288870151387760510, -10.36305467784173118 ) ) ;
#38463=CARTESIAN_POINT ( 'NONE',  ( 124.8223148109119762, 0.9020085738987339008, -11.91225656197089222 ) ) ;
#38464=CARTESIAN_POINT ( 'NONE',  ( 118.1285681442453068, -7.893985811506177619, -18.51759400769804742 ) ) ;
#38466=CARTESIAN_POINT ( 'NONE',  ( 114.9518748109119883, -7.643976991954077427, -18.09477374809248928 ) ) ;
#38469=CARTESIAN_POINT ( 'NONE',  ( 120.0005481442453146, -5.638512984488999180, -18.83840828888717311 ) ) ;
#38471=CARTESIAN_POINT ( 'NONE',  ( 117.4478481442453131, 0.2603800115204892296, -16.42320221600525088 ) ) ;
#38474=CARTESIAN_POINT ( 'NONE',  ( 123.9714148109119805, -0.4660016031367893996, -10.09054647747474043 ) ) ;
#38475=DIRECTION ( 'NONE',  ( 1.000000000000000000, 0.000000000000000000, 0.000000000000000000 ) ) ;
#38476=CARTESIAN_POINT ( 'NONE',  ( 115.8595014775786609, -7.643976991954077427, -18.09477374809248928 ) ) ;
#38480=CARTESIAN_POINT ( 'NONE',  ( 121.0783548109119749, -9.565557343593413364, -10.61323700422348004 ) ) ;
#38482=CARTESIAN_POINT ( 'NONE',  ( 120.7379948109119709, 0.4262465694468514643, -12.03445270309931736 ) ) ;
#38484=CARTESIAN_POINT ( 'NONE',  ( 121.1350814775786233, -9.859900752359378018, -12.68260735090039759 ) ) ;
#38486=CARTESIAN_POINT ( 'NONE',  ( 114.1577014775786552, -6.344957434206662583, -7.627207830600332805 ) ) ;
#38488=CARTESIAN_POINT ( 'NONE',  ( 119.0361948109119652, -2.084020599724406786, -8.691656652584148546 ) ) ;
#38490=CARTESIAN_POINT ( 'NONE',  ( 116.2565881442452991, -9.261995988541697145, -16.69588392320189030 ) ) ;
#38492=CARTESIAN_POINT ( 'NONE',  ( 115.6893214775786447, -9.859900752359374465, -12.68260735090037983 ) ) ;
#38495=CARTESIAN_POINT ( 'NONE',  ( 121.8158014775786171, -5.638512984488999180, -18.83840828888717311 ) ) ;
#38497=CARTESIAN_POINT ( 'NONE',  ( 126.3671785243040659, -8.266574344583974110, -9.628621930846563259 ) ) ;
#38498=CARTESIAN_POINT ( 'NONE',  ( 116.6536748109119941, -10.15424416112533912, -14.75197769757731336 ) ) ;
#38501=CARTESIAN_POINT ( 'NONE',  ( 125.3895814775786448, -7.893985811506177619, -18.51759400769804742 ) ) ;
#38505=CARTESIAN_POINT ( 'NONE',  ( 114.7249681442453237, 0.2603800115204892296, -16.42320221600525088 ) ) ;
#38506=CARTESIAN_POINT ( 'NONE',  ( 112.5126281442453120, -10.30919188438810075, -12.61870101168855918 ) ) ;
#38507=CARTESIAN_POINT ( 'NONE',  ( 124.8223148109119762, 0.9020085738987339008, -11.91225656197089222 ) ) ;
#38508=CARTESIAN_POINT ( 'NONE',  ( 116.7104014775786425, -8.899110576539710493, -16.42337572283490132 ) ) ;
#38510=CARTESIAN_POINT ( 'NONE',  ( 120.2841814775786276, 0.9020085738987339008, -11.91225656197089222 ) ) ;
#38514=CARTESIAN_POINT ( 'NONE',  ( 121.4187148109119789, -3.505236298600246325, -18.68346056562440793 ) ) ;
#38515=ORIENTED_EDGE ( 'NONE', *, *, #798, .F. ) ;
#38517=CARTESIAN_POINT ( 'NONE',  ( 115.7460481442453357, 0.9020085738987339008, -11.91225656197089222 ) ) ;
#38518=CARTESIAN_POINT ( 'NONE',  ( 124.9357681442453014, -7.643976991954077427, -18.09477374809248928 ) ) ;
#38520=CARTESIAN_POINT ( 'NONE',  ( 112.3991748109119868, -8.166667518702817929, -8.995218007635859436 ) ) ;
#38521=CARTESIAN_POINT ( 'NONE',  ( 120.5678148109119832, -8.166667518702819706, -8.995218007635861213 ) ) ;
#38523=CARTESIAN_POINT ( 'NONE',  ( 121.6456214775786293, 0.4262465694468514643, -12.03445270309931736 ) ) ;
#38524=ORIENTED_EDGE ( 'NONE', *, *, #40070, .T. ) ;
#38526=CARTESIAN_POINT ( 'NONE',  ( 116.0296814775786345, -8.166667518702817929, -8.995218007635861213 ) ) ;
#38529=CARTESIAN_POINT ( 'NONE',  ( 125.2194014775786286, 0.1319031606808879209, -14.10382304977623669 ) ) ;
#38533=CARTESIAN_POINT ( 'NONE',  ( 124.6521348109119884, -1.561330072975668948, -17.79121239304076951 ) ) ;
#38536=CARTESIAN_POINT ( 'NONE',  ( 122.8368814775786291, -1.561330072975668948, -17.79121239304076951 ) ) ;
#38537=CARTESIAN_POINT ( 'NONE',  ( 120.8514481442452961, -7.893985811506177619, -18.51759400769804742 ) ) ;
#38538=CARTESIAN_POINT ( 'NONE',  ( 121.7023481442452919, -0.8288870151387760510, -10.36305467784173118 ) ) ;
#38539=CARTESIAN_POINT ( 'NONE',  ( 120.1140014775786398, -7.894159318335828068, -9.358103419637847864 ) ) ;
#38541=CARTESIAN_POINT ( 'NONE',  ( 114.6682414775786469, -1.561330072975668060, -17.79121239304076596 ) ) ;
#38543=CARTESIAN_POINT ( 'NONE',  ( 124.9924948109119924, -5.574606645276184658, -18.38911715685858539 ) ) ;
#38548=CARTESIAN_POINT ( 'NONE',  ( 124.9924948109119924, -4.089484607189486809, -7.948022111789456723 ) ) ;
#38549=CARTESIAN_POINT ( 'NONE',  ( 112.3424481442453384, -6.344957434206662583, -7.627207830600332805 ) ) ;
#38551=CARTESIAN_POINT ( 'NONE',  ( 111.4915481442453142, -1.833838273342658365, -17.42832698103878286 ) ) ;
#38554=CARTESIAN_POINT ( 'NONE',  ( 124.9924948109119924, -4.089484607189486809, -7.948022111789456723 ) ) ;
#38555=CARTESIAN_POINT ( 'NONE',  ( 125.2761281442453054, -10.63000616557722466, -14.87417383870573495 ) ) ;
#38557=CARTESIAN_POINT ( 'NONE',  ( 115.9729548109119861, -6.344957434206662583, -7.627207830600332805 ) ) ;
#38561=CARTESIAN_POINT ( 'NONE',  ( 126.2597653975816883, -7.679457989152358444, -9.236116388709978864 ) ) ;
#38562=CARTESIAN_POINT ( 'NONE',  ( 116.2565881442453133, -0.8288870151387760510, -10.36305467784173118 ) ) ;
#38563=CARTESIAN_POINT ( 'NONE',  ( 114.2144281442453178, -8.166667518702817929, -8.995218007635859436 ) ) ;
#38567=CARTESIAN_POINT ( 'NONE',  ( 122.6099748109119929, -0.8288870151387760510, -10.36305467784173118 ) ) ;
#38568=CARTESIAN_POINT ( 'NONE',  ( 119.9438214775786378, -2.084020599724406786, -8.691656652584148546 ) ) ;
#38569=CARTESIAN_POINT ( 'NONE',  ( 125.5030348109119558, -3.383040157471821630, -19.15922257007629170 ) ) ;
#38570=VERTEX_POINT ( 'NONE', #7310 ) ;
#38571=CARTESIAN_POINT ( 'NONE',  ( 125.7299414775786346, -10.15424416112533912, -14.75197769757731336 ) ) ;
#38574=CARTESIAN_POINT ( 'NONE',  ( 115.0086014775786509, -5.574606645277164318, -18.38911715685844683 ) ) ;
#38577=CARTESIAN_POINT ( 'NONE',  ( 126.3230600034150370, -9.125685433939677793, -16.10726513031420737 ) ) ;
#38578=CARTESIAN_POINT ( 'NONE',  ( 111.8886348109120092, -3.383040157471821630, -19.15922257007629170 ) ) ;
#38581=CARTESIAN_POINT ( 'NONE',  ( 119.7736414775786358, 0.1319031606808879209, -14.10382304977623669 ) ) ;
#38582=CARTESIAN_POINT ( 'NONE',  ( 112.1722681442453222, -8.899110576539710493, -16.42337572283490132 ) ) ;
#38586=CARTESIAN_POINT ( 'NONE',  ( 121.3393286996681866, -1.172797794773259072, -17.05961127468926719 ) ) ;
#38591=CARTESIAN_POINT ( 'NONE',  ( 112.6828081442453282, -7.893985811506177619, -18.51759400769804742 ) ) ;
#38592=CARTESIAN_POINT ( 'NONE',  ( 113.0231681442453322, 0.9020085738987339008, -11.91225656197089222 ) ) ;
#38593=CARTESIAN_POINT ( 'NONE',  ( 117.7314814775786260, -5.574606645277164318, -18.38911715685844683 ) ) ;
#38594=CARTESIAN_POINT ( 'NONE',  ( 114.1460714802850305, -3.929494816604741203, -18.62311481910882804 ) ) ;
#38596=CARTESIAN_POINT ( 'NONE',  ( 116.0864081442453113, -0.1624402480850797581, -16.17319339645315424 ) ) ;
#38600=CARTESIAN_POINT ( 'NONE',  ( 114.8951481442453115, -0.4660016031367893996, -10.09054647747474043 ) ) ;
#38601=VERTEX_POINT ( 'NONE', #473 ) ;
#38603=CARTESIAN_POINT ( 'NONE',  ( 116.9940348109119839, -9.988377603198976828, -10.36322818467138340 ) ) ;
#38606=CARTESIAN_POINT ( 'NONE',  ( 112.9097148109120070, 0.2603800115204892296, -16.42320221600525088 ) ) ;
#38607=CARTESIAN_POINT ( 'NONE',  ( 113.3068014775786594, -8.166667518702817929, -8.995218007635859436 ) ) ;
#38608=CARTESIAN_POINT ( 'NONE',  ( 124.5386814775786206, -4.153390946401325223, -8.397313243818185668 ) ) ;
#38614=CARTESIAN_POINT ( 'NONE',  ( 117.5045748109119756, -9.859900752359374465, -12.68260735090039404 ) ) ;
#38615=CARTESIAN_POINT ( 'NONE',  ( 111.2184548109119788, -8.862178061932382889, -16.39564131203247399 ) ) ;
#38619=CARTESIAN_POINT ( 'NONE',  ( 125.6732148109119862, 0.5811942927096110934, -14.16772938898807510 ) ) ;
#38621=CARTESIAN_POINT ( 'NONE',  ( 122.4965214775786251, -10.30919188438810075, -12.61870101168855918 ) ) ;
#38623=CARTESIAN_POINT ( 'NONE',  ( 116.3700414775786527, -5.638512984488999180, -18.83840828888717311 ) ) ;
#38625=CARTESIAN_POINT ( 'NONE',  ( 115.0653281442453277, -3.505236298600246325, -18.68346056562440793 ) ) ;
#38626=CARTESIAN_POINT ( 'NONE',  ( 126.0703014775786102, -9.988377603198980381, -10.36322818467138518 ) ) ;
#38628=CARTESIAN_POINT ( 'NONE',  ( 117.5613014775786525, 0.9020085738987339008, -11.91225656197089222 ) ) ;
#38629=CARTESIAN_POINT ( 'NONE',  ( 117.9016614775786280, -0.1624402480850797581, -16.17319339645315424 ) ) ;
#38631=CARTESIAN_POINT ( 'NONE',  ( 120.9081748109119872, -4.153390946401325223, -8.397313243818185668 ) ) ;
#38633=CARTESIAN_POINT ( 'NONE',  ( 116.7104014775786425, -0.4660016031367893996, -10.09054647747474043 ) ) ;
#38634=CARTESIAN_POINT ( 'NONE',  ( 136.5689201998072804, 0.8250495500204333421, -12.80989719292719009 ) ) ;
#38638=CARTESIAN_POINT ( 'NONE',  ( 126.4230588806227189, 0.2350761378584792227, -13.57469946490973989 ) ) ;
#38641=CARTESIAN_POINT ( 'NONE',  ( 114.1577014775786552, -6.344957434206662583, -7.627207830600332805 ) ) ;
#38643=CARTESIAN_POINT ( 'NONE',  ( 112.5693548109119888, 0.4262465694468514643, -12.03445270309931736 ) ) ;
#38648=CARTESIAN_POINT ( 'NONE',  ( 112.7962614775786676, -6.222761293078241884, -8.102969835052219238 ) ) ;
#38654=CARTESIAN_POINT ( 'NONE',  ( 115.6893214775786447, 0.5811942927096154232, -14.16772938898807155 ) ) ;
#38655=CARTESIAN_POINT ( 'NONE',  ( 123.8579614775786126, -9.859900752359378018, -12.68260735090039759 ) ) ;
#38656=CARTESIAN_POINT ( 'NONE',  ( 118.4689281442453392, -10.15424416112533912, -14.75197769757731336 ) ) ;
#38659=CARTESIAN_POINT ( 'NONE',  ( 123.5176014775786228, -9.261995988541697145, -16.69588392320189030 ) ) ;
#38661=CARTESIAN_POINT ( 'NONE',  ( 118.6958348109119754, -3.505236298600246325, -18.68346056562440793 ) ) ;
#38664=CARTESIAN_POINT ( 'NONE',  ( 113.7038881442453402, -6.222761293078241884, -8.102969835052219238 ) ) ;
#38667=CARTESIAN_POINT ( 'NONE',  ( 120.1140014775786398, -7.894159318335828068, -9.358103419637847864 ) ) ;
#38669=CARTESIAN_POINT ( 'NONE',  ( 118.7525614775786380, -1.833838273342659253, -17.42832698103878286 ) ) ;
#38670=CARTESIAN_POINT ( 'NONE',  ( 116.8238548109119819, -5.574606645277192740, -18.38911715685844328 ) ) ;
#38677=CARTESIAN_POINT ( 'NONE',  ( 116.4834948109119779, -1.561330072975668504, -17.79121239304076951 ) ) ;
#38678=CARTESIAN_POINT ( 'NONE',  ( 115.1787814775786387, -9.988377603198976828, -10.36322818467138340 ) ) ;
#38680=CARTESIAN_POINT ( 'NONE',  ( 113.3635281442453504, -9.988377603198976828, -10.36322818467138340 ) ) ;
#38685=CARTESIAN_POINT ( 'NONE',  ( 121.6456214775786293, -10.63000616557722466, -14.87417383870573495 ) ) ;
#38686=CARTESIAN_POINT ( 'NONE',  ( 116.8238548109119819, -4.089484607189486809, -7.948022111789456723 ) ) ;
#38687=CARTESIAN_POINT ( 'NONE',  ( 120.2841814775786276, -10.15424416112533912, -14.75197769757731336 ) ) ;
#38689=CARTESIAN_POINT ( 'NONE',  ( 125.4463081442452932, -5.638512984488999180, -18.83840828888717311 ) ) ;
#38690=CARTESIAN_POINT ( 'NONE',  ( 121.1350814775786233, 0.5811942927096110934, -14.16772938898807510 ) ) ;
#38693=CARTESIAN_POINT ( 'NONE',  ( 116.9940348109119839, -0.1624402480850797581, -16.17319339645315424 ) ) ;
#38695=ORIENTED_EDGE ( 'NONE', *, *, #10825, .T. ) ;
#38696=CARTESIAN_POINT ( 'NONE',  ( 123.1205148109119563, -1.834011780172310813, -8.268836392978581529 ) ) ;
#38698=CARTESIAN_POINT ( 'NONE',  ( 120.2274548109119934, 0.5811942927096110934, -14.16772938898807510 ) ) ;
#38703=CARTESIAN_POINT ( 'NONE',  ( 119.6784740574772457, -2.443475742715334853, -17.86549347949429389 ) ) ;
#38704=CARTESIAN_POINT ( 'NONE',  ( 114.2144281442453178, -1.833838273342658809, -17.42832698103878286 ) ) ;
#38706=CARTESIAN_POINT ( 'NONE',  ( 120.6812681442452941, 0.1319031606808879209, -14.10382304977623669 ) ) ;
#38708=CARTESIAN_POINT ( 'NONE',  ( 122.7801548109119665, -6.222761293078241884, -8.102969835052219238 ) ) ;
#38711=CARTESIAN_POINT ( 'NONE',  ( 120.3409081442453044, -8.899110576539710493, -16.42337572283490132 ) ) ;
#38713=CARTESIAN_POINT ( 'NONE',  ( 115.5191414775786569, -3.383040157471821630, -19.15922257007629170 ) ) ;
#38714=CARTESIAN_POINT ( 'NONE',  ( 112.7395348109119766, -5.638512984488999180, -18.83840828888717311 ) ) ;
#38716=CARTESIAN_POINT ( 'NONE',  ( 119.3765548109119834, -10.15424416112533912, -14.75197769757731336 ) ) ;
#38718=CARTESIAN_POINT ( 'NONE',  ( 115.7460481442453357, 0.9020085738987339008, -11.91225656197089222 ) ) ;
#38723=CARTESIAN_POINT ( 'NONE',  ( 124.2550481442452792, -9.988377603198980381, -10.36322818467138518 ) ) ;
#38725=CARTESIAN_POINT ( 'NONE',  ( 126.5561942423852315, -8.491916856930616930, -9.711375107224954562 ) ) ;
#38726=CARTESIAN_POINT ( 'NONE',  ( 121.3619881442452879, -5.574606645277164318, -18.38911715685844683 ) ) ;
#38734=CARTESIAN_POINT ( 'NONE',  ( 116.2565881442452991, -9.261995988541697145, -16.69588392320189030 ) ) ;
#38735=AXIS2_PLACEMENT_3D ( 'NONE', #16894, #41294, #3192 ) ;
#38736=CARTESIAN_POINT ( 'NONE',  ( 125.2194014775786286, 0.1319031606808879209, -14.10382304977623669 ) ) ;
#38737=CARTESIAN_POINT ( 'NONE',  ( 124.0281414775786146, -1.834011780172310813, -8.268836392978581529 ) ) ;
#38739=CARTESIAN_POINT ( 'NONE',  ( 119.4900081442453086, -7.643976991954077427, -18.09477374809248928 ) ) ;
#38740=CARTESIAN_POINT ( 'NONE',  ( 126.2275303246277502, -4.044442676264679015, -8.456153826979251775 ) ) ;
#38741=CARTESIAN_POINT ( 'NONE',  ( 124.0848681442452772, -4.089484607189486809, -7.948022111789456723 ) ) ;
#38742=CARTESIAN_POINT ( 'NONE',  ( 111.8424481442453242, -6.210324830718715994, -8.151390318758327425 ) ) ;
#38747=VERTEX_POINT ( 'NONE', #44242 ) ;
#38749=CARTESIAN_POINT ( 'NONE',  ( 120.0005481442453146, -5.638512984488999180, -18.83840828888717311 ) ) ;
#38751=CARTESIAN_POINT ( 'NONE',  ( 136.7478768735732046, -8.464786658626188398, -17.71247759265823873 ) ) ;
#38754=CARTESIAN_POINT ( 'NONE',  ( 122.7801548109119665, -3.383040157471821630, -19.15922257007629170 ) ) ;
#38756=CARTESIAN_POINT ( 'NONE',  ( 123.5743281442453139, -2.084020599724406786, -8.691656652584148546 ) ) ;
#38758=CARTESIAN_POINT ( 'NONE',  ( 113.8740681442453138, 0.5811942927096154232, -14.16772938898807155 ) ) ;
#38763=CARTESIAN_POINT ( 'NONE',  ( 111.4348214775786801, -3.505236298600246325, -18.68346056562440793 ) ) ;
#38767=CARTESIAN_POINT ( 'NONE',  ( 123.4608748109119745, -10.63000616557722466, -14.87417383870573495 ) ) ;
#38768=CARTESIAN_POINT ( 'NONE',  ( 122.2128881442453263, -1.834011780172310813, -8.268836392978581529 ) ) ;
#38769=CARTESIAN_POINT ( 'NONE',  ( 123.8012348109119642, -9.565557343593413364, -10.61323700422348004 ) ) ;
#38770=CARTESIAN_POINT ( 'NONE',  ( 120.7379948109119709, 0.4262465694468514643, -12.03445270309931736 ) ) ;
#38771=CARTESIAN_POINT ( 'NONE',  ( 125.6626748109119802, -9.522524984348629928, -10.63868154973292768 ) ) ;
#38772=CARTESIAN_POINT ( 'NONE',  ( 117.3343948109119737, -3.383040157471821630, -19.15922257007629170 ) ) ;
#38781=CARTESIAN_POINT ( 'NONE',  ( 125.5030348109119558, -3.383040157471821630, -19.15922257007629170 ) ) ;
#38782=CARTESIAN_POINT ( 'NONE',  ( 124.9924948109119924, -5.574606645277164318, -18.38911715685844683 ) ) ;
#38784=CARTESIAN_POINT ( 'NONE',  ( 112.5126281442453120, 0.1319031606808879209, -14.10382304977623669 ) ) ;
#38788=CARTESIAN_POINT ( 'NONE',  ( 123.0637881442452937, -0.4660016031367893996, -10.09054647747474043 ) ) ;
#38790=CARTESIAN_POINT ( 'NONE',  ( 114.4980614775786592, -7.893985811506177619, -18.51759400769804742 ) ) ;
#38795=CARTESIAN_POINT ( 'NONE',  ( 116.0864081442453113, -0.1624402480850797581, -16.17319339645315424 ) ) ;
#38797=CARTESIAN_POINT ( 'NONE',  ( 113.9307948109119906, 0.9020085738987339008, -11.91225656197089222 ) ) ;
#38799=CARTESIAN_POINT ( 'NONE',  ( 113.0231681442453322, 0.9020085738987339008, -11.91225656197089222 ) ) ;
#38800=CARTESIAN_POINT ( 'NONE',  ( 118.3554748109119856, -9.565557343593388495, -10.61323700422345162 ) ) ;
#38802=CARTESIAN_POINT ( 'NONE',  ( 121.3052614775786111, -7.643976991954077427, -18.09477374809248928 ) ) ;
#38803=CARTESIAN_POINT ( 'NONE',  ( 125.8433948109119456, -1.834011780172310813, -8.268836392978581529 ) ) ;
#38809=CARTESIAN_POINT ( 'NONE',  ( 113.5904348109119866, -2.084020599724406786, -8.691656652584148546 ) ) ;
#38814=CARTESIAN_POINT ( 'NONE',  ( 122.7801548109119665, -6.222761293078241884, -8.102969835052219238 ) ) ;
#38816=CARTESIAN_POINT ( 'NONE',  ( 117.5613014775786525, -10.15424416112533912, -14.75197769757731336 ) ) ;
#38817=CARTESIAN_POINT ( 'NONE',  ( 117.6747548109119919, -7.643976991954077427, -18.09477374809248928 ) ) ;
#38826=CARTESIAN_POINT ( 'NONE',  ( 111.9453614775786434, -1.561330072975668060, -17.79121239304076596 ) ) ;
#38827=CARTESIAN_POINT ( 'NONE',  ( 126.1837548109119496, 0.4262465694468514643, -12.03445270309931736 ) ) ;
#38828=CARTESIAN_POINT ( 'NONE',  ( 117.9583881442453048, 0.1319031606808879209, -14.10382304977623669 ) ) ;
#38829=CARTESIAN_POINT ( 'NONE',  ( 138.2184548109119930, 2.066246953222917959, -14.37896053134723040 ) ) ;
#38831=CARTESIAN_POINT ( 'NONE',  ( 114.6115148109119986, -6.222761293078241884, -8.102969835052219238 ) ) ;
#38836=CARTESIAN_POINT ( 'NONE',  ( 114.1577014775786552, -6.344957434206662583, -7.627207830600332805 ) ) ;
#38838=CARTESIAN_POINT ( 'NONE',  ( 118.3554748109119998, 0.2603800115204892296, -16.42320221600525088 ) ) ;
#38841=CARTESIAN_POINT ( 'NONE',  ( 114.2711548109119803, -9.988377603198976828, -10.36322818467138340 ) ) ;
#38842=CARTESIAN_POINT ( 'NONE',  ( 115.2922348109119781, -10.63000616557722466, -14.87417383870573495 ) ) ;
#38843=CARTESIAN_POINT ( 'NONE',  ( 127.0264730702700433, -10.25983759373953319, -13.69028692805868452 ) ) ;
#38846=B_SPLINE_CURVE_WITH_KNOTS ( 'NONE', 3,
 ( #32142, #39215, #14830, #21887, #42645, #35783, #4552, #18478, #32367, #1134, #15052, #12761, #9560, #19590, #44449, #37124, #26885, #40346, #40804, #12989, #23476, #13216, #37362, #20053, #5672, #26661, #9795, #22782, #33471, #2251 ),
 .UNSPECIFIED., .F., .F.,
 ( 4, 2, 2, 1, 1, 1, 2, 2, 2, 1, 1, 1, 2, 2, 1, 1, 2, 2, 4 ),
 ( 0.000000000000000000, 0.2499999999998695488, 0.3749999999997916111, 0.4374999999997516986, 0.4687499999997186140, 0.4843749999996893041, 0.4921874999996895261, 0.4999999999996898037, 0.6249999999999032996, 0.6875000000000216493, 0.7187500000000807132, 0.7343750000000988098, 0.7421875000001069145, 0.7500000000001149081, 0.8125000000000915934, 0.8437500000000796030, 0.8593750000000660583, 0.8750000000000524025, 1.000000000000000000 ),
 .UNSPECIFIED. ) ;
#38848=CARTESIAN_POINT ( 'NONE',  ( 112.3058127483929383, -2.423081321603721694, -17.89265170041262465 ) ) ;
#38850=CARTESIAN_POINT ( 'NONE',  ( 115.2922348109119781, 0.4262465694468514643, -12.03445270309931736 ) ) ;
#38853=CARTESIAN_POINT ( 'NONE',  ( 118.0151148109119816, -10.63000616557722111, -14.87417383870573850 ) ) ;
#38855=CARTESIAN_POINT ( 'NONE',  ( 127.0915067942480192, -5.196864950038682984, -7.966870886606466584 ) ) ;
#38856=CARTESIAN_POINT ( 'NONE',  ( 115.6325948109119821, -9.565557343593413364, -10.61323700422348004 ) ) ;
#38858=CARTESIAN_POINT ( 'NONE',  ( 125.7299414775786346, 0.9020085738987339008, -11.91225656197089222 ) ) ;
#38859=CARTESIAN_POINT ( 'NONE',  ( 115.8595014775786609, -1.834011780172310813, -8.268836392978581529 ) ) ;
#38860=ORIENTED_EDGE ( 'NONE', *, *, #2161, .T. ) ;
#38861=CARTESIAN_POINT ( 'NONE',  ( 115.2922348109119781, 0.4262465694468514643, -12.03445270309931736 ) ) ;
#38862=CARTESIAN_POINT ( 'NONE',  ( 112.0588148109119828, 0.5811942927096154232, -14.16772938898807155 ) ) ;
#38863=CARTESIAN_POINT ( 'NONE',  ( 117.3343948109119737, -3.383040157471821630, -19.15922257007629170 ) ) ;
#38864=CARTESIAN_POINT ( 'NONE',  ( 117.8449348109119938, -1.833838273342659253, -17.42832698103878286 ) ) ;
#38866=CARTESIAN_POINT ( 'NONE',  ( 122.3263414775786373, -3.505236298600246325, -18.68346056562440793 ) ) ;
#38868=CARTESIAN_POINT ( 'NONE',  ( 116.7671281442453335, -1.834011780172310813, -8.268836392978581529 ) ) ;
#38874=CARTESIAN_POINT ( 'NONE',  ( 112.9664414775786412, 0.5811942927096154232, -14.16772938898807155 ) ) ;
#38876=CARTESIAN_POINT ( 'NONE',  ( 115.2922348109119781, 0.4262465694468514643, -12.03445270309931736 ) ) ;
#38880=CARTESIAN_POINT ( 'NONE',  ( 114.4413348109119823, -0.8288870151387760510, -10.36305467784173118 ) ) ;
#38885=CARTESIAN_POINT ( 'NONE',  ( 119.6601881442453106, -8.166667518702819706, -8.995218007635861213 ) ) ;
#38886=CARTESIAN_POINT ( 'NONE',  ( 123.4041481442452834, 0.1319031606808879209, -14.10382304977623669 ) ) ;
#38887=CARTESIAN_POINT ( 'NONE',  ( 117.6180281442453150, -8.899110576539710493, -16.42337572283490132 ) ) ;
#38888=CARTESIAN_POINT ( 'NONE',  ( 113.2500748109119968, -3.505236298600246325, -18.68346056562440793 ) ) ;
#38890=CARTESIAN_POINT ( 'NONE',  ( 137.5082292857711650, -8.089093314163772419, -9.561117199659015853 ) ) ;
#38891=CARTESIAN_POINT ( 'NONE',  ( 123.0070614775786169, 0.9020085738987339008, -11.91225656197089222 ) ) ;
#38893=CARTESIAN_POINT ( 'NONE',  ( 118.7525614775786380, -1.833838273342659253, -17.42832698103878286 ) ) ;
#38894=CARTESIAN_POINT ( 'NONE',  ( 114.6115148109119986, -6.222761293078241884, -8.102969835052219238 ) ) ;
#38897=CARTESIAN_POINT ( 'NONE',  ( 120.0572748109119772, -6.222761293078241884, -8.102969835052219238 ) ) ;
#38898=CARTESIAN_POINT ( 'NONE',  ( 124.3117748109119844, 0.1319031606808879209, -14.10382304977623669 ) ) ;
#38904=CARTESIAN_POINT ( 'NONE',  ( 118.3554748109119998, 0.2603800115204892296, -16.42320221600525088 ) ) ;
#38905=CARTESIAN_POINT ( 'NONE',  ( 114.5547881442453217, -5.638512984488999180, -18.83840828888717311 ) ) ;
#38907=CARTESIAN_POINT ( 'NONE',  ( 114.3278814775786429, -10.30919188438810075, -12.61870101168855918 ) ) ;
#38911=CARTESIAN_POINT ( 'NONE',  ( 123.9146881442452894, 0.9020085738987339008, -11.91225656197089222 ) ) ;
#38912=CARTESIAN_POINT ( 'NONE',  ( 115.0086014775786509, -4.089484607189486809, -7.948022111789456723 ) ) ;
#38913=CARTESIAN_POINT ( 'NONE',  ( 122.0994348109119443, -10.15424416112533912, -14.75197769757731336 ) ) ;
#38914=PRODUCT_CONTEXT ( 'NONE', #23025, 'mechanical' ) ;
#38915=CARTESIAN_POINT ( 'NONE',  ( 124.3685014775786328, -10.63000616557722466, -14.87417383870573495 ) ) ;
#38916=CARTESIAN_POINT ( 'NONE',  ( 122.3830681442452857, -8.166667518702819706, -8.995218007635861213 ) ) ;
#38917=VECTOR ( 'NONE', #7532, 1000.000000000000000 ) ;
#38920=CARTESIAN_POINT ( 'NONE',  ( 115.1787814775786387, -0.1624402480850797581, -16.17319339645315424 ) ) ;
#38923=CARTESIAN_POINT ( 'NONE',  ( 121.0216281442452981, -1.561330072975668948, -17.79121239304076951 ) ) ;
#38925=CARTESIAN_POINT ( 'NONE',  ( 117.7314814775786260, -4.089484607189486809, -7.948022111789456723 ) ) ;
#38930=CARTESIAN_POINT ( 'NONE',  ( 117.2776681442452968, -4.153390946401321671, -8.397313243818183892 ) ) ;
#38931=EDGE_CURVE ( 'NONE', #38146, #1246, #9808, .T. ) ;
#38932=CARTESIAN_POINT ( 'NONE',  ( 127.5515731338752516, -0.8914282735556431359, -17.43429686027660352 ) ) ;
#38935=CARTESIAN_POINT ( 'NONE',  ( 118.4689281442453250, -10.15424416112533912, -14.75197769757731336 ) ) ;
#38938=CARTESIAN_POINT ( 'NONE',  ( 121.8618404811916918, -3.807985514183269693, -19.09877912889401230 ) ) ;
#38939=CARTESIAN_POINT ( 'NONE',  ( 120.2274548109119934, -9.859900752359378018, -12.68260735090039759 ) ) ;
#38941=CARTESIAN_POINT ( 'NONE',  ( 128.2184548109119930, -4.863998795839242995, -13.39321520033831447 ) ) ;
#38942=CARTESIAN_POINT ( 'NONE',  ( 119.4900081442453086, -7.643976991954077427, -18.09477374809248928 ) ) ;
#38943=CARTESIAN_POINT ( 'NONE',  ( 113.6471614775786492, -5.638512984488999180, -18.83840828888717311 ) ) ;
#38944=CARTESIAN_POINT ( 'NONE',  ( 118.7525614775786380, -8.166667518702819706, -8.995218007635861213 ) ) ;
#38945=CARTESIAN_POINT ( 'NONE',  ( 113.3068014775786594, -8.166667518702817929, -8.995218007635859436 ) ) ;
#38948=CARTESIAN_POINT ( 'NONE',  ( 121.6456214775786293, 0.4262465694468514643, -12.03445270309931736 ) ) ;
#38949=EDGE_LOOP ( 'NONE', ( #3234, #26791, #20167, #13659 ) ) ;
#38950=CARTESIAN_POINT ( 'NONE',  ( 115.6325948109119821, 0.2603800115204892296, -16.42320221600525088 ) ) ;
#38955=CARTESIAN_POINT ( 'NONE',  ( 125.0492214775786266, -6.344957434206665248, -7.627207830600338134 ) ) ;
#38957=CARTESIAN_POINT ( 'NONE',  ( 126.3243314201095160, -8.199742859958636387, -9.597805110430360997 ) ) ;
#38958=CARTESIAN_POINT ( 'NONE',  ( 121.1918081442452859, -10.15424416112533912, -14.75197769757731336 ) ) ;
#38965=CARTESIAN_POINT ( 'NONE',  ( 115.8027748109119841, -0.4660016031367893996, -10.09054647747474043 ) ) ;
#38966=CARTESIAN_POINT ( 'NONE',  ( 114.2711548109119803, -9.988377603198976828, -10.36322818467138340 ) ) ;
#38968=CARTESIAN_POINT ( 'NONE',  ( 121.7023481442452919, -0.8288870151387760510, -10.36305467784173118 ) ) ;
#38970=CARTESIAN_POINT ( 'NONE',  ( 123.5743281442453139, -7.893985811506177619, -18.51759400769804742 ) ) ;
#38971=CARTESIAN_POINT ( 'NONE',  ( 111.2646414775786496, -8.899110576539710493, -16.42337572283490132 ) ) ;
#38972=CARTESIAN_POINT ( 'NONE',  ( 118.7315769107182177, -2.467220198592778413, -17.83387418641524391 ) ) ;
#38974=ADVANCED_FACE ( 'NONE', ( #7478 ), #471, .T. ) ;
#38980=CARTESIAN_POINT ( 'NONE',  ( 120.6812681442452941, -10.30919188438810075, -12.61870101168855918 ) ) ;
#38981=CARTESIAN_POINT ( 'NONE',  ( 137.5098831408920717, -8.939295190008330394, -16.29222226817870123 ) ) ;
#38983=CARTESIAN_POINT ( 'NONE',  ( 136.9012041053448172, 0.1731349627440442185, -11.10994756160400954 ) ) ;
#38984=CARTESIAN_POINT ( 'NONE',  ( 124.9924948109119924, -4.089484607189486809, -7.948022111789456723 ) ) ;
#38986=DIRECTION ( 'NONE',  ( 0.000000000000000000, 0.6004852223388321697, -0.7996358532186279566 ) ) ;
#38987=CARTESIAN_POINT ( 'NONE',  ( 123.8579614775786126, -9.859900752359378018, -12.68260735090039759 ) ) ;
#38988=ORIENTED_EDGE ( 'NONE', *, *, #9323, .T. ) ;
#38989=CARTESIAN_POINT ( 'NONE',  ( 113.3068014775786594, -8.166667518702817929, -8.995218007635859436 ) ) ;
#38995=CARTESIAN_POINT ( 'NONE',  ( 135.4522060580519849, -5.622586528377011561, -7.441387646177292758 ) ) ;
#38996=CARTESIAN_POINT ( 'NONE',  ( 124.2550481442452792, -9.988377603198980381, -10.36322818467138518 ) ) ;
#38997=CARTESIAN_POINT ( 'NONE',  ( 111.7184548109119788, -8.862178061932382889, -16.39564131203247399 ) ) ;
#39000=CARTESIAN_POINT ( 'NONE',  ( 121.9292548109119849, -1.561330072975668948, -17.79121239304076951 ) ) ;
#39001=CARTESIAN_POINT ( 'NONE',  ( 121.0783548109119749, 0.2603800115204892296, -16.42320221600525088 ) ) ;
#39002=CARTESIAN_POINT ( 'NONE',  ( 124.7088614775786226, -9.565557343593413364, -10.61323700422348004 ) ) ;
#39004=CARTESIAN_POINT ( 'NONE',  ( 123.6310548109119765, -4.153390946401325223, -8.397313243818185668 ) ) ;
#39006=CARTESIAN_POINT ( 'NONE',  ( 121.0783548109119749, 0.2603800115204892296, -16.42320221600525088 ) ) ;
#39007=VERTEX_POINT ( 'NONE', #42603 ) ;
#39008=VERTEX_POINT ( 'NONE', #11369 ) ;
#39009=CARTESIAN_POINT ( 'NONE',  ( 122.4013540574772492, -2.443475742715334853, -17.86549347949429389 ) ) ;
#39014=CARTESIAN_POINT ( 'NONE',  ( 126.1837548109119211, -10.63000616557722466, -14.87417383870573495 ) ) ;
#39015=CARTESIAN_POINT ( 'NONE',  ( 126.6375681442452930, -10.15424416112533912, -14.75197769757731336 ) ) ;
#39017=CARTESIAN_POINT ( 'NONE',  ( 112.2289948109119848, -7.643976991954077427, -18.09477374809248928 ) ) ;
#39020=CARTESIAN_POINT ( 'NONE',  ( 125.7299414775786346, 0.9020085738987339008, -11.91225656197089222 ) ) ;
#39023=CARTESIAN_POINT ( 'NONE',  ( 117.8449348109119938, -8.166667518702817929, -8.995218007635861213 ) ) ;
#39028=CARTESIAN_POINT ( 'NONE',  ( 116.7104014775786425, -8.899110576539710493, -16.42337572283490132 ) ) ;
#39029=CARTESIAN_POINT ( 'NONE',  ( 117.1642148109119859, -9.261995988541697145, -16.69588392320189030 ) ) ;
#39031=CARTESIAN_POINT ( 'NONE',  ( 112.7962614775786676, -3.383040157471821630, -19.15922257007629170 ) ) ;
#39032=CARTESIAN_POINT ( 'NONE',  ( 124.8790414775786246, -8.899110576539710493, -16.42337572283490132 ) ) ;
#39033=CARTESIAN_POINT ( 'NONE',  ( 120.7947214775786193, -0.8288870151387760510, -10.36305467784173118 ) ) ;
#39034=CARTESIAN_POINT ( 'NONE',  ( 116.8238548109119819, -5.574606645277164318, -18.38911715685844683 ) ) ;
#39039=CARTESIAN_POINT ( 'NONE',  ( 116.5402214775786405, -9.565557343593413364, -10.61323700422348004 ) ) ;
#39043=CARTESIAN_POINT ( 'NONE',  ( 111.9453614775786434, -1.561330072975668060, -17.79121239304076596 ) ) ;
#39045=CARTESIAN_POINT ( 'NONE',  ( 113.1366214775786432, -7.643976991954077427, -18.09477374809248928 ) ) ;
#39049=CARTESIAN_POINT ( 'NONE',  ( 118.6958348109119754, -3.505236298600246325, -18.68346056562440793 ) ) ;
#39050=CARTESIAN_POINT ( 'NONE',  ( 119.0361948109119652, -2.084020599724406786, -8.691656652584148546 ) ) ;
#39055=DIRECTION ( 'NONE',  ( 1.000000000000000000, 0.000000000000000000, 0.000000000000000000 ) ) ;
#39058=CARTESIAN_POINT ( 'NONE',  ( 113.4769814775786330, -10.63000616557722466, -14.87417383870573495 ) ) ;
#39060=CARTESIAN_POINT ( 'NONE',  ( 111.8319081442453182, -5.638512984488999180, -18.83840828888717311 ) ) ;
#39062=CARTESIAN_POINT ( 'NONE',  ( 117.1642148109119859, -0.8288870151387760510, -10.36305467784173118 ) ) ;
#39065=CARTESIAN_POINT ( 'NONE',  ( 116.8805814775786445, -3.505236298600246325, -18.68346056562440793 ) ) ;
#39070=CARTESIAN_POINT ( 'NONE',  ( 113.3068014775786594, -8.166667518702817929, -8.995218007635859436 ) ) ;
#39072=CARTESIAN_POINT ( 'NONE',  ( 118.2987481442453088, -1.561330072975668504, -17.79121239304076951 ) ) ;
#39075=CARTESIAN_POINT ( 'NONE',  ( 118.1852948109119836, -5.638512984488999180, -18.83840828888717311 ) ) ;
#39076=CARTESIAN_POINT ( 'NONE',  ( 114.6682414775786469, -1.561330072975668060, -17.79121239304076596 ) ) ;
#39077=CARTESIAN_POINT ( 'NONE',  ( 125.7299414775786346, -10.15424416112533912, -14.75197769757731336 ) ) ;
#39084=CARTESIAN_POINT ( 'NONE',  ( 115.8027748109119841, -8.899110576539710493, -16.42337572283490132 ) ) ;
#39089=CARTESIAN_POINT ( 'NONE',  ( 114.6115148109119986, -6.222761293078241884, -8.102969835052219238 ) ) ;
#39091=CARTESIAN_POINT ( 'NONE',  ( 123.8012348109119642, 0.2603800115204892296, -16.42320221600525088 ) ) ;
#39092=CARTESIAN_POINT ( 'NONE',  ( 121.5888948109119809, -10.30919188438810075, -12.61870101168855918 ) ) ;
#39094=CARTESIAN_POINT ( 'NONE',  ( 117.2209414775786485, -2.084020599724406786, -8.691656652584148546 ) ) ;
#39096=CARTESIAN_POINT ( 'NONE',  ( 118.4122014775786340, 0.5811942927096110934, -14.16772938898807510 ) ) ;
#39097=CARTESIAN_POINT ( 'NONE',  ( 120.4543614775786295, -5.574606645277164318, -18.38911715685844683 ) ) ;
#39099=CARTESIAN_POINT ( 'NONE',  ( 121.9859814775786333, -9.565557343593413364, -10.61323700422348004 ) ) ;
#39100=CARTESIAN_POINT ( 'NONE',  ( 118.6391081442452986, -4.089484607189486809, -7.948022111789456723 ) ) ;
#39101=CARTESIAN_POINT ( 'NONE',  ( 136.6523348889540443, 0.4072479916814358836, -15.49606817166481321 ) ) ;
#39105=CARTESIAN_POINT ( 'NONE',  ( 127.7425183523501744, 0.8652765085452543969, -12.77968882490997338 ) ) ;
#39108=CARTESIAN_POINT ( 'NONE',  ( 114.2711548109119803, -9.988377603198976828, -10.36322818467138340 ) ) ;
#39111=CARTESIAN_POINT ( 'NONE',  ( 116.2565881442453133, -0.8288870151387760510, -10.36305467784173118 ) ) ;
#39116=CARTESIAN_POINT ( 'NONE',  ( 122.1057533359170293, -2.311015703046761072, -18.04188382666269774 ) ) ;
#39120=CARTESIAN_POINT ( 'NONE',  ( 120.3976348109119812, -1.834011780172310813, -8.268836392978581529 ) ) ;
#39121=CARTESIAN_POINT ( 'NONE',  ( 118.1852948109119836, -4.153390946401325223, -8.397313243818185668 ) ) ;
#39122=CARTESIAN_POINT ( 'NONE',  ( 111.4348214775786801, -3.505236298600246325, -18.68346056562440793 ) ) ;
#39125=CARTESIAN_POINT ( 'NONE',  ( 124.5954081442453116, -3.383040157471821630, -19.15922257007629170 ) ) ;
#39127=CARTESIAN_POINT ( 'NONE',  ( 118.9794681442453026, -0.8288870151387760510, -10.36305467784173118 ) ) ;
#39128=CARTESIAN_POINT ( 'NONE',  ( 116.8805814775786445, -3.505236298600246325, -18.68346056562440793 ) ) ;
#39131=CARTESIAN_POINT ( 'NONE',  ( 119.0361948109119652, -2.084020599724406786, -8.691656652584148546 ) ) ;
#39132=CARTESIAN_POINT ( 'NONE',  ( 124.2550481442452792, -0.1624402480850797581, -16.17319339645315424 ) ) ;
#39133=CARTESIAN_POINT ( 'NONE',  ( 114.2827848082056050, -0.1020945015694959546, -15.74893487844866691 ) ) ;
#39141=CARTESIAN_POINT ( 'NONE',  ( 119.3198281442452924, 0.5811942927096110934, -14.16772938898807510 ) ) ;
#39142=CARTESIAN_POINT ( 'NONE',  ( 119.4900081442453086, -1.834011780172310813, -8.268836392978581529 ) ) ;
#39144=CARTESIAN_POINT ( 'NONE',  ( 112.8529881442453302, -1.561330072975668060, -17.79121239304076596 ) ) ;
#39146=CARTESIAN_POINT ( 'NONE',  ( 117.3320321015961412, -1.040089454026966287, -17.23633227186632766 ) ) ;
#39147=CARTESIAN_POINT ( 'NONE',  ( 115.9729548109119861, -6.344957434206662583, -7.627207830600332805 ) ) ;
#39148=CARTESIAN_POINT ( 'NONE',  ( 121.9859814775786333, -9.565557343593413364, -10.61323700422348004 ) ) ;
#39150=CARTESIAN_POINT ( 'NONE',  ( 125.7299414775786346, 0.9020085738987339008, -11.91225656197089222 ) ) ;
#39151=CARTESIAN_POINT ( 'NONE',  ( 120.6812681442452941, -10.30919188438810075, -12.61870101168855918 ) ) ;
#39154=CARTESIAN_POINT ( 'NONE',  ( 117.1074881442453233, 0.4262465694468514643, -12.03445270309931736 ) ) ;
#39159=CARTESIAN_POINT ( 'NONE',  ( 118.8660148109119774, -10.30919188438810075, -12.61870101168855918 ) ) ;
#39160=VERTEX_POINT ( 'NONE', #5410 ) ;
#39165=CARTESIAN_POINT ( 'NONE',  ( 117.2209414775786485, -2.084020599724406786, -8.691656652584148546 ) ) ;
#39168=CARTESIAN_POINT ( 'NONE',  ( 120.7379948109119709, 0.4262465694468514643, -12.03445270309931736 ) ) ;
#39170=CARTESIAN_POINT ( 'NONE',  ( 121.0216281442452981, -7.894159318335828068, -9.358103419637847864 ) ) ;
#39172=CARTESIAN_POINT ( 'NONE',  ( 122.8368814775786291, -7.894159318335828068, -9.358103419637847864 ) ) ;
#39173=CARTESIAN_POINT ( 'NONE',  ( 113.5904348109119866, -7.893985811506177619, -18.51759400769804742 ) ) ;
#39174=CARTESIAN_POINT ( 'NONE',  ( 118.8660148109119774, -10.30919188438810075, -12.61870101168855918 ) ) ;
#39175=CARTESIAN_POINT ( 'NONE',  ( 125.6732148109119862, -9.859900752359378018, -12.68260735090039759 ) ) ;
#39177=CARTESIAN_POINT ( 'NONE',  ( 119.4900081442453086, -7.643976991954077427, -18.09477374809248928 ) ) ;
#39179=CARTESIAN_POINT ( 'NONE',  ( 121.9859814775786333, 0.2603800115204892296, -16.42320221600525088 ) ) ;
#39181=CARTESIAN_POINT ( 'NONE',  ( 115.7460481442453215, -10.15424416112534267, -14.75197769757730804 ) ) ;
#39184=CARTESIAN_POINT ( 'NONE',  ( 125.6164881442453094, 0.2603800115204892296, -16.42320221600525088 ) ) ;
#39185=EDGE_LOOP ( 'NONE', ( #42163, #25542, #14833, #26152 ) ) ;
#39187=CARTESIAN_POINT ( 'NONE',  ( 120.1707281442453166, -9.565557343593413364, -10.61323700422348004 ) ) ;
#39193=CARTESIAN_POINT ( 'NONE',  ( 115.3489614775786407, -9.261995988541697145, -16.69588392320189030 ) ) ;
#39194=CARTESIAN_POINT ( 'NONE',  ( 113.3068014775786594, -8.166667518702817929, -8.995218007635859436 ) ) ;
#39196=CARTESIAN_POINT ( 'NONE',  ( 120.7947214775786193, -0.8288870151387760510, -10.36305467784173118 ) ) ;
#39198=CARTESIAN_POINT ( 'NONE',  ( 127.7429221096697489, -2.658770238890374227, -8.068785233703032134 ) ) ;
#39200=CARTESIAN_POINT ( 'NONE',  ( 122.0994348109119443, 0.9020085738987339008, -11.91225656197089222 ) ) ;
#39201=CARTESIAN_POINT ( 'NONE',  ( 112.0588148109119828, -9.859900752359374465, -12.68260735090039404 ) ) ;
#39208=CARTESIAN_POINT ( 'NONE',  ( 121.8725281442453223, -3.383040157471821630, -19.15922257007629170 ) ) ;
#39209=CARTESIAN_POINT ( 'NONE',  ( 137.4282737236245850, -9.220636156388909654, -16.02682550729275235 ) ) ;
#39212=CARTESIAN_POINT ( 'NONE',  ( 111.8319081442453182, -5.638512984488999180, -18.83840828888717311 ) ) ;
#39213=B_SPLINE_CURVE_WITH_KNOTS ( 'NONE', 3,
 ( #31992, #7154, #14677, #42273, #10594, #754, #10813, #27700, #24938, #21064 ),
 .UNSPECIFIED., .F., .F.,
 ( 4, 3, 3, 4 ),
 ( 0.000000000000000000, 1.701546542203679946E-05, 3.403093084406070369E-05, 6.582972837196660498E-05 ),
 .UNSPECIFIED. ) ;
#39214=CARTESIAN_POINT ( 'NONE',  ( 112.6828081442453282, -2.084020599724406786, -8.691656652584148546 ) ) ;
#39215=CARTESIAN_POINT ( 'NONE',  ( 127.9806007748782690, -4.168156794478616867, -19.23317562329109265 ) ) ;
#39216=CARTESIAN_POINT ( 'NONE',  ( 123.2906948109119867, -1.833838273342659697, -17.42832698103878286 ) ) ;
#39218=CARTESIAN_POINT ( 'NONE',  ( 117.1074881442453233, -10.63000616557722466, -14.87417383870573495 ) ) ;
#39221=CARTESIAN_POINT ( 'NONE',  ( 137.2528433483945491, -4.978162001089776467, -8.133589847931153471 ) ) ;
#39222=CARTESIAN_POINT ( 'NONE',  ( 111.3213681442453264, -7.643976991954077427, -18.09477374809248928 ) ) ;
#39226=CARTESIAN_POINT ( 'NONE',  ( 121.8158014775786171, -5.638512984488999180, -18.83840828888717311 ) ) ;
#39227=CARTESIAN_POINT ( 'NONE',  ( 123.1205148109119563, -7.643976991954077427, -18.09477374809248928 ) ) ;
#39229=CARTESIAN_POINT ( 'NONE',  ( 124.0281414775786146, -7.643976991954077427, -18.09477374809248928 ) ) ;
#39231=CARTESIAN_POINT ( 'NONE',  ( 119.6034614775786196, -6.344957434206665248, -7.627207830600338134 ) ) ;
#39233=ORIENTED_EDGE ( 'NONE', *, *, #36815, .T. ) ;
#39234=CARTESIAN_POINT ( 'NONE',  ( 126.5041214912249217, -8.563610148337030381, -16.96555754258860205 ) ) ;
#39239=CARTESIAN_POINT ( 'NONE',  ( 125.7866681442453256, -8.899110576539117190, -16.42337572283568647 ) ) ;
#39240=CARTESIAN_POINT ( 'NONE',  ( 113.7038881442453402, -3.383040157471821630, -19.15922257007629170 ) ) ;
#39242=CARTESIAN_POINT ( 'NONE',  ( 113.1933481442453058, -5.574606645277164318, -18.38911715685844683 ) ) ;
#39248=CARTESIAN_POINT ( 'NONE',  ( 116.5969481442453031, 0.5811942927096154232, -14.16772938898807155 ) ) ;
#39252=ORIENTED_EDGE ( 'NONE', *, *, #26706, .F. ) ;
#39253=CARTESIAN_POINT ( 'NONE',  ( 126.2275303246277502, -7.775514682367814956, -9.322671934392364079 ) ) ;
#39254=CARTESIAN_POINT ( 'NONE',  ( 118.3554748109119998, -9.565557343593413364, -10.61323700422348004 ) ) ;
#39255=CARTESIAN_POINT ( 'NONE',  ( 115.1220548109119761, -8.166667518702817929, -8.995218007635861213 ) ) ;
#39258=CARTESIAN_POINT ( 'NONE',  ( 125.5597614775786326, -7.894159318335828068, -9.358103419637847864 ) ) ;
#39260=CARTESIAN_POINT ( 'NONE',  ( 120.4543614775786295, -5.574606645277164318, -18.38911715685844683 ) ) ;
#39261=CARTESIAN_POINT ( 'NONE',  ( 117.5613014775786525, -10.15424416112533912, -14.75197769757731336 ) ) ;
#39267=CARTESIAN_POINT ( 'NONE',  ( 121.6508338206745066, -2.348512537728041583, -17.99195118506215962 ) ) ;
#39268=CARTESIAN_POINT ( 'NONE',  ( 116.2565881442453133, -0.8288870151387760510, -10.36305467784173118 ) ) ;
#39271=CARTESIAN_POINT ( 'NONE',  ( 127.0066334552993084, -9.721555348279057540, -15.73849928315003410 ) ) ;
#39272=CARTESIAN_POINT ( 'NONE',  ( 116.2565881442452991, -9.261995988541697145, -16.69588392320189030 ) ) ;
#39274=CARTESIAN_POINT ( 'NONE',  ( 112.7395348109119766, -4.153390946401321671, -8.397313243818183892 ) ) ;
#39277=CARTESIAN_POINT ( 'NONE',  ( 122.4965214775786251, 0.1319031606808879209, -14.10382304977623669 ) ) ;
#39278=CARTESIAN_POINT ( 'NONE',  ( 117.6180281442453150, -8.899110576539710493, -16.42337572283490132 ) ) ;
#39282=CARTESIAN_POINT ( 'NONE',  ( 112.1243801106810167, -8.918668529216430940, -16.32041580884654053 ) ) ;
#39286=CARTESIAN_POINT ( 'NONE',  ( 125.7299414775786346, -10.15424416112533912, -14.75197769757731336 ) ) ;
#39287=CARTESIAN_POINT ( 'NONE',  ( 121.4754414775786131, -1.833838273342659697, -17.42832698103878286 ) ) ;
#39290=CARTESIAN_POINT ( 'NONE',  ( 121.4754414775786131, -1.833838273342659697, -17.42832698103878286 ) ) ;
#39291=EDGE_CURVE ( 'NONE', #6072, #26433, #10404, .T. ) ;
#39296=CARTESIAN_POINT ( 'NONE',  ( 115.9162281442453235, -4.089484607189486809, -7.948022111789456723 ) ) ;
#39298=CARTESIAN_POINT ( 'NONE',  ( 118.0151148109119816, -10.63000616557722466, -14.87417383870573495 ) ) ;
#39301=CARTESIAN_POINT ( 'NONE',  ( 116.7671281442453335, -1.834011780172310813, -8.268836392978581529 ) ) ;
#39303=CARTESIAN_POINT ( 'NONE',  ( 118.3554748109119998, 0.2603800115204892296, -16.42320221600525088 ) ) ;
#39304=CARTESIAN_POINT ( 'NONE',  ( 127.3669547543159979, -10.41873247251588452, -13.86088658824870556 ) ) ;
#39311=CARTESIAN_POINT ( 'NONE',  ( 121.5888948109119809, 0.1319031606808879209, -14.10382304977623669 ) ) ;
#39313=CARTESIAN_POINT ( 'NONE',  ( 118.1285681442452926, -7.893985811506194494, -18.51759400769804031 ) ) ;
#39316=CARTESIAN_POINT ( 'NONE',  ( 121.7918886830089775, -1.087735405160626723, -17.17288456429612964 ) ) ;
#39317=CARTESIAN_POINT ( 'NONE',  ( 112.9097148109120070, -9.565557343593413364, -10.61323700422348004 ) ) ;
#39319=CARTESIAN_POINT ( 'NONE',  ( 122.2696148109119889, -4.089484607189486809, -7.948022111789456723 ) ) ;
#39320=CARTESIAN_POINT ( 'NONE',  ( 121.0783548109119749, 0.2603800115204892296, -16.42320221600525088 ) ) ;
#39323=CARTESIAN_POINT ( 'NONE',  ( 119.9438214775786378, -2.084020599724406786, -8.691656652584148546 ) ) ;
#39325=CARTESIAN_POINT ( 'NONE',  ( 118.2987481442453088, -1.561330072975668504, -17.79121239304076951 ) ) ;
#39326=CARTESIAN_POINT ( 'NONE',  ( 118.5256548109119876, -8.899110576539710493, -16.42337572283490132 ) ) ;
#39327=ORIENTED_EDGE ( 'NONE', *, *, #37870, .F. ) ;
#39329=CARTESIAN_POINT ( 'NONE',  ( 123.1772414775786189, -5.574606645277164318, -18.38911715685844683 ) ) ;
#39330=CARTESIAN_POINT ( 'NONE',  ( 120.2274548109119934, 0.5811942927096110934, -14.16772938898807510 ) ) ;
#39332=CARTESIAN_POINT ( 'NONE',  ( 113.0798948109119948, -8.899110576539710493, -16.42337572283490132 ) ) ;
#39334=CARTESIAN_POINT ( 'NONE',  ( 114.3077902067644516, -1.223627541775731631, -16.99192386690444323 ) ) ;
#39338=CARTESIAN_POINT ( 'NONE',  ( 119.0361948109119652, -7.893985811506177619, -18.51759400769804742 ) ) ;
#39340=CARTESIAN_POINT ( 'NONE',  ( 137.5098831408899400, -9.795576067877142634, -12.56145304104146021 ) ) ;
#39341=CARTESIAN_POINT ( 'NONE',  ( 117.2776681442452968, -4.153390946401321671, -8.397313243818183892 ) ) ;
#39342=CARTESIAN_POINT ( 'NONE',  ( 111.6050014775786536, 0.1319031606808879209, -14.10382304977623669 ) ) ;
#39346=CARTESIAN_POINT ( 'NONE',  ( 121.9883441868944658, -2.239543233855044946, -18.13706010537467606 ) ) ;
#39347=CARTESIAN_POINT ( 'NONE',  ( 113.7414098793805408, -2.191907684172563986, -18.20049396185734025 ) ) ;
#39350=CARTESIAN_POINT ( 'NONE',  ( 119.3765548109119834, 0.9020085738987339008, -11.91225656197089222 ) ) ;
#39351=CARTESIAN_POINT ( 'NONE',  ( 118.8660148109119774, 0.1319031606808879209, -14.10382304977623669 ) ) ;
#39352=CARTESIAN_POINT ( 'NONE',  ( 114.3846081442453197, 0.4262465694468514643, -12.03445270309931736 ) ) ;
#39355=CARTESIAN_POINT ( 'NONE',  ( 124.2550481442452792, -9.988377603198980381, -10.36322818467138518 ) ) ;
#39357=CARTESIAN_POINT ( 'NONE',  ( 119.9438214775786378, -2.084020599724406786, -8.691656652584148546 ) ) ;
#39358=EDGE_CURVE ( 'NONE', #25347, #38119, #15748, .T. ) ;
#39359=CARTESIAN_POINT ( 'NONE',  ( 121.4187148109119789, -3.505236298600246325, -18.68346056562440793 ) ) ;
#39360=CARTESIAN_POINT ( 'NONE',  ( 118.1285681442453068, -2.084020599724406786, -8.691656652584148546 ) ) ;
#39363=CARTESIAN_POINT ( 'NONE',  ( 124.3117748109119844, 0.1319031606808879209, -14.10382304977623669 ) ) ;
#39364=CARTESIAN_POINT ( 'NONE',  ( 123.9146881442452894, -10.15424416112533912, -14.75197769757731336 ) ) ;
#39372=CARTESIAN_POINT ( 'NONE',  ( 117.8449348109119938, -8.166667518702817929, -8.995218007635861213 ) ) ;
#39373=CARTESIAN_POINT ( 'NONE',  ( 119.6601881442453106, -8.166667518702819706, -8.995218007635861213 ) ) ;
#39375=CARTESIAN_POINT ( 'NONE',  ( 113.0798948109119948, -0.4660016031367893996, -10.09054647747474043 ) ) ;
#39379=CARTESIAN_POINT ( 'NONE',  ( 116.1431348109119881, -10.30919188438810075, -12.61870101168855918 ) ) ;
#39381=CARTESIAN_POINT ( 'NONE',  ( 121.3619881442452879, -5.574606645277164318, -18.38911715685844683 ) ) ;
#39383=CARTESIAN_POINT ( 'NONE',  ( 115.2355081442453155, 0.1319031606808879209, -14.10382304977623669 ) ) ;
#39384=CARTESIAN_POINT ( 'NONE',  ( 121.9859814775786333, 0.2603800115204892296, -16.42320221600525088 ) ) ;
#39386=CARTESIAN_POINT ( 'NONE',  ( 116.2565881442453133, -0.8288870151387760510, -10.36305467784173118 ) ) ;
#39391=CARTESIAN_POINT ( 'NONE',  ( 120.0572748109119772, -3.383040157471821630, -19.15922257007629170 ) ) ;
#39397=CARTESIAN_POINT ( 'NONE',  ( 114.8384214775786489, -10.15424416112533912, -14.75197769757731336 ) ) ;
#39400=CARTESIAN_POINT ( 'NONE',  ( 124.9924948109119924, -5.574606645277164318, -18.38911715685844683 ) ) ;
#39401=LINE ( 'NONE', #8166, #6915 ) ;
#39402=CARTESIAN_POINT ( 'NONE',  ( 120.5678148109119832, -1.833838273342659253, -17.42832698103878286 ) ) ;
#39405=CARTESIAN_POINT ( 'NONE',  ( 124.4819548109119722, -2.084020599724406786, -8.691656652584148546 ) ) ;
#39407=CARTESIAN_POINT ( 'NONE',  ( 113.8740681442453138, 0.5811942927096154232, -14.16772938898807155 ) ) ;
#39408=CARTESIAN_POINT ( 'NONE',  ( 120.2274548109119934, 0.5811942927096110934, -14.16772938898807510 ) ) ;
#39409=CARTESIAN_POINT ( 'NONE',  ( 113.7038881442453402, -3.383040157471821630, -19.15922257007629170 ) ) ;
#39411=CARTESIAN_POINT ( 'NONE',  ( 121.2485348109119769, -8.899110576539710493, -16.42337572283490132 ) ) ;
#39413=CARTESIAN_POINT ( 'NONE',  ( 119.6034614775786196, -6.344957434206665248, -7.627207830600338134 ) ) ;
#39416=CARTESIAN_POINT ( 'NONE',  ( 112.7962614775786676, -6.222761293078241884, -8.102969835052219238 ) ) ;
#39417=CARTESIAN_POINT ( 'NONE',  ( 137.9323468215654316, -2.878351188643373693, -17.28639180419563104 ) ) ;
#39420=CARTESIAN_POINT ( 'NONE',  ( 120.0572748109119772, -6.222761293078241884, -8.102969835052219238 ) ) ;
#39426=CARTESIAN_POINT ( 'NONE',  ( 116.1998614775786507, -10.63000616557722466, -14.87417383870573495 ) ) ;
#39427=CARTESIAN_POINT ( 'NONE',  ( 125.9001214775786224, -4.089484607189486809, -7.948022111789456723 ) ) ;
#39429=CARTESIAN_POINT ( 'NONE',  ( 121.8725281442453223, -6.222761293078241884, -8.102969835052219238 ) ) ;
#39431=CARTESIAN_POINT ( 'NONE',  ( 112.7395348109119766, -4.153390946401321671, -8.397313243818183892 ) ) ;
#39437=CARTESIAN_POINT ( 'NONE',  ( 111.7184548109119788, -9.261995988541697145, -16.69588392320189030 ) ) ;
#39441=CARTESIAN_POINT ( 'NONE',  ( 122.2128881442453263, -1.834011780172310813, -8.268836392978581529 ) ) ;
#39445=CARTESIAN_POINT ( 'NONE',  ( 136.8340972670101507, 0.2256513543513796738, -11.12430961515349814 ) ) ;
#39446=CARTESIAN_POINT ( 'NONE',  ( 124.3117748109119844, -10.30919188438810075, -12.61870101168855918 ) ) ;
#39448=CARTESIAN_POINT ( 'NONE',  ( 122.5532481442453019, 0.4262465694468514643, -12.03445270309931736 ) ) ;
#39450=CARTESIAN_POINT ( 'NONE',  ( 117.9583881442453048, -10.30919188438810075, -12.61870101168855918 ) ) ;
#39452=CARTESIAN_POINT ( 'NONE',  ( 116.5817225628257177, -2.263366209404225504, -18.10533625161308180 ) ) ;
#39453=CARTESIAN_POINT ( 'NONE',  ( 112.6764896192402432, -1.111561923218668646, -17.14115599315433869 ) ) ;
#39455=CARTESIAN_POINT ( 'NONE',  ( 124.9357681442453014, -1.834011780172310813, -8.268836392978581529 ) ) ;
#39457=DIRECTION ( 'NONE',  ( 0.000000000000000000, -0.6004852223388320587, 0.7996358532186281787 ) ) ;
#39458=CARTESIAN_POINT ( 'NONE',  ( 111.2646414775786496, -8.899110576539710493, -16.42337572283490132 ) ) ;
#39459=CARTESIAN_POINT ( 'NONE',  ( 125.6732148109119862, -9.859900752359378018, -12.68260735090039759 ) ) ;
#39461=CARTESIAN_POINT ( 'NONE',  ( 123.7445081442452874, -7.894159318335828068, -9.358103419637847864 ) ) ;
#39462=CARTESIAN_POINT ( 'NONE',  ( 112.6828081442453282, -2.084020599724406786, -8.691656652584148546 ) ) ;
#39463=CARTESIAN_POINT ( 'NONE',  ( 119.8303681442453126, -10.63000616557722466, -14.87417383870573495 ) ) ;
#39465=CARTESIAN_POINT ( 'NONE',  ( 127.0400190879709612, -8.468517614608312982, -17.42856087967522782 ) ) ;
#39469=CARTESIAN_POINT ( 'NONE',  ( 125.8328548109119964, -8.862178061931794915, -16.39564131203325559 ) ) ;
#39470=CARTESIAN_POINT ( 'NONE',  ( 114.8384214775786489, 0.9020085738987339008, -11.91225656197089222 ) ) ;
#39472=CARTESIAN_POINT ( 'NONE',  ( 116.9940348109119839, -0.1624402480850797581, -16.17319339645315424 ) ) ;
#39474=CARTESIAN_POINT ( 'NONE',  ( 135.3184548109119874, -1.889072916127989776, -18.60376373290417362 ) ) ;
#39477=CARTESIAN_POINT ( 'NONE',  ( 135.3184548109119874, -4.863998795839242995, -13.39321520033831447 ) ) ;
#39478=CARTESIAN_POINT ( 'NONE',  ( 116.8805814775786445, -6.344957434206662583, -7.627207830600332805 ) ) ;
#39482=CARTESIAN_POINT ( 'NONE',  ( 127.0066334553006158, -7.209282878650888016, -8.535658647897701456 ) ) ;
#39483=CARTESIAN_POINT ( 'NONE',  ( 118.1852948109119836, -4.153390946401325223, -8.397313243818185668 ) ) ;
#39484=CARTESIAN_POINT ( 'NONE',  ( 114.6115148109119986, -3.383040157471821630, -19.15922257007629170 ) ) ;
#39485=CARTESIAN_POINT ( 'NONE',  ( 112.9097148109120070, 0.2603800115204892296, -16.42320221600525088 ) ) ;
#39486=CARTESIAN_POINT ( 'NONE',  ( 124.5386814775786206, -4.153390946401325223, -8.397313243818185668 ) ) ;
#39487=CARTESIAN_POINT ( 'NONE',  ( 124.1983214775786166, -1.833838273342659697, -17.42832698103878286 ) ) ;
#39488=CARTESIAN_POINT ( 'NONE',  ( 115.8027748109119841, -8.899110576539710493, -16.42337572283490132 ) ) ;
#39494=DIRECTION ( 'NONE',  ( 1.000000000000000000, 0.000000000000000000, 0.000000000000000000 ) ) ;
#39495=CARTESIAN_POINT ( 'NONE',  ( 117.6747548109119919, -7.643976991954077427, -18.09477374809248928 ) ) ;
#39496=ORIENTED_EDGE ( 'NONE', *, *, #24773, .T. ) ;
#39498=CARTESIAN_POINT ( 'NONE',  ( 114.2144281442453178, -8.166667518702817929, -8.995218007635859436 ) ) ;
#39501=CARTESIAN_POINT ( 'NONE',  ( 112.3424481442453384, -3.505236298600246325, -18.68346056562440793 ) ) ;
#39505=CARTESIAN_POINT ( 'NONE',  ( 123.9714148109119805, -8.899110576539710493, -16.42337572283490132 ) ) ;
#39506=CARTESIAN_POINT ( 'NONE',  ( 118.6958348109119754, -3.505236298600246325, -18.68346056562440793 ) ) ;
#39508=CARTESIAN_POINT ( 'NONE',  ( 116.5402214775786405, -9.565557343593393824, -10.61323700422345340 ) ) ;
#39513=CARTESIAN_POINT ( 'NONE',  ( 115.6325948109119821, 0.2603800115204892296, -16.42320221600525088 ) ) ;
#39515=CARTESIAN_POINT ( 'NONE',  ( 126.4673881442452910, -7.894159318335828068, -9.358103419637847864 ) ) ;
#39516=CARTESIAN_POINT ( 'NONE',  ( 122.2128881442453263, -7.643976991954077427, -18.09477374809248928 ) ) ;
#39521=CARTESIAN_POINT ( 'NONE',  ( 121.4187148109119789, -3.505236298600246325, -18.68346056562440793 ) ) ;
#39527=CARTESIAN_POINT ( 'NONE',  ( 118.4122014775786340, 0.5811942927096110934, -14.16772938898807510 ) ) ;
#39530=CARTESIAN_POINT ( 'NONE',  ( 117.4478481442453131, 0.2603800115204892296, -16.42320221600525088 ) ) ;
#39533=CARTESIAN_POINT ( 'NONE',  ( 116.8238548109119819, -4.089484607189486809, -7.948022111789456723 ) ) ;
#39534=CARTESIAN_POINT ( 'NONE',  ( 118.4689281442453392, 0.9020085738987339008, -11.91225656197089222 ) ) ;
#39539=AXIS2_PLACEMENT_3D ( 'NONE', #6766, #23649, #30476 ) ;
#39542=CARTESIAN_POINT ( 'NONE',  ( 121.8725281442453223, -6.222761293078241884, -8.102969835052219238 ) ) ;
#39545=CARTESIAN_POINT ( 'NONE',  ( 115.5758681442453053, -7.894159318335828068, -9.358103419637847864 ) ) ;
#39547=CARTESIAN_POINT ( 'NONE',  ( 114.0442481442453300, -7.643976991954077427, -18.09477374809248928 ) ) ;
#39548=CARTESIAN_POINT ( 'NONE',  ( 121.7023481442452777, -9.261995988541697145, -16.69588392320189030 ) ) ;
#39551=CARTESIAN_POINT ( 'NONE',  ( 119.8870948109119752, -0.8288870151387760510, -10.36305467784173118 ) ) ;
#39552=CARTESIAN_POINT ( 'NONE',  ( 113.9875214775786532, -0.4660016031367893996, -10.09054647747474043 ) ) ;
#39553=CARTESIAN_POINT ( 'NONE',  ( 120.6245414775786458, -9.988377603198976828, -10.36322818467138340 ) ) ;
#39554=CARTESIAN_POINT ( 'NONE',  ( 118.3554748109119998, -9.565557343593413364, -10.61323700422348004 ) ) ;
#39555=ORIENTED_EDGE ( 'NONE', *, *, #18308, .T. ) ;
#39557=AXIS2_PLACEMENT_3D ( 'NONE', #41029, #44219, #12980 ) ;
#39558=EDGE_CURVE ( 'NONE', #21031, #35460, #37014, .T. ) ;
#39559=CARTESIAN_POINT ( 'NONE',  ( 120.3409081442453044, -0.4660016031367893996, -10.09054647747474043 ) ) ;
#39566=CARTESIAN_POINT ( 'NONE',  ( 116.9940348109119839, -0.1624402480850797581, -16.17319339645315424 ) ) ;
#39567=CARTESIAN_POINT ( 'NONE',  ( 111.2646414775786496, -8.899110576539710493, -16.42337572283490132 ) ) ;
#39572=CARTESIAN_POINT ( 'NONE',  ( 113.5337081442453240, -0.8288870151387760510, -10.36305467784173118 ) ) ;
#39576=CARTESIAN_POINT ( 'NONE',  ( 120.1707281442453166, 0.2603800115204892296, -16.42320221600525088 ) ) ;
#39577=CARTESIAN_POINT ( 'NONE',  ( 124.5386814775786206, -4.153390946401325223, -8.397313243818185668 ) ) ;
#39578=ORIENTED_EDGE ( 'NONE', *, *, #3077, .F. ) ;
#39579=CARTESIAN_POINT ( 'NONE',  ( 136.7741008876033391, -9.164476617390489466, -9.793428787663129853 ) ) ;
#39581=CARTESIAN_POINT ( 'NONE',  ( 126.2333338125966833, 0.07078918107596827991, -14.24356987566622479 ) ) ;
#39583=CARTESIAN_POINT ( 'NONE',  ( 118.8092881442453290, -0.1624402480850797581, -16.17319339645315424 ) ) ;
#39584=CARTESIAN_POINT ( 'NONE',  ( 122.7234281442452755, -4.153390946401325223, -8.397313243818185668 ) ) ;
#39586=CARTESIAN_POINT ( 'NONE',  ( 115.1787814775786387, -0.1624402480850797581, -16.17319339645315424 ) ) ;
#39587=CARTESIAN_POINT ( 'NONE',  ( 120.8451296192402253, -1.111561923218658210, -17.14115599315433158 ) ) ;
#39589=CARTESIAN_POINT ( 'NONE',  ( 123.4041481442452834, 0.1319031606808879209, -14.10382304977623669 ) ) ;
#39590=CARTESIAN_POINT ( 'NONE',  ( 125.0492214775786266, -3.505236298600246325, -18.68346056562440793 ) ) ;
#39597=CARTESIAN_POINT ( 'NONE',  ( 122.5532481442453019, -10.63000616557722466, -14.87417383870573495 ) ) ;
#39598=CARTESIAN_POINT ( 'NONE',  ( 116.9940348109119839, -9.988377603198976828, -10.36322818467138340 ) ) ;
#39600=CARTESIAN_POINT ( 'NONE',  ( 112.0020881442453344, 0.2603800115204892296, -16.42320221600525088 ) ) ;
#39601=CARTESIAN_POINT ( 'NONE',  ( 138.2184548109119930, -10.81584935473217080, -14.15181583611863303 ) ) ;
#39605=CARTESIAN_POINT ( 'NONE',  ( 117.2209414775786485, -7.893985811506177619, -18.51759400769804742 ) ) ;
#39606=CARTESIAN_POINT ( 'NONE',  ( 124.0848681442452772, -5.574606645277164318, -18.38911715685844683 ) ) ;
#39608=CARTESIAN_POINT ( 'NONE',  ( 115.3489614775786407, -0.8288870151387760510, -10.36305467784173118 ) ) ;
#39609=CARTESIAN_POINT ( 'NONE',  ( 120.3976348109119812, -1.834011780172310813, -8.268836392978581529 ) ) ;
#39611=CARTESIAN_POINT ( 'NONE',  ( 118.9794681442453026, -0.8288870151387760510, -10.36305467784173118 ) ) ;
#39615=EDGE_CURVE ( 'NONE', #34606, #32113, #36228, .T. ) ;
#39618=CARTESIAN_POINT ( 'NONE',  ( 120.2841814775786276, 0.9020085738987339008, -11.91225656197089222 ) ) ;
#39623=CARTESIAN_POINT ( 'NONE',  ( 119.8870948109119752, -0.8288870151387760510, -10.36305467784173118 ) ) ;
#39626=CARTESIAN_POINT ( 'NONE',  ( 123.8012348109119642, -9.565557343593413364, -10.61323700422348004 ) ) ;
#39628=CARTESIAN_POINT ( 'NONE',  ( 123.5743281442453139, -2.084020599724406786, -8.691656652584148546 ) ) ;
#39631=CARTESIAN_POINT ( 'NONE',  ( 117.5613014775786525, -10.15424416112533912, -14.75197769757731336 ) ) ;
#39632=CARTESIAN_POINT ( 'NONE',  ( 123.1772414775786189, -5.574606645277164318, -18.38911715685844683 ) ) ;
#39633=CARTESIAN_POINT ( 'NONE',  ( 114.6682414775786469, -1.561330072975668060, -17.79121239304076596 ) ) ;
#39634=CARTESIAN_POINT ( 'NONE',  ( 119.7169148109119874, -9.988377603198976828, -10.36322818467138340 ) ) ;
#39635=CARTESIAN_POINT ( 'NONE',  ( 114.4980614775786592, -7.893985811506177619, -18.51759400769804742 ) ) ;
#39637=CARTESIAN_POINT ( 'NONE',  ( 123.9146881442452894, -10.15424416112533912, -14.75197769757731336 ) ) ;
#39639=CARTESIAN_POINT ( 'NONE',  ( 119.7736414775786358, -10.30919188438810075, -12.61870101168855918 ) ) ;
#39642=CARTESIAN_POINT ( 'NONE',  ( 138.2184548109119930, -9.067395352211066850, -7.795764227807919333 ) ) ;
#39644=CARTESIAN_POINT ( 'NONE',  ( 112.6260814775786514, -0.8288870151387760510, -10.36305467784173118 ) ) ;
#39646=CARTESIAN_POINT ( 'NONE',  ( 125.5597614775786326, -1.561330072975669392, -17.79121239304076951 ) ) ;
#39647=EDGE_LOOP ( 'NONE', ( #304, #21817, #9719, #42068 ) ) ;
#39648=CARTESIAN_POINT ( 'NONE',  ( 122.7801548109119665, -6.222761293078241884, -8.102969835052219238 ) ) ;
#39654=CARTESIAN_POINT ( 'NONE',  ( 116.4834948109119779, -1.561330072975668504, -17.79121239304076951 ) ) ;
#39656=CARTESIAN_POINT ( 'NONE',  ( 119.8870948109119752, -0.8288870151387760510, -10.36305467784173118 ) ) ;
#39660=CARTESIAN_POINT ( 'NONE',  ( 114.6881864975817820, -2.215723800389698184, -18.16877924232191788 ) ) ;
#39664=B_SPLINE_CURVE_WITH_KNOTS ( 'NONE', 3,
 ( #13780, #33831, #37718, #20627, #38160, #20179, #13558, #27916, #41826, #45022 ),
 .UNSPECIFIED., .F., .F.,
 ( 4, 3, 3, 4 ),
 ( 0.000000000000000000, 0.0001671877548681254834, 0.0003343755096277620112, 0.0006463528481650629171 ),
 .UNSPECIFIED. ) ;
#39665=CARTESIAN_POINT ( 'NONE',  ( 121.7590748109119687, -7.893985811506177619, -18.51759400769804742 ) ) ;
#39666=CARTESIAN_POINT ( 'NONE',  ( 136.3568202015718782, -10.23338508054624718, -15.60949798484924322 ) ) ;
#39668=CARTESIAN_POINT ( 'NONE',  ( 115.6893214775786447, 0.5811942927096154232, -14.16772938898807155 ) ) ;
#39669=CARTESIAN_POINT ( 'NONE',  ( 111.6617281442453304, 0.4262465694468514643, -12.03445270309931736 ) ) ;
#39671=CARTESIAN_POINT ( 'NONE',  ( 122.6099748109119929, -0.8288870151387760510, -10.36305467784173118 ) ) ;
#39673=CARTESIAN_POINT ( 'NONE',  ( 119.7169148109119874, -9.988377603198976828, -10.36322818467138340 ) ) ;
#39675=CARTESIAN_POINT ( 'NONE',  ( 116.9163235773848726, -2.467220198592778413, -17.83387418641524391 ) ) ;
#39677=CARTESIAN_POINT ( 'NONE',  ( 136.3514896075899969, -5.513217599145076697, -7.616394449054343596 ) ) ;
#39679=CARTESIAN_POINT ( 'NONE',  ( 114.9518748109119883, -7.643976991954077427, -18.09477374809248928 ) ) ;
#39683=CARTESIAN_POINT ( 'NONE',  ( 113.3635281442453504, -0.1624402480850797581, -16.17319339645315424 ) ) ;
#39684=CARTESIAN_POINT ( 'NONE',  ( 125.8433948109119456, -7.643976991954077427, -18.09477374809248928 ) ) ;
#39686=CARTESIAN_POINT ( 'NONE',  ( 124.1415948109119540, -3.505236298600246325, -18.68346056562440793 ) ) ;
#39688=CARTESIAN_POINT ( 'NONE',  ( 119.7736414775786358, -10.30919188438810075, -12.61870101168855918 ) ) ;
#39689=VERTEX_POINT ( 'NONE', #11087 ) ;
#39690=CARTESIAN_POINT ( 'NONE',  ( 127.1653849502246629, -8.462563953427153507, -17.51752121746688573 ) ) ;
#39696=CARTESIAN_POINT ( 'NONE',  ( 113.7606148109119886, -1.561330072975668060, -17.79121239304076596 ) ) ;
#39701=CARTESIAN_POINT ( 'NONE',  ( 122.7801548109119665, -6.222761293078217903, -8.102969835052215686 ) ) ;
#39702=CARTESIAN_POINT ( 'NONE',  ( 112.3991748109119868, -8.166667518702817929, -8.995218007635859436 ) ) ;
#39703=CARTESIAN_POINT ( 'NONE',  ( 121.0216281442452981, -1.561330072975668948, -17.79121239304076951 ) ) ;
#39709=CARTESIAN_POINT ( 'NONE',  ( 117.3911214775786505, -7.894159318335828068, -9.358103419637847864 ) ) ;
#39710=CARTESIAN_POINT ( 'NONE',  ( 117.5045748109119756, 0.5811942927096110934, -14.16772938898807510 ) ) ;
#39711=CARTESIAN_POINT ( 'NONE',  ( 112.4559014775786494, -9.988377603198976828, -10.36322818467138340 ) ) ;
#39712=CARTESIAN_POINT ( 'NONE',  ( 124.4819548109119722, -2.084020599724406786, -8.691656652584148546 ) ) ;
#39713=CARTESIAN_POINT ( 'NONE',  ( 125.1626748109119802, -0.1624402480850797581, -16.17319339645315424 ) ) ;
#39714=CARTESIAN_POINT ( 'NONE',  ( 116.7671281442453335, -7.643976991954077427, -18.09477374809248928 ) ) ;
#39717=CARTESIAN_POINT ( 'NONE',  ( 121.6901161498677055, -2.324775150319219108, -18.02356106541841996 ) ) ;
#39718=CARTESIAN_POINT ( 'NONE',  ( 116.1998614775786507, 0.4262465694468514643, -12.03445270309931736 ) ) ;
#39719=ORIENTED_EDGE ( 'NONE', *, *, #44253, .F. ) ;
#39721=CARTESIAN_POINT ( 'NONE',  ( 113.9307948109119906, 0.9020085738987339008, -11.91225656197089222 ) ) ;
#39723=CARTESIAN_POINT ( 'NONE',  ( 125.6164881442453094, -9.565557343593413364, -10.61323700422348004 ) ) ;
#39726=CARTESIAN_POINT ( 'NONE',  ( 120.6245414775786458, -0.1624402480850797581, -16.17319339645315424 ) ) ;
#39727=CARTESIAN_POINT ( 'NONE',  ( 116.2565881442453133, -0.8288870151387760510, -10.36305467784173118 ) ) ;
#39732=CARTESIAN_POINT ( 'NONE',  ( 115.4624148109119943, -5.638512984488999180, -18.83840828888717311 ) ) ;
#39733=CARTESIAN_POINT ( 'NONE',  ( 114.8951481442453115, -0.4660016031367893996, -10.09054647747474043 ) ) ;
#39734=CARTESIAN_POINT ( 'NONE',  ( 117.2209414775786485, -2.084020599724406786, -8.691656652584148546 ) ) ;
#39735=CARTESIAN_POINT ( 'NONE',  ( 119.8303681442453126, 0.4262465694468514643, -12.03445270309931736 ) ) ;
#39737=ORIENTED_EDGE ( 'NONE', *, *, #2130, .T. ) ;
#39739=CARTESIAN_POINT ( 'NONE',  ( 119.0361948109119652, -2.084020599724406786, -8.691656652584148546 ) ) ;
#39740=CARTESIAN_POINT ( 'NONE',  ( 124.4252281442452812, -0.8288870151387760510, -10.36305467784173118 ) ) ;
#39745=CARTESIAN_POINT ( 'NONE',  ( 118.5256548109119876, -0.4660016031367893996, -10.09054647747474043 ) ) ;
#39747=CARTESIAN_POINT ( 'NONE',  ( 122.0994348109119443, 0.9020085738987339008, -11.91225656197089222 ) ) ;
#39750=CARTESIAN_POINT ( 'NONE',  ( 116.1998614775786507, -10.63000616557722466, -14.87417383870573495 ) ) ;
#39751=CARTESIAN_POINT ( 'NONE',  ( 116.5402214775786405, 0.2603800115204892296, -16.42320221600525088 ) ) ;
#39752=CARTESIAN_POINT ( 'NONE',  ( 126.4536383592486999, -9.979787239928239018, -13.25019936256093089 ) ) ;
#39754=ORIENTED_EDGE ( 'NONE', *, *, #3333, .T. ) ;
#39757=CARTESIAN_POINT ( 'NONE',  ( 118.8660148109119774, 0.1319031606808879209, -14.10382304977623669 ) ) ;
#39760=CARTESIAN_POINT ( 'NONE',  ( 115.6893214775786447, -9.859900752359374465, -12.68260735090039404 ) ) ;
#39763=CARTESIAN_POINT ( 'NONE',  ( 113.0798948109119948, -8.899110576539710493, -16.42337572283490132 ) ) ;
#39764=CARTESIAN_POINT ( 'NONE',  ( 120.7379948109119709, -10.63000616557722466, -14.87417383870573495 ) ) ;
#39766=CARTESIAN_POINT ( 'NONE',  ( 117.7882081442453170, -3.505236298600246325, -18.68346056562440793 ) ) ;
#39767=CARTESIAN_POINT ( 'NONE',  ( 116.2565881442452991, -9.261995988541697145, -16.69588392320189030 ) ) ;
#39768=CARTESIAN_POINT ( 'NONE',  ( 120.9081748109119872, -5.638512984488999180, -18.83840828888717311 ) ) ;
#39769=CARTESIAN_POINT ( 'NONE',  ( 119.2063748109119814, -7.894159318335828068, -9.358103419637847864 ) ) ;
#39771=CARTESIAN_POINT ( 'NONE',  ( 123.4608748109119745, 0.4262465694468514643, -12.03445270309931736 ) ) ;
#39774=CARTESIAN_POINT ( 'NONE',  ( 118.9227414775786400, -10.63000616557722466, -14.87417383870573495 ) ) ;
#39775=CARTESIAN_POINT ( 'NONE',  ( 112.2857214775786474, -5.574606645277164318, -18.38911715685844683 ) ) ;
#39776=CARTESIAN_POINT ( 'NONE',  ( 121.9859814775786333, 0.2603800115204892296, -16.42320221600525088 ) ) ;
#39779=CARTESIAN_POINT ( 'NONE',  ( 127.9597256070077975, -3.007186152783901445, -14.61697626063841149 ) ) ;
#39783=CARTESIAN_POINT ( 'NONE',  ( 137.3802547664365363, -9.825762579687179255, -12.05248962777355715 ) ) ;
#39784=CARTESIAN_POINT ( 'NONE',  ( 115.8027748109119841, -8.899110576539710493, -16.42337572283490132 ) ) ;
#39785=CARTESIAN_POINT ( 'NONE',  ( 125.7866681442452688, -0.4660016031367893996, -10.09054647747474043 ) ) ;
#39787=CARTESIAN_POINT ( 'NONE',  ( 112.1234697116520920, -8.918491192341182483, -16.31914947962552631 ) ) ;
#39789=CARTESIAN_POINT ( 'NONE',  ( 116.9940348109119839, -0.1624402480850797581, -16.17319339645315424 ) ) ;
#39796=CARTESIAN_POINT ( 'NONE',  ( 117.9016614775786280, -9.988377603198976828, -10.36322818467138340 ) ) ;
#39797=CARTESIAN_POINT ( 'NONE',  ( 122.4397948109119767, -0.1624402480850797581, -16.17319339645315424 ) ) ;
#39800=CARTESIAN_POINT ( 'NONE',  ( 124.8223148109119762, 0.9020085738987339008, -11.91225656197089222 ) ) ;
#39802=CARTESIAN_POINT ( 'NONE',  ( 123.8012348109119642, -9.565557343593413364, -10.61323700422348004 ) ) ;
#39804=CARTESIAN_POINT ( 'NONE',  ( 122.2696148109119889, -5.574606645277164318, -18.38911715685844683 ) ) ;
#39806=CARTESIAN_POINT ( 'NONE',  ( 115.1220548109119761, -1.833838273342658809, -17.42832698103878286 ) ) ;
#39808=CARTESIAN_POINT ( 'NONE',  ( 120.9625387682627746, -1.040089454026966287, -17.23633227186632766 ) ) ;
#39810=CARTESIAN_POINT ( 'NONE',  ( 125.4463081442452932, -4.153390946401325223, -8.397313243818185668 ) ) ;
#39811=CARTESIAN_POINT ( 'NONE',  ( 125.4463081442452932, -4.153390946401325223, -8.397313243818185668 ) ) ;
#39817=CARTESIAN_POINT ( 'NONE',  ( 122.8368814775786291, -1.561330072975668948, -17.79121239304076951 ) ) ;
#39818=CARTESIAN_POINT ( 'NONE',  ( 116.7671281442453335, -1.834011780172310813, -8.268836392978581529 ) ) ;
#39820=CARTESIAN_POINT ( 'NONE',  ( 115.9729548109119861, -6.344957434206662583, -7.627207830600332805 ) ) ;
#39825=CARTESIAN_POINT ( 'NONE',  ( 119.0361948109119652, -7.893985811506177619, -18.51759400769804742 ) ) ;
#39826=CARTESIAN_POINT ( 'NONE',  ( 124.3117748109119844, 0.1319031606808879209, -14.10382304977623669 ) ) ;
#39829=EDGE_CURVE ( 'NONE', #25860, #2614, #12585, .T. ) ;
#39830=CARTESIAN_POINT ( 'NONE',  ( 113.9307948109119764, -10.15424416112533912, -14.75197769757731336 ) ) ;
#39831=CARTESIAN_POINT ( 'NONE',  ( 124.5386814775786206, -5.638512984488999180, -18.83840828888717311 ) ) ;
#39834=CIRCLE ( 'NONE', #4106, 4.999999999999998224 ) ;
#39836=CARTESIAN_POINT ( 'NONE',  ( 120.5110881442453206, -3.505236298600246325, -18.68346056562440793 ) ) ;
#39842=CARTESIAN_POINT ( 'NONE',  ( 121.2485348109119769, -0.4660016031367893996, -10.09054647747474043 ) ) ;
#39843=CARTESIAN_POINT ( 'NONE',  ( 125.7299414775786346, -10.15424416112533912, -14.75197769757731336 ) ) ;
#39844=CARTESIAN_POINT ( 'NONE',  ( 111.3214083975491775, -7.642508564524847614, -18.09498261449271084 ) ) ;
#39846=CARTESIAN_POINT ( 'NONE',  ( 117.9016614775786280, -0.1624402480850797581, -16.17319339645315424 ) ) ;
#39849=CARTESIAN_POINT ( 'NONE',  ( 122.3263414775786373, -3.505236298600246325, -18.68346056562440793 ) ) ;
#39851=CARTESIAN_POINT ( 'NONE',  ( 123.6877814775786533, -6.222761293078241884, -8.102969835052219238 ) ) ;
#39854=CARTESIAN_POINT ( 'NONE',  ( 124.3117748109119844, -10.30919188438810075, -12.61870101168855918 ) ) ;
#39855=CARTESIAN_POINT ( 'NONE',  ( 118.5823814775786360, -7.643976991954077427, -18.09477374809248928 ) ) ;
#39856=CARTESIAN_POINT ( 'NONE',  ( 124.0848681442452772, -5.574606645277164318, -18.38911715685844683 ) ) ;
#39857=CARTESIAN_POINT ( 'NONE',  ( 118.0151148109119816, -10.63000616557722466, -14.87417383870573495 ) ) ;
#39858=CARTESIAN_POINT ( 'NONE',  ( 114.1009748109119784, -4.089484607189486809, -7.948022111789456723 ) ) ;
#39860=CARTESIAN_POINT ( 'NONE',  ( 124.4819548109119722, -2.084020599724406786, -8.691656652584148546 ) ) ;
#39862=CARTESIAN_POINT ( 'NONE',  ( 121.1918081442452859, 0.9020085738987339008, -11.91225656197089222 ) ) ;
#39870=CARTESIAN_POINT ( 'NONE',  ( 112.0588148109119828, 0.5811942927096154232, -14.16772938898807155 ) ) ;
#39877=CARTESIAN_POINT ( 'NONE',  ( 113.8173414775786512, 0.2603800115204892296, -16.42320221600525088 ) ) ;
#39879=CARTESIAN_POINT ( 'NONE',  ( 125.6164881442453094, -9.565557343593413364, -10.61323700422348004 ) ) ;
#39880=CARTESIAN_POINT ( 'NONE',  ( 114.4413348109119823, -0.8288870151387760510, -10.36305467784173118 ) ) ;
#39884=CARTESIAN_POINT ( 'NONE',  ( 124.4252281442452812, -9.261995988541709579, -16.69588392320187253 ) ) ;
#39885=CARTESIAN_POINT ( 'NONE',  ( 115.5758681442453053, -1.561330072975668060, -17.79121239304076951 ) ) ;
#39887=AXIS2_PLACEMENT_3D ( 'NONE', #31090, #38153, #20832 ) ;
#39888=CARTESIAN_POINT ( 'NONE',  ( 123.4608748109119745, -10.63000616557722466, -14.87417383870573495 ) ) ;
#39889=CARTESIAN_POINT ( 'NONE',  ( 136.7036351579049267, -10.04987633766737076, -15.63786568088821483 ) ) ;
#39892=CARTESIAN_POINT ( 'NONE',  ( 113.9307948109119906, 0.9020085738987339008, -11.91225656197089222 ) ) ;
#39893=CARTESIAN_POINT ( 'NONE',  ( 125.6732148109119862, 0.5811942927096110934, -14.16772938898807510 ) ) ;
#39895=CARTESIAN_POINT ( 'NONE',  ( 126.5241148109119393, -9.565557343593413364, -10.61323700422348004 ) ) ;
#39897=CARTESIAN_POINT ( 'NONE',  ( 119.4332814775786318, -0.4660016031367893996, -10.09054647747474043 ) ) ;
#39901=CARTESIAN_POINT ( 'NONE',  ( 137.5082292857710513, -4.434782517277369607, -8.403026514009534154 ) ) ;
#39902=CARTESIAN_POINT ( 'NONE',  ( 114.4413348109119823, -0.8288870151387760510, -10.36305467784173118 ) ) ;
#39905=B_SPLINE_CURVE_WITH_KNOTS ( 'NONE', 3,
 ( #15169, #18375, #32263, #8109, #1031, #28859, #42771, #22010, #4671, #32484, #29076, #42987, #44577, #23603, #13111, #19713, #27246, #6023, #16762, #23369, #2833, #30206, #37721, #40241, #29977, #33834, #33599, #30659, #13342, #34291 ),
 .UNSPECIFIED., .F., .F.,
 ( 4, 2, 2, 1, 2, 2, 2, 1, 1, 2, 2, 2, 1, 1, 1, 2, 2, 4 ),
 ( 0.000000000000000000, 0.03124999999996751210, 0.06249999999993502420, 0.09374999999990253630, 0.1093749999998813865, 0.1249999999998602229, 0.1874999999997779832, 0.2187499999997450095, 0.2343749999997195577, 0.2421874999997072619, 0.2499999999996949385, 0.3749999999996284639, 0.4374999999996059818, 0.4687499999995839439, 0.4843749999995833888, 0.4921874999995830557, 0.4999999999995827782, 1.000000000000000000 ),
 .UNSPECIFIED. ) ;
#39906=CARTESIAN_POINT ( 'NONE',  ( 113.8173414775786512, -9.565557343593413364, -10.61323700422348004 ) ) ;
#39907=CARTESIAN_POINT ( 'NONE',  ( 113.1933481442453058, -4.089484607189486809, -7.948022111789456723 ) ) ;
#39909=CARTESIAN_POINT ( 'NONE',  ( 123.3474214775786209, -0.1624402480850797581, -16.17319339645315424 ) ) ;
#39911=CARTESIAN_POINT ( 'NONE',  ( 118.1852948109119836, -5.638512984488999180, -18.83840828888717311 ) ) ;
#39912=CARTESIAN_POINT ( 'NONE',  ( 120.5110881442453206, -6.344957434206665248, -7.627207830600338134 ) ) ;
#39913=VERTEX_POINT ( 'NONE', #5801 ) ;
#39914=CARTESIAN_POINT ( 'NONE',  ( 126.3671785243095940, -8.628592065323934079, -16.79579074909501202 ) ) ;
#39919=CARTESIAN_POINT ( 'NONE',  ( 127.3434826498009755, -10.05615397309841441, -11.38986721830345061 ) ) ;
#39920=CARTESIAN_POINT ( 'NONE',  ( 114.1009748109119784, -4.089484607189486809, -7.948022111789456723 ) ) ;
#39924=CARTESIAN_POINT ( 'NONE',  ( 113.8740681442453138, -9.859900752359374465, -12.68260735090039404 ) ) ;
#39926=CARTESIAN_POINT ( 'NONE',  ( 112.9664414775786412, 0.5811942927096154232, -14.16772938898807155 ) ) ;
#39927=CARTESIAN_POINT ( 'NONE',  ( 119.6601881442453106, -8.166667518702819706, -8.995218007635861213 ) ) ;
#39929=CARTESIAN_POINT ( 'NONE',  ( 119.5668260817262336, -2.423081321603731908, -17.89265170041263175 ) ) ;
#39932=CARTESIAN_POINT ( 'NONE',  ( 119.8303681442453126, 0.4262465694468514643, -12.03445270309931736 ) ) ;
#39933=CARTESIAN_POINT ( 'NONE',  ( 114.4980614775786592, -7.893985811506177619, -18.51759400769804742 ) ) ;
#39934=CARTESIAN_POINT ( 'NONE',  ( 114.8384214775786489, 0.9020085738987339008, -11.91225656197089222 ) ) ;
#39935=CARTESIAN_POINT ( 'NONE',  ( 118.3179530757767566, -0.9924539043446216624, -17.29976612834909133 ) ) ;
#39936=CARTESIAN_POINT ( 'NONE',  ( 121.6456214775786293, 0.4262465694468514643, -12.03445270309931736 ) ) ;
#39937=CARTESIAN_POINT ( 'NONE',  ( 119.2631014775786298, -9.565557343593413364, -10.61323700422348004 ) ) ;
#39941=CARTESIAN_POINT ( 'NONE',  ( 113.4769814775786330, -10.63000616557722466, -14.87417383870573495 ) ) ;
#39942=CARTESIAN_POINT ( 'NONE',  ( 118.2987481442453088, -7.894159318335828068, -9.358103419637847864 ) ) ;
#39943=EDGE_LOOP ( 'NONE', ( #36210, #27910, #30614, #25015 ) ) ;
#39945=CARTESIAN_POINT ( 'NONE',  ( 115.1787814775786387, -9.988377603198976828, -10.36322818467138340 ) ) ;
#39947=CARTESIAN_POINT ( 'NONE',  ( 113.6471614775786492, -4.153390946401321671, -8.397313243818183892 ) ) ;
#39950=CARTESIAN_POINT ( 'NONE',  ( 123.1772414775786189, -5.574606645277164318, -18.38911715685844683 ) ) ;
#39951=CARTESIAN_POINT ( 'NONE',  ( 122.7234281442452755, -4.153390946401325223, -8.397313243818185668 ) ) ;
#39958=CARTESIAN_POINT ( 'NONE',  ( 115.1787814775786387, -9.988377603198976828, -10.36322818467138340 ) ) ;
#39959=CARTESIAN_POINT ( 'NONE',  ( 113.9307948109119906, 0.9020085738987339008, -11.91225656197089222 ) ) ;
#39960=CARTESIAN_POINT ( 'NONE',  ( 115.5758681442453053, -7.894159318335828068, -9.358103419637847864 ) ) ;
#39961=CARTESIAN_POINT ( 'NONE',  ( 120.5110881442453206, -3.505236298600246325, -18.68346056562440793 ) ) ;
#39964=CARTESIAN_POINT ( 'NONE',  ( 118.4689281442453392, -10.15424416112533912, -14.75197769757731336 ) ) ;
#39965=DIRECTION ( 'NONE',  ( -1.000000000000000000, 0.000000000000000000, 0.000000000000000000 ) ) ;
#39967=CARTESIAN_POINT ( 'NONE',  ( 113.9997534719562395, -1.125321370491267237, -17.12283323191015327 ) ) ;
#39969=CARTESIAN_POINT ( 'NONE',  ( 117.2209414775786485, -7.893985811506177619, -18.51759400769804742 ) ) ;
#39971=CARTESIAN_POINT ( 'NONE',  ( 122.0427081442452817, 0.5811942927096110934, -14.16772938898807510 ) ) ;
#39974=CARTESIAN_POINT ( 'NONE',  ( 115.6893214775786447, 0.5811942927096154232, -14.16772938898807155 ) ) ;
#39975=CARTESIAN_POINT ( 'NONE',  ( 117.2209414775786485, -7.893985811506177619, -18.51759400769804742 ) ) ;
#39978=VERTEX_POINT ( 'NONE', #3069 ) ;
#39981=CARTESIAN_POINT ( 'NONE',  ( 119.0361948109119652, -2.084020599724406786, -8.691656652584148546 ) ) ;
#39984=CARTESIAN_POINT ( 'NONE',  ( 118.7525614775786380, -1.833838273342659253, -17.42832698103878286 ) ) ;
#39987=CARTESIAN_POINT ( 'NONE',  ( 111.7184548109119788, -0.8288870151387760510, -10.36305467784173118 ) ) ;
#39988=CARTESIAN_POINT ( 'NONE',  ( 119.1496481442453046, -3.383040157471821630, -19.15922257007629170 ) ) ;
#39990=CARTESIAN_POINT ( 'NONE',  ( 120.2841814775786276, -10.15424416112533912, -14.75197769757731336 ) ) ;
#39991=CARTESIAN_POINT ( 'NONE',  ( 116.1431348109119881, -10.30919188438810075, -12.61870101168855918 ) ) ;
#39992=CARTESIAN_POINT ( 'NONE',  ( 121.3052614775786111, -1.834011780172310813, -8.268836392978581529 ) ) ;
#39994=CARTESIAN_POINT ( 'NONE',  ( 119.4332814775786318, -8.899110576539710493, -16.42337572283490132 ) ) ;
#39996=CARTESIAN_POINT ( 'NONE',  ( 125.7866681442452688, -8.899110576539710493, -16.42337572283490132 ) ) ;
#39997=CARTESIAN_POINT ( 'NONE',  ( 118.9794681442453026, -9.261995988541697145, -16.69588392320189030 ) ) ;
#40000=CARTESIAN_POINT ( 'NONE',  ( 122.7801548109119665, -3.383040157471821630, -19.15922257007629170 ) ) ;
#40001=CARTESIAN_POINT ( 'NONE',  ( 117.4110664975817713, -2.215723800389698184, -18.16877924232191788 ) ) ;
#40009=CARTESIAN_POINT ( 'NONE',  ( 119.3198281442452924, -9.859900752359374465, -12.68260735090039404 ) ) ;
#40010=CARTESIAN_POINT ( 'NONE',  ( 125.5597614775786326, -1.561330072975669392, -17.79121239304076951 ) ) ;
#40015=CARTESIAN_POINT ( 'NONE',  ( 115.5758681442453053, -7.894159318335828068, -9.358103419637847864 ) ) ;
#40016=CARTESIAN_POINT ( 'NONE',  ( 115.0252186403692320, -1.196538596002799215, -17.02799684832027083 ) ) ;
#40020=CARTESIAN_POINT ( 'NONE',  ( 122.7234281442452755, -5.638512984488999180, -18.83840828888717311 ) ) ;
#40021=CARTESIAN_POINT ( 'NONE',  ( 123.9146881442452894, -10.15424416112533912, -14.75197769757731336 ) ) ;
#40023=CARTESIAN_POINT ( 'NONE',  ( 111.7184548109119788, -9.261995988541697145, -16.69588392320189030 ) ) ;
#40024=CARTESIAN_POINT ( 'NONE',  ( 125.1626748109119802, -9.988377603198980381, -10.36322818467138518 ) ) ;
#40027=CARTESIAN_POINT ( 'NONE',  ( 122.6099748109119929, -0.8288870151387760510, -10.36305467784173118 ) ) ;
#40028=CARTESIAN_POINT ( 'NONE',  ( 118.8660148109119774, 0.1319031606808879209, -14.10382304977623669 ) ) ;
#40029=CARTESIAN_POINT ( 'NONE',  ( 121.0408330757767459, -0.9924539043446216624, -17.29976612834909133 ) ) ;
#40033=DIRECTION ( 'NONE',  ( 0.000000000000000000, 0.6004852223388321697, -0.7996358532186279566 ) ) ;
#40037=CARTESIAN_POINT ( 'NONE',  ( 122.8936081442453059, 0.2603800115204892296, -16.42320221600525088 ) ) ;
#40038=CARTESIAN_POINT ( 'NONE',  ( 117.9583881442453048, -10.30919188438810075, -12.61870101168855918 ) ) ;
#40040=CARTESIAN_POINT ( 'NONE',  ( 114.8951481442453115, -0.4660016031367893996, -10.09054647747474043 ) ) ;
#40041=CARTESIAN_POINT ( 'NONE',  ( 123.7184548109119788, -4.683672500039349984, -14.88233656108870662 ) ) ;
#40044=CARTESIAN_POINT ( 'NONE',  ( 124.2550481442452792, -9.988377603198980381, -10.36322818467138518 ) ) ;
#40045=CARTESIAN_POINT ( 'NONE',  ( 120.5678148109119832, -8.166667518702819706, -8.995218007635861213 ) ) ;
#40047=CARTESIAN_POINT ( 'NONE',  ( 124.4252281442452812, -0.8288870151387760510, -10.36305467784173118 ) ) ;
#40048=CARTESIAN_POINT ( 'NONE',  ( 112.9097148109120070, -9.565557343593413364, -10.61323700422348004 ) ) ;
#40049=CARTESIAN_POINT ( 'NONE',  ( 112.2289948109119848, -7.643976991954077427, -18.09477374809248928 ) ) ;
#40050=ADVANCED_FACE ( 'NONE', ( #37951 ), #32089, .T. ) ;
#40053=CARTESIAN_POINT ( 'NONE',  ( 118.9227414775786542, 0.4262465694468514643, -12.03445270309931736 ) ) ;
#40058=EDGE_CURVE ( 'NONE', #32113, #37411, #43536, .T. ) ;
#40061=CARTESIAN_POINT ( 'NONE',  ( 123.3474214775786209, -9.988377603198976828, -10.36322818467138340 ) ) ;
#40064=CARTESIAN_POINT ( 'NONE',  ( 117.7314814775786260, -5.574606645277164318, -18.38911715685844683 ) ) ;
#40067=CARTESIAN_POINT ( 'NONE',  ( 122.8368814775786291, -7.894159318335828068, -9.358103419637847864 ) ) ;
#40068=B_SPLINE_CURVE_WITH_KNOTS ( 'NONE', 3,
 ( #9115, #44458, #33949, #19149, #33032, #9342, #40583, #12318, #23018, #23251, #1806, #30536, #40127, #26450, #37133, #8891, #22789, #5909, #19829, #27123, #2717, #13224, #36683 ),
 .UNSPECIFIED., .F., .F.,
 ( 4, 2, 2, 1, 1, 2, 2, 2, 1, 1, 1, 2, 2, 4 ),
 ( 0.000000000000000000, 0.1249999999999793499, 0.1874999999999680811, 0.2187499999999644451, 0.2343749999999615308, 0.2421874999999592548, 0.2499999999999569511, 0.3749999999999196754, 0.4374999999999041322, 0.4687499999998942513, 0.4843749999998913647, 0.4921874999998912537, 0.4999999999998911981, 1.000000000000000000 ),
 .UNSPECIFIED. ) ;
#40070=EDGE_CURVE ( 'NONE', #39689, #44717, #39213, .T. ) ;
#40074=CARTESIAN_POINT ( 'NONE',  ( 123.2906948109119867, -8.166667518702819706, -8.995218007635861213 ) ) ;
#40075=CARTESIAN_POINT ( 'NONE',  ( 116.8238548109119819, -5.574606645277164318, -18.38911715685844683 ) ) ;
#40076=CARTESIAN_POINT ( 'NONE',  ( 122.5532481442453019, 0.4262465694468514643, -12.03445270309931736 ) ) ;
#40079=CARTESIAN_POINT ( 'NONE',  ( 123.8579614775786126, 0.5811942927096110934, -14.16772938898807510 ) ) ;
#40080=CARTESIAN_POINT ( 'NONE',  ( 114.2711548109119803, -9.988377603198976828, -10.36322818467138340 ) ) ;
#40082=CARTESIAN_POINT ( 'NONE',  ( 138.2184548109119930, -4.863998795839242995, -13.39321520033831447 ) ) ;
#40085=CARTESIAN_POINT ( 'NONE',  ( 123.2339681442453241, -3.505236298600246325, -18.68346056562440793 ) ) ;
#40086=CARTESIAN_POINT ( 'NONE',  ( 121.1350814775786233, 0.5811942927096110934, -14.16772938898807510 ) ) ;
#40090=CARTESIAN_POINT ( 'NONE',  ( 113.5904348109119866, -2.084020599724406786, -8.691656652584148546 ) ) ;
#40096=CARTESIAN_POINT ( 'NONE',  ( 125.1059481442452750, -1.833838273342660141, -17.42832698103878286 ) ) ;
#40102=CARTESIAN_POINT ( 'NONE',  ( 119.7736414775786358, -10.30919188438810075, -12.61870101168855918 ) ) ;
#40103=CARTESIAN_POINT ( 'NONE',  ( 112.9204024739652112, 0.3208234527006389447, -15.99825685930876595 ) ) ;
#40104=CARTESIAN_POINT ( 'NONE',  ( 122.6099748109119929, -0.8288870151387760510, -10.36305467784173118 ) ) ;
#40105=CARTESIAN_POINT ( 'NONE',  ( 114.1577014775786552, -3.505236298600246325, -18.68346056562440793 ) ) ;
#40107=CARTESIAN_POINT ( 'NONE',  ( 123.9714148109119805, -0.4660016031367668621, -10.09054647747477063 ) ) ;
#40108=CARTESIAN_POINT ( 'NONE',  ( 113.7606148109119886, -1.561330072975668060, -17.79121239304076596 ) ) ;
#40111=CARTESIAN_POINT ( 'NONE',  ( 125.9001214775786224, -4.089484607189486809, -7.948022111789456723 ) ) ;
#40113=VERTEX_POINT ( 'NONE', #17874 ) ;
#40114=CARTESIAN_POINT ( 'NONE',  ( 115.9729548109119861, -6.344957434206662583, -7.627207830600332805 ) ) ;
#40115=CARTESIAN_POINT ( 'NONE',  ( 114.3278814775786429, 0.1319031606808879209, -14.10382304977623669 ) ) ;
#40117=EDGE_CURVE ( 'NONE', #17200, #452, #8206, .T. ) ;
#40118=CARTESIAN_POINT ( 'NONE',  ( 113.7606148109119886, -1.561330072975668060, -17.79121239304076596 ) ) ;
#40119=ORIENTED_EDGE ( 'NONE', *, *, #1608, .T. ) ;
#40121=CARTESIAN_POINT ( 'NONE',  ( 122.4965214775786251, -10.30919188438810075, -12.61870101168855918 ) ) ;
#40125=CARTESIAN_POINT ( 'NONE',  ( 111.8886348109120092, -6.222761293078232114, -8.102969835052212133 ) ) ;
#40127=CARTESIAN_POINT ( 'NONE',  ( 123.5612461215935554, -4.267240530208148641, -15.43691621075543452 ) ) ;
#40128=CARTESIAN_POINT ( 'NONE',  ( 115.1787814775786387, -0.1624402480850797581, -16.17319339645315424 ) ) ;
#40131=CARTESIAN_POINT ( 'NONE',  ( 125.6164881442453094, 0.2603800115204892296, -16.42320221600525088 ) ) ;
#40132=CARTESIAN_POINT ( 'NONE',  ( 112.3991748109119868, -8.166667518702817929, -8.995218007635859436 ) ) ;
#40134=CARTESIAN_POINT ( 'NONE',  ( 111.8319081442453182, -5.638512984488999180, -18.83840828888717311 ) ) ;
#40135=CARTESIAN_POINT ( 'NONE',  ( 114.3278814775786429, 0.1319031606808879209, -14.10382304977623669 ) ) ;
#40136=CARTESIAN_POINT ( 'NONE',  ( 122.0994348109119443, 0.9020085738987339008, -11.91225656197089222 ) ) ;
#40138=CARTESIAN_POINT ( 'NONE',  ( 122.8368814775786291, -1.561330072975668948, -17.79121239304076951 ) ) ;
#40140=CARTESIAN_POINT ( 'NONE',  ( 127.0915067942439691, -8.465631742269270177, -17.46559197649120776 ) ) ;
#40145=CARTESIAN_POINT ( 'NONE',  ( 125.5492214775786550, -6.210324830719740064, -8.151390318758597431 ) ) ;
#40146=CARTESIAN_POINT ( 'NONE',  ( 116.2565881442452991, -9.261995988541697145, -16.69588392320189030 ) ) ;
#40148=CARTESIAN_POINT ( 'NONE',  ( 124.9924948109119924, -4.089484607189486809, -7.948022111789456723 ) ) ;
#40152=CARTESIAN_POINT ( 'NONE',  ( 113.6471614775786492, -4.153390946401321671, -8.397313243818183892 ) ) ;
#40153=( BOUNDED_SURFACE ( )  B_SPLINE_SURFACE ( 1, 2, ( 
 ( #25694, #11112, #28891, #32515, #14527, #39600, #11564, #14978, #28441, #391, #8361, #7678, #28668, #24788, #32298, #836, #17948, #4485, #4254, #1063, #39144, #7909, #22265, #18406, #39375, #35710, #18172, #36159, #21816, #38680, #21366, #35937, #7446, #14755, #25471, #29106, #25014, #8143, #4928, #18843, #22044, #4705, #14304, #18625, #35480, #1290, #38907, #28222, #42572, #42129, #35249, #21593, #4026, #31847, #617, #11335, #40040, #36381, #33399, #33179, #40272, #43689, #19522, #8806, #9039, #5599, #43248, #37053, #12465, #26590, #12239, #12013, #40503, #1955, #37284, #39820, #8587, #32734, #6052, #23175, #22710, #16332, #22936, #2173, #15881, #25915, #15428, #5824, #44156, #19300, #29778, #36829, #26365, #22487, #30006, #29556, #1508, #16103, #29333, #19744, #43922, #5152, #33628, #19069, #32953, #40729, #1730, #15655, #9264, #36608, #12691, #43473, #2404, #30234, #12921, #26136, #5383, #26817, #9485, #23398, #13371, #34095, #20210, #2862, #13812, #17236, #6289, #38191, #27723, #3534, #27275, #10394, #3092, #27045, #16792, #20434, #37516, #2632, #10174, #24519, #38406, #23863, #20875, #41639, #17018, #30688, #9949, #37749, #24304, #41189, #24080, #27499, #44607, #40963, #6749, #6519, #6967, #34752, #34318, #19974, #37973, #30910, #17450, #44832, #31345, #13589, #27946, #16564, #33862, #41419, #9717, #41856, #31127, #45052, #119, #3314, #20659, #14032, #10617, #30459, #34535, #44379, #13142, #23630, #25418, #4432, #39319, #4649, #779, #35427, #38621, #1012, #18571, #28839, #8087, #7398, #566, #28615, #18121, #42524, #3975, #11285, #18349, #339, #21989, #4203, #10837, #35879, #34964, #24962, #14701, #14252, #25193, #39091, #28169, #32463, #7860, #1238, #14928, #32016, #15150, #42749, #31794, #11514, #29056, #21316, #7626, #42964, #21540, #35200, #11730, #21766, #17674, #25644, #35660, #3752, #7177, #31570, #21086, #42078, #32241, #24733, #17897, #11059, #14476, #28385, #42297, #38858, #12411, #33347, #29723, #43416, #16283, #1896, #4877, #15374, #29956 ),
 ( #2121, #5328, #36997, #16050, #19013, #43871, #12643, #25858, #39987, #5768, #8753, #8533, #19689, #33127, #18795, #30185, #19244, #36106, #26539, #32684, #40449, #9211, #15824, #22658, #36554, #22435, #12182, #1454, #43637, #11959, #32899, #36328, #39763, #5098, #23120, #36776, #1675, #33576, #2351, #44103, #15598, #12868, #26311, #29278, #29501, #40219, #26083, #22210, #8984, #39547, #8309, #22882, #43194, #5547, #19464, #44330, #16739, #30634, #34481, #2810, #16963, #34267, #26988, #33809, #13539, #44550, #3260, #13762, #13314, #66, #30857, #37698, #17185, #23810, #31075, #20381, #34700, #23342, #26768, #6470, #2580, #3487, #24029, #37919, #45002, #10125, #44780, #20821, #27671, #41586, #27221, #31292, #10343, #41138, #24248, #6695, #38140, #6912, #3041, #9898, #13090, #20606, #17403, #40677, #9429, #6000, #37226, #27447, #19923, #16510, #30409, #40908, #9662, #23581, #34042, #37464, #41369, #6237, #20159, #7128, #41806, #32185, #25364, #509, #11007, #21485, #14420, #21039, #11231, #10784, #27892, #31957, #10564, #4371, #24906, #34912, #14873, #13978, #287, #21931, #28115, #42020, #21712, #21263, #35370, #24460, #42468, #24681, #42691, #3703, #11460, #35599, #31515, #38568, #31740, #7572, #14646, #38352, #17622, #8024, #32409, #28785, #39260, #7346, #25139, #957, #35144, #35823, #39033, #28561, #3923, #14198, #4597, #17843, #42242, #28330, #723, #38802, #4148, #18066, #7804, #18290, #18518, #39936, #23059, #19189, #40164, #36502, #5044, #36945, #8697, #11676, #22158, #36720, #25585, #15539, #43584, #15995, #43132, #5271, #5715, #19633, #22828, #22602, #43817, #33068, #36277, #1840, #29225, #1182, #1618, #33296, #15769, #8477, #26031, #18742, #36052, #15096, #22381, #4819, #29672, #29444, #12354, #12128, #26254, #18959, #8926, #5489, #39487, #19409, #2072, #29901, #25803, #12582, #26487, #11902, #40391, #29005, #42914, #9153, #8252, #32633, #1399, #32849, #15315, #39713, #43359, #23522, #44725, #30572, #44276, #33984, #23285, #26709, #3206, #30351, #9376 ) ),
 .UNSPECIFIED., .F., .F., .T. ) 
 B_SPLINE_SURFACE_WITH_KNOTS ( ( 2, 2 ),
 ( 3, 2, 2, 2, 2, 2, 2, 2, 2, 2, 2, 2, 2, 2, 2, 2, 2, 2, 2, 2, 2, 2, 2, 2, 2, 2, 2, 2, 2, 2, 2, 2, 2, 2, 2, 2, 2, 2, 2, 2, 2, 2, 2, 2, 2, 2, 2, 2, 2, 2, 2, 2, 2, 2, 2, 2, 2, 2, 2, 2, 2, 2, 2, 2, 2, 2, 2, 2, 2, 2, 2, 2, 2, 2, 2, 2, 2, 2, 2, 2, 2, 2, 2, 2, 2, 2, 2, 2, 2, 2, 2, 2, 2, 2, 2, 2, 2, 2, 2, 2, 2, 2, 2, 2, 2, 2, 2, 2, 2, 2, 2, 2, 2, 2, 2, 2, 2, 2, 2, 2, 2, 2, 2, 2, 2, 2, 2, 2, 3 ),
 ( 0.000000000000000000, 1.000000000000000000 ),
 ( 0.000000000000000000, 0.007812500000000000000, 0.01562500000000000000, 0.02343750000000000000, 0.03125000000000000000, 0.03906250000000000000, 0.04687500000000000000, 0.05468750000000000000, 0.06250000000000000000, 0.07031250000000000000, 0.07812500000000000000, 0.08593750000000000000, 0.09375000000000000000, 0.1015625000000000000, 0.1093750000000000000, 0.1171875000000000000, 0.1250000000000000000, 0.1328125000000000000, 0.1406250000000000000, 0.1484375000000000000, 0.1562500000000000000, 0.1640625000000000000, 0.1718750000000000000, 0.1796875000000000000, 0.1875000000000000000, 0.1953125000000000000, 0.2031250000000000000, 0.2109375000000000000, 0.2187500000000000000, 0.2265625000000000000, 0.2343750000000000000, 0.2421875000000000000, 0.2500000000000000000, 0.2578125000000000000, 0.2656250000000000000, 0.2734375000000000000, 0.2812500000000000000, 0.2890625000000000000, 0.2968750000000000000, 0.3046875000000000000, 0.3125000000000000000, 0.3203125000000000000, 0.3281250000000000000, 0.3359375000000000000, 0.3437500000000000000, 0.3515625000000000000, 0.3593750000000000000, 0.3671875000000000000, 0.3750000000000000000, 0.3828125000000000000, 0.3906250000000000000, 0.3984375000000000000, 0.4062500000000000000, 0.4140625000000000000, 0.4218750000000000000, 0.4296875000000000000, 0.4375000000000000000, 0.4453125000000000000, 0.4531250000000000000, 0.4609375000000000000, 0.4687500000000000000, 0.4765625000000000000, 0.4843750000000000000, 0.4921875000000000000, 0.5000000000000000000, 0.5078125000000000000, 0.5156250000000000000, 0.5234375000000000000, 0.5312500000000000000, 0.5390625000000000000, 0.5468750000000000000, 0.5546875000000000000, 0.5625000000000000000, 0.5703125000000000000, 0.5781250000000000000, 0.5859375000000000000, 0.5937500000000000000, 0.6015625000000000000, 0.6093750000000000000, 0.6171875000000000000, 0.6250000000000000000, 0.6328125000000000000, 0.6406250000000000000, 0.6484375000000000000, 0.6562500000000000000, 0.6640625000000000000, 0.6718750000000000000, 0.6796875000000000000, 0.6875000000000000000, 0.6953125000000000000, 0.7031250000000000000, 0.7109375000000000000, 0.7187500000000000000, 0.7265625000000000000, 0.7343750000000000000, 0.7421875000000000000, 0.7500000000000000000, 0.7578125000000000000, 0.7656250000000000000, 0.7734375000000000000, 0.7812500000000000000, 0.7890625000000000000, 0.7968750000000000000, 0.8046875000000000000, 0.8125000000000000000, 0.8203125000000000000, 0.8281250000000000000, 0.8359375000000000000, 0.8437500000000000000, 0.8515625000000000000, 0.8593750000000000000, 0.8671875000000000000, 0.8750000000000000000, 0.8828125000000000000, 0.8906250000000000000, 0.8984375000000000000, 0.9062500000000000000, 0.9140625000000000000, 0.9218750000000000000, 0.9296875000000000000, 0.9375000000000000000, 0.9453125000000000000, 0.9531250000000000000, 0.9609375000000000000, 0.9687500000000000000, 0.9765625000000000000, 0.9843750000000000000, 0.9921875000000000000, 1.000000000000000000 ),
 .UNSPECIFIED. ) 
 GEOMETRIC_REPRESENTATION_ITEM ( )  RATIONAL_B_SPLINE_SURFACE ( (
 ( 1.000000000000000000, 0.9238795325112869605, 1.000000000000000000, 0.9238795325112869605, 1.000000000000000000, 0.9238795325112869605, 1.000000000000000000, 0.9238795325112869605, 1.000000000000000000, 0.9238795325112869605, 1.000000000000000000, 0.9238795325112869605, 1.000000000000000000, 0.9238795325112869605, 1.000000000000000000, 0.9238795325112869605, 1.000000000000000000, 0.9238795325112869605, 1.000000000000000000, 0.9238795325112869605, 1.000000000000000000, 0.9238795325112869605, 1.000000000000000000, 0.9238795325112869605, 1.000000000000000000, 0.9238795325112869605, 1.000000000000000000, 0.9238795325112869605, 1.000000000000000000, 0.9238795325112869605, 1.000000000000000000, 0.9238795325112869605, 1.000000000000000000, 0.9238795325112869605, 1.000000000000000000, 0.9238795325112869605, 1.000000000000000000, 0.9238795325112869605, 1.000000000000000000, 0.9238795325112869605, 1.000000000000000000, 0.9238795325112869605, 1.000000000000000000, 0.9238795325112869605, 1.000000000000000000, 0.9238795325112869605, 1.000000000000000000, 0.9238795325112869605, 1.000000000000000000, 0.9238795325112869605, 1.000000000000000000, 0.9238795325112869605, 1.000000000000000000, 0.9238795325112869605, 1.000000000000000000, 0.9238795325112869605, 1.000000000000000000, 0.9238795325112869605, 1.000000000000000000, 0.9238795325112869605, 1.000000000000000000, 0.9238795325112869605, 1.000000000000000000, 0.9238795325112869605, 1.000000000000000000, 0.9238795325112869605, 1.000000000000000000, 0.9238795325112869605, 1.000000000000000000, 0.9238795325112869605, 1.000000000000000000, 0.9238795325112869605, 1.000000000000000000, 0.9238795325112869605, 1.000000000000000000, 0.9238795325112869605, 1.000000000000000000, 0.9238795325112869605, 1.000000000000000000, 0.9238795325112869605, 1.000000000000000000, 0.9238795325112869605, 1.000000000000000000, 0.9238795325112869605, 1.000000000000000000, 0.9238795325112869605, 1.000000000000000000, 0.9238795325112869605, 1.000000000000000000, 0.9238795325112869605, 1.000000000000000000, 0.9238795325112869605, 1.000000000000000000, 0.9238795325112869605, 1.000000000000000000, 0.9238795325112869605, 1.000000000000000000, 0.9238795325112869605, 1.000000000000000000, 0.9238795325112869605, 1.000000000000000000, 0.9238795325112869605, 1.000000000000000000, 0.9238795325112869605, 1.000000000000000000, 0.9238795325112869605, 1.000000000000000000, 0.9238795325112869605, 1.000000000000000000, 0.9238795325112869605, 1.000000000000000000, 0.9238795325112869605, 1.000000000000000000, 0.9238795325112869605, 1.000000000000000000, 0.9238795325112869605, 1.000000000000000000, 0.9238795325112869605, 1.000000000000000000, 0.9238795325112869605, 1.000000000000000000, 0.9238795325112869605, 1.000000000000000000, 0.9238795325112869605, 1.000000000000000000, 0.9238795325112869605, 1.000000000000000000, 0.9238795325112869605, 1.000000000000000000, 0.9238795325112869605, 1.000000000000000000, 0.9238795325112869605, 1.000000000000000000, 0.9238795325112869605, 1.000000000000000000, 0.9238795325112869605, 1.000000000000000000, 0.9238795325112869605, 1.000000000000000000, 0.9238795325112869605, 1.000000000000000000, 0.9238795325112869605, 1.000000000000000000, 0.9238795325112869605, 1.000000000000000000, 0.9238795325112869605, 1.000000000000000000, 0.9238795325112869605, 1.000000000000000000, 0.9238795325112869605, 1.000000000000000000, 0.9238795325112869605, 1.000000000000000000, 0.9238795325112869605, 1.000000000000000000, 0.9238795325112869605, 1.000000000000000000, 0.9238795325112869605, 1.000000000000000000, 0.9238795325112869605, 1.000000000000000000, 0.9238795325112869605, 1.000000000000000000, 0.9238795325112869605, 1.000000000000000000, 0.9238795325112869605, 1.000000000000000000, 0.9238795325112869605, 1.000000000000000000, 0.9238795325112869605, 1.000000000000000000, 0.9238795325112869605, 1.000000000000000000, 0.9238795325112869605, 1.000000000000000000, 0.9238795325112869605, 1.000000000000000000, 0.9238795325112869605, 1.000000000000000000, 0.9238795325112869605, 1.000000000000000000, 0.9238795325112869605, 1.000000000000000000, 0.9238795325112869605, 1.000000000000000000, 0.9238795325112869605, 1.000000000000000000, 0.9238795325112869605, 1.000000000000000000, 0.9238795325112869605, 1.000000000000000000, 0.9238795325112869605, 1.000000000000000000, 0.9238795325112869605, 1.000000000000000000, 0.9238795325112869605, 1.000000000000000000, 0.9238795325112869605, 1.000000000000000000, 0.9238795325112869605, 1.000000000000000000, 0.9238795325112869605, 1.000000000000000000, 0.9238795325112869605, 1.000000000000000000, 0.9238795325112869605, 1.000000000000000000, 0.9238795325112869605, 1.000000000000000000, 0.9238795325112869605, 1.000000000000000000, 0.9238795325112869605, 1.000000000000000000, 0.9238795325112869605, 1.000000000000000000, 0.9238795325112869605, 1.000000000000000000, 0.9238795325112869605, 1.000000000000000000, 0.9238795325112869605, 1.000000000000000000, 0.9238795325112869605, 1.000000000000000000, 0.9238795325112869605, 1.000000000000000000, 0.9238795325112869605, 1.000000000000000000, 0.9238795325112869605, 1.000000000000000000, 0.9238795325112869605, 1.000000000000000000, 0.9238795325112869605, 1.000000000000000000, 0.9238795325112869605, 1.000000000000000000, 0.9238795325112869605, 1.000000000000000000, 0.9238795325112869605, 1.000000000000000000, 0.9238795325112869605, 1.000000000000000000, 0.9238795325112869605, 1.000000000000000000, 0.9238795325112869605, 1.000000000000000000, 0.9238795325112869605, 1.000000000000000000, 0.9238795325112869605, 1.000000000000000000, 0.9238795325112869605, 1.000000000000000000, 0.9238795325112869605, 1.000000000000000000, 0.9238795325112869605, 1.000000000000000000, 0.9238795325112869605, 1.000000000000000000),
 ( 1.000000000000000000, 0.9238795325112869605, 1.000000000000000000, 0.9238795325112869605, 1.000000000000000000, 0.9238795325112869605, 1.000000000000000000, 0.9238795325112869605, 1.000000000000000000, 0.9238795325112869605, 1.000000000000000000, 0.9238795325112869605, 1.000000000000000000, 0.9238795325112869605, 1.000000000000000000, 0.9238795325112869605, 1.000000000000000000, 0.9238795325112869605, 1.000000000000000000, 0.9238795325112869605, 1.000000000000000000, 0.9238795325112869605, 1.000000000000000000, 0.9238795325112869605, 1.000000000000000000, 0.9238795325112869605, 1.000000000000000000, 0.9238795325112869605, 1.000000000000000000, 0.9238795325112869605, 1.000000000000000000, 0.9238795325112869605, 1.000000000000000000, 0.9238795325112869605, 1.000000000000000000, 0.9238795325112869605, 1.000000000000000000, 0.9238795325112869605, 1.000000000000000000, 0.9238795325112869605, 1.000000000000000000, 0.9238795325112869605, 1.000000000000000000, 0.9238795325112869605, 1.000000000000000000, 0.9238795325112869605, 1.000000000000000000, 0.9238795325112869605, 1.000000000000000000, 0.9238795325112869605, 1.000000000000000000, 0.9238795325112869605, 1.000000000000000000, 0.9238795325112869605, 1.000000000000000000, 0.9238795325112869605, 1.000000000000000000, 0.9238795325112869605, 1.000000000000000000, 0.9238795325112869605, 1.000000000000000000, 0.9238795325112869605, 1.000000000000000000, 0.9238795325112869605, 1.000000000000000000, 0.9238795325112869605, 1.000000000000000000, 0.9238795325112869605, 1.000000000000000000, 0.9238795325112869605, 1.000000000000000000, 0.9238795325112869605, 1.000000000000000000, 0.9238795325112869605, 1.000000000000000000, 0.9238795325112869605, 1.000000000000000000, 0.9238795325112869605, 1.000000000000000000, 0.9238795325112869605, 1.000000000000000000, 0.9238795325112869605, 1.000000000000000000, 0.9238795325112869605, 1.000000000000000000, 0.9238795325112869605, 1.000000000000000000, 0.9238795325112869605, 1.000000000000000000, 0.9238795325112869605, 1.000000000000000000, 0.9238795325112869605, 1.000000000000000000, 0.9238795325112869605, 1.000000000000000000, 0.9238795325112869605, 1.000000000000000000, 0.9238795325112869605, 1.000000000000000000, 0.9238795325112869605, 1.000000000000000000, 0.9238795325112869605, 1.000000000000000000, 0.9238795325112869605, 1.000000000000000000, 0.9238795325112869605, 1.000000000000000000, 0.9238795325112869605, 1.000000000000000000, 0.9238795325112869605, 1.000000000000000000, 0.9238795325112869605, 1.000000000000000000, 0.9238795325112869605, 1.000000000000000000, 0.9238795325112869605, 1.000000000000000000, 0.9238795325112869605, 1.000000000000000000, 0.9238795325112869605, 1.000000000000000000, 0.9238795325112869605, 1.000000000000000000, 0.9238795325112869605, 1.000000000000000000, 0.9238795325112869605, 1.000000000000000000, 0.9238795325112869605, 1.000000000000000000, 0.9238795325112869605, 1.000000000000000000, 0.9238795325112869605, 1.000000000000000000, 0.9238795325112869605, 1.000000000000000000, 0.9238795325112869605, 1.000000000000000000, 0.9238795325112869605, 1.000000000000000000, 0.9238795325112869605, 1.000000000000000000, 0.9238795325112869605, 1.000000000000000000, 0.9238795325112869605, 1.000000000000000000, 0.9238795325112869605, 1.000000000000000000, 0.9238795325112869605, 1.000000000000000000, 0.9238795325112869605, 1.000000000000000000, 0.9238795325112869605, 1.000000000000000000, 0.9238795325112869605, 1.000000000000000000, 0.9238795325112869605, 1.000000000000000000, 0.9238795325112869605, 1.000000000000000000, 0.9238795325112869605, 1.000000000000000000, 0.9238795325112869605, 1.000000000000000000, 0.9238795325112869605, 1.000000000000000000, 0.9238795325112869605, 1.000000000000000000, 0.9238795325112869605, 1.000000000000000000, 0.9238795325112869605, 1.000000000000000000, 0.9238795325112869605, 1.000000000000000000, 0.9238795325112869605, 1.000000000000000000, 0.9238795325112869605, 1.000000000000000000, 0.9238795325112869605, 1.000000000000000000, 0.9238795325112869605, 1.000000000000000000, 0.9238795325112869605, 1.000000000000000000, 0.9238795325112869605, 1.000000000000000000, 0.9238795325112869605, 1.000000000000000000, 0.9238795325112869605, 1.000000000000000000, 0.9238795325112869605, 1.000000000000000000, 0.9238795325112869605, 1.000000000000000000, 0.9238795325112869605, 1.000000000000000000, 0.9238795325112869605, 1.000000000000000000, 0.9238795325112869605, 1.000000000000000000, 0.9238795325112869605, 1.000000000000000000, 0.9238795325112869605, 1.000000000000000000, 0.9238795325112869605, 1.000000000000000000, 0.9238795325112869605, 1.000000000000000000, 0.9238795325112869605, 1.000000000000000000, 0.9238795325112869605, 1.000000000000000000, 0.9238795325112869605, 1.000000000000000000, 0.9238795325112869605, 1.000000000000000000, 0.9238795325112869605, 1.000000000000000000, 0.9238795325112869605, 1.000000000000000000, 0.9238795325112869605, 1.000000000000000000, 0.9238795325112869605, 1.000000000000000000, 0.9238795325112869605, 1.000000000000000000, 0.9238795325112869605, 1.000000000000000000, 0.9238795325112869605, 1.000000000000000000, 0.9238795325112869605, 1.000000000000000000, 0.9238795325112869605, 1.000000000000000000, 0.9238795325112869605, 1.000000000000000000, 0.9238795325112869605, 1.000000000000000000, 0.9238795325112869605, 1.000000000000000000, 0.9238795325112869605, 1.000000000000000000, 0.9238795325112869605, 1.000000000000000000, 0.9238795325112869605, 1.000000000000000000, 0.9238795325112869605, 1.000000000000000000, 0.9238795325112869605, 1.000000000000000000, 0.9238795325112869605, 1.000000000000000000, 0.9238795325112869605, 1.000000000000000000, 0.9238795325112869605, 1.000000000000000000, 0.9238795325112869605, 1.000000000000000000) ) ) 
 REPRESENTATION_ITEM ( '' )  SURFACE ( )  );
#40154=CARTESIAN_POINT ( 'NONE',  ( 121.2485348109119769, -0.4660016031367893996, -10.09054647747474043 ) ) ;
#40160=CARTESIAN_POINT ( 'NONE',  ( 119.7169148109119874, -0.1624402480850797581, -16.17319339645315424 ) ) ;
#40161=CARTESIAN_POINT ( 'NONE',  ( 118.4689281442453392, 0.9020085738987339008, -11.91225656197089222 ) ) ;
#40162=CARTESIAN_POINT ( 'NONE',  ( 114.0442481442453300, -1.834011780172310813, -8.268836392978581529 ) ) ;
#40163=CARTESIAN_POINT ( 'NONE',  ( 118.6842048136183365, -3.929494816604741203, -18.62311481910882804 ) ) ;
#40164=CARTESIAN_POINT ( 'NONE',  ( 121.8158014775786171, -4.153390946401325223, -8.397313243818185668 ) ) ;
#40165=CARTESIAN_POINT ( 'NONE',  ( 120.9649014775786355, -6.222761293078241884, -8.102969835052219238 ) ) ;
#40168=CARTESIAN_POINT ( 'NONE',  ( 113.3068014775786594, -8.166667518702817929, -8.995218007635859436 ) ) ;
#40169=CARTESIAN_POINT ( 'NONE',  ( 122.4965214775786251, 0.1319031606808879209, -14.10382304977623669 ) ) ;
#40172=CARTESIAN_POINT ( 'NONE',  ( 116.7671281442453335, -1.834011780172310813, -8.268836392978581529 ) ) ;
#40174=CARTESIAN_POINT ( 'NONE',  ( 116.3133148109120043, -2.084020599724406786, -8.691656652584148546 ) ) ;
#40175=ORIENTED_EDGE ( 'NONE', *, *, #7441, .T. ) ;
#40178=CARTESIAN_POINT ( 'NONE',  ( 123.6877814775786533, -6.222761293078241884, -8.102969835052219238 ) ) ;
#40179=CARTESIAN_POINT ( 'NONE',  ( 121.5888948109119809, 0.1319031606808879209, -14.10382304977623669 ) ) ;
#40184=CARTESIAN_POINT ( 'NONE',  ( 118.1852948109119836, -5.638512984488999180, -18.83840828888717311 ) ) ;
#40187=CARTESIAN_POINT ( 'NONE',  ( 117.1642148109119859, -9.261995988541697145, -16.69588392320189030 ) ) ;
#40188=CARTESIAN_POINT ( 'NONE',  ( 116.5969481442453031, 0.5811942927096154232, -14.16772938898807155 ) ) ;
#40189=CARTESIAN_POINT ( 'NONE',  ( 116.7671281442453335, -7.643976991954077427, -18.09477374809248928 ) ) ;
#40190=CARTESIAN_POINT ( 'NONE',  ( 122.4397948109119767, -0.1624402480850797581, -16.17319339645315424 ) ) ;
#40191=CARTESIAN_POINT ( 'NONE',  ( 113.4769814775786330, -10.63000616557722466, -14.87417383870573495 ) ) ;
#40193=CARTESIAN_POINT ( 'NONE',  ( 119.8870948109119752, -0.8288870151387760510, -10.36305467784173118 ) ) ;
#40199=CARTESIAN_POINT ( 'NONE',  ( 117.9016614775786280, -9.988377603198976828, -10.36322818467138340 ) ) ;
#40201=CARTESIAN_POINT ( 'NONE',  ( 119.6034614775786196, -6.344957434206665248, -7.627207830600338134 ) ) ;
#40204=CARTESIAN_POINT ( 'NONE',  ( 120.2841814775786276, 0.9020085738987339008, -11.91225656197089222 ) ) ;
#40205=CARTESIAN_POINT ( 'NONE',  ( 117.3343948109119737, -3.383040157471821630, -19.15922257007629170 ) ) ;
#40209=CARTESIAN_POINT ( 'NONE',  ( 128.2184548109119930, -4.863998795839242995, -13.39321520033831447 ) ) ;
#40211=CONICAL_SURFACE ( 'NONE', #18370, 5.999999999999997335, 0.4636476090008060935 ) ;
#40212=CARTESIAN_POINT ( 'NONE',  ( 119.2631014775786298, -9.565557343593413364, -10.61323700422348004 ) ) ;
#40216=CARTESIAN_POINT ( 'NONE',  ( 118.2420214775786320, -6.222761293078241884, -8.102969835052219238 ) ) ;
#40219=CARTESIAN_POINT ( 'NONE',  ( 113.8173414775786512, -9.565557343593413364, -10.61323700422348004 ) ) ;
#40220=CARTESIAN_POINT ( 'NONE',  ( 122.0994348109119443, 0.9020085738987339008, -11.91225656197089222 ) ) ;
#40222=CARTESIAN_POINT ( 'NONE',  ( 122.1561614775786353, -8.899110576539710493, -16.42337572283490132 ) ) ;
#40224=CARTESIAN_POINT ( 'NONE',  ( 114.3278814775786429, -10.30919188438810075, -12.61870101168855918 ) ) ;
#40225=CARTESIAN_POINT ( 'NONE',  ( 121.9292548109119849, -1.561330072975668948, -17.79121239304076951 ) ) ;
#40226=CARTESIAN_POINT ( 'NONE',  ( 122.2696148109119889, -5.574606645277164318, -18.38911715685844683 ) ) ;
#40228=CARTESIAN_POINT ( 'NONE',  ( 123.2906948109119867, -1.833838273342659697, -17.42832698103878286 ) ) ;
#40229=CARTESIAN_POINT ( 'NONE',  ( 124.6521348109119884, -1.561330072975668948, -17.79121239304076951 ) ) ;
#40232=CARTESIAN_POINT ( 'NONE',  ( 126.1837548109119211, -10.63000616557722466, -14.87417383870573495 ) ) ;
#40239=CARTESIAN_POINT ( 'NONE',  ( 120.5678148109119832, -1.833838273342659253, -17.42832698103878286 ) ) ;
#40240=CARTESIAN_POINT ( 'NONE',  ( 126.2404814775786264, -9.261995988541697145, -16.69588392320189030 ) ) ;
#40241=CARTESIAN_POINT ( 'NONE',  ( 126.9733055311670284, -0.02945601996773287642, -11.03864623346424523 ) ) ;
#40242=VERTEX_POINT ( 'NONE', #32880 ) ;
#40246=CARTESIAN_POINT ( 'NONE',  ( 117.7882081442453170, -3.505236298600246325, -18.68346056562440793 ) ) ;
#40252=CARTESIAN_POINT ( 'NONE',  ( 122.8368814775786291, -1.561330072975668948, -17.79121239304076951 ) ) ;
#40254=CARTESIAN_POINT ( 'NONE',  ( 121.1350814775786233, -9.859900752359378018, -12.68260735090039759 ) ) ;
#40255=ORIENTED_EDGE ( 'NONE', *, *, #33228, .T. ) ;
#40259=CARTESIAN_POINT ( 'NONE',  ( 120.1707281442453166, -9.565557343593413364, -10.61323700422348004 ) ) ;
#40260=CARTESIAN_POINT ( 'NONE',  ( 118.8092881442453290, -0.1624402480850797581, -16.17319339645315424 ) ) ;
#40261=CARTESIAN_POINT ( 'NONE',  ( 119.5633519737025523, -1.196538596002817867, -17.02799684832028504 ) ) ;
#40263=CARTESIAN_POINT ( 'NONE',  ( 116.7104014775786425, -0.4660016031367729128, -10.09054647747476174 ) ) ;
#40269=CARTESIAN_POINT ( 'NONE',  ( 120.0572748109119772, -3.383040157471821630, -19.15922257007629170 ) ) ;
#40270=CARTESIAN_POINT ( 'NONE',  ( 122.0427081442452817, 0.5811942927096110934, -14.16772938898807510 ) ) ;
#40271=FACE_OUTER_BOUND ( 'NONE', #43057, .T. ) ;
#40272=CARTESIAN_POINT ( 'NONE',  ( 115.1220548109119761, -8.166667518702817929, -8.995218007635861213 ) ) ;
#40277=CARTESIAN_POINT ( 'NONE',  ( 123.8012348109119642, 0.2603800115204892296, -16.42320221600525088 ) ) ;
#40279=CARTESIAN_POINT ( 'NONE',  ( 121.5888948109119809, -10.30919188438810075, -12.61870101168855918 ) ) ;
#40280=CARTESIAN_POINT ( 'NONE',  ( 124.8790414775786246, -8.899110576539710493, -16.42337572283490132 ) ) ;
#40282=CARTESIAN_POINT ( 'NONE',  ( 112.9664414775786412, -9.859900752359374465, -12.68260735090039404 ) ) ;
#40283=CARTESIAN_POINT ( 'NONE',  ( 115.6325948109119821, -9.565557343593413364, -10.61323700422348004 ) ) ;
#40284=CARTESIAN_POINT ( 'NONE',  ( 125.7866681442452688, -0.4660016031367893996, -10.09054647747474043 ) ) ;
#40285=CARTESIAN_POINT ( 'NONE',  ( 123.6310548109119765, -5.638512984488999180, -18.83840828888717311 ) ) ;
#40288=CARTESIAN_POINT ( 'NONE',  ( 120.3976348109119812, -7.643976991954077427, -18.09477374809248928 ) ) ;
#40293=CARTESIAN_POINT ( 'NONE',  ( 122.6099748109119929, -9.261995988541697145, -16.69588392320189030 ) ) ;
#40299=CARTESIAN_POINT ( 'NONE',  ( 122.8936081442453059, -9.565557343593413364, -10.61323700422348004 ) ) ;
#40300=CARTESIAN_POINT ( 'NONE',  ( 123.5288836215688235, -1.135392229370316919, -17.10942237759952533 ) ) ;
#40301=CARTESIAN_POINT ( 'NONE',  ( 123.9714148109119805, -8.899110576539710493, -16.42337572283490132 ) ) ;
#40304=CARTESIAN_POINT ( 'NONE',  ( 124.9924948109119924, -4.089484607189486809, -7.948022111789456723 ) ) ;
#40305=CARTESIAN_POINT ( 'NONE',  ( 119.3765548109119834, -10.15424416112533912, -14.75197769757731336 ) ) ;
#40308=CARTESIAN_POINT ( 'NONE',  ( 122.3830681442452857, -8.166667518702819706, -8.995218007635861213 ) ) ;
#40309=CARTESIAN_POINT ( 'NONE',  ( 116.6536748109119941, 0.9020085738987339008, -11.91225656197089222 ) ) ;
#40311=CARTESIAN_POINT ( 'NONE',  ( 112.9097148109120070, -9.565557343593413364, -10.61323700422348004 ) ) ;
#40312=CARTESIAN_POINT ( 'NONE',  ( 124.1983214775786166, -1.833838273342659697, -17.42832698103878286 ) ) ;
#40313=CARTESIAN_POINT ( 'NONE',  ( 122.6099748109119929, -9.261995988541697145, -16.69588392320189030 ) ) ;
#40318=CARTESIAN_POINT ( 'NONE',  ( 113.8173414775786512, -9.565557343593413364, -10.61323700422348004 ) ) ;
#40319=CARTESIAN_POINT ( 'NONE',  ( 117.2209414775786485, -2.084020599724406786, -8.691656652584148546 ) ) ;
#40322=VERTEX_POINT ( 'NONE', #36085 ) ;
#40323=CARTESIAN_POINT ( 'NONE',  ( 125.1626748109119802, -0.1624402480850797581, -16.17319339645315424 ) ) ;
#40330=CARTESIAN_POINT ( 'NONE',  ( 118.1285681442453068, -7.893985811506177619, -18.51759400769804742 ) ) ;
#40331=CARTESIAN_POINT ( 'NONE',  ( 124.7655881442452852, -9.859900752359378018, -12.68260735090039759 ) ) ;
#40332=CARTESIAN_POINT ( 'NONE',  ( 114.5547881442453217, -4.153390946401321671, -8.397313243818183892 ) ) ;
#40335=CARTESIAN_POINT ( 'NONE',  ( 114.3278814775786429, -10.30919188438810075, -12.61870101168855918 ) ) ;
#40338=CARTESIAN_POINT ( 'NONE',  ( 125.6164881442453094, 0.2603800115204892296, -16.42320221600525088 ) ) ;
#40342=CARTESIAN_POINT ( 'NONE',  ( 114.4413348109119823, -9.261995988541697145, -16.69588392320189030 ) ) ;
#40345=CARTESIAN_POINT ( 'NONE',  ( 113.3635281442453504, -0.1624402480850797581, -16.17319339645315424 ) ) ;
#40346=CARTESIAN_POINT ( 'NONE',  ( 126.5254139958929045, -4.932287615856277618, -18.54625524651014956 ) ) ;
#40347=CARTESIAN_POINT ( 'NONE',  ( 113.1933481442453058, -4.089484607189486809, -7.948022111789456723 ) ) ;
#40349=CARTESIAN_POINT ( 'NONE',  ( 122.9503348109119827, 0.5811942927096110934, -14.16772938898807510 ) ) ;
#40353=CARTESIAN_POINT ( 'NONE',  ( 112.4567343740715870, -2.419733177069674834, -17.89711025544712086 ) ) ;
#40354=CARTESIAN_POINT ( 'NONE',  ( 115.8595014775786609, -7.643976991954077427, -18.09477374809248928 ) ) ;
#40357=CARTESIAN_POINT ( 'NONE',  ( 113.1933481442453058, -5.574606645277164318, -18.38911715685844683 ) ) ;
#40358=CARTESIAN_POINT ( 'NONE',  ( 113.7606148109119886, -1.561330072975668060, -17.79121239304076596 ) ) ;
#40360=CARTESIAN_POINT ( 'NONE',  ( 126.0703014775786102, -0.1624402480850797581, -16.17319339645315424 ) ) ;
#40361=CARTESIAN_POINT ( 'NONE',  ( 114.8384214775786489, -10.15424416112533912, -14.75197769757731336 ) ) ;
#40362=CARTESIAN_POINT ( 'NONE',  ( 124.7088614775786226, 0.2603800115204892296, -16.42320221600525088 ) ) ;
#40364=CARTESIAN_POINT ( 'NONE',  ( 121.5321681442453183, -9.988377603198976828, -10.36322818467138340 ) ) ;
#40366=CARTESIAN_POINT ( 'NONE',  ( 113.0798948109119948, -0.4660016031367893996, -10.09054647747474043 ) ) ;
#40368=EDGE_CURVE ( 'NONE', #39689, #6914, #2366, .T. ) ;
#40372=CARTESIAN_POINT ( 'NONE',  ( 117.1074881442453233, -10.63000616557722466, -14.87417383870573495 ) ) ;
#40375=CARTESIAN_POINT ( 'NONE',  ( 124.2193060444391790, -1.267766418764731728, -16.93314635290706605 ) ) ;
#40376=CARTESIAN_POINT ( 'NONE',  ( 120.8557914811013347, -2.280480477428469488, -18.08254604495227014 ) ) ;
#40377=CARTESIAN_POINT ( 'NONE',  ( 115.4624148109119943, -4.153390946401321671, -8.397313243818183892 ) ) ;
#40378=EDGE_CURVE ( 'NONE', #6291, #40322, #32093, .T. ) ;
#40380=CARTESIAN_POINT ( 'NONE',  ( 121.5321681442453183, -9.988377603198976828, -10.36322818467138340 ) ) ;
#40381=ADVANCED_FACE ( 'NONE', ( #37479 ), #31531, .F. ) ;
#40383=FACE_OUTER_BOUND ( 'NONE', #23596, .T. ) ;
#40386=CARTESIAN_POINT ( 'NONE',  ( 122.4397948109119767, -0.1624402480850797581, -16.17319339645315424 ) ) ;
#40387=CARTESIAN_POINT ( 'NONE',  ( 120.6812681442452941, -10.30919188438810075, -12.61870101168855918 ) ) ;
#40388=CARTESIAN_POINT ( 'NONE',  ( 113.7038881442453402, -6.222761293078241884, -8.102969835052219238 ) ) ;
#40389=CARTESIAN_POINT ( 'NONE',  ( 114.5547881442453217, -5.638512984488999180, -18.83840828888717311 ) ) ;
#40390=CARTESIAN_POINT ( 'NONE',  ( 136.3817460758107813, -7.085787385089622248, -18.75052711434078390 ) ) ;
#40391=CARTESIAN_POINT ( 'NONE',  ( 124.6521348109119884, -7.894159318335828068, -9.358103419637847864 ) ) ;
#40392=CARTESIAN_POINT ( 'NONE',  ( 118.4122014775786340, -9.859900752359374465, -12.68260735090039404 ) ) ;
#40396=CARTESIAN_POINT ( 'NONE',  ( 112.6260814775786514, -9.261995988541697145, -16.69588392320189030 ) ) ;
#40397=CARTESIAN_POINT ( 'NONE',  ( 121.4187148109119789, -3.505236298600246325, -18.68346056562440793 ) ) ;
#40403=CARTESIAN_POINT ( 'NONE',  ( 117.2209414775786485, -7.893985811506177619, -18.51759400769804742 ) ) ;
#40406=CARTESIAN_POINT ( 'NONE',  ( 116.6536748109119941, -10.15424416112533912, -14.75197769757731336 ) ) ;
#40409=CARTESIAN_POINT ( 'NONE',  ( 124.1983214775786166, -1.833838273342659697, -17.42832698103878286 ) ) ;
#40410=B_SPLINE_CURVE_WITH_KNOTS ( 'NONE', 3,
 ( #41509, #13466, #6614, #31219 ),
 .UNSPECIFIED., .F., .F.,
 ( 4, 4 ),
 ( 0.01196303694811591892, 0.01338272309942444005 ),
 .UNSPECIFIED. ) ;
#40411=CARTESIAN_POINT ( 'NONE',  ( 120.2841814775786276, -10.15424416112533912, -14.75197769757731336 ) ) ;
#40414=CARTESIAN_POINT ( 'NONE',  ( 119.7169148109119874, -9.988377603198976828, -10.36322818467138340 ) ) ;
#40416=CARTESIAN_POINT ( 'NONE',  ( 116.9940348109119839, -9.988377603198976828, -10.36322818467138340 ) ) ;
#40417=CARTESIAN_POINT ( 'NONE',  ( 116.8238548109119819, -4.089484607189486809, -7.948022111789456723 ) ) ;
#40418=CARTESIAN_POINT ( 'NONE',  ( 115.4624148109119943, -4.153390946401321671, -8.397313243818183892 ) ) ;
#40420=CARTESIAN_POINT ( 'NONE',  ( 124.0848681442452772, -5.574606645277164318, -18.38911715685844683 ) ) ;
#40421=CARTESIAN_POINT ( 'NONE',  ( 112.1722681442453222, -0.4660016031367893996, -10.09054647747474043 ) ) ;
#40423=CARTESIAN_POINT ( 'NONE',  ( 123.9714148109119805, -8.899110576539710493, -16.42337572283490132 ) ) ;
#40424=CARTESIAN_POINT ( 'NONE',  ( 122.2076758011493922, -1.149058757900107697, -17.09122335155391781 ) ) ;
#40426=MECHANICAL_DESIGN_GEOMETRIC_PRESENTATION_REPRESENTATION('',(#30201),#9109);
#40430=CARTESIAN_POINT ( 'NONE',  ( 118.8660148109119774, -10.30919188438810075, -12.61870101168855918 ) ) ;
#40432=CARTESIAN_POINT ( 'NONE',  ( 119.0929214775786278, -5.638512984488999180, -18.83840828888717311 ) ) ;
#40433=CARTESIAN_POINT ( 'NONE',  ( 112.8529881442453302, -7.894159318335828068, -9.358103419637847864 ) ) ;
#40435=CARTESIAN_POINT ( 'NONE',  ( 120.6812681442452941, -10.30919188438810075, -12.61870101168855918 ) ) ;
#40436=CARTESIAN_POINT ( 'NONE',  ( 121.9859814775786333, 0.2603800115204892296, -16.42320221600525088 ) ) ;
#40443=CARTESIAN_POINT ( 'NONE',  ( 122.7801548109119665, -6.222761293078241884, -8.102969835052219238 ) ) ;
#40446=CARTESIAN_POINT ( 'NONE',  ( 116.9373081442452929, -1.833838273342659253, -17.42832698103878286 ) ) ;
#40449=CARTESIAN_POINT ( 'NONE',  ( 112.3991748109119868, -1.833838273342658809, -17.42832698103878286 ) ) ;
#40450=CARTESIAN_POINT ( 'NONE',  ( 122.0427081442452817, 0.5811942927096110934, -14.16772938898807510 ) ) ;
#40451=EDGE_CURVE ( 'NONE', #13784, #45010, #44271, .T. ) ;
#40452=VERTEX_POINT ( 'NONE', #6482 ) ;
#40453=CARTESIAN_POINT ( 'NONE',  ( 122.7234281442452755, -4.153390946401325223, -8.397313243818185668 ) ) ;
#40454=CARTESIAN_POINT ( 'NONE',  ( 113.7038881442453402, -3.383040157471821630, -19.15922257007629170 ) ) ;
#40455=CARTESIAN_POINT ( 'NONE',  ( 122.6667014775786413, -7.893985811506177619, -18.51759400769804742 ) ) ;
#40456=CARTESIAN_POINT ( 'NONE',  ( 122.2128881442453263, -7.643976991954077427, -18.09477374809248928 ) ) ;
#40460=CARTESIAN_POINT ( 'NONE',  ( 125.1059481442452750, -8.166667518702819706, -8.995218007635861213 ) ) ;
#40461=ADVANCED_FACE ( 'NONE', ( #13992 ), #17197, .T. ) ;
#40462=CARTESIAN_POINT ( 'NONE',  ( 113.3635281442453504, -0.1624402480850797581, -16.17319339645315424 ) ) ;
#40463=CARTESIAN_POINT ( 'NONE',  ( 123.7445081442452874, -1.561330072975668948, -17.79121239304076951 ) ) ;
#40472=CARTESIAN_POINT ( 'NONE',  ( 119.9438214775786378, -2.084020599724406786, -8.691656652584148546 ) ) ;
#40473=CARTESIAN_POINT ( 'NONE',  ( 114.8951481442453115, -8.899110576539710493, -16.42337572283490132 ) ) ;
#40474=CARTESIAN_POINT ( 'NONE',  ( 125.4463081442452932, -4.153390946401321671, -8.397313243818183892 ) ) ;
#40477=CARTESIAN_POINT ( 'NONE',  ( 115.4624148109119943, -4.153390946401321671, -8.397313243818183892 ) ) ;
#40478=CARTESIAN_POINT ( 'NONE',  ( 113.5904348109119866, -2.084020599724406786, -8.691656652584148546 ) ) ;
#40481=CARTESIAN_POINT ( 'NONE',  ( 112.0020881442453344, -9.565557343593413364, -10.61323700422348004 ) ) ;
#40483=CARTESIAN_POINT ( 'NONE',  ( 121.5321681442453183, -9.988377603198976828, -10.36322818467138340 ) ) ;
#40485=CARTESIAN_POINT ( 'NONE',  ( 124.4252281442452812, -0.8288870151387760510, -10.36305467784173118 ) ) ;
#40490=CARTESIAN_POINT ( 'NONE',  ( 123.7445081442452874, -7.894159318335828068, -9.358103419637847864 ) ) ;
#40491=CARTESIAN_POINT ( 'NONE',  ( 118.6958348109119754, -3.505236298600246325, -18.68346056562440793 ) ) ;
#40492=CARTESIAN_POINT ( 'NONE',  ( 120.8060036215688484, -1.135392229370310258, -17.10942237759953244 ) ) ;
#40496=CARTESIAN_POINT ( 'NONE',  ( 113.1933481442453058, -5.574606645277164318, -18.38911715685844683 ) ) ;
#40500=CARTESIAN_POINT ( 'NONE',  ( 120.8514481442452961, -7.893985811506177619, -18.51759400769804742 ) ) ;
#40501=CARTESIAN_POINT ( 'NONE',  ( 120.4543614775786295, -4.089484607189486809, -7.948022111789456723 ) ) ;
#40503=CARTESIAN_POINT ( 'NONE',  ( 115.8027748109119841, -0.4660016031367893996, -10.09054647747474043 ) ) ;
#40504=CARTESIAN_POINT ( 'NONE',  ( 113.6471614775786492, -5.638512984488999180, -18.83840828888717311 ) ) ;
#40506=CARTESIAN_POINT ( 'NONE',  ( 113.0798948109119948, -8.899110576539710493, -16.42337572283490132 ) ) ;
#40508=CARTESIAN_POINT ( 'NONE',  ( 111.2646414775786496, -8.899110576539710493, -16.42337572283490132 ) ) ;
#40509=CARTESIAN_POINT ( 'NONE',  ( 118.8660148109119774, -10.30919188438810075, -12.61870101168855918 ) ) ;
#40510=CARTESIAN_POINT ( 'NONE',  ( 124.2550481442452792, -0.1624402480850797581, -16.17319339645315424 ) ) ;
#40511=CARTESIAN_POINT ( 'NONE',  ( 126.2404814775786264, -9.261995988541697145, -16.69588392320189030 ) ) ;
#40512=VERTEX_POINT ( 'NONE', #27908 ) ;
#40513=CARTESIAN_POINT ( 'NONE',  ( 118.9794681442453026, -0.8288870151387760510, -10.36305467784173118 ) ) ;
#40514=CARTESIAN_POINT ( 'NONE',  ( 111.2646414775786496, -8.899110576539710493, -16.42337572283490132 ) ) ;
#40517=CARTESIAN_POINT ( 'NONE',  ( 120.1707281442453166, -9.565557343593413364, -10.61323700422348004 ) ) ;
#40521=EDGE_LOOP ( 'NONE', ( #4631, #28909, #11516, #35757, #39233, #8675 ) ) ;
#40523=CARTESIAN_POINT ( 'NONE',  ( 124.5386814775786206, -5.638512984488999180, -18.83840828888717311 ) ) ;
#40526=CARTESIAN_POINT ( 'NONE',  ( 112.3991748109119868, -8.166667518702817929, -8.995218007635859436 ) ) ;
#40531=CARTESIAN_POINT ( 'NONE',  ( 135.7445839641027305, -4.121996687475771637, -19.31599879726310576 ) ) ;
#40535=CARTESIAN_POINT ( 'NONE',  ( 116.5969481442453031, -9.859900752359374465, -12.68260735090039404 ) ) ;
#40536=CARTESIAN_POINT ( 'NONE',  ( 125.2761281442453054, 0.4262465694468514643, -12.03445270309931736 ) ) ;
#40538=CARTESIAN_POINT ( 'NONE',  ( 123.1772414775786189, -4.089484607189486809, -7.948022111789456723 ) ) ;
#40539=CARTESIAN_POINT ( 'NONE',  ( 116.4267681442453153, -3.383040157471821630, -19.15922257007629170 ) ) ;
#40542=CARTESIAN_POINT ( 'NONE',  ( 124.5954081442453116, -6.222761293078241884, -8.102969835052219238 ) ) ;
#40543=CARTESIAN_POINT ( 'NONE',  ( 124.8223148109119762, 0.9020085738987339008, -11.91225656197089222 ) ) ;
#40547=CARTESIAN_POINT ( 'NONE',  ( 114.8951481442453115, -8.899110576539710493, -16.42337572283490132 ) ) ;
#40548=CARTESIAN_POINT ( 'NONE',  ( 117.1642148109119859, -0.8288870151387760510, -10.36305467784173118 ) ) ;
#40553=CARTESIAN_POINT ( 'NONE',  ( 122.4514248082055587, -0.1020945015695078478, -15.74893487844866691 ) ) ;
#40554=CARTESIAN_POINT ( 'NONE',  ( 124.3685014775786328, 0.4262465694468514643, -12.03445270309931736 ) ) ;
#40562=CARTESIAN_POINT ( 'NONE',  ( 118.1852948109119836, -5.638512984488999180, -18.83840828888717311 ) ) ;
#40563=CARTESIAN_POINT ( 'NONE',  ( 125.1059481442452750, -1.833838273342660141, -17.42832698103878286 ) ) ;
#40564=CARTESIAN_POINT ( 'NONE',  ( 115.2922348109119781, 0.4262465694468514643, -12.03445270309931736 ) ) ;
#40566=CARTESIAN_POINT ( 'NONE',  ( 114.7664692294923867, -2.263366209404213958, -18.10533625161307114 ) ) ;
#40567=CARTESIAN_POINT ( 'NONE',  ( 112.7962614775786676, -3.383040157471821630, -19.15922257007629170 ) ) ;
#40569=CARTESIAN_POINT ( 'NONE',  ( 122.7234281442452755, -5.638512984488999180, -18.83840828888717311 ) ) ;
#40572=CARTESIAN_POINT ( 'NONE',  ( 113.9875214775786532, -0.4660016031367893996, -10.09054647747474043 ) ) ;
#40573=CARTESIAN_POINT ( 'NONE',  ( 112.7962614775786676, -6.222761293078241884, -8.102969835052219238 ) ) ;
#40575=CARTESIAN_POINT ( 'NONE',  ( 112.9097148109120070, 0.2603800115204892296, -16.42320221600525088 ) ) ;
#40577=CARTESIAN_POINT ( 'NONE',  ( 123.2906948109119867, -8.166667518702819706, -8.995218007635861213 ) ) ;
#40581=CARTESIAN_POINT ( 'NONE',  ( 124.7446598611595761, -1.036737761566197014, -17.24079555149560861 ) ) ;
#40582=CARTESIAN_POINT ( 'NONE',  ( 115.4624148109119943, -4.153390946401321671, -8.397313243818183892 ) ) ;
#40583=CARTESIAN_POINT ( 'NONE',  ( 123.6188425880120150, -4.416445946866398131, -15.23819856170553955 ) ) ;
#40584=CARTESIAN_POINT ( 'NONE',  ( 114.4980614775786734, -2.084020599724406786, -8.691656652584148546 ) ) ;
#40587=CARTESIAN_POINT ( 'NONE',  ( 114.2144281442453178, -1.833838273342658809, -17.42832698103878286 ) ) ;
#40588=CARTESIAN_POINT ( 'NONE',  ( 116.8805814775786445, -6.344957434206662583, -7.627207830600332805 ) ) ;
#40590=CARTESIAN_POINT ( 'NONE',  ( 112.9664414775786412, 0.5811942927096154232, -14.16772938898807155 ) ) ;
#40591=CARTESIAN_POINT ( 'NONE',  ( 114.6682414775786469, -7.894159318335828068, -9.358103419637847864 ) ) ;
#40592=CARTESIAN_POINT ( 'NONE',  ( 123.6877814775786533, -3.383040157471821630, -19.15922257007629170 ) ) ;
#40594=CARTESIAN_POINT ( 'NONE',  ( 120.9649014775786355, -3.383040157471821630, -19.15922257007629170 ) ) ;
#40595=VERTEX_POINT ( 'NONE', #30871 ) ;
#40596=CARTESIAN_POINT ( 'NONE',  ( 114.5547881442453217, -5.638512984488999180, -18.83840828888717311 ) ) ;
#40601=CARTESIAN_POINT ( 'NONE',  ( 117.2209414775786485, -7.893985811506177619, -18.51759400769804742 ) ) ;
#40603=CARTESIAN_POINT ( 'NONE',  ( 126.0703014775786102, -9.988377603198980381, -10.36322818467138518 ) ) ;
#40604=CARTESIAN_POINT ( 'NONE',  ( 124.7195491406318411, 0.3208234527006150749, -15.99825685930877128 ) ) ;
#40605=CARTESIAN_POINT ( 'NONE',  ( 112.7962614775786676, -6.222761293078241884, -8.102969835052219238 ) ) ;
#40608=CARTESIAN_POINT ( 'NONE',  ( 119.5467348109119712, -4.089484607189486809, -7.948022111789456723 ) ) ;
#40610=CARTESIAN_POINT ( 'NONE',  ( 119.6392035773848761, -2.467220198592778413, -17.83387418641524391 ) ) ;
#40611=VERTEX_POINT ( 'NONE', #79 ) ;
#40613=CARTESIAN_POINT ( 'NONE',  ( 120.8514481442452961, -2.084020599724406786, -8.691656652584148546 ) ) ;
#40614=CARTESIAN_POINT ( 'NONE',  ( 121.4187148109119789, -6.344957434206665248, -7.627207830600338134 ) ) ;
#40616=CARTESIAN_POINT ( 'NONE',  ( 114.1577014775786552, -3.505236298600246325, -18.68346056562440793 ) ) ;
#40617=CARTESIAN_POINT ( 'NONE',  ( 116.9940348109119839, -9.988377603198976828, -10.36322818467138340 ) ) ;
#40619=CARTESIAN_POINT ( 'NONE',  ( 127.3669547543381810, -1.266902555130286379, -9.134731740105504372 ) ) ;
#40620=CARTESIAN_POINT ( 'NONE',  ( 118.9227414775786542, 0.4262465694468514643, -12.03445270309931736 ) ) ;
#40623=CARTESIAN_POINT ( 'NONE',  ( 114.8384214775786489, 0.9020085738987339008, -11.91225656197089222 ) ) ;
#40624=CARTESIAN_POINT ( 'NONE',  ( 120.9649014775786355, -6.222761293078241884, -8.102969835052219238 ) ) ;
#40627=CARTESIAN_POINT ( 'NONE',  ( 118.4122014775786340, 0.5811942927096110934, -14.16772938898807510 ) ) ;
#40629=CARTESIAN_POINT ( 'NONE',  ( 116.8805814775786445, -3.505236298600246325, -18.68346056562440793 ) ) ;
#40630=EDGE_CURVE ( 'NONE', #24205, #34050, #16674, .T. ) ;
#40633=CARTESIAN_POINT ( 'NONE',  ( 111.7751814775786556, -7.893985811506177619, -18.51759400769804742 ) ) ;
#40634=CARTESIAN_POINT ( 'NONE',  ( 121.5321681442453183, -0.1624402480850797581, -16.17319339645315424 ) ) ;
#40638=EDGE_CURVE ( 'NONE', #5980, #2538, #2705, .T. ) ;
#40639=CARTESIAN_POINT ( 'NONE',  ( 118.0718414775786300, -9.261995988541697145, -16.69588392320189030 ) ) ;
#40641=CARTESIAN_POINT ( 'NONE',  ( 119.4332814775786318, -0.4660016031367893996, -10.09054647747474043 ) ) ;
#40642=CARTESIAN_POINT ( 'NONE',  ( 114.4413348109119823, -9.261995988541697145, -16.69588392320189030 ) ) ;
#40643=CARTESIAN_POINT ( 'NONE',  ( 120.2274548109119934, -9.859900752359374465, -12.68260735090039404 ) ) ;
#40645=CARTESIAN_POINT ( 'NONE',  ( 112.2857214775786474, -4.089484607189486809, -7.948022111789456723 ) ) ;
#40647=CARTESIAN_POINT ( 'NONE',  ( 121.8158014775786171, -4.153390946401325223, -8.397313243818185668 ) ) ;
#40649=ADVANCED_FACE ( 'NONE', ( #18146 ), #2662, .T. ) ;
#40654=CARTESIAN_POINT ( 'NONE',  ( 121.2485348109119769, -0.4660016031367893996, -10.09054647747474043 ) ) ;
#40655=CARTESIAN_POINT ( 'NONE',  ( 121.7023481442452919, -0.8288870151387760510, -10.36305467784173118 ) ) ;
#40658=CARTESIAN_POINT ( 'NONE',  ( 120.2841814775786276, 0.9020085738987339008, -11.91225656197089222 ) ) ;
#40660=CARTESIAN_POINT ( 'NONE',  ( 121.5888948109119809, -10.30919188438810075, -12.61870101168855918 ) ) ;
#40663=CARTESIAN_POINT ( 'NONE',  ( 122.1561614775786353, -0.4660016031367893996, -10.09054647747474043 ) ) ;
#40665=CARTESIAN_POINT ( 'NONE',  ( 124.4252281442452812, -0.8288870151387760510, -10.36305467784173118 ) ) ;
#40667=CARTESIAN_POINT ( 'NONE',  ( 111.7297369549021937, -1.135392229370322026, -17.10942237759953954 ) ) ;
#40671=CARTESIAN_POINT ( 'NONE',  ( 124.7088614775786226, -9.565557343593413364, -10.61323700422348004 ) ) ;
#40674=CARTESIAN_POINT ( 'NONE',  ( 117.5613014775786525, -10.15424416112533912, -14.75197769757731336 ) ) ;
#40677=CARTESIAN_POINT ( 'NONE',  ( 117.1074881442453233, 0.4262465694468514643, -12.03445270309931736 ) ) ;
#40679=CARTESIAN_POINT ( 'NONE',  ( 123.3474214775786209, -9.988377603198976828, -10.36322818467138340 ) ) ;
#40680=ORIENTED_EDGE ( 'NONE', *, *, #20085, .F. ) ;
#40681=CARTESIAN_POINT ( 'NONE',  ( 121.4754414775786131, -1.833838273342659697, -17.42832698103878286 ) ) ;
#40682=CARTESIAN_POINT ( 'NONE',  ( 117.6747548109119919, -1.834011780172310813, -8.268836392978581529 ) ) ;
#40683=CARTESIAN_POINT ( 'NONE',  ( 124.3685014775786328, -10.63000616557722466, -14.87417383870573495 ) ) ;
#40684=CONICAL_SURFACE ( 'NONE', #3528, 0.04618666666666765286, 0.7853981633974476129 ) ;
#40685=CARTESIAN_POINT ( 'NONE',  ( 122.5532481442453019, 0.4262465694468514643, -12.03445270309931736 ) ) ;
#40688=CARTESIAN_POINT ( 'NONE',  ( 123.8579614775786126, 0.5811942927096110934, -14.16772938898807510 ) ) ;
#40689=CARTESIAN_POINT ( 'NONE',  ( 115.3489614775786407, -0.8288870151387760510, -10.36305467784173118 ) ) ;
#40690=CARTESIAN_POINT ( 'NONE',  ( 124.1415948109119540, -6.344957434206665248, -7.627207830600338134 ) ) ;
#40693=ORIENTED_EDGE ( 'NONE', *, *, #38931, .T. ) ;
#40697=CARTESIAN_POINT ( 'NONE',  ( 120.6245414775786458, -0.1624402480850797581, -16.17319339645315424 ) ) ;
#40698=CARTESIAN_POINT ( 'NONE',  ( 115.6325948109119821, -9.565557343593413364, -10.61323700422348004 ) ) ;
#40700=EDGE_LOOP ( 'NONE', ( #42415, #2084, #34208, #30754 ) ) ;
#40702=CARTESIAN_POINT ( 'NONE',  ( 116.0864081442453113, -0.1624402480850797581, -16.17319339645315424 ) ) ;
#40703=CARTESIAN_POINT ( 'NONE',  ( 113.8740681442453138, -9.859900752359374465, -12.68260735090039404 ) ) ;
#40705=CARTESIAN_POINT ( 'NONE',  ( 111.2646414775786496, -8.899110576539710493, -16.42337572283490132 ) ) ;
#40707=CARTESIAN_POINT ( 'NONE',  ( 121.7590748109119687, -7.893985811506177619, -18.51759400769804742 ) ) ;
#40708=CARTESIAN_POINT ( 'NONE',  ( 112.9097148109120070, 0.2603800115204892296, -16.42320221600525088 ) ) ;
#40711=CARTESIAN_POINT ( 'NONE',  ( 113.7015254349294793, -1.040089454026971172, -17.23633227186634187 ) ) ;
#40714=CARTESIAN_POINT ( 'NONE',  ( 111.7751814775786556, -7.893985811506177619, -18.51759400769804742 ) ) ;
#40715=CARTESIAN_POINT ( 'NONE',  ( 120.6812681442452941, 0.1319031606808879209, -14.10382304977623669 ) ) ;
#40720=FACE_OUTER_BOUND ( 'NONE', #14996, .T. ) ;
#40721=CARTESIAN_POINT ( 'NONE',  ( 113.1366214775786432, -7.643976991954091638, -18.09477374809248218 ) ) ;
#40725=CARTESIAN_POINT ( 'NONE',  ( 123.4608748109119745, -10.63000616557722466, -14.87417383870573495 ) ) ;
#40726=CARTESIAN_POINT ( 'NONE',  ( 121.7590748109119687, -7.893985811506177619, -18.51759400769804742 ) ) ;
#40728=EDGE_CURVE ( 'NONE', #15771, #10224, #37517, .T. ) ;
#40729=CARTESIAN_POINT ( 'NONE',  ( 117.6747548109119919, -1.834011780172310813, -8.268836392978581529 ) ) ;
#40730=CARTESIAN_POINT ( 'NONE',  ( 112.4559014775786494, -9.988377603198976828, -10.36322818467138340 ) ) ;
#40732=CARTESIAN_POINT ( 'NONE',  ( 112.3424481442453384, -3.505236298600246325, -18.68346056562440793 ) ) ;
#40733=CARTESIAN_POINT ( 'NONE',  ( 125.2761281442453054, -10.63000616557722466, -14.87417383870573495 ) ) ;
#40734=CARTESIAN_POINT ( 'NONE',  ( 120.7379948109119709, -10.63000616557722466, -14.87417383870573495 ) ) ;
#40735=CARTESIAN_POINT ( 'NONE',  ( 113.0231681442453322, 0.9020085738987339008, -11.91225656197089222 ) ) ;
#40737=CARTESIAN_POINT ( 'NONE',  ( 113.4202548109119846, 0.1319031606808879209, -14.10382304977623669 ) ) ;
#40738=EDGE_LOOP ( 'NONE', ( #9228, #32635, #15634, #43590 ) ) ;
#40739=CARTESIAN_POINT ( 'NONE',  ( 118.0151148109119816, 0.4262465694468514643, -12.03445270309931736 ) ) ;
#40740=CARTESIAN_POINT ( 'NONE',  ( 114.6682414775786469, -7.894159318335828068, -9.358103419637847864 ) ) ;
#40743=CARTESIAN_POINT ( 'NONE',  ( 122.0994348109119443, -10.15424416112533912, -14.75197769757731336 ) ) ;
#40746=ORIENTED_EDGE ( 'NONE', *, *, #29592, .T. ) ;
#40749=CARTESIAN_POINT ( 'NONE',  ( 124.3117748109119844, -10.30919188438810075, -12.61870101168855918 ) ) ;
#40756=CARTESIAN_POINT ( 'NONE',  ( 138.2184548109119930, -8.536181032868617180, -18.13822074491315561 ) ) ;
#40757=CARTESIAN_POINT ( 'NONE',  ( 136.3620199738656993, -4.220151613809025370, -19.16374751516046970 ) ) ;
#40760=CARTESIAN_POINT ( 'NONE',  ( 121.6456214775786293, 0.4262465694468514643, -12.03445270309931736 ) ) ;
#40762=ORIENTED_EDGE ( 'NONE', *, *, #15556, .T. ) ;
#40763=CARTESIAN_POINT ( 'NONE',  ( 122.2696148109119889, -4.089484607189486809, -7.948022111789456723 ) ) ;
#40764=CARTESIAN_POINT ( 'NONE',  ( 119.6601881442453106, -8.166667518702819706, -8.995218007635861213 ) ) ;
#40766=CARTESIAN_POINT ( 'NONE',  ( 113.3068014775786594, -1.833838273342658809, -17.42832698103878286 ) ) ;
#40767=CARTESIAN_POINT ( 'NONE',  ( 113.4769814775786330, -10.63000616557722466, -14.87417383870573495 ) ) ;
#40768=CARTESIAN_POINT ( 'NONE',  ( 124.7655881442452852, 0.5811942927096110934, -14.16772938898807510 ) ) ;
#40772=CARTESIAN_POINT ( 'NONE',  ( 117.1074881442453233, 0.4262465694468514643, -12.03445270309931736 ) ) ;
#40773=CARTESIAN_POINT ( 'NONE',  ( 116.8238548109119819, -5.574606645277164318, -18.38911715685844683 ) ) ;
#40779=CARTESIAN_POINT ( 'NONE',  ( 124.1299648136183293, -3.929494816604725216, -18.62311481910882094 ) ) ;
#40780=CARTESIAN_POINT ( 'NONE',  ( 111.9453614775786434, -1.561330072975668060, -17.79121239304076596 ) ) ;
#40781=CARTESIAN_POINT ( 'NONE',  ( 112.0020881442453344, 0.2603800115204892296, -16.42320221600525088 ) ) ;
#40788=CARTESIAN_POINT ( 'NONE',  ( 118.2987481442453088, -1.561330072975668504, -17.79121239304076951 ) ) ;
#40790=CARTESIAN_POINT ( 'NONE',  ( 123.6310548109119765, -4.153390946401325223, -8.397313243818185668 ) ) ;
#40791=CARTESIAN_POINT ( 'NONE',  ( 114.6682414775786469, -7.894159318335828068, -9.358103419637847864 ) ) ;
#40795=CARTESIAN_POINT ( 'NONE',  ( 120.6245414775786458, -9.988377603198976828, -10.36322818467138340 ) ) ;
#40796=CARTESIAN_POINT ( 'NONE',  ( 112.8529881442453302, -1.561330072975668060, -17.79121239304076596 ) ) ;
#40799=CARTESIAN_POINT ( 'NONE',  ( 123.5743281442453139, -7.893985811506177619, -18.51759400769804742 ) ) ;
#40802=CARTESIAN_POINT ( 'NONE',  ( 117.9016614775786280, -9.988377603198976828, -10.36322818467138340 ) ) ;
#40803=CARTESIAN_POINT ( 'NONE',  ( 114.6682414775786469, -7.894159318335828068, -9.358103419637847864 ) ) ;
#40804=CARTESIAN_POINT ( 'NONE',  ( 126.5125895482189833, -4.945298539089557188, -18.53964231575977095 ) ) ;
#40805=CARTESIAN_POINT ( 'NONE',  ( 126.1837548109119496, 0.4262465694468514643, -12.03445270309931736 ) ) ;
#40807=CARTESIAN_POINT ( 'NONE',  ( 123.1205148109119563, -1.834011780172310813, -8.268836392978581529 ) ) ;
#40813=CARTESIAN_POINT ( 'NONE',  ( 116.3700414775786527, -4.153390946401321671, -8.397313243818183892 ) ) ;
#40814=CARTESIAN_POINT ( 'NONE',  ( 136.4173705901582423, -2.656029227767985113, -8.046337796338329795 ) ) ;
#40815=CARTESIAN_POINT ( 'NONE',  ( 116.9373081442452929, -1.833838273342659253, -17.42832698103878286 ) ) ;
#40819=CARTESIAN_POINT ( 'NONE',  ( 116.7671281442453335, -7.643976991954077427, -18.09477374809248928 ) ) ;
#40821=CARTESIAN_POINT ( 'NONE',  ( 115.9162281442453235, -4.089484607189486809, -7.948022111789456723 ) ) ;
#40823=CARTESIAN_POINT ( 'NONE',  ( 112.1722681442453222, -0.4660016031367893996, -10.09054647747474043 ) ) ;
#40824=CARTESIAN_POINT ( 'NONE',  ( 115.2922348109119781, 0.4262465694468514643, -12.03445270309931736 ) ) ;
#40825=CARTESIAN_POINT ( 'NONE',  ( 125.0492214775786266, -6.344957434206665248, -7.627207830600338134 ) ) ;
#40826=CARTESIAN_POINT ( 'NONE',  ( 120.4543614775786295, -4.089484607189486809, -7.948022111789456723 ) ) ;
#40828=CARTESIAN_POINT ( 'NONE',  ( 111.9453614775786434, -1.561330072975668060, -17.79121239304076596 ) ) ;
#40834=CARTESIAN_POINT ( 'NONE',  ( 119.5467348109119712, -4.089484607189486809, -7.948022111789456723 ) ) ;
#40838=CARTESIAN_POINT ( 'NONE',  ( 115.6325948109119821, -9.565557343593413364, -10.61323700422348004 ) ) ;
#40840=CARTESIAN_POINT ( 'NONE',  ( 122.7234281442452755, -5.638512984488999180, -18.83840828888717311 ) ) ;
#40845=CARTESIAN_POINT ( 'NONE',  ( 121.4187148109119789, -3.505236298600246325, -18.68346056562440793 ) ) ;
#40846=CARTESIAN_POINT ( 'NONE',  ( 119.9438214775786378, -7.893985811506177619, -18.51759400769804742 ) ) ;
#40848=CARTESIAN_POINT ( 'NONE',  ( 112.1722681442453222, -8.899110576539710493, -16.42337572283490132 ) ) ;
#40849=CARTESIAN_POINT ( 'NONE',  ( 114.3846081442453197, -10.63000616557722466, -14.87417383870573495 ) ) ;
#40852=CARTESIAN_POINT ( 'NONE',  ( 119.1496481442453046, -6.222761293078241884, -8.102969835052219238 ) ) ;
#40856=CARTESIAN_POINT ( 'NONE',  ( 113.3635281442453504, -9.988377603198976828, -10.36322818467138340 ) ) ;
#40857=CARTESIAN_POINT ( 'NONE',  ( 121.9292548109119849, -7.894159318335828068, -9.358103419637847864 ) ) ;
#40861=CARTESIAN_POINT ( 'NONE',  ( 137.4443952029671721, -1.138448121875069941, -9.933366089684859901 ) ) ;
#40862=CARTESIAN_POINT ( 'NONE',  ( 118.3554748109119998, 0.2603800115204892296, -16.42320221600525088 ) ) ;
#40864=CARTESIAN_POINT ( 'NONE',  ( 117.8449348109119938, -1.833838273342659253, -17.42832698103878286 ) ) ;
#40867=CARTESIAN_POINT ( 'NONE',  ( 124.8223148109119762, -10.15424416112533912, -14.75197769757731336 ) ) ;
#40868=CARTESIAN_POINT ( 'NONE',  ( 119.3765548109119834, -10.15424416112533912, -14.75197769757731336 ) ) ;
#40871=CARTESIAN_POINT ( 'NONE',  ( 123.2906948109119867, -8.166667518702819706, -8.995218007635861213 ) ) ;
#40874=CARTESIAN_POINT ( 'NONE',  ( 119.1496481442453046, -3.383040157471821630, -19.15922257007629170 ) ) ;
#40875=CARTESIAN_POINT ( 'NONE',  ( 118.6958348109119754, -6.344957434206665248, -7.627207830600338134 ) ) ;
#40876=CARTESIAN_POINT ( 'NONE',  ( 119.8870948109119752, -0.8288870151387760510, -10.36305467784173118 ) ) ;
#40877=CARTESIAN_POINT ( 'NONE',  ( 125.6732148109119862, -9.859900752359378018, -12.68260735090039759 ) ) ;
#40878=CARTESIAN_POINT ( 'NONE',  ( 112.1155414775786454, 0.9020085738987339008, -11.91225656197089222 ) ) ;
#40880=CARTESIAN_POINT ( 'NONE',  ( 122.6099748109119929, -0.8288870151387760510, -10.36305467784173118 ) ) ;
#40886=CARTESIAN_POINT ( 'NONE',  ( 120.7379948109119709, -10.63000616557722466, -14.87417383870573495 ) ) ;
#40887=CARTESIAN_POINT ( 'NONE',  ( 122.4965214775786251, 0.1319031606808879209, -14.10382304977623669 ) ) ;
#40890=CARTESIAN_POINT ( 'NONE',  ( 122.8368814775786291, -1.561330072975668948, -17.79121239304076951 ) ) ;
#40891=CARTESIAN_POINT ( 'NONE',  ( 135.3184548109119874, -4.105398160058917334, -19.34506575923121474 ) ) ;
#40893=CARTESIAN_POINT ( 'NONE',  ( 121.7590748109119687, -7.893985811506177619, -18.51759400769804742 ) ) ;
#40894=CARTESIAN_POINT ( 'NONE',  ( 122.5532481442453019, -10.63000616557722466, -14.87417383870573495 ) ) ;
#40895=CARTESIAN_POINT ( 'NONE',  ( 111.3768994516356230, -3.941856523015780489, -18.57470496855048481 ) ) ;
#40896=CARTESIAN_POINT ( 'NONE',  ( 125.3328548109119964, -0.8288870151387760510, -10.36305467784173118 ) ) ;
#40901=DIRECTION ( 'NONE',  ( -1.000000000000000000, 0.000000000000000000, 0.000000000000000000 ) ) ;
#40902=CARTESIAN_POINT ( 'NONE',  ( 118.3179530757767566, -0.9924539043446216624, -17.29976612834909133 ) ) ;
#40903=CARTESIAN_POINT ( 'NONE',  ( 122.9503348109119827, -9.859900752359378018, -12.68260735090039759 ) ) ;
#40906=CARTESIAN_POINT ( 'NONE',  ( 118.1852948109119836, -4.153390946401325223, -8.397313243818185668 ) ) ;
#40908=CARTESIAN_POINT ( 'NONE',  ( 117.5613014775786525, -10.15424416112533912, -14.75197769757731336 ) ) ;
#40909=CARTESIAN_POINT ( 'NONE',  ( 123.9714148109119805, -0.4660016031367893996, -10.09054647747474043 ) ) ;
#40912=CARTESIAN_POINT ( 'NONE',  ( 121.4187148109119789, -3.505236298600246325, -18.68346056562440793 ) ) ;
#40913=CARTESIAN_POINT ( 'NONE',  ( 119.6601881442453106, -8.166667518702819706, -8.995218007635861213 ) ) ;
#40914=CARTESIAN_POINT ( 'NONE',  ( 124.7655881442452852, 0.5811942927096110934, -14.16772938898807510 ) ) ;
#40915=CARTESIAN_POINT ( 'NONE',  ( 123.8579614775786126, -9.859900752359378018, -12.68260735090039759 ) ) ;
#40917=DIRECTION ( 'NONE',  ( 0.000000000000000000, 0.6004852223388321697, -0.7996358532186279566 ) ) ;
#40919=CARTESIAN_POINT ( 'NONE',  ( 125.6164881442453094, 0.2603800115204892296, -16.42320221600525088 ) ) ;
#40920=CARTESIAN_POINT ( 'NONE',  ( 116.2565881442453133, -0.8288870151387760510, -10.36305467784173118 ) ) ;
#40921=CARTESIAN_POINT ( 'NONE',  ( 124.8790414775786246, -0.4660016031367893996, -10.09054647747474043 ) ) ;
#40931=CARTESIAN_POINT ( 'NONE',  ( 121.0216281442452981, -7.894159318335828068, -9.358103419637847864 ) ) ;
#40932=CARTESIAN_POINT ( 'NONE',  ( 115.0086014775786509, -5.574606645277164318, -18.38911715685844683 ) ) ;
#40933=CARTESIAN_POINT ( 'NONE',  ( 127.7425183523502881, -7.050714571525749541, -18.72418924296322729 ) ) ;
#40935=CARTESIAN_POINT ( 'NONE',  ( 125.3328548109119964, -9.261995988541029234, -16.69588392320277848 ) ) ;
#40936=CARTESIAN_POINT ( 'NONE',  ( 119.3198281442452924, -9.859900752359374465, -12.68260735090039404 ) ) ;
#40937=CARTESIAN_POINT ( 'NONE',  ( 113.7606148109119886, -7.894159318335828068, -9.358103419637847864 ) ) ;
#40939=CARTESIAN_POINT ( 'NONE',  ( 111.4915481442453142, -1.833838273342658365, -17.42832698103878286 ) ) ;
#40941=CARTESIAN_POINT ( 'NONE',  ( 124.1415948109119540, -6.344957434206665248, -7.627207830600338134 ) ) ;
#40942=CARTESIAN_POINT ( 'NONE',  ( 125.9568481442452850, -3.505236298600246325, -18.68346056562440793 ) ) ;
#40944=CARTESIAN_POINT ( 'NONE',  ( 114.8384214775786489, 0.9020085738987339008, -11.91225656197089222 ) ) ;
#40947=CARTESIAN_POINT ( 'NONE',  ( 125.9001214775786224, -5.574606645277164318, -18.38911715685844683 ) ) ;
#40948=CARTESIAN_POINT ( 'NONE',  ( 121.1350814775786233, -9.859900752359378018, -12.68260735090039759 ) ) ;
#40952=AXIS2_PLACEMENT_3D ( 'NONE', #43846, #23555, #16024 ) ;
#40955=CARTESIAN_POINT ( 'NONE',  ( 112.3424481442453384, -3.505236298600246325, -18.68346056562440793 ) ) ;
#40959=CARTESIAN_POINT ( 'NONE',  ( 124.2550481442452792, -9.988377603198980381, -10.36322818467138518 ) ) ;
#40960=CARTESIAN_POINT ( 'NONE',  ( 120.5110881442453206, -6.344957434206665248, -7.627207830600338134 ) ) ;
#40963=CARTESIAN_POINT ( 'NONE',  ( 120.3976348109119812, -1.834011780172310813, -8.268836392978581529 ) ) ;
#40964=CARTESIAN_POINT ( 'NONE',  ( 114.2711548109119803, -9.988377603198976828, -10.36322818467138340 ) ) ;
#40966=CARTESIAN_POINT ( 'NONE',  ( 113.3635281442453504, -0.1624402480850797581, -16.17319339645315424 ) ) ;
#40967=ADVANCED_FACE ( 'NONE', ( #36591 ), #33383, .T. ) ;
#40968=CARTESIAN_POINT ( 'NONE',  ( 126.0703014775786102, -9.988377603198980381, -10.36322818467138518 ) ) ;
#40969=CARTESIAN_POINT ( 'NONE',  ( 125.1059481442452750, -8.166667518702819706, -8.995218007635861213 ) ) ;
#40970=CARTESIAN_POINT ( 'NONE',  ( 113.0798948109119948, -0.4660016031367893996, -10.09054647747474043 ) ) ;
#40971=CARTESIAN_POINT ( 'NONE',  ( 113.9875214775786532, -8.899110576539710493, -16.42337572283490132 ) ) ;
#40973=CARTESIAN_POINT ( 'NONE',  ( 117.3911214775786505, -7.894159318335828068, -9.358103419637847864 ) ) ;
#40975=VECTOR ( 'NONE', #36944, 1000.000000000000114 ) ;
#40978=CARTESIAN_POINT ( 'NONE',  ( 124.3117748109119844, 0.1319031606808879209, -14.10382304977623669 ) ) ;
#40981=VERTEX_POINT ( 'NONE', #23155 ) ;
#40985=CARTESIAN_POINT ( 'NONE',  ( 125.9001214775786224, -4.089484607189486809, -7.948022111789456723 ) ) ;
#40988=CARTESIAN_POINT ( 'NONE',  ( 111.8319081442453182, -5.638512984488999180, -18.83840828888717311 ) ) ;
#40989=B_SPLINE_CURVE_WITH_KNOTS ( 'NONE', 3,
 ( #28145, #14230, #3293, #17215, #34730, #17430, #7376, #24939, #42056, #25620 ),
 .UNSPECIFIED., .F., .F.,
 ( 4, 3, 3, 4 ),
 ( 0.000000000000000000, 0.0001671877548681274892, 0.0003343755096277665107, 0.0006463528481650629171 ),
 .UNSPECIFIED. ) ;
#40990=CARTESIAN_POINT ( 'NONE',  ( 112.7395348109119766, -5.638512984488999180, -18.83840828888717311 ) ) ;
#40993=CARTESIAN_POINT ( 'NONE',  ( 123.2724088976799948, -1.244021962887374544, -16.96476564598603076 ) ) ;
#40994=CARTESIAN_POINT ( 'NONE',  ( 118.1285681442453068, -7.893985811506177619, -18.51759400769804742 ) ) ;
#40995=CARTESIAN_POINT ( 'NONE',  ( 137.4923962881472903, -5.828094238520085568, -18.32084130032456315 ) ) ;
#40998=CARTESIAN_POINT ( 'NONE',  ( 120.9081748109119872, -4.153390946401325223, -8.397313243818185668 ) ) ;
#41001=CARTESIAN_POINT ( 'NONE',  ( 123.2906948109119867, -8.166667518702819706, -8.995218007635861213 ) ) ;
#41002=CARTESIAN_POINT ( 'NONE',  ( 119.2631014775786298, 0.2603800115204892296, -16.42320221600525088 ) ) ;
#41004=CARTESIAN_POINT ( 'NONE',  ( 113.5337081442453240, -9.261995988541698921, -16.69588392320188674 ) ) ;
#41006=CARTESIAN_POINT ( 'NONE',  ( 124.1415948109119540, -6.344957434206665248, -7.627207830600338134 ) ) ;
#41010=CARTESIAN_POINT ( 'NONE',  ( 117.8449348109119938, -1.833838273342659253, -17.42832698103878286 ) ) ;
#41012=CARTESIAN_POINT ( 'NONE',  ( 118.4689281442453250, -10.15424416112533912, -14.75197769757731336 ) ) ;
#41017=CARTESIAN_POINT ( 'NONE',  ( 115.4624148109119943, -5.638512984488999180, -18.83840828888717311 ) ) ;
#41022=CARTESIAN_POINT ( 'NONE',  ( 123.5975415792130292, -3.161545974351341659, -14.41132075528343570 ) ) ;
#41023=CARTESIAN_POINT ( 'NONE',  ( 111.4966152579028034, -1.277474013852379908, -16.92021923864711752 ) ) ;
#41026=CARTESIAN_POINT ( 'NONE',  ( 116.7104014775786425, -0.4660016031367893996, -10.09054647747474043 ) ) ;
#41027=CARTESIAN_POINT ( 'NONE',  ( 113.4769814775786330, -10.63000616557722466, -14.87417383870573495 ) ) ;
#41028=CARTESIAN_POINT ( 'NONE',  ( 116.6536748109119941, -10.15424416112533912, -14.75197769757731336 ) ) ;
#41029=CARTESIAN_POINT ( 'NONE',  ( 151.2860562277021472, -4.863998795839242995, -13.39321520033831447 ) ) ;
#41030=CARTESIAN_POINT ( 'NONE',  ( 121.7023481442452777, -9.261995988541697145, -16.69588392320189030 ) ) ;
#41031=CARTESIAN_POINT ( 'NONE',  ( 117.3343948109119737, -3.383040157471821630, -19.15922257007629170 ) ) ;
#41034=CARTESIAN_POINT ( 'NONE',  ( 114.3278814775786429, 0.1319031606808879209, -14.10382304977623669 ) ) ;
#41037=CARTESIAN_POINT ( 'NONE',  ( 116.3133148109119759, -7.893985811506177619, -18.51759400769804742 ) ) ;
#41039=CARTESIAN_POINT ( 'NONE',  ( 118.2795432127138611, -2.191907684172563986, -18.20049396185734025 ) ) ;
#41040=CARTESIAN_POINT ( 'NONE',  ( 115.0653281442453277, -6.344957434206662583, -7.627207830600332805 ) ) ;
#41042=CARTESIAN_POINT ( 'NONE',  ( 120.8514481442452961, -7.893985811506177619, -18.51759400769804742 ) ) ;
#41047=CARTESIAN_POINT ( 'NONE',  ( 118.0151148109119816, 0.4262465694468514643, -12.03445270309931736 ) ) ;
#41049=CARTESIAN_POINT ( 'NONE',  ( 118.7525614775786380, -1.833838273342659253, -17.42832698103878286 ) ) ;
#41052=CARTESIAN_POINT ( 'NONE',  ( 115.7460481442453357, -10.15424416112533912, -14.75197769757731336 ) ) ;
#41053=CARTESIAN_POINT ( 'NONE',  ( 114.8384214775786489, 0.9020085738987339008, -11.91225656197089222 ) ) ;
#41055=CARTESIAN_POINT ( 'NONE',  ( 126.5241148109119393, -9.565557343593413364, -10.61323700422348004 ) ) ;
#41056=CARTESIAN_POINT ( 'NONE',  ( 116.2565881442453133, -0.8288870151387760510, -10.36305467784173118 ) ) ;
#41057=CARTESIAN_POINT ( 'NONE',  ( 112.8529881442453160, -7.894159318335828068, -9.358103419637847864 ) ) ;
#41058=CARTESIAN_POINT ( 'NONE',  ( 117.9016614775786280, -0.1624402480850797581, -16.17319339645315424 ) ) ;
#41059=VERTEX_POINT ( 'NONE', #37037 ) ;
#41060=FACE_OUTER_BOUND ( 'NONE', #37579, .T. ) ;
#41065=CARTESIAN_POINT ( 'NONE',  ( 118.3554748109119998, 0.2603800115204892296, -16.42320221600525088 ) ) ;
#41067=CARTESIAN_POINT ( 'NONE',  ( 124.7655881442452852, 0.5811942927096110934, -14.16772938898807510 ) ) ;
#41068=CARTESIAN_POINT ( 'NONE',  ( 121.0024232127138504, -2.191907684172563986, -18.20049396185734025 ) ) ;
#41069=CARTESIAN_POINT ( 'NONE',  ( 118.6958348109119754, -3.505236298600246325, -18.68346056562440793 ) ) ;
#41071=CARTESIAN_POINT ( 'NONE',  ( 122.3263414775786373, -6.344957434206665248, -7.627207830600338134 ) ) ;
#41076=CARTESIAN_POINT ( 'NONE',  ( 111.7751814775786556, -7.893985811506177619, -18.51759400769804742 ) ) ;
#41077=CARTESIAN_POINT ( 'NONE',  ( 124.2550481442452792, -0.1624402480850797581, -16.17319339645315424 ) ) ;
#41079=CARTESIAN_POINT ( 'NONE',  ( 121.1350814775786233, 0.5811942927096110934, -14.16772938898807510 ) ) ;
#41080=CARTESIAN_POINT ( 'NONE',  ( 113.0231681442453180, -10.15424416112533912, -14.75197769757731336 ) ) ;
#41081=CARTESIAN_POINT ( 'NONE',  ( 119.1496481442453046, -3.383040157471821630, -19.15922257007629170 ) ) ;
#41082=CARTESIAN_POINT ( 'NONE',  ( 123.3116793777725064, -1.267766418764731728, -16.93314635290706605 ) ) ;
#41083=CARTESIAN_POINT ( 'NONE',  ( 126.6211808763518576, -1.201114777694167746, -9.700051355915984885 ) ) ;
#41084=CARTESIAN_POINT ( 'NONE',  ( 124.4252281442452812, -0.8288870151387760510, -10.36305467784173118 ) ) ;
#41088=CARTESIAN_POINT ( 'NONE',  ( 116.8238548109119819, -4.089484607189486809, -7.948022111789456723 ) ) ;
#41089=CARTESIAN_POINT ( 'NONE',  ( 119.9438214775786378, -2.084020599724406786, -8.691656652584148546 ) ) ;
#41092=CARTESIAN_POINT ( 'NONE',  ( 137.3802547664329552, -0.4074658335668200904, -10.83275452620230084 ) ) ;
#41093=CARTESIAN_POINT ( 'NONE',  ( 118.9227414775786400, -10.63000616557722466, -14.87417383870573495 ) ) ;
#41095=CARTESIAN_POINT ( 'NONE',  ( 117.2776681442452968, -4.153390946401321671, -8.397313243818183892 ) ) ;
#41098=CARTESIAN_POINT ( 'NONE',  ( 112.5693548109119888, -10.63000616557722466, -14.87417383870573495 ) ) ;
#41103=CARTESIAN_POINT ( 'NONE',  ( 122.8368814775786291, -1.561330072975668948, -17.79121239304076951 ) ) ;
#41106=CARTESIAN_POINT ( 'NONE',  ( 121.6456214775786293, -10.63000616557722466, -14.87417383870573495 ) ) ;
#41107=CARTESIAN_POINT ( 'NONE',  ( 118.1852948109119836, -5.638512984488999180, -18.83840828888717311 ) ) ;
#41108=CARTESIAN_POINT ( 'NONE',  ( 119.7169148109119874, -0.1624402480850797581, -16.17319339645315424 ) ) ;
#41109=CARTESIAN_POINT ( 'NONE',  ( 123.8012348109119642, -9.565557343593413364, -10.61323700422348004 ) ) ;
#41110=CARTESIAN_POINT ( 'NONE',  ( 112.3023386403692427, -1.196538596002803212, -17.02799684832027438 ) ) ;
#41112=CARTESIAN_POINT ( 'NONE',  ( 122.5532481442453019, 0.4262465694468514643, -12.03445270309931736 ) ) ;
#41113=CARTESIAN_POINT ( 'NONE',  ( 122.1683934719562075, -1.125321370491285444, -17.12283323191017814 ) ) ;
#41118=CARTESIAN_POINT ( 'NONE',  ( 123.1205148109119563, -1.834011780172310813, -8.268836392978581529 ) ) ;
#41119=CARTESIAN_POINT ( 'NONE',  ( 121.2485348109119769, -8.899110576539710493, -16.42337572283490132 ) ) ;
#41121=CARTESIAN_POINT ( 'NONE',  ( 125.6732148109119862, 0.5811942927096110934, -14.16772938898807510 ) ) ;
#41122=CARTESIAN_POINT ( 'NONE',  ( 112.5693548109119888, 0.4262465694468514643, -12.03445270309931736 ) ) ;
#41123=CARTESIAN_POINT ( 'NONE',  ( 121.8725281442452939, -6.222761293078261424, -8.102969835052221015 ) ) ;
#41124=CARTESIAN_POINT ( 'NONE',  ( 118.4689281442453392, 0.9020085738987339008, -11.91225656197089222 ) ) ;
#41125=CARTESIAN_POINT ( 'NONE',  ( 121.0783548109119749, 0.2603800115204892296, -16.42320221600525088 ) ) ;
#41127=CARTESIAN_POINT ( 'NONE',  ( 113.0798948109119948, -0.4660016031367893996, -10.09054647747474043 ) ) ;
#41133=CARTESIAN_POINT ( 'NONE',  ( 118.7735460444391862, -1.267766418764730840, -16.93314635290706605 ) ) ;
#41134=CARTESIAN_POINT ( 'NONE',  ( 125.2761281442453054, 0.4262465694468514643, -12.03445270309931736 ) ) ;
#41137=CARTESIAN_POINT ( 'NONE',  ( 121.9292548109119849, -7.894159318335828068, -9.358103419637847864 ) ) ;
#41138=CARTESIAN_POINT ( 'NONE',  ( 116.5402214775786405, -9.565557343593413364, -10.61323700422348004 ) ) ;
#41139=CARTESIAN_POINT ( 'NONE',  ( 122.3830681442452857, -8.166667518702819706, -8.995218007635861213 ) ) ;
#41142=CARTESIAN_POINT ( 'NONE',  ( 123.3474214775786209, -0.1624402480850797581, -16.17319339645315424 ) ) ;
#41143=CARTESIAN_POINT ( 'NONE',  ( 116.9940348109119839, -9.988377603198976828, -10.36322818467138340 ) ) ;
#41144=CARTESIAN_POINT ( 'NONE',  ( 123.9146881442452894, 0.9020085738987339008, -11.91225656197089222 ) ) ;
#41145=CARTESIAN_POINT ( 'NONE',  ( 121.8725281442453223, -6.222761293078241884, -8.102969835052219238 ) ) ;
#41147=CARTESIAN_POINT ( 'NONE',  ( 123.7253032127138397, -2.191907684172563986, -18.20049396185734025 ) ) ;
#41148=CARTESIAN_POINT ( 'NONE',  ( 125.6732148109119862, 0.5811942927096110934, -14.16772938898807510 ) ) ;
#41149=CARTESIAN_POINT ( 'NONE',  ( 113.7038881442453402, -6.222761293078241884, -8.102969835052219238 ) ) ;
#41150=CARTESIAN_POINT ( 'NONE',  ( 124.2550481442452792, -9.988377603198980381, -10.36322818467138518 ) ) ;
#41151=CARTESIAN_POINT ( 'NONE',  ( 123.8328548109119822, -4.863998795839244771, -13.39321520033831625 ) ) ;
#41158=CARTESIAN_POINT ( 'NONE',  ( 124.1983214775786166, -1.833838273342659697, -17.42832698103878286 ) ) ;
#41159=CARTESIAN_POINT ( 'NONE',  ( 115.4056881442453459, -2.084020599724406786, -8.691656652584148546 ) ) ;
#41160=CARTESIAN_POINT ( 'NONE',  ( 126.2184548109119788, -5.568102603702699049, -18.34339073538272302 ) ) ;
#41167=CARTESIAN_POINT ( 'NONE',  ( 111.7751814775786556, -2.084020599724406786, -8.691656652584148546 ) ) ;
#41169=CARTESIAN_POINT ( 'NONE',  ( 124.7088614775786226, 0.2603800115204892296, -16.42320221600525088 ) ) ;
#41170=CARTESIAN_POINT ( 'NONE',  ( 125.5030348109119558, -6.222761293078241884, -8.102969835052219238 ) ) ;
#41172=CARTESIAN_POINT ( 'NONE',  ( 114.1009748109119784, -4.089484607189486809, -7.948022111789456723 ) ) ;
#41173=CARTESIAN_POINT ( 'NONE',  ( 127.0150841466606551, 0.2316552957976503180, -15.17538186860604732 ) ) ;
#41175=CARTESIAN_POINT ( 'NONE',  ( 123.6877814775786533, -6.222761293078241884, -8.102969835052219238 ) ) ;
#41176=CARTESIAN_POINT ( 'NONE',  ( 121.8158014775786171, -4.153390946401325223, -8.397313243818185668 ) ) ;
#41181=CARTESIAN_POINT ( 'NONE',  ( 113.8173414775786512, -9.565557343593413364, -10.61323700422348004 ) ) ;
#41186=CARTESIAN_POINT ( 'NONE',  ( 126.1837548109119211, -10.63000616557722466, -14.87417383870573495 ) ) ;
#41187=CARTESIAN_POINT ( 'NONE',  ( 120.2841814775786276, 0.9020085738987339008, -11.91225656197089222 ) ) ;
#41188=CARTESIAN_POINT ( 'NONE',  ( 110.2184548109119788, -5.044325091639137781, -11.90409383958792411 ) ) ;
#41189=CARTESIAN_POINT ( 'NONE',  ( 120.1707281442453166, 0.2603800115204892296, -16.42320221600525088 ) ) ;
#41190=ADVANCED_FACE ( 'NONE', ( #43455 ), #44639, .T. ) ;
#41191=CARTESIAN_POINT ( 'NONE',  ( 112.9097148109120070, 0.2603800115204892296, -16.42320221600525088 ) ) ;
#41194=CARTESIAN_POINT ( 'NONE',  ( 125.2194014775786286, -10.30919188438810075, -12.61870101168855918 ) ) ;
#41195=CARTESIAN_POINT ( 'NONE',  ( 124.6521348109119884, -1.561330072975668948, -17.79121239304076951 ) ) ;
#41196=CARTESIAN_POINT ( 'NONE',  ( 114.1009748109119784, -4.089484607189486809, -7.948022111789456723 ) ) ;
#41197=CARTESIAN_POINT ( 'NONE',  ( 126.0703014775786102, -9.988377603198980381, -10.36322818467138518 ) ) ;
#41200=CARTESIAN_POINT ( 'NONE',  ( 117.6180281442453150, -8.899110576539710493, -16.42337572283490132 ) ) ;
#41202=CARTESIAN_POINT ( 'NONE',  ( 113.1933481442453058, -4.089484607189486809, -7.948022111789456723 ) ) ;
#41203=CARTESIAN_POINT ( 'NONE',  ( 123.2339681442453241, -3.505236298600246325, -18.68346056562440793 ) ) ;
#41213=CARTESIAN_POINT ( 'NONE',  ( 112.2289948109119848, -7.643976991954077427, -18.09477374809248928 ) ) ;
#41217=CARTESIAN_POINT ( 'NONE',  ( 119.8303681442453126, -10.63000616557722466, -14.87417383870573495 ) ) ;
#41218=CARTESIAN_POINT ( 'NONE',  ( 137.0223538766786646, -4.519491365511462355, -18.82947256965501381 ) ) ;
#41221=CARTESIAN_POINT ( 'NONE',  ( 125.0849635773846842, -2.467220198597905867, -17.83387418641800437 ) ) ;
#41223=CARTESIAN_POINT ( 'NONE',  ( 120.7379948109119709, 0.4262465694468514643, -12.03445270309931736 ) ) ;
#41226=CARTESIAN_POINT ( 'NONE',  ( 118.2987481442453088, -1.561330072975668504, -17.79121239304076951 ) ) ;
#41228=CARTESIAN_POINT ( 'NONE',  ( 116.4834948109119779, -7.894159318335828068, -9.358103419637847864 ) ) ;
#41230=CARTESIAN_POINT ( 'NONE',  ( 113.4202548109119846, 0.1319031606808879209, -14.10382304977623669 ) ) ;
#41234=CARTESIAN_POINT ( 'NONE',  ( 117.7882081442453170, -3.505236298600246325, -18.68346056562440793 ) ) ;
#41235=CARTESIAN_POINT ( 'NONE',  ( 119.4900081442453086, -7.643976991954077427, -18.09477374809248928 ) ) ;
#41242=CARTESIAN_POINT ( 'NONE',  ( 112.5693548109119888, -10.63000616557722466, -14.87417383870573495 ) ) ;
#41249=CARTESIAN_POINT ( 'NONE',  ( 123.5909359023132907, -3.144421331627774041, -14.43411955300261340 ) ) ;
#41251=CARTESIAN_POINT ( 'NONE',  ( 123.2339681442453241, -6.344957434206665248, -7.627207830600338134 ) ) ;
#41252=CARTESIAN_POINT ( 'NONE',  ( 113.0231681442453322, 0.9020085738987339008, -11.91225656197089222 ) ) ;
#41253=CARTESIAN_POINT ( 'NONE',  ( 120.1707281442453166, -9.565557343593413364, -10.61323700422348004 ) ) ;
#41257=CARTESIAN_POINT ( 'NONE',  ( 121.1918081442452859, 0.9020085738987339008, -11.91225656197089222 ) ) ;
#41258=CARTESIAN_POINT ( 'NONE',  ( 119.3765548109119834, 0.9020085738987339008, -11.91225656197089222 ) ) ;
#41259=AXIS2_PLACEMENT_3D ( 'NONE', #30940, #20005, #33891 ) ;
#41261=CARTESIAN_POINT ( 'NONE',  ( 113.7038881442453402, -6.222761293078241884, -8.102969835052219238 ) ) ;
#41264=CARTESIAN_POINT ( 'NONE',  ( 116.8805814775786445, -6.344957434206662583, -7.627207830600332805 ) ) ;
#41267=CARTESIAN_POINT ( 'NONE',  ( 116.0864081442453113, -9.988377603198976828, -10.36322818467138340 ) ) ;
#41269=CARTESIAN_POINT ( 'NONE',  ( 126.0135748109119902, -8.166667518702819706, -8.995218007635861213 ) ) ;
#41273=CARTESIAN_POINT ( 'NONE',  ( 114.8951481442453115, -8.899110576539710493, -16.42337572283490132 ) ) ;
#41275=CARTESIAN_POINT ( 'NONE',  ( 118.8092881442453290, -0.1624402480850797581, -16.17319339645315424 ) ) ;
#41278=CARTESIAN_POINT ( 'NONE',  ( 115.1787814775786387, -0.1624402480850797581, -16.17319339645315424 ) ) ;
#41279=CARTESIAN_POINT ( 'NONE',  ( 116.9373081442452929, -8.166667518702817929, -8.995218007635861213 ) ) ;
#41281=CARTESIAN_POINT ( 'NONE',  ( 117.5045748109119756, 0.5811942927096110934, -14.16772938898807510 ) ) ;
#41282=CARTESIAN_POINT ( 'NONE',  ( 112.2857214775786474, -5.574606645277164318, -18.38911715685844683 ) ) ;
#41283=CARTESIAN_POINT ( 'NONE',  ( 117.1642148109119859, -0.8288870151387760510, -10.36305467784173118 ) ) ;
#41285=CARTESIAN_POINT ( 'NONE',  ( 112.1722681442453222, -0.4660016031367893996, -10.09054647747474043 ) ) ;
#41288=AXIS2_PLACEMENT_3D ( 'NONE', #32427, #10800, #24696 ) ;
#41292=CARTESIAN_POINT ( 'NONE',  ( 118.9227414775786400, -10.63000616557722466, -14.87417383870573495 ) ) ;
#41293=ORIENTED_EDGE ( 'NONE', *, *, #31181, .F. ) ;
#41294=DIRECTION ( 'NONE',  ( 1.000000000000000000, 0.000000000000000000, 0.000000000000000000 ) ) ;
#41295=CARTESIAN_POINT ( 'NONE',  ( 118.5823814775786360, -7.643976991954077427, -18.09477374809248928 ) ) ;
#41296=CARTESIAN_POINT ( 'NONE',  ( 124.2666781415389039, -0.1020945015694913471, -15.74893487844866691 ) ) ;
#41299=CARTESIAN_POINT ( 'NONE',  ( 121.8158014775786171, -5.638512984488999180, -18.83840828888717311 ) ) ;
#41301=CARTESIAN_POINT ( 'NONE',  ( 124.3640859692789462, -1.179503403430468333, -17.05068175419387089 ) ) ;
#41304=CARTESIAN_POINT ( 'NONE',  ( 122.8936081442453059, -9.565557343593413364, -10.61323700422348004 ) ) ;
#41305=CARTESIAN_POINT ( 'NONE',  ( 125.1059481442452750, -8.166667518702819706, -8.995218007635861213 ) ) ;
#41307=CARTESIAN_POINT ( 'NONE',  ( 118.4689281442453392, -10.15424416112533912, -14.75197769757731336 ) ) ;
#41308=CARTESIAN_POINT ( 'NONE',  ( 119.0929214775786278, -5.638512984488999180, -18.83840828888717311 ) ) ;
#41311=CARTESIAN_POINT ( 'NONE',  ( 126.6827570900246656, -1.214894069026291934, -9.643484958278310870 ) ) ;
#41312=CARTESIAN_POINT ( 'NONE',  ( 121.5888948109119809, 0.1319031606808879209, -14.10382304977623669 ) ) ;
#41316=CARTESIAN_POINT ( 'NONE',  ( 116.7104014775786425, -0.4660016031367893996, -10.09054647747474043 ) ) ;
#41317=CARTESIAN_POINT ( 'NONE',  ( 125.5597614775786326, -7.894159318335828068, -9.358103419637847864 ) ) ;
#41320=CARTESIAN_POINT ( 'NONE',  ( 135.4522060580625293, -1.191823701641487432, -8.648235046535946324 ) ) ;
#41321=CARTESIAN_POINT ( 'NONE',  ( 123.0070614775786169, 0.9020085738987339008, -11.91225656197089222 ) ) ;
#41323=CARTESIAN_POINT ( 'NONE',  ( 119.8870948109119752, -0.8288870151387760510, -10.36305467784173118 ) ) ;
#41327=CARTESIAN_POINT ( 'NONE',  ( 125.9001214775786224, -5.574606645277164318, -18.38911715685844683 ) ) ;
#41328=CARTESIAN_POINT ( 'NONE',  ( 124.1983214775786166, -1.833838273342659697, -17.42832698103878286 ) ) ;
#41332=CARTESIAN_POINT ( 'NONE',  ( 121.9292548109119849, -1.561330072975668948, -17.79121239304076951 ) ) ;
#41335=CARTESIAN_POINT ( 'NONE',  ( 119.7736414775786358, -10.30919188438810075, -12.61870101168855918 ) ) ;
#41336=CARTESIAN_POINT ( 'NONE',  ( 118.8660148109119774, -10.30919188438810075, -12.61870101168855918 ) ) ;
#41337=CARTESIAN_POINT ( 'NONE',  ( 120.8514481442452961, -2.084020599724406786, -8.691656652584148546 ) ) ;
#41339=CARTESIAN_POINT ( 'NONE',  ( 116.3700414775786527, -5.638512984488999180, -18.83840828888717311 ) ) ;
#41343=CARTESIAN_POINT ( 'NONE',  ( 122.8368814775786291, -7.894159318335828068, -9.358103419637847864 ) ) ;
#41349=CARTESIAN_POINT ( 'NONE',  ( 121.8725281442453223, -3.383040157471821630, -19.15922257007629170 ) ) ;
#41350=CARTESIAN_POINT ( 'NONE',  ( 121.8725281442453223, -6.222761293078241884, -8.102969835052219238 ) ) ;
#41352=CARTESIAN_POINT ( 'NONE',  ( 124.4252281442452812, -9.261995988541697145, -16.69588392320189030 ) ) ;
#41355=CARTESIAN_POINT ( 'NONE',  ( 122.4397948109119767, -9.988377603198976828, -10.36322818467138340 ) ) ;
#41356=CARTESIAN_POINT ( 'NONE',  ( 121.5321681442453183, -9.988377603198976828, -10.36322818467138340 ) ) ;
#41358=CARTESIAN_POINT ( 'NONE',  ( 113.3635281442453504, -9.988377603198976828, -10.36322818467138340 ) ) ;
#41363=CARTESIAN_POINT ( 'NONE',  ( 114.2327140574772670, -2.443475742715324639, -17.86549347949428679 ) ) ;
#41364=CARTESIAN_POINT ( 'NONE',  ( 124.7655881442452852, -9.859900752359378018, -12.68260735090039759 ) ) ;
#41365=EDGE_CURVE ( 'NONE', #33919, #6291, #8800, .T. ) ;
#41368=CARTESIAN_POINT ( 'NONE',  ( 123.2339681442453241, -3.505236298600246325, -18.68346056562440793 ) ) ;
#41369=CARTESIAN_POINT ( 'NONE',  ( 117.8449348109119938, -1.833838273342659253, -17.42832698103878286 ) ) ;
#41370=CARTESIAN_POINT ( 'NONE',  ( 111.5482748109120053, -0.1624402480850797581, -16.17319339645315424 ) ) ;
#41374=CARTESIAN_POINT ( 'NONE',  ( 119.3765548109119834, 0.9020085738987339008, -11.91225656197089222 ) ) ;
#41380=CARTESIAN_POINT ( 'NONE',  ( 114.5547881442453217, -4.153390946401321671, -8.397313243818183892 ) ) ;
#41381=CARTESIAN_POINT ( 'NONE',  ( 112.2289948109119848, -7.643976991954077427, -18.09477374809248928 ) ) ;
#41389=CARTESIAN_POINT ( 'NONE',  ( 121.9859814775786333, -9.565557343593413364, -10.61323700422348004 ) ) ;
#41390=CARTESIAN_POINT ( 'NONE',  ( 114.2711548109119803, -0.1624402480850797581, -16.17319339645315424 ) ) ;
#41393=LINE ( 'NONE', #23605, #34589 ) ;
#41399=CARTESIAN_POINT ( 'NONE',  ( 112.4559014775786494, -9.988377603198976828, -10.36322818467138340 ) ) ;
#41401=CARTESIAN_POINT ( 'NONE',  ( 112.9664414775786412, 0.5811942927096154232, -14.16772938898807155 ) ) ;
#41404=CARTESIAN_POINT ( 'NONE',  ( 125.9568481442452850, -3.505236298600246325, -18.68346056562440793 ) ) ;
#41405=CARTESIAN_POINT ( 'NONE',  ( 123.7445081442452874, -7.894159318335828068, -9.358103419637847864 ) ) ;
#41410=CARTESIAN_POINT ( 'NONE',  ( 113.0231681442453180, -10.15424416112533912, -14.75197769757731336 ) ) ;
#41416=CARTESIAN_POINT ( 'NONE',  ( 124.4819548109119722, -7.893985811506177619, -18.51759400769804742 ) ) ;
#41417=CARTESIAN_POINT ( 'NONE',  ( 112.0588148109119828, -9.859900752359374465, -12.68260735090039404 ) ) ;
#41419=CARTESIAN_POINT ( 'NONE',  ( 121.3052614775786111, -1.834011780172310813, -8.268836392978581529 ) ) ;
#41420=CARTESIAN_POINT ( 'NONE',  ( 117.1074881442453233, -10.63000616557722466, -14.87417383870573495 ) ) ;
#41422=CARTESIAN_POINT ( 'NONE',  ( 111.7184548109119788, -0.8288870151387760510, -10.36305467784173118 ) ) ;
#41423=CARTESIAN_POINT ( 'NONE',  ( 123.2339681442453241, -6.344957434206665248, -7.627207830600338134 ) ) ;
#41424=CARTESIAN_POINT ( 'NONE',  ( 115.7460481442453357, 0.9020085738987339008, -11.91225656197089222 ) ) ;
#41425=CARTESIAN_POINT ( 'NONE',  ( 116.5969481442453031, -9.859900752359374465, -12.68260735090039404 ) ) ;
#41427=CARTESIAN_POINT ( 'NONE',  ( 117.3343948109119737, -6.222761293078241884, -8.102969835052219238 ) ) ;
#41428=CARTESIAN_POINT ( 'NONE',  ( 115.1220548109119761, -8.166667518702817929, -8.995218007635861213 ) ) ;
#41429=CARTESIAN_POINT ( 'NONE',  ( 122.7234281442452755, -4.153390946401325223, -8.397313243818185668 ) ) ;
#41434=CARTESIAN_POINT ( 'NONE',  ( 125.5597614775786326, -1.561330072975669392, -17.79121239304076951 ) ) ;
#41441=CARTESIAN_POINT ( 'NONE',  ( 117.3343948109119737, -3.383040157471821630, -19.15922257007629170 ) ) ;
#41445=CARTESIAN_POINT ( 'NONE',  ( 122.6667014775786413, -2.084020599724406786, -8.691656652584148546 ) ) ;
#41448=CARTESIAN_POINT ( 'NONE',  ( 117.9016614775786280, -9.988377603198976828, -10.36322818467138340 ) ) ;
#41449=CARTESIAN_POINT ( 'NONE',  ( 126.2404814775786264, -9.261995988541697145, -16.69588392320189030 ) ) ;
#41450=CARTESIAN_POINT ( 'NONE',  ( 114.0442481442453300, -7.643976991954077427, -18.09477374809248928 ) ) ;
#41451=CARTESIAN_POINT ( 'NONE',  ( 112.5693548109119888, 0.4262465694468514643, -12.03445270309931736 ) ) ;
#41455=CARTESIAN_POINT ( 'NONE',  ( 116.6536748109119941, -10.15424416112533912, -14.75197769757731336 ) ) ;
#41456=CARTESIAN_POINT ( 'NONE',  ( 121.0216281442452981, -7.894159318335828068, -9.358103419637847864 ) ) ;
#41461=CARTESIAN_POINT ( 'NONE',  ( 114.0442481442453300, -1.834011780172310813, -8.268836392978581529 ) ) ;
#41462=CARTESIAN_POINT ( 'NONE',  ( 116.5969481442453031, 0.5811942927096154232, -14.16772938898807155 ) ) ;
#41466=CARTESIAN_POINT ( 'NONE',  ( 123.4588159614330749, -2.807939993087918751, -14.88215444561602219 ) ) ;
#41469=CARTESIAN_POINT ( 'NONE',  ( 121.9292548109119849, -1.561330072975668948, -17.79121239304076951 ) ) ;
#41470=CARTESIAN_POINT ( 'NONE',  ( 114.3278814775786429, -10.30919188438810075, -12.61870101168855918 ) ) ;
#41471=CARTESIAN_POINT ( 'NONE',  ( 119.7169148109119874, -0.1624402480850797581, -16.17319339645315424 ) ) ;
#41472=( NAMED_UNIT ( * ) PLANE_ANGLE_UNIT ( ) SI_UNIT ( $, .RADIAN. ) );
#41475=CARTESIAN_POINT ( 'NONE',  ( 123.0637881442452937, -0.4660016031367893996, -10.09054647747474043 ) ) ;
#41476=CARTESIAN_POINT ( 'NONE',  ( 117.2776681442452968, -5.638512984488999180, -18.83840828888717311 ) ) ;
#41477=EDGE_CURVE ( 'NONE', #37342, #37016, #23399, .T. ) ;
#41479=CARTESIAN_POINT ( 'NONE',  ( 112.0588148109119828, -9.859900752359374465, -12.68260735090039404 ) ) ;
#41481=ORIENTED_EDGE ( 'NONE', *, *, #5828, .F. ) ;
#41482=CARTESIAN_POINT ( 'NONE',  ( 116.6536748109119941, 0.9020085738987339008, -11.91225656197089222 ) ) ;
#41484=CARTESIAN_POINT ( 'NONE',  ( 116.9373081442452929, -8.166667518702817929, -8.995218007635861213 ) ) ;
#41487=CARTESIAN_POINT ( 'NONE',  ( 124.9924948109119924, -4.089484607189486809, -7.948022111789456723 ) ) ;
#41492=CARTESIAN_POINT ( 'NONE',  ( 115.7460481442453357, -10.15424416112533912, -14.75197769757731336 ) ) ;
#41496=CARTESIAN_POINT ( 'NONE',  ( 116.8238548109119819, -5.574606645277164318, -18.38911715685844683 ) ) ;
#41497=VECTOR ( 'NONE', #11204, 1000.000000000000000 ) ;
#41499=CARTESIAN_POINT ( 'NONE',  ( 115.6325948109119821, -9.565557343593413364, -10.61323700422348004 ) ) ;
#41500=FACE_OUTER_BOUND ( 'NONE', #13037, .T. ) ;
#41501=CARTESIAN_POINT ( 'NONE',  ( 114.0442481442453300, -1.834011780172310813, -8.268836392978581529 ) ) ;
#41502=CARTESIAN_POINT ( 'NONE',  ( 126.1270281442452870, -10.30919188438810075, -12.61870101168855918 ) ) ;
#41504=CARTESIAN_POINT ( 'NONE',  ( 116.0864081442453113, -0.1624402480850797581, -16.17319339645315424 ) ) ;
#41506=CARTESIAN_POINT ( 'NONE',  ( 115.2922348109119781, -10.63000616557722466, -14.87417383870573495 ) ) ;
#41509=CARTESIAN_POINT ( 'NONE',  ( 110.2184548109119788, -1.904930392188239452, -16.08466725871020842 ) ) ;
#41510=CARTESIAN_POINT ( 'NONE',  ( 127.9673516049440138, -4.191936442424658793, -15.53703219575882954 ) ) ;
#41511=CARTESIAN_POINT ( 'NONE',  ( 121.3619881442452879, -4.089484607189486809, -7.948022111789456723 ) ) ;
#41515=CARTESIAN_POINT ( 'NONE',  ( 116.3700414775786527, -4.153390946401321671, -8.397313243818183892 ) ) ;
#41517=CARTESIAN_POINT ( 'NONE',  ( 123.0637881442452937, -0.4660016031367893996, -10.09054647747474043 ) ) ;
#41519=CARTESIAN_POINT ( 'NONE',  ( 124.6713397424434078, -0.9924539043446091169, -17.29976612834908423 ) ) ;
#41521=CARTESIAN_POINT ( 'NONE',  ( 112.7395348109119766, -5.638512984488999180, -18.83840828888717311 ) ) ;
#41522=CARTESIAN_POINT ( 'NONE',  ( 112.1722681442453222, -0.4660016031367893996, -10.09054647747474043 ) ) ;
#41523=CARTESIAN_POINT ( 'NONE',  ( 123.0070614775786169, 0.9020085738987339008, -11.91225656197089222 ) ) ;
#41524=CARTESIAN_POINT ( 'NONE',  ( 117.1074881442453233, 0.4262465694468514643, -12.03445270309931736 ) ) ;
#41526=CARTESIAN_POINT ( 'NONE',  ( 118.8092881442453290, -9.988377603198976828, -10.36322818467138340 ) ) ;
#41528=CARTESIAN_POINT ( 'NONE',  ( 123.4608748109119745, 0.4262465694468514643, -12.03445270309931736 ) ) ;
#41532=CARTESIAN_POINT ( 'NONE',  ( 115.4056881442453459, -7.893985811506177619, -18.51759400769804742 ) ) ;
#41533=CARTESIAN_POINT ( 'NONE',  ( 124.0848681442452772, -5.574606645277164318, -18.38911715685844683 ) ) ;
#41536=CARTESIAN_POINT ( 'NONE',  ( 137.0105207745634743, -1.266623274720264369, -9.287743120492423898 ) ) ;
#41537=CARTESIAN_POINT ( 'NONE',  ( 121.0783548109119749, 0.2603800115204892296, -16.42320221600525088 ) ) ;
#41539=CARTESIAN_POINT ( 'NONE',  ( 120.6245414775786458, -0.1624402480850797581, -16.17319339645315424 ) ) ;
#41543=CARTESIAN_POINT ( 'NONE',  ( 114.8951481442453115, -0.4660016031367893996, -10.09054647747474043 ) ) ;
#41549=CARTESIAN_POINT ( 'NONE',  ( 123.3474214775786209, -9.988377603198976828, -10.36322818467138340 ) ) ;
#41550=CARTESIAN_POINT ( 'NONE',  ( 111.6428307106015438, -9.187052517560628573, -16.66868250367536319 ) ) ;
#41552=CARTESIAN_POINT ( 'NONE',  ( 119.9438214775786378, -7.893985811506177619, -18.51759400769804742 ) ) ;
#41553=CARTESIAN_POINT ( 'NONE',  ( 118.4689281442453392, 0.9020085738987339008, -11.91225656197089222 ) ) ;
#41554=CARTESIAN_POINT ( 'NONE',  ( 120.6812681442452941, 0.1319031606808879209, -14.10382304977623669 ) ) ;
#41556=CARTESIAN_POINT ( 'NONE',  ( 125.4924948109119924, -4.159894987976798575, -8.443039665293765594 ) ) ;
#41557=CARTESIAN_POINT ( 'NONE',  ( 116.0296814775786345, -8.166667518702817929, -8.995218007635861213 ) ) ;
#41559=CARTESIAN_POINT ( 'NONE',  ( 112.5693548109119888, -10.63000616557722466, -14.87417383870573495 ) ) ;
#41565=CARTESIAN_POINT ( 'NONE',  ( 125.2761281442453054, -10.63000616557722466, -14.87417383870573495 ) ) ;
#41566=CARTESIAN_POINT ( 'NONE',  ( 111.7751814775786556, -7.893985811506177619, -18.51759400769804742 ) ) ;
#41568=CARTESIAN_POINT ( 'NONE',  ( 126.1837548109119211, -10.63000616557722466, -14.87417383870573495 ) ) ;
#41570=CARTESIAN_POINT ( 'NONE',  ( 123.0070614775786169, 0.9020085738987339008, -11.91225656197089222 ) ) ;
#41571=CARTESIAN_POINT ( 'NONE',  ( 123.9146881442452894, 0.9020085738987339008, -11.91225656197089222 ) ) ;
#41573=CARTESIAN_POINT ( 'NONE',  ( 112.1155414775786454, 0.9020085738987339008, -11.91225656197089222 ) ) ;
#41579=CARTESIAN_POINT ( 'NONE',  ( 113.8740681442453138, -9.859900752359374465, -12.68260735090039404 ) ) ;
#41580=CARTESIAN_POINT ( 'NONE',  ( 113.5337081442453240, -9.261995988541697145, -16.69588392320189030 ) ) ;
#41584=CARTESIAN_POINT ( 'NONE',  ( 120.3976348109119812, -7.643976991954077427, -18.09477374809248928 ) ) ;
#41586=CARTESIAN_POINT ( 'NONE',  ( 116.3133148109120043, -2.084020599724406786, -8.691656652584148546 ) ) ;
#41587=CARTESIAN_POINT ( 'NONE',  ( 113.2500748109119968, -3.505236298600246325, -18.68346056562440793 ) ) ;
#41590=CARTESIAN_POINT ( 'NONE',  ( 119.8870948109119752, -9.261995988541697145, -16.69588392320189030 ) ) ;
#41592=CARTESIAN_POINT ( 'NONE',  ( 113.3068014775786594, -1.833838273342658809, -17.42832698103878286 ) ) ;
#41595=EDGE_CURVE ( 'NONE', #35460, #38024, #19588, .T. ) ;
#41597=CARTESIAN_POINT ( 'NONE',  ( 119.7169148109119874, -0.1624402480850797581, -16.17319339645315424 ) ) ;
#41598=CARTESIAN_POINT ( 'NONE',  ( 112.5126281442453120, 0.1319031606808879209, -14.10382304977623669 ) ) ;
#41606=EDGE_CURVE ( 'NONE', #43185, #35115, #1003, .T. ) ;
#41610=CARTESIAN_POINT ( 'NONE',  ( 122.7801548109119665, -6.222761293078241884, -8.102969835052219238 ) ) ;
#41611=CARTESIAN_POINT ( 'NONE',  ( 118.5823814775786360, -7.643976991954077427, -18.09477374809248928 ) ) ;
#41612=CYLINDRICAL_SURFACE ( 'NONE', #18480, 1.999999999999998890 ) ;
#41613=ORIENTED_EDGE ( 'NONE', *, *, #21674, .T. ) ;
#41614=CARTESIAN_POINT ( 'NONE',  ( 127.5515732256049262, -2.090882025624695384, -18.33502473074995720 ) ) ;
#41615=CARTESIAN_POINT ( 'NONE',  ( 115.4624148109119943, -4.153390946401321671, -8.397313243818183892 ) ) ;
#41618=CARTESIAN_POINT ( 'NONE',  ( 124.8790414775786246, -8.899110576539710493, -16.42337572283490132 ) ) ;
#41620=CARTESIAN_POINT ( 'NONE',  ( 114.7816948109119863, 0.5811942927096154232, -14.16772938898807155 ) ) ;
#41621=CARTESIAN_POINT ( 'NONE',  ( 126.8396850857678970, 0.1815689017518152260, -15.05047689119776422 ) ) ;
#41623=CARTESIAN_POINT ( 'NONE',  ( 113.5904348109119866, -7.893985811506177619, -18.51759400769804742 ) ) ;
#41624=CARTESIAN_POINT ( 'NONE',  ( 115.6325948109119821, 0.2603800115204892296, -16.42320221600525088 ) ) ;
#41625=CARTESIAN_POINT ( 'NONE',  ( 123.8579614775786126, -9.859900752359378018, -12.68260735090039759 ) ) ;
#41631=CARTESIAN_POINT ( 'NONE',  ( 117.6180281442453150, -8.899110576539710493, -16.42337572283490132 ) ) ;
#41635=CARTESIAN_POINT ( 'NONE',  ( 126.1270281442452870, -10.30919188438810075, -12.61870101168855918 ) ) ;
#41636=CARTESIAN_POINT ( 'NONE',  ( 125.9568481442452850, -6.344957434206665248, -7.627207830600338134 ) ) ;
#41637=CARTESIAN_POINT ( 'NONE',  ( 120.0005481442453146, -4.153390946401307460, -8.397313243818183892 ) ) ;
#41638=( BOUNDED_CURVE ( )  B_SPLINE_CURVE ( 2, ( #15710, #40103, #26196, #8863, #22765, #33010, #1785, #43528, #12957, #19105, #36420, #33899, #41004, #2445, #1996, #43511, #9758 ),
 .UNSPECIFIED., .F., .T. ) 
 B_SPLINE_CURVE_WITH_KNOTS ( ( 3, 2, 2, 2, 2, 2, 2, 2, 3 ),
 ( 0.07950466748089210500, 0.08593750000000000000, 0.09375000000000000000, 0.1015625000000000000, 0.1093750000000000000, 0.1171875000000000000, 0.1250000000000000000, 0.1328125000000000000, 0.1392453325190584068 ),
 .UNSPECIFIED. ) 
 CURVE ( )  GEOMETRIC_REPRESENTATION_ITEM ( )  RATIONAL_B_SPLINE_CURVE ( ( 0.9778625265006459788, 0.9373222120152200354, 1.000000000000000000, 0.9238795325112869605, 1.000000000000000000, 0.9238795325112869605, 1.000000000000000000, 0.9238795325112869605, 1.000000000000000000, 0.9238795325112869605, 1.000000000000000000, 0.9238795325112869605, 1.000000000000000000, 0.9238795325112869605, 1.000000000000000000, 0.9373222120157019832, 0.9778625265000240319 ) ) 
 REPRESENTATION_ITEM ( '' )  );
#41639=CARTESIAN_POINT ( 'NONE',  ( 119.8303681442453126, -10.63000616557722466, -14.87417383870573495 ) ) ;
#41640=CARTESIAN_POINT ( 'NONE',  ( 117.7882081442453170, -6.344957434206665248, -7.627207830600338134 ) ) ;
#41641=ORIENTED_EDGE ( 'NONE', *, *, #21172, .T. ) ;
#41642=CARTESIAN_POINT ( 'NONE',  ( 114.8384214775786489, -10.15424416112533912, -14.75197769757731336 ) ) ;
#41644=CARTESIAN_POINT ( 'NONE',  ( 124.3117748109119844, -10.30919188438810075, -12.61870101168855918 ) ) ;
#41645=CARTESIAN_POINT ( 'NONE',  ( 112.9097148109120070, 0.2603800115204892296, -16.42320221600525088 ) ) ;
#41646=CARTESIAN_POINT ( 'NONE',  ( 116.5402214775786405, -9.565557343593413364, -10.61323700422348004 ) ) ;
#41648=CARTESIAN_POINT ( 'NONE',  ( 120.7379948109119709, 0.4262465694468514643, -12.03445270309931736 ) ) ;
#41649=CARTESIAN_POINT ( 'NONE',  ( 117.9583881442453048, -10.30919188438810075, -12.61870101168855918 ) ) ;
#41657=CARTESIAN_POINT ( 'NONE',  ( 114.6115148109119986, -3.383040157471821630, -19.15922257007629170 ) ) ;
#41660=CARTESIAN_POINT ( 'NONE',  ( 112.3424481442453384, -3.505236298600246325, -18.68346056562440793 ) ) ;
#41661=B_SPLINE_CURVE_WITH_KNOTS ( 'NONE', 3,
 ( #21526, #28601, #11501, #999, #39304, #32001, #21976, #32450, #28370, #22198, #32227, #38843, #36094, #17883, #7847, #42735, #42283, #35864, #4637, #11045, #1441, #39752, #8521, #11719, #18558, #32673, #1224, #25179, #15138, #18108 ),
 .UNSPECIFIED., .F., .F.,
 ( 4, 2, 2, 1, 1, 1, 2, 2, 2, 1, 1, 1, 2, 2, 1, 1, 2, 2, 4 ),
 ( 0.000000000000000000, 0.2499999999999658606, 0.3749999999999484857, 0.4374999999999535372, 0.4687499999999424349, 0.4843749999999234501, 0.4921874999999282796, 0.4999999999999330536, 0.6249999999999854561, 0.6875000000000218714, 0.7187500000000519584, 0.7343750000000555112, 0.7421875000000458522, 0.7500000000000361933, 0.8125000000000430767, 0.8437500000000454081, 0.8593750000000381917, 0.8750000000000309752, 1.000000000000000000 ),
 .UNSPECIFIED. ) ;
#41665=CARTESIAN_POINT ( 'NONE',  ( 119.7169148109119874, -9.988377603198976828, -10.36322818467138340 ) ) ;
#41669=CARTESIAN_POINT ( 'NONE',  ( 120.7947214775786193, -0.8288870151387760510, -10.36305467784173118 ) ) ;
#41671=CARTESIAN_POINT ( 'NONE',  ( 125.7866681442452688, -0.4660016031367893996, -10.09054647747474043 ) ) ;
#41672=CARTESIAN_POINT ( 'NONE',  ( 118.1285681442453068, -7.893985811506177619, -18.51759400769804742 ) ) ;
#41674=CARTESIAN_POINT ( 'NONE',  ( 115.1787814775786387, -0.1624402480850797581, -16.17319339645315424 ) ) ;
#41675=CARTESIAN_POINT ( 'NONE',  ( 113.9875214775786532, -8.899110576539710493, -16.42337572283490132 ) ) ;
#41678=CARTESIAN_POINT ( 'NONE',  ( 118.5256548109119876, -8.899110576539710493, -16.42337572283490132 ) ) ;
#41679=CARTESIAN_POINT ( 'NONE',  ( 121.9292548109119849, -7.894159318335828068, -9.358103419637847864 ) ) ;
#41683=CARTESIAN_POINT ( 'NONE',  ( 112.6260814775786514, -9.261995988541697145, -16.69588392320189030 ) ) ;
#41684=CARTESIAN_POINT ( 'NONE',  ( 115.5191414775786569, -3.383040157471821630, -19.15922257007629170 ) ) ;
#41688=CARTESIAN_POINT ( 'NONE',  ( 120.9649014775786355, -3.383040157471821630, -19.15922257007629170 ) ) ;
#41689=CARTESIAN_POINT ( 'NONE',  ( 112.3424481442453384, -6.344957434206662583, -7.627207830600332805 ) ) ;
#41690=CARTESIAN_POINT ( 'NONE',  ( 118.9227414775786542, 0.4262465694468514643, -12.03445270309931736 ) ) ;
#41691=( NAMED_UNIT ( * ) SI_UNIT ( $, .STERADIAN. ) SOLID_ANGLE_UNIT ( ) );
#41692=CARTESIAN_POINT ( 'NONE',  ( 123.4608748109119745, -10.63000616557722466, -14.87417383870573495 ) ) ;
#41693=CARTESIAN_POINT ( 'NONE',  ( 119.0929214775786278, -5.638512984488999180, -18.83840828888717311 ) ) ;
#41695=CARTESIAN_POINT ( 'NONE',  ( 111.4915481442453142, -1.833838273342658365, -17.42832698103878286 ) ) ;
#41698=VERTEX_POINT ( 'NONE', #36098 ) ;
#41699=CARTESIAN_POINT ( 'NONE',  ( 119.3198281442452924, 0.5811942927096110934, -14.16772938898807510 ) ) ;
#41701=CARTESIAN_POINT ( 'NONE',  ( 116.8805814775786445, -6.344957434206662583, -7.627207830600332805 ) ) ;
#41704=CARTESIAN_POINT ( 'NONE',  ( 126.0703014775786102, -9.988377603198980381, -10.36322818467138518 ) ) ;
#41709=CARTESIAN_POINT ( 'NONE',  ( 119.7169148109119874, -0.1624402480850797581, -16.17319339645315424 ) ) ;
#41712=CARTESIAN_POINT ( 'NONE',  ( 117.3343948109119737, -6.222761293078241884, -8.102969835052219238 ) ) ;
#41715=CARTESIAN_POINT ( 'NONE',  ( 120.6812681442452941, 0.1319031606808879209, -14.10382304977623669 ) ) ;
#41716=CARTESIAN_POINT ( 'NONE',  ( 116.2565881442452991, -9.261995988541697145, -16.69588392320189030 ) ) ;
#41718=CARTESIAN_POINT ( 'NONE',  ( 117.2776681442452968, -4.153390946401321671, -8.397313243818183892 ) ) ;
#41719=EDGE_LOOP ( 'NONE', ( #43108, #33704, #5100, #5434 ) ) ;
#41720=CARTESIAN_POINT ( 'NONE',  ( 115.1220548109119761, -8.166667518702817929, -8.995218007635861213 ) ) ;
#41722=CARTESIAN_POINT ( 'NONE',  ( 116.0086969107182142, -2.467220198592777525, -17.83387418641524391 ) ) ;
#41726=CARTESIAN_POINT ( 'NONE',  ( 123.9146881442452894, 0.9020085738987339008, -11.91225656197089222 ) ) ;
#41728=CARTESIAN_POINT ( 'NONE',  ( 127.1653849502245350, -8.988304812967710333, -9.794650042750394192 ) ) ;
#41729=CARTESIAN_POINT ( 'NONE',  ( 117.0507614775786465, 0.1319031606808879209, -14.10382304977623669 ) ) ;
#41732=CARTESIAN_POINT ( 'NONE',  ( 122.0994348109119443, 0.9020085738987339008, -11.91225656197089222 ) ) ;
#41737=CARTESIAN_POINT ( 'NONE',  ( 112.6828081442453282, -7.893985811506177619, -18.51759400769804742 ) ) ;
#41738=CARTESIAN_POINT ( 'NONE',  ( 123.4608748109119745, -10.63000616557722466, -14.87417383870573495 ) ) ;
#41739=CARTESIAN_POINT ( 'NONE',  ( 116.9373081442452929, -1.833838273342659253, -17.42832698103878286 ) ) ;
#41741=CARTESIAN_POINT ( 'NONE',  ( 117.5613014775786525, 0.9020085738987339008, -11.91225656197089222 ) ) ;
#41743=CARTESIAN_POINT ( 'NONE',  ( 123.7445081442452874, -7.894159318335828068, -9.358103419637847864 ) ) ;
#41750=CARTESIAN_POINT ( 'NONE',  ( 118.3554748109119998, 0.2603800115204892296, -16.42320221600525088 ) ) ;
#41751=CARTESIAN_POINT ( 'NONE',  ( 124.1983214775786166, -1.833838273342659697, -17.42832698103878286 ) ) ;
#41752=VERTEX_POINT ( 'NONE', #8079 ) ;
#41754=CARTESIAN_POINT ( 'NONE',  ( 137.2865145795275339, -1.213646807504741520, -9.647614279156686123 ) ) ;
#41755=CARTESIAN_POINT ( 'NONE',  ( 121.1350814775786233, 0.5811942927096110934, -14.16772938898807510 ) ) ;
#41757=CARTESIAN_POINT ( 'NONE',  ( 121.1918081442452859, -10.15424416112533912, -14.75197769757731336 ) ) ;
#41760=CARTESIAN_POINT ( 'NONE',  ( 115.7460481442453357, 0.9020085738987339008, -11.91225656197089222 ) ) ;
#41761=B_SPLINE_CURVE_WITH_KNOTS ( 'NONE', 3,
 ( #23782, #36973, #44523, #16712, #13287, #40424, #41113, #17536, #23314, #7262 ),
 .UNSPECIFIED., .F., .F.,
 ( 4, 3, 3, 4 ),
 ( 1.939479807224430197E-18, 0.0001671877548681299829, 0.0003343755096277730159, 0.0006463528481650649771 ),
 .UNSPECIFIED. ) ;
#41762=CARTESIAN_POINT ( 'NONE',  ( 124.7088614775786226, -9.565557343593413364, -10.61323700422348004 ) ) ;
#41765=CARTESIAN_POINT ( 'NONE',  ( 120.5110881442453206, -6.344957434206665248, -7.627207830600338134 ) ) ;
#41769=CARTESIAN_POINT ( 'NONE',  ( 123.8579614775786126, 0.5811942927096110934, -14.16772938898807510 ) ) ;
#41770=CARTESIAN_POINT ( 'NONE',  ( 117.5045748109119756, 0.5811942927096110934, -14.16772938898807510 ) ) ;
#41771=CARTESIAN_POINT ( 'NONE',  ( 121.9859814775786333, -9.565557343593413364, -10.61323700422348004 ) ) ;
#41772=CARTESIAN_POINT ( 'NONE',  ( 121.5321681442453183, -0.1624402480850797581, -16.17319339645315424 ) ) ;
#41774=CARTESIAN_POINT ( 'NONE',  ( 114.3846081442453197, -10.63000616557722466, -14.87417383870573495 ) ) ;
#41784=CARTESIAN_POINT ( 'NONE',  ( 124.9252281442453238, -8.862178061931794915, -16.39564131203325559 ) ) ;
#41785=CARTESIAN_POINT ( 'NONE',  ( 126.6942948109119840, -8.899110576539710493, -16.42337572283490132 ) ) ;
#41787=CARTESIAN_POINT ( 'NONE',  ( 123.2339681442453241, -6.344957434206665248, -7.627207830600338134 ) ) ;
#41790=CARTESIAN_POINT ( 'NONE',  ( 123.0637881442452937, -0.4660016031367893996, -10.09054647747474043 ) ) ;
#41791=CARTESIAN_POINT ( 'NONE',  ( 126.2404814775786264, -9.261995988541697145, -16.69588392320189030 ) ) ;
#41793=CARTESIAN_POINT ( 'NONE',  ( 112.5693548109119888, -10.63000616557722466, -14.87417383870573495 ) ) ;
#41800=CARTESIAN_POINT ( 'NONE',  ( 115.1220548109119761, -1.833838273342658809, -17.42832698103878286 ) ) ;
#41801=CARTESIAN_POINT ( 'NONE',  ( 114.0442481442453300, -1.834011780172310813, -8.268836392978581529 ) ) ;
#41805=CARTESIAN_POINT ( 'NONE',  ( 121.3052614775786111, -7.643976991954077427, -18.09477374809248928 ) ) ;
#41806=CARTESIAN_POINT ( 'NONE',  ( 118.0718414775786442, -0.8288870151387760510, -10.36305467784173118 ) ) ;
#41807=CARTESIAN_POINT ( 'NONE',  ( 113.3635281442453504, -0.1624402480850797581, -16.17319339645315424 ) ) ;
#41813=CARTESIAN_POINT ( 'NONE',  ( 113.9875214775786532, -8.899110576539710493, -16.42337572283490132 ) ) ;
#41819=CARTESIAN_POINT ( 'NONE',  ( 118.2987481442453088, -7.894159318335828068, -9.358103419637847864 ) ) ;
#41820=CARTESIAN_POINT ( 'NONE',  ( 114.0442481442453300, -7.643976991954077427, -18.09477374809248928 ) ) ;
#41826=CARTESIAN_POINT ( 'NONE',  ( 118.2062230939976644, -2.236191541394346061, -18.14152338500401029 ) ) ;
#41827=CARTESIAN_POINT ( 'NONE',  ( 121.9292548109119849, -7.894159318335828068, -9.358103419637847864 ) ) ;
#41828=CARTESIAN_POINT ( 'NONE',  ( 119.1496481442453046, -6.222761293078241884, -8.102969835052219238 ) ) ;
#41832=CARTESIAN_POINT ( 'NONE',  ( 117.2209414775786485, -2.084020599724406786, -8.691656652584148546 ) ) ;
#41836=CARTESIAN_POINT ( 'NONE',  ( 115.9729548109119861, -6.344957434206662583, -7.627207830600332805 ) ) ;
#41838=CARTESIAN_POINT ( 'NONE',  ( 113.4769814775786330, -10.63000616557722466, -14.87417383870573495 ) ) ;
#41839=DIRECTION ( 'NONE',  ( 1.000000000000000000, 0.000000000000000000, 0.000000000000000000 ) ) ;
#41841=CARTESIAN_POINT ( 'NONE',  ( 113.9875214775786532, -0.4660016031367893996, -10.09054647747474043 ) ) ;
#41843=CARTESIAN_POINT ( 'NONE',  ( 113.7038881442453402, -3.383040157471821630, -19.15922257007629170 ) ) ;
#41844=CARTESIAN_POINT ( 'NONE',  ( 125.3895814775786448, -2.084020599724406786, -8.691656652584148546 ) ) ;
#41849=CARTESIAN_POINT ( 'NONE',  ( 115.5758681442453053, -7.894159318335828068, -9.358103419637847864 ) ) ;
#41853=CARTESIAN_POINT ( 'NONE',  ( 126.5041214912238416, -4.774006015657890067, -8.251167430307914330 ) ) ;
#41854=CARTESIAN_POINT ( 'NONE',  ( 125.5597614775786326, -1.561330072975669392, -17.79121239304076951 ) ) ;
#41855=CARTESIAN_POINT ( 'NONE',  ( 136.4689272580744444, 0.8652765085456386451, -12.77968882490968561 ) ) ;
#41856=CARTESIAN_POINT ( 'NONE',  ( 121.4187148109119789, -6.344957434206665248, -7.627207830600338134 ) ) ;
#41857=CARTESIAN_POINT ( 'NONE',  ( 116.3133148109119759, -7.893985811506177619, -18.51759400769804742 ) ) ;
#41859=CARTESIAN_POINT ( 'NONE',  ( 116.2565881442453133, -0.8288870151387760510, -10.36305467784173118 ) ) ;
#41860=CARTESIAN_POINT ( 'NONE',  ( 122.5532481442453019, -10.63000616557722466, -14.87417383870573495 ) ) ;
#41861=CARTESIAN_POINT ( 'NONE',  ( 118.2420214775786320, -3.383040157471821630, -19.15922257007629170 ) ) ;
#41862=CARTESIAN_POINT ( 'NONE',  ( 115.2922348109119781, 0.4262465694468514643, -12.03445270309931736 ) ) ;
#41865=CARTESIAN_POINT ( 'NONE',  ( 119.5467348109119712, -5.574606645277164318, -18.38911715685844683 ) ) ;
#41867=CARTESIAN_POINT ( 'NONE',  ( 115.7460481442453357, 0.9020085738987339008, -11.91225656197089222 ) ) ;
#41868=CARTESIAN_POINT ( 'NONE',  ( 136.9144124994549259, 0.3076051572492725650, -15.33370174593263435 ) ) ;
#41873=CARTESIAN_POINT ( 'NONE',  ( 116.3700414775786527, -5.638512984488999180, -18.83840828888717311 ) ) ;
#41874=CARTESIAN_POINT ( 'NONE',  ( 136.7082020370515636, -10.48511845154063593, -13.91967875158812973 ) ) ;
#41879=CARTESIAN_POINT ( 'NONE',  ( 118.2420214775786320, -3.383040157471821630, -19.15922257007629170 ) ) ;
#41882=CARTESIAN_POINT ( 'NONE',  ( 119.1871698793805194, -2.191907684172563986, -18.20049396185734025 ) ) ;
#41884=CARTESIAN_POINT ( 'NONE',  ( 120.9081748109119872, -4.153390946401325223, -8.397313243818185668 ) ) ;
#41885=ORIENTED_EDGE ( 'NONE', *, *, #2425, .F. ) ;
#41886=CARTESIAN_POINT ( 'NONE',  ( 125.1626748109119802, -9.988377603198980381, -10.36322818467138518 ) ) ;
#41887=CARTESIAN_POINT ( 'NONE',  ( 122.4965214775786251, -10.30919188438810075, -12.61870101168855918 ) ) ;
#41889=CARTESIAN_POINT ( 'NONE',  ( 114.7816948109119863, -9.859900752359374465, -12.68260735090039404 ) ) ;
#41891=CARTESIAN_POINT ( 'NONE',  ( 114.3278814775786429, 0.1319031606808879209, -14.10382304977623669 ) ) ;
#41894=CARTESIAN_POINT ( 'NONE',  ( 119.7736414775786358, 0.1319031606808879209, -14.10382304977623669 ) ) ;
#41895=CARTESIAN_POINT ( 'NONE',  ( 121.5321681442453183, -0.1624402480850797581, -16.17319339645315424 ) ) ;
#41896=CARTESIAN_POINT ( 'NONE',  ( 151.2860562277021472, -4.863998795839242995, -13.39321520033831447 ) ) ;
#41901=CARTESIAN_POINT ( 'NONE',  ( 112.1722681442453222, -0.4660016031367893996, -10.09054647747474043 ) ) ;
#41902=CARTESIAN_POINT ( 'NONE',  ( 113.1366214775786432, -1.834011780172310813, -8.268836392978581529 ) ) ;
#41908=CARTESIAN_POINT ( 'NONE',  ( 120.4543614775786295, -4.089484607189486809, -7.948022111789456723 ) ) ;
#41909=CARTESIAN_POINT ( 'NONE',  ( 113.8173414775786512, 0.2603800115204892296, -16.42320221600525088 ) ) ;
#41911=CARTESIAN_POINT ( 'NONE',  ( 122.9503348109119827, -9.859900752359378018, -12.68260735090039759 ) ) ;
#41912=( NAMED_UNIT ( * ) SI_UNIT ( $, .STERADIAN. ) SOLID_ANGLE_UNIT ( ) );
#41913=CARTESIAN_POINT ( 'NONE',  ( 111.7184548109119788, -0.8288870151387760510, -10.36305467784173118 ) ) ;
#41914=CARTESIAN_POINT ( 'NONE',  ( 117.1074881442453233, -10.63000616557722466, -14.87417383870573495 ) ) ;
#41916=CARTESIAN_POINT ( 'NONE',  ( 113.3068014775786594, -1.833838273342658809, -17.42832698103878286 ) ) ;
#41918=CARTESIAN_POINT ( 'NONE',  ( 119.9438214775786378, -7.893985811506177619, -18.51759400769804742 ) ) ;
#41920=CARTESIAN_POINT ( 'NONE',  ( 117.3343948109119737, -3.383040157471821630, -19.15922257007629170 ) ) ;
#41922=ORIENTED_EDGE ( 'NONE', *, *, #19165, .F. ) ;
#41924=CARTESIAN_POINT ( 'NONE',  ( 124.5386814775786206, -5.638512984488999180, -18.83840828888717311 ) ) ;
#41925=EDGE_CURVE ( 'NONE', #31472, #23145, #17216, .T. ) ;
#41927=CARTESIAN_POINT ( 'NONE',  ( 112.7395348109119766, -4.153390946401321671, -8.397313243818183892 ) ) ;
#41929=CARTESIAN_POINT ( 'NONE',  ( 120.9081748109119872, -4.153390946401325223, -8.397313243818185668 ) ) ;
#41932=CARTESIAN_POINT ( 'NONE',  ( 121.1350814775786233, -9.859900752359378018, -12.68260735090039759 ) ) ;
#41935=CARTESIAN_POINT ( 'NONE',  ( 120.9081748109119872, -4.153390946401325223, -8.397313243818185668 ) ) ;
#41937=CARTESIAN_POINT ( 'NONE',  ( 116.8805814775786445, -6.344957434206662583, -7.627207830600332805 ) ) ;
#41938=CARTESIAN_POINT ( 'NONE',  ( 123.2906948109119867, -8.166667518702798390, -8.995218007635845225 ) ) ;
#41939=CARTESIAN_POINT ( 'NONE',  ( 120.3409081442453044, -8.899110576539710493, -16.42337572283490132 ) ) ;
#41941=CARTESIAN_POINT ( 'NONE',  ( 116.3133148109119759, -7.893985811506177619, -18.51759400769804742 ) ) ;
#41947=CARTESIAN_POINT ( 'NONE',  ( 122.7801548109119665, -3.383040157471821630, -19.15922257007629170 ) ) ;
#41948=VERTEX_POINT ( 'NONE', #8976 ) ;
#41949=CARTESIAN_POINT ( 'NONE',  ( 118.3969758961590486, -2.263366209404196638, -18.10533625161307114 ) ) ;
#41950=CARTESIAN_POINT ( 'NONE',  ( 118.2420214775786320, -6.222761293078241884, -8.102969835052219238 ) ) ;
#41957=CARTESIAN_POINT ( 'NONE',  ( 115.8595014775786609, -1.834011780172310813, -8.268836392978581529 ) ) ;
#41958=CARTESIAN_POINT ( 'NONE',  ( 126.1837548109119496, 0.4262465694468514643, -12.03445270309931736 ) ) ;
#41959=CARTESIAN_POINT ( 'NONE',  ( 122.3263414775786373, -6.344957434206665248, -7.627207830600338134 ) ) ;
#41960=CARTESIAN_POINT ( 'NONE',  ( 116.0296814775786345, -1.833838273342658809, -17.42832698103878286 ) ) ;
#41962=CARTESIAN_POINT ( 'NONE',  ( 117.6747548109119919, -1.834011780172310813, -8.268836392978581529 ) ) ;
#41966=CARTESIAN_POINT ( 'NONE',  ( 123.9146881442452894, -10.15424416112533912, -14.75197769757731336 ) ) ;
#41970=CARTESIAN_POINT ( 'NONE',  ( 117.7314814775786260, -4.089484607189486809, -7.948022111789456723 ) ) ;
#41971=CARTESIAN_POINT ( 'NONE',  ( 123.9146881442452894, -10.15424416112533912, -14.75197769757731336 ) ) ;
#41974=CARTESIAN_POINT ( 'NONE',  ( 135.8497638153261278, 0.6772939217498697984, -11.19057417008355770 ) ) ;
#41975=CARTESIAN_POINT ( 'NONE',  ( 122.3830681442452857, -8.166667518702819706, -8.995218007635861213 ) ) ;
#41977=CARTESIAN_POINT ( 'NONE',  ( 121.5888948109119809, 0.1319031606808879209, -14.10382304977623669 ) ) ;
#41979=EDGE_LOOP ( 'NONE', ( #37815, #10132, #39719, #18010, #6463 ) ) ;
#41980=CARTESIAN_POINT ( 'NONE',  ( 112.9664414775786412, 0.5811942927096154232, -14.16772938898807155 ) ) ;
#41981=CARTESIAN_POINT ( 'NONE',  ( 124.2550481442452792, -0.1624402480850797581, -16.17319339645315424 ) ) ;
#41982=CARTESIAN_POINT ( 'NONE',  ( 120.3976348109119812, -1.834011780172310591, -8.268836392978581529 ) ) ;
#41984=CARTESIAN_POINT ( 'NONE',  ( 125.3328548109119964, -9.261995988541697145, -16.69588392320189030 ) ) ;
#41988=CARTESIAN_POINT ( 'NONE',  ( 124.7088614775786226, 0.2603800115204892296, -16.42320221600525088 ) ) ;
#41989=CARTESIAN_POINT ( 'NONE',  ( 121.0216281442452981, -1.561330072975668948, -17.79121239304076951 ) ) ;
#41990=CARTESIAN_POINT ( 'NONE',  ( 125.1626748109119802, -0.1624402480850797581, -16.17319339645315424 ) ) ;
#41991=CARTESIAN_POINT ( 'NONE',  ( 121.1918081442452859, -10.15424416112533912, -14.75197769757731336 ) ) ;
#41992=CARTESIAN_POINT ( 'NONE',  ( 125.8328548109119964, -8.862178061931773598, -16.39564131203328401 ) ) ;
#41993=CARTESIAN_POINT ( 'NONE',  ( 115.1220548109119761, -8.166667518702817929, -8.995218007635861213 ) ) ;
#41994=ADVANCED_FACE ( 'NONE', ( #36546 ), #22874, .T. ) ;
#41997=CARTESIAN_POINT ( 'NONE',  ( 124.8790414775786388, -8.899110576539117190, -16.42337572283568647 ) ) ;
#42001=CARTESIAN_POINT ( 'NONE',  ( 124.3117748109119844, -10.30919188438810075, -12.61870101168855918 ) ) ;
#42002=CARTESIAN_POINT ( 'NONE',  ( 126.1837548109119496, 0.4262465694468514643, -12.03445270309931736 ) ) ;
#42004=CARTESIAN_POINT ( 'NONE',  ( 114.6682414775786469, -7.894159318335828068, -9.358103419637847864 ) ) ;
#42007=CARTESIAN_POINT ( 'NONE',  ( 124.3117748109119844, -10.30919188438810075, -12.61870101168855918 ) ) ;
#42008=CARTESIAN_POINT ( 'NONE',  ( 124.0848681442452772, -4.089484607189486809, -7.948022111789456723 ) ) ;
#42010=CARTESIAN_POINT ( 'NONE',  ( 112.3991748109119868, -8.166667518702817929, -8.995218007635859436 ) ) ;
#42014=CARTESIAN_POINT ( 'NONE',  ( 116.5969481442453031, -9.859900752359374465, -12.68260735090039404 ) ) ;
#42015=CARTESIAN_POINT ( 'NONE',  ( 113.8740681442453138, 0.5811942927096154232, -14.16772938898807155 ) ) ;
#42018=CARTESIAN_POINT ( 'NONE',  ( 121.7023481442452777, -0.8288870151387760510, -10.36305467784173118 ) ) ;
#42019=UNCERTAINTY_MEASURE_WITH_UNIT (LENGTH_MEASURE( 1.000000000000000082E-05 ), #14534, 'distance_accuracy_value', 'NONE');
#42020=CARTESIAN_POINT ( 'NONE',  ( 119.2631014775786298, -9.565557343593413364, -10.61323700422348004 ) ) ;
#42021=CARTESIAN_POINT ( 'NONE',  ( 111.6050014775786536, 0.1319031606808879209, -14.10382304977623669 ) ) ;
#42027=CARTESIAN_POINT ( 'NONE',  ( 115.3489614775786407, -0.8288870151387760510, -10.36305467784173118 ) ) ;
#42031=CARTESIAN_POINT ( 'NONE',  ( 112.2289948109119848, -1.834011780172310813, -8.268836392978581529 ) ) ;
#42035=ORIENTED_EDGE ( 'NONE', *, *, #21963, .T. ) ;
#42036=CARTESIAN_POINT ( 'NONE',  ( 119.2631014775786298, -9.565557343593413364, -10.61323700422348004 ) ) ;
#42037=CARTESIAN_POINT ( 'NONE',  ( 114.3846081442453197, 0.4262465694468514643, -12.03445270309931736 ) ) ;
#42045=CARTESIAN_POINT ( 'NONE',  ( 114.2711548109119803, -9.988377603198976828, -10.36322818467138340 ) ) ;
#42047=CARTESIAN_POINT ( 'NONE',  ( 122.2128881442453263, -7.643976991954077427, -18.09477374809248928 ) ) ;
#42048=CARTESIAN_POINT ( 'NONE',  ( 119.4900081442453086, -7.643976991954077427, -18.09477374809248928 ) ) ;
#42049=CARTESIAN_POINT ( 'NONE',  ( 113.7038881442453260, -6.222761293078232114, -8.102969835052212133 ) ) ;
#42051=EDGE_CURVE ( 'NONE', #32220, #45010, #13082, .T. ) ;
#42053=CARTESIAN_POINT ( 'NONE',  ( 117.2776681442452968, -4.153390946401321671, -8.397313243818183892 ) ) ;
#42056=CARTESIAN_POINT ( 'NONE',  ( 116.5760198611596081, -1.036737761566197014, -17.24079555149560861 ) ) ;
#42057=CARTESIAN_POINT ( 'NONE',  ( 114.4980614775786592, -7.893985811506177619, -18.51759400769804742 ) ) ;
#42059=CARTESIAN_POINT ( 'NONE',  ( 116.3133148109119759, -7.893985811506177619, -18.51759400769804742 ) ) ;
#42062=CARTESIAN_POINT ( 'NONE',  ( 114.4980614775786592, -7.893985811506177619, -18.51759400769804742 ) ) ;
#42063=CARTESIAN_POINT ( 'NONE',  ( 113.1366214775786432, -1.834011780172310813, -8.268836392978581529 ) ) ;
#42065=CARTESIAN_POINT ( 'NONE',  ( 124.0848681442452772, -5.574606645277164318, -18.38911715685844683 ) ) ;
#42068=ORIENTED_EDGE ( 'NONE', *, *, #7164, .T. ) ;
#42069=CARTESIAN_POINT ( 'NONE',  ( 120.5495288976800055, -1.244021962887374544, -16.96476564598603076 ) ) ;
#42071=CARTESIAN_POINT ( 'NONE',  ( 117.2776681442452968, -4.153390946401321671, -8.397313243818183892 ) ) ;
#42073=CARTESIAN_POINT ( 'NONE',  ( 122.6995153496756501, -1.087735405160626723, -17.17288456429612964 ) ) ;
#42075=CARTESIAN_POINT ( 'NONE',  ( 127.0264730702696028, -5.161070523558970891, -7.997376402438204579 ) ) ;
#42076=CARTESIAN_POINT ( 'NONE',  ( 126.1270281442452870, -10.30919188438810075, -12.61870101168855918 ) ) ;
#42078=CARTESIAN_POINT ( 'NONE',  ( 125.2761281442453054, -10.63000616557722466, -14.87417383870573495 ) ) ;
#42079=CARTESIAN_POINT ( 'NONE',  ( 114.8384214775786489, 0.9020085738987339008, -11.91225656197089222 ) ) ;
#42081=CARTESIAN_POINT ( 'NONE',  ( 114.7249681442453237, -9.565557343593413364, -10.61323700422348004 ) ) ;
#42083=CARTESIAN_POINT ( 'NONE',  ( 119.2063748109119814, -1.561330072975668504, -17.79121239304076951 ) ) ;
#42084=CARTESIAN_POINT ( 'NONE',  ( 115.9729548109119861, -3.505236298600246325, -18.68346056562440793 ) ) ;
#42086=CARTESIAN_POINT ( 'NONE',  ( 123.0637881442452937, -8.899110576539710493, -16.42337572283490132 ) ) ;
#42088=CARTESIAN_POINT ( 'NONE',  ( 115.1787814775786387, -9.988377603198976828, -10.36322818467138340 ) ) ;
#42092=CARTESIAN_POINT ( 'NONE',  ( 126.8316248077902486, 0.4396069532502042687, -13.21529045708529182 ) ) ;
#42094=CARTESIAN_POINT ( 'NONE',  ( 113.8173414775786512, 0.2603800115204892296, -16.42320221600525088 ) ) ;
#42095=CARTESIAN_POINT ( 'NONE',  ( 136.2267163768109981, -10.68226541249164896, -14.07034713969670747 ) ) ;
#42101=CARTESIAN_POINT ( 'NONE',  ( 112.4559014775786778, -0.1624402480850797581, -16.17319339645315424 ) ) ;
#42103=CARTESIAN_POINT ( 'NONE',  ( 111.6669404873412077, -2.348512537728060234, -17.99195118506215962 ) ) ;
#42105=CARTESIAN_POINT ( 'NONE',  ( 116.5969481442453031, 0.5811942927096154232, -14.16772938898807155 ) ) ;
#42107=B_SPLINE_CURVE_WITH_KNOTS ( 'NONE', 3,
 ( #36355, #22015, #18596, #40016, #32708, #29079, #8781, #26339, #22235, #4901 ),
 .UNSPECIFIED., .F., .F.,
 ( 4, 3, 3, 4 ),
 ( 2.453269466693399854E-18, 0.0001671877548681249956, 0.0003343755096277640170, 0.0006463528481650609656 ),
 .UNSPECIFIED. ) ;
#42109=CARTESIAN_POINT ( 'NONE',  ( 119.3765548109119834, -10.15424416112533912, -14.75197769757731336 ) ) ;
#42113=CARTESIAN_POINT ( 'NONE',  ( 124.5386814775786206, -5.638512984488999180, -18.83840828888717311 ) ) ;
#42115=CARTESIAN_POINT ( 'NONE',  ( 115.0653281442453277, -3.505236298600246325, -18.68346056562440793 ) ) ;
#42116=CARTESIAN_POINT ( 'NONE',  ( 111.9453614775786434, -7.894159318335828068, -9.358103419637847864 ) ) ;
#42119=CARTESIAN_POINT ( 'NONE',  ( 120.7379948109119709, 0.4262465694468514643, -12.03445270309931736 ) ) ;
#42120=CARTESIAN_POINT ( 'NONE',  ( 118.8092881442453290, -0.1624402480850797581, -16.17319339645315424 ) ) ;
#42121=CARTESIAN_POINT ( 'NONE',  ( 116.7671281442453193, -7.643976991954101408, -18.09477374809246797 ) ) ;
#42126=CARTESIAN_POINT ( 'NONE',  ( 115.9162281442453235, -4.089484607189486809, -7.948022111789456723 ) ) ;
#42127=CARTESIAN_POINT ( 'NONE',  ( 115.8027748109119841, -0.4660016031367893996, -10.09054647747474043 ) ) ;
#42129=CARTESIAN_POINT ( 'NONE',  ( 114.4980614775786592, -7.893985811506177619, -18.51759400769804742 ) ) ;
#42131=CARTESIAN_POINT ( 'NONE',  ( 113.3277860444392076, -1.267766418764742165, -16.93314635290707315 ) ) ;
#42132=CARTESIAN_POINT ( 'NONE',  ( 121.4754414775786131, -8.166667518702819706, -8.995218007635861213 ) ) ;
#42133=CARTESIAN_POINT ( 'NONE',  ( 115.8595014775786609, -1.834011780172310813, -8.268836392978581529 ) ) ;
#42134=CARTESIAN_POINT ( 'NONE',  ( 121.7023481442452919, -0.8288870151387760510, -10.36305467784173118 ) ) ;
#42136=CARTESIAN_POINT ( 'NONE',  ( 111.6050014775786536, 0.1319031606808879209, -14.10382304977623669 ) ) ;
#42137=CARTESIAN_POINT ( 'NONE',  ( 123.0637881442452937, -0.4660016031367893996, -10.09054647747474043 ) ) ;
#42140=CARTESIAN_POINT ( 'NONE',  ( 116.1431348109119881, 0.1319031606808879209, -14.10382304977623669 ) ) ;
#42143=CARTESIAN_POINT ( 'NONE',  ( 122.8936081442453059, 0.2603800115204892296, -16.42320221600525088 ) ) ;
#42146=CARTESIAN_POINT ( 'NONE',  ( 119.2063748109119814, -1.561330072975668504, -17.79121239304076951 ) ) ;
#42149=CARTESIAN_POINT ( 'NONE',  ( 125.2761281442453054, -10.63000616557722466, -14.87417383870573495 ) ) ;
#42151=CARTESIAN_POINT ( 'NONE',  ( 115.5758681442453053, -7.894159318335828068, -9.358103419637847864 ) ) ;
#42154=CARTESIAN_POINT ( 'NONE',  ( 121.5321681442453183, -0.1624402480850797581, -16.17319339645315424 ) ) ;
#42156=CARTESIAN_POINT ( 'NONE',  ( 120.4543614775786295, -5.574606645277164318, -18.38911715685844683 ) ) ;
#42158=CARTESIAN_POINT ( 'NONE',  ( 120.2841814775786276, -10.15424416112533912, -14.75197769757731336 ) ) ;
#42160=CARTESIAN_POINT ( 'NONE',  ( 116.8238548109119819, -4.089484607189486809, -7.948022111789456723 ) ) ;
#42162=CARTESIAN_POINT ( 'NONE',  ( 119.3198281442452924, -9.859900752359374465, -12.68260735090039404 ) ) ;
#42163=ORIENTED_EDGE ( 'NONE', *, *, #7558, .F. ) ;
#42164=CARTESIAN_POINT ( 'NONE',  ( 116.1431348109119881, -10.30919188438810075, -12.61870101168855918 ) ) ;
#42170=CARTESIAN_POINT ( 'NONE',  ( 124.1415948109119540, -6.344957434206665248, -7.627207830600338134 ) ) ;
#42172=CARTESIAN_POINT ( 'NONE',  ( 127.3669547543381526, -9.122482256072121487, -9.796118959629435352 ) ) ;
#42173=CARTESIAN_POINT ( 'NONE',  ( 120.6812681442452941, 0.1319031606808879209, -14.10382304977623669 ) ) ;
#42174=CARTESIAN_POINT ( 'NONE',  ( 116.3133148109119759, -7.893985811506194494, -18.51759400769804031 ) ) ;
#42180=CARTESIAN_POINT ( 'NONE',  ( 115.2922348109119781, -10.63000616557722466, -14.87417383870573495 ) ) ;
#42181=CARTESIAN_POINT ( 'NONE',  ( 124.4252281442452812, -0.8288870151387760510, -10.36305467784173118 ) ) ;
#42182=CARTESIAN_POINT ( 'NONE',  ( 123.2906948109119867, -8.166667518702819706, -8.995218007635861213 ) ) ;
#42183=CARTESIAN_POINT ( 'NONE',  ( 116.5402214775786405, -9.565557343593413364, -10.61323700422348004 ) ) ;
#42184=CARTESIAN_POINT ( 'NONE',  ( 127.0150841466604277, -3.081832127571603408, -8.297561108701472676 ) ) ;
#42185=CARTESIAN_POINT ( 'NONE',  ( 0.000000000000000000, 0.000000000000000000, 0.000000000000000000 ) ) ;
#42186=CARTESIAN_POINT ( 'NONE',  ( 122.6099748109119929, -9.261995988541697145, -16.69588392320189030 ) ) ;
#42190=CARTESIAN_POINT ( 'NONE',  ( 124.9357681442453014, -7.643976991954077427, -18.09477374809248928 ) ) ;
#42193=CARTESIAN_POINT ( 'NONE',  ( 119.6601881442453106, -8.166667518702819706, -8.995218007635861213 ) ) ;
#42194=CARTESIAN_POINT ( 'NONE',  ( 124.9924948109119924, -5.574606645277164318, -18.38911715685844683 ) ) ;
#42196=CARTESIAN_POINT ( 'NONE',  ( 136.8611794030201168, 0.2047575970914792265, -11.11870408231551899 ) ) ;
#42197=CARTESIAN_POINT ( 'NONE',  ( 121.5321681442453183, -9.988377603198976828, -10.36322818467138340 ) ) ;
#42199=CARTESIAN_POINT ( 'NONE',  ( 119.6601881442453106, -1.833838273342659253, -17.42832698103878286 ) ) ;
#42201=CARTESIAN_POINT ( 'NONE',  ( 115.4624148109119943, -5.638512984488999180, -18.83840828888717311 ) ) ;
#42205=CARTESIAN_POINT ( 'NONE',  ( 120.7947214775786193, -9.261995988541706026, -16.69588392320187964 ) ) ;
#42207=CARTESIAN_POINT ( 'NONE',  ( 111.2646414775786496, -8.899110576539710493, -16.42337572283490132 ) ) ;
#42211=CARTESIAN_POINT ( 'NONE',  ( 122.6099748109119929, -9.261995988541697145, -16.69588392320189030 ) ) ;
#42212=CARTESIAN_POINT ( 'NONE',  ( 121.6456214775786293, -10.63000616557722466, -14.87417383870573495 ) ) ;
#42213=CARTESIAN_POINT ( 'NONE',  ( 123.5176014775786228, -0.8288870151387760510, -10.36305467784173118 ) ) ;
#42214=CARTESIAN_POINT ( 'NONE',  ( 119.4332814775786318, -8.899110576539710493, -16.42337572283490132 ) ) ;
#42216=CARTESIAN_POINT ( 'NONE',  ( 116.6536748109119941, 0.9020085738987339008, -11.91225656197089222 ) ) ;
#42223=CARTESIAN_POINT ( 'NONE',  ( 124.6521348109119884, -1.561330072975668948, -17.79121239304076951 ) ) ;
#42224=CARTESIAN_POINT ( 'NONE',  ( 112.7962614775786676, -3.383040157471821630, -19.15922257007629170 ) ) ;
#42226=CARTESIAN_POINT ( 'NONE',  ( 113.6471614775786492, -4.153390946401321671, -8.397313243818183892 ) ) ;
#42229=CARTESIAN_POINT ( 'NONE',  ( 123.7445081442452874, -1.561330072975668948, -17.79121239304076951 ) ) ;
#42230=CARTESIAN_POINT ( 'NONE',  ( 124.3117748109119844, -10.30919188438810075, -12.61870101168855918 ) ) ;
#42232=CARTESIAN_POINT ( 'NONE',  ( 114.6682414775786469, -1.561330072975668060, -17.79121239304076596 ) ) ;
#42235=VERTEX_POINT ( 'NONE', #17616 ) ;
#42236=CARTESIAN_POINT ( 'NONE',  ( 126.4915402333594301, -7.429179904925708122, -8.943053816332739103 ) ) ;
#42237=CARTESIAN_POINT ( 'NONE',  ( 114.0442481442453300, -7.643976991954077427, -18.09477374809248928 ) ) ;
#42238=CARTESIAN_POINT ( 'NONE',  ( 112.9664414775786412, 0.5811942927096154232, -14.16772938898807155 ) ) ;
#42242=CARTESIAN_POINT ( 'NONE',  ( 121.1350814775786233, -9.859900752359378018, -12.68260735090039759 ) ) ;
#42243=CARTESIAN_POINT ( 'NONE',  ( 112.9664414775786412, -9.859900752359374465, -12.68260735090039404 ) ) ;
#42248=CARTESIAN_POINT ( 'NONE',  ( 115.0653281442453277, -3.505236298600246325, -18.68346056562440793 ) ) ;
#42251=CARTESIAN_POINT ( 'NONE',  ( 126.5621572004020408, -9.382143744326477020, -15.91102935692771680 ) ) ;
#42252=CARTESIAN_POINT ( 'NONE',  ( 112.1722681442453222, -0.4660016031367893996, -10.09054647747474043 ) ) ;
#42254=CARTESIAN_POINT ( 'NONE',  ( 125.3328548109119964, -0.8288870151387760510, -10.36305467784173118 ) ) ;
#42256=CARTESIAN_POINT ( 'NONE',  ( 118.7525614775786380, -1.833838273342659253, -17.42832698103878286 ) ) ;
#42257=CARTESIAN_POINT ( 'NONE',  ( 117.2209414775786485, -2.084020599724406786, -8.691656652584148546 ) ) ;
#42265=CARTESIAN_POINT ( 'NONE',  ( 114.0442481442453300, -1.834011780172310813, -8.268836392978581529 ) ) ;
#42266=CARTESIAN_POINT ( 'NONE',  ( 112.2289948109119848, -1.834011780172310813, -8.268836392978581529 ) ) ;
#42267=CARTESIAN_POINT ( 'NONE',  ( 118.0718414775786442, -0.8288870151387760510, -10.36305467784173118 ) ) ;
#42268=CARTESIAN_POINT ( 'NONE',  ( 113.4202548109119846, 0.1319031606808870605, -14.10382304977625090 ) ) ;
#42270=CARTESIAN_POINT ( 'NONE',  ( 115.3489614775786407, -0.8288870151387760510, -10.36305467784173118 ) ) ;
#42273=CARTESIAN_POINT ( 'NONE',  ( 125.1613296207260078, -1.288565105604724703, -16.90544979172889484 ) ) ;
#42275=CARTESIAN_POINT ( 'NONE',  ( 114.0442481442453300, -1.834011780172310813, -8.268836392978581529 ) ) ;
#42278=CARTESIAN_POINT ( 'NONE',  ( 117.0507614775786465, -10.30919188438810075, -12.61870101168855918 ) ) ;
#42281=CARTESIAN_POINT ( 'NONE',  ( 112.5126281442453120, -10.30919188438810075, -12.61870101168855918 ) ) ;
#42282=CARTESIAN_POINT ( 'NONE',  ( 112.9664414775786412, 0.5811942927096154232, -14.16772938898807155 ) ) ;
#42283=CARTESIAN_POINT ( 'NONE',  ( 126.5561942423865105, -10.03277835551166497, -13.35508656583795606 ) ) ;
#42290=CARTESIAN_POINT ( 'NONE',  ( 117.7314814775786260, -5.574606645277164318, -18.38911715685844683 ) ) ;
#42294=CARTESIAN_POINT ( 'NONE',  ( 126.2455040230451573, -4.383286045279406018, -8.401547924378691690 ) ) ;
#42295=CARTESIAN_POINT ( 'NONE',  ( 124.5386814775786206, -5.638512984488999180, -18.83840828888717311 ) ) ;
#42296=CARTESIAN_POINT ( 'NONE',  ( 119.8303681442452984, 0.4262465694468589028, -12.03445270309934578 ) ) ;
#42297=CARTESIAN_POINT ( 'NONE',  ( 125.6732148109119862, 0.5811942927096110934, -14.16772938898807510 ) ) ;
#42298=CARTESIAN_POINT ( 'NONE',  ( 116.5969481442453031, 0.5811942927096154232, -14.16772938898807155 ) ) ;
#42299=ORIENTED_EDGE ( 'NONE', *, *, #36685, .F. ) ;
#42300=CARTESIAN_POINT ( 'NONE',  ( 114.0442481442453300, -7.643976991954077427, -18.09477374809248928 ) ) ;
#42301=CARTESIAN_POINT ( 'NONE',  ( 116.6536748109119941, 0.9020085738987339008, -11.91225656197089222 ) ) ;
#42302=CARTESIAN_POINT ( 'NONE',  ( 114.4413348109119823, -0.8288870151387760510, -10.36305467784173118 ) ) ;
#42303=ORIENTED_EDGE ( 'NONE', *, *, #21448, .T. ) ;
#42304=EDGE_CURVE ( 'NONE', #7925, #43873, #34035, .T. ) ;
#42305=CARTESIAN_POINT ( 'NONE',  ( 122.2696148109119889, -5.574606645277164318, -18.38911715685844683 ) ) ;
#42306=EDGE_CURVE ( 'NONE', #30977, #6072, #15717, .T. ) ;
#42307=EDGE_CURVE ( 'NONE', #28482, #43185, #7723, .T. ) ;
#42309=CARTESIAN_POINT ( 'NONE',  ( 118.4689281442453392, 0.9020085738987339008, -11.91225656197089222 ) ) ;
#42310=CARTESIAN_POINT ( 'NONE',  ( 137.1522193784430499, 0.2019376872246030630, -15.10340397907687127 ) ) ;
#42314=CARTESIAN_POINT ( 'NONE',  ( 126.9164742704674609, 0.4800028309212418520, -13.16027790502670847 ) ) ;
#42316=CARTESIAN_POINT ( 'NONE',  ( 116.2565881442452991, -9.261995988541697145, -16.69588392320189030 ) ) ;
#42317=CARTESIAN_POINT ( 'NONE',  ( 136.0617147589309752, -10.72514783119565074, -14.09777631113067287 ) ) ;
#42318=CARTESIAN_POINT ( 'NONE',  ( 114.8384214775786489, -10.15424416112533912, -14.75197769757731336 ) ) ;
#42322=CARTESIAN_POINT ( 'NONE',  ( 114.0442481442453300, -7.643976991954077427, -18.09477374809248928 ) ) ;
#42328=CARTESIAN_POINT ( 'NONE',  ( 119.2631014775786298, 0.2603800115204892296, -16.42320221600525088 ) ) ;
#42329=CARTESIAN_POINT ( 'NONE',  ( 124.9357681442453014, -7.643976991954077427, -18.09477374809248928 ) ) ;
#42330=CARTESIAN_POINT ( 'NONE',  ( 120.5678148109119832, -1.833838273342659253, -17.42832698103878286 ) ) ;
#42331=CARTESIAN_POINT ( 'NONE',  ( 113.1933481442453058, -5.574606645277164318, -18.38911715685844683 ) ) ;
#42333=CARTESIAN_POINT ( 'NONE',  ( 137.4443952029542118, -8.323847906524228790, -9.667664526382553802 ) ) ;
#42334=CARTESIAN_POINT ( 'NONE',  ( 121.1918081442452859, 0.9020085738987339008, -11.91225656197089222 ) ) ;
#42336=CARTESIAN_POINT ( 'NONE',  ( 118.9227414775786542, 0.4262465694468514643, -12.03445270309931736 ) ) ;
#42338=CARTESIAN_POINT ( 'NONE',  ( 114.5547881442453217, -4.153390946401321671, -8.397313243818183892 ) ) ;
#42342=CARTESIAN_POINT ( 'NONE',  ( 121.3052614775786111, -7.643976991954077427, -18.09477374809248928 ) ) ;
#42344=CARTESIAN_POINT ( 'NONE',  ( 124.7088614775786226, -9.565557343593413364, -10.61323700422348004 ) ) ;
#42350=CARTESIAN_POINT ( 'NONE',  ( 116.0296814775786345, -8.166667518702817929, -8.995218007635861213 ) ) ;
#42351=CARTESIAN_POINT ( 'NONE',  ( 113.8173414775786512, 0.2603800115204892296, -16.42320221600525088 ) ) ;
#42356=CARTESIAN_POINT ( 'NONE',  ( 124.3117748109119844, -10.30919188438810075, -12.61870101168855918 ) ) ;
#42357=CARTESIAN_POINT ( 'NONE',  ( 117.6180281442453150, -0.4660016031367893996, -10.09054647747474043 ) ) ;
#42358=CARTESIAN_POINT ( 'NONE',  ( 123.0637881442452937, -8.899110576539710493, -16.42337572283490132 ) ) ;
#42359=CARTESIAN_POINT ( 'NONE',  ( 123.9146881442452894, 0.9020085738987339008, -11.91225656197089222 ) ) ;
#42360=CARTESIAN_POINT ( 'NONE',  ( 121.8158014775786171, -5.638512984488999180, -18.83840828888717311 ) ) ;
#42364=CARTESIAN_POINT ( 'NONE',  ( 114.6682414775786469, -7.894159318335828068, -9.358103419637847864 ) ) ;
#42367=CARTESIAN_POINT ( 'NONE',  ( 119.8870948109119752, -9.261995988541697145, -16.69588392320189030 ) ) ;
#42369=CARTESIAN_POINT ( 'NONE',  ( 117.6747548109119919, -1.834011780172310813, -8.268836392978581529 ) ) ;
#42374=CARTESIAN_POINT ( 'NONE',  ( 113.9875214775786532, -8.899110576539710493, -16.42337572283490132 ) ) ;
#42376=CARTESIAN_POINT ( 'NONE',  ( 121.1918081442452859, -10.15424416112533912, -14.75197769757731336 ) ) ;
#42378=CARTESIAN_POINT ( 'NONE',  ( 121.9292548109119849, -7.894159318335828068, -9.358103419637847864 ) ) ;
#42380=CARTESIAN_POINT ( 'NONE',  ( 119.2063748109119814, -7.894159318335828068, -9.358103419637847864 ) ) ;
#42381=CARTESIAN_POINT ( 'NONE',  ( 114.1577014775786552, -6.344957434206662583, -7.627207830600332805 ) ) ;
#42382=CARTESIAN_POINT ( 'NONE',  ( 119.4332814775786318, -0.4660016031367893996, -10.09054647747474043 ) ) ;
#42383=CARTESIAN_POINT ( 'NONE',  ( 126.3539348109119800, -4.153390946401325223, -8.397313243818185668 ) ) ;
#42385=CARTESIAN_POINT ( 'NONE',  ( 120.0572748109119772, -6.222761293078241884, -8.102969835052219238 ) ) ;
#42387=CARTESIAN_POINT ( 'NONE',  ( 117.1642148109119859, -9.261995988541697145, -16.69588392320189030 ) ) ;
#42393=CARTESIAN_POINT ( 'NONE',  ( 122.4965214775786251, -10.30919188438810075, -12.61870101168855918 ) ) ;
#42395=CARTESIAN_POINT ( 'NONE',  ( 127.0264730702701286, -8.889494433193872780, -9.787842429323326598 ) ) ;
#42396=CARTESIAN_POINT ( 'NONE',  ( 122.6667014775786413, -2.084020599724406786, -8.691656652584148546 ) ) ;
#42400=CARTESIAN_POINT ( 'NONE',  ( 125.6164881442453094, 0.2603800115204892296, -16.42320221600525088 ) ) ;
#42403=CARTESIAN_POINT ( 'NONE',  ( 115.4624148109119943, -5.638512984488999180, -18.83840828888717311 ) ) ;
#42405=CARTESIAN_POINT ( 'NONE',  ( 124.4819548109119722, -2.084020599724406786, -8.691656652584148546 ) ) ;
#42407=CARTESIAN_POINT ( 'NONE',  ( 122.1561614775786353, -8.899110576539710493, -16.42337572283490132 ) ) ;
#42408=CARTESIAN_POINT ( 'NONE',  ( 126.2758031835872430, -3.873803345569537093, -8.462975944311656562 ) ) ;
#42410=CARTESIAN_POINT ( 'NONE',  ( 121.7590748109119687, -7.893985811506177619, -18.51759400769804742 ) ) ;
#42411=CARTESIAN_POINT ( 'NONE',  ( 111.4348214775786801, -3.505236298600246325, -18.68346056562440793 ) ) ;
#42415=ORIENTED_EDGE ( 'NONE', *, *, #17484, .T. ) ;
#42417=CARTESIAN_POINT ( 'NONE',  ( 122.0994348109119443, 0.9020085738987339008, -11.91225656197089222 ) ) ;
#42418=CARTESIAN_POINT ( 'NONE',  ( 137.3019930433569016, -8.520726449178049222, -17.11237870612375644 ) ) ;
#42423=CARTESIAN_POINT ( 'NONE',  ( 112.4559014775786778, -0.1624402480850797581, -16.17319339645315424 ) ) ;
#42425=CARTESIAN_POINT ( 'NONE',  ( 122.4965214775786251, 0.1319031606808879209, -14.10382304977623669 ) ) ;
#42428=CARTESIAN_POINT ( 'NONE',  ( 112.8529881442453302, -1.561330072975668060, -17.79121239304076596 ) ) ;
#42429=DIRECTION ( 'NONE',  ( 0.000000000000000000, -0.6004852223388320587, 0.7996358532186281787 ) ) ;
#42431=CARTESIAN_POINT ( 'NONE',  ( 138.2184548109119930, -7.067465109756605912, -7.812468278694988832 ) ) ;
#42432=CARTESIAN_POINT ( 'NONE',  ( 124.1983214775786166, -8.166667518702819706, -8.995218007635861213 ) ) ;
#42435=CARTESIAN_POINT ( 'NONE',  ( 124.5386814775786206, -5.638512984488999180, -18.83840828888717311 ) ) ;
#42436=CARTESIAN_POINT ( 'NONE',  ( 123.8012348109119642, 0.2603800115204892296, -16.42320221600525088 ) ) ;
#42437=CARTESIAN_POINT ( 'NONE',  ( 124.5386814775786206, -4.153390946401325223, -8.397313243818185668 ) ) ;
#42438=CARTESIAN_POINT ( 'NONE',  ( 123.2339681442453241, -3.505236298600246325, -18.68346056562440793 ) ) ;
#42440=CARTESIAN_POINT ( 'NONE',  ( 120.5110881442453206, -6.344957434206665248, -7.627207830600338134 ) ) ;
#42447=CARTESIAN_POINT ( 'NONE',  ( 125.8433948109119456, -1.834011780172310813, -8.268836392978581529 ) ) ;
#42448=CARTESIAN_POINT ( 'NONE',  ( 126.0135748109119902, -1.833838273342660141, -17.42832698103878286 ) ) ;
#42450=CARTESIAN_POINT ( 'NONE',  ( 112.8529881442453160, -7.894159318335828068, -9.358103419637847864 ) ) ;
#42452=CARTESIAN_POINT ( 'NONE',  ( 118.9227414775786542, 0.4262465694468589028, -12.03445270309934578 ) ) ;
#42453=CARTESIAN_POINT ( 'NONE',  ( 125.9001214775786224, -4.089484607189486809, -7.948022111789456723 ) ) ;
#42454=CARTESIAN_POINT ( 'NONE',  ( 126.1270281442452870, -10.30919188438810075, -12.61870101168855918 ) ) ;
#42456=CARTESIAN_POINT ( 'NONE',  ( 114.7816948109119863, 0.5811942927096154232, -14.16772938898807155 ) ) ;
#42462=CARTESIAN_POINT ( 'NONE',  ( 113.6471614775786492, -4.153390946401321671, -8.397313243818183892 ) ) ;
#42464=CARTESIAN_POINT ( 'NONE',  ( 125.8433948109119456, -7.643976991954077427, -18.09477374809248928 ) ) ;
#42465=CARTESIAN_POINT ( 'NONE',  ( 113.3635281442453504, -9.988377603198976828, -10.36322818467138340 ) ) ;
#42466=CARTESIAN_POINT ( 'NONE',  ( 124.6521348109119884, -7.894159318335828068, -9.358103419637847864 ) ) ;
#42468=CARTESIAN_POINT ( 'NONE',  ( 119.5467348109119712, -5.574606645277164318, -18.38911715685844683 ) ) ;
#42469=CARTESIAN_POINT ( 'NONE',  ( 114.6115148109119986, -6.222761293078241884, -8.102969835052219238 ) ) ;
#42475=CARTESIAN_POINT ( 'NONE',  ( 116.7671281442453335, -7.643976991954077427, -18.09477374809248928 ) ) ;
#42477=CARTESIAN_POINT ( 'NONE',  ( 126.2184548109092930, -8.879494022685642918, -16.37258252134538949 ) ) ;
#42478=CARTESIAN_POINT ( 'NONE',  ( 112.4559014775786494, -9.988377603198976828, -10.36322818467138340 ) ) ;
#42480=CARTESIAN_POINT ( 'NONE',  ( 118.9907502882355033, -1.135392229370316031, -17.10942237759952533 ) ) ;
#42483=CARTESIAN_POINT ( 'NONE',  ( 117.8449348109119938, -1.833838273342659253, -17.42832698103878286 ) ) ;
#42484=CARTESIAN_POINT ( 'NONE',  ( 118.8092881442453290, -0.1624402480850797581, -16.17319339645315424 ) ) ;
#42489=CARTESIAN_POINT ( 'NONE',  ( 121.0408330757767459, -0.9924539043446216624, -17.29976612834909133 ) ) ;
#42494=CARTESIAN_POINT ( 'NONE',  ( 112.6260814775786514, -9.261995988541697145, -16.69588392320189030 ) ) ;
#42495=CARTESIAN_POINT ( 'NONE',  ( 113.4202548109119846, -10.30919188438810075, -12.61870101168855918 ) ) ;
#42496=CARTESIAN_POINT ( 'NONE',  ( 118.2420214775786320, -6.222761293078241884, -8.102969835052219238 ) ) ;
#42498=ORIENTED_EDGE ( 'NONE', *, *, #45007, .F. ) ;
#42499=CARTESIAN_POINT ( 'NONE',  ( 116.1998614775786507, 0.4262465694468514643, -12.03445270309931736 ) ) ;
#42504=CARTESIAN_POINT ( 'NONE',  ( 115.8027748109119841, -0.4660016031367893996, -10.09054647747474043 ) ) ;
#42506=CARTESIAN_POINT ( 'NONE',  ( 118.0718414775786300, -9.261995988541697145, -16.69588392320189030 ) ) ;
#42507=CARTESIAN_POINT ( 'NONE',  ( 114.6490365460471992, -2.191907684172563986, -18.20049396185734025 ) ) ;
#42509=CARTESIAN_POINT ( 'NONE',  ( 117.9016614775786280, -9.988377603198976828, -10.36322818467138340 ) ) ;
#42510=CARTESIAN_POINT ( 'NONE',  ( 113.9307948109119906, 0.9020085738987339008, -11.91225656197089222 ) ) ;
#42517=CARTESIAN_POINT ( 'NONE',  ( 116.3133148109120043, -2.084020599724406786, -8.691656652584148546 ) ) ;
#42521=CARTESIAN_POINT ( 'NONE',  ( 121.8701654349294472, -1.040089454026960292, -17.23633227186633476 ) ) ;
#42522=CARTESIAN_POINT ( 'NONE',  ( 113.1366214775786432, -7.643976991954077427, -18.09477374809248928 ) ) ;
#42523=CARTESIAN_POINT ( 'NONE',  ( 135.5177942504587350, 1.083030826940885927, -12.63729283143848825 ) ) ;
#42524=CARTESIAN_POINT ( 'NONE',  ( 123.0070614775786169, 0.9020085738987339008, -11.91225656197089222 ) ) ;
#42525=CARTESIAN_POINT ( 'NONE',  ( 121.4754414775786131, -8.166667518702819706, -8.995218007635861213 ) ) ;
#42527=CLOSED_SHELL ( 'NONE', ( #31227, #31743, #21375, #8459, #40461, #26448, #13332, #23164, #23158, #15571, #27816, #26190, #15828, #4660, #43546, #33947, #20566, #4192, #1908, #23356, #33113, #34559, #40967, #41994, #8011, #30163, #40649, #26191, #10038, #11113, #27656, #34816, #7000, #35429, #10271, #44112, #10518, #3334, #26507, #8872, #11176, #16010, #25054, #33728, #27314, #26437, #38367, #22589, #28969, #40381, #23218, #38974, #3027, #20191, #28459, #9447, #15551, #2740, #19151, #41190, #23749, #21394, #18348, #42923, #12620, #21434, #17858, #14823, #3303, #6350, #10602, #27013, #19818, #40050, #19355, #25932, #9457, #3563, #24799, #25023 ) ) ;
#42528=CARTESIAN_POINT ( 'NONE',  ( 116.7671281442453335, -7.643976991954077427, -18.09477374809248928 ) ) ;
#42529=CARTESIAN_POINT ( 'NONE',  ( 112.7962614775786676, -3.383040157471821630, -19.15922257007629170 ) ) ;
#42530=CARTESIAN_POINT ( 'NONE',  ( 118.1285681442453068, -7.893985811506177619, -18.51759400769804742 ) ) ;
#42531=CARTESIAN_POINT ( 'NONE',  ( 120.3409081442453044, -8.899110576539710493, -16.42337572283490132 ) ) ;
#42533=CARTESIAN_POINT ( 'NONE',  ( 120.0005481442453146, -4.153390946401325223, -8.397313243818185668 ) ) ;
#42534=CARTESIAN_POINT ( 'NONE',  ( 121.2485348109119769, -0.4660016031367893996, -10.09054647747474043 ) ) ;
#42535=CARTESIAN_POINT ( 'NONE',  ( 136.9555737971644760, 0.6158828431329258501, -13.00173388423986864 ) ) ;
#42538=CARTESIAN_POINT ( 'NONE',  ( 127.3815943569765210, 0.6976231769725066423, -12.91654422016494053 ) ) ;
#42540=CARTESIAN_POINT ( 'NONE',  ( 115.5758681442453053, -1.561330072975668060, -17.79121239304076951 ) ) ;
#42541=CARTESIAN_POINT ( 'NONE',  ( 137.1399781294006175, -10.21614541919964658, -13.63713482494530638 ) ) ;
#42542=CARTESIAN_POINT ( 'NONE',  ( 116.0296814775786345, -1.833838273342658809, -17.42832698103878286 ) ) ;
#42546=CARTESIAN_POINT ( 'NONE',  ( 112.5126281442453120, 0.1319031606808879209, -14.10382304977623669 ) ) ;
#42550=CARTESIAN_POINT ( 'NONE',  ( 119.0929214775786278, -5.638512984488999180, -18.83840828888717311 ) ) ;
#42551=CARTESIAN_POINT ( 'NONE',  ( 119.6601881442453106, -1.833838273342659253, -17.42832698103878286 ) ) ;
#42552=CARTESIAN_POINT ( 'NONE',  ( 111.3213681442453264, -7.643976991954077427, -18.09477374809248928 ) ) ;
#42554=CARTESIAN_POINT ( 'NONE',  ( 136.7036351578981055, -7.108649276388896432, -8.207337658509201717 ) ) ;
#42555=CARTESIAN_POINT ( 'NONE',  ( 121.8725281442453223, -3.383040157471821630, -19.15922257007629170 ) ) ;
#42557=CARTESIAN_POINT ( 'NONE',  ( 120.1140014775786398, -7.894159318335828068, -9.358103419637847864 ) ) ;
#42558=EDGE_CURVE ( 'NONE', #37411, #32004, #11350, .T. ) ;
#42559=CARTESIAN_POINT ( 'NONE',  ( 115.0653281442453277, -3.505236298600246325, -18.68346056562440793 ) ) ;
#42562=CARTESIAN_POINT ( 'NONE',  ( 120.6245414775786458, -0.1624402480850797581, -16.17319339645315424 ) ) ;
#42563=CARTESIAN_POINT ( 'NONE',  ( 125.3895814775786448, -2.084020599724406786, -8.691656652584148546 ) ) ;
#42569=CARTESIAN_POINT ( 'NONE',  ( 118.9794681442453026, -9.261995988541697145, -16.69588392320189030 ) ) ;
#42570=CARTESIAN_POINT ( 'NONE',  ( 118.0151148109119816, -10.63000616557722466, -14.87417383870573495 ) ) ;
#42572=CARTESIAN_POINT ( 'NONE',  ( 114.4413348109119823, -9.261995988541697145, -16.69588392320189030 ) ) ;
#42574=CARTESIAN_POINT ( 'NONE',  ( 123.2184548109119788, -4.863998795839242995, -13.39321520033831447 ) ) ;
#42577=CARTESIAN_POINT ( 'NONE',  ( 116.9940348109119839, -9.988377603198976828, -10.36322818467138340 ) ) ;
#42578=CARTESIAN_POINT ( 'NONE',  ( 122.1561614775786353, -8.899110576539710493, -16.42337572283490132 ) ) ;
#42579=CARTESIAN_POINT ( 'NONE',  ( 112.0588148109119828, -9.859900752359374465, -12.68260735090039404 ) ) ;
#42580=CARTESIAN_POINT ( 'NONE',  ( 122.8936081442453059, 0.2603800115204892296, -16.42320221600525088 ) ) ;
#42584=CARTESIAN_POINT ( 'NONE',  ( 115.4624148109119943, -4.153390946401321671, -8.397313243818183892 ) ) ;
#42591=CARTESIAN_POINT ( 'NONE',  ( 118.9794681442453026, -9.261995988541697145, -16.69588392320189030 ) ) ;
#42596=CARTESIAN_POINT ( 'NONE',  ( 116.3133148109120043, -2.084020599724406786, -8.691656652584148546 ) ) ;
#42599=CARTESIAN_POINT ( 'NONE',  ( 119.0361948109119652, -2.084020599724406786, -8.691656652584148546 ) ) ;
#42602=CARTESIAN_POINT ( 'NONE',  ( 122.0994348109119443, -10.15424416112533912, -14.75197769757731336 ) ) ;
#42603=CARTESIAN_POINT ( 'NONE',  ( 121.9484597424434043, -0.9924539043446216624, -17.29976612834909133 ) ) ;
#42604=CARTESIAN_POINT ( 'NONE',  ( 120.0005481442453146, -4.153390946401325223, -8.397313243818185668 ) ) ;
#42606=CARTESIAN_POINT ( 'NONE',  ( 113.5337081442453240, -9.261995988541697145, -16.69588392320189030 ) ) ;
#42607=CARTESIAN_POINT ( 'NONE',  ( 118.5256548109119876, -0.4660016031367893996, -10.09054647747474043 ) ) ;
#42608=CARTESIAN_POINT ( 'NONE',  ( 112.3991748109119868, -8.166667518702817929, -8.995218007635859436 ) ) ;
#42612=CARTESIAN_POINT ( 'NONE',  ( 121.3052614775786111, -7.643976991954077427, -18.09477374809248928 ) ) ;
#42614=CARTESIAN_POINT ( 'NONE',  ( 119.8870948109119752, -9.261995988541697145, -16.69588392320189030 ) ) ;
#42619=CARTESIAN_POINT ( 'NONE',  ( 125.1059481442452750, -8.166667518702819706, -8.995218007635861213 ) ) ;
#42622=CARTESIAN_POINT ( 'NONE',  ( 120.5110881442453206, -3.505236298600246325, -18.68346056562440793 ) ) ;
#42625=CARTESIAN_POINT ( 'NONE',  ( 111.6155414775786596, 0.3778260857407392814, -12.04688916545883970 ) ) ;
#42627=VERTEX_POINT ( 'NONE', #22596 ) ;
#42628=CARTESIAN_POINT ( 'NONE',  ( 115.1220548109119761, -8.166667518702817929, -8.995218007635861213 ) ) ;
#42629=CARTESIAN_POINT ( 'NONE',  ( 113.8740681442453138, 0.5811942927096154232, -14.16772938898807155 ) ) ;
#42631=CARTESIAN_POINT ( 'NONE',  ( 118.9227414775786542, 0.4262465694468514643, -12.03445270309931736 ) ) ;
#42632=CARTESIAN_POINT ( 'NONE',  ( 126.7702028005446238, -3.262292498975457367, -8.366245766736872369 ) ) ;
#42633=CARTESIAN_POINT ( 'NONE',  ( 124.3117748109119844, -10.30919188438810075, -12.61870101168855918 ) ) ;
#42639=CARTESIAN_POINT ( 'NONE',  ( 121.7023481442452777, -9.261995988541697145, -16.69588392320189030 ) ) ;
#42643=CARTESIAN_POINT ( 'NONE',  ( 112.5693548109119888, 0.4262465694468514643, -12.03445270309931736 ) ) ;
#42645=CARTESIAN_POINT ( 'NONE',  ( 127.3669547543380958, -4.396327407923800834, -18.94794887702561681 ) ) ;
#42646=CARTESIAN_POINT ( 'NONE',  ( 122.4397948109119767, -0.1624402480850797581, -16.17319339645315424 ) ) ;
#42648=CARTESIAN_POINT ( 'NONE',  ( 116.4834948109119779, -1.561330072975668504, -17.79121239304076951 ) ) ;
#42652=CARTESIAN_POINT ( 'NONE',  ( 125.0492214775786266, -6.344957434206665248, -7.627207830600338134 ) ) ;
#42656=CARTESIAN_POINT ( 'NONE',  ( 122.4965214775786251, -10.30919188438810075, -12.61870101168855918 ) ) ;
#42657=CARTESIAN_POINT ( 'NONE',  ( 122.4397948109119767, -9.988377603198976828, -10.36322818467138340 ) ) ;
#42658=CARTESIAN_POINT ( 'NONE',  ( 123.5743281442453139, -2.084020599724406786, -8.691656652584148546 ) ) ;
#42660=CARTESIAN_POINT ( 'NONE',  ( 125.0492214775786266, -3.505236298600246325, -18.68346056562440793 ) ) ;
#42661=CARTESIAN_POINT ( 'NONE',  ( 113.4202548109119846, 0.1319031606808879209, -14.10382304977623669 ) ) ;
#42662=CARTESIAN_POINT ( 'NONE',  ( 121.4754414775786131, -8.166667518702819706, -8.995218007635861213 ) ) ;
#42666=CARTESIAN_POINT ( 'NONE',  ( 117.7480986403692214, -1.196538596002806099, -17.02799684832026372 ) ) ;
#42670=CARTESIAN_POINT ( 'NONE',  ( 124.9357681442453156, -7.643976991953167044, -18.09477374809303285 ) ) ;
#42671=CARTESIAN_POINT ( 'NONE',  ( 116.9940348109119839, -9.988377603198976828, -10.36322818467138340 ) ) ;
#42673=CARTESIAN_POINT ( 'NONE',  ( 111.6050014775786536, 0.1319031606808879209, -14.10382304977623669 ) ) ;
#42675=CARTESIAN_POINT ( 'NONE',  ( 119.0929214775786278, -4.153390946401311012, -8.397313243818187445 ) ) ;
#42678=CARTESIAN_POINT ( 'NONE',  ( 123.0637881442452937, -8.899110576539703388, -16.42337572283491198 ) ) ;
#42681=CARTESIAN_POINT ( 'NONE',  ( 116.4267681442453153, -3.383040157471821630, -19.15922257007629170 ) ) ;
#42686=CARTESIAN_POINT ( 'NONE',  ( 119.5467348109119712, -5.574606645277164318, -18.38911715685844683 ) ) ;
#42687=CARTESIAN_POINT ( 'NONE',  ( 115.4624148109119943, -5.638512984488999180, -18.83840828888717311 ) ) ;
#42689=CARTESIAN_POINT ( 'NONE',  ( 112.6828081442453282, -7.893985811506177619, -18.51759400769804742 ) ) ;
#42690=CARTESIAN_POINT ( 'NONE',  ( 124.2550481442452792, -0.1624402480850797581, -16.17319339645315424 ) ) ;
#42691=CARTESIAN_POINT ( 'NONE',  ( 119.6601881442453106, -1.833838273342659253, -17.42832698103878286 ) ) ;
#42692=CARTESIAN_POINT ( 'NONE',  ( 114.4413348109119823, -0.8288870151387760510, -10.36305467784173118 ) ) ;
#42697=CARTESIAN_POINT ( 'NONE',  ( 119.2631014775786298, -9.565557343593413364, -10.61323700422348004 ) ) ;
#42698=VERTEX_POINT ( 'NONE', #29217 ) ;
#42700=CARTESIAN_POINT ( 'NONE',  ( 115.6893214775786447, 0.5811942927096154232, -14.16772938898807155 ) ) ;
#42702=CARTESIAN_POINT ( 'NONE',  ( 125.5597614775786326, -7.894159318335828068, -9.358103419637847864 ) ) ;
#42706=CARTESIAN_POINT ( 'NONE',  ( 121.8725281442453223, -6.222761293078241884, -8.102969835052219238 ) ) ;
#42707=CARTESIAN_POINT ( 'NONE',  ( 116.1998614775786507, 0.4262465694468514643, -12.03445270309931736 ) ) ;
#42716=CARTESIAN_POINT ( 'NONE',  ( 112.3424481442453384, -6.344957434206662583, -7.627207830600332805 ) ) ;
#42718=CARTESIAN_POINT ( 'NONE',  ( 125.3895814775786448, -2.084020599724406786, -8.691656652584148546 ) ) ;
#42719=CARTESIAN_POINT ( 'NONE',  ( 119.6034614775786196, -3.505236298600246325, -18.68346056562440793 ) ) ;
#42722=CARTESIAN_POINT ( 'NONE',  ( 118.1852948109119836, -4.153390946401325223, -8.397313243818185668 ) ) ;
#42728=CARTESIAN_POINT ( 'NONE',  ( 116.7104014775786425, -0.4660016031367893996, -10.09054647747474043 ) ) ;
#42730=CARTESIAN_POINT ( 'NONE',  ( 115.6325948109119821, 0.2603800115204892296, -16.42320221600525088 ) ) ;
#42731=CARTESIAN_POINT ( 'NONE',  ( 114.3278814775786429, -10.30919188438809542, -12.61870101168854852 ) ) ;
#42733=CARTESIAN_POINT ( 'NONE',  ( 115.0086014775786509, -4.089484607189486809, -7.948022111789456723 ) ) ;
#42734=CARTESIAN_POINT ( 'NONE',  ( 118.1285681442453068, -7.893985811506177619, -18.51759400769804742 ) ) ;
#42735=CARTESIAN_POINT ( 'NONE',  ( 126.6211808763573998, -10.06551012219619778, -13.41462627083012293 ) ) ;
#42736=CARTESIAN_POINT ( 'NONE',  ( 138.2184548109119930, -10.36826876090623450, -11.00511718064541178 ) ) ;
#42742=CARTESIAN_POINT ( 'NONE',  ( 120.2274548109119934, -9.859900752359374465, -12.68260735090039404 ) ) ;
#42746=CARTESIAN_POINT ( 'NONE',  ( 126.3115243456352488, -4.515721963253167104, -8.358698628921043650 ) ) ;
#42747=CARTESIAN_POINT ( 'NONE',  ( 114.1009748109119784, -5.574606645277164318, -18.38911715685844683 ) ) ;
#42749=CARTESIAN_POINT ( 'NONE',  ( 124.2550481442452792, -9.988377603198980381, -10.36322818467138518 ) ) ;
#42750=B_SPLINE_CURVE_WITH_KNOTS ( 'NONE', 3,
 ( #38262, #21170, #24159, #415, #13889, #2945, #14332, #27580, #7255, #3610 ),
 .UNSPECIFIED., .F., .F.,
 ( 4, 3, 3, 4 ),
 ( 0.000000000000000000, 0.0001671877560958130043, 0.0003343755126086585196, 0.0006438490228507220145 ),
 .UNSPECIFIED. ) ;
#42751=CARTESIAN_POINT ( 'NONE',  ( 120.5678148109119832, -8.166667518702819706, -8.995218007635861213 ) ) ;
#42754=CARTESIAN_POINT ( 'NONE',  ( 118.0151148109119816, 0.4262465694468514643, -12.03445270309931736 ) ) ;
#42755=CARTESIAN_POINT ( 'NONE',  ( 112.1155414775786454, 0.9020085738987339008, -11.91225656197089222 ) ) ;
#42756=CARTESIAN_POINT ( 'NONE',  ( 119.3198281442452924, 0.5811942927096110934, -14.16772938898807510 ) ) ;
#42757=CARTESIAN_POINT ( 'NONE',  ( 120.9649014775786355, -6.222761293078241884, -8.102969835052219238 ) ) ;
#42759=CARTESIAN_POINT ( 'NONE',  ( 124.8790414775786246, -8.899110576539710493, -16.42337572283490132 ) ) ;
#42760=CARTESIAN_POINT ( 'NONE',  ( 119.5467348109119712, -4.089484607189486809, -7.948022111789456723 ) ) ;
#42761=CARTESIAN_POINT ( 'NONE',  ( 137.3173478096594806, 0.3375151974989685777, -13.37218143070558263 ) ) ;
#42768=CARTESIAN_POINT ( 'NONE',  ( 118.2987481442453088, -1.561330072975668504, -17.79121239304076951 ) ) ;
#42769=CARTESIAN_POINT ( 'NONE',  ( 136.2315975805985317, -10.25943272008531792, -11.12509562936944896 ) ) ;
#42770=CARTESIAN_POINT ( 'NONE',  ( 117.0507614775786465, 0.1319031606808879209, -14.10382304977623669 ) ) ;
#42771=CARTESIAN_POINT ( 'NONE',  ( 126.2597653975769134, -0.7068999842200600625, -10.57775600701587493 ) ) ;
#42772=CARTESIAN_POINT ( 'NONE',  ( 117.6747548109119776, -7.643976991954101408, -18.09477374809246797 ) ) ;
#42775=CARTESIAN_POINT ( 'NONE',  ( 115.2922348109119781, -10.63000616557721756, -14.87417383870574206 ) ) ;
#42777=CARTESIAN_POINT ( 'NONE',  ( 123.8370331944929035, -1.036737761566197014, -17.24079555149560861 ) ) ;
#42779=CARTESIAN_POINT ( 'NONE',  ( 118.3554748109119998, 0.2603800115204892296, -16.42320221600525088 ) ) ;
#42780=EDGE_CURVE ( 'NONE', #37342, #39008, #19864, .T. ) ;
#42781=CARTESIAN_POINT ( 'NONE',  ( 118.5256548109119876, -8.899110576539710493, -16.42337572283490132 ) ) ;
#42782=CARTESIAN_POINT ( 'NONE',  ( 113.8173414775786512, -9.565557343593413364, -10.61323700422348004 ) ) ;
#42785=CARTESIAN_POINT ( 'NONE',  ( 123.8579614775786126, 0.5811942927096110934, -14.16772938898807510 ) ) ;
#42787=CARTESIAN_POINT ( 'NONE',  ( 119.2631014775786298, -9.565557343593413364, -10.61323700422348004 ) ) ;
#42788=CARTESIAN_POINT ( 'NONE',  ( 116.7104014775786425, -8.899110576539710493, -16.42337572283490132 ) ) ;
#42791=CARTESIAN_POINT ( 'NONE',  ( 122.6099748109119929, -0.8288870151387760510, -10.36305467784173118 ) ) ;
#42792=CARTESIAN_POINT ( 'NONE',  ( 122.7234281442452755, -4.153390946401325223, -8.397313243818185668 ) ) ;
#42793=DIRECTION ( 'NONE',  ( 0.000000000000000000, 0.6004852223388321697, -0.7996358532186279566 ) ) ;
#42800=CARTESIAN_POINT ( 'NONE',  ( 116.9940348109119839, -9.988377603198976828, -10.36322818467138340 ) ) ;
#42801=CARTESIAN_POINT ( 'NONE',  ( 120.1140014775786398, -1.561330072975668504, -17.79121239304076951 ) ) ;
#42804=ORIENTED_EDGE ( 'NONE', *, *, #31525, .T. ) ;
#42805=CARTESIAN_POINT ( 'NONE',  ( 117.0306702067644409, -1.223627541775731631, -16.99192386690444323 ) ) ;
#42806=CARTESIAN_POINT ( 'NONE',  ( 117.7314814775786260, -4.089484607189486809, -7.948022111789456723 ) ) ;
#42807=CARTESIAN_POINT ( 'NONE',  ( 123.7445081442452874, -7.894159318335828068, -9.358103419637847864 ) ) ;
#42809=CARTESIAN_POINT ( 'NONE',  ( 125.1626748109119802, -9.988377603198980381, -10.36322818467138518 ) ) ;
#42810=CARTESIAN_POINT ( 'NONE',  ( 121.4754414775786131, -8.166667518702819706, -8.995218007635861213 ) ) ;
#42812=CARTESIAN_POINT ( 'NONE',  ( 115.4056881442453459, -2.084020599724406786, -8.691656652584148546 ) ) ;
#42817=CARTESIAN_POINT ( 'NONE',  ( 120.9649014775786355, -3.383040157471821630, -19.15922257007629170 ) ) ;
#42823=CARTESIAN_POINT ( 'NONE',  ( 116.8805814775786445, -3.505236298600246325, -18.68346056562440793 ) ) ;
#42826=CARTESIAN_POINT ( 'NONE',  ( 123.8579614775786126, -9.859900752359378018, -12.68260735090039759 ) ) ;
#42828=CARTESIAN_POINT ( 'NONE',  ( 123.2339681442453241, -3.505236298600246325, -18.68346056562440793 ) ) ;
#42830=CARTESIAN_POINT ( 'NONE',  ( 121.8158014775786171, -4.153390946401325223, -8.397313243818185668 ) ) ;
#42831=CARTESIAN_POINT ( 'NONE',  ( 112.9664414775786412, 0.5811942927096154232, -14.16772938898807155 ) ) ;
#42832=CARTESIAN_POINT ( 'NONE',  ( 119.1496481442453046, -3.383040157471821630, -19.15922257007629170 ) ) ;
#42833=CARTESIAN_POINT ( 'NONE',  ( 112.0020881442453344, 0.2603800115204892296, -16.42320221600525088 ) ) ;
#42835=CARTESIAN_POINT ( 'NONE',  ( 121.5888948109119809, 0.1319031606808879209, -14.10382304977623669 ) ) ;
#42837=CARTESIAN_POINT ( 'NONE',  ( 121.9292548109119849, -1.561330072975668948, -17.79121239304076951 ) ) ;
#42841=CARTESIAN_POINT ( 'NONE',  ( 114.5547881442453217, -4.153390946401321671, -8.397313243818183892 ) ) ;
#42846=CARTESIAN_POINT ( 'NONE',  ( 122.9503348109119827, -9.859900752359378018, -12.68260735090039759 ) ) ;
#42852=ORIENTED_EDGE ( 'NONE', *, *, #27906, .T. ) ;
#42853=CARTESIAN_POINT ( 'NONE',  ( 114.1577014775786552, -6.344957434206662583, -7.627207830600332805 ) ) ;
#42855=CARTESIAN_POINT ( 'NONE',  ( 120.9649014775786355, -6.222761293078241884, -8.102969835052219238 ) ) ;
#42856=CARTESIAN_POINT ( 'NONE',  ( 112.6260814775786514, -0.8288870151387760510, -10.36305467784173118 ) ) ;
#42859=LINE ( 'NONE', #32357, #13557 ) ;
#42863=CARTESIAN_POINT ( 'NONE',  ( 119.0361948109119652, -7.893985811506177619, -18.51759400769804742 ) ) ;
#42870=CARTESIAN_POINT ( 'NONE',  ( 112.0588148109119828, -9.859900752359374465, -12.68260735090039404 ) ) ;
#42872=CARTESIAN_POINT ( 'NONE',  ( 122.7801548109119665, -6.222761293078241884, -8.102969835052219238 ) ) ;
#42874=CARTESIAN_POINT ( 'NONE',  ( 118.5823814775786360, -1.834011780172310813, -8.268836392978581529 ) ) ;
#42876=CARTESIAN_POINT ( 'NONE',  ( 120.1332064091100733, -0.9924539043446216624, -17.29976612834909133 ) ) ;
#42878=CARTESIAN_POINT ( 'NONE',  ( 112.2857214775786474, -5.574606645277164318, -18.38911715685844683 ) ) ;
#42882=CARTESIAN_POINT ( 'NONE',  ( 125.9568481442452850, -6.344957434206665248, -7.627207830600338134 ) ) ;
#42883=CARTESIAN_POINT ( 'NONE',  ( 126.2972081442452890, -2.084020599724406786, -8.691656652584148546 ) ) ;
#42885=CARTESIAN_POINT ( 'NONE',  ( 124.9357681442453014, -7.643976991954077427, -18.09477374809248928 ) ) ;
#42887=CARTESIAN_POINT ( 'NONE',  ( 118.6391081442452986, -4.089484607189486809, -7.948022111789456723 ) ) ;
#42889=CARTESIAN_POINT ( 'NONE',  ( 126.2184548109092361, -8.793414587017092998, -16.48721015983629457 ) ) ;
#42891=EDGE_CURVE ( 'NONE', #12393, #35460, #18400, .T. ) ;
#42894=CARTESIAN_POINT ( 'NONE',  ( 125.5030348109119842, -6.222761293079280165, -8.102969835052485692 ) ) ;
#42895=CARTESIAN_POINT ( 'NONE',  ( 113.9875214775786532, -0.4660016031367893996, -10.09054647747474043 ) ) ;
#42897=CARTESIAN_POINT ( 'NONE',  ( 111.6617281442453304, 0.4262465694468514643, -12.03445270309931736 ) ) ;
#42900=CARTESIAN_POINT ( 'NONE',  ( 126.1270281442452870, -10.30919188438810075, -12.61870101168855918 ) ) ;
#42903=CARTESIAN_POINT ( 'NONE',  ( 115.7460481442453357, 0.9020085738987339008, -11.91225656197089222 ) ) ;
#42908=CARTESIAN_POINT ( 'NONE',  ( 126.2872529661375438, -7.630682474280415128, -9.187169839767605595 ) ) ;
#42909=CARTESIAN_POINT ( 'NONE',  ( 120.7379948109119709, 0.4262465694468514643, -12.03445270309931736 ) ) ;
#42910=CARTESIAN_POINT ( 'NONE',  ( 116.9373081442452929, -8.166667518702817929, -8.995218007635861213 ) ) ;
#42911=CARTESIAN_POINT ( 'NONE',  ( 112.0588148109119828, 0.5811942927096154232, -14.16772938898807155 ) ) ;
#42912=CARTESIAN_POINT ( 'NONE',  ( 124.3117748109119844, 0.1319031606808879209, -14.10382304977623669 ) ) ;
#42914=CARTESIAN_POINT ( 'NONE',  ( 124.7655881442452852, -9.859900752359378018, -12.68260735090039759 ) ) ;
#42915=CARTESIAN_POINT ( 'NONE',  ( 114.1577014775786552, -3.505236298600246325, -18.68346056562440793 ) ) ;
#42919=CARTESIAN_POINT ( 'NONE',  ( 118.2420214775786320, -6.222761293078241884, -8.102969835052219238 ) ) ;
#42922=DIRECTION ( 'NONE',  ( 1.000000000000000000, 0.000000000000000000, 0.000000000000000000 ) ) ;
#42923=ADVANCED_FACE ( 'NONE', ( #2746 ), #16943, .T. ) ;
#42924=CARTESIAN_POINT ( 'NONE',  ( 116.4834948109119779, -1.561330072975668504, -17.79121239304076951 ) ) ;
#42929=CARTESIAN_POINT ( 'NONE',  ( 120.9081748109119872, -4.153390946401325223, -8.397313243818185668 ) ) ;
#42930=CARTESIAN_POINT ( 'NONE',  ( 117.7314814775786260, -5.574606645277164318, -18.38911715685844683 ) ) ;
#42931=EDGE_CURVE ( 'NONE', #33919, #20193, #12983, .T. ) ;
#42934=ORIENTED_EDGE ( 'NONE', *, *, #34011, .T. ) ;
#42938=CARTESIAN_POINT ( 'NONE',  ( 116.7671281442453335, -1.834011780172310813, -8.268836392978581529 ) ) ;
#42939=CARTESIAN_POINT ( 'NONE',  ( 112.2857214775786474, -4.089484607189486809, -7.948022111789456723 ) ) ;
#42940=CARTESIAN_POINT ( 'NONE',  ( 122.2696148109119889, -5.574606645277164318, -18.38911715685844683 ) ) ;
#42942=ORIENTED_EDGE ( 'NONE', *, *, #31338, .F. ) ;
#42943=CARTESIAN_POINT ( 'NONE',  ( 119.7736414775786358, 0.1319031606808879209, -14.10382304977623669 ) ) ;
#42946=CARTESIAN_POINT ( 'NONE',  ( 118.2420214775786320, -3.383040157471821630, -19.15922257007629170 ) ) ;
#42948=CARTESIAN_POINT ( 'NONE',  ( 116.4834948109119779, -1.561330072975668504, -17.79121239304076951 ) ) ;
#42951=CARTESIAN_POINT ( 'NONE',  ( 115.0653281442453277, -6.344957434206662583, -7.627207830600332805 ) ) ;
#42952=CARTESIAN_POINT ( 'NONE',  ( 118.2420214775786320, -3.383040157471821630, -19.15922257007629170 ) ) ;
#42958=CARTESIAN_POINT ( 'NONE',  ( 121.6456214775786293, 0.4262465694468514643, -12.03445270309931736 ) ) ;
#42962=CARTESIAN_POINT ( 'NONE',  ( 115.5191414775786569, -6.222761293078241884, -8.102969835052219238 ) ) ;
#42964=CARTESIAN_POINT ( 'NONE',  ( 124.5954081442453116, -3.383040157471821630, -19.15922257007629170 ) ) ;
#42965=CARTESIAN_POINT ( 'NONE',  ( 121.3619881442452879, -4.089484607189486809, -7.948022111789456723 ) ) ;
#42968=CARTESIAN_POINT ( 'NONE',  ( 117.7314814775786260, -5.574606645277164318, -18.38911715685844683 ) ) ;
#42970=CARTESIAN_POINT ( 'NONE',  ( 120.0005481442453146, -5.638512984488999180, -18.83840828888717311 ) ) ;
#42971=CARTESIAN_POINT ( 'NONE',  ( 119.7736414775786358, 0.1319031606808879209, -14.10382304977623669 ) ) ;
#42974=CARTESIAN_POINT ( 'NONE',  ( 119.2063748109119814, -1.561330072975668504, -17.79121239304076951 ) ) ;
#42976=CARTESIAN_POINT ( 'NONE',  ( 112.6260814775786514, -0.8288870151387760510, -10.36305467784173118 ) ) ;
#42979=CARTESIAN_POINT ( 'NONE',  ( 126.2184548109119788, 0.08617673920515746266, -14.09731900820182915 ) ) ;
#42982=CARTESIAN_POINT ( 'NONE',  ( 119.3198281442452924, 0.5811942927096110934, -14.16772938898807510 ) ) ;
#42985=CARTESIAN_POINT ( 'NONE',  ( 114.6115148109119986, -6.222761293078241884, -8.102969835052219238 ) ) ;
#42986=CARTESIAN_POINT ( 'NONE',  ( 125.6732148109119862, 0.5811942927096110934, -14.16772938898807510 ) ) ;
#42987=CARTESIAN_POINT ( 'NONE',  ( 126.3509913981939405, -0.5655071077596977025, -10.71139246774309051 ) ) ;
#42988=CARTESIAN_POINT ( 'NONE',  ( 117.5045748109119756, -9.859900752359374465, -12.68260735090039404 ) ) ;
#42990=CARTESIAN_POINT ( 'NONE',  ( 114.1577014775786552, -3.505236298600246325, -18.68346056562440793 ) ) ;
#42994=CARTESIAN_POINT ( 'NONE',  ( 120.8514481442452961, -7.893985811506177619, -18.51759400769804742 ) ) ;
#42995=CARTESIAN_POINT ( 'NONE',  ( 121.4187148109119789, -3.505236298600246325, -18.68346056562440793 ) ) ;
#42997=CARTESIAN_POINT ( 'NONE',  ( 136.8340972670087297, -7.132904381023736917, -8.303565050146163529 ) ) ;
#42998=CARTESIAN_POINT ( 'NONE',  ( 125.2194014775786286, -10.30919188438810075, -12.61870101168855918 ) ) ;
#43000=CARTESIAN_POINT ( 'NONE',  ( 120.8514481442452961, -2.084020599724406786, -8.691656652584148546 ) ) ;
#43001=CARTESIAN_POINT ( 'NONE',  ( 122.6667014775786413, -2.084020599724406786, -8.691656652584148546 ) ) ;
#43002=CARTESIAN_POINT ( 'NONE',  ( 115.2355081442453155, 0.1319031606808879209, -14.10382304977623669 ) ) ;
#43005=CARTESIAN_POINT ( 'NONE',  ( 123.8579614775786126, -9.859900752359378018, -12.68260735090039759 ) ) ;
#43006=CARTESIAN_POINT ( 'NONE',  ( 124.8223148109119762, -10.15424416112533912, -14.75197769757731336 ) ) ;
#43014=CARTESIAN_POINT ( 'NONE',  ( 118.1852948109119836, -5.638512984488999180, -18.83840828888717311 ) ) ;
#43015=CARTESIAN_POINT ( 'NONE',  ( 116.8805814775786445, -6.344957434206662583, -7.627207830600332805 ) ) ;
#43019=ORIENTED_EDGE ( 'NONE', *, *, #15556, .F. ) ;
#43022=CARTESIAN_POINT ( 'NONE',  ( 118.2420214775786320, -3.383040157471821630, -19.15922257007629170 ) ) ;
#43023=CARTESIAN_POINT ( 'NONE',  ( 125.9568481442452850, -3.505236298600246325, -18.68346056562440793 ) ) ;
#43026=CARTESIAN_POINT ( 'NONE',  ( 115.2922348109119781, 0.4262465694468514643, -12.03445270309931736 ) ) ;
#43027=CARTESIAN_POINT ( 'NONE',  ( 121.4187148109119789, -6.344957434206665248, -7.627207830600338134 ) ) ;
#43030=CARTESIAN_POINT ( 'NONE',  ( 117.1642148109119859, -0.8288870151387760510, -10.36305467784173118 ) ) ;
#43035=CARTESIAN_POINT ( 'NONE',  ( 118.5823814775786360, -1.834011780172310813, -8.268836392978581529 ) ) ;
#43040=CARTESIAN_POINT ( 'NONE',  ( 125.0849635773846842, -2.467220198597905867, -17.83387418641800437 ) ) ;
#43041=CARTESIAN_POINT ( 'NONE',  ( 119.7736414775786358, 0.1319031606808879209, -14.10382304977623669 ) ) ;
#43043=CARTESIAN_POINT ( 'NONE',  ( 123.9601326669217372, -2.334846009198419559, -18.01015021110789505 ) ) ;
#43044=CARTESIAN_POINT ( 'NONE',  ( 122.6667014775786413, -2.084020599724406786, -8.691656652584148546 ) ) ;
#43045=CARTESIAN_POINT ( 'NONE',  ( 121.3619881442452879, -4.089484607189477039, -7.948022111789462052 ) ) ;
#43046=CARTESIAN_POINT ( 'NONE',  ( 123.4041481442452834, 0.1319031606808879209, -14.10382304977623669 ) ) ;
#43049=CARTESIAN_POINT ( 'NONE',  ( 119.2631014775786298, -9.565557343593413364, -10.61323700422348004 ) ) ;
#43050=CARTESIAN_POINT ( 'NONE',  ( 123.0070614775786169, -10.15424416112533912, -14.75197769757731336 ) ) ;
#43052=CARTESIAN_POINT ( 'NONE',  ( 112.0020881442453344, 0.2603800115204892296, -16.42320221600525088 ) ) ;
#43053=CARTESIAN_POINT ( 'NONE',  ( 120.4543614775786295, -4.089484607189486809, -7.948022111789456723 ) ) ;
#43054=CARTESIAN_POINT ( 'NONE',  ( 114.5547881442453217, -5.638512984488999180, -18.83840828888717311 ) ) ;
#43056=CARTESIAN_POINT ( 'NONE',  ( 125.1626748109119802, -0.1624402480850797581, -16.17319339645315424 ) ) ;
#43057=EDGE_LOOP ( 'NONE', ( #23965, #44852, #29380, #11854 ) ) ;
#43058=CARTESIAN_POINT ( 'NONE',  ( 118.9227414775786400, -10.63000616557722466, -14.87417383870573495 ) ) ;
#43062=CARTESIAN_POINT ( 'NONE',  ( 114.2711548109119803, -0.1624402480850797581, -16.17319339645315424 ) ) ;
#43064=CARTESIAN_POINT ( 'NONE',  ( 124.6521348109119884, -1.561330072975668948, -17.79121239304076951 ) ) ;
#43066=CARTESIAN_POINT ( 'NONE',  ( 120.2841814775786276, -10.15424416112533912, -14.75197769757731336 ) ) ;
#43071=ORIENTED_EDGE ( 'NONE', *, *, #27820, .T. ) ;
#43072=CARTESIAN_POINT ( 'NONE',  ( 116.4267681442453153, -3.383040157471821630, -19.15922257007629170 ) ) ;
#43073=CARTESIAN_POINT ( 'NONE',  ( 125.3328548109119964, -9.261995988541697145, -16.69588392320189030 ) ) ;
#43075=CARTESIAN_POINT ( 'NONE',  ( 119.7169148109119874, -0.1624402480850797581, -16.17319339645315424 ) ) ;
#43076=CARTESIAN_POINT ( 'NONE',  ( 126.4599182912938318, -3.568828463829896602, -8.438959581207143401 ) ) ;
#43077=CARTESIAN_POINT ( 'NONE',  ( 111.2751814775786556, -7.618532446445550832, -18.05174138884716228 ) ) ;
#43080=FACE_OUTER_BOUND ( 'NONE', #41719, .T. ) ;
#43084=CARTESIAN_POINT ( 'NONE',  ( 121.1918081442452859, 0.9020085738987339008, -11.91225656197089222 ) ) ;
#43087=CARTESIAN_POINT ( 'NONE',  ( 115.3489614775786407, -9.261995988541697145, -16.69588392320189030 ) ) ;
#43088=CARTESIAN_POINT ( 'NONE',  ( 111.4348214775786801, -3.505236298600246325, -18.68346056562440793 ) ) ;
#43091=CARTESIAN_POINT ( 'NONE',  ( 124.0848681442452772, -5.574606645277164318, -18.38911715685844683 ) ) ;
#43093=CARTESIAN_POINT ( 'NONE',  ( 117.5045748109119756, 0.5811942927096110934, -14.16772938898807510 ) ) ;
#43097=CARTESIAN_POINT ( 'NONE',  ( 137.2865145795249475, -4.931349962157201006, -8.163486744682481699 ) ) ;
#43098=CARTESIAN_POINT ( 'NONE',  ( 112.9097148109120070, -9.565557343593413364, -10.61323700422348004 ) ) ;
#43102=CARTESIAN_POINT ( 'NONE',  ( 111.7184548109119788, -0.8288870151387760510, -10.36305467784173118 ) ) ;
#43103=CARTESIAN_POINT ( 'NONE',  ( 112.6828081442453282, -7.893985811506177619, -18.51759400769804742 ) ) ;
#43105=CARTESIAN_POINT ( 'NONE',  ( 124.3685014775786328, 0.4262465694468514643, -12.03445270309931736 ) ) ;
#43107=CARTESIAN_POINT ( 'NONE',  ( 119.4332814775786318, -0.4660016031367893996, -10.09054647747474043 ) ) ;
#43108=ORIENTED_EDGE ( 'NONE', *, *, #33926, .T. ) ;
#43109=CARTESIAN_POINT ( 'NONE',  ( 126.3444272079807007, -8.643527312879829338, -16.76218589705026574 ) ) ;
#43113=CARTESIAN_POINT ( 'NONE',  ( 126.3999550322252361, -9.807393774667220399, -12.17702641686377873 ) ) ;
#43114=CARTESIAN_POINT ( 'NONE',  ( 114.7249681442453237, 0.2603800115204892296, -16.42320221600525088 ) ) ;
#43116=CARTESIAN_POINT ( 'NONE',  ( 117.0507614775786465, 0.1319031606808879209, -14.10382304977623669 ) ) ;
#43118=CARTESIAN_POINT ( 'NONE',  ( 151.2860562277021472, -2.211393927326563702, -15.67656524173425758 ) ) ;
#43121=CARTESIAN_POINT ( 'NONE',  ( 122.4040527111058339, -1.267766418764731728, -16.93314635290706605 ) ) ;
#43122=CARTESIAN_POINT ( 'NONE',  ( 112.2289948109119848, -1.834011780172310813, -8.268836392978581529 ) ) ;
#43123=CARTESIAN_POINT ( 'NONE',  ( 116.7104014775786425, -0.4660016031367893996, -10.09054647747474043 ) ) ;
#43128=CARTESIAN_POINT ( 'NONE',  ( 118.6391081442452986, -5.574606645277164318, -18.38911715685844683 ) ) ;
#43129=CARTESIAN_POINT ( 'NONE',  ( 114.8951481442453115, -0.4660016031367893996, -10.09054647747474043 ) ) ;
#43130=FACE_OUTER_BOUND ( 'NONE', #27894, .T. ) ;
#43131=CARTESIAN_POINT ( 'NONE',  ( 117.9132914748722385, -0.1020945015694949415, -15.74893487844865625 ) ) ;
#43132=CARTESIAN_POINT ( 'NONE',  ( 122.4965214775786251, 0.1319031606808879209, -14.10382304977623669 ) ) ;
#43133=CARTESIAN_POINT ( 'NONE',  ( 115.6325948109119821, -9.565557343593413364, -10.61323700422348004 ) ) ;
#43139=CARTESIAN_POINT ( 'NONE',  ( 119.4900081442453086, -7.643976991954077427, -18.09477374809248928 ) ) ;
#43142=CARTESIAN_POINT ( 'NONE',  ( 113.5337081442453240, -9.261995988541697145, -16.69588392320189030 ) ) ;
#43144=CARTESIAN_POINT ( 'NONE',  ( 113.7606148109119886, -7.894159318335828068, -9.358103419637847864 ) ) ;
#43145=EDGE_CURVE ( 'NONE', #6217, #29655, #19507, .T. ) ;
#43149=CARTESIAN_POINT ( 'NONE',  ( 122.6667014775786413, -2.084020599724406786, -8.691656652584148546 ) ) ;
#43150=CARTESIAN_POINT ( 'NONE',  ( 116.9373081442452929, -1.833838273342659253, -17.42832698103878286 ) ) ;
#43153=ORIENTED_EDGE ( 'NONE', *, *, #2472, .F. ) ;
#43159=CARTESIAN_POINT ( 'NONE',  ( 117.8449348109119938, -8.166667518702817929, -8.995218007635861213 ) ) ;
#43160=CARTESIAN_POINT ( 'NONE',  ( 111.7751814775786556, -7.893985811506177619, -18.51759400769804742 ) ) ;
#43161=CARTESIAN_POINT ( 'NONE',  ( 117.0507614775786465, 0.1319031606808879209, -14.10382304977623669 ) ) ;
#43162=CARTESIAN_POINT ( 'NONE',  ( 123.0637881442452937, -8.899110576539710493, -16.42337572283490132 ) ) ;
#43165=CARTESIAN_POINT ( 'NONE',  ( 118.9227414775786542, 0.4262465694468514643, -12.03445270309931736 ) ) ;
#43167=CARTESIAN_POINT ( 'NONE',  ( 123.6877814775786533, -6.222761293078241884, -8.102969835052219238 ) ) ;
#43172=CARTESIAN_POINT ( 'NONE',  ( 118.4689281442453392, 0.9020085738987339008, -11.91225656197089222 ) ) ;
#43174=EDGE_CURVE ( 'NONE', #20751, #39978, #23805, .T. ) ;
#43175=CARTESIAN_POINT ( 'NONE',  ( 121.8158014775786171, -5.638512984488999180, -18.83840828888717311 ) ) ;
#43176=CARTESIAN_POINT ( 'NONE',  ( 115.2581675888224169, -2.372251574601226043, -17.96033910819752322 ) ) ;
#43178=CARTESIAN_POINT ( 'NONE',  ( 117.6747548109119919, -1.834011780172310813, -8.268836392978581529 ) ) ;
#43181=CARTESIAN_POINT ( 'NONE',  ( 119.1496481442453046, -3.383040157471821630, -19.15922257007629170 ) ) ;
#43185=VERTEX_POINT ( 'NONE', #23130 ) ;
#43187=CARTESIAN_POINT ( 'NONE',  ( 123.2184548109119788, -6.965697074025154478, -10.59448971407311646 ) ) ;
#43189=CARTESIAN_POINT ( 'NONE',  ( 119.5467348109119712, -5.574606645277164318, -18.38911715685844683 ) ) ;
#43192=CARTESIAN_POINT ( 'NONE',  ( 113.7606148109119886, -7.894159318335828068, -9.358103419637847864 ) ) ;
#43193=CARTESIAN_POINT ( 'NONE',  ( 123.7253032127138397, -2.191907684172563986, -18.20049396185734025 ) ) ;
#43194=CARTESIAN_POINT ( 'NONE',  ( 114.2144281442453178, -1.833838273342658809, -17.42832698103878286 ) ) ;
#43195=CARTESIAN_POINT ( 'NONE',  ( 118.1852948109119836, -5.638512984488999180, -18.83840828888717311 ) ) ;
#43197=CARTESIAN_POINT ( 'NONE',  ( 117.6747548109119919, -7.643976991954077427, -18.09477374809248928 ) ) ;
#43198=CARTESIAN_POINT ( 'NONE',  ( 114.5547881442453217, -5.638512984488999180, -18.83840828888717311 ) ) ;
#43199=CARTESIAN_POINT ( 'NONE',  ( 121.5321681442453183, -9.988377603198976828, -10.36322818467138340 ) ) ;
#43200=CARTESIAN_POINT ( 'NONE',  ( 121.4754414775786131, -1.833838273342659697, -17.42832698103878286 ) ) ;
#43202=CARTESIAN_POINT ( 'NONE',  ( 124.1415948109119540, -3.505236298600246325, -18.68346056562440793 ) ) ;
#43204=CARTESIAN_POINT ( 'NONE',  ( 122.1561614775786353, -0.4660016031367893996, -10.09054647747474043 ) ) ;
#43206=CARTESIAN_POINT ( 'NONE',  ( 121.8725281442453223, -3.383040157471821630, -19.15922257007629170 ) ) ;
#43208=CARTESIAN_POINT ( 'NONE',  ( 127.8473378044042477, -3.224434522777662515, -14.32704208324133255 ) ) ;
#43213=CARTESIAN_POINT ( 'NONE',  ( 115.4056881442453459, -2.084020599724406786, -8.691656652584148546 ) ) ;
#43214=CARTESIAN_POINT ( 'NONE',  ( 112.1155414775786454, -10.15424416112533912, -14.75197769757731336 ) ) ;
#43218=CARTESIAN_POINT ( 'NONE',  ( 115.8027748109119841, -8.899110576539710493, -16.42337572283490132 ) ) ;
#43223=CARTESIAN_POINT ( 'NONE',  ( 120.5678148109119832, -8.166667518702819706, -8.995218007635861213 ) ) ;
#43224=CARTESIAN_POINT ( 'NONE',  ( 121.7590748109119687, -2.084020599724406786, -8.691656652584148546 ) ) ;
#43227=CARTESIAN_POINT ( 'NONE',  ( 125.0492214775786266, -6.344957434206665248, -7.627207830600338134 ) ) ;
#43229=CARTESIAN_POINT ( 'NONE',  ( 121.9859814775786333, -9.565557343593413364, -10.61323700422348004 ) ) ;
#43230=CARTESIAN_POINT ( 'NONE',  ( 120.2274548109119934, -9.859900752359374465, -12.68260735090039404 ) ) ;
#43232=CARTESIAN_POINT ( 'NONE',  ( 114.7816948109119863, -9.859900752359374465, -12.68260735090039404 ) ) ;
#43235=CARTESIAN_POINT ( 'NONE',  ( 125.1626748109119802, -0.1624402480850797581, -16.17319339645315424 ) ) ;
#43237=CARTESIAN_POINT ( 'NONE',  ( 123.5176014775786228, -0.8288870151387760510, -10.36305467784173118 ) ) ;
#43239=CARTESIAN_POINT ( 'NONE',  ( 112.7395348109119766, -4.153390946401321671, -8.397313243818183892 ) ) ;
#43242=DIRECTION ( 'NONE',  ( 1.000000000000000000, 0.000000000000000000, 0.000000000000000000 ) ) ;
#43244=CARTESIAN_POINT ( 'NONE',  ( 121.1918081442452859, 0.9020085738987339008, -11.91225656197089222 ) ) ;
#43245=CARTESIAN_POINT ( 'NONE',  ( 119.0929214775786278, -5.638512984488999180, -18.83840828888717311 ) ) ;
#43248=CARTESIAN_POINT ( 'NONE',  ( 115.4624148109119943, -5.638512984488999180, -18.83840828888717311 ) ) ;
#43250=VERTEX_POINT ( 'NONE', #17411 ) ;
#43253=CARTESIAN_POINT ( 'NONE',  ( 120.2274548109119934, 0.5811942927096110934, -14.16772938898807510 ) ) ;
#43254=CARTESIAN_POINT ( 'NONE',  ( 125.1626748109119802, -0.1624402480850797581, -16.17319339645315424 ) ) ;
#43256=CARTESIAN_POINT ( 'NONE',  ( 113.1933481442453058, -5.574606645277164318, -18.38911715685844683 ) ) ;
#43257=CARTESIAN_POINT ( 'NONE',  ( 123.9146881442452894, 0.9020085738987339008, -11.91225656197089222 ) ) ;
#43259=CARTESIAN_POINT ( 'NONE',  ( 121.7023481442452777, -0.8288870151387760510, -10.36305467784173118 ) ) ;
#43261=CARTESIAN_POINT ( 'NONE',  ( 151.2860562277021472, -4.863998795839242995, -13.39321520033831447 ) ) ;
#43265=CARTESIAN_POINT ( 'NONE',  ( 121.9292548109119849, -1.561330072975668948, -17.79121239304076951 ) ) ;
#43270=CARTESIAN_POINT ( 'NONE',  ( 119.4332814775786318, -8.899110576539710493, -16.42337572283490132 ) ) ;
#43273=CARTESIAN_POINT ( 'NONE',  ( 125.1059481442452750, -1.833838273342660141, -17.42832698103878286 ) ) ;
#43276=CARTESIAN_POINT ( 'NONE',  ( 117.3911214775786505, -7.894159318335828068, -9.358103419637847864 ) ) ;
#43277=CARTESIAN_POINT ( 'NONE',  ( 123.4608748109119745, 0.4262465694468514643, -12.03445270309931736 ) ) ;
#43278=CARTESIAN_POINT ( 'NONE',  ( 119.7736414775786358, -10.30919188438810075, -12.61870101168855918 ) ) ;
#43279=CARTESIAN_POINT ( 'NONE',  ( 117.3911214775786505, -1.561330072975668504, -17.79121239304076951 ) ) ;
#43281=CARTESIAN_POINT ( 'NONE',  ( 125.5030348109119558, -6.222761293078241884, -8.102969835052219238 ) ) ;
#43283=CARTESIAN_POINT ( 'NONE',  ( 118.6958348109119754, -6.344957434206665248, -7.627207830600338134 ) ) ;
#43288=CARTESIAN_POINT ( 'NONE',  ( 112.5693548109119888, 0.4262465694468514643, -12.03445270309931736 ) ) ;
#43293=CARTESIAN_POINT ( 'NONE',  ( 126.6375681442452930, -10.15424416112533912, -14.75197769757731336 ) ) ;
#43300=CARTESIAN_POINT ( 'NONE',  ( 115.8595014775786609, -1.834011780172310813, -8.268836392978581529 ) ) ;
#43301=CARTESIAN_POINT ( 'NONE',  ( 125.7299414775786346, 0.9020085738987339008, -11.91225656197089222 ) ) ;
#43302=CARTESIAN_POINT ( 'NONE',  ( 119.2063748109119814, -7.894159318335828068, -9.358103419637847864 ) ) ;
#43303=CARTESIAN_POINT ( 'NONE',  ( 113.4769814775786330, 0.4262465694468514643, -12.03445270309931736 ) ) ;
#43306=CARTESIAN_POINT ( 'NONE',  ( 113.8173414775786512, 0.2603800115204892296, -16.42320221600525088 ) ) ;
#43308=EDGE_CURVE ( 'NONE', #29255, #2299, #3930, .T. ) ;
#43309=CARTESIAN_POINT ( 'NONE',  ( 123.7445081442452874, -1.561330072975668948, -17.79121239304076951 ) ) ;
#43311=CARTESIAN_POINT ( 'NONE',  ( 137.2528433483972776, -8.502389972432839116, -17.19305753011830618 ) ) ;
#43313=CARTESIAN_POINT ( 'NONE',  ( 112.9097148109120070, 0.2603800115204892296, -16.42320221600525088 ) ) ;
#43314=CARTESIAN_POINT ( 'NONE',  ( 111.8319081442453182, -4.153390946401321671, -8.397313243818183892 ) ) ;
#43316=CARTESIAN_POINT ( 'NONE',  ( 122.0994348109119443, -10.15424416112533912, -14.75197769757731336 ) ) ;
#43317=CIRCLE ( 'NONE', #7636, 5.999999999999997335 ) ;
#43319=CARTESIAN_POINT ( 'NONE',  ( 118.9794681442453026, -9.261995988541697145, -16.69588392320189030 ) ) ;
#43324=CARTESIAN_POINT ( 'NONE',  ( 137.0105207745552889, -5.223277318015287385, -7.946479427247078675 ) ) ;
#43326=CARTESIAN_POINT ( 'NONE',  ( 115.4056881442453459, -2.084020599724406786, -8.691656652584148546 ) ) ;
#43329=CARTESIAN_POINT ( 'NONE',  ( 112.5126281442453120, 0.1319031606808879209, -14.10382304977623669 ) ) ;
#43330=CARTESIAN_POINT ( 'NONE',  ( 111.8319081442453182, -5.638512984488999180, -18.83840828888717311 ) ) ;
#43332=CARTESIAN_POINT ( 'NONE',  ( 125.3895814775786448, -2.084020599724406786, -8.691656652584148546 ) ) ;
#43334=CARTESIAN_POINT ( 'NONE',  ( 120.8514481442452961, -7.893985811506177619, -18.51759400769804742 ) ) ;
#43335=CARTESIAN_POINT ( 'NONE',  ( 120.3409081442453044, -0.4660016031367893996, -10.09054647747474043 ) ) ;
#43337=CARTESIAN_POINT ( 'NONE',  ( 128.2184548109119930, -8.536181032868617180, -18.13822074491315561 ) ) ;
#43341=CARTESIAN_POINT ( 'NONE',  ( 126.3509913982061050, -9.799826457514038580, -12.25005761896067824 ) ) ;
#43342=CARTESIAN_POINT ( 'NONE',  ( 116.1431348109119881, -10.30919188438810075, -12.61870101168855918 ) ) ;
#43346=CARTESIAN_POINT ( 'NONE',  ( 115.1787814775786387, -0.1624402480850797581, -16.17319339645315424 ) ) ;
#43347=( BOUNDED_SURFACE ( )  B_SPLINE_SURFACE ( 1, 2, ( 
 ( #23210, #19335, #2669, #19785, #16602, #13181, #36646, #15921, #37089, #29819, #12504, #30495, #26401, #40311, #5863, #16367, #9075, #30269, #44195, #26853, #40766, #20014, #22977, #27084, #9523, #23440, #1766, #36867, #37324, #6095, #15692, #6554, #35000, #41450, #10208, #31165, #13408, #38443, #13626, #21126, #3571, #17055, #7213, #17274, #38223, #28207, #41889, #31381, #3784, #31608, #27311, #42115, #23898, #41674, #152, #9987, #17708, #27536, #14066, #27985, #6328, #23669, #377, #37557, #34788, #34352, #30723, #20246, #10431, #30947, #34132, #37781, #14288, #44870, #2901, #16830, #41228, #3355, #17483, #10651, #45084, #44646, #24557, #13843, #7003, #20471, #3130, #24116, #38010, #6784, #34572, #20694, #27759, #24339, #20914, #25677, #11319, #28651, #31832, #28425, #8125, #4011, #29316, #25229, #602, #32278, #4470, #1046, #11768, #35464, #14513, #32498, #7662, #24770, #28874, #38661, #38893, #39583, #8345, #42336, #39127, #21800, #35694, #18157, #32053, #42787, #22246, #1273, #18390, #11548, #14962, #32718, #15412, #21577, #820, #17933, #25455, #39357, #22027, #35920, #42557, #4686, #4239, #7894, #18607, #11097, #24998, #1490, #35235, #15185, #7430, #14739, #29088, #43000, #36142, #4910, #21351, #18826, #10875, #34024, #41119, #20138, #29542, #27201, #26967, #44530, #13067, #16719, #40655, #20361, #6216, #41350, #9410, #43229, #23788, #2792, #34462, #36365, #3241, #11996, #5137, #25898, #40887, #27428, #30613, #13293, #34248, #13519, #9641, #6453, #44312, #10106, #16490, #2561, #23321, #9878, #3020, #19053, #37678, #16942, #30837, #17167, #44760, #24010, #5979, #39802, #33789, #37898, #8571, #32939, #37444, #6676, #20583, #22471, #1714, #23563, #15638, #43458, #12222, #26121, #30390, #37206, #19904, #3469, #21020, #34893, #38782, #14626, #267, #7324, #4352, #17384, #14176, #28093, #21244, #31273, #46, #13960, #3682, #24889, #706, #28544, #44984, #35121, #42448, #27871, #11214, #42002, #17603, #25119, #10766, #20802, #3904, #14402, #13742, #39015, #41785 ),
 ( #38333, #41566, #10540, #7785, #24442, #31056, #27651, #7110, #24662, #10987, #7553, #38549, #21694, #21468, #17822, #488, #31496, #31719, #28312, #42224, #18046, #35351, #4126, #31940, #35579, #10325, #24228, #38118, #6892, #34681, #35806, #15521, #11441, #36703, #32615, #39240, #39696, #11884, #8461, #19170, #42895, #8004, #39920, #15076, #32168, #36260, #937, #1160, #1824, #33050, #21913, #1381, #29205, #43114, #25564, #39470, #5027, #29654, #4576, #25787, #32391, #43567, #1601, #15753, #26236, #25346, #18501, #22364, #28988, #11657, #12336, #8234, #22141, #18942, #29428, #36033, #15296, #32832, #43342, #12112, #40146, #4802, #8910, #36486, #26015, #18272, #18723, #8681, #22585, #22808, #5253, #14856, #28765, #42671, #13014, #40372, #20304, #40601, #2963, #30554, #44026, #34189, #44258, #20081, #10054, #23732, #13242, #16891, #13468, #9135, #23957, #5698, #23505, #27144, #36926, #30784, #9361, #41065, #9822, #5927, #30110, #37623, #16434, #6397, #33736, #44707, #27370, #41292, #19849, #23269, #26468, #23039, #2735, #43798, #5471, #2507, #19615, #26913, #40834, #9589, #19391, #12788, #33499, #33280, #2278, #2055, #37390, #15978, #16208, #29881, #12563, #26690, #30332, #6162, #33967, #37151, #16660, #44475, #4066, #24174, #3627, #6843, #17990, #21187, #35293, #655, #31004, #10267, #208, #44931, #41511, #31889, #20750, #3415, #28039, #35065, #34629, #34841, #38495, #14122, #17546, #21411, #38066, #28488, #10930, #3846, #11157, #24391, #31662, #13689, #42393, #17331, #14570, #10489, #38279, #41947, #27598, #7495, #27812, #37839, #17766, #31221, #6616, #31440, #7271, #20529, #24832, #431, #34409, #3190, #40285, #17114, #13903, #10711, #14347, #41726, #7059, #20969, #28261, #42170, #24612, #38723, #22533, #29603, #36209, #35756, #32112, #43519, #43064, #32340, #35523, #11381, #33001, #18452, #25062, #38955, #42619, #4750, #4976, #18887, #32563, #1775, #1551, #18671, #39646, #39184, #7949, #15701, #4295, #15473, #21636, #14799, #11832, #25740, #8409, #22314, #18216 ) ),
 .UNSPECIFIED., .F., .F., .T. ) 
 B_SPLINE_SURFACE_WITH_KNOTS ( ( 2, 2 ),
 ( 3, 2, 2, 2, 2, 2, 2, 2, 2, 2, 2, 2, 2, 2, 2, 2, 2, 2, 2, 2, 2, 2, 2, 2, 2, 2, 2, 2, 2, 2, 2, 2, 2, 2, 2, 2, 2, 2, 2, 2, 2, 2, 2, 2, 2, 2, 2, 2, 2, 2, 2, 2, 2, 2, 2, 2, 2, 2, 2, 2, 2, 2, 2, 2, 2, 2, 2, 2, 2, 2, 2, 2, 2, 2, 2, 2, 2, 2, 2, 2, 2, 2, 2, 2, 2, 2, 2, 2, 2, 2, 2, 2, 2, 2, 2, 2, 2, 2, 2, 2, 2, 2, 2, 2, 2, 2, 2, 2, 2, 2, 2, 2, 2, 2, 2, 2, 2, 2, 2, 2, 2, 2, 2, 2, 2, 2, 2, 2, 3 ),
 ( 0.000000000000000000, 1.000000000000000000 ),
 ( 0.000000000000000000, 0.007812500000000000000, 0.01562500000000000000, 0.02343750000000000000, 0.03125000000000000000, 0.03906250000000000000, 0.04687500000000000000, 0.05468750000000000000, 0.06250000000000000000, 0.07031250000000000000, 0.07812500000000000000, 0.08593750000000000000, 0.09375000000000000000, 0.1015625000000000000, 0.1093750000000000000, 0.1171875000000000000, 0.1250000000000000000, 0.1328125000000000000, 0.1406250000000000000, 0.1484375000000000000, 0.1562500000000000000, 0.1640625000000000000, 0.1718750000000000000, 0.1796875000000000000, 0.1875000000000000000, 0.1953125000000000000, 0.2031250000000000000, 0.2109375000000000000, 0.2187500000000000000, 0.2265625000000000000, 0.2343750000000000000, 0.2421875000000000000, 0.2500000000000000000, 0.2578125000000000000, 0.2656250000000000000, 0.2734375000000000000, 0.2812500000000000000, 0.2890625000000000000, 0.2968750000000000000, 0.3046875000000000000, 0.3125000000000000000, 0.3203125000000000000, 0.3281250000000000000, 0.3359375000000000000, 0.3437500000000000000, 0.3515625000000000000, 0.3593750000000000000, 0.3671875000000000000, 0.3750000000000000000, 0.3828125000000000000, 0.3906250000000000000, 0.3984375000000000000, 0.4062500000000000000, 0.4140625000000000000, 0.4218750000000000000, 0.4296875000000000000, 0.4375000000000000000, 0.4453125000000000000, 0.4531250000000000000, 0.4609375000000000000, 0.4687500000000000000, 0.4765625000000000000, 0.4843750000000000000, 0.4921875000000000000, 0.5000000000000000000, 0.5078125000000000000, 0.5156250000000000000, 0.5234375000000000000, 0.5312500000000000000, 0.5390625000000000000, 0.5468750000000000000, 0.5546875000000000000, 0.5625000000000000000, 0.5703125000000000000, 0.5781250000000000000, 0.5859375000000000000, 0.5937500000000000000, 0.6015625000000000000, 0.6093750000000000000, 0.6171875000000000000, 0.6250000000000000000, 0.6328125000000000000, 0.6406250000000000000, 0.6484375000000000000, 0.6562500000000000000, 0.6640625000000000000, 0.6718750000000000000, 0.6796875000000000000, 0.6875000000000000000, 0.6953125000000000000, 0.7031250000000000000, 0.7109375000000000000, 0.7187500000000000000, 0.7265625000000000000, 0.7343750000000000000, 0.7421875000000000000, 0.7500000000000000000, 0.7578125000000000000, 0.7656250000000000000, 0.7734375000000000000, 0.7812500000000000000, 0.7890625000000000000, 0.7968750000000000000, 0.8046875000000000000, 0.8125000000000000000, 0.8203125000000000000, 0.8281250000000000000, 0.8359375000000000000, 0.8437500000000000000, 0.8515625000000000000, 0.8593750000000000000, 0.8671875000000000000, 0.8750000000000000000, 0.8828125000000000000, 0.8906250000000000000, 0.8984375000000000000, 0.9062500000000000000, 0.9140625000000000000, 0.9218750000000000000, 0.9296875000000000000, 0.9375000000000000000, 0.9453125000000000000, 0.9531250000000000000, 0.9609375000000000000, 0.9687500000000000000, 0.9765625000000000000, 0.9843750000000000000, 0.9921875000000000000, 1.000000000000000000 ),
 .UNSPECIFIED. ) 
 GEOMETRIC_REPRESENTATION_ITEM ( )  RATIONAL_B_SPLINE_SURFACE ( (
 ( 1.000000000000000000, 0.9238795325112869605, 1.000000000000000000, 0.9238795325112869605, 1.000000000000000000, 0.9238795325112869605, 1.000000000000000000, 0.9238795325112869605, 1.000000000000000000, 0.9238795325112869605, 1.000000000000000000, 0.9238795325112869605, 1.000000000000000000, 0.9238795325112869605, 1.000000000000000000, 0.9238795325112869605, 1.000000000000000000, 0.9238795325112869605, 1.000000000000000000, 0.9238795325112869605, 1.000000000000000000, 0.9238795325112869605, 1.000000000000000000, 0.9238795325112869605, 1.000000000000000000, 0.9238795325112869605, 1.000000000000000000, 0.9238795325112869605, 1.000000000000000000, 0.9238795325112869605, 1.000000000000000000, 0.9238795325112869605, 1.000000000000000000, 0.9238795325112869605, 1.000000000000000000, 0.9238795325112869605, 1.000000000000000000, 0.9238795325112869605, 1.000000000000000000, 0.9238795325112869605, 1.000000000000000000, 0.9238795325112869605, 1.000000000000000000, 0.9238795325112869605, 1.000000000000000000, 0.9238795325112869605, 1.000000000000000000, 0.9238795325112869605, 1.000000000000000000, 0.9238795325112869605, 1.000000000000000000, 0.9238795325112869605, 1.000000000000000000, 0.9238795325112869605, 1.000000000000000000, 0.9238795325112869605, 1.000000000000000000, 0.9238795325112869605, 1.000000000000000000, 0.9238795325112869605, 1.000000000000000000, 0.9238795325112869605, 1.000000000000000000, 0.9238795325112869605, 1.000000000000000000, 0.9238795325112869605, 1.000000000000000000, 0.9238795325112869605, 1.000000000000000000, 0.9238795325112869605, 1.000000000000000000, 0.9238795325112869605, 1.000000000000000000, 0.9238795325112869605, 1.000000000000000000, 0.9238795325112869605, 1.000000000000000000, 0.9238795325112869605, 1.000000000000000000, 0.9238795325112869605, 1.000000000000000000, 0.9238795325112869605, 1.000000000000000000, 0.9238795325112869605, 1.000000000000000000, 0.9238795325112869605, 1.000000000000000000, 0.9238795325112869605, 1.000000000000000000, 0.9238795325112869605, 1.000000000000000000, 0.9238795325112869605, 1.000000000000000000, 0.9238795325112869605, 1.000000000000000000, 0.9238795325112869605, 1.000000000000000000, 0.9238795325112869605, 1.000000000000000000, 0.9238795325112869605, 1.000000000000000000, 0.9238795325112869605, 1.000000000000000000, 0.9238795325112869605, 1.000000000000000000, 0.9238795325112869605, 1.000000000000000000, 0.9238795325112869605, 1.000000000000000000, 0.9238795325112869605, 1.000000000000000000, 0.9238795325112869605, 1.000000000000000000, 0.9238795325112869605, 1.000000000000000000, 0.9238795325112869605, 1.000000000000000000, 0.9238795325112869605, 1.000000000000000000, 0.9238795325112869605, 1.000000000000000000, 0.9238795325112869605, 1.000000000000000000, 0.9238795325112869605, 1.000000000000000000, 0.9238795325112869605, 1.000000000000000000, 0.9238795325112869605, 1.000000000000000000, 0.9238795325112869605, 1.000000000000000000, 0.9238795325112869605, 1.000000000000000000, 0.9238795325112869605, 1.000000000000000000, 0.9238795325112869605, 1.000000000000000000, 0.9238795325112869605, 1.000000000000000000, 0.9238795325112869605, 1.000000000000000000, 0.9238795325112869605, 1.000000000000000000, 0.9238795325112869605, 1.000000000000000000, 0.9238795325112869605, 1.000000000000000000, 0.9238795325112869605, 1.000000000000000000, 0.9238795325112869605, 1.000000000000000000, 0.9238795325112869605, 1.000000000000000000, 0.9238795325112869605, 1.000000000000000000, 0.9238795325112869605, 1.000000000000000000, 0.9238795325112869605, 1.000000000000000000, 0.9238795325112869605, 1.000000000000000000, 0.9238795325112869605, 1.000000000000000000, 0.9238795325112869605, 1.000000000000000000, 0.9238795325112869605, 1.000000000000000000, 0.9238795325112869605, 1.000000000000000000, 0.9238795325112869605, 1.000000000000000000, 0.9238795325112869605, 1.000000000000000000, 0.9238795325112869605, 1.000000000000000000, 0.9238795325112869605, 1.000000000000000000, 0.9238795325112869605, 1.000000000000000000, 0.9238795325112869605, 1.000000000000000000, 0.9238795325112869605, 1.000000000000000000, 0.9238795325112869605, 1.000000000000000000, 0.9238795325112869605, 1.000000000000000000, 0.9238795325112869605, 1.000000000000000000, 0.9238795325112869605, 1.000000000000000000, 0.9238795325112869605, 1.000000000000000000, 0.9238795325112869605, 1.000000000000000000, 0.9238795325112869605, 1.000000000000000000, 0.9238795325112869605, 1.000000000000000000, 0.9238795325112869605, 1.000000000000000000, 0.9238795325112869605, 1.000000000000000000, 0.9238795325112869605, 1.000000000000000000, 0.9238795325112869605, 1.000000000000000000, 0.9238795325112869605, 1.000000000000000000, 0.9238795325112869605, 1.000000000000000000, 0.9238795325112869605, 1.000000000000000000, 0.9238795325112869605, 1.000000000000000000, 0.9238795325112869605, 1.000000000000000000, 0.9238795325112869605, 1.000000000000000000, 0.9238795325112869605, 1.000000000000000000, 0.9238795325112869605, 1.000000000000000000, 0.9238795325112869605, 1.000000000000000000, 0.9238795325112869605, 1.000000000000000000, 0.9238795325112869605, 1.000000000000000000, 0.9238795325112869605, 1.000000000000000000, 0.9238795325112869605, 1.000000000000000000, 0.9238795325112869605, 1.000000000000000000, 0.9238795325112869605, 1.000000000000000000, 0.9238795325112869605, 1.000000000000000000, 0.9238795325112869605, 1.000000000000000000, 0.9238795325112869605, 1.000000000000000000, 0.9238795325112869605, 1.000000000000000000, 0.9238795325112869605, 1.000000000000000000, 0.9238795325112869605, 1.000000000000000000, 0.9238795325112869605, 1.000000000000000000, 0.9238795325112869605, 1.000000000000000000, 0.9238795325112869605, 1.000000000000000000, 0.9238795325112869605, 1.000000000000000000),
 ( 1.000000000000000000, 0.9238795325112869605, 1.000000000000000000, 0.9238795325112869605, 1.000000000000000000, 0.9238795325112869605, 1.000000000000000000, 0.9238795325112869605, 1.000000000000000000, 0.9238795325112869605, 1.000000000000000000, 0.9238795325112869605, 1.000000000000000000, 0.9238795325112869605, 1.000000000000000000, 0.9238795325112869605, 1.000000000000000000, 0.9238795325112869605, 1.000000000000000000, 0.9238795325112869605, 1.000000000000000000, 0.9238795325112869605, 1.000000000000000000, 0.9238795325112869605, 1.000000000000000000, 0.9238795325112869605, 1.000000000000000000, 0.9238795325112869605, 1.000000000000000000, 0.9238795325112869605, 1.000000000000000000, 0.9238795325112869605, 1.000000000000000000, 0.9238795325112869605, 1.000000000000000000, 0.9238795325112869605, 1.000000000000000000, 0.9238795325112869605, 1.000000000000000000, 0.9238795325112869605, 1.000000000000000000, 0.9238795325112869605, 1.000000000000000000, 0.9238795325112869605, 1.000000000000000000, 0.9238795325112869605, 1.000000000000000000, 0.9238795325112869605, 1.000000000000000000, 0.9238795325112869605, 1.000000000000000000, 0.9238795325112869605, 1.000000000000000000, 0.9238795325112869605, 1.000000000000000000, 0.9238795325112869605, 1.000000000000000000, 0.9238795325112869605, 1.000000000000000000, 0.9238795325112869605, 1.000000000000000000, 0.9238795325112869605, 1.000000000000000000, 0.9238795325112869605, 1.000000000000000000, 0.9238795325112869605, 1.000000000000000000, 0.9238795325112869605, 1.000000000000000000, 0.9238795325112869605, 1.000000000000000000, 0.9238795325112869605, 1.000000000000000000, 0.9238795325112869605, 1.000000000000000000, 0.9238795325112869605, 1.000000000000000000, 0.9238795325112869605, 1.000000000000000000, 0.9238795325112869605, 1.000000000000000000, 0.9238795325112869605, 1.000000000000000000, 0.9238795325112869605, 1.000000000000000000, 0.9238795325112869605, 1.000000000000000000, 0.9238795325112869605, 1.000000000000000000, 0.9238795325112869605, 1.000000000000000000, 0.9238795325112869605, 1.000000000000000000, 0.9238795325112869605, 1.000000000000000000, 0.9238795325112869605, 1.000000000000000000, 0.9238795325112869605, 1.000000000000000000, 0.9238795325112869605, 1.000000000000000000, 0.9238795325112869605, 1.000000000000000000, 0.9238795325112869605, 1.000000000000000000, 0.9238795325112869605, 1.000000000000000000, 0.9238795325112869605, 1.000000000000000000, 0.9238795325112869605, 1.000000000000000000, 0.9238795325112869605, 1.000000000000000000, 0.9238795325112869605, 1.000000000000000000, 0.9238795325112869605, 1.000000000000000000, 0.9238795325112869605, 1.000000000000000000, 0.9238795325112869605, 1.000000000000000000, 0.9238795325112869605, 1.000000000000000000, 0.9238795325112869605, 1.000000000000000000, 0.9238795325112869605, 1.000000000000000000, 0.9238795325112869605, 1.000000000000000000, 0.9238795325112869605, 1.000000000000000000, 0.9238795325112869605, 1.000000000000000000, 0.9238795325112869605, 1.000000000000000000, 0.9238795325112869605, 1.000000000000000000, 0.9238795325112869605, 1.000000000000000000, 0.9238795325112869605, 1.000000000000000000, 0.9238795325112869605, 1.000000000000000000, 0.9238795325112869605, 1.000000000000000000, 0.9238795325112869605, 1.000000000000000000, 0.9238795325112869605, 1.000000000000000000, 0.9238795325112869605, 1.000000000000000000, 0.9238795325112869605, 1.000000000000000000, 0.9238795325112869605, 1.000000000000000000, 0.9238795325112869605, 1.000000000000000000, 0.9238795325112869605, 1.000000000000000000, 0.9238795325112869605, 1.000000000000000000, 0.9238795325112869605, 1.000000000000000000, 0.9238795325112869605, 1.000000000000000000, 0.9238795325112869605, 1.000000000000000000, 0.9238795325112869605, 1.000000000000000000, 0.9238795325112869605, 1.000000000000000000, 0.9238795325112869605, 1.000000000000000000, 0.9238795325112869605, 1.000000000000000000, 0.9238795325112869605, 1.000000000000000000, 0.9238795325112869605, 1.000000000000000000, 0.9238795325112869605, 1.000000000000000000, 0.9238795325112869605, 1.000000000000000000, 0.9238795325112869605, 1.000000000000000000, 0.9238795325112869605, 1.000000000000000000, 0.9238795325112869605, 1.000000000000000000, 0.9238795325112869605, 1.000000000000000000, 0.9238795325112869605, 1.000000000000000000, 0.9238795325112869605, 1.000000000000000000, 0.9238795325112869605, 1.000000000000000000, 0.9238795325112869605, 1.000000000000000000, 0.9238795325112869605, 1.000000000000000000, 0.9238795325112869605, 1.000000000000000000, 0.9238795325112869605, 1.000000000000000000, 0.9238795325112869605, 1.000000000000000000, 0.9238795325112869605, 1.000000000000000000, 0.9238795325112869605, 1.000000000000000000, 0.9238795325112869605, 1.000000000000000000, 0.9238795325112869605, 1.000000000000000000, 0.9238795325112869605, 1.000000000000000000, 0.9238795325112869605, 1.000000000000000000, 0.9238795325112869605, 1.000000000000000000, 0.9238795325112869605, 1.000000000000000000, 0.9238795325112869605, 1.000000000000000000, 0.9238795325112869605, 1.000000000000000000, 0.9238795325112869605, 1.000000000000000000, 0.9238795325112869605, 1.000000000000000000, 0.9238795325112869605, 1.000000000000000000, 0.9238795325112869605, 1.000000000000000000, 0.9238795325112869605, 1.000000000000000000, 0.9238795325112869605, 1.000000000000000000, 0.9238795325112869605, 1.000000000000000000, 0.9238795325112869605, 1.000000000000000000, 0.9238795325112869605, 1.000000000000000000, 0.9238795325112869605, 1.000000000000000000, 0.9238795325112869605, 1.000000000000000000, 0.9238795325112869605, 1.000000000000000000, 0.9238795325112869605, 1.000000000000000000, 0.9238795325112869605, 1.000000000000000000, 0.9238795325112869605, 1.000000000000000000) ) ) 
 REPRESENTATION_ITEM ( '' )  SURFACE ( )  );
#43348=CARTESIAN_POINT ( 'NONE',  ( 123.1249303192116713, -2.378957183258601393, -17.95140958770220152 ) ) ;
#43349=CARTESIAN_POINT ( 'NONE',  ( 118.7525614775786380, -8.166667518702819706, -8.995218007635861213 ) ) ;
#43355=CARTESIAN_POINT ( 'NONE',  ( 117.6180281442453150, -8.899110576539710493, -16.42337572283490132 ) ) ;
#43356=CARTESIAN_POINT ( 'NONE',  ( 116.4267681442453153, -3.383040157471821630, -19.15922257007629170 ) ) ;
#43357=CARTESIAN_POINT ( 'NONE',  ( 112.6260814775786514, -9.261995988541697145, -16.69588392320189030 ) ) ;
#43358=CARTESIAN_POINT ( 'NONE',  ( 136.1055339648910376, -7.166517036409639552, -18.81773387731445624 ) ) ;
#43359=CARTESIAN_POINT ( 'NONE',  ( 125.2194014775786286, 0.1319031606808879209, -14.10382304977623669 ) ) ;
#43360=CARTESIAN_POINT ( 'NONE',  ( 116.8805814775786445, -3.505236298600246325, -18.68346056562440793 ) ) ;
#43364=CARTESIAN_POINT ( 'NONE',  ( 112.6828081442453282, -7.893985811506177619, -18.51759400769804742 ) ) ;
#43365=CARTESIAN_POINT ( 'NONE',  ( 117.9583881442453048, 0.1319031606808879209, -14.10382304977623669 ) ) ;
#43368=CARTESIAN_POINT ( 'NONE',  ( 113.3068014775786594, -8.166667518702817929, -8.995218007635859436 ) ) ;
#43370=CARTESIAN_POINT ( 'NONE',  ( 112.5693548109119888, 0.4262465694468514643, -12.03445270309931736 ) ) ;
#43373=CARTESIAN_POINT ( 'NONE',  ( 120.5110881442453206, -3.505236298600246325, -18.68346056562440793 ) ) ;
#43375=CARTESIAN_POINT ( 'NONE',  ( 122.6099748109119929, -0.8288870151387760510, -10.36305467784173118 ) ) ;
#43383=CARTESIAN_POINT ( 'NONE',  ( 115.2355081442453155, -10.30919188438810075, -12.61870101168855918 ) ) ;
#43384=CARTESIAN_POINT ( 'NONE',  ( 114.4980614775786592, -7.893985811506177619, -18.51759400769804742 ) ) ;
#43385=CARTESIAN_POINT ( 'NONE',  ( 117.2776681442452968, -4.153390946401321671, -8.397313243818183892 ) ) ;
#43386=CARTESIAN_POINT ( 'NONE',  ( 122.4965214775786251, 0.1319031606808879209, -14.10382304977623669 ) ) ;
#43390=CARTESIAN_POINT ( 'NONE',  ( 121.2485348109119769, -8.899110576539710493, -16.42337572283490132 ) ) ;
#43391=CARTESIAN_POINT ( 'NONE',  ( 125.6164881442453094, -9.565557343593413364, -10.61323700422348004 ) ) ;
#43395=CARTESIAN_POINT ( 'NONE',  ( 120.1140014775786398, -1.561330072975668504, -17.79121239304076951 ) ) ;
#43397=CARTESIAN_POINT ( 'NONE',  ( 121.0783548109119749, 0.2603800115204892296, -16.42320221600525088 ) ) ;
#43400=CARTESIAN_POINT ( 'NONE',  ( 117.1074881442453233, -10.63000616557722466, -14.87417383870573495 ) ) ;
#43401=CARTESIAN_POINT ( 'NONE',  ( 115.9729548109119861, -6.344957434206662583, -7.627207830600332805 ) ) ;
#43405=ORIENTED_EDGE ( 'NONE', *, *, #43434, .T. ) ;
#43408=CARTESIAN_POINT ( 'NONE',  ( 119.7169148109119874, -0.1624402480850797581, -16.17319339645315424 ) ) ;
#43412=CARTESIAN_POINT ( 'NONE',  ( 118.1285681442453068, -2.084020599724406786, -8.691656652584148546 ) ) ;
#43416=CARTESIAN_POINT ( 'NONE',  ( 125.9568481442452850, -6.344957434206665248, -7.627207830600338134 ) ) ;
#43417=CARTESIAN_POINT ( 'NONE',  ( 120.8514481442452961, -7.893985811506177619, -18.51759400769804742 ) ) ;
#43421=CARTESIAN_POINT ( 'NONE',  ( 120.1140014775786398, -7.894159318335828068, -9.358103419637847864 ) ) ;
#43422=CARTESIAN_POINT ( 'NONE',  ( 114.2711548109119803, -9.988377603198976828, -10.36322818467138340 ) ) ;
#43423=CARTESIAN_POINT ( 'NONE',  ( 123.2906948109119867, -8.166667518702819706, -8.995218007635861213 ) ) ;
#43424=CARTESIAN_POINT ( 'NONE',  ( 121.3619881442452879, -5.574606645277164318, -18.38911715685844683 ) ) ;
#43426=CARTESIAN_POINT ( 'NONE',  ( 125.2761281442453054, 0.4262465694468514643, -12.03445270309931736 ) ) ;
#43427=CIRCLE ( 'NONE', #17239, 3.499999999999998668 ) ;
#43428=CARTESIAN_POINT ( 'NONE',  ( 118.5823814775786360, -1.834011780172310813, -8.268836392978581529 ) ) ;
#43430=CARTESIAN_POINT ( 'NONE',  ( 122.7234281442452755, -5.638512984488999180, -18.83840828888717311 ) ) ;
#43432=DIRECTION ( 'NONE',  ( 1.000000000000000000, 0.000000000000000000, 0.000000000000000000 ) ) ;
#43434=EDGE_CURVE ( 'NONE', #17999, #23145, #43989, .T. ) ;
#43436=CARTESIAN_POINT ( 'NONE',  ( 137.2446579711038908, -1.128119387170134047, -17.11910725436554870 ) ) ;
#43439=CARTESIAN_POINT ( 'NONE',  ( 136.5935259641925654, -10.15732810381489593, -11.25679434072407581 ) ) ;
#43440=CARTESIAN_POINT ( 'NONE',  ( 118.0718414775786442, -0.8288870151387760510, -10.36305467784173118 ) ) ;
#43441=CARTESIAN_POINT ( 'NONE',  ( 125.0492214775786266, -6.344957434206665248, -7.627207830600338134 ) ) ;
#43444=CARTESIAN_POINT ( 'NONE',  ( 115.7523666692504065, -2.311015703046737535, -18.04188382666267998 ) ) ;
#43446=CARTESIAN_POINT ( 'NONE',  ( 117.3343948109119737, -6.222761293078241884, -8.102969835052219238 ) ) ;
#43452=CARTESIAN_POINT ( 'NONE',  ( 122.5532481442453019, -10.63000616557722466, -14.87417383870573495 ) ) ;
#43453=CARTESIAN_POINT ( 'NONE',  ( 123.4041481442452834, 0.1319031606808879209, -14.10382304977623669 ) ) ;
#43455=FACE_OUTER_BOUND ( 'NONE', #43731, .T. ) ;
#43458=CARTESIAN_POINT ( 'NONE',  ( 124.4819548109119722, -2.084020599724406786, -8.691656652584148546 ) ) ;
#43459=CARTESIAN_POINT ( 'NONE',  ( 120.6245414775786458, -0.1624402480850797581, -16.17319339645315424 ) ) ;
#43460=CIRCLE ( 'NONE', #2658, 5.999999999999997335 ) ;
#43461=CARTESIAN_POINT ( 'NONE',  ( 119.7169148109119874, -0.1624402480850797581, -16.17319339645315424 ) ) ;
#43470=CARTESIAN_POINT ( 'NONE',  ( 120.3409081442453044, -0.4660016031367893996, -10.09054647747474043 ) ) ;
#43471=CARTESIAN_POINT ( 'NONE',  ( 118.8092881442453290, -9.988377603198976828, -10.36322818467138340 ) ) ;
#43473=CARTESIAN_POINT ( 'NONE',  ( 118.0151148109119816, -10.63000616557722466, -14.87417383870573495 ) ) ;
#43478=CARTESIAN_POINT ( 'NONE',  ( 121.3052614775786111, -1.834011780172310813, -8.268836392978581529 ) ) ;
#43479=CARTESIAN_POINT ( 'NONE',  ( 120.0572748109119772, -3.383040157471821630, -19.15922257007629170 ) ) ;
#43480=CARTESIAN_POINT ( 'NONE',  ( 125.2761281442453054, 0.4262465694468514643, -12.03445270309931736 ) ) ;
#43483=CARTESIAN_POINT ( 'NONE',  ( 113.7606148109119886, -7.894159318335828068, -9.358103419637847864 ) ) ;
#43484=CARTESIAN_POINT ( 'NONE',  ( 123.7445081442452874, -1.561330072975668948, -17.79121239304076951 ) ) ;
#43486=CARTESIAN_POINT ( 'NONE',  ( 119.2063748109119814, -7.894159318335828068, -9.358103419637847864 ) ) ;
#43492=CARTESIAN_POINT ( 'NONE',  ( 121.8725281442453223, -3.383040157471821630, -19.15922257007629170 ) ) ;
#43496=CARTESIAN_POINT ( 'NONE',  ( 119.5467348109119712, -5.574606645277164318, -18.38911715685844683 ) ) ;
#43497=CARTESIAN_POINT ( 'NONE',  ( 112.0588148109119828, 0.5811942927096154232, -14.16772938898807155 ) ) ;
#43500=CARTESIAN_POINT ( 'NONE',  ( 122.0994348109119443, -10.15424416112533912, -14.75197769757731336 ) ) ;
#43501=CARTESIAN_POINT ( 'NONE',  ( 123.3116793777725064, -1.267766418764731728, -16.93314635290706605 ) ) ;
#43502=CARTESIAN_POINT ( 'NONE',  ( 124.8790414775786246, -8.899110576539710493, -16.42337572283490132 ) ) ;
#43505=CARTESIAN_POINT ( 'NONE',  ( 122.9503348109119827, 0.5811942927096110934, -14.16772938898807510 ) ) ;
#43506=CARTESIAN_POINT ( 'NONE',  ( 118.0718414775786442, -0.8288870151387760510, -10.36305467784173118 ) ) ;
#43507=CARTESIAN_POINT ( 'NONE',  ( 122.4397948109119767, -0.1624402480850797581, -16.17319339645315424 ) ) ;
#43509=CARTESIAN_POINT ( 'NONE',  ( 121.9292548109119849, -1.561330072975668948, -17.79121239304076951 ) ) ;
#43510=CARTESIAN_POINT ( 'NONE',  ( 116.5969481442453031, 0.5811942927096154232, -14.16772938898807155 ) ) ;
#43511=CARTESIAN_POINT ( 'NONE',  ( 113.6932004811916954, -3.807985514183293230, -19.09877912889401230 ) ) ;
#43512=CARTESIAN_POINT ( 'NONE',  ( 125.3895814775786448, -2.084020599724406786, -8.691656652584148546 ) ) ;
#43513=CARTESIAN_POINT ( 'NONE',  ( 121.6456214775786293, -10.63000616557722466, -14.87417383870573495 ) ) ;
#43517=CARTESIAN_POINT ( 'NONE',  ( 112.7395348109119766, -4.153390946401321671, -8.397313243818183892 ) ) ;
#43519=CARTESIAN_POINT ( 'NONE',  ( 124.5954081442453116, -3.383040157471821630, -19.15922257007629170 ) ) ;
#43521=CARTESIAN_POINT ( 'NONE',  ( 124.7088614775786226, -9.565557343593413364, -10.61323700422348004 ) ) ;
#43527=CARTESIAN_POINT ( 'NONE',  ( 119.2631014775786298, 0.2603800115204892296, -16.42320221600525088 ) ) ;
#43528=CARTESIAN_POINT ( 'NONE',  ( 113.2500748109119968, -6.344957434206662583, -7.627207830600333693 ) ) ;
#43529=CARTESIAN_POINT ( 'NONE',  ( 122.9503348109119827, -9.859900752359378018, -12.68260735090039759 ) ) ;
#43530=CARTESIAN_POINT ( 'NONE',  ( 116.2565881442453133, -0.8288870151387760510, -10.36305467784173118 ) ) ;
#43532=CARTESIAN_POINT ( 'NONE',  ( 124.3685014775786186, -10.63000616557722999, -14.87417383870572962 ) ) ;
#43533=CARTESIAN_POINT ( 'NONE',  ( 115.9729548109119861, -6.344957434206662583, -7.627207830600332805 ) ) ;
#43536=CIRCLE ( 'NONE', #37710, 4.999999999999998224 ) ;
#43537=CARTESIAN_POINT ( 'NONE',  ( 125.6732148109119862, 0.5811942927096110934, -14.16772938898807510 ) ) ;
#43540=CARTESIAN_POINT ( 'NONE',  ( 115.9162281442453235, -4.089484607189486809, -7.948022111789456723 ) ) ;
#43541=CARTESIAN_POINT ( 'NONE',  ( 112.8529881442453160, -7.894159318335828068, -9.358103419637847864 ) ) ;
#43543=CARTESIAN_POINT ( 'NONE',  ( 113.3635281442453504, -9.988377603198976828, -10.36322818467138340 ) ) ;
#43545=CARTESIAN_POINT ( 'NONE',  ( 117.7314814775786260, -4.089484607189486809, -7.948022111789456723 ) ) ;
#43546=ADVANCED_FACE ( 'NONE', ( #29012 ), #23096, .T. ) ;
#43551=CARTESIAN_POINT ( 'NONE',  ( 113.3635281442453504, -0.1624402480850797581, -16.17319339645315424 ) ) ;
#43554=CARTESIAN_POINT ( 'NONE',  ( 113.3068014775786594, -1.833838273342658809, -17.42832698103878286 ) ) ;
#43555=CARTESIAN_POINT ( 'NONE',  ( 125.5030348109119558, -6.222761293078241884, -8.102969835052219238 ) ) ;
#43557=CARTESIAN_POINT ( 'NONE',  ( 126.6375681442452930, -10.15424416112533912, -14.75197769757731336 ) ) ;
#43558=CARTESIAN_POINT ( 'NONE',  ( 112.9097148109120070, -9.565557343593413364, -10.61323700422348004 ) ) ;
#43559=CARTESIAN_POINT ( 'NONE',  ( 121.9292548109119849, -1.561330072975668948, -17.79121239304076951 ) ) ;
#43560=CARTESIAN_POINT ( 'NONE',  ( 122.7234281442452755, -5.638512984488999180, -18.83840828888717311 ) ) ;
#43562=CARTESIAN_POINT ( 'NONE',  ( 126.3243314201126850, -8.659408885743252071, -16.72895926446462411 ) ) ;
#43566=CARTESIAN_POINT ( 'NONE',  ( 128.2184548109119930, -10.36826876090625760, -11.00511718064540467 ) ) ;
#43567=CARTESIAN_POINT ( 'NONE',  ( 115.1787814775786387, -9.988377603198976828, -10.36322818467138340 ) ) ;
#43572=CARTESIAN_POINT ( 'NONE',  ( 112.6260814775786514, -0.8288870151387760510, -10.36305467784173118 ) ) ;
#43573=CARTESIAN_POINT ( 'NONE',  ( 123.2697102440515238, -2.467220198592778413, -17.83387418641524391 ) ) ;
#43574=CARTESIAN_POINT ( 'NONE',  ( 118.2420214775786320, -3.383040157471821630, -19.15922257007629170 ) ) ;
#43576=CARTESIAN_POINT ( 'NONE',  ( 119.4944236525450236, -2.378957183258601393, -17.95140958770220152 ) ) ;
#43579=CARTESIAN_POINT ( 'NONE',  ( 118.2420214775786320, -6.222761293078241884, -8.102969835052219238 ) ) ;
#43580=CARTESIAN_POINT ( 'NONE',  ( 116.5402214775786405, 0.2603800115204892296, -16.42320221600525088 ) ) ;
#43581=CARTESIAN_POINT ( 'NONE',  ( 114.7816948109119863, -9.859900752359374465, -12.68260735090039404 ) ) ;
#43582=CARTESIAN_POINT ( 'NONE',  ( 114.2144281442453178, -8.166667518702817929, -8.995218007635859436 ) ) ;
#43583=CYLINDRICAL_SURFACE ( 'NONE', #7449, 4.999999999999998224 ) ;
#43584=CARTESIAN_POINT ( 'NONE',  ( 122.3830681442452857, -1.833838273342659697, -17.42832698103878286 ) ) ;
#43585=CARTESIAN_POINT ( 'NONE',  ( 120.8514481442452961, -2.084020599724406786, -8.691656652584148546 ) ) ;
#43588=CARTESIAN_POINT ( 'NONE',  ( 112.7395348109119766, -5.638512984488999180, -18.83840828888717311 ) ) ;
#43589=CARTESIAN_POINT ( 'NONE',  ( 122.9503348109119827, -9.859900752359378018, -12.68260735090039759 ) ) ;
#43590=ORIENTED_EDGE ( 'NONE', *, *, #35896, .T. ) ;
#43592=CARTESIAN_POINT ( 'NONE',  ( 116.6536748109119941, 0.9020085738987339008, -11.91225656197089222 ) ) ;
#43594=CARTESIAN_POINT ( 'NONE',  ( 115.1787814775786387, -0.1624402480850797581, -16.17319339645315424 ) ) ;
#43597=CARTESIAN_POINT ( 'NONE',  ( 123.5743281442453139, -2.084020599724406786, -8.691656652584148546 ) ) ;
#43599=CARTESIAN_POINT ( 'NONE',  ( 119.3198281442452924, -9.859900752359374465, -12.68260735090039404 ) ) ;
#43605=CARTESIAN_POINT ( 'NONE',  ( 115.2922348109119781, -10.63000616557722466, -14.87417383870573495 ) ) ;
#43606=CARTESIAN_POINT ( 'NONE',  ( 114.7816948109119863, 0.5811942927096154232, -14.16772938898807155 ) ) ;
#43607=CARTESIAN_POINT ( 'NONE',  ( 117.6747548109119919, -7.643976991954077427, -18.09477374809248928 ) ) ;
#43609=CARTESIAN_POINT ( 'NONE',  ( 120.4543614775786295, -5.574606645277164318, -18.38911715685844683 ) ) ;
#43610=CARTESIAN_POINT ( 'NONE',  ( 111.8886348109120092, -3.383040157471821630, -19.15922257007629170 ) ) ;
#43612=CARTESIAN_POINT ( 'NONE',  ( 118.5823814775786360, -7.643976991954077427, -18.09477374809248928 ) ) ;
#43618=CARTESIAN_POINT ( 'NONE',  ( 117.4478481442453131, 0.2603800115204892296, -16.42320221600525088 ) ) ;
#43620=CARTESIAN_POINT ( 'NONE',  ( 121.0216281442452981, -1.561330072975668948, -17.79121239304076951 ) ) ;
#43621=CARTESIAN_POINT ( 'NONE',  ( 115.4833430939976893, -2.236191541394345172, -18.14152338500401029 ) ) ;
#43623=CARTESIAN_POINT ( 'NONE',  ( 118.5256548109119876, -0.4660016031367893996, -10.09054647747474043 ) ) ;
#43624=CARTESIAN_POINT ( 'NONE',  ( 116.3700414775786527, -5.638512984488999180, -18.83840828888717311 ) ) ;
#43630=CARTESIAN_POINT ( 'NONE',  ( 121.3619881442452879, -5.574606645277164318, -18.38911715685844683 ) ) ;
#43633=CARTESIAN_POINT ( 'NONE',  ( 118.6958348109119754, -3.505236298600246325, -18.68346056562440793 ) ) ;
#43637=CARTESIAN_POINT ( 'NONE',  ( 112.8529881442453160, -7.894159318335828068, -9.358103419637847864 ) ) ;
#43638=CARTESIAN_POINT ( 'NONE',  ( 124.7088614775786226, 0.2603800115204892296, -16.42320221600525088 ) ) ;
#43640=CARTESIAN_POINT ( 'NONE',  ( 117.3911214775786505, -7.894159318335828068, -9.358103419637847864 ) ) ;
#43641=CARTESIAN_POINT ( 'NONE',  ( 114.2144281442453178, -8.166667518702817929, -8.995218007635859436 ) ) ;
#43642=CARTESIAN_POINT ( 'NONE',  ( 121.0783548109119749, 0.2603800115204892296, -16.42320221600525088 ) ) ;
#43643=CARTESIAN_POINT ( 'NONE',  ( 122.9503348109119827, -9.859900752359378018, -12.68260735090039759 ) ) ;
#43646=CARTESIAN_POINT ( 'NONE',  ( 124.3117748109119844, -10.30919188438810075, -12.61870101168855918 ) ) ;
#43647=CARTESIAN_POINT ( 'NONE',  ( 112.7395348109119766, -4.153390946401321671, -8.397313243818183892 ) ) ;
#43648=CARTESIAN_POINT ( 'NONE',  ( 124.0281414775786146, -1.834011780172310813, -8.268836392978581529 ) ) ;
#43651=CARTESIAN_POINT ( 'NONE',  ( 138.2184548109120499, -2.342207185915014644, -15.50236782978752537 ) ) ;
#43656=CARTESIAN_POINT ( 'NONE',  ( 136.7036351579054383, -10.11817554825837639, -11.31345360030072023 ) ) ;
#43657=CARTESIAN_POINT ( 'NONE',  ( 120.2274548109119934, -9.859900752359374465, -12.68260735090039404 ) ) ;
#43658=CARTESIAN_POINT ( 'NONE',  ( 125.3328548109119964, -9.261995988541697145, -16.69588392320189030 ) ) ;
#43663=CARTESIAN_POINT ( 'NONE',  ( 116.1431348109119881, 0.1319031606808879209, -14.10382304977623669 ) ) ;
#43669=CARTESIAN_POINT ( 'NONE',  ( 121.9292548109119849, -1.561330072975668948, -17.79121239304076951 ) ) ;
#43670=CARTESIAN_POINT ( 'NONE',  ( 123.7445081442452874, -7.894159318335828068, -9.358103419637847864 ) ) ;
#43671=ORIENTED_EDGE ( 'NONE', *, *, #5904, .F. ) ;
#43675=CARTESIAN_POINT ( 'NONE',  ( 121.3619881442452879, -5.574606645277164318, -18.38911715685844683 ) ) ;
#43676=CARTESIAN_POINT ( 'NONE',  ( 121.4187148109119789, -3.505236298600246325, -18.68346056562440793 ) ) ;
#43677=CARTESIAN_POINT ( 'NONE',  ( 119.6811727111058588, -1.267766418764730840, -16.93314635290706605 ) ) ;
#43686=CARTESIAN_POINT ( 'NONE',  ( 121.7023481442452777, -9.261995988541697145, -16.69588392320189030 ) ) ;
#43687=CARTESIAN_POINT ( 'NONE',  ( 122.7234281442452755, -5.638512984488999180, -18.83840828888717311 ) ) ;
#43689=CARTESIAN_POINT ( 'NONE',  ( 115.1787814775786387, -9.988377603198976828, -10.36322818467138340 ) ) ;
#43695=CARTESIAN_POINT ( 'NONE',  ( 121.2485348109119769, -0.4660016031367893996, -10.09054647747474043 ) ) ;
#43696=CARTESIAN_POINT ( 'NONE',  ( 119.9438214775786378, -7.893985811506177619, -18.51759400769804742 ) ) ;
#43698=CARTESIAN_POINT ( 'NONE',  ( 126.5241148109119393, -9.565557343593413364, -10.61323700422348004 ) ) ;
#43700=CARTESIAN_POINT ( 'NONE',  ( 112.5693548109119888, 0.4262465694468514643, -12.03445270309931736 ) ) ;
#43701=CARTESIAN_POINT ( 'NONE',  ( 112.9664414775786412, -9.859900752359374465, -12.68260735090039404 ) ) ;
#43702=CARTESIAN_POINT ( 'NONE',  ( 124.3685014775786328, -10.63000616557722466, -14.87417383870573495 ) ) ;
#43706=CARTESIAN_POINT ( 'NONE',  ( 120.0005481442453146, -4.153390946401325223, -8.397313243818185668 ) ) ;
#43713=CARTESIAN_POINT ( 'NONE',  ( 124.0848681442452772, -4.089484607189486809, -7.948022111789456723 ) ) ;
#43719=CARTESIAN_POINT ( 'NONE',  ( 119.4900081442453086, -7.643976991954077427, -18.09477374809248928 ) ) ;
#43723=CARTESIAN_POINT ( 'NONE',  ( 123.1772414775786189, -5.574606645277164318, -18.38911715685844683 ) ) ;
#43725=CARTESIAN_POINT ( 'NONE',  ( 123.5176014775786228, -0.8288870151387760510, -10.36305467784173118 ) ) ;
#43728=CARTESIAN_POINT ( 'NONE',  ( 125.2194014775786286, -10.30919188438810075, -12.61870101168855918 ) ) ;
#43729=CARTESIAN_POINT ( 'NONE',  ( 118.3554748109119998, -9.565557343593413364, -10.61323700422348004 ) ) ;
#43730=CARTESIAN_POINT ( 'NONE',  ( 125.7299414775786346, -10.15424416112533912, -14.75197769757731336 ) ) ;
#43731=EDGE_LOOP ( 'NONE', ( #29017, #21269, #43671, #44045 ) ) ;
#43732=CARTESIAN_POINT ( 'NONE',  ( 124.7088614775786226, 0.2603800115204892296, -16.42320221600525088 ) ) ;
#43733=CARTESIAN_POINT ( 'NONE',  ( 113.9307948109119906, 0.9020085738987339008, -11.91225656197089222 ) ) ;
#43735=CARTESIAN_POINT ( 'NONE',  ( 138.2184548109119930, -11.79424454490141017, -12.40746986932944473 ) ) ;
#43736=CARTESIAN_POINT ( 'NONE',  ( 124.9357681442453014, -7.643976991954077427, -18.09477374809248928 ) ) ;
#43737=CARTESIAN_POINT ( 'NONE',  ( 123.2339681442453241, -6.344957434206665248, -7.627207830600338134 ) ) ;
#43748=CARTESIAN_POINT ( 'NONE',  ( 123.7445081442452874, -7.894159318335828068, -9.358103419637847864 ) ) ;
#43757=CARTESIAN_POINT ( 'NONE',  ( 119.7169148109119874, -9.988377603198976828, -10.36322818467138340 ) ) ;
#43758=CARTESIAN_POINT ( 'NONE',  ( 124.4819548109119722, -2.084020599724406786, -8.691656652584148546 ) ) ;
#43759=CARTESIAN_POINT ( 'NONE',  ( 115.4056881442453459, -2.084020599724406786, -8.691656652584148546 ) ) ;
#43760=CARTESIAN_POINT ( 'NONE',  ( 116.2443561498677269, -2.324775150319240868, -18.02356106541842351 ) ) ;
#43761=CARTESIAN_POINT ( 'NONE',  ( 114.8056076054816259, -2.287189184988692059, -18.07361239780447448 ) ) ;
#43762=CARTESIAN_POINT ( 'NONE',  ( 115.1220548109119761, -8.166667518702817929, -8.995218007635861213 ) ) ;
#43765=CARTESIAN_POINT ( 'NONE',  ( 124.5386814775786206, -5.638512984488999180, -18.83840828888717311 ) ) ;
#43768=CARTESIAN_POINT ( 'NONE',  ( 116.0864081442453113, -9.988377603198976828, -10.36322818467138340 ) ) ;
#43769=CARTESIAN_POINT ( 'NONE',  ( 114.0442481442453300, -7.643976991954077427, -18.09477374809248928 ) ) ;
#43771=CARTESIAN_POINT ( 'NONE',  ( 112.2857214775786474, -4.089484607189486809, -7.948022111789456723 ) ) ;
#43774=CARTESIAN_POINT ( 'NONE',  ( 122.8936081442453059, 0.2603800115204892296, -16.42320221600525088 ) ) ;
#43779=CARTESIAN_POINT ( 'NONE',  ( 137.0596819398155617, -3.051825027028553627, -8.284924315246177784 ) ) ;
#43780=CARTESIAN_POINT ( 'NONE',  ( 114.1577014775786552, -3.505236298600246325, -18.68346056562440793 ) ) ;
#43783=CARTESIAN_POINT ( 'NONE',  ( 112.7395348109119766, -4.153390946401321671, -8.397313243818183892 ) ) ;
#43784=CARTESIAN_POINT ( 'NONE',  ( 113.5904348109119866, -7.893985811506177619, -18.51759400769804742 ) ) ;
#43786=CARTESIAN_POINT ( 'NONE',  ( 112.6260814775786514, -9.261995988541697145, -16.69588392320189030 ) ) ;
#43787=CARTESIAN_POINT ( 'NONE',  ( 114.5547881442453217, -4.153390946401321671, -8.397313243818183892 ) ) ;
#43788=CARTESIAN_POINT ( 'NONE',  ( 122.7801548109119665, -3.383040157471821630, -19.15922257007629170 ) ) ;
#43790=CARTESIAN_POINT ( 'NONE',  ( 123.3474214775786209, -9.988377603198976828, -10.36322818467138340 ) ) ;
#43792=CARTESIAN_POINT ( 'NONE',  ( 113.8173414775786512, 0.2603800115204892296, -16.42320221600525088 ) ) ;
#43798=CARTESIAN_POINT ( 'NONE',  ( 119.2631014775786298, 0.2603800115204892296, -16.42320221600525088 ) ) ;
#43803=CARTESIAN_POINT ( 'NONE',  ( 113.3635281442453504, -0.1624402480850797581, -16.17319339645315424 ) ) ;
#43805=CARTESIAN_POINT ( 'NONE',  ( 120.6245414775786458, -9.988377603198976828, -10.36322818467138340 ) ) ;
#43811=CARTESIAN_POINT ( 'NONE',  ( 121.1918081442452859, -10.15424416112533912, -14.75197769757731336 ) ) ;
#43812=CARTESIAN_POINT ( 'NONE',  ( 118.1852948109119836, -5.638512984488999180, -18.83840828888717311 ) ) ;
#43813=CARTESIAN_POINT ( 'NONE',  ( 114.6682414775786469, -7.894159318335828068, -9.358103419637847864 ) ) ;
#43814=CARTESIAN_POINT ( 'NONE',  ( 115.8595014775786609, -1.834011780172310813, -8.268836392978581529 ) ) ;
#43817=CARTESIAN_POINT ( 'NONE',  ( 122.8368814775786291, -7.894159318335828068, -9.358103419637847864 ) ) ;
#43818=CARTESIAN_POINT ( 'NONE',  ( 118.5823814775786360, -7.643976991954077427, -18.09477374809248928 ) ) ;
#43822=CARTESIAN_POINT ( 'NONE',  ( 112.1722681442453222, -0.4660016031367893996, -10.09054647747474043 ) ) ;
#43823=CARTESIAN_POINT ( 'NONE',  ( 120.5110881442453206, -3.505236298600246325, -18.68346056562440793 ) ) ;
#43826=CARTESIAN_POINT ( 'NONE',  ( 118.0718414775786300, -9.261995988541697145, -16.69588392320189030 ) ) ;
#43828=CARTESIAN_POINT ( 'NONE',  ( 115.2355081442453155, 0.1319031606808879209, -14.10382304977623669 ) ) ;
#43832=CARTESIAN_POINT ( 'NONE',  ( 124.7655881442452852, -9.859900752359378018, -12.68260735090039759 ) ) ;
#43833=CARTESIAN_POINT ( 'NONE',  ( 119.4332814775786318, -8.899110576539710493, -16.42337572283490132 ) ) ;
#43836=CARTESIAN_POINT ( 'NONE',  ( 119.4332814775786318, -0.4660016031367893996, -10.09054647747474043 ) ) ;
#43839=CARTESIAN_POINT ( 'NONE',  ( 117.3343948109119737, -3.383040157471821630, -19.15922257007629170 ) ) ;
#43840=CARTESIAN_POINT ( 'NONE',  ( 116.7671281442453335, -1.834011780172310813, -8.268836392978581529 ) ) ;
#43841=CARTESIAN_POINT ( 'NONE',  ( 116.1998614775786507, 0.4262465694468514643, -12.03445270309931736 ) ) ;
#43842=CARTESIAN_POINT ( 'NONE',  ( 125.1626748109119802, -0.1624402480850797581, -16.17319339645315424 ) ) ;
#43843=CARTESIAN_POINT ( 'NONE',  ( 113.8173414775786512, 0.2603800115204892296, -16.42320221600525088 ) ) ;
#43845=CARTESIAN_POINT ( 'NONE',  ( 123.1205148109119563, -7.643976991954077427, -18.09477374809248928 ) ) ;
#43846=CARTESIAN_POINT ( 'NONE',  ( 138.2184548109119930, -5.044325091639137781, -11.90409383958792411 ) ) ;
#43851=CARTESIAN_POINT ( 'NONE',  ( 118.9794681442453026, -9.261995988541697145, -16.69588392320189030 ) ) ;
#43853=CARTESIAN_POINT ( 'NONE',  ( 120.4543614775786295, -4.089484607189486809, -7.948022111789456723 ) ) ;
#43854=CARTESIAN_POINT ( 'NONE',  ( 112.7395348109119766, -4.153390946401321671, -8.397313243818183892 ) ) ;
#43856=CARTESIAN_POINT ( 'NONE',  ( 120.0572748109119772, -3.383040157471821630, -19.15922257007629170 ) ) ;
#43857=CARTESIAN_POINT ( 'NONE',  ( 121.6456214775786293, -10.63000616557722466, -14.87417383870573495 ) ) ;
#43860=VERTEX_POINT ( 'NONE', #44172 ) ;
#43864=CARTESIAN_POINT ( 'NONE',  ( 122.6099748109119929, -0.8288870151387760510, -10.36305467784173118 ) ) ;
#43868=CARTESIAN_POINT ( 'NONE',  ( 116.5969481442453031, -9.859900752359374465, -12.68260735090039404 ) ) ;
#43871=CARTESIAN_POINT ( 'NONE',  ( 111.5482748109120053, -0.1624402480850797581, -16.17319339645315424 ) ) ;
#43872=CARTESIAN_POINT ( 'NONE',  ( 124.1983214775786166, -8.166667518702819706, -8.995218007635861213 ) ) ;
#43873=VERTEX_POINT ( 'NONE', #33645 ) ;
#43874=CARTESIAN_POINT ( 'NONE',  ( 122.5532481442453019, 0.4262465694468514643, -12.03445270309931736 ) ) ;
#43876=CARTESIAN_POINT ( 'NONE',  ( 116.6536748109119941, 0.9020085738987339008, -11.91225656197089222 ) ) ;
#43877=CARTESIAN_POINT ( 'NONE',  ( 122.5532481442453019, -10.63000616557722466, -14.87417383870573495 ) ) ;
#43878=CARTESIAN_POINT ( 'NONE',  ( 121.7590748109119687, -2.084020599724406786, -8.691656652584148546 ) ) ;
#43881=CARTESIAN_POINT ( 'NONE',  ( 124.2550481442452792, -9.988377603198980381, -10.36322818467138518 ) ) ;
#43883=CARTESIAN_POINT ( 'NONE',  ( 112.9664414775786412, -9.859900752359374465, -12.68260735090039404 ) ) ;
#43884=CARTESIAN_POINT ( 'NONE',  ( 111.8886348109120092, -6.222761293078241884, -8.102969835052219238 ) ) ;
#43888=CARTESIAN_POINT ( 'NONE',  ( 127.9519950909192261, -3.021983423502168087, -14.59726296296260273 ) ) ;
#43892=CARTESIAN_POINT ( 'NONE',  ( 120.7379948109119709, 0.4262465694468514643, -12.03445270309931736 ) ) ;
#43893=CARTESIAN_POINT ( 'NONE',  ( 111.4915481442453142, -1.833838273342658365, -17.42832698103878286 ) ) ;
#43894=CARTESIAN_POINT ( 'NONE',  ( 125.6164881442453094, -9.565557343593397377, -10.61323700422345695 ) ) ;
#43897=( GEOMETRIC_REPRESENTATION_CONTEXT ( 3 ) GLOBAL_UNCERTAINTY_ASSIGNED_CONTEXT ( ( #28784 ) ) GLOBAL_UNIT_ASSIGNED_CONTEXT ( ( #24795, #31629, #41912 ) ) REPRESENTATION_CONTEXT ( 'NONE', 'WORKASPACE' ) );
#43898=CARTESIAN_POINT ( 'NONE',  ( 117.8449348109119938, -1.833838273342659253, -17.42832698103878286 ) ) ;
#43899=CARTESIAN_POINT ( 'NONE',  ( 113.4769814775786330, 0.4262465694468514643, -12.03445270309931736 ) ) ;
#43903=CARTESIAN_POINT ( 'NONE',  ( 123.5743281442453139, -7.893985811506177619, -18.51759400769804742 ) ) ;
#43904=CARTESIAN_POINT ( 'NONE',  ( 122.2696148109119889, -5.574606645277164318, -18.38911715685844683 ) ) ;
#43907=CARTESIAN_POINT ( 'NONE',  ( 126.2758031835812744, 0.06624046018700967264, -14.38341065059502455 ) ) ;
#43909=CARTESIAN_POINT ( 'NONE',  ( 120.7379948109119709, 0.4262465694468514643, -12.03445270309931736 ) ) ;
#43910=CARTESIAN_POINT ( 'NONE',  ( 119.6034614775786196, -3.505236298600246325, -18.68346056562440793 ) ) ;
#43911=CARTESIAN_POINT ( 'NONE',  ( 119.2988998611595832, -1.036737761566197014, -17.24079555149560861 ) ) ;
#43913=CARTESIAN_POINT ( 'NONE',  ( 116.7671281442453193, -1.834011780172314143, -8.268836392978577976 ) ) ;
#43915=CARTESIAN_POINT ( 'NONE',  ( 112.3991748109119868, -1.833838273342658809, -17.42832698103878286 ) ) ;
#43919=CARTESIAN_POINT ( 'NONE',  ( 120.2274548109119934, 0.5811942927096110934, -14.16772938898807510 ) ) ;
#43920=CARTESIAN_POINT ( 'NONE',  ( 122.6667014775786413, -7.893985811506177619, -18.51759400769804742 ) ) ;
#43922=CARTESIAN_POINT ( 'NONE',  ( 117.3911214775786505, -1.561330072975668504, -17.79121239304076951 ) ) ;
#43923=CARTESIAN_POINT ( 'NONE',  ( 112.1155414775786454, 0.9020085738987339008, -11.91225656197089222 ) ) ;
#43927=CARTESIAN_POINT ( 'NONE',  ( 111.3780948109119890, -5.574606645277164318, -18.38911715685844683 ) ) ;
#43929=CARTESIAN_POINT ( 'NONE',  ( 121.7023481442452777, -9.261995988541697145, -16.69588392320189030 ) ) ;
#43930=CARTESIAN_POINT ( 'NONE',  ( 111.7751814775786556, -7.893985811506177619, -18.51759400769804742 ) ) ;
#43932=CARTESIAN_POINT ( 'NONE',  ( 114.2711548109119803, -0.1624402480850797581, -16.17319339645315424 ) ) ;
#43934=CARTESIAN_POINT ( 'NONE',  ( 117.9583881442453048, 0.1319031606808879209, -14.10382304977623669 ) ) ;
#43935=CARTESIAN_POINT ( 'NONE',  ( 124.1415948109119540, -6.344957434206665248, -7.627207830600338134 ) ) ;
#43938=CARTESIAN_POINT ( 'NONE',  ( 121.3052614775786111, -7.643976991954077427, -18.09477374809248928 ) ) ;
#43940=FACE_OUTER_BOUND ( 'NONE', #35593, .T. ) ;
#43943=CARTESIAN_POINT ( 'NONE',  ( 124.3685014775786328, -10.63000616557722466, -14.87417383870573495 ) ) ;
#43951=CARTESIAN_POINT ( 'NONE',  ( 125.0492214775786266, -3.505236298600246325, -18.68346056562440793 ) ) ;
#43955=CARTESIAN_POINT ( 'NONE',  ( 117.9016614775786280, -0.1624402480850797581, -16.17319339645315424 ) ) ;
#43958=CARTESIAN_POINT ( 'NONE',  ( 123.2339681442453241, -6.344957434206665248, -7.627207830600338134 ) ) ;
#43959=CARTESIAN_POINT ( 'NONE',  ( 115.2922348109119781, -10.63000616557722466, -14.87417383870573495 ) ) ;
#43962=CARTESIAN_POINT ( 'NONE',  ( 123.4041481442452834, 0.1319031606808879209, -14.10382304977623669 ) ) ;
#43963=CARTESIAN_POINT ( 'NONE',  ( 124.5954081442453116, -3.383040157471821630, -19.15922257007629170 ) ) ;
#43968=CARTESIAN_POINT ( 'NONE',  ( 117.1642148109119859, -0.8288870151387760510, -10.36305467784173118 ) ) ;
#43969=CARTESIAN_POINT ( 'NONE',  ( 114.9518748109119883, -7.643976991954077427, -18.09477374809248928 ) ) ;
#43973=FACE_OUTER_BOUND ( 'NONE', #6904, .T. ) ;
#43974=CARTESIAN_POINT ( 'NONE',  ( 126.3539348109119800, -4.153390946401325223, -8.397313243818185668 ) ) ;
#43982=CARTESIAN_POINT ( 'NONE',  ( 120.2274548109119934, 0.5811942927096110934, -14.16772938898807510 ) ) ;
#43983=CARTESIAN_POINT ( 'NONE',  ( 125.7866681442452688, -8.899110576539710493, -16.42337572283490132 ) ) ;
#43984=CARTESIAN_POINT ( 'NONE',  ( 114.7249681442453237, -9.565557343593413364, -10.61323700422348004 ) ) ;
#43986=CARTESIAN_POINT ( 'NONE',  ( 124.3117748109119844, -10.30919188438810075, -12.61870101168855918 ) ) ;
#43988=CARTESIAN_POINT ( 'NONE',  ( 115.0653281442453277, -6.344957434206662583, -7.627207830600332805 ) ) ;
#43989=B_SPLINE_CURVE_WITH_KNOTS ( 'NONE', 3,
 ( #24915, #42477, #10791, #21270, #31750, #7579, #37927, #28122, #20615, #14428, #38577, #6921, #35152, #20828, #17850, #73, #21493, #28338, #42251, #38360, #11014, #4157, #34490, #25811, #29234, #39271, #1627, #8033, #18525, #35831 ),
 .UNSPECIFIED., .F., .F.,
 ( 4, 2, 2, 1, 2, 2, 2, 1, 1, 2, 2, 2, 1, 1, 1, 2, 2, 4 ),
 ( 0.000000000000000000, 0.03125000000001906114, 0.06250000000003812228, 0.09375000000005717649, 0.1093750000000654754, 0.1250000000000737743, 0.1875000000000648370, 0.2187500000000515976, 0.2343750000000364708, 0.2421875000000286438, 0.2500000000000208167, 0.3749999999999322209, 0.4374999999998873679, 0.4687499999998644973, 0.4843749999998639977, 0.4921874999998633871, 0.4999999999998627764, 1.000000000000000000 ),
 .UNSPECIFIED. ) ;
#43993=CARTESIAN_POINT ( 'NONE',  ( 123.6310548109119765, -5.638512984488999180, -18.83840828888717311 ) ) ;
#43995=CARTESIAN_POINT ( 'NONE',  ( 113.4202548109119846, -10.30919188438810075, -12.61870101168855918 ) ) ;
#43996=CARTESIAN_POINT ( 'NONE',  ( 114.1577014775786552, -3.505236298600246325, -18.68346056562440793 ) ) ;
#43997=EDGE_CURVE ( 'NONE', #18302, #36520, #8519, .T. ) ;
#43999=CARTESIAN_POINT ( 'NONE',  ( 112.6260814775786514, -9.261995988541697145, -16.69588392320189030 ) ) ;
#44001=CARTESIAN_POINT ( 'NONE',  ( 122.8368814775786291, -1.561330072975668948, -17.79121239304076951 ) ) ;
#44008=CARTESIAN_POINT ( 'NONE',  ( 135.3184548109119874, -2.475900776146298110, -7.888945235271312306 ) ) ;
#44009=CARTESIAN_POINT ( 'NONE',  ( 112.5693548109119888, 0.4262465694468514643, -12.03445270309931736 ) ) ;
#44012=CARTESIAN_POINT ( 'NONE',  ( 115.2355081442453155, 0.1319031606808879209, -14.10382304977623669 ) ) ;
#44013=CARTESIAN_POINT ( 'NONE',  ( 114.9518748109119883, -1.834011780172310813, -8.268836392978581529 ) ) ;
#44015=CARTESIAN_POINT ( 'NONE',  ( 125.8433948109119456, -7.643976991954077427, -18.09477374809248928 ) ) ;
#44016=CARTESIAN_POINT ( 'NONE',  ( 114.1577014775786552, -3.505236298600246325, -18.68346056562440793 ) ) ;
#44017=CARTESIAN_POINT ( 'NONE',  ( 122.4965214775786251, -10.30919188438810075, -12.61870101168855918 ) ) ;
#44019=CARTESIAN_POINT ( 'NONE',  ( 121.7590748109119687, -7.893985811506177619, -18.51759400769804742 ) ) ;
#44021=CARTESIAN_POINT ( 'NONE',  ( 111.8319081442453182, -5.638512984488999180, -18.83840828888717311 ) ) ;
#44025=CARTESIAN_POINT ( 'NONE',  ( 128.2184548109119930, -3.719473736431747390, -16.16631137400202078 ) ) ;
#44026=CARTESIAN_POINT ( 'NONE',  ( 117.3911214775786505, -1.561330072975668504, -17.79121239304076951 ) ) ;
#44031=CARTESIAN_POINT ( 'NONE',  ( 114.6115148109119986, -6.222761293078241884, -8.102969835052219238 ) ) ;
#44033=CARTESIAN_POINT ( 'NONE',  ( 119.3765548109119834, 0.9020085738987339008, -11.91225656197089222 ) ) ;
#44036=ORIENTED_EDGE ( 'NONE', *, *, #31181, .T. ) ;
#44038=CARTESIAN_POINT ( 'NONE',  ( 123.4041481442452834, 0.1319031606808879209, -14.10382304977623669 ) ) ;
#44039=CARTESIAN_POINT ( 'NONE',  ( 120.9081748109119872, -5.638512984488999180, -18.83840828888717311 ) ) ;
#44040=CARTESIAN_POINT ( 'NONE',  ( 112.9097148109120070, -9.565557343593413364, -10.61323700422348004 ) ) ;
#44041=CARTESIAN_POINT ( 'NONE',  ( 115.8027748109119841, -0.4660016031367893996, -10.09054647747474043 ) ) ;
#44043=CARTESIAN_POINT ( 'NONE',  ( 127.1653849502244782, -1.265433638251248327, -9.268909183209913749 ) ) ;
#44044=CARTESIAN_POINT ( 'NONE',  ( 118.9794681442453026, -0.8288870151387760510, -10.36305467784173118 ) ) ;
#44045=ORIENTED_EDGE ( 'NONE', *, *, #10407, .T. ) ;
#44046=EDGE_CURVE ( 'NONE', #20392, #40242, #12162, .T. ) ;
#44048=CARTESIAN_POINT ( 'NONE',  ( 119.3198281442452924, 0.5811942927096084288, -14.16772938898808931 ) ) ;
#44049=CARTESIAN_POINT ( 'NONE',  ( 114.6115148109119986, -3.383040157471821630, -19.15922257007629170 ) ) ;
#44050=CARTESIAN_POINT ( 'NONE',  ( 119.5467348109119712, -5.574606645277164318, -18.38911715685844683 ) ) ;
#44053=CARTESIAN_POINT ( 'NONE',  ( 117.9016614775786280, -9.988377603198976828, -10.36322818467138340 ) ) ;
#44056=CARTESIAN_POINT ( 'NONE',  ( 114.7816948109119863, -9.859900752359374465, -12.68260735090039404 ) ) ;
#44059=CARTESIAN_POINT ( 'NONE',  ( 125.3895814775786448, -2.084020599724406786, -8.691656652584148546 ) ) ;
#44060=CARTESIAN_POINT ( 'NONE',  ( 122.0427081442452817, -9.859900752359378018, -12.68260735090039759 ) ) ;
#44064=CARTESIAN_POINT ( 'NONE',  ( 119.1496481442453046, -3.383040157471821630, -19.15922257007629170 ) ) ;
#44067=CARTESIAN_POINT ( 'NONE',  ( 119.3765548109119834, 0.9020085738987339008, -11.91225656197089222 ) ) ;
#44068=CARTESIAN_POINT ( 'NONE',  ( 116.4834948109119779, -1.561330072975668504, -17.79121239304076951 ) ) ;
#44069=CARTESIAN_POINT ( 'NONE',  ( 117.1074881442453233, 0.4262465694468514643, -12.03445270309931736 ) ) ;
#44073=CARTESIAN_POINT ( 'NONE',  ( 112.2630620330015461, -1.172797794773250413, -17.05961127468924943 ) ) ;
#44075=CARTESIAN_POINT ( 'NONE',  ( 123.5176014775786228, -0.8288870151387760510, -10.36305467784173118 ) ) ;
#44082=CARTESIAN_POINT ( 'NONE',  ( 123.6310548109119765, -5.638512984488999180, -18.83840828888717311 ) ) ;
#44083=EDGE_LOOP ( 'NONE', ( #23844, #36487, #23263, #23344 ) ) ;
#44084=CARTESIAN_POINT ( 'NONE',  ( 119.5467348109119712, -4.089484607189486809, -7.948022111789456723 ) ) ;
#44085=DIRECTION ( 'NONE',  ( 0.000000000000000000, 0.6004852223388322807, -0.7996358532186280677 ) ) ;
#44087=CARTESIAN_POINT ( 'NONE',  ( 120.2274548109119934, 0.5811942927096110934, -14.16772938898807510 ) ) ;
#44088=CARTESIAN_POINT ( 'NONE',  ( 122.4397948109119767, -9.988377603198976828, -10.36322818467138340 ) ) ;
#44091=CARTESIAN_POINT ( 'NONE',  ( 125.6732148109119862, -9.859900752359378018, -12.68260735090039759 ) ) ;
#44096=CARTESIAN_POINT ( 'NONE',  ( 114.1934435773848833, -2.467220198592768199, -17.83387418641523325 ) ) ;
#44097=CARTESIAN_POINT ( 'NONE',  ( 124.6521348109119884, -7.894159318335828068, -9.358103419637847864 ) ) ;
#44100=CARTESIAN_POINT ( 'NONE',  ( 117.1642148109119859, -0.8288870151387760510, -10.36305467784173118 ) ) ;
#44103=CARTESIAN_POINT ( 'NONE',  ( 113.4769814775786330, 0.4262465694468514643, -12.03445270309931736 ) ) ;
#44104=CARTESIAN_POINT ( 'NONE',  ( 122.9503348109119827, 0.5811942927096110934, -14.16772938898807510 ) ) ;
#44106=CARTESIAN_POINT ( 'NONE',  ( 123.5176014775786228, -0.8288870151387760510, -10.36305467784173118 ) ) ;
#44107=CARTESIAN_POINT ( 'NONE',  ( 113.9307948109119906, 0.9020085738987339008, -11.91225656197089222 ) ) ;
#44108=CARTESIAN_POINT ( 'NONE',  ( 123.3474214775786209, -9.988377603198976828, -10.36322818467138340 ) ) ;
#44109=CARTESIAN_POINT ( 'NONE',  ( 124.6521348109119884, -7.894159318335828068, -9.358103419637847864 ) ) ;
#44110=VERTEX_POINT ( 'NONE', #15161 ) ;
#44112=ADVANCED_FACE ( 'NONE', ( #16062 ), #18034, .T. ) ;
#44113=CARTESIAN_POINT ( 'NONE',  ( 123.0070614775786169, 0.9020085738987339008, -11.91225656197089222 ) ) ;
#44114=CARTESIAN_POINT ( 'NONE',  ( 114.3846081442453197, 0.4262465694468514643, -12.03445270309931736 ) ) ;
#44115=CARTESIAN_POINT ( 'NONE',  ( 124.9924948109119924, -4.089484607189486809, -7.948022111789456723 ) ) ;
#44118=LINE ( 'NONE', #32697, #24979 ) ;
#44120=CARTESIAN_POINT ( 'NONE',  ( 137.8430364429465840, -1.575724663492070965, -16.52305390663654450 ) ) ;
#44122=EDGE_CURVE ( 'NONE', #23072, #11415, #28018, .T. ) ;
#44125=CARTESIAN_POINT ( 'NONE',  ( 120.9081748109119872, -4.153390946401325223, -8.397313243818185668 ) ) ;
#44126=CARTESIAN_POINT ( 'NONE',  ( 112.3424481442453384, -3.505236298600246325, -18.68346056562440793 ) ) ;
#44127=CARTESIAN_POINT ( 'NONE',  ( 126.8024586715757778, -6.490782095255248407, -18.42897405940419020 ) ) ;
#44129=CARTESIAN_POINT ( 'NONE',  ( 115.7914926669217834, -2.334846009198389805, -18.01015021110788439 ) ) ;
#44130=CARTESIAN_POINT ( 'NONE',  ( 117.3911214775786505, -7.894159318335828068, -9.358103419637847864 ) ) ;
#44133=CARTESIAN_POINT ( 'NONE',  ( 112.1155414775786454, -10.15424416112533912, -14.75197769757731336 ) ) ;
#44135=CARTESIAN_POINT ( 'NONE',  ( 121.3052614775786111, -1.834011780172310813, -8.268836392978581529 ) ) ;
#44137=CARTESIAN_POINT ( 'NONE',  ( 126.2972081442452890, -2.084020599724406786, -8.691656652584148546 ) ) ;
#44142=CARTESIAN_POINT ( 'NONE',  ( 125.7866681442452688, -8.899110576539710493, -16.42337572283490132 ) ) ;
#44143=CARTESIAN_POINT ( 'NONE',  ( 120.4543614775786295, -5.574606645277164318, -18.38911715685844683 ) ) ;
#44149=CARTESIAN_POINT ( 'NONE',  ( 113.2500748109119968, -3.505236298600246325, -18.68346056562440793 ) ) ;
#44153=CARTESIAN_POINT ( 'NONE',  ( 125.3328548109119964, -9.261995988541697145, -16.69588392320189030 ) ) ;
#44154=CARTESIAN_POINT ( 'NONE',  ( 120.9649014775786355, -3.383040157471821630, -19.15922257007629170 ) ) ;
#44156=CARTESIAN_POINT ( 'NONE',  ( 116.7104014775786425, -0.4660016031367893996, -10.09054647747474043 ) ) ;
#44157=CARTESIAN_POINT ( 'NONE',  ( 112.3991748109119868, -8.166667518702817929, -8.995218007635859436 ) ) ;
#44159=CARTESIAN_POINT ( 'NONE',  ( 112.7395348109119766, -4.153390946401321671, -8.397313243818183892 ) ) ;
#44161=CARTESIAN_POINT ( 'NONE',  ( 124.9357681442453014, -1.834011780172310813, -8.268836392978581529 ) ) ;
#44162=CARTESIAN_POINT ( 'NONE',  ( 118.4689281442453392, 0.9020085738987339008, -11.91225656197089222 ) ) ;
#44163=CARTESIAN_POINT ( 'NONE',  ( 112.7962614775786676, -3.383040157471821630, -19.15922257007629170 ) ) ;
#44164=CARTESIAN_POINT ( 'NONE',  ( 125.8433948109119456, -1.834011780172310813, -8.268836392978581529 ) ) ;
#44166=CARTESIAN_POINT ( 'NONE',  ( 119.3765548109119834, -10.15424416112533912, -14.75197769757731336 ) ) ;
#44168=CARTESIAN_POINT ( 'NONE',  ( 125.3328548109119964, -9.261995988541697145, -16.69588392320189030 ) ) ;
#44169=B_SPLINE_CURVE_WITH_KNOTS ( 'NONE', 3,
 ( #27185, #34880, #34669, #24213, #23772, #2778, #22904, #20348, #36797, #17154 ),
 .UNSPECIFIED., .F., .F.,
 ( 4, 3, 3, 4 ),
 ( 0.000000000000000000, 0.0001671877548681239927, 0.0003343755096277624991, 0.0006463528481650629171 ),
 .UNSPECIFIED. ) ;
#44171=CARTESIAN_POINT ( 'NONE',  ( 122.9503348109119827, -9.859900752359378018, -12.68260735090039759 ) ) ;
#44172=CARTESIAN_POINT ( 'NONE',  ( 128.2184548109119930, -8.536181032868617180, -18.13822074491315561 ) ) ;
#44176=CARTESIAN_POINT ( 'NONE',  ( 122.4965214775786251, -10.30919188438810075, -12.61870101168855918 ) ) ;
#44181=CARTESIAN_POINT ( 'NONE',  ( 112.7855738145250513, -3.807985514183288345, -19.09877912889401230 ) ) ;
#44187=CARTESIAN_POINT ( 'NONE',  ( 125.1235803781499953, -2.490773129849583434, -17.80250993700375517 ) ) ;
#44188=CARTESIAN_POINT ( 'NONE',  ( 124.6521348109119884, -1.561330072975668948, -17.79121239304076951 ) ) ;
#44189=CARTESIAN_POINT ( 'NONE',  ( 120.1140014775786398, -7.894159318335828068, -9.358103419637847864 ) ) ;
#44192=CARTESIAN_POINT ( 'NONE',  ( 122.6667014775786413, -7.893985811506177619, -18.51759400769804742 ) ) ;
#44193=CARTESIAN_POINT ( 'NONE',  ( 117.7882081442453170, -6.344957434206665248, -7.627207830600338134 ) ) ;
#44195=CARTESIAN_POINT ( 'NONE',  ( 113.1933481442453058, -5.574606645277164318, -18.38911715685844683 ) ) ;
#44196=CARTESIAN_POINT ( 'NONE',  ( 112.0588148109119828, 0.5811942927096154232, -14.16772938898807155 ) ) ;
#44197=CARTESIAN_POINT ( 'NONE',  ( 125.1626748109119802, -9.988377603198980381, -10.36322818467138518 ) ) ;
#44201=CARTESIAN_POINT ( 'NONE',  ( 117.7314814775786260, -5.574606645277164318, -18.38911715685844683 ) ) ;
#44202=CARTESIAN_POINT ( 'NONE',  ( 115.9729548109119861, -3.505236298600246325, -18.68346056562440793 ) ) ;
#44208=CARTESIAN_POINT ( 'NONE',  ( 126.2972081442452890, -2.084020599724406786, -8.691656652584148546 ) ) ;
#44213=CARTESIAN_POINT ( 'NONE',  ( 111.4926360275532176, -1.279900991230100260, -16.91698735540673226 ) ) ;
#44216=CARTESIAN_POINT ( 'NONE',  ( 119.8870948109119752, -9.261995988541697145, -16.69588392320189030 ) ) ;
#44217=CARTESIAN_POINT ( 'NONE',  ( 123.4041481442452834, 0.1319031606808879209, -14.10382304977623669 ) ) ;
#44218=CARTESIAN_POINT ( 'NONE',  ( 115.8595014775786609, -7.643976991954077427, -18.09477374809248928 ) ) ;
#44219=DIRECTION ( 'NONE',  ( 1.000000000000000000, 0.000000000000000000, 0.000000000000000000 ) ) ;
#44220=CARTESIAN_POINT ( 'NONE',  ( 120.5678148109119832, -8.166667518702819706, -8.995218007635861213 ) ) ;
#44221=CARTESIAN_POINT ( 'NONE',  ( 113.1366214775786432, -1.834011780172310813, -8.268836392978581529 ) ) ;
#44224=CARTESIAN_POINT ( 'NONE',  ( 122.8936081442453059, 0.2603800115204892296, -16.42320221600525088 ) ) ;
#44225=CARTESIAN_POINT ( 'NONE',  ( 123.2184548109119788, -3.410847707154505137, -16.57729307524250828 ) ) ;
#44227=CARTESIAN_POINT ( 'NONE',  ( 119.6034614775786196, -6.344957434206665248, -7.627207830600338134 ) ) ;
#44228=CARTESIAN_POINT ( 'NONE',  ( 113.9307948109119764, -10.15424416112533912, -14.75197769757731336 ) ) ;
#44230=CARTESIAN_POINT ( 'NONE',  ( 113.4202548109119846, -10.30919188438810075, -12.61870101168855918 ) ) ;
#44232=CARTESIAN_POINT ( 'NONE',  ( 120.6812681442452941, -10.30919188438810075, -12.61870101168855918 ) ) ;
#44237=CARTESIAN_POINT ( 'NONE',  ( 116.7104014775786425, -8.899110576539710493, -16.42337572283490132 ) ) ;
#44238=CARTESIAN_POINT ( 'NONE',  ( 137.3527759848290088, -3.463350433249969829, -8.419698276038079854 ) ) ;
#44239=CARTESIAN_POINT ( 'NONE',  ( 119.4332814775786318, -8.899110576539710493, -16.42337572283490132 ) ) ;
#44242=CARTESIAN_POINT ( 'NONE',  ( 128.2184548109119930, -10.36826876090625760, -11.00511718064540467 ) ) ;
#44243=CARTESIAN_POINT ( 'NONE',  ( 116.4267681442453153, -6.222761293078241884, -8.102969835052219238 ) ) ;
#44244=CARTESIAN_POINT ( 'NONE',  ( 114.5547881442453217, -5.638512984488999180, -18.83840828888717311 ) ) ;
#44246=CARTESIAN_POINT ( 'NONE',  ( 125.7299414775786346, -10.15424416112533912, -14.75197769757731336 ) ) ;
#44247=CARTESIAN_POINT ( 'NONE',  ( 116.3700414775786527, -4.153390946401321671, -8.397313243818183892 ) ) ;
#44248=CARTESIAN_POINT ( 'NONE',  ( 123.7445081442452874, -1.561330072975668948, -17.79121239304076951 ) ) ;
#44250=CARTESIAN_POINT ( 'NONE',  ( 123.1205148109119563, -1.834011780172310813, -8.268836392978581529 ) ) ;
#44252=CARTESIAN_POINT ( 'NONE',  ( 114.2144281442453178, -8.166667518702817929, -8.995218007635859436 ) ) ;
#44253=EDGE_CURVE ( 'NONE', #41752, #21031, #34102, .T. ) ;
#44258=CARTESIAN_POINT ( 'NONE',  ( 117.5045748109119756, 0.5811942927096110934, -14.16772938898807510 ) ) ;
#44260=CARTESIAN_POINT ( 'NONE',  ( 126.1837548109119211, -10.63000616557722466, -14.87417383870573495 ) ) ;
#44262=CARTESIAN_POINT ( 'NONE',  ( 113.5337081442453240, -0.8288870151387760510, -10.36305467784173118 ) ) ;
#44263=CARTESIAN_POINT ( 'NONE',  ( 124.8790414775786246, -8.899110576539426276, -16.42337572283528146 ) ) ;
#44264=CARTESIAN_POINT ( 'NONE',  ( 122.7801548109119665, -3.383040157471821630, -19.15922257007629170 ) ) ;
#44269=CARTESIAN_POINT ( 'NONE',  ( 122.8368814775786291, -7.894159318335828068, -9.358103419637847864 ) ) ;
#44270=CARTESIAN_POINT ( 'NONE',  ( 118.9227414775786400, -10.63000616557722466, -14.87417383870573495 ) ) ;
#44271=CIRCLE ( 'NONE', #39887, 5.999999999999997335 ) ;
#44272=CARTESIAN_POINT ( 'NONE',  ( 115.0086014775786509, -5.574606645277164318, -18.38911715685844683 ) ) ;
#44273=CARTESIAN_POINT ( 'NONE',  ( 115.5758681442453053, -1.561330072975668060, -17.79121239304076951 ) ) ;
#44276=CARTESIAN_POINT ( 'NONE',  ( 125.4463081442452932, -4.153390946401325223, -8.397313243818185668 ) ) ;
#44277=CARTESIAN_POINT ( 'NONE',  ( 120.5678148109119832, -1.833838273342659253, -17.42832698103878286 ) ) ;
#44279=EDGE_CURVE ( 'NONE', #11415, #40595, #5282, .T. ) ;
#44282=CARTESIAN_POINT ( 'NONE',  ( 113.8173414775786512, 0.2603800115204892296, -16.42320221600525088 ) ) ;
#44283=CARTESIAN_POINT ( 'NONE',  ( 120.0005481442453146, -4.153390946401325223, -8.397313243818185668 ) ) ;
#44286=CARTESIAN_POINT ( 'NONE',  ( 117.4478481442453131, 0.2603800115204892296, -16.42320221600525088 ) ) ;
#44288=CARTESIAN_POINT ( 'NONE',  ( 115.4056881442453459, -2.084020599724406786, -8.691656652584148546 ) ) ;
#44291=CARTESIAN_POINT ( 'NONE',  ( 112.1155414775786454, 0.9020085738987339008, -11.91225656197089222 ) ) ;
#44292=CARTESIAN_POINT ( 'NONE',  ( 120.5678148109119832, -1.833838273342659253, -17.42832698103878286 ) ) ;
#44295=CARTESIAN_POINT ( 'NONE',  ( 119.9438214775786378, -7.893985811506177619, -18.51759400769804742 ) ) ;
#44298=CARTESIAN_POINT ( 'NONE',  ( 118.4122014775786340, 0.5811942927096110934, -14.16772938898807510 ) ) ;
#44299=CARTESIAN_POINT ( 'NONE',  ( 119.9438214775786378, -7.893985811506177619, -18.51759400769804742 ) ) ;
#44300=CARTESIAN_POINT ( 'NONE',  ( 119.9438214775786378, -2.084020599724406786, -8.691656652584148546 ) ) ;
#44301=CARTESIAN_POINT ( 'NONE',  ( 124.5386814775786206, -4.153390946401325223, -8.397313243818185668 ) ) ;
#44302=CARTESIAN_POINT ( 'NONE',  ( 112.8529881442453302, -1.561330072975668060, -17.79121239304076596 ) ) ;
#44304=CARTESIAN_POINT ( 'NONE',  ( 123.0070614775786169, -10.15424416112533912, -14.75197769757731336 ) ) ;
#44305=FACE_OUTER_BOUND ( 'NONE', #24204, .T. ) ;
#44311=CARTESIAN_POINT ( 'NONE',  ( 122.2696148109119889, -4.089484607189486809, -7.948022111789456723 ) ) ;
#44312=CARTESIAN_POINT ( 'NONE',  ( 122.9503348109119827, -9.859900752359378018, -12.68260735090039759 ) ) ;
#44314=CARTESIAN_POINT ( 'NONE',  ( 123.8579614775786126, 0.5811942927096110934, -14.16772938898807510 ) ) ;
#44315=CARTESIAN_POINT ( 'NONE',  ( 113.7606148109119886, -7.894159318335828068, -9.358103419637847864 ) ) ;
#44317=CARTESIAN_POINT ( 'NONE',  ( 119.9438214775786378, -7.893985811506177619, -18.51759400769804742 ) ) ;
#44318=CARTESIAN_POINT ( 'NONE',  ( 122.7234281442452755, -5.638512984488999180, -18.83840828888717311 ) ) ;
#44320=CARTESIAN_POINT ( 'NONE',  ( 124.3685014775786328, 0.4262465694468514643, -12.03445270309931736 ) ) ;
#44326=CARTESIAN_POINT ( 'NONE',  ( 122.8936081442453059, -9.565557343593413364, -10.61323700422348004 ) ) ;
#44329=CARTESIAN_POINT ( 'NONE',  ( 116.3700414775786527, -4.153390946401321671, -8.397313243818183892 ) ) ;
#44330=CARTESIAN_POINT ( 'NONE',  ( 114.3846081442453197, 0.4262465694468514643, -12.03445270309931736 ) ) ;
#44331=CARTESIAN_POINT ( 'NONE',  ( 123.5176014775786228, -9.261995988541697145, -16.69588392320189030 ) ) ;
#44333=CARTESIAN_POINT ( 'NONE',  ( 122.2128881442453263, -7.643976991954077427, -18.09477374809248928 ) ) ;
#44334=CARTESIAN_POINT ( 'NONE',  ( 117.7314814775786260, -4.089484607189486809, -7.948022111789456723 ) ) ;
#44335=CARTESIAN_POINT ( 'NONE',  ( 125.1059481442452750, -8.166667518702819706, -8.995218007635861213 ) ) ;
#44336=CARTESIAN_POINT ( 'NONE',  ( 123.8012348109119642, -9.565557343593413364, -10.61323700422348004 ) ) ;
#44339=CARTESIAN_POINT ( 'NONE',  ( 123.2697102440515238, -2.467220198592778413, -17.83387418641524391 ) ) ;
#44340=CARTESIAN_POINT ( 'NONE',  ( 123.6877814775786533, -3.383040157471821630, -19.15922257007629170 ) ) ;
#44341=CARTESIAN_POINT ( 'NONE',  ( 114.6115148109119986, -6.222761293078241884, -8.102969835052219238 ) ) ;
#44342=CARTESIAN_POINT ( 'NONE',  ( 123.9714148109119805, -0.4660016031367893996, -10.09054647747474043 ) ) ;
#44349=CARTESIAN_POINT ( 'NONE',  ( 118.8660148109119774, 0.1319031606808879209, -14.10382304977623669 ) ) ;
#44350=CARTESIAN_POINT ( 'NONE',  ( 112.9097148109120070, -9.565557343593413364, -10.61323700422348004 ) ) ;
#44354=CARTESIAN_POINT ( 'NONE',  ( 121.0216281442452981, -7.894159318335828068, -9.358103419637847864 ) ) ;
#44357=CARTESIAN_POINT ( 'NONE',  ( 111.6155414775786596, 0.3778260857407392814, -12.04688916545883792 ) ) ;
#44359=CARTESIAN_POINT ( 'NONE',  ( 123.7445081442452874, -1.561330072975668948, -17.79121239304076951 ) ) ;
#44360=CARTESIAN_POINT ( 'NONE',  ( 126.1837548109119496, 0.4262465694468514643, -12.03445270309931736 ) ) ;
#44362=CARTESIAN_POINT ( 'NONE',  ( 112.6260814775786514, -9.261995988541697145, -16.69588392320189030 ) ) ;
#44366=CARTESIAN_POINT ( 'NONE',  ( 112.0020881442453344, 0.2603800115204892296, -16.42320221600525088 ) ) ;
#44367=CARTESIAN_POINT ( 'NONE',  ( 119.4332814775786318, -8.899110576539710493, -16.42337572283490132 ) ) ;
#44372=CARTESIAN_POINT ( 'NONE',  ( 114.8384214775786489, -10.15424416112533912, -14.75197769757731336 ) ) ;
#44376=CARTESIAN_POINT ( 'NONE',  ( 124.3117748109119844, -10.30919188438810075, -12.61870101168855918 ) ) ;
#44377=CARTESIAN_POINT ( 'NONE',  ( 120.7947214775786193, -9.261995988541697145, -16.69588392320189030 ) ) ;
#44379=CARTESIAN_POINT ( 'NONE',  ( 121.9859814775786333, 0.2603800115204892296, -16.42320221600525088 ) ) ;
#44380=FACE_OUTER_BOUND ( 'NONE', #14887, .T. ) ;
#44382=CARTESIAN_POINT ( 'NONE',  ( 112.1722681442453222, -8.899110576539710493, -16.42337572283490132 ) ) ;
#44383=CARTESIAN_POINT ( 'NONE',  ( 124.8223148109119762, 0.9020085738987339008, -11.91225656197089222 ) ) ;
#44384=CARTESIAN_POINT ( 'NONE',  ( 123.8579614775786126, 0.5811942927096110934, -14.16772938898807510 ) ) ;
#44385=CARTESIAN_POINT ( 'NONE',  ( 114.2711548109119803, -9.988377603198976828, -10.36322818467138340 ) ) ;
#44386=CARTESIAN_POINT ( 'NONE',  ( 113.9307948109119764, -10.15424416112533912, -14.75197769757731336 ) ) ;
#44388=CARTESIAN_POINT ( 'NONE',  ( 116.9940348109119839, -0.1624402480850797581, -16.17319339645315424 ) ) ;
#44392=CARTESIAN_POINT ( 'NONE',  ( 122.4965214775786251, 0.1319031606808879209, -14.10382304977623669 ) ) ;
#44397=CARTESIAN_POINT ( 'NONE',  ( 114.5700137256649072, -1.063912429576158614, -17.20460841810473696 ) ) ;
#44400=CARTESIAN_POINT ( 'NONE',  ( 112.6260814775786514, -9.261995988541697145, -16.69588392320189030 ) ) ;
#44401=CARTESIAN_POINT ( 'NONE',  ( 112.8337832127138682, -2.191907684172563986, -18.20049396185734025 ) ) ;
#44402=CARTESIAN_POINT ( 'NONE',  ( 123.2184548109119788, -6.965697074025154478, -10.59448971407311646 ) ) ;
#44405=CARTESIAN_POINT ( 'NONE',  ( 119.0361948109119652, -7.893985811506177619, -18.51759400769804742 ) ) ;
#44408=CARTESIAN_POINT ( 'NONE',  ( 124.8790414775786246, -0.4660016031367893996, -10.09054647747474043 ) ) ;
#44409=CARTESIAN_POINT ( 'NONE',  ( 122.0994348109119443, -10.15424416112533912, -14.75197769757731336 ) ) ;
#44410=CARTESIAN_POINT ( 'NONE',  ( 124.8790414775786246, -8.899110576539710493, -16.42337572283490132 ) ) ;
#44412=CARTESIAN_POINT ( 'NONE',  ( 124.0281414775786146, -1.834011780172310813, -8.268836392978581529 ) ) ;
#44413=CARTESIAN_POINT ( 'NONE',  ( 117.9583881442453048, -10.30919188438810075, -12.61870101168855918 ) ) ;
#44415=FACE_OUTER_BOUND ( 'NONE', #7447, .T. ) ;
#44416=CARTESIAN_POINT ( 'NONE',  ( 122.3263414775786373, -6.344957434206665248, -7.627207830600338134 ) ) ;
#44420=CARTESIAN_POINT ( 'NONE',  ( 116.3700414775786527, -4.153390946401321671, -8.397313243818183892 ) ) ;
#44421=CARTESIAN_POINT ( 'NONE',  ( 118.3554748109119998, -9.565557343593413364, -10.61323700422348004 ) ) ;
#44427=CARTESIAN_POINT ( 'NONE',  ( 115.1220548109119761, -8.166667518702817929, -8.995218007635861213 ) ) ;
#44428=FACE_OUTER_BOUND ( 'NONE', #26869, .T. ) ;
#44435=CARTESIAN_POINT ( 'NONE',  ( 117.0507614775786465, -10.30919188438810075, -12.61870101168855918 ) ) ;
#44437=CARTESIAN_POINT ( 'NONE',  ( 124.0848681442452772, -5.574606645277164318, -18.38911715685844683 ) ) ;
#44439=CARTESIAN_POINT ( 'NONE',  ( 117.5045748109119756, -9.859900752359374465, -12.68260735090039404 ) ) ;
#44442=CARTESIAN_POINT ( 'NONE',  ( 123.1205148109119563, -1.834011780172310813, -8.268836392978581529 ) ) ;
#44443=CARTESIAN_POINT ( 'NONE',  ( 119.9438214775786378, -7.893985811506177619, -18.51759400769804742 ) ) ;
#44445=CARTESIAN_POINT ( 'NONE',  ( 113.5337081442453240, -0.8288870151387760510, -10.36305467784173118 ) ) ;
#44448=CARTESIAN_POINT ( 'NONE',  ( 118.5823814775786360, -1.834011780172310813, -8.268836392978581529 ) ) ;
#44449=CARTESIAN_POINT ( 'NONE',  ( 126.6827570900183844, -4.792845811650923160, -18.62498157970546941 ) ) ;
#44450=CARTESIAN_POINT ( 'NONE',  ( 111.8886348109120092, -3.383040157471821630, -19.15922257007629170 ) ) ;
#44452=CARTESIAN_POINT ( 'NONE',  ( 121.8725281442453223, -3.383040157471821630, -19.15922257007629170 ) ) ;
#44455=CARTESIAN_POINT ( 'NONE',  ( 112.9664414775786412, -9.859900752359374465, -12.68260735090039404 ) ) ;
#44457=CARTESIAN_POINT ( 'NONE',  ( 117.9016614775786280, -0.1624402480850797581, -16.17319339645315424 ) ) ;
#44458=CARTESIAN_POINT ( 'NONE',  ( 123.7017273619992466, -4.637278545147846209, -14.94411704847414946 ) ) ;
#44459=CARTESIAN_POINT ( 'NONE',  ( 118.5256548109119876, -8.899110576539710493, -16.42337572283490132 ) ) ;
#44461=CARTESIAN_POINT ( 'NONE',  ( 114.1009748109119784, -5.574606645277164318, -18.38911715685844683 ) ) ;
#44463=CARTESIAN_POINT ( 'NONE',  ( 114.7249681442453237, 0.2603800115204892296, -16.42320221600525088 ) ) ;
#44465=CARTESIAN_POINT ( 'NONE',  ( 112.9097148109120070, 0.2603800115204892296, -16.42320221600525088 ) ) ;
#44466=CARTESIAN_POINT ( 'NONE',  ( 115.2355081442453155, 0.1319031606808879209, -14.10382304977623669 ) ) ;
#44467=CARTESIAN_POINT ( 'NONE',  ( 124.1983214775786166, -8.166667518702819706, -8.995218007635861213 ) ) ;
#44468=CARTESIAN_POINT ( 'NONE',  ( 116.3700414775786527, -4.153390946401321671, -8.397313243818183892 ) ) ;
#44470=CARTESIAN_POINT ( 'NONE',  ( 113.4202548109119846, -10.30919188438810075, -12.61870101168855918 ) ) ;
#44475=CARTESIAN_POINT ( 'NONE',  ( 120.6245414775786458, -9.988377603198976828, -10.36322818467138340 ) ) ;
#44478=CARTESIAN_POINT ( 'NONE',  ( 120.5861007241439324, -2.443475742715334853, -17.86549347949429389 ) ) ;
#44479=CARTESIAN_POINT ( 'NONE',  ( 117.7882081442453170, -3.505236298600246325, -18.68346056562440793 ) ) ;
#44481=CARTESIAN_POINT ( 'NONE',  ( 124.8223148109119762, 0.9020085738987339008, -11.91225656197089222 ) ) ;
#44485=CARTESIAN_POINT ( 'NONE',  ( 111.8886348109120092, -3.383040157471821630, -19.15922257007629170 ) ) ;
#44486=CARTESIAN_POINT ( 'NONE',  ( 124.1415948109119540, -3.505236298600246325, -18.68346056562440793 ) ) ;
#44487=CARTESIAN_POINT ( 'NONE',  ( 120.1140014775786398, -1.561330072975668504, -17.79121239304076951 ) ) ;
#44489=CARTESIAN_POINT ( 'NONE',  ( 114.1009748109119784, -5.574606645277164318, -18.38911715685844683 ) ) ;
#44490=CARTESIAN_POINT ( 'NONE',  ( 118.0718414775786300, -9.261995988541697145, -16.69588392320189030 ) ) ;
#44493=CARTESIAN_POINT ( 'NONE',  ( 117.7314814775786260, -5.574606645277164318, -18.38911715685844683 ) ) ;
#44496=CIRCLE ( 'NONE', #4409, 5.999999999999997335 ) ;
#44497=CARTESIAN_POINT ( 'NONE',  ( 115.8595014775786609, -1.834011780172310813, -8.268836392978581529 ) ) ;
#44498=CARTESIAN_POINT ( 'NONE',  ( 121.0216281442452981, -7.894159318335828068, -9.358103419637847864 ) ) ;
#44503=CARTESIAN_POINT ( 'NONE',  ( 117.0507614775786465, -10.30919188438810075, -12.61870101168855918 ) ) ;
#44505=CARTESIAN_POINT ( 'NONE',  ( 115.6893214775786447, -9.859900752359374465, -12.68260735090039404 ) ) ;
#44508=CARTESIAN_POINT ( 'NONE',  ( 112.5126281442453120, -10.30919188438810075, -12.61870101168855918 ) ) ;
#44509=CARTESIAN_POINT ( 'NONE',  ( 125.6164881442453094, -9.565557343593413364, -10.61323700422348004 ) ) ;
#44512=CARTESIAN_POINT ( 'NONE',  ( 122.8936081442453059, 0.2603800115204892296, -16.42320221600525088 ) ) ;
#44513=DIRECTION ( 'NONE',  ( -1.000000000000000000, 0.000000000000000000, 0.000000000000000000 ) ) ;
#44515=CARTESIAN_POINT ( 'NONE',  ( 121.1350814775786233, 0.5811942927096110934, -14.16772938898807510 ) ) ;
#44516=CARTESIAN_POINT ( 'NONE',  ( 119.8870948109119752, -9.261995988541697145, -16.69588392320189030 ) ) ;
#44517=CARTESIAN_POINT ( 'NONE',  ( 119.7736414775786358, 0.1319031606808879209, -14.10382304977623669 ) ) ;
#44518=CARTESIAN_POINT ( 'NONE',  ( 124.0281414775786146, -7.643976991954077427, -18.09477374809248928 ) ) ;
#44519=CARTESIAN_POINT ( 'NONE',  ( 113.0231681442453322, 0.9020085738987339008, -11.91225656197089222 ) ) ;
#44521=ORIENTED_EDGE ( 'NONE', *, *, #23105, .T. ) ;
#44522=CARTESIAN_POINT ( 'NONE',  ( 125.0492214775786266, -3.505236298600246325, -18.68346056562440793 ) ) ;
#44523=CARTESIAN_POINT ( 'NONE',  ( 122.3255085810856997, -1.220279397241718966, -16.99638242193886484 ) ) ;
#44529=CARTESIAN_POINT ( 'NONE',  ( 122.4397948109119767, -9.988377603198976828, -10.36322818467138340 ) ) ;
#44530=CARTESIAN_POINT ( 'NONE',  ( 121.5321681442453183, -0.1624402480850797581, -16.17319339645315424 ) ) ;
#44532=ORIENTED_EDGE ( 'NONE', *, *, #29013, .T. ) ;
#44533=CARTESIAN_POINT ( 'NONE',  ( 123.0637881442452937, -0.4660016031367893996, -10.09054647747474043 ) ) ;
#44534=CARTESIAN_POINT ( 'NONE',  ( 114.1577014775786552, -3.505236298600246325, -18.68346056562440793 ) ) ;
#44535=CARTESIAN_POINT ( 'NONE',  ( 121.8158014775786171, -4.153390946401271933, -8.397313243818190998 ) ) ;
#44536=CARTESIAN_POINT ( 'NONE',  ( 121.3619881442452879, -4.089484607189486809, -7.948022111789456723 ) ) ;
#44537=CARTESIAN_POINT ( 'NONE',  ( 120.2841814775786276, 0.9020085738987339008, -11.91225656197089222 ) ) ;
#44539=CARTESIAN_POINT ( 'NONE',  ( 126.5808414775786446, -9.859900752359378018, -12.68260735090039759 ) ) ;
#44540=CARTESIAN_POINT ( 'NONE',  ( 111.6573126359456012, -1.179503403430504527, -17.05068175419384957 ) ) ;
#44544=CARTESIAN_POINT ( 'NONE',  ( 112.2289948109119848, -7.643976991954077427, -18.09477374809248928 ) ) ;
#44545=CARTESIAN_POINT ( 'NONE',  ( 125.2194014775786286, 0.1319031606808879209, -14.10382304977623669 ) ) ;
#44548=CARTESIAN_POINT ( 'NONE',  ( 120.5678148109119832, -1.833838273342659253, -17.42832698103878286 ) ) ;
#44550=CARTESIAN_POINT ( 'NONE',  ( 114.9518748109119883, -7.643976991954077427, -18.09477374809248928 ) ) ;
#44551=CARTESIAN_POINT ( 'NONE',  ( 124.8223148109119762, 0.9020085738987339008, -11.91225656197089222 ) ) ;
#44554=CARTESIAN_POINT ( 'NONE',  ( 121.6456214775786293, 0.4262465694468514643, -12.03445270309931736 ) ) ;
#44555=CARTESIAN_POINT ( 'NONE',  ( 118.2987481442453088, -1.561330072975668504, -17.79121239304076951 ) ) ;
#44556=CARTESIAN_POINT ( 'NONE',  ( 123.6310548109119765, -5.638512984488999180, -18.83840828888717311 ) ) ;
#44557=CARTESIAN_POINT ( 'NONE',  ( 122.8368814775786291, -7.894159318335828068, -9.358103419637847864 ) ) ;
#44560=( BOUNDED_SURFACE ( )  B_SPLINE_SURFACE ( 1, 2, ( 
 ( #39437, #35996, #18468, #1347, #18236, #4991, #35314, #4085, #32132, #900, #18009, #31908, #14590, #28508, #11179, #14819, #28732, #11403, #25310, #40567, #40796, #6125, #37117, #29395, #1566, #44221, #20044, #12752, #12302, #8648, #15489, #19582, #8871, #12075, #33016, #9551, #40108, #43306, #25979, #19133, #26429, #26652, #9327, #9100, #23467, #23234, #40335, #26202, #5889, #30076, #33463, #22770, #33700, #12528, #19811, #29845, #2470, #30295, #16396, #43988, #43762, #19360, #33246, #15944, #12982, #26878, #1791, #37353, #39885, #2020, #23001, #22548, #36669, #36447, #5216, #43533, #15716, #2241, #29618, #5440, #36893, #5663, #16172, #13655, #24579, #17080, #10015, #6810, #173, #20271, #44896, #2928, #14089, #17300, #31405, #41914, #27109, #6359, #41476, #41031, #37586, #28006, #16857, #44672, #24141, #31192, #30749, #30972, #34597, #10234, #27561, #17507, #34157, #38464, #7025, #45111, #7237, #20497, #13434, #38033, #34378, #38246, #10677, #6581, #3159, #20717, #30521, #13869, #27780, #3381, #41693, #27337, #3595, #10456, #24359, #41258, #23924, #13210, #33927, #2697, #23699, #16626, #37806, #20935, #34809, #44443, #9785, #15210, #25702, #11571, #3809, #21153, #18635, #39609, #32306, #31855, #28230, #35026, #39151, #28451, #31631, #7455, #29115, #14536, #17733, #399, #38690, #843, #1073, #14985, #28678, #43027, #42810, #14763, #624, #25478, #4492, #7916, #42360, #8149, #32076, #39384, #4262, #28899, #4715, #35946, #18414, #18181, #38916, #7687, #35488, #32523, #22053, #21374, #1298, #11795, #21601, #42580, #14314, #11122, #42137, #10898, #17956, #24798, #21826, #35257, #4034, #25022, #11343, #25254, #35720, #12931, #43484, #5392, #19310, #43257, #26374, #9048, #22948, #43935, #33640, #1966, #30016, #43702, #5609, #29790, #39831, #36841, #36617, #19533, #22718, #26829, #16116, #37063, #8370, #5836, #5161, #22276, #33409, #12475, #44168, #1517, #36170, #4936, #15436, #18851, #33191, #19758, #40284, #2186, #12701, #23185, #15893, #26601, #8817, #2416, #26147 ),
 ( #40514, #32743, #9277, #16342, #15664, #29343, #12251, #30245, #12022, #25925, #8597, #32964, #22495, #36390, #19078, #1741, #29566, #40049, #729, #31748, #71, #515, #17848, #13768, #31298, #13983, #3928, #24913, #10570, #17627, #14651, #6065, #10789, #31082, #17191, #27678, #41592, #24257, #27898, #35150, #11012, #38809, #9497, #31522, #7577, #10348, #21491, #24467, #41813, #35376, #38358, #45009, #292, #24686, #23412, #14426, #34919, #14206, #3707, #18071, #40740, #38145, #3492, #3266, #21044, #28120, #38574, #42248, #4155, #28336, #6919, #7133, #42027, #20826, #34488, #7352, #21268, #31964, #34706, #37296, #19984, #17409, #18965, #11236, #28566, #26036, #33074, #39718, #39268, #35605, #1846, #1404, #35829, #39039, #14879, #36507, #21937, #42475, #25145, #963, #8258, #8483, #22387, #36057, #5279, #5050, #22163, #8030, #32854, #11909, #15321, #4603, #15545, #39495, #1625, #11684, #36282, #12134, #43365, #25809, #25590, #1189, #15101, #42919, #39942, #29450, #28791, #8703, #22608, #29010, #4826, #19197, #18523, #4378, #7810, #25369, #21719, #29232, #18295, #11466, #32190, #42697, #32416, #18747, #32638, #43139, #44050, #36949, #33762, #27168, #2077, #26715, #29908, #41089, #44283, #13262, #23756, #8933, #33301, #23291, #22834, #19415, #9847, #43823, #26493, #5949, #13036, #12589, #12814, #16457, #37175, #40624, #44498, #16001, #6420, #33991, #26935, #34214, #2303, #40397, #19873, #16233, #20105, #37646, #33523, #30136, #2530, #12361, #40857, #9611, #30358, #23530, #9161, #30578, #9381, #37416, #23065, #5720, #40169, #20328, #15775, #5494, #29677, #19638, #6185, #2759, #43589, #16685, #26261, #36728, #14147, #21437, #34652, #20551, #38302, #3437, #7296, #14372, #20772, #17356, #10511, #44731, #28062, #41971, #7081, #10737, #41533, #17792, #41751, #20990, #27619, #38088, #27395, #31688, #10955, #37864, #7521, #3211, #34864, #24636, #34432, #38518, #42194, #2986, #21213, #30807, #16913, #456, #13490, #35090, #13712, #10076, #41317, #3651, #10291, #23978, #17137 ) ),
 .UNSPECIFIED., .F., .F., .T. ) 
 B_SPLINE_SURFACE_WITH_KNOTS ( ( 2, 2 ),
 ( 3, 2, 2, 2, 2, 2, 2, 2, 2, 2, 2, 2, 2, 2, 2, 2, 2, 2, 2, 2, 2, 2, 2, 2, 2, 2, 2, 2, 2, 2, 2, 2, 2, 2, 2, 2, 2, 2, 2, 2, 2, 2, 2, 2, 2, 2, 2, 2, 2, 2, 2, 2, 2, 2, 2, 2, 2, 2, 2, 2, 2, 2, 2, 2, 2, 2, 2, 2, 2, 2, 2, 2, 2, 2, 2, 2, 2, 2, 2, 2, 2, 2, 2, 2, 2, 2, 2, 2, 2, 2, 2, 2, 2, 2, 2, 2, 2, 2, 2, 2, 2, 2, 2, 2, 2, 2, 2, 2, 2, 2, 2, 2, 2, 2, 2, 2, 2, 2, 2, 2, 2, 2, 2, 2, 2, 2, 2, 2, 3 ),
 ( 0.000000000000000000, 1.000000000000000000 ),
 ( 0.000000000000000000, 0.007812500000000000000, 0.01562500000000000000, 0.02343750000000000000, 0.03125000000000000000, 0.03906250000000000000, 0.04687500000000000000, 0.05468750000000000000, 0.06250000000000000000, 0.07031250000000000000, 0.07812500000000000000, 0.08593750000000000000, 0.09375000000000000000, 0.1015625000000000000, 0.1093750000000000000, 0.1171875000000000000, 0.1250000000000000000, 0.1328125000000000000, 0.1406250000000000000, 0.1484375000000000000, 0.1562500000000000000, 0.1640625000000000000, 0.1718750000000000000, 0.1796875000000000000, 0.1875000000000000000, 0.1953125000000000000, 0.2031250000000000000, 0.2109375000000000000, 0.2187500000000000000, 0.2265625000000000000, 0.2343750000000000000, 0.2421875000000000000, 0.2500000000000000000, 0.2578125000000000000, 0.2656250000000000000, 0.2734375000000000000, 0.2812500000000000000, 0.2890625000000000000, 0.2968750000000000000, 0.3046875000000000000, 0.3125000000000000000, 0.3203125000000000000, 0.3281250000000000000, 0.3359375000000000000, 0.3437500000000000000, 0.3515625000000000000, 0.3593750000000000000, 0.3671875000000000000, 0.3750000000000000000, 0.3828125000000000000, 0.3906250000000000000, 0.3984375000000000000, 0.4062500000000000000, 0.4140625000000000000, 0.4218750000000000000, 0.4296875000000000000, 0.4375000000000000000, 0.4453125000000000000, 0.4531250000000000000, 0.4609375000000000000, 0.4687500000000000000, 0.4765625000000000000, 0.4843750000000000000, 0.4921875000000000000, 0.5000000000000000000, 0.5078125000000000000, 0.5156250000000000000, 0.5234375000000000000, 0.5312500000000000000, 0.5390625000000000000, 0.5468750000000000000, 0.5546875000000000000, 0.5625000000000000000, 0.5703125000000000000, 0.5781250000000000000, 0.5859375000000000000, 0.5937500000000000000, 0.6015625000000000000, 0.6093750000000000000, 0.6171875000000000000, 0.6250000000000000000, 0.6328125000000000000, 0.6406250000000000000, 0.6484375000000000000, 0.6562500000000000000, 0.6640625000000000000, 0.6718750000000000000, 0.6796875000000000000, 0.6875000000000000000, 0.6953125000000000000, 0.7031250000000000000, 0.7109375000000000000, 0.7187500000000000000, 0.7265625000000000000, 0.7343750000000000000, 0.7421875000000000000, 0.7500000000000000000, 0.7578125000000000000, 0.7656250000000000000, 0.7734375000000000000, 0.7812500000000000000, 0.7890625000000000000, 0.7968750000000000000, 0.8046875000000000000, 0.8125000000000000000, 0.8203125000000000000, 0.8281250000000000000, 0.8359375000000000000, 0.8437500000000000000, 0.8515625000000000000, 0.8593750000000000000, 0.8671875000000000000, 0.8750000000000000000, 0.8828125000000000000, 0.8906250000000000000, 0.8984375000000000000, 0.9062500000000000000, 0.9140625000000000000, 0.9218750000000000000, 0.9296875000000000000, 0.9375000000000000000, 0.9453125000000000000, 0.9531250000000000000, 0.9609375000000000000, 0.9687500000000000000, 0.9765625000000000000, 0.9843750000000000000, 0.9921875000000000000, 1.000000000000000000 ),
 .UNSPECIFIED. ) 
 GEOMETRIC_REPRESENTATION_ITEM ( )  RATIONAL_B_SPLINE_SURFACE ( (
 ( 1.000000000000000000, 0.9238795325112869605, 1.000000000000000000, 0.9238795325112869605, 1.000000000000000000, 0.9238795325112869605, 1.000000000000000000, 0.9238795325112869605, 1.000000000000000000, 0.9238795325112869605, 1.000000000000000000, 0.9238795325112869605, 1.000000000000000000, 0.9238795325112869605, 1.000000000000000000, 0.9238795325112869605, 1.000000000000000000, 0.9238795325112869605, 1.000000000000000000, 0.9238795325112869605, 1.000000000000000000, 0.9238795325112869605, 1.000000000000000000, 0.9238795325112869605, 1.000000000000000000, 0.9238795325112869605, 1.000000000000000000, 0.9238795325112869605, 1.000000000000000000, 0.9238795325112869605, 1.000000000000000000, 0.9238795325112869605, 1.000000000000000000, 0.9238795325112869605, 1.000000000000000000, 0.9238795325112869605, 1.000000000000000000, 0.9238795325112869605, 1.000000000000000000, 0.9238795325112869605, 1.000000000000000000, 0.9238795325112869605, 1.000000000000000000, 0.9238795325112869605, 1.000000000000000000, 0.9238795325112869605, 1.000000000000000000, 0.9238795325112869605, 1.000000000000000000, 0.9238795325112869605, 1.000000000000000000, 0.9238795325112869605, 1.000000000000000000, 0.9238795325112869605, 1.000000000000000000, 0.9238795325112869605, 1.000000000000000000, 0.9238795325112869605, 1.000000000000000000, 0.9238795325112869605, 1.000000000000000000, 0.9238795325112869605, 1.000000000000000000, 0.9238795325112869605, 1.000000000000000000, 0.9238795325112869605, 1.000000000000000000, 0.9238795325112869605, 1.000000000000000000, 0.9238795325112869605, 1.000000000000000000, 0.9238795325112869605, 1.000000000000000000, 0.9238795325112869605, 1.000000000000000000, 0.9238795325112869605, 1.000000000000000000, 0.9238795325112869605, 1.000000000000000000, 0.9238795325112869605, 1.000000000000000000, 0.9238795325112869605, 1.000000000000000000, 0.9238795325112869605, 1.000000000000000000, 0.9238795325112869605, 1.000000000000000000, 0.9238795325112869605, 1.000000000000000000, 0.9238795325112869605, 1.000000000000000000, 0.9238795325112869605, 1.000000000000000000, 0.9238795325112869605, 1.000000000000000000, 0.9238795325112869605, 1.000000000000000000, 0.9238795325112869605, 1.000000000000000000, 0.9238795325112869605, 1.000000000000000000, 0.9238795325112869605, 1.000000000000000000, 0.9238795325112869605, 1.000000000000000000, 0.9238795325112869605, 1.000000000000000000, 0.9238795325112869605, 1.000000000000000000, 0.9238795325112869605, 1.000000000000000000, 0.9238795325112869605, 1.000000000000000000, 0.9238795325112869605, 1.000000000000000000, 0.9238795325112869605, 1.000000000000000000, 0.9238795325112869605, 1.000000000000000000, 0.9238795325112869605, 1.000000000000000000, 0.9238795325112869605, 1.000000000000000000, 0.9238795325112869605, 1.000000000000000000, 0.9238795325112869605, 1.000000000000000000, 0.9238795325112869605, 1.000000000000000000, 0.9238795325112869605, 1.000000000000000000, 0.9238795325112869605, 1.000000000000000000, 0.9238795325112869605, 1.000000000000000000, 0.9238795325112869605, 1.000000000000000000, 0.9238795325112869605, 1.000000000000000000, 0.9238795325112869605, 1.000000000000000000, 0.9238795325112869605, 1.000000000000000000, 0.9238795325112869605, 1.000000000000000000, 0.9238795325112869605, 1.000000000000000000, 0.9238795325112869605, 1.000000000000000000, 0.9238795325112869605, 1.000000000000000000, 0.9238795325112869605, 1.000000000000000000, 0.9238795325112869605, 1.000000000000000000, 0.9238795325112869605, 1.000000000000000000, 0.9238795325112869605, 1.000000000000000000, 0.9238795325112869605, 1.000000000000000000, 0.9238795325112869605, 1.000000000000000000, 0.9238795325112869605, 1.000000000000000000, 0.9238795325112869605, 1.000000000000000000, 0.9238795325112869605, 1.000000000000000000, 0.9238795325112869605, 1.000000000000000000, 0.9238795325112869605, 1.000000000000000000, 0.9238795325112869605, 1.000000000000000000, 0.9238795325112869605, 1.000000000000000000, 0.9238795325112869605, 1.000000000000000000, 0.9238795325112869605, 1.000000000000000000, 0.9238795325112869605, 1.000000000000000000, 0.9238795325112869605, 1.000000000000000000, 0.9238795325112869605, 1.000000000000000000, 0.9238795325112869605, 1.000000000000000000, 0.9238795325112869605, 1.000000000000000000, 0.9238795325112869605, 1.000000000000000000, 0.9238795325112869605, 1.000000000000000000, 0.9238795325112869605, 1.000000000000000000, 0.9238795325112869605, 1.000000000000000000, 0.9238795325112869605, 1.000000000000000000, 0.9238795325112869605, 1.000000000000000000, 0.9238795325112869605, 1.000000000000000000, 0.9238795325112869605, 1.000000000000000000, 0.9238795325112869605, 1.000000000000000000, 0.9238795325112869605, 1.000000000000000000, 0.9238795325112869605, 1.000000000000000000, 0.9238795325112869605, 1.000000000000000000, 0.9238795325112869605, 1.000000000000000000, 0.9238795325112869605, 1.000000000000000000, 0.9238795325112869605, 1.000000000000000000, 0.9238795325112869605, 1.000000000000000000, 0.9238795325112869605, 1.000000000000000000, 0.9238795325112869605, 1.000000000000000000, 0.9238795325112869605, 1.000000000000000000, 0.9238795325112869605, 1.000000000000000000, 0.9238795325112869605, 1.000000000000000000, 0.9238795325112869605, 1.000000000000000000, 0.9238795325112869605, 1.000000000000000000, 0.9238795325112869605, 1.000000000000000000, 0.9238795325112869605, 1.000000000000000000, 0.9238795325112869605, 1.000000000000000000, 0.9238795325112869605, 1.000000000000000000, 0.9238795325112869605, 1.000000000000000000, 0.9238795325112869605, 1.000000000000000000, 0.9238795325112869605, 1.000000000000000000, 0.9238795325112869605, 1.000000000000000000, 0.9238795325112869605, 1.000000000000000000, 0.9238795325112869605, 1.000000000000000000),
 ( 1.000000000000000000, 0.9238795325112869605, 1.000000000000000000, 0.9238795325112869605, 1.000000000000000000, 0.9238795325112869605, 1.000000000000000000, 0.9238795325112869605, 1.000000000000000000, 0.9238795325112869605, 1.000000000000000000, 0.9238795325112869605, 1.000000000000000000, 0.9238795325112869605, 1.000000000000000000, 0.9238795325112869605, 1.000000000000000000, 0.9238795325112869605, 1.000000000000000000, 0.9238795325112869605, 1.000000000000000000, 0.9238795325112869605, 1.000000000000000000, 0.9238795325112869605, 1.000000000000000000, 0.9238795325112869605, 1.000000000000000000, 0.9238795325112869605, 1.000000000000000000, 0.9238795325112869605, 1.000000000000000000, 0.9238795325112869605, 1.000000000000000000, 0.9238795325112869605, 1.000000000000000000, 0.9238795325112869605, 1.000000000000000000, 0.9238795325112869605, 1.000000000000000000, 0.9238795325112869605, 1.000000000000000000, 0.9238795325112869605, 1.000000000000000000, 0.9238795325112869605, 1.000000000000000000, 0.9238795325112869605, 1.000000000000000000, 0.9238795325112869605, 1.000000000000000000, 0.9238795325112869605, 1.000000000000000000, 0.9238795325112869605, 1.000000000000000000, 0.9238795325112869605, 1.000000000000000000, 0.9238795325112869605, 1.000000000000000000, 0.9238795325112869605, 1.000000000000000000, 0.9238795325112869605, 1.000000000000000000, 0.9238795325112869605, 1.000000000000000000, 0.9238795325112869605, 1.000000000000000000, 0.9238795325112869605, 1.000000000000000000, 0.9238795325112869605, 1.000000000000000000, 0.9238795325112869605, 1.000000000000000000, 0.9238795325112869605, 1.000000000000000000, 0.9238795325112869605, 1.000000000000000000, 0.9238795325112869605, 1.000000000000000000, 0.9238795325112869605, 1.000000000000000000, 0.9238795325112869605, 1.000000000000000000, 0.9238795325112869605, 1.000000000000000000, 0.9238795325112869605, 1.000000000000000000, 0.9238795325112869605, 1.000000000000000000, 0.9238795325112869605, 1.000000000000000000, 0.9238795325112869605, 1.000000000000000000, 0.9238795325112869605, 1.000000000000000000, 0.9238795325112869605, 1.000000000000000000, 0.9238795325112869605, 1.000000000000000000, 0.9238795325112869605, 1.000000000000000000, 0.9238795325112869605, 1.000000000000000000, 0.9238795325112869605, 1.000000000000000000, 0.9238795325112869605, 1.000000000000000000, 0.9238795325112869605, 1.000000000000000000, 0.9238795325112869605, 1.000000000000000000, 0.9238795325112869605, 1.000000000000000000, 0.9238795325112869605, 1.000000000000000000, 0.9238795325112869605, 1.000000000000000000, 0.9238795325112869605, 1.000000000000000000, 0.9238795325112869605, 1.000000000000000000, 0.9238795325112869605, 1.000000000000000000, 0.9238795325112869605, 1.000000000000000000, 0.9238795325112869605, 1.000000000000000000, 0.9238795325112869605, 1.000000000000000000, 0.9238795325112869605, 1.000000000000000000, 0.9238795325112869605, 1.000000000000000000, 0.9238795325112869605, 1.000000000000000000, 0.9238795325112869605, 1.000000000000000000, 0.9238795325112869605, 1.000000000000000000, 0.9238795325112869605, 1.000000000000000000, 0.9238795325112869605, 1.000000000000000000, 0.9238795325112869605, 1.000000000000000000, 0.9238795325112869605, 1.000000000000000000, 0.9238795325112869605, 1.000000000000000000, 0.9238795325112869605, 1.000000000000000000, 0.9238795325112869605, 1.000000000000000000, 0.9238795325112869605, 1.000000000000000000, 0.9238795325112869605, 1.000000000000000000, 0.9238795325112869605, 1.000000000000000000, 0.9238795325112869605, 1.000000000000000000, 0.9238795325112869605, 1.000000000000000000, 0.9238795325112869605, 1.000000000000000000, 0.9238795325112869605, 1.000000000000000000, 0.9238795325112869605, 1.000000000000000000, 0.9238795325112869605, 1.000000000000000000, 0.9238795325112869605, 1.000000000000000000, 0.9238795325112869605, 1.000000000000000000, 0.9238795325112869605, 1.000000000000000000, 0.9238795325112869605, 1.000000000000000000, 0.9238795325112869605, 1.000000000000000000, 0.9238795325112869605, 1.000000000000000000, 0.9238795325112869605, 1.000000000000000000, 0.9238795325112869605, 1.000000000000000000, 0.9238795325112869605, 1.000000000000000000, 0.9238795325112869605, 1.000000000000000000, 0.9238795325112869605, 1.000000000000000000, 0.9238795325112869605, 1.000000000000000000, 0.9238795325112869605, 1.000000000000000000, 0.9238795325112869605, 1.000000000000000000, 0.9238795325112869605, 1.000000000000000000, 0.9238795325112869605, 1.000000000000000000, 0.9238795325112869605, 1.000000000000000000, 0.9238795325112869605, 1.000000000000000000, 0.9238795325112869605, 1.000000000000000000, 0.9238795325112869605, 1.000000000000000000, 0.9238795325112869605, 1.000000000000000000, 0.9238795325112869605, 1.000000000000000000, 0.9238795325112869605, 1.000000000000000000, 0.9238795325112869605, 1.000000000000000000, 0.9238795325112869605, 1.000000000000000000, 0.9238795325112869605, 1.000000000000000000, 0.9238795325112869605, 1.000000000000000000, 0.9238795325112869605, 1.000000000000000000, 0.9238795325112869605, 1.000000000000000000, 0.9238795325112869605, 1.000000000000000000, 0.9238795325112869605, 1.000000000000000000, 0.9238795325112869605, 1.000000000000000000, 0.9238795325112869605, 1.000000000000000000, 0.9238795325112869605, 1.000000000000000000, 0.9238795325112869605, 1.000000000000000000, 0.9238795325112869605, 1.000000000000000000, 0.9238795325112869605, 1.000000000000000000, 0.9238795325112869605, 1.000000000000000000, 0.9238795325112869605, 1.000000000000000000, 0.9238795325112869605, 1.000000000000000000, 0.9238795325112869605, 1.000000000000000000, 0.9238795325112869605, 1.000000000000000000, 0.9238795325112869605, 1.000000000000000000, 0.9238795325112869605, 1.000000000000000000) ) ) 
 REPRESENTATION_ITEM ( '' )  SURFACE ( )  );
#44563=CARTESIAN_POINT ( 'NONE',  ( 123.7445081442452874, -1.561330072975668948, -17.79121239304076951 ) ) ;
#44564=CARTESIAN_POINT ( 'NONE',  ( 115.0086014775786509, -5.574606645277164318, -18.38911715685844683 ) ) ;
#44565=CARTESIAN_POINT ( 'NONE',  ( 125.6164881442453094, 0.2603800115204892296, -16.42320221600525088 ) ) ;
#44570=CARTESIAN_POINT ( 'NONE',  ( 111.2646414775786496, -8.899110576539710493, -16.42337572283490132 ) ) ;
#44575=CARTESIAN_POINT ( 'NONE',  ( 121.2485348109119769, -8.899110576539710493, -16.42337572283490132 ) ) ;
#44576=CARTESIAN_POINT ( 'NONE',  ( 115.3489614775786407, -0.8288870151387760510, -10.36305467784173118 ) ) ;
#44577=CARTESIAN_POINT ( 'NONE',  ( 126.3999550322131284, -0.5085153482442246187, -10.75768242470931213 ) ) ;
#44582=CARTESIAN_POINT ( 'NONE',  ( 112.6828081442453282, -2.084020599724406786, -8.691656652584148546 ) ) ;
#44587=CARTESIAN_POINT ( 'NONE',  ( 126.2404814775786264, -9.261995988541697145, -16.69588392320189030 ) ) ;
#44588=CARTESIAN_POINT ( 'NONE',  ( 113.1933481442453058, -4.089484607189486809, -7.948022111789456723 ) ) ;
#44589=ORIENTED_EDGE ( 'NONE', *, *, #26167, .T. ) ;
#44590=CARTESIAN_POINT ( 'NONE',  ( 113.4202548109119846, -10.30919188438810075, -12.61870101168855918 ) ) ;
#44591=CARTESIAN_POINT ( 'NONE',  ( 126.4852516627934023, 0.09531265143840929321, -14.71874934724275974 ) ) ;
#44593=CARTESIAN_POINT ( 'NONE',  ( 125.2194014775786286, 0.1319031606808879209, -14.10382304977623669 ) ) ;
#44594=CARTESIAN_POINT ( 'NONE',  ( 122.5532481442453019, 0.4262465694468514643, -12.03445270309931736 ) ) ;
#44598=CARTESIAN_POINT ( 'NONE',  ( 117.1642148109119859, -9.261995988541702474, -16.69588392320188319 ) ) ;
#44600=CARTESIAN_POINT ( 'NONE',  ( 112.4559014775786778, -0.1624402480850797581, -16.17319339645315424 ) ) ;
#44604=CARTESIAN_POINT ( 'NONE',  ( 125.0492214775786266, -6.344957434206665248, -7.627207830600338134 ) ) ;
#44605=CARTESIAN_POINT ( 'NONE',  ( 123.0070614775786169, 0.9020085738987339008, -11.91225656197089222 ) ) ;
#44607=CARTESIAN_POINT ( 'NONE',  ( 120.3409081442453044, -0.4660016031367893996, -10.09054647747474043 ) ) ;
#44608=CARTESIAN_POINT ( 'NONE',  ( 111.8886348109120092, -3.383040157471821630, -19.15922257007629170 ) ) ;
#44609=ORIENTED_EDGE ( 'NONE', *, *, #31852, .T. ) ;
#44610=CARTESIAN_POINT ( 'NONE',  ( 112.3991748109119868, -1.833838273342658809, -17.42832698103878286 ) ) ;
#44611=CARTESIAN_POINT ( 'NONE',  ( 112.5126281442453120, 0.1319031606808879209, -14.10382304977623669 ) ) ;
#44612=CARTESIAN_POINT ( 'NONE',  ( 124.0281414775786146, -1.834011780172310813, -8.268836392978581529 ) ) ;
#44613=CARTESIAN_POINT ( 'NONE',  ( 114.6115148109119986, -3.383040157471821630, -19.15922257007629170 ) ) ;
#44615=CARTESIAN_POINT ( 'NONE',  ( 111.7184548109119788, -0.8288870151387760510, -10.36305467784173118 ) ) ;
#44616=ORIENTED_EDGE ( 'NONE', *, *, #10407, .F. ) ;
#44617=CARTESIAN_POINT ( 'NONE',  ( 116.8805814775786445, -3.505236298600246325, -18.68346056562440793 ) ) ;
#44618=CARTESIAN_POINT ( 'NONE',  ( 113.0798948109119948, -0.4660016031367893996, -10.09054647747474043 ) ) ;
#44620=CARTESIAN_POINT ( 'NONE',  ( 124.7655881442452852, -9.859900752359378018, -12.68260735090039759 ) ) ;
#44625=DIRECTION ( 'NONE',  ( -0.7071067811865480168, -0.5654279342907823080, -0.4246071727180995570 ) ) ;
#44630=CARTESIAN_POINT ( 'NONE',  ( 112.7962614775786676, -3.383040157471821630, -19.15922257007629170 ) ) ;
#44635=CARTESIAN_POINT ( 'NONE',  ( 117.6180281442453150, -0.4660016031367893996, -10.09054647747474043 ) ) ;
#44639=( BOUNDED_SURFACE ( )  B_SPLINE_SURFACE ( 1, 2, ( 
 ( #40023, #26348, #23614, #3733, #44814, #17219, #20418, #6274, #7158, #31327, #9932, #20194, #6950, #13572, #20855, #30669, #44362, #13353, #14014, #101, #34078, #27482, #41401, #10156, #37732, #24501, #21069, #34948, #23845, #24065, #44590, #41838, #13793, #37500, #37956, #30443, #27706, #6731, #2845, #16775, #10598, #27257, #41172, #13124, #20641, #6502, #34518, #31109, #3296, #45034, #27929, #34301, #27029, #3516, #41620, #40944, #17003, #9700, #3074, #30892, #10376, #24285, #38171, #38385, #34733, #17433, #32445, #7607, #15133, #42730, #11040, #1219, #11266, #28149, #25400, #21521, #24713, #10817, #17656, #4183, #14233, #42059, #8068, #29039, #42948, #28364, #35858, #28595, #35408, #11714, #25625, #7841, #35179, #38603, #42278, #28820, #22193, #35638, #24942, #7379, #3956, #39530, #4632, #8291, #21747, #32221, #11495, #18553, #36089, #25174, #31552, #39298, #42506, #31775, #994, #21296, #39072, #38838, #18101, #320, #4414, #17878, #21971, #31996, #546, #14458, #759, #14681, #18328, #14909, #40432, #2334, #16264, #15580, #23100, #15806, #22642, #30167, #44084, #40201, #22418, #29263, #29484, #16032, #9412, #22866, #12165, #15358, #36311, #12849, #36980, #40658, #8967, #19447, #43853, #5749, #26750, #12394, #23323, #26523, #29707, #18997, #33330, #25839, #43620, #43397, #19669, #26294, #9193, #11943, #1658, #29940, #32884, #33557, #4860, #18778, #2104, #12625, #43175, #32668, #19228, #36759, #39971, #39747, #1436, #8515, #26067, #5081, #8734, #33109, #36538, #5312, #1879, #5528, #20804, #6894, #40890, #6455, #3023, #16945, #44533, #31275, #13962, #41787, #30616, #30839, #6218, #3471, #20586, #30392, #44762, #27873, #34464, #13521, #44314, #9643, #17386, #23565, #20141, #10544, #27430, #34026, #34250, #37900, #41352, #10108, #34683, #37446, #37209, #10327, #3243, #5981, #23790, #19906, #33791, #2794, #2563, #13295, #16492, #48, #6678, #26969, #13070, #27203, #16721, #17169, #41121, #9880, #31058, #37680, #20363, #24012, #44986, #13745, #27653, #41568, #24230 ),
 ( #38121, #8006, #25121, #28546, #38551, #939, #42673, #42897, #708, #7327, #21246, #35808, #14858, #28767, #28314, #11443, #25348, #39017, #269, #32170, #1162, #21915, #38784, #14628, #24444, #10768, #7555, #21470, #42450, #35353, #15078, #24664, #28990, #18274, #39242, #4578, #38335, #14404, #18503, #7112, #14178, #4129, #42226, #32393, #18049, #7787, #35123, #21022, #21696, #34895, #31942, #11216, #35582, #3684, #17605, #3906, #31721, #31498, #4354, #28096, #42004, #10989, #24891, #17824, #491, #43969, #22143, #12733, #2222, #34138, #36035, #2676, #8236, #1383, #30277, #12964, #26860, #19793, #26635, #18725, #33442, #16375, #22985, #44202, #33677, #4804, #11659, #6335, #9766, #16151, #23677, #11886, #25566, #37096, #30729, #32617, #37566, #37333, #40773, #15298, #29207, #39472, #43116, #26409, #40548, #40319, #2453, #16837, #13188, #9083, #9309, #36874, #23217, #30056, #2907, #5644, #16608, #19565, #5871, #9532, #23447, #6104, #20024, #33906, #30501, #44421, #27090, #41012, #20252, #20919, #37787, #44653, #38669, #42120, #3362, #10880, #44877, #13415, #24344, #17939, #6560, #24777, #24562, #14073, #20478, #41235, #27319, #34358, #9995, #27764, #23904, #7010, #4017, #383, #3139, #17061, #30954, #157, #14294, #17281, #31172, #10214, #13633, #35007, #38016, #34579, #17489, #3577, #27544, #38448, #7436, #34794, #41456, #3789, #28212, #27990, #31387, #24123, #21131, #17715, #6792, #41895, #20700, #45093, #21357, #31613, #35240, #13849, #41679, #10438, #10656, #38228, #7219, #8577, #15418, #1052, #8132, #5143, #18162, #14968, #28880, #22033, #42792, #22478, #32058, #36372, #25683, #1496, #29323, #607, #21806, #12002, #31838, #7668, #11553, #35699, #43237, #25461, #1279, #14746, #25905, #29095, #8351, #39364, #4694, #35928, #14518, #28430, #28658, #39132, #38898, #18614, #32505, #15191, #4475, #32288, #4917, #42344, #22255, #43006, #826, #11776, #21583, #39590, #11325, #18832, #36149, #32724, #35470, #42563, #39811, #25235, #11102, #25005, #4245, #7899, #18395 ) ),
 .UNSPECIFIED., .F., .F., .F. ) 
 B_SPLINE_SURFACE_WITH_KNOTS ( ( 2, 2 ),
 ( 3, 2, 2, 2, 2, 2, 2, 2, 2, 2, 2, 2, 2, 2, 2, 2, 2, 2, 2, 2, 2, 2, 2, 2, 2, 2, 2, 2, 2, 2, 2, 2, 2, 2, 2, 2, 2, 2, 2, 2, 2, 2, 2, 2, 2, 2, 2, 2, 2, 2, 2, 2, 2, 2, 2, 2, 2, 2, 2, 2, 2, 2, 2, 2, 2, 2, 2, 2, 2, 2, 2, 2, 2, 2, 2, 2, 2, 2, 2, 2, 2, 2, 2, 2, 2, 2, 2, 2, 2, 2, 2, 2, 2, 2, 2, 2, 2, 2, 2, 2, 2, 2, 2, 2, 2, 2, 2, 2, 2, 2, 2, 2, 2, 2, 2, 2, 2, 2, 2, 2, 2, 2, 2, 2, 2, 2, 2, 2, 3 ),
 ( 0.000000000000000000, 1.000000000000000000 ),
 ( 0.000000000000000000, 0.007812500000000000000, 0.01562500000000000000, 0.02343750000000000000, 0.03125000000000000000, 0.03906250000000000000, 0.04687500000000000000, 0.05468750000000000000, 0.06250000000000000000, 0.07031250000000000000, 0.07812500000000000000, 0.08593750000000000000, 0.09375000000000000000, 0.1015625000000000000, 0.1093750000000000000, 0.1171875000000000000, 0.1250000000000000000, 0.1328125000000000000, 0.1406250000000000000, 0.1484375000000000000, 0.1562500000000000000, 0.1640625000000000000, 0.1718750000000000000, 0.1796875000000000000, 0.1875000000000000000, 0.1953125000000000000, 0.2031250000000000000, 0.2109375000000000000, 0.2187500000000000000, 0.2265625000000000000, 0.2343750000000000000, 0.2421875000000000000, 0.2500000000000000000, 0.2578125000000000000, 0.2656250000000000000, 0.2734375000000000000, 0.2812500000000000000, 0.2890625000000000000, 0.2968750000000000000, 0.3046875000000000000, 0.3125000000000000000, 0.3203125000000000000, 0.3281250000000000000, 0.3359375000000000000, 0.3437500000000000000, 0.3515625000000000000, 0.3593750000000000000, 0.3671875000000000000, 0.3750000000000000000, 0.3828125000000000000, 0.3906250000000000000, 0.3984375000000000000, 0.4062500000000000000, 0.4140625000000000000, 0.4218750000000000000, 0.4296875000000000000, 0.4375000000000000000, 0.4453125000000000000, 0.4531250000000000000, 0.4609375000000000000, 0.4687500000000000000, 0.4765625000000000000, 0.4843750000000000000, 0.4921875000000000000, 0.5000000000000000000, 0.5078125000000000000, 0.5156250000000000000, 0.5234375000000000000, 0.5312500000000000000, 0.5390625000000000000, 0.5468750000000000000, 0.5546875000000000000, 0.5625000000000000000, 0.5703125000000000000, 0.5781250000000000000, 0.5859375000000000000, 0.5937500000000000000, 0.6015625000000000000, 0.6093750000000000000, 0.6171875000000000000, 0.6250000000000000000, 0.6328125000000000000, 0.6406250000000000000, 0.6484375000000000000, 0.6562500000000000000, 0.6640625000000000000, 0.6718750000000000000, 0.6796875000000000000, 0.6875000000000000000, 0.6953125000000000000, 0.7031250000000000000, 0.7109375000000000000, 0.7187500000000000000, 0.7265625000000000000, 0.7343750000000000000, 0.7421875000000000000, 0.7500000000000000000, 0.7578125000000000000, 0.7656250000000000000, 0.7734375000000000000, 0.7812500000000000000, 0.7890625000000000000, 0.7968750000000000000, 0.8046875000000000000, 0.8125000000000000000, 0.8203125000000000000, 0.8281250000000000000, 0.8359375000000000000, 0.8437500000000000000, 0.8515625000000000000, 0.8593750000000000000, 0.8671875000000000000, 0.8750000000000000000, 0.8828125000000000000, 0.8906250000000000000, 0.8984375000000000000, 0.9062500000000000000, 0.9140625000000000000, 0.9218750000000000000, 0.9296875000000000000, 0.9375000000000000000, 0.9453125000000000000, 0.9531250000000000000, 0.9609375000000000000, 0.9687500000000000000, 0.9765625000000000000, 0.9843750000000000000, 0.9921875000000000000, 1.000000000000000000 ),
 .UNSPECIFIED. ) 
 GEOMETRIC_REPRESENTATION_ITEM ( )  RATIONAL_B_SPLINE_SURFACE ( (
 ( 1.000000000000000000, 0.9238795325112869605, 1.000000000000000000, 0.9238795325112869605, 1.000000000000000000, 0.9238795325112869605, 1.000000000000000000, 0.9238795325112869605, 1.000000000000000000, 0.9238795325112869605, 1.000000000000000000, 0.9238795325112869605, 1.000000000000000000, 0.9238795325112869605, 1.000000000000000000, 0.9238795325112869605, 1.000000000000000000, 0.9238795325112869605, 1.000000000000000000, 0.9238795325112869605, 1.000000000000000000, 0.9238795325112869605, 1.000000000000000000, 0.9238795325112869605, 1.000000000000000000, 0.9238795325112869605, 1.000000000000000000, 0.9238795325112869605, 1.000000000000000000, 0.9238795325112869605, 1.000000000000000000, 0.9238795325112869605, 1.000000000000000000, 0.9238795325112869605, 1.000000000000000000, 0.9238795325112869605, 1.000000000000000000, 0.9238795325112869605, 1.000000000000000000, 0.9238795325112869605, 1.000000000000000000, 0.9238795325112869605, 1.000000000000000000, 0.9238795325112869605, 1.000000000000000000, 0.9238795325112869605, 1.000000000000000000, 0.9238795325112869605, 1.000000000000000000, 0.9238795325112869605, 1.000000000000000000, 0.9238795325112869605, 1.000000000000000000, 0.9238795325112869605, 1.000000000000000000, 0.9238795325112869605, 1.000000000000000000, 0.9238795325112869605, 1.000000000000000000, 0.9238795325112869605, 1.000000000000000000, 0.9238795325112869605, 1.000000000000000000, 0.9238795325112869605, 1.000000000000000000, 0.9238795325112869605, 1.000000000000000000, 0.9238795325112869605, 1.000000000000000000, 0.9238795325112869605, 1.000000000000000000, 0.9238795325112869605, 1.000000000000000000, 0.9238795325112869605, 1.000000000000000000, 0.9238795325112869605, 1.000000000000000000, 0.9238795325112869605, 1.000000000000000000, 0.9238795325112869605, 1.000000000000000000, 0.9238795325112869605, 1.000000000000000000, 0.9238795325112869605, 1.000000000000000000, 0.9238795325112869605, 1.000000000000000000, 0.9238795325112869605, 1.000000000000000000, 0.9238795325112869605, 1.000000000000000000, 0.9238795325112869605, 1.000000000000000000, 0.9238795325112869605, 1.000000000000000000, 0.9238795325112869605, 1.000000000000000000, 0.9238795325112869605, 1.000000000000000000, 0.9238795325112869605, 1.000000000000000000, 0.9238795325112869605, 1.000000000000000000, 0.9238795325112869605, 1.000000000000000000, 0.9238795325112869605, 1.000000000000000000, 0.9238795325112869605, 1.000000000000000000, 0.9238795325112869605, 1.000000000000000000, 0.9238795325112869605, 1.000000000000000000, 0.9238795325112869605, 1.000000000000000000, 0.9238795325112869605, 1.000000000000000000, 0.9238795325112869605, 1.000000000000000000, 0.9238795325112869605, 1.000000000000000000, 0.9238795325112869605, 1.000000000000000000, 0.9238795325112869605, 1.000000000000000000, 0.9238795325112869605, 1.000000000000000000, 0.9238795325112869605, 1.000000000000000000, 0.9238795325112869605, 1.000000000000000000, 0.9238795325112869605, 1.000000000000000000, 0.9238795325112869605, 1.000000000000000000, 0.9238795325112869605, 1.000000000000000000, 0.9238795325112869605, 1.000000000000000000, 0.9238795325112869605, 1.000000000000000000, 0.9238795325112869605, 1.000000000000000000, 0.9238795325112869605, 1.000000000000000000, 0.9238795325112869605, 1.000000000000000000, 0.9238795325112869605, 1.000000000000000000, 0.9238795325112869605, 1.000000000000000000, 0.9238795325112869605, 1.000000000000000000, 0.9238795325112869605, 1.000000000000000000, 0.9238795325112869605, 1.000000000000000000, 0.9238795325112869605, 1.000000000000000000, 0.9238795325112869605, 1.000000000000000000, 0.9238795325112869605, 1.000000000000000000, 0.9238795325112869605, 1.000000000000000000, 0.9238795325112869605, 1.000000000000000000, 0.9238795325112869605, 1.000000000000000000, 0.9238795325112869605, 1.000000000000000000, 0.9238795325112869605, 1.000000000000000000, 0.9238795325112869605, 1.000000000000000000, 0.9238795325112869605, 1.000000000000000000, 0.9238795325112869605, 1.000000000000000000, 0.9238795325112869605, 1.000000000000000000, 0.9238795325112869605, 1.000000000000000000, 0.9238795325112869605, 1.000000000000000000, 0.9238795325112869605, 1.000000000000000000, 0.9238795325112869605, 1.000000000000000000, 0.9238795325112869605, 1.000000000000000000, 0.9238795325112869605, 1.000000000000000000, 0.9238795325112869605, 1.000000000000000000, 0.9238795325112869605, 1.000000000000000000, 0.9238795325112869605, 1.000000000000000000, 0.9238795325112869605, 1.000000000000000000, 0.9238795325112869605, 1.000000000000000000, 0.9238795325112869605, 1.000000000000000000, 0.9238795325112869605, 1.000000000000000000, 0.9238795325112869605, 1.000000000000000000, 0.9238795325112869605, 1.000000000000000000, 0.9238795325112869605, 1.000000000000000000, 0.9238795325112869605, 1.000000000000000000, 0.9238795325112869605, 1.000000000000000000, 0.9238795325112869605, 1.000000000000000000, 0.9238795325112869605, 1.000000000000000000, 0.9238795325112869605, 1.000000000000000000, 0.9238795325112869605, 1.000000000000000000, 0.9238795325112869605, 1.000000000000000000, 0.9238795325112869605, 1.000000000000000000, 0.9238795325112869605, 1.000000000000000000, 0.9238795325112869605, 1.000000000000000000, 0.9238795325112869605, 1.000000000000000000, 0.9238795325112869605, 1.000000000000000000, 0.9238795325112869605, 1.000000000000000000, 0.9238795325112869605, 1.000000000000000000, 0.9238795325112869605, 1.000000000000000000, 0.9238795325112869605, 1.000000000000000000, 0.9238795325112869605, 1.000000000000000000, 0.9238795325112869605, 1.000000000000000000, 0.9238795325112869605, 1.000000000000000000, 0.9238795325112869605, 1.000000000000000000, 0.9238795325112869605, 1.000000000000000000, 0.9238795325112869605, 1.000000000000000000),
 ( 1.000000000000000000, 0.9238795325112869605, 1.000000000000000000, 0.9238795325112869605, 1.000000000000000000, 0.9238795325112869605, 1.000000000000000000, 0.9238795325112869605, 1.000000000000000000, 0.9238795325112869605, 1.000000000000000000, 0.9238795325112869605, 1.000000000000000000, 0.9238795325112869605, 1.000000000000000000, 0.9238795325112869605, 1.000000000000000000, 0.9238795325112869605, 1.000000000000000000, 0.9238795325112869605, 1.000000000000000000, 0.9238795325112869605, 1.000000000000000000, 0.9238795325112869605, 1.000000000000000000, 0.9238795325112869605, 1.000000000000000000, 0.9238795325112869605, 1.000000000000000000, 0.9238795325112869605, 1.000000000000000000, 0.9238795325112869605, 1.000000000000000000, 0.9238795325112869605, 1.000000000000000000, 0.9238795325112869605, 1.000000000000000000, 0.9238795325112869605, 1.000000000000000000, 0.9238795325112869605, 1.000000000000000000, 0.9238795325112869605, 1.000000000000000000, 0.9238795325112869605, 1.000000000000000000, 0.9238795325112869605, 1.000000000000000000, 0.9238795325112869605, 1.000000000000000000, 0.9238795325112869605, 1.000000000000000000, 0.9238795325112869605, 1.000000000000000000, 0.9238795325112869605, 1.000000000000000000, 0.9238795325112869605, 1.000000000000000000, 0.9238795325112869605, 1.000000000000000000, 0.9238795325112869605, 1.000000000000000000, 0.9238795325112869605, 1.000000000000000000, 0.9238795325112869605, 1.000000000000000000, 0.9238795325112869605, 1.000000000000000000, 0.9238795325112869605, 1.000000000000000000, 0.9238795325112869605, 1.000000000000000000, 0.9238795325112869605, 1.000000000000000000, 0.9238795325112869605, 1.000000000000000000, 0.9238795325112869605, 1.000000000000000000, 0.9238795325112869605, 1.000000000000000000, 0.9238795325112869605, 1.000000000000000000, 0.9238795325112869605, 1.000000000000000000, 0.9238795325112869605, 1.000000000000000000, 0.9238795325112869605, 1.000000000000000000, 0.9238795325112869605, 1.000000000000000000, 0.9238795325112869605, 1.000000000000000000, 0.9238795325112869605, 1.000000000000000000, 0.9238795325112869605, 1.000000000000000000, 0.9238795325112869605, 1.000000000000000000, 0.9238795325112869605, 1.000000000000000000, 0.9238795325112869605, 1.000000000000000000, 0.9238795325112869605, 1.000000000000000000, 0.9238795325112869605, 1.000000000000000000, 0.9238795325112869605, 1.000000000000000000, 0.9238795325112869605, 1.000000000000000000, 0.9238795325112869605, 1.000000000000000000, 0.9238795325112869605, 1.000000000000000000, 0.9238795325112869605, 1.000000000000000000, 0.9238795325112869605, 1.000000000000000000, 0.9238795325112869605, 1.000000000000000000, 0.9238795325112869605, 1.000000000000000000, 0.9238795325112869605, 1.000000000000000000, 0.9238795325112869605, 1.000000000000000000, 0.9238795325112869605, 1.000000000000000000, 0.9238795325112869605, 1.000000000000000000, 0.9238795325112869605, 1.000000000000000000, 0.9238795325112869605, 1.000000000000000000, 0.9238795325112869605, 1.000000000000000000, 0.9238795325112869605, 1.000000000000000000, 0.9238795325112869605, 1.000000000000000000, 0.9238795325112869605, 1.000000000000000000, 0.9238795325112869605, 1.000000000000000000, 0.9238795325112869605, 1.000000000000000000, 0.9238795325112869605, 1.000000000000000000, 0.9238795325112869605, 1.000000000000000000, 0.9238795325112869605, 1.000000000000000000, 0.9238795325112869605, 1.000000000000000000, 0.9238795325112869605, 1.000000000000000000, 0.9238795325112869605, 1.000000000000000000, 0.9238795325112869605, 1.000000000000000000, 0.9238795325112869605, 1.000000000000000000, 0.9238795325112869605, 1.000000000000000000, 0.9238795325112869605, 1.000000000000000000, 0.9238795325112869605, 1.000000000000000000, 0.9238795325112869605, 1.000000000000000000, 0.9238795325112869605, 1.000000000000000000, 0.9238795325112869605, 1.000000000000000000, 0.9238795325112869605, 1.000000000000000000, 0.9238795325112869605, 1.000000000000000000, 0.9238795325112869605, 1.000000000000000000, 0.9238795325112869605, 1.000000000000000000, 0.9238795325112869605, 1.000000000000000000, 0.9238795325112869605, 1.000000000000000000, 0.9238795325112869605, 1.000000000000000000, 0.9238795325112869605, 1.000000000000000000, 0.9238795325112869605, 1.000000000000000000, 0.9238795325112869605, 1.000000000000000000, 0.9238795325112869605, 1.000000000000000000, 0.9238795325112869605, 1.000000000000000000, 0.9238795325112869605, 1.000000000000000000, 0.9238795325112869605, 1.000000000000000000, 0.9238795325112869605, 1.000000000000000000, 0.9238795325112869605, 1.000000000000000000, 0.9238795325112869605, 1.000000000000000000, 0.9238795325112869605, 1.000000000000000000, 0.9238795325112869605, 1.000000000000000000, 0.9238795325112869605, 1.000000000000000000, 0.9238795325112869605, 1.000000000000000000, 0.9238795325112869605, 1.000000000000000000, 0.9238795325112869605, 1.000000000000000000, 0.9238795325112869605, 1.000000000000000000, 0.9238795325112869605, 1.000000000000000000, 0.9238795325112869605, 1.000000000000000000, 0.9238795325112869605, 1.000000000000000000, 0.9238795325112869605, 1.000000000000000000, 0.9238795325112869605, 1.000000000000000000, 0.9238795325112869605, 1.000000000000000000, 0.9238795325112869605, 1.000000000000000000, 0.9238795325112869605, 1.000000000000000000, 0.9238795325112869605, 1.000000000000000000, 0.9238795325112869605, 1.000000000000000000, 0.9238795325112869605, 1.000000000000000000, 0.9238795325112869605, 1.000000000000000000, 0.9238795325112869605, 1.000000000000000000, 0.9238795325112869605, 1.000000000000000000, 0.9238795325112869605, 1.000000000000000000, 0.9238795325112869605, 1.000000000000000000, 0.9238795325112869605, 1.000000000000000000, 0.9238795325112869605, 1.000000000000000000) ) ) 
 REPRESENTATION_ITEM ( '' )  SURFACE ( )  );
#44640=CARTESIAN_POINT ( 'NONE',  ( 122.0427081442452817, -9.859900752359378018, -12.68260735090039759 ) ) ;
#44644=CARTESIAN_POINT ( 'NONE',  ( 121.1350814775786233, 0.5811942927096110934, -14.16772938898807510 ) ) ;
#44646=CARTESIAN_POINT ( 'NONE',  ( 116.7671281442453335, -7.643976991954077427, -18.09477374809248928 ) ) ;
#44647=CARTESIAN_POINT ( 'NONE',  ( 125.2194014775786286, -10.30919188438810075, -12.61870101168855918 ) ) ;
#44651=CARTESIAN_POINT ( 'NONE',  ( 116.9373081442452929, -1.833838273342659253, -17.42832698103878286 ) ) ;
#44653=CARTESIAN_POINT ( 'NONE',  ( 118.6958348109119754, -3.505236298600246325, -18.68346056562440793 ) ) ;
#44654=CARTESIAN_POINT ( 'NONE',  ( 136.0831615568885127, -1.935278198691274598, -18.54223449093250764 ) ) ;
#44658=CARTESIAN_POINT ( 'NONE',  ( 114.6682414775786469, -1.561330072975668060, -17.79121239304076596 ) ) ;
#44659=CARTESIAN_POINT ( 'NONE',  ( 113.0686126669217799, -2.334846009198400019, -18.01015021110789149 ) ) ;
#44667=CARTESIAN_POINT ( 'NONE',  ( 122.9503348109119827, 0.5811942927096110934, -14.16772938898807510 ) ) ;
#44668=CARTESIAN_POINT ( 'NONE',  ( 114.2711548109119803, -9.988377603198976828, -10.36322818467138340 ) ) ;
#44669=CARTESIAN_POINT ( 'NONE',  ( 117.3343948109119737, -6.222761293078241884, -8.102969835052219238 ) ) ;
#44671=CARTESIAN_POINT ( 'NONE',  ( 120.3409081442453044, -0.4660016031367893996, -10.09054647747474043 ) ) ;
#44672=CARTESIAN_POINT ( 'NONE',  ( 117.5613014775786525, 0.9020085738987339008, -11.91225656197089222 ) ) ;
#44674=CARTESIAN_POINT ( 'NONE',  ( 113.0798948109119948, -8.899110576539710493, -16.42337572283490132 ) ) ;
#44677=CARTESIAN_POINT ( 'NONE',  ( 118.0151148109119816, -10.63000616557722466, -14.87417383870573495 ) ) ;
#44681=CARTESIAN_POINT ( 'NONE',  ( 114.8951481442453115, -0.4660016031367893996, -10.09054647747474043 ) ) ;
#44684=CARTESIAN_POINT ( 'NONE',  ( 120.2274548109119934, 0.5811942927096110934, -14.16772938898807510 ) ) ;
#44686=CARTESIAN_POINT ( 'NONE',  ( 112.2289948109119848, -7.643976991954077427, -18.09477374809248928 ) ) ;
#44687=CARTESIAN_POINT ( 'NONE',  ( 125.0091119737025451, -1.196538596002817867, -17.02799684832028504 ) ) ;
#44688=CARTESIAN_POINT ( 'NONE',  ( 114.7816948109119863, -9.859900752359374465, -12.68260735090039404 ) ) ;
#44689=CARTESIAN_POINT ( 'NONE',  ( 111.3850766211417067, -8.962231996695310343, -16.26240453864375723 ) ) ;
#44690=CARTESIAN_POINT ( 'NONE',  ( 116.6536748109119941, -10.15424416112533912, -14.75197769757731336 ) ) ;
#44694=CARTESIAN_POINT ( 'NONE',  ( 116.0864081442453113, -0.1624402480850797581, -16.17319339645315424 ) ) ;
#44695=CARTESIAN_POINT ( 'NONE',  ( 116.7104014775786425, -0.4660016031367893996, -10.09054647747474043 ) ) ;
#44697=CARTESIAN_POINT ( 'NONE',  ( 115.9729548109119861, -6.344957434206662583, -7.627207830600332805 ) ) ;
#44698=CARTESIAN_POINT ( 'NONE',  ( 113.7606148109119886, -7.894159318335828068, -9.358103419637847864 ) ) ;
#44699=CARTESIAN_POINT ( 'NONE',  ( 112.1722681442453222, -8.899110576539710493, -16.42337572283490132 ) ) ;
#44700=CARTESIAN_POINT ( 'NONE',  ( 115.7460481442453357, -10.15424416112533912, -14.75197769757731336 ) ) ;
#44701=ORIENTED_EDGE ( 'NONE', *, *, #3333, .F. ) ;
#44702=CARTESIAN_POINT ( 'NONE',  ( 114.7816948109119863, 0.5811942927096154232, -14.16772938898807155 ) ) ;
#44707=CARTESIAN_POINT ( 'NONE',  ( 118.8092881442453290, -9.988377603198976828, -10.36322818467138340 ) ) ;
#44708=ORIENTED_EDGE ( 'NONE', *, *, #6916, .T. ) ;
#44711=CARTESIAN_POINT ( 'NONE',  ( 119.6034614775786196, -3.505236298600246325, -18.68346056562440793 ) ) ;
#44712=CARTESIAN_POINT ( 'NONE',  ( 128.0511146350394256, 1.009132413410308571, -12.67876786587022231 ) ) ;
#44713=CARTESIAN_POINT ( 'NONE',  ( 125.1626748109119802, -9.988377603198980381, -10.36322818467138518 ) ) ;
#44716=CARTESIAN_POINT ( 'NONE',  ( 124.5930454349294365, -1.040089454026960292, -17.23633227186633476 ) ) ;
#44717=VERTEX_POINT ( 'NONE', #31907 ) ;
#44718=CARTESIAN_POINT ( 'NONE',  ( 112.5126281442453120, -10.30919188438810075, -12.61870101168855918 ) ) ;
#44719=CARTESIAN_POINT ( 'NONE',  ( 121.8158014775786171, -4.153390946401325223, -8.397313243818185668 ) ) ;
#44720=CARTESIAN_POINT ( 'NONE',  ( 125.0492214775786266, -6.344957434206665248, -7.627207830600338134 ) ) ;
#44722=CARTESIAN_POINT ( 'NONE',  ( 117.2209414775786485, -2.084020599724406786, -8.691656652584148546 ) ) ;
#44723=CARTESIAN_POINT ( 'NONE',  ( 120.0005481442453146, -5.638512984488999180, -18.83840828888717311 ) ) ;
#44725=CARTESIAN_POINT ( 'NONE',  ( 125.3328548109119964, -0.8288870151387760510, -10.36305467784173118 ) ) ;
#44726=CARTESIAN_POINT ( 'NONE',  ( 121.9292548109119849, -7.894159318335828068, -9.358103419637847864 ) ) ;
#44730=CARTESIAN_POINT ( 'NONE',  ( 115.1220548109119761, -8.166667518702817929, -8.995218007635861213 ) ) ;
#44731=CARTESIAN_POINT ( 'NONE',  ( 123.8012348109119642, -9.565557343593413364, -10.61323700422348004 ) ) ;
#44732=ORIENTED_EDGE ( 'NONE', *, *, #17958, .F. ) ;
#44734=CARTESIAN_POINT ( 'NONE',  ( 137.2352176311277958, -1.230918739026949371, -9.566601454791083370 ) ) ;
#44735=CARTESIAN_POINT ( 'NONE',  ( 119.9438214775786378, -7.893985811506177619, -18.51759400769804742 ) ) ;
#44737=CARTESIAN_POINT ( 'NONE',  ( 118.4122014775786340, -9.859900752359374465, -12.68260735090039404 ) ) ;
#44739=ORIENTED_EDGE ( 'NONE', *, *, #6637, .F. ) ;
#44740=CARTESIAN_POINT ( 'NONE',  ( 126.6942948109119840, -8.899110576539710493, -16.42337572283490132 ) ) ;
#44741=CARTESIAN_POINT ( 'NONE',  ( 123.1205148109119563, -7.643976991954077427, -18.09477374809248928 ) ) ;
#44744=CARTESIAN_POINT ( 'NONE',  ( 121.0216281442452981, -1.561330072975668948, -17.79121239304076951 ) ) ;
#44745=CARTESIAN_POINT ( 'NONE',  ( 111.4915825099123339, -9.071269598371342724, -16.57136686325032926 ) ) ;
#44748=CARTESIAN_POINT ( 'NONE',  ( 120.0572748109119772, -3.383040157471821630, -19.15922257007629170 ) ) ;
#44749=CARTESIAN_POINT ( 'NONE',  ( 118.5823814775786360, -1.834011780172310813, -8.268836392978581529 ) ) ;
#44750=CARTESIAN_POINT ( 'NONE',  ( 121.1918081442452859, -10.15424416112533912, -14.75197769757731336 ) ) ;
#44751=CARTESIAN_POINT ( 'NONE',  ( 124.3685014775786328, 0.4262465694468514643, -12.03445270309931736 ) ) ;
#44752=CARTESIAN_POINT ( 'NONE',  ( 117.5613014775786525, 0.9020085738987339008, -11.91225656197089222 ) ) ;
#44754=CARTESIAN_POINT ( 'NONE',  ( 125.2761281442453054, 0.4262465694468514643, -12.03445270309931736 ) ) ;
#44759=CARTESIAN_POINT ( 'NONE',  ( 121.1918081442452859, 0.9020085738987339008, -11.91225656197089222 ) ) ;
#44760=CARTESIAN_POINT ( 'NONE',  ( 123.6310548109119765, -4.153390946401325223, -8.397313243818185668 ) ) ;
#44762=CARTESIAN_POINT ( 'NONE',  ( 123.6310548109119765, -5.638512984488999180, -18.83840828888717311 ) ) ;
#44764=CARTESIAN_POINT ( 'NONE',  ( 113.3068014775786594, -1.833838273342658809, -17.42832698103878286 ) ) ;
#44766=CARTESIAN_POINT ( 'NONE',  ( 124.9357681442453014, -1.834011780172310813, -8.268836392978581529 ) ) ;
#44767=CARTESIAN_POINT ( 'NONE',  ( 120.7379948109119709, -10.63000616557722466, -14.87417383870573495 ) ) ;
#44769=CARTESIAN_POINT ( 'NONE',  ( 113.2500748109119968, -6.344957434206662583, -7.627207830600332805 ) ) ;
#44770=CARTESIAN_POINT ( 'NONE',  ( 111.8079953496756787, -1.087735405160635382, -17.17288456429613674 ) ) ;
#44773=ORIENTED_EDGE ( 'NONE', *, *, #29199, .F. ) ;
#44774=DIRECTION ( 'NONE',  ( 0.000000000000000000, 0.6004852223388323917, -0.7996358532186279566 ) ) ;
#44775=CARTESIAN_POINT ( 'NONE',  ( 118.5378868052895456, -1.125321370491268125, -17.12283323191015327 ) ) ;
#44776=CARTESIAN_POINT ( 'NONE',  ( 124.2550481442452792, -0.1624402480850797581, -16.17319339645315424 ) ) ;
#44779=CARTESIAN_POINT ( 'NONE',  ( 123.0070614775786169, -10.15424416112533912, -14.75197769757731336 ) ) ;
#44780=CARTESIAN_POINT ( 'NONE',  ( 116.1431348109119881, 0.1319031606808879209, -14.10382304977623669 ) ) ;
#44781=CARTESIAN_POINT ( 'NONE',  ( 112.7395348109119766, -4.153390946401321671, -8.397313243818183892 ) ) ;
#44784=CARTESIAN_POINT ( 'NONE',  ( 121.1350814775786233, -9.859900752359378018, -12.68260735090039759 ) ) ;
#44785=CARTESIAN_POINT ( 'NONE',  ( 117.3343948109119737, -3.383040157471821630, -19.15922257007629170 ) ) ;
#44790=CARTESIAN_POINT ( 'NONE',  ( 115.7460481442453357, -10.15424416112533912, -14.75197769757731336 ) ) ;
#44791=CARTESIAN_POINT ( 'NONE',  ( 113.9875214775786532, -8.899110576539710493, -16.42337572283490132 ) ) ;
#44792=CARTESIAN_POINT ( 'NONE',  ( 115.0653281442453135, -6.344957434206662583, -7.627207830600333693 ) ) ;
#44800=CARTESIAN_POINT ( 'NONE',  ( 124.3685014775786328, 0.4262465694468514643, -12.03445270309931736 ) ) ;
#44801=CARTESIAN_POINT ( 'NONE',  ( 113.4202548109119846, 0.1319031606808879209, -14.10382304977623669 ) ) ;
#44802=CARTESIAN_POINT ( 'NONE',  ( 126.2561087589866275, -5.799764584263661149, -18.32404662456333000 ) ) ;
#44806=CARTESIAN_POINT ( 'NONE',  ( 112.1722681442453222, -8.899110576539710493, -16.42337572283490132 ) ) ;
#44812=CARTESIAN_POINT ( 'NONE',  ( 124.6521348109119884, -7.894159318335828068, -9.358103419637847864 ) ) ;
#44814=CARTESIAN_POINT ( 'NONE',  ( 111.9453614775786434, -1.561330072975668060, -17.79121239304076596 ) ) ;
#44817=CARTESIAN_POINT ( 'NONE',  ( 125.6732148109119862, -9.859900752359378018, -12.68260735090039759 ) ) ;
#44818=CARTESIAN_POINT ( 'NONE',  ( 122.3830681442452857, -1.833838273342659697, -17.42832698103878286 ) ) ;
#44822=CARTESIAN_POINT ( 'NONE',  ( 120.4709786403692249, -1.196538596002817867, -17.02799684832028504 ) ) ;
#44824=CARTESIAN_POINT ( 'NONE',  ( 112.9097148109119928, -9.565557343593411588, -10.61323700422346583 ) ) ;
#44826=CARTESIAN_POINT ( 'NONE',  ( 117.5045748109119756, 0.5811942927096067635, -14.16772938898808576 ) ) ;
#44829=CARTESIAN_POINT ( 'NONE',  ( 111.8886348109120092, -6.222761293078241884, -8.102969835052219238 ) ) ;
#44831=( BOUNDED_SURFACE ( )  B_SPLINE_SURFACE ( 1, 2, ( 
 ( #23726, #19610, #44021, #19843, #40828, #2729, #15973, #26463, #41285, #20523, #16885, #27365, #12782, #30549, #34183, #16202, #13463, #13235, #16654, #30105, #2049, #10048, #9354, #30325, #40366, #33961, #33731, #33494, #6156, #5921, #44470, #9583, #23499, #23952, #20076, #9817, #37385, #43792, #6391, #9129, #20298, #2958, #27137, #16429, #44252, #26684, #2502, #36921, #30777, #2272, #40596, #23264, #13009, #26908, #44702, #37833, #6610, #29876, #5691, #17984, #41720, #24827, #17541, #41506, #20744, #34836, #6838, #17109, #24607, #38950, #7717, #38718, #38272, #7489, #10925, #34623, #24386, #7053, #42164, #10484, #38490, #41941, #3409, #10261, #21182, #20964, #21406, #35287, #3621, #34403, #7265, #201, #4060, #31434, #31884, #28034, #42387, #30999, #3184, #14117, #24168, #11151, #31657, #425, #649, #17760, #35059, #28483, #14564, #25057, #10704, #44925, #13683, #3840, #27593, #14341, #38060, #17326, #28255, #31216, #45142, #13899, #27805, #43283, #8627, #7943, #15019, #43058, #32558, #11825, #18446, #25732, #18880, #14793, #22527, #18665, #25283, #36423, #4290, #39413, #29145, #28707, #39639, #8403, #42614, #32994, #15236, #19110, #15466, #1325, #1768, #29372, #1102, #12054, #25955, #21854, #22086, #15694, #35974, #35750, #29596, #22307, #32107, #12282, #36203, #21630, #40086, #39862, #28930, #5192, #4970, #32771, #4745, #11377, #18209, #43513, #26178, #8176, #1545, #35518, #42837, #39179, #874, #32335, #4523, #11598, #25508, #44416, #19787, #29821, #9759, #8847, #40313, #16831, #22980, #36869, #16603, #16146, #30272, #5421, #37327, #5639, #37561, #43737, #6330, #30496, #26403, #19560, #26630, #2449, #9526, #22747, #19338, #2902, #27312, #23671, #34133, #33437, #6098, #41006, #2216, #20247, #20018, #23442, #30050, #36648, #30724, #43963, #37091, #33223, #40768, #40543, #9077, #12959, #12727, #33901, #16369, #44197, #44647, #26855, #2671, #13182, #9304, #13409, #27085, #1998, #12507, #15924, #23212, #5865, #33671, #10876, #38011, #31382, #17935, #14514, #17710 ),
 ( #7432, #10433, #10209, #21352, #34789, #6555, #31834, #20915, #37782, #378, #20472, #35002, #42116, #3573, #24340, #38224, #24117, #13844, #34353, #153, #13628, #34573, #6786, #41451, #20695, #3785, #38444, #27539, #14290, #31609, #3357, #9990, #14068, #23899, #28208, #7006, #17056, #24772, #41230, #17275, #4012, #31167, #45088, #38664, #27760, #17485, #3133, #24558, #41675, #35236, #30948, #603, #44872, #27986, #41891, #10652, #7214, #21127, #42338, #38894, #22474, #1717, #43232, #8573, #25231, #11771, #15414, #42559, #39806, #39586, #43002, #11320, #28426, #36368, #35695, #11549, #7663, #15187, #14963, #821, #32501, #32282, #29091, #22029, #35923, #5139, #1275, #22249, #18609, #1048, #19055, #4689, #21579, #4241, #18828, #35466, #42788, #25679, #11998, #39128, #8347, #32941, #11098, #4913, #36145, #25901, #32720, #18391, #1492, #7895, #25000, #28876, #29319, #18158, #4471, #8127, #14741, #32054, #28653, #25457, #21802, #39360, #16088, #23160, #26577, #2392, #22924, #37041, #33615, #26123, #19961, #40491, #9474, #40260, #40028, #23385, #29993, #20198, #22699, #36595, #15640, #34082, #6039, #36817, #44367, #5811, #30223, #43910, #8792, #43461, #33850, #27033, #2160, #12679, #16552, #9026, #5371, #5586, #19288, #16320, #9252, #19730, #44143, #12909, #19509, #26805, #40715, #33167, #2619, #37270, #30447, #33387, #1943, #13129, #40948, #29544, #15868, #29765, #12225, #43676, #9705, #23618, #37504, #6278, #12451, #26352, #41176, #30674, #21075, #14238, #34522, #45039, #3738, #27487, #23850, #24506, #44818, #16781, #20860, #44594, #38391, #13799, #37736, #17661, #2849, #34306, #10822, #17007, #30896, #10604, #10161, #24291, #13357, #31332, #13576, #31557, #6507, #325, #7163, #20422, #41405, #20646, #41625, #3521, #27262, #9936, #42065, #21302, #28155, #24719, #24069, #106, #34952, #37960, #38608, #14019, #17439, #6736, #3079, #7384, #3300, #31115, #17224, #34739, #27711, #10381, #6955, #38177, #27934, #41844, #28825, #11948, #8075, #29044, #25405, #39077, #25844 ) ),
 .UNSPECIFIED., .F., .F., .T. ) 
 B_SPLINE_SURFACE_WITH_KNOTS ( ( 2, 2 ),
 ( 3, 2, 2, 2, 2, 2, 2, 2, 2, 2, 2, 2, 2, 2, 2, 2, 2, 2, 2, 2, 2, 2, 2, 2, 2, 2, 2, 2, 2, 2, 2, 2, 2, 2, 2, 2, 2, 2, 2, 2, 2, 2, 2, 2, 2, 2, 2, 2, 2, 2, 2, 2, 2, 2, 2, 2, 2, 2, 2, 2, 2, 2, 2, 2, 2, 2, 2, 2, 2, 2, 2, 2, 2, 2, 2, 2, 2, 2, 2, 2, 2, 2, 2, 2, 2, 2, 2, 2, 2, 2, 2, 2, 2, 2, 2, 2, 2, 2, 2, 2, 2, 2, 2, 2, 2, 2, 2, 2, 2, 2, 2, 2, 2, 2, 2, 2, 2, 2, 2, 2, 2, 2, 2, 2, 2, 2, 2, 2, 3 ),
 ( 0.000000000000000000, 1.000000000000000000 ),
 ( 0.000000000000000000, 0.007812500000000000000, 0.01562500000000000000, 0.02343750000000000000, 0.03125000000000000000, 0.03906250000000000000, 0.04687500000000000000, 0.05468750000000000000, 0.06250000000000000000, 0.07031250000000000000, 0.07812500000000000000, 0.08593750000000000000, 0.09375000000000000000, 0.1015625000000000000, 0.1093750000000000000, 0.1171875000000000000, 0.1250000000000000000, 0.1328125000000000000, 0.1406250000000000000, 0.1484375000000000000, 0.1562500000000000000, 0.1640625000000000000, 0.1718750000000000000, 0.1796875000000000000, 0.1875000000000000000, 0.1953125000000000000, 0.2031250000000000000, 0.2109375000000000000, 0.2187500000000000000, 0.2265625000000000000, 0.2343750000000000000, 0.2421875000000000000, 0.2500000000000000000, 0.2578125000000000000, 0.2656250000000000000, 0.2734375000000000000, 0.2812500000000000000, 0.2890625000000000000, 0.2968750000000000000, 0.3046875000000000000, 0.3125000000000000000, 0.3203125000000000000, 0.3281250000000000000, 0.3359375000000000000, 0.3437500000000000000, 0.3515625000000000000, 0.3593750000000000000, 0.3671875000000000000, 0.3750000000000000000, 0.3828125000000000000, 0.3906250000000000000, 0.3984375000000000000, 0.4062500000000000000, 0.4140625000000000000, 0.4218750000000000000, 0.4296875000000000000, 0.4375000000000000000, 0.4453125000000000000, 0.4531250000000000000, 0.4609375000000000000, 0.4687500000000000000, 0.4765625000000000000, 0.4843750000000000000, 0.4921875000000000000, 0.5000000000000000000, 0.5078125000000000000, 0.5156250000000000000, 0.5234375000000000000, 0.5312500000000000000, 0.5390625000000000000, 0.5468750000000000000, 0.5546875000000000000, 0.5625000000000000000, 0.5703125000000000000, 0.5781250000000000000, 0.5859375000000000000, 0.5937500000000000000, 0.6015625000000000000, 0.6093750000000000000, 0.6171875000000000000, 0.6250000000000000000, 0.6328125000000000000, 0.6406250000000000000, 0.6484375000000000000, 0.6562500000000000000, 0.6640625000000000000, 0.6718750000000000000, 0.6796875000000000000, 0.6875000000000000000, 0.6953125000000000000, 0.7031250000000000000, 0.7109375000000000000, 0.7187500000000000000, 0.7265625000000000000, 0.7343750000000000000, 0.7421875000000000000, 0.7500000000000000000, 0.7578125000000000000, 0.7656250000000000000, 0.7734375000000000000, 0.7812500000000000000, 0.7890625000000000000, 0.7968750000000000000, 0.8046875000000000000, 0.8125000000000000000, 0.8203125000000000000, 0.8281250000000000000, 0.8359375000000000000, 0.8437500000000000000, 0.8515625000000000000, 0.8593750000000000000, 0.8671875000000000000, 0.8750000000000000000, 0.8828125000000000000, 0.8906250000000000000, 0.8984375000000000000, 0.9062500000000000000, 0.9140625000000000000, 0.9218750000000000000, 0.9296875000000000000, 0.9375000000000000000, 0.9453125000000000000, 0.9531250000000000000, 0.9609375000000000000, 0.9687500000000000000, 0.9765625000000000000, 0.9843750000000000000, 0.9921875000000000000, 1.000000000000000000 ),
 .UNSPECIFIED. ) 
 GEOMETRIC_REPRESENTATION_ITEM ( )  RATIONAL_B_SPLINE_SURFACE ( (
 ( 1.000000000000000000, 0.9238795325112869605, 1.000000000000000000, 0.9238795325112869605, 1.000000000000000000, 0.9238795325112869605, 1.000000000000000000, 0.9238795325112869605, 1.000000000000000000, 0.9238795325112869605, 1.000000000000000000, 0.9238795325112869605, 1.000000000000000000, 0.9238795325112869605, 1.000000000000000000, 0.9238795325112869605, 1.000000000000000000, 0.9238795325112869605, 1.000000000000000000, 0.9238795325112869605, 1.000000000000000000, 0.9238795325112869605, 1.000000000000000000, 0.9238795325112869605, 1.000000000000000000, 0.9238795325112869605, 1.000000000000000000, 0.9238795325112869605, 1.000000000000000000, 0.9238795325112869605, 1.000000000000000000, 0.9238795325112869605, 1.000000000000000000, 0.9238795325112869605, 1.000000000000000000, 0.9238795325112869605, 1.000000000000000000, 0.9238795325112869605, 1.000000000000000000, 0.9238795325112869605, 1.000000000000000000, 0.9238795325112869605, 1.000000000000000000, 0.9238795325112869605, 1.000000000000000000, 0.9238795325112869605, 1.000000000000000000, 0.9238795325112869605, 1.000000000000000000, 0.9238795325112869605, 1.000000000000000000, 0.9238795325112869605, 1.000000000000000000, 0.9238795325112869605, 1.000000000000000000, 0.9238795325112869605, 1.000000000000000000, 0.9238795325112869605, 1.000000000000000000, 0.9238795325112869605, 1.000000000000000000, 0.9238795325112869605, 1.000000000000000000, 0.9238795325112869605, 1.000000000000000000, 0.9238795325112869605, 1.000000000000000000, 0.9238795325112869605, 1.000000000000000000, 0.9238795325112869605, 1.000000000000000000, 0.9238795325112869605, 1.000000000000000000, 0.9238795325112869605, 1.000000000000000000, 0.9238795325112869605, 1.000000000000000000, 0.9238795325112869605, 1.000000000000000000, 0.9238795325112869605, 1.000000000000000000, 0.9238795325112869605, 1.000000000000000000, 0.9238795325112869605, 1.000000000000000000, 0.9238795325112869605, 1.000000000000000000, 0.9238795325112869605, 1.000000000000000000, 0.9238795325112869605, 1.000000000000000000, 0.9238795325112869605, 1.000000000000000000, 0.9238795325112869605, 1.000000000000000000, 0.9238795325112869605, 1.000000000000000000, 0.9238795325112869605, 1.000000000000000000, 0.9238795325112869605, 1.000000000000000000, 0.9238795325112869605, 1.000000000000000000, 0.9238795325112869605, 1.000000000000000000, 0.9238795325112869605, 1.000000000000000000, 0.9238795325112869605, 1.000000000000000000, 0.9238795325112869605, 1.000000000000000000, 0.9238795325112869605, 1.000000000000000000, 0.9238795325112869605, 1.000000000000000000, 0.9238795325112869605, 1.000000000000000000, 0.9238795325112869605, 1.000000000000000000, 0.9238795325112869605, 1.000000000000000000, 0.9238795325112869605, 1.000000000000000000, 0.9238795325112869605, 1.000000000000000000, 0.9238795325112869605, 1.000000000000000000, 0.9238795325112869605, 1.000000000000000000, 0.9238795325112869605, 1.000000000000000000, 0.9238795325112869605, 1.000000000000000000, 0.9238795325112869605, 1.000000000000000000, 0.9238795325112869605, 1.000000000000000000, 0.9238795325112869605, 1.000000000000000000, 0.9238795325112869605, 1.000000000000000000, 0.9238795325112869605, 1.000000000000000000, 0.9238795325112869605, 1.000000000000000000, 0.9238795325112869605, 1.000000000000000000, 0.9238795325112869605, 1.000000000000000000, 0.9238795325112869605, 1.000000000000000000, 0.9238795325112869605, 1.000000000000000000, 0.9238795325112869605, 1.000000000000000000, 0.9238795325112869605, 1.000000000000000000, 0.9238795325112869605, 1.000000000000000000, 0.9238795325112869605, 1.000000000000000000, 0.9238795325112869605, 1.000000000000000000, 0.9238795325112869605, 1.000000000000000000, 0.9238795325112869605, 1.000000000000000000, 0.9238795325112869605, 1.000000000000000000, 0.9238795325112869605, 1.000000000000000000, 0.9238795325112869605, 1.000000000000000000, 0.9238795325112869605, 1.000000000000000000, 0.9238795325112869605, 1.000000000000000000, 0.9238795325112869605, 1.000000000000000000, 0.9238795325112869605, 1.000000000000000000, 0.9238795325112869605, 1.000000000000000000, 0.9238795325112869605, 1.000000000000000000, 0.9238795325112869605, 1.000000000000000000, 0.9238795325112869605, 1.000000000000000000, 0.9238795325112869605, 1.000000000000000000, 0.9238795325112869605, 1.000000000000000000, 0.9238795325112869605, 1.000000000000000000, 0.9238795325112869605, 1.000000000000000000, 0.9238795325112869605, 1.000000000000000000, 0.9238795325112869605, 1.000000000000000000, 0.9238795325112869605, 1.000000000000000000, 0.9238795325112869605, 1.000000000000000000, 0.9238795325112869605, 1.000000000000000000, 0.9238795325112869605, 1.000000000000000000, 0.9238795325112869605, 1.000000000000000000, 0.9238795325112869605, 1.000000000000000000, 0.9238795325112869605, 1.000000000000000000, 0.9238795325112869605, 1.000000000000000000, 0.9238795325112869605, 1.000000000000000000, 0.9238795325112869605, 1.000000000000000000, 0.9238795325112869605, 1.000000000000000000, 0.9238795325112869605, 1.000000000000000000, 0.9238795325112869605, 1.000000000000000000, 0.9238795325112869605, 1.000000000000000000, 0.9238795325112869605, 1.000000000000000000, 0.9238795325112869605, 1.000000000000000000, 0.9238795325112869605, 1.000000000000000000, 0.9238795325112869605, 1.000000000000000000, 0.9238795325112869605, 1.000000000000000000, 0.9238795325112869605, 1.000000000000000000, 0.9238795325112869605, 1.000000000000000000, 0.9238795325112869605, 1.000000000000000000, 0.9238795325112869605, 1.000000000000000000, 0.9238795325112869605, 1.000000000000000000, 0.9238795325112869605, 1.000000000000000000, 0.9238795325112869605, 1.000000000000000000, 0.9238795325112869605, 1.000000000000000000, 0.9238795325112869605, 1.000000000000000000),
 ( 1.000000000000000000, 0.9238795325112869605, 1.000000000000000000, 0.9238795325112869605, 1.000000000000000000, 0.9238795325112869605, 1.000000000000000000, 0.9238795325112869605, 1.000000000000000000, 0.9238795325112869605, 1.000000000000000000, 0.9238795325112869605, 1.000000000000000000, 0.9238795325112869605, 1.000000000000000000, 0.9238795325112869605, 1.000000000000000000, 0.9238795325112869605, 1.000000000000000000, 0.9238795325112869605, 1.000000000000000000, 0.9238795325112869605, 1.000000000000000000, 0.9238795325112869605, 1.000000000000000000, 0.9238795325112869605, 1.000000000000000000, 0.9238795325112869605, 1.000000000000000000, 0.9238795325112869605, 1.000000000000000000, 0.9238795325112869605, 1.000000000000000000, 0.9238795325112869605, 1.000000000000000000, 0.9238795325112869605, 1.000000000000000000, 0.9238795325112869605, 1.000000000000000000, 0.9238795325112869605, 1.000000000000000000, 0.9238795325112869605, 1.000000000000000000, 0.9238795325112869605, 1.000000000000000000, 0.9238795325112869605, 1.000000000000000000, 0.9238795325112869605, 1.000000000000000000, 0.9238795325112869605, 1.000000000000000000, 0.9238795325112869605, 1.000000000000000000, 0.9238795325112869605, 1.000000000000000000, 0.9238795325112869605, 1.000000000000000000, 0.9238795325112869605, 1.000000000000000000, 0.9238795325112869605, 1.000000000000000000, 0.9238795325112869605, 1.000000000000000000, 0.9238795325112869605, 1.000000000000000000, 0.9238795325112869605, 1.000000000000000000, 0.9238795325112869605, 1.000000000000000000, 0.9238795325112869605, 1.000000000000000000, 0.9238795325112869605, 1.000000000000000000, 0.9238795325112869605, 1.000000000000000000, 0.9238795325112869605, 1.000000000000000000, 0.9238795325112869605, 1.000000000000000000, 0.9238795325112869605, 1.000000000000000000, 0.9238795325112869605, 1.000000000000000000, 0.9238795325112869605, 1.000000000000000000, 0.9238795325112869605, 1.000000000000000000, 0.9238795325112869605, 1.000000000000000000, 0.9238795325112869605, 1.000000000000000000, 0.9238795325112869605, 1.000000000000000000, 0.9238795325112869605, 1.000000000000000000, 0.9238795325112869605, 1.000000000000000000, 0.9238795325112869605, 1.000000000000000000, 0.9238795325112869605, 1.000000000000000000, 0.9238795325112869605, 1.000000000000000000, 0.9238795325112869605, 1.000000000000000000, 0.9238795325112869605, 1.000000000000000000, 0.9238795325112869605, 1.000000000000000000, 0.9238795325112869605, 1.000000000000000000, 0.9238795325112869605, 1.000000000000000000, 0.9238795325112869605, 1.000000000000000000, 0.9238795325112869605, 1.000000000000000000, 0.9238795325112869605, 1.000000000000000000, 0.9238795325112869605, 1.000000000000000000, 0.9238795325112869605, 1.000000000000000000, 0.9238795325112869605, 1.000000000000000000, 0.9238795325112869605, 1.000000000000000000, 0.9238795325112869605, 1.000000000000000000, 0.9238795325112869605, 1.000000000000000000, 0.9238795325112869605, 1.000000000000000000, 0.9238795325112869605, 1.000000000000000000, 0.9238795325112869605, 1.000000000000000000, 0.9238795325112869605, 1.000000000000000000, 0.9238795325112869605, 1.000000000000000000, 0.9238795325112869605, 1.000000000000000000, 0.9238795325112869605, 1.000000000000000000, 0.9238795325112869605, 1.000000000000000000, 0.9238795325112869605, 1.000000000000000000, 0.9238795325112869605, 1.000000000000000000, 0.9238795325112869605, 1.000000000000000000, 0.9238795325112869605, 1.000000000000000000, 0.9238795325112869605, 1.000000000000000000, 0.9238795325112869605, 1.000000000000000000, 0.9238795325112869605, 1.000000000000000000, 0.9238795325112869605, 1.000000000000000000, 0.9238795325112869605, 1.000000000000000000, 0.9238795325112869605, 1.000000000000000000, 0.9238795325112869605, 1.000000000000000000, 0.9238795325112869605, 1.000000000000000000, 0.9238795325112869605, 1.000000000000000000, 0.9238795325112869605, 1.000000000000000000, 0.9238795325112869605, 1.000000000000000000, 0.9238795325112869605, 1.000000000000000000, 0.9238795325112869605, 1.000000000000000000, 0.9238795325112869605, 1.000000000000000000, 0.9238795325112869605, 1.000000000000000000, 0.9238795325112869605, 1.000000000000000000, 0.9238795325112869605, 1.000000000000000000, 0.9238795325112869605, 1.000000000000000000, 0.9238795325112869605, 1.000000000000000000, 0.9238795325112869605, 1.000000000000000000, 0.9238795325112869605, 1.000000000000000000, 0.9238795325112869605, 1.000000000000000000, 0.9238795325112869605, 1.000000000000000000, 0.9238795325112869605, 1.000000000000000000, 0.9238795325112869605, 1.000000000000000000, 0.9238795325112869605, 1.000000000000000000, 0.9238795325112869605, 1.000000000000000000, 0.9238795325112869605, 1.000000000000000000, 0.9238795325112869605, 1.000000000000000000, 0.9238795325112869605, 1.000000000000000000, 0.9238795325112869605, 1.000000000000000000, 0.9238795325112869605, 1.000000000000000000, 0.9238795325112869605, 1.000000000000000000, 0.9238795325112869605, 1.000000000000000000, 0.9238795325112869605, 1.000000000000000000, 0.9238795325112869605, 1.000000000000000000, 0.9238795325112869605, 1.000000000000000000, 0.9238795325112869605, 1.000000000000000000, 0.9238795325112869605, 1.000000000000000000, 0.9238795325112869605, 1.000000000000000000, 0.9238795325112869605, 1.000000000000000000, 0.9238795325112869605, 1.000000000000000000, 0.9238795325112869605, 1.000000000000000000, 0.9238795325112869605, 1.000000000000000000, 0.9238795325112869605, 1.000000000000000000, 0.9238795325112869605, 1.000000000000000000, 0.9238795325112869605, 1.000000000000000000, 0.9238795325112869605, 1.000000000000000000, 0.9238795325112869605, 1.000000000000000000, 0.9238795325112869605, 1.000000000000000000, 0.9238795325112869605, 1.000000000000000000) ) ) 
 REPRESENTATION_ITEM ( '' )  SURFACE ( )  );
#44832=CARTESIAN_POINT ( 'NONE',  ( 120.9649014775786355, -3.383040157471821630, -19.15922257007629170 ) ) ;
#44833=CARTESIAN_POINT ( 'NONE',  ( 112.0020881442453344, 0.2603800115204892296, -16.42320221600525088 ) ) ;
#44835=CARTESIAN_POINT ( 'NONE',  ( 112.9664414775786412, -9.859900752359374465, -12.68260735090039404 ) ) ;
#44838=CARTESIAN_POINT ( 'NONE',  ( 125.9001214775786224, -4.089484607189486809, -7.948022111789456723 ) ) ;
#44839=CARTESIAN_POINT ( 'NONE',  ( 124.9924948109119924, -4.089484607189486809, -7.948022111789456723 ) ) ;
#44840=CARTESIAN_POINT ( 'NONE',  ( 114.1577014775786552, -6.344957434206662583, -7.627207830600332805 ) ) ;
#44841=CARTESIAN_POINT ( 'NONE',  ( 116.1998614775786507, 0.4262465694468514643, -12.03445270309931736 ) ) ;
#44844=CARTESIAN_POINT ( 'NONE',  ( 118.9227414775786542, 0.4262465694468514643, -12.03445270309931736 ) ) ;
#44845=EDGE_CURVE ( 'NONE', #21905, #3495, #42859, .T. ) ;
#44848=CARTESIAN_POINT ( 'NONE',  ( 116.9373081442452929, -8.166667518702817929, -8.995218007635861213 ) ) ;
#44849=CARTESIAN_POINT ( 'NONE',  ( 123.0070614775786169, -10.15424416112533912, -14.75197769757731336 ) ) ;
#44852=ORIENTED_EDGE ( 'NONE', *, *, #11469, .T. ) ;
#44858=CARTESIAN_POINT ( 'NONE',  ( 112.3991748109119868, -1.833838273342658809, -17.42832698103878286 ) ) ;
#44861=CARTESIAN_POINT ( 'NONE',  ( 119.4332814775786318, -0.4660016031367893996, -10.09054647747474043 ) ) ;
#44862=CARTESIAN_POINT ( 'NONE',  ( 136.4577890465943995, -4.246979716881710942, -19.12709517244668334 ) ) ;
#44864=CARTESIAN_POINT ( 'NONE',  ( 118.9794681442453026, -9.261995988541702474, -16.69588392320187964 ) ) ;
#44865=CARTESIAN_POINT ( 'NONE',  ( 121.5888948109119809, 0.1319031606808879209, -14.10382304977623669 ) ) ;
#44867=CARTESIAN_POINT ( 'NONE',  ( 126.1270281442452870, -10.30919188438810075, -12.61870101168855918 ) ) ;
#44868=CARTESIAN_POINT ( 'NONE',  ( 119.2063748109119814, -1.561330072975668504, -17.79121239304076951 ) ) ;
#44870=CARTESIAN_POINT ( 'NONE',  ( 116.3133148109120043, -2.084020599724406786, -8.691656652584148546 ) ) ;
#44872=CARTESIAN_POINT ( 'NONE',  ( 114.2144281442453178, -1.833838273342658809, -17.42832698103878286 ) ) ;
#44876=CARTESIAN_POINT ( 'NONE',  ( 118.3554748109119998, -9.565557343593413364, -10.61323700422348004 ) ) ;
#44877=CARTESIAN_POINT ( 'NONE',  ( 118.9794681442453026, -0.8288870151387760510, -10.36305467784173118 ) ) ;
#44883=CARTESIAN_POINT ( 'NONE',  ( 113.5337081442453240, -9.261995988541697145, -16.69588392320189030 ) ) ;
#44884=CARTESIAN_POINT ( 'NONE',  ( 115.1220548109119761, -8.166667518702817929, -8.995218007635861213 ) ) ;
#44888=LINE ( 'NONE', #5881, #10130 ) ;
#44890=CARTESIAN_POINT ( 'NONE',  ( 121.4187148109119789, -6.344957434206665248, -7.627207830600338134 ) ) ;
#44891=CARTESIAN_POINT ( 'NONE',  ( 113.0798948109119948, -0.4660016031367893996, -10.09054647747474043 ) ) ;
#44892=CARTESIAN_POINT ( 'NONE',  ( 117.0507614775786465, 0.1319031606808879209, -14.10382304977623669 ) ) ;
#44895=CARTESIAN_POINT ( 'NONE',  ( 122.4965214775786251, -10.30919188438810075, -12.61870101168855918 ) ) ;
#44896=CARTESIAN_POINT ( 'NONE',  ( 116.8238548109119819, -4.089484607189486809, -7.948022111789456723 ) ) ;
#44899=CARTESIAN_POINT ( 'NONE',  ( 111.9453614775786434, -7.894159318335828068, -9.358103419637847864 ) ) ;
#44900=CARTESIAN_POINT ( 'NONE',  ( 117.8659193777725278, -1.267766418764730840, -16.93314635290706605 ) ) ;
#44903=CARTESIAN_POINT ( 'NONE',  ( 117.8449348109119938, -8.166667518702817929, -8.995218007635861213 ) ) ;
#44906=CARTESIAN_POINT ( 'NONE',  ( 115.6325948109119821, 0.2603800115204892296, -16.42320221600525088 ) ) ;
#44909=CARTESIAN_POINT ( 'NONE',  ( 123.8012348109119642, 0.2603800115204892296, -16.42320221600525088 ) ) ;
#44914=CARTESIAN_POINT ( 'NONE',  ( 117.3343948109119737, -6.222761293078241884, -8.102969835052219238 ) ) ;
#44916=CARTESIAN_POINT ( 'NONE',  ( 117.0507614775786465, 0.1319031606808879209, -14.10382304977623669 ) ) ;
#44919=CARTESIAN_POINT ( 'NONE',  ( 115.5191414775786569, -6.222761293078241884, -8.102969835052219238 ) ) ;
#44921=CARTESIAN_POINT ( 'NONE',  ( 114.4413348109119823, -9.261995988541697145, -16.69588392320189030 ) ) ;
#44922=CARTESIAN_POINT ( 'NONE',  ( 111.3780948109119890, -5.574606645277164318, -18.38911715685844683 ) ) ;
#44923=CARTESIAN_POINT ( 'NONE',  ( 118.2420214775786320, -6.222761293078241884, -8.102969835052219238 ) ) ;
#44925=CARTESIAN_POINT ( 'NONE',  ( 118.0151148109119816, -10.63000616557722466, -14.87417383870573495 ) ) ;
#44929=CARTESIAN_POINT ( 'NONE',  ( 111.2646414775786496, -8.862178061932382889, -16.39564131203247399 ) ) ;
#44931=CARTESIAN_POINT ( 'NONE',  ( 121.3052614775786111, -1.834011780172310813, -8.268836392978581529 ) ) ;
#44933=CARTESIAN_POINT ( 'NONE',  ( 126.2184548109105435, -7.866424907533402511, -9.395035934245175469 ) ) ;
#44934=CARTESIAN_POINT ( 'NONE',  ( 119.7736414775786358, 0.1319031606808879209, -14.10382304977623669 ) ) ;
#44938=CARTESIAN_POINT ( 'NONE',  ( 122.1561614775786353, -0.4660016031367893996, -10.09054647747474043 ) ) ;
#44940=CARTESIAN_POINT ( 'NONE',  ( 124.5147686830089810, -1.087735405160626723, -17.17288456429612964 ) ) ;
#44943=CARTESIAN_POINT ( 'NONE',  ( 112.0020881442453344, 0.2603800115204892296, -16.42320221600525088 ) ) ;
#44944=CARTESIAN_POINT ( 'NONE',  ( 123.8579614775786126, 0.5811942927096110934, -14.16772938898807510 ) ) ;
#44945=CARTESIAN_POINT ( 'NONE',  ( 117.3911214775786505, -7.894159318335828068, -9.358103419637847864 ) ) ;
#44947=CARTESIAN_POINT ( 'NONE',  ( 117.8449348109119938, -8.166667518702817929, -8.995218007635861213 ) ) ;
#44949=CARTESIAN_POINT ( 'NONE',  ( 123.4041481442452834, 0.1319031606808879209, -14.10382304977623669 ) ) ;
#44954=CARTESIAN_POINT ( 'NONE',  ( 118.0718414775786300, -9.261995988541697145, -16.69588392320189030 ) ) ;
#44955=CARTESIAN_POINT ( 'NONE',  ( 135.8419766445518633, -8.523023866441993945, -18.08927214266044103 ) ) ;
#44959=CARTESIAN_POINT ( 'NONE',  ( 122.4965214775786251, -10.30919188438810075, -12.61870101168855918 ) ) ;
#44961=CARTESIAN_POINT ( 'NONE',  ( 120.1140014775786398, -7.894159318335828068, -9.358103419637847864 ) ) ;
#44963=ORIENTED_EDGE ( 'NONE', *, *, #9703, .F. ) ;
#44965=CARTESIAN_POINT ( 'NONE',  ( 115.8595014775786609, -1.834011780172310813, -8.268836392978581529 ) ) ;
#44969=CARTESIAN_POINT ( 'NONE',  ( 123.0070614775786169, 0.9020085738987339008, -11.91225656197089222 ) ) ;
#44972=CARTESIAN_POINT ( 'NONE',  ( 119.6034614775786196, -6.344957434206665248, -7.627207830600338134 ) ) ;
#44973=CARTESIAN_POINT ( 'NONE',  ( 119.2631014775786298, 0.2603800115204892296, -16.42320221600525088 ) ) ;
#44974=CARTESIAN_POINT ( 'NONE',  ( 118.5823814775786360, -7.643976991954077427, -18.09477374809248928 ) ) ;
#44976=CARTESIAN_POINT ( 'NONE',  ( 117.7314814775786260, -4.089484607189486809, -7.948022111789456723 ) ) ;
#44978=CARTESIAN_POINT ( 'NONE',  ( 126.2972081442452890, -2.084020599724406786, -8.691656652584148546 ) ) ;
#44979=CARTESIAN_POINT ( 'NONE',  ( 125.3328548109119964, -0.8288870151393684660, -10.36305467784094247 ) ) ;
#44983=CARTESIAN_POINT ( 'NONE',  ( 121.7023481442452777, -9.261995988541697145, -16.69588392320189030 ) ) ;
#44984=CARTESIAN_POINT ( 'NONE',  ( 125.9001214775786224, -5.574606645277164318, -18.38911715685844683 ) ) ;
#44986=CARTESIAN_POINT ( 'NONE',  ( 126.0135748109119902, -8.166667518702819706, -8.995218007635861213 ) ) ;
#44989=CARTESIAN_POINT ( 'NONE',  ( 124.0848681442452772, -4.089484607189486809, -7.948022111789456723 ) ) ;
#44990=CARTESIAN_POINT ( 'NONE',  ( 123.7445081442452874, -1.561330072975668948, -17.79121239304076951 ) ) ;
#44992=CARTESIAN_POINT ( 'NONE',  ( 126.5241148109119393, -9.565557343593413364, -10.61323700422348004 ) ) ;
#44993=CARTESIAN_POINT ( 'NONE',  ( 111.5125327111057345, -1.267766418764825875, -16.93314635290698789 ) ) ;
#44997=CARTESIAN_POINT ( 'NONE',  ( 114.3846081442453197, 0.4262465694468514643, -12.03445270309931736 ) ) ;
#44998=CARTESIAN_POINT ( 'NONE',  ( 112.4559014775786494, -9.988377603198976828, -10.36322818467138340 ) ) ;
#45001=CARTESIAN_POINT ( 'NONE',  ( 121.8158014775786171, -4.153390946401325223, -8.397313243818185668 ) ) ;
#45002=CARTESIAN_POINT ( 'NONE',  ( 116.0296814775786345, -1.833838273342658809, -17.42832698103878286 ) ) ;
#45003=CARTESIAN_POINT ( 'NONE',  ( 111.4915481442453142, -1.833838273342658365, -17.42832698103878286 ) ) ;
#45006=CARTESIAN_POINT ( 'NONE',  ( 118.2420214775786320, -3.383040157471821630, -19.15922257007629170 ) ) ;
#45007=EDGE_CURVE ( 'NONE', #2614, #30977, #33822, .T. ) ;
#45009=CARTESIAN_POINT ( 'NONE',  ( 114.1577014775786552, -3.505236298600246325, -18.68346056562440793 ) ) ;
#45010=VERTEX_POINT ( 'NONE', #15943 ) ;
#45013=CARTESIAN_POINT ( 'NONE',  ( 113.4769814775786330, 0.4262465694468514643, -12.03445270309931736 ) ) ;
#45015=CARTESIAN_POINT ( 'NONE',  ( 115.4624148109119943, -4.153390946401321671, -8.397313243818183892 ) ) ;
#45016=CARTESIAN_POINT ( 'NONE',  ( 117.7515727483929311, -2.423081321603731908, -17.89265170041263175 ) ) ;
#45022=CARTESIAN_POINT ( 'NONE',  ( 118.2795432127138611, -2.191907684172563986, -18.20049396185734025 ) ) ;
#45023=CARTESIAN_POINT ( 'NONE',  ( 124.0281414775786146, -7.643976991954077427, -18.09477374809248928 ) ) ;
#45024=CARTESIAN_POINT ( 'NONE',  ( 114.8384214775786489, -10.15424416112533912, -14.75197769757731336 ) ) ;
#45025=CARTESIAN_POINT ( 'NONE',  ( 120.1332064091100733, -0.9924539043446216624, -17.29976612834909133 ) ) ;
#45027=DIRECTION ( 'NONE',  ( 1.000000000000000000, 0.000000000000000000, 0.000000000000000000 ) ) ;
#45028=CARTESIAN_POINT ( 'NONE',  ( 117.4478481442453131, -9.565557343593413364, -10.61323700422348004 ) ) ;
#45031=CARTESIAN_POINT ( 'NONE',  ( 125.4463081442452932, -4.153390946401325223, -8.397313243818185668 ) ) ;
#45034=CARTESIAN_POINT ( 'NONE',  ( 114.4980614775786592, -7.893985811506177619, -18.51759400769804742 ) ) ;
#45037=CARTESIAN_POINT ( 'NONE',  ( 126.6375681442452930, -10.15424416112533912, -14.75197769757731336 ) ) ;
#45038=CARTESIAN_POINT ( 'NONE',  ( 115.4624148109119943, -5.638512984488999180, -18.83840828888717311 ) ) ;
#45039=CARTESIAN_POINT ( 'NONE',  ( 122.0994348109119443, -10.15424416112533912, -14.75197769757731336 ) ) ;
#45044=CARTESIAN_POINT ( 'NONE',  ( 116.6536748109119941, -10.15424416112533912, -14.75197769757731336 ) ) ;
#45047=CARTESIAN_POINT ( 'NONE',  ( 111.7184548109119788, -9.244942279156937559, -16.71734234406761388 ) ) ;
#45049=CARTESIAN_POINT ( 'NONE',  ( 123.6877814775786533, -3.383040157471821630, -19.15922257007629170 ) ) ;
#45050=CARTESIAN_POINT ( 'NONE',  ( 112.3991748109119868, -1.833838273342658809, -17.42832698103878286 ) ) ;
#45052=CARTESIAN_POINT ( 'NONE',  ( 121.5321681442453183, -9.988377603198976828, -10.36322818467138340 ) ) ;
#45053=CARTESIAN_POINT ( 'NONE',  ( 116.1998614775786507, -10.63000616557722466, -14.87417383870573495 ) ) ;
#45055=CARTESIAN_POINT ( 'NONE',  ( 114.3846081442453197, 0.4262465694468514643, -12.03445270309931736 ) ) ;
#45056=CARTESIAN_POINT ( 'NONE',  ( 124.5954081442453116, -3.383040157471821630, -19.15922257007629170 ) ) ;
#45057=CARTESIAN_POINT ( 'NONE',  ( 114.7249681442453237, 0.2603800115204892296, -16.42320221600525088 ) ) ;
#45058=CARTESIAN_POINT ( 'NONE',  ( 115.5191414775786569, -6.222761293078241884, -8.102969835052219238 ) ) ;
#45059=VERTEX_POINT ( 'NONE', #2240 ) ;
#45060=CARTESIAN_POINT ( 'NONE',  ( 120.1140014775786398, -7.894159318335828068, -9.358103419637847864 ) ) ;
#45061=CARTESIAN_POINT ( 'NONE',  ( 116.4834948109119779, -1.561330072975668504, -17.79121239304076951 ) ) ;
#45065=CARTESIAN_POINT ( 'NONE',  ( 111.7184548109119788, -9.261995988541697145, -16.69588392320189030 ) ) ;
#45066=CARTESIAN_POINT ( 'NONE',  ( 111.7184548109119788, -9.244942279156937559, -16.71734234406761388 ) ) ;
#45068=CARTESIAN_POINT ( 'NONE',  ( 113.4769814775786330, -10.63000616557722466, -14.87417383870573495 ) ) ;
#45070=CARTESIAN_POINT ( 'NONE',  ( 113.6471614775786492, -4.153390946401321671, -8.397313243818183892 ) ) ;
#45074=CARTESIAN_POINT ( 'NONE',  ( 117.2209414775786485, -7.893985811506177619, -18.51759400769804742 ) ) ;
#45075=CARTESIAN_POINT ( 'NONE',  ( 136.8676504264525988, -4.417203549486936609, -18.92742781940280850 ) ) ;
#45077=CARTESIAN_POINT ( 'NONE',  ( 118.8660148109119774, -10.30919188438809719, -12.61870101168856273 ) ) ;
#45079=CARTESIAN_POINT ( 'NONE',  ( 121.8725281442453223, -6.222761293078241884, -8.102969835052219238 ) ) ;
#45081=CARTESIAN_POINT ( 'NONE',  ( 135.8419766445417736, -9.560055738161365113, -9.734190129735562635 ) ) ;
#45082=CARTESIAN_POINT ( 'NONE',  ( 119.7169148109119874, -9.988377603198976828, -10.36322818467138340 ) ) ;
#45084=CARTESIAN_POINT ( 'NONE',  ( 116.7104014775786425, -8.899110576539710493, -16.42337572283490132 ) ) ;
#45088=CARTESIAN_POINT ( 'NONE',  ( 113.6471614775786492, -4.153390946401321671, -8.397313243818183892 ) ) ;
#45092=CARTESIAN_POINT ( 'NONE',  ( 120.5110881442453206, -3.505236298600246325, -18.68346056562440793 ) ) ;
#45093=CARTESIAN_POINT ( 'NONE',  ( 121.6456214775786293, 0.4262465694468514643, -12.03445270309931736 ) ) ;
#45098=CARTESIAN_POINT ( 'NONE',  ( 112.9664414775786412, 0.5811942927096154232, -14.16772938898807155 ) ) ;
#45099=CARTESIAN_POINT ( 'NONE',  ( 114.2711548109119803, -9.988377603198976828, -10.36322818467138340 ) ) ;
#45102=FACE_OUTER_BOUND ( 'NONE', #404, .T. ) ;
#45104=CARTESIAN_POINT ( 'NONE',  ( 120.9081748109119872, -5.638512984488999180, -18.83840828888717311 ) ) ;
#45105=CARTESIAN_POINT ( 'NONE',  ( 126.2972081442452890, -2.084020599724406786, -8.691656652584148546 ) ) ;
#45106=CARTESIAN_POINT ( 'NONE',  ( 118.5256548109119876, -8.899110576539710493, -16.42337572283490132 ) ) ;
#45110=CARTESIAN_POINT ( 'NONE',  ( 122.2696148109119889, -4.089484607189486809, -7.948022111789456723 ) ) ;
#45111=CARTESIAN_POINT ( 'NONE',  ( 118.2420214775786320, -3.383040157471821630, -19.15922257007629170 ) ) ;
#45114=CARTESIAN_POINT ( 'NONE',  ( 114.2711548109119803, -0.1624402480850797581, -16.17319339645315424 ) ) ;
#45117=CARTESIAN_POINT ( 'NONE',  ( 118.8092881442453290, -9.988377603198976828, -10.36322818467138340 ) ) ;
#45118=EDGE_CURVE ( 'NONE', #8883, #40452, #36285, .T. ) ;
#45121=CARTESIAN_POINT ( 'NONE',  ( 114.6682414775786469, -1.561330072975668060, -17.79121239304076596 ) ) ;
#45124=CARTESIAN_POINT ( 'NONE',  ( 123.5743281442453139, -7.893985811506177619, -18.51759400769804742 ) ) ;
#45126=CARTESIAN_POINT ( 'NONE',  ( 135.3184548109119874, -4.863998795839242995, -13.39321520033831447 ) ) ;
#45128=CARTESIAN_POINT ( 'NONE',  ( 117.6180281442453150, -8.899110576539710493, -16.42337572283490132 ) ) ;
#45131=CARTESIAN_POINT ( 'NONE',  ( 118.1285681442453068, -2.084020599724406786, -8.691656652584148546 ) ) ;
#45134=CARTESIAN_POINT ( 'NONE',  ( 118.0718414775786442, -0.8288870151387760510, -10.36305467784173118 ) ) ;
#45137=CARTESIAN_POINT ( 'NONE',  ( 114.6682414775786469, -1.561330072975668060, -17.79121239304076596 ) ) ;
#45140=CARTESIAN_POINT ( 'NONE',  ( 116.4834948109119779, -7.894159318335828068, -9.358103419637847864 ) ) ;
#45142=CARTESIAN_POINT ( 'NONE',  ( 118.5256548109119876, -0.4660016031367893996, -10.09054647747474043 ) ) ;
#45144=CARTESIAN_POINT ( 'NONE',  ( 115.1430393777725385, -1.267766418764730840, -16.93314635290706605 ) ) ;
#45148=CARTESIAN_POINT ( 'NONE',  ( 123.5743281442453139, -7.893985811506177619, -18.51759400769804742 ) ) ;
#45184=COLOUR_RGB('Black',0.12,0.14,0.17);
#45185=FILL_AREA_STYLE_COLOUR('',#45184);
#45186=FILL_AREA_STYLE('',(#45185));
#45187=SURFACE_STYLE_FILL_AREA(#45186);
#45188=SURFACE_SIDE_STYLE('',(#45187));
#45189=SURFACE_STYLE_USAGE(.BOTH.,#45188);
#45190=PRESENTATION_STYLE_ASSIGNMENT((#45189));
ENDSEC;
END-ISO-10303-21;
